#104872=CARTESIAN_POINT ( 'NONE',  ( -0.02919842301641034990, 1.352617229779122132, -2.329362550481127947 ) ) ;
#104875=CARTESIAN_POINT ( 'NONE',  ( 6.925078400183521055, 0.5534609092465185842, 2.295239920751692253 ) ) ;
#104876=CARTESIAN_POINT ( 'NONE',  ( 6.369096972855497363, 1.760372669148374758, -0.5393517311068628528 ) ) ;
#104878=CARTESIAN_POINT ( 'NONE',  ( 2.571226905367568261, 0.1023410288747768487, -2.058482174549924437 ) ) ;
#104884=CARTESIAN_POINT ( 'NONE',  ( 1.077108160694364214, -0.04970969036830223675, -2.060456431261459276 ) ) ;
#104893=CARTESIAN_POINT ( 'NONE',  ( 5.373716497573798101, 2.127666891504222058, -0.5857064233696291922 ) ) ;
#104894=CARTESIAN_POINT ( 'NONE',  ( 0.7730135719010817752, -2.035059957909639561, -0.7290066412228360937 ) ) ;
#104896=CARTESIAN_POINT ( 'NONE',  ( 6.416260824072121061, -1.810972107014690913, 0.05430519662179972284 ) ) ;
#104897=CARTESIAN_POINT ( 'NONE',  ( 0.7609543035823238544, -0.05432987398422234326, -2.015980609757315190 ) ) ;
#104899=CARTESIAN_POINT ( 'NONE',  ( 1.353307579497017965, -1.032721833433938530, 2.053394521917959015 ) ) ;
#104901=CARTESIAN_POINT ( 'NONE',  ( 6.586579894266019863, -1.172543786506787145, 1.511232097859278145 ) ) ;
#104902=CARTESIAN_POINT ( 'NONE',  ( 1.973319494866377699, 1.790917844098998124, -0.5403536831049270406 ) ) ;
#104903=CARTESIAN_POINT ( 'NONE',  ( 2.325407997918966796, -1.497503195670712328, -1.350734289967000512 ) ) ;
#104908=CARTESIAN_POINT ( 'NONE',  ( 4.899102953068730670, 1.751457851224359041, -1.169261236274852012 ) ) ;
#104913=CARTESIAN_POINT ( 'NONE',  ( 4.676038720085195166, 1.997217120926295442, -0.3003719491122060492 ) ) ;
#104915=CARTESIAN_POINT ( 'NONE',  ( 6.250444628687981563, -2.052375444028589957, -0.2060817263721328174 ) ) ;
#104917=CARTESIAN_POINT ( 'NONE',  ( 5.413408226029434722, -0.3230527293765028674, 2.137217106551466905 ) ) ;
#104923=CARTESIAN_POINT ( 'NONE',  ( 1.944024895830529731, 1.496304202470769340, 1.573470141065239414 ) ) ;
#104926=CARTESIAN_POINT ( 'NONE',  ( 1.557894219809667247, -1.301531972126177772, 1.302644501960325885 ) ) ;
#104928=CARTESIAN_POINT ( 'NONE',  ( 3.351304529449970371, 0.5305821810032870234, -2.126252377916526992 ) ) ;
#104929=CARTESIAN_POINT ( 'NONE',  ( 6.983263157960386991, 3.689421308571324776, 2.567857239638075217 ) ) ;
#104930=CARTESIAN_POINT ( 'NONE',  ( 4.258826902089789535, -1.679047235397194804, 1.516690725115140692 ) ) ;
#104937=CARTESIAN_POINT ( 'NONE',  ( 5.712081065023381754, -0.7967057657092267986, -1.580296573674238259 ) ) ;
#104940=CARTESIAN_POINT ( 'NONE',  ( 1.817543918834242378, -0.2582919827684154179, 2.089997942319920199 ) ) ;
#104943=CARTESIAN_POINT ( 'NONE',  ( 1.275766937089892750, -1.922257851437941811, 0.4282784019480969651 ) ) ;
#104945=CARTESIAN_POINT ( 'NONE',  ( 0.1331565106231328843, 0.003911343561965873426, -1.946049565259087455 ) ) ;
#104946=CARTESIAN_POINT ( 'NONE',  ( 5.537325978022108686, -0.03587880057049273180, 1.811405195203552587 ) ) ;
#104950=CARTESIAN_POINT ( 'NONE',  ( 4.715616592392388284, -1.834479983729628616, 0.3652084810651031743 ) ) ;
#104952=ORIENTED_EDGE ( 'NONE', *, *, #56424, .F. ) ;
#104953=CARTESIAN_POINT ( 'NONE',  ( 6.051642586050197892, 1.563818258945087969, 1.356687170345115989 ) ) ;
#104956=CARTESIAN_POINT ( 'NONE',  ( 0.2739938332866619364, -2.030697503880642518, 0.4024348779970430834 ) ) ;
#104963=CARTESIAN_POINT ( 'NONE',  ( 5.494571831323358246, 1.932540981948445147, 0.3370517209014682325 ) ) ;
#104965=CARTESIAN_POINT ( 'NONE',  ( 2.460314346279086628, 1.556669099887195484, 1.281166478716524892 ) ) ;
#104968=CARTESIAN_POINT ( 'NONE',  ( 0.6619992422990974568, 1.085049530943157148, 1.904046507712559455 ) ) ;
#104970=CARTESIAN_POINT ( 'NONE',  ( 1.985418980784030119, 1.286400883397397221, 1.358229366437320618 ) ) ;
#104972=CARTESIAN_POINT ( 'NONE',  ( 3.902593620319398937, -1.991888969257959774, -0.2912845021679384971 ) ) ;
#104975=CARTESIAN_POINT ( 'NONE',  ( 4.763340612834221943, 1.975027209670917161, -0.7632558447715469541 ) ) ;
#104978=CARTESIAN_POINT ( 'NONE',  ( 5.758279222819879806, -2.070544812512797428, -0.003756845764937844813 ) ) ;
#104979=CARTESIAN_POINT ( 'NONE',  ( 0.7848512634026264534, 1.842159585024247148, -0.9888006619010838438 ) ) ;
#104980=CARTESIAN_POINT ( 'NONE',  ( 6.720655732516636505, 1.219515403015670296, 2.385684514189966521 ) ) ;
#104981=CARTESIAN_POINT ( 'NONE',  ( 6.721730220878607831, -1.769880579078547012, 0.4471725050417332814 ) ) ;
#104988=CARTESIAN_POINT ( 'NONE',  ( -0.1051951494144076904, -0.1375245761873785666, -1.781266614511106683 ) ) ;
#104996=CARTESIAN_POINT ( 'NONE',  ( 6.204703874486805049, 1.882480396761162744, 0.7231267579426368108 ) ) ;
#104997=CARTESIAN_POINT ( 'NONE',  ( 0.08289510313583270396, -1.381697626658566547, 1.608636130391014163 ) ) ;
#104999=CARTESIAN_POINT ( 'NONE',  ( -0.1399997263889594112, -0.002789056014654289761, -2.000146600338557956 ) ) ;
#105003=CARTESIAN_POINT ( 'NONE',  ( 3.924621296410530480, -1.326038130087652922, 1.456277141313151224 ) ) ;
#105004=CARTESIAN_POINT ( 'NONE',  ( 4.148064665909578785, 0.9530284220014314522, 1.777003606838889915 ) ) ;
#105006=CARTESIAN_POINT ( 'NONE',  ( 4.875033280109006384, 2.045454206080063120, -0.7869404205859964474 ) ) ;
#105008=CARTESIAN_POINT ( 'NONE',  ( 3.188414472400236566, -1.897621675979482614, -0.3308535721826404985 ) ) ;
#105010=CARTESIAN_POINT ( 'NONE',  ( -0.02988540731099428513, 0.2551080090007939449, -1.761437810625957834 ) ) ;
#105011=CARTESIAN_POINT ( 'NONE',  ( 0.01274299142895937362, -0.9473294304004549193, -1.991142614049784099 ) ) ;
#105017=ORIENTED_EDGE ( 'NONE', *, *, #130874, .F. ) ;
#105018=CARTESIAN_POINT ( 'NONE',  ( 5.190276988288149873, 1.015767153246112775, -1.687157232322311629 ) ) ;
#105020=CARTESIAN_POINT ( 'NONE',  ( 0.5033352851749985923, -1.932590057610440226, 0.1917435184634954937 ) ) ;
#105021=CARTESIAN_POINT ( 'NONE',  ( 4.002593568968414672, -1.991494762441379462, -0.2932518702276361022 ) ) ;
#105022=CARTESIAN_POINT ( 'NONE',  ( 5.483857608503296177, 2.120574376644312586, 0.8868611222285858187 ) ) ;
#105024=CARTESIAN_POINT ( 'NONE',  ( 3.660865129197692358, 1.469539745679597553, -1.141665872729610287 ) ) ;
#105030=CARTESIAN_POINT ( 'NONE',  ( 5.776921370525399446, 1.931409454660049319, -0.8010388902379047549 ) ) ;
#105035=CARTESIAN_POINT ( 'NONE',  ( 0.9260630535584664091, 1.089557764695957554, -1.464779044915397455 ) ) ;
#105038=CARTESIAN_POINT ( 'NONE',  ( 2.812812116114179251, 0.9611239539163253243, -1.443176275507858319 ) ) ;
#105043=CARTESIAN_POINT ( 'NONE',  ( 6.561400879130542485, 1.800260439488234443, 1.213256210689506176 ) ) ;
#105045=CARTESIAN_POINT ( 'NONE',  ( 5.109893933574640279, -1.816543354971979163, 0.1824992186492402357 ) ) ;
#105046=CARTESIAN_POINT ( 'NONE',  ( 3.625789200213443753, 1.914935786268581852, -0.4253726038727227432 ) ) ;
#105051=CARTESIAN_POINT ( 'NONE',  ( 3.862070080935349203, 0.7130468835700142227, -1.997148454185311506 ) ) ;
#105055=CARTESIAN_POINT ( 'NONE',  ( 2.079047829753433163, 1.930162853665925216, 0.7490395704240898622 ) ) ;
#105058=CARTESIAN_POINT ( 'NONE',  ( 4.600346979525781421, -1.047586700562872286, 1.958737397810013325 ) ) ;
#105060=CARTESIAN_POINT ( 'NONE',  ( 2.303761666418477461, 1.498124540730429333, -1.743551778261544838 ) ) ;
#105062=CARTESIAN_POINT ( 'NONE',  ( 6.403195902773025416, -1.745507933166186465, 1.098531482539546023 ) ) ;
#105068=CARTESIAN_POINT ( 'NONE',  ( 3.375170810042011915, -1.688748480992762868, -0.8973671847329609541 ) ) ;
#105070=CARTESIAN_POINT ( 'NONE',  ( 4.084733067335220902, -0.1695706708978762522, -1.716391344981627709 ) ) ;
#105071=CARTESIAN_POINT ( 'NONE',  ( 1.991423064788412800, -0.4370762659771566527, 1.968445590580846893 ) ) ;
#105072=CARTESIAN_POINT ( 'NONE',  ( 4.254688019566841284, 2.229798712500128843, -0.5580973643144919727 ) ) ;
#105073=CARTESIAN_POINT ( 'NONE',  ( 3.831548730252303248, -2.092150397999822165, 0.8615055239265239084 ) ) ;
#105074=CARTESIAN_POINT ( 'NONE',  ( 6.322895070704796616, 1.964426112044151518, 0.7597984924697271936 ) ) ;
#105077=CARTESIAN_POINT ( 'NONE',  ( 4.200303217096891473, -0.5537481437246688509, -1.680960689856024537 ) ) ;
#105079=CARTESIAN_POINT ( 'NONE',  ( 1.289493641233057319, 1.738593318175378766, 1.494007209952723958 ) ) ;
#105080=CARTESIAN_POINT ( 'NONE',  ( 5.824118960990139371, 1.775556191179916699, 0.4867722729226392486 ) ) ;
#105082=CARTESIAN_POINT ( 'NONE',  ( 5.314472526525434226, 2.023830839259177949, 0.8410439265160508659 ) ) ;
#105086=CARTESIAN_POINT ( 'NONE',  ( 6.057099581687969803, 1.694805161836069107, -1.188877858866774107 ) ) ;
#105087=CARTESIAN_POINT ( 'NONE',  ( 1.094935803221647186, 1.780670018850015079, 0.9462964651613046119 ) ) ;
#105089=CARTESIAN_POINT ( 'NONE',  ( 4.178288987252887665, -1.108116244417625573, 1.575729328202896573 ) ) ;
#105091=CARTESIAN_POINT ( 'NONE',  ( 0.7564555125054818197, 0.8934716743186126298, -2.033981271184843731 ) ) ;
#105098=CARTESIAN_POINT ( 'NONE',  ( 2.453501617077270325, 1.514643136537169310, 1.246875331876770021 ) ) ;
#105104=CARTESIAN_POINT ( 'NONE',  ( 0.3267250850040852583, -1.348467290049197853, 1.560915443186759122 ) ) ;
#105107=CARTESIAN_POINT ( 'NONE',  ( 0.3041012005207919255, -0.5996659824250392123, 2.181524510355018265 ) ) ;
#105111=CARTESIAN_POINT ( 'NONE',  ( 1.563515255687727645, 1.843751956470768283, -0.3144994141817195055 ) ) ;
#105112=CARTESIAN_POINT ( 'NONE',  ( 6.819718782980952909, -1.336886906709513712, 1.104006757392479887 ) ) ;
#105115=CARTESIAN_POINT ( 'NONE',  ( 3.650093349144762023, 0.7902683543556283663, 2.044282924279612779 ) ) ;
#105116=CARTESIAN_POINT ( 'NONE',  ( 5.508889292638126989, 1.751971812537992834, -1.501964572959401778 ) ) ;
#105117=CARTESIAN_POINT ( 'NONE',  ( 6.837187436585446143, -1.842956594435873896, 0.9222261209423606720 ) ) ;
#105118=CARTESIAN_POINT ( 'NONE',  ( 2.712754350931959380, -0.1900897480172674958, 1.932619341894822540 ) ) ;
#105121=CARTESIAN_POINT ( 'NONE',  ( -0.1104750535120248289, 7.629137130509052511, -2.703481013110929254 ) ) ;
#105124=CARTESIAN_POINT ( 'NONE',  ( 3.815077410725797424, 1.076317812134291119, -1.704938119663282903 ) ) ;
#105128=CARTESIAN_POINT ( 'NONE',  ( 0.6799654140086827114, -1.016662149479659494, 1.516215539243186639 ) ) ;
#105134=CARTESIAN_POINT ( 'NONE',  ( 6.227427239534573999, -1.941376443541954488, 0.6920112976290059281 ) ) ;
#105139=CARTESIAN_POINT ( 'NONE',  ( 5.233071810066631357, 1.866936204443689462, 0.7709723521613828234 ) ) ;
#105140=CARTESIAN_POINT ( 'NONE',  ( 6.270221287042929248, 2.215581787426896376, -0.1604564985231044516 ) ) ;
#105144=CARTESIAN_POINT ( 'NONE',  ( 5.137599278355773791, -1.455842209265911569, -1.458961989641535117 ) ) ;
#105145=CARTESIAN_POINT ( 'NONE',  ( 3.832657856672665009, 0.6767144645295587457, -1.899618369658891748 ) ) ;
#105152=CARTESIAN_POINT ( 'NONE',  ( 4.534529724472468715, 1.956261425488527106, -0.4871295050740409582 ) ) ;
#105153=CARTESIAN_POINT ( 'NONE',  ( 3.503688343963583307, -0.7473321665184139428, -1.682825604429179833 ) ) ;
#105156=CARTESIAN_POINT ( 'NONE',  ( 2.034188542434863578, -1.509292173632442280, -1.745791301847523513 ) ) ;
#105158=CARTESIAN_POINT ( 'NONE',  ( 4.183022562662654487, -0.2072598778708051315, -2.151613130492259440 ) ) ;
#105161=CARTESIAN_POINT ( 'NONE',  ( 3.462589497157672724, 1.809959297682335100, 1.416443637550690804 ) ) ;
#105163=CARTESIAN_POINT ( 'NONE',  ( 2.500682550815761740, 1.503739811390795378, -1.112508705057350999 ) ) ;
#105164=CARTESIAN_POINT ( 'NONE',  ( 0.2277241186354854174, -1.209499947282626220, -1.557479245376863330 ) ) ;
#105169=CARTESIAN_POINT ( 'NONE',  ( 1.629795212970772456, -2.077151576879713080, 0.7458654493318407352 ) ) ;
#105175=CARTESIAN_POINT ( 'NONE',  ( 6.086792475191005636, -0.2889037430471863566, -1.950060635722290936 ) ) ;
#105177=CARTESIAN_POINT ( 'NONE',  ( 6.129535273836777876, -2.175136813519952916, 0.7712226964542520102 ) ) ;
#105178=CARTESIAN_POINT ( 'NONE',  ( 0.6429252097494702056, -0.2364460082661112295, -1.947484529462916836 ) ) ;
#105179=CARTESIAN_POINT ( 'NONE',  ( 2.834894798709301611, -1.972450601023918448, -0.6029180858937719378 ) ) ;
#105186=CARTESIAN_POINT ( 'NONE',  ( 6.303213947599001443, -1.837614076384209261, 1.156103312670229810 ) ) ;
#105188=CARTESIAN_POINT ( 'NONE',  ( 4.704558828624370470, 1.604442792107749760, 0.9031527321438773681 ) ) ;
#105190=CARTESIAN_POINT ( 'NONE',  ( 6.269083535738129598, 2.097726667780253074, -0.6343229546324488100 ) ) ;
#105195=CARTESIAN_POINT ( 'NONE',  ( 0.3285747216504387724, 1.318609938922534752, -1.385187620709791512 ) ) ;
#105196=CARTESIAN_POINT ( 'NONE',  ( 1.779799802231885275, -0.9501279348179264561, 1.492983415055911367 ) ) ;
#105197=CARTESIAN_POINT ( 'NONE',  ( 0.1176276963383571517, -0.5100272734060510293, 1.842954807014775653 ) ) ;
#105199=CARTESIAN_POINT ( 'NONE',  ( 3.392102565403580350, -0.7792391910043224845, -1.750150251150209391 ) ) ;
#105201=CARTESIAN_POINT ( 'NONE',  ( 4.615651692036619735, 0.4336440386765746946, -1.921039654613013292 ) ) ;
#105202=CARTESIAN_POINT ( 'NONE',  ( 6.539320575229290000, 0.004092658091040673150, 2.003502637948690879 ) ) ;
#105204=CARTESIAN_POINT ( 'NONE',  ( 3.238977024203249400, -1.650389259550872456, 0.8806316622528218563 ) ) ;
#105205=CARTESIAN_POINT ( 'NONE',  ( 6.357991264096761519, 1.719682601729131566, -0.1347253291539267650 ) ) ;
#105207=CARTESIAN_POINT ( 'NONE',  ( 1.787996309160574837, 1.523479866092191548, 1.596893430481533649 ) ) ;
#105210=CARTESIAN_POINT ( 'NONE',  ( 0.2036765287981847083, -1.593398458586914757, -1.309455759714562850 ) ) ;
#105217=CARTESIAN_POINT ( 'NONE',  ( 2.734898984476673789, -1.980466496001157317, -0.6033880717724803278 ) ) ;
#105221=CARTESIAN_POINT ( 'NONE',  ( 0.8561247329088355063, 0.8163843618401511737, -1.847503835822896789 ) ) ;
#105225=CARTESIAN_POINT ( 'NONE',  ( 0.1747926744264677590, 6.948552888299643904, -2.450368216405907962 ) ) ;
#105227=CARTESIAN_POINT ( 'NONE',  ( 5.554064478179312481, 1.779353385700060075, -0.9478964821433707444 ) ) ;
#105228=CARTESIAN_POINT ( 'NONE',  ( 5.436718845459293625, -1.505851745483515858, 1.184076087961029700 ) ) ;
#105230=CARTESIAN_POINT ( 'NONE',  ( 3.984055765753656164, -2.167877601896048390, -0.3204034371554059235 ) ) ;
#105232=CARTESIAN_POINT ( 'NONE',  ( 2.179812656587180264, 1.874749209517186710, -0.3766967574026017229 ) ) ;
#105236=CARTESIAN_POINT ( 'NONE',  ( 0.5972800738224989248, -0.2930464221381040013, 1.994874516246990748 ) ) ;
#105239=CARTESIAN_POINT ( 'NONE',  ( 5.917560222199001352, -1.216239291071326001, -1.822900893127032962 ) ) ;
#105241=CARTESIAN_POINT ( 'NONE',  ( 2.783889825318270450, -0.8885198777363271239, 1.478144978849999847 ) ) ;
#105247=CARTESIAN_POINT ( 'NONE',  ( 0.1390251588108057101, -0.1389306544097475005, -1.930426113910483688 ) ) ;
#105254=CARTESIAN_POINT ( 'NONE',  ( 4.107922266221023300, -0.6895048676278795474, 1.675321109400946806 ) ) ;
#105258=CARTESIAN_POINT ( 'NONE',  ( 3.791515551631476910, 1.704436734775734985, -0.6137984976519753610 ) ) ;
#105262=CARTESIAN_POINT ( 'NONE',  ( 4.826513810146395578, -1.216237885654298800, 1.408704720340781869 ) ) ;
#105265=CARTESIAN_POINT ( 'NONE',  ( 3.110843951327123325, 0.04995152196871639055, 1.915135415325731394 ) ) ;
#105267=FACE_OUTER_BOUND ( 'NONE', #13561, .T. ) ;
#105275=CARTESIAN_POINT ( 'NONE',  ( 1.623107816722869412, -1.968041427791475728, 0.7057566781872460782 ) ) ;
#105277=CARTESIAN_POINT ( 'NONE',  ( 6.510771785681003010, 1.426997308145862453, -1.294280627073117529 ) ) ;
#105279=CARTESIAN_POINT ( 'NONE',  ( 2.010518257881420023, 1.354885872097401078, -1.223726681998098087 ) ) ;
#105281=CARTESIAN_POINT ( 'NONE',  ( 0.8438408207818194340, -1.215224102361469161, -1.476598726422105656 ) ) ;
#105283=CARTESIAN_POINT ( 'NONE',  ( 1.662492070209736994, -0.7059575147525645189, -1.838877744480153620 ) ) ;
#105284=CARTESIAN_POINT ( 'NONE',  ( 3.895986966309549882, -0.6120611862858457153, -1.843141947886927978 ) ) ;
#105288=CARTESIAN_POINT ( 'NONE',  ( 6.034019871906543209, 1.107478494666002344, 1.495390754572333725 ) ) ;
#105290=CARTESIAN_POINT ( 'NONE',  ( 3.691739789689612472, 1.995538565534977549, -0.7177698711837015022 ) ) ;
#105298=CARTESIAN_POINT ( 'NONE',  ( 3.492628380820805400, -0.3572889717703279788, -1.790209119249221548 ) ) ;
#105303=CARTESIAN_POINT ( 'NONE',  ( 4.170664822833985319, -1.745344833062393075, -0.6735866001992969476 ) ) ;
#105305=CARTESIAN_POINT ( 'NONE',  ( 1.646969920108354524, -1.627708819445686572, 1.030247865989121880 ) ) ;
#105306=CARTESIAN_POINT ( 'NONE',  ( 6.772321408939014020, -0.9219223515295159599, -1.731591420108986812 ) ) ;
#105312=CARTESIAN_POINT ( 'NONE',  ( -0.0001774970986804374768, -2.075397304607224047, 0.4179963677126071753 ) ) ;
#105316=CARTESIAN_POINT ( 'NONE',  ( 4.733297664174529906, 0.005294743050891088411, -2.070434559870132585 ) ) ;
#105317=CARTESIAN_POINT ( 'NONE',  ( 0.4328342922346357646, -1.301571265828086688, -1.302605208699902928 ) ) ;
#105320=CARTESIAN_POINT ( 'NONE',  ( 5.010469735608720221, -2.183386834666663390, 0.7190086036765501731 ) ) ;
#105324=CARTESIAN_POINT ( 'NONE',  ( 0.8675860333910101474, 2.207824459889203172, -0.6162223019612712571 ) ) ;
#105327=CARTESIAN_POINT ( 'NONE',  ( 4.470608273529505183, -0.001430698596973853159, -1.942124712226586558 ) ) ;
#105332=CARTESIAN_POINT ( 'NONE',  ( 6.011958326525193463, -0.6379227081053112647, 1.803018720113582773 ) ) ;
#105333=CARTESIAN_POINT ( 'NONE',  ( 5.964077395145577221, -1.074666730956087335, 1.706109649615504154 ) ) ;
#105337=CARTESIAN_POINT ( 'NONE',  ( 2.484421436082083101, -0.3582009261528392163, -2.059553721446294894 ) ) ;
#105338=CARTESIAN_POINT ( 'NONE',  ( 0.7777615046654516862, -0.9880915000441170548, 1.468120464595161989 ) ) ;
#105341=CARTESIAN_POINT ( 'NONE',  ( 4.681715291062889861, -1.083280430520225046, 2.020132927424389102 ) ) ;
#105342=CARTESIAN_POINT ( 'NONE',  ( 1.833560160614732704, 1.721085009045751901, 0.2571270737643116533 ) ) ;
#105346=CARTESIAN_POINT ( 'NONE',  ( 2.073226780758777643, 1.288078611216292302, -1.160843940205048774 ) ) ;
#105348=CARTESIAN_POINT ( 'NONE',  ( 1.767777038385684785, -1.847514956963384414, 0.2233714002321494363 ) ) ;
#105349=CARTESIAN_POINT ( 'NONE',  ( 1.961612892103332229, 1.804449789391232795, 1.207184914618843807 ) ) ;
#105351=CARTESIAN_POINT ( 'NONE',  ( 4.663296154398564042, 1.879804967172087782, -0.7303043177912388328 ) ) ;
#105352=CARTESIAN_POINT ( 'NONE',  ( 3.281250000000002665, 0.7852924748301588487, 1.895863743164012849 ) ) ;
#105354=CARTESIAN_POINT ( 'NONE',  ( 1.043825456435763410, 0.7835056195745603302, -1.760039731681047215 ) ) ;
#105356=CARTESIAN_POINT ( 'NONE',  ( 4.869482922584397855, -1.877140712267670430, -1.187567259214457271 ) ) ;
#105357=ORIENTED_EDGE ( 'NONE', *, *, #182948, .F. ) ;
#105358=CARTESIAN_POINT ( 'NONE',  ( -0.2110808730067300354, 7.629137130509040077, -2.397154524934116182 ) ) ;
#105363=CARTESIAN_POINT ( 'NONE',  ( 0.1533981569187261029, 0.3862642299664406642, 2.187325829255863940 ) ) ;
#105364=CARTESIAN_POINT ( 'NONE',  ( 5.283633159863808437, -1.863482887291990409, 0.6137318589548645953 ) ) ;
#105367=CARTESIAN_POINT ( 'NONE',  ( 0.1811626231076196580, -0.1537715369321658587, -2.127283700313627346 ) ) ;
#105370=CARTESIAN_POINT ( 'NONE',  ( 3.244635591053147916, -2.031700879476082466, -0.3553325473293292847 ) ) ;
#105374=CARTESIAN_POINT ( 'NONE',  ( 5.342975940791072631, -1.604858128155508101, 0.9606422304059699657 ) ) ;
#105375=CARTESIAN_POINT ( 'NONE',  ( 3.691823404346205706, 1.489760995587570358, 0.8873103889329400085 ) ) ;
#105376=CARTESIAN_POINT ( 'NONE',  ( 3.596946774904510757, -0.5014486528964605672, 1.666646126512297821 ) ) ;
#105377=CARTESIAN_POINT ( 'NONE',  ( 1.312523894619976650, 1.535058519010788602, -1.702700526841523399 ) ) ;
#105379=CARTESIAN_POINT ( 'NONE',  ( 4.212501570603551571, 1.912301062189927015, 0.8455808105151915166 ) ) ;
#105380=CARTESIAN_POINT ( 'NONE',  ( 5.929623787841700633, 0.9553189508899215809, -1.690649115374833311 ) ) ;
#105384=CARTESIAN_POINT ( 'NONE',  ( 1.037732671793228700, -1.587836052788630603, 1.242728777923551409 ) ) ;
#105385=CARTESIAN_POINT ( 'NONE',  ( 0.5805319366703353134, 1.050441701016215923, 1.842106252469346117 ) ) ;
#105387=CARTESIAN_POINT ( 'NONE',  ( 6.311172677262812059, 1.158691452862798954, -1.650079838712660063 ) ) ;
#105390=CARTESIAN_POINT ( 'NONE',  ( 2.824977599723184074, 1.534285384246200090, -1.463936014953904463 ) ) ;
#105391=CARTESIAN_POINT ( 'NONE',  ( 4.125493313500066428, -1.746467973620144942, 0.5319596651164605339 ) ) ;
#105399=CARTESIAN_POINT ( 'NONE',  ( 2.408468576312505771, -2.014670991514801113, -0.1442217307643048063 ) ) ;
#105400=CARTESIAN_POINT ( 'NONE',  ( 5.456176519787153012, 2.204477245749701719, -0.1032804940204190558 ) ) ;
#105402=CARTESIAN_POINT ( 'NONE',  ( 3.449909520549806707, -0.7582208578979282576, 1.699682486939468440 ) ) ;
#105409=CARTESIAN_POINT ( 'NONE',  ( 4.617693566336190436, -1.789886777702164089, 0.3589094947460610974 ) ) ;
#105413=CARTESIAN_POINT ( 'NONE',  ( 1.071195256775770543, 1.317505809736085665, -1.127239923523750909 ) ) ;
#105414=CARTESIAN_POINT ( 'NONE',  ( 0.5150585655138568697, -0.9269755740852363424, -1.472709990541859693 ) ) ;
#105415=CARTESIAN_POINT ( 'NONE',  ( 5.303480822065511191, 1.883932040028640786, 1.332532017187069817 ) ) ;
#105417=CARTESIAN_POINT ( 'NONE',  ( 6.784453917077649443, -2.118420112955111456, -0.4290502581522498415 ) ) ;
#105419=CARTESIAN_POINT ( 'NONE',  ( 5.905696578591778767, 0.4397782949263558949, 2.255800006528754675 ) ) ;
#105423=CARTESIAN_POINT ( 'NONE',  ( 6.280143113937574739, -0.9989825818290422044, 1.581392243879369053 ) ) ;
#105425=CARTESIAN_POINT ( 'NONE',  ( 3.006014587165442453, -0.7710369221427433306, 1.750240277048662030 ) ) ;
#105428=CARTESIAN_POINT ( 'NONE',  ( 4.969440760808212509, 0.2186952961555181096, -2.196011921426939129 ) ) ;
#105429=CARTESIAN_POINT ( 'NONE',  ( 5.067619284625084930, 1.424172025040346679, 1.566925857267987832 ) ) ;
#105431=CARTESIAN_POINT ( 'NONE',  ( 6.983263157960366563, 2.446371134953594151, 2.328889586965996905 ) ) ;
#105434=CARTESIAN_POINT ( 'NONE',  ( 5.584674446412367210, -1.345185468269005424, 1.639207791927596247 ) ) ;
#105435=ADVANCED_FACE ( 'NONE', ( #7453 ), #124511, .T. ) ;
#105436=CARTESIAN_POINT ( 'NONE',  ( 2.696638560983040112, -2.301352489519994382, -0.1704845361689636130 ) ) ;
#105437=CARTESIAN_POINT ( 'NONE',  ( 3.701569118832209515, -1.483977648892897960, -1.283320388228793130 ) ) ;
#105438=CARTESIAN_POINT ( 'NONE',  ( 6.983263157960404754, -0.005959781318053481922, 2.045923054782183392 ) ) ;
#105442=CARTESIAN_POINT ( 'NONE',  ( 5.542203953035277131, 0.8216685229280199509, 1.841735684200429990 ) ) ;
#105445=CARTESIAN_POINT ( 'NONE',  ( 3.379888771869215436, -2.093702847677909595, 0.5742949676477026033 ) ) ;
#105447=CARTESIAN_POINT ( 'NONE',  ( 0.7211286721200690364, 1.601891702520108485, -1.389630591760198541 ) ) ;
#105450=CARTESIAN_POINT ( 'NONE',  ( 0.1333692844072585093, 7.629137130509075604, -2.653547345224527287 ) ) ;
#105452=CARTESIAN_POINT ( 'NONE',  ( 0.6497718435918962143, 0.6490781098625525436, -1.955935974237718256 ) ) ;
#105456=DIRECTION ( 'NONE',  ( -0.9999980456341539536, 0.000000000000000000, -0.001977050295949901899 ) ) ;
#105459=CARTESIAN_POINT ( 'NONE',  ( 2.824755571612533434, 1.383597569638248315, -1.320258682893655999 ) ) ;
#105460=CARTESIAN_POINT ( 'NONE',  ( 5.541803865142582275, 0.7143684798897788069, -1.619465043896466616 ) ) ;
#105464=CARTESIAN_POINT ( 'NONE',  ( 0.2108110590392465178, 1.506053368259860248, -1.006445417241896845 ) ) ;
#105466=CARTESIAN_POINT ( 'NONE',  ( 1.235391793297924812, 0.5527703352327991704, -1.834263772151963456 ) ) ;
#105467=CARTESIAN_POINT ( 'NONE',  ( 2.453653613718423276, 1.598880132357576755, 1.315258840600006085 ) ) ;
#105469=CARTESIAN_POINT ( 'NONE',  ( 6.262560305340551636, -1.321439916381482060, 1.324322166508178356 ) ) ;
#105470=CARTESIAN_POINT ( 'NONE',  ( 3.070728972534173096, -1.687097908962056803, -0.6982200720766564839 ) ) ;
#105471=CARTESIAN_POINT ( 'NONE',  ( 5.233140740401229785, 0.1595256157847015632, 2.201181388321731269 ) ) ;
#105474=CARTESIAN_POINT ( 'NONE',  ( 4.422371107804410784, 0.9697015505613596487, 1.820508916172391300 ) ) ;
#105478=CARTESIAN_POINT ( 'NONE',  ( 0.8960494714182369869, -0.7788709108395329705, 2.016556642405589184 ) ) ;
#105479=CARTESIAN_POINT ( 'NONE',  ( 6.531696417657103737, 1.982406992490031383, -0.5971068152322634992 ) ) ;
#105481=CARTESIAN_POINT ( 'NONE',  ( 3.831458500214664387, -1.998831773244442056, 0.8233788064144487162 ) ) ;
#105482=CARTESIAN_POINT ( 'NONE',  ( 4.776038667982859032, 1.997392889608617716, -0.2983725866285909523 ) ) ;
#105483=CARTESIAN_POINT ( 'NONE',  ( 6.620655732516650183, -0.005281389526671976913, 2.273887028200880511 ) ) ;
#105489=CARTESIAN_POINT ( 'NONE',  ( 2.641814858895009444, 2.006371511526034546, -0.2024640970367599380 ) ) ;
#105494=CARTESIAN_POINT ( 'NONE',  ( 6.205323455156911194, 1.660478276859885582, -0.9486371710855368011 ) ) ;
#105498=CARTESIAN_POINT ( 'NONE',  ( 3.937125189161301719, -1.678018027730580286, -1.117815418662113425 ) ) ;
#105501=CARTESIAN_POINT ( 'NONE',  ( 6.053657651994457822, 0.4959367165196375549, -1.651908409946404976 ) ) ;
#105505=CARTESIAN_POINT ( 'NONE',  ( 5.852782322939767745, -1.474943281369223369, 1.150351685248012457 ) ) ;
#105507=CARTESIAN_POINT ( 'NONE',  ( 2.588806720547200513, 2.007000696110202043, 0.5072723548179418618 ) ) ;
#105510=CARTESIAN_POINT ( 'NONE',  ( 0.3863424973270003226, -0.6820169105002243937, -1.897691504806876761 ) ) ;
#105511=CARTESIAN_POINT ( 'NONE',  ( 1.634716215409822260, 1.691188361570634235, 0.6499044650936767198 ) ) ;
#105517=CARTESIAN_POINT ( 'NONE',  ( 6.046487378053778450, -1.350936885689631772, 1.358403761460762471 ) ) ;
#105524=CARTESIAN_POINT ( 'NONE',  ( 2.993221558690632556, 1.854768100113469265, -1.110066390340218367 ) ) ;
#105527=CARTESIAN_POINT ( 'NONE',  ( 0.6684183810189650021, 2.117893379942568988, -0.1100008709709817956 ) ) ;
#105528=CARTESIAN_POINT ( 'NONE',  ( 5.965807262869927463, 1.798080572464531679, -0.3147057940002598864 ) ) ;
#105529=CARTESIAN_POINT ( 'NONE',  ( 2.161341668630599955, 0.3408821015241836894, -1.941522824740661290 ) ) ;
#105530=CARTESIAN_POINT ( 'NONE',  ( 5.062724140118719518, 0.5608846916410530348, 1.828269531156314853 ) ) ;
#105533=CARTESIAN_POINT ( 'NONE',  ( 4.404722228293363351, 0.5232710054461316984, 1.898709409516568192 ) ) ;
#105534=CARTESIAN_POINT ( 'NONE',  ( 6.567919353034534780, -1.191429365117269157, 1.534444726360333799 ) ) ;
#105542=CARTESIAN_POINT ( 'NONE',  ( 5.109976026518994630, -0.6845719981980763480, 1.785733525123212928 ) ) ;
#105544=CARTESIAN_POINT ( 'NONE',  ( 0.8334014933106950185, 0.1641056870149599223, 2.200712145998296343 ) ) ;
#105546=CARTESIAN_POINT ( 'NONE',  ( 5.742843059509288750, 1.940770921862687182, 0.5345600180575919014 ) ) ;
#105547=CARTESIAN_POINT ( 'NONE',  ( 0.07661050522435489119, 4.099791711901569435, -2.265836654070508605 ) ) ;
#105551=CARTESIAN_POINT ( 'NONE',  ( 2.453653613718423276, 1.598880132357576755, 1.315258840600006085 ) ) ;
#105555=CARTESIAN_POINT ( 'NONE',  ( 0.9894095316701527754, 1.906041449620498929, -1.019753361306941386 ) ) ;
#105565=CARTESIAN_POINT ( 'NONE',  ( 4.676219527341594073, 1.289314336954486384, 1.159937944992680547 ) ) ;
#105567=CARTESIAN_POINT ( 'NONE',  ( 2.782155020660907141, -1.188329515115684076, -1.695063343828225877 ) ) ;
#105568=CARTESIAN_POINT ( 'NONE',  ( 4.710634317702605323, 2.026528413205666013, 0.6131292256000410168 ) ) ;
#105572=CARTESIAN_POINT ( 'NONE',  ( 2.184365610098043309, 1.138103218778206971, -1.607087707149345901 ) ) ;
#105575=CARTESIAN_POINT ( 'NONE',  ( 4.400488903878751579, 1.773513045242902209, -1.452268937634313417 ) ) ;
#105576=CARTESIAN_POINT ( 'NONE',  ( 1.365546509989667534, 1.798985258052044900, -0.3101867277976525505 ) ) ;
#105580=CARTESIAN_POINT ( 'NONE',  ( 3.234638274129162827, 1.273785088661258058, -1.559031609643942717 ) ) ;
#105581=CARTESIAN_POINT ( 'NONE',  ( 3.643363735869999509, 1.775428317022755609, -0.8347113108059034392 ) ) ;
#105585=CARTESIAN_POINT ( 'NONE',  ( 5.595677694052432649, -2.090823719441712747, -0.0008997866532325231618 ) ) ;
#105586=CARTESIAN_POINT ( 'NONE',  ( 4.469463222250699808, 1.716395428585426153, -0.4311418314640375615 ) ) ;
#105588=CARTESIAN_POINT ( 'NONE',  ( 0.4280004979528989617, 1.123059939108238314, -1.881669248891951085 ) ) ;
#105589=CARTESIAN_POINT ( 'NONE',  ( 5.173663570605946838, -0.9624332111635640619, 1.449765197900940938 ) ) ;
#105591=CARTESIAN_POINT ( 'NONE',  ( 0.1331715793776913348, 0.7364730991098663582, -2.038600455735229300 ) ) ;
#105593=CARTESIAN_POINT ( 'NONE',  ( 6.346320258841911865, 0.3977546830747305528, -2.263887401186816639 ) ) ;
#105594=CARTESIAN_POINT ( 'NONE',  ( -0.07626876867936756288, -1.353788312843669406, -1.724171373301164767 ) ) ;
#105595=CARTESIAN_POINT ( 'NONE',  ( 5.764916378462246804, -1.734034293797588999, 0.002837784182162239165 ) ) ;
#105596=CARTESIAN_POINT ( 'NONE',  ( 2.332911791115964473, 2.140974936812658935, 0.5348262304398290201 ) ) ;
#105598=CARTESIAN_POINT ( 'NONE',  ( 5.740740459546420205, -2.117024774779395102, -0.4812451790989195621 ) ) ;
#105599=CARTESIAN_POINT ( 'NONE',  ( 0.7962977453638077074, -0.9578387366565711547, -1.888411434433327374 ) ) ;
#105600=CARTESIAN_POINT ( 'NONE',  ( 4.093750000000002665, -1.895863743164171611, -0.7852924748297696045 ) ) ;
#105602=CARTESIAN_POINT ( 'NONE',  ( 6.727182134110234024, -0.002100931800118072384, 2.089081857379895268 ) ) ;
#105603=CARTESIAN_POINT ( 'NONE',  ( 4.278288924157873652, -1.109688035731031475, 1.574481611047764851 ) ) ;
#105604=CARTESIAN_POINT ( 'NONE',  ( 1.366231352279376310, 0.6402347118669349246, -2.127050378772620487 ) ) ;
#105606=CARTESIAN_POINT ( 'NONE',  ( 1.312523894619976650, 1.535058519010788602, -1.702700526841523399 ) ) ;
#105610=CARTESIAN_POINT ( 'NONE',  ( 3.616091037371416572, -0.6436381315554053906, 2.126022720447027670 ) ) ;
#105618=CARTESIAN_POINT ( 'NONE',  ( 2.338517726396415863, 0.5350873343827439177, -1.944071628254496087 ) ) ;
#105620=CARTESIAN_POINT ( 'NONE',  ( 6.883263157960402445, -0.003972766660574957552, 2.046037087719229319 ) ) ;
#105623=CARTESIAN_POINT ( 'NONE',  ( 6.356985390939413172, 0.2876776518413763917, -1.716344579348449084 ) ) ;
#105625=CARTESIAN_POINT ( 'NONE',  ( 1.035986422354659320, 1.742213337529074035, 0.3100009841157587154 ) ) ;
#105626=CARTESIAN_POINT ( 'NONE',  ( 0.5455463417442986129, -1.458554840210561476, 1.392547631435703037 ) ) ;
#105627=CARTESIAN_POINT ( 'NONE',  ( 0.3800845246329161431, -0.2246070939678334044, -1.827447590993152682 ) ) ;
#105628=CARTESIAN_POINT ( 'NONE',  ( 4.599361256383265761, -0.6123007911535255365, 2.209042870082494225 ) ) ;
#105629=CARTESIAN_POINT ( 'NONE',  ( 3.943160212656390051, 0.6185462545997171269, -1.734258544408360470 ) ) ;
#105634=CARTESIAN_POINT ( 'NONE',  ( 3.258640109524315154, -1.383274205585843797, 1.191454006006509303 ) ) ;
#105635=CARTESIAN_POINT ( 'NONE',  ( 4.219375079941334761, 1.978050461189932552, 0.3905991720301109082 ) ) ;
#105637=CARTESIAN_POINT ( 'NONE',  ( 3.239431411193524735, -1.996134195211620721, 1.065073381557869903 ) ) ;
#105639=CARTESIAN_POINT ( 'NONE',  ( 5.596739085487917542, -0.5086175864091507792, -2.043493955398622219 ) ) ;
#105641=CARTESIAN_POINT ( 'NONE',  ( 3.297389726143421740, -1.827171938055579536, 0.9735347560282039403 ) ) ;
#105644=CARTESIAN_POINT ( 'NONE',  ( 5.988958055669808545, -2.013456733998910231, -0.6654305520411087915 ) ) ;
#105647=CARTESIAN_POINT ( 'NONE',  ( 0.6449897232218603227, -1.652859335204670543, 0.9894661712252955654 ) ) ;
#105654=CARTESIAN_POINT ( 'NONE',  ( 0.5982529507728174822, 1.497540282193830841, 1.640895070279895895 ) ) ;
#105655=CARTESIAN_POINT ( 'NONE',  ( 2.274573006691050558, -1.296483931956838198, 1.659472957066634669 ) ) ;
#105658=CARTESIAN_POINT ( 'NONE',  ( 6.965680890820083349, -0.4048625726877760900, 1.822745621051139020 ) ) ;
#105667=CARTESIAN_POINT ( 'NONE',  ( 3.350005920730843911, -0.7974703105717847462, 1.792663495558038056 ) ) ;
#105668=CARTESIAN_POINT ( 'NONE',  ( 2.079201547314021070, -0.1057080177612122196, -2.159229931372666389 ) ) ;
#105669=CARTESIAN_POINT ( 'NONE',  ( 1.118424870118275738, -0.04499623084481922664, 1.840855209834332928 ) ) ;
#105672=CARTESIAN_POINT ( 'NONE',  ( 3.134399458026761121, -1.534476879465409782, 0.8210378458504956622 ) ) ;
#105676=CARTESIAN_POINT ( 'NONE',  ( 0.4796413896344040029, 2.016494124141111399, -0.7793912508547717888 ) ) ;
#105677=CARTESIAN_POINT ( 'NONE',  ( 3.462267382487670631, 1.587593928739635896, 1.242537129137813556 ) ) ;
#105679=CARTESIAN_POINT ( 'NONE',  ( 0.6730137850648570952, -2.035850703004048246, -0.7271551459356735414 ) ) ;
#105680=CARTESIAN_POINT ( 'NONE',  ( 2.746899856880557600, -1.639987585725300123, 1.093844759732710781 ) ) ;
#105681=CARTESIAN_POINT ( 'NONE',  ( 6.609000000000053276, 6.037706995087852135, 2.494900065673964829 ) ) ;
#105682=CARTESIAN_POINT ( 'NONE',  ( 2.770961567126817737, 1.843342918492569149, -0.6114499264749191365 ) ) ;
#105693=CARTESIAN_POINT ( 'NONE',  ( 5.456226512670824036, 2.305251103711564387, -0.1065007851034898423 ) ) ;
#105695=CARTESIAN_POINT ( 'NONE',  ( 3.643363735869999509, 1.775428317022755609, -0.8347113108059034392 ) ) ;
#105697=CARTESIAN_POINT ( 'NONE',  ( 0.8443752267504719411, 0.3905955241953715795, -1.978051186352240309 ) ) ;
#105699=CARTESIAN_POINT ( 'NONE',  ( 2.870428589035282751, -2.086819620220676352, -0.3573068958101219827 ) ) ;
#105702=CARTESIAN_POINT ( 'NONE',  ( 2.888418961059231904, 1.578855305991919478, -0.9468669452540460219 ) ) ;
#105706=CARTESIAN_POINT ( 'NONE',  ( 4.377262645480927361, -1.895543854172193399, -0.9507902649282941043 ) ) ;
#105707=CARTESIAN_POINT ( 'NONE',  ( 0.1988192939417210425, -0.4940924592915455493, 1.773541111592655373 ) ) ;
#105711=CARTESIAN_POINT ( 'NONE',  ( 4.393860645892766037, -0.7923225987812362314, 1.902584447174461291 ) ) ;
#105713=CARTESIAN_POINT ( 'NONE',  ( 1.927068723821170559, -1.203646435588998420, -1.393412863611859454 ) ) ;
#105717=B_SPLINE_CURVE_WITH_KNOTS ( 'NONE', 3,
 ( #201608, #186442, #38079, #102008, #185375, #183251, #182173, #137725, #67337, #2339, #34854, #33802, #119387, #17528, #118320, #136657, #53257, #104151, #184306, #100929, #19676, #200548, #83616, #68416, #149698, #36995, #134543, #103079, #18610, #70538, #1279, #170199, #168078, #20729, #85756, #133482, #151837, #3413, #169134, #21783, #69479, #135587, #86824, #87892, #152888, #4466, #202682, #120470, #153965, #5532, #71612, #55389, #23938, #76958, #109551, #72694, #121544, #7686, #107408, #173431, #175556, #25011, #188583, #91113, #106325, #125810, #172348, #138789, #40216, #43427, #39146, #90042, #124745, #41300, #9830, #174501, #156100, #105227, #73769, #122622, #42366, #139865, #191772, #205896, #8767, #26078, #190704, #74849, #75906, #27146, #157172, #10883, #159284, #93250, #171267, #143083, #57530, #22861, #123687, #189649, #108477, #140948, #59651, #92192, #158241, #206961, #142010, #209077, #208025, #58590, #187515, #88974, #155029, #6614, #204809, #56460, #110611, #16202, #127959, #144158, #64966, #131119, #78033, #14074, #113811, #44494, #30366, #177682, #130071, #126878, #11960, #145214, #197108, #62847, #180860, #210149, #61792, #147316, #82284, #48747, #32482, #96453, #193913, #213343, #13019, #114860, #45560, #98556, #148377, #179811, #163564, #111675, #31430, #162504, #211221, #29294, #60714, #194985, #176611, #97507, #15148, #164617, #81234, #146269, #80164, #160357, #212281, #192835, #28223, #94316, #46621, #95386, #161438, #79096, #129008, #112742, #63915, #178753, #196066, #47696, #168872, #149432, #167813, #152625, #34605, #185105, #119124, #101746, #85491, #52988, #199219, #68150, #151578, #150515, #4212, #36730, #102817, #84426, #69215, #136396, #20476, #99616, #66009, #181911, #19413, #86563, #166751, #133213, #198163, #70280, #135334, #37812, #202412, #54069, #17270, #3146, #120203, #49797, #184048, #116988, #201348, #186178, #182988, #50866, #103888, #169936, #21520, #87631, #214378, #132158, #83346, #18347, #33543, #100673, #2076, #115923, #165682, #1013, #67078, #134283, #200288, #51939, #118063, #35666, #124485, #189390, #89792, #138526, #109285, #73503, #203480, #190443, #58329, #104965, #55133, #6354, #24747, #42103, #26881, #72424, #157983, #139605, #156912, #171007, #153703, #175295, #38881, #122360, #22604, #5271, #90849, #137466, #23680, #108216, #173169, #9571, #155837, #88711, #205629, #204549, #57266, #39958, #71348, #8502, #106065, #74583, #154770, #174240, #56198, #25813, #121278, #172088, #91923, #141755, #41032, #43173, #191507, #125546, #187254, #188317, #7422, #206702, #123428, #107142, #140686, #75648, #207762, #59389, #146001, #177412, #162231, #14874, #113542, #29029, #195788, #127686, #179545, #47426, #31166, #160090, #142813, #63654, #13818, #130851, #80966, #97239, #110347, #46352, #212011, #76697, #62576, #209882, #79891, #159029, #44225, #95112, #147058, #161162, #213078, #27957, #94050, #64708, #176350, #45288, #126607, #77768, #12748, #208820, #180595, #129809, #10622, #92984, #192570, #112470, #163293, #78822, #11693, #144943, #143888, #61520, #210950, #128738, #60450, #196849, #48486, #193646, #111408, #194712, #178479, #114604, #30091, #96180, #36475, #32220, #1817, #148114, #181649, #165411, #18074, #150249, #164355, #98293, #183793, #15939, #116719, #201086, #51680 ),
 .UNSPECIFIED., .F., .F.,
 ( 4, 1, 1, 1, 1, 1, 1, 1, 1, 1, 1, 1, 1, 1, 1, 1, 1, 1, 1, 1, 1, 1, 1, 1, 1, 1, 1, 1, 1, 1, 1, 1, 1, 1, 1, 1, 1, 1, 1, 1, 1, 1, 1, 1, 1, 1, 1, 1, 1, 1, 1, 1, 1, 1, 1, 1, 1, 1, 1, 1, 1, 1, 1, 1, 1, 1, 1, 1, 1, 1, 1, 1, 1, 1, 1, 1, 1, 1, 1, 1, 1, 1, 1, 1, 1, 1, 1, 1, 1, 1, 1, 1, 1, 1, 1, 1, 1, 1, 1, 1, 1, 1, 1, 1, 1, 1, 1, 1, 1, 1, 1, 1, 1, 1, 1, 1, 1, 1, 1, 1, 1, 1, 1, 1, 1, 1, 1, 1, 1, 1, 1, 1, 1, 1, 1, 1, 1, 1, 1, 1, 1, 1, 1, 1, 1, 1, 1, 1, 1, 1, 1, 1, 1, 1, 1, 1, 1, 1, 1, 1, 1, 1, 1, 1, 1, 1, 1, 1, 1, 1, 1, 1, 1, 1, 1, 1, 1, 1, 1, 1, 1, 1, 1, 1, 1, 1, 1, 1, 1, 1, 1, 1, 1, 1, 1, 1, 1, 1, 1, 1, 1, 1, 1, 1, 1, 1, 1, 1, 1, 1, 1, 1, 1, 1, 1, 1, 1, 1, 1, 1, 1, 1, 1, 1, 1, 1, 1, 1, 1, 1, 1, 1, 1, 1, 1, 1, 1, 1, 1, 1, 1, 1, 1, 1, 1, 1, 1, 1, 1, 1, 1, 1, 1, 1, 1, 1, 1, 1, 1, 1, 1, 1, 1, 1, 1, 1, 1, 1, 1, 1, 1, 1, 1, 1, 1, 1, 1, 1, 1, 1, 1, 1, 1, 1, 1, 1, 1, 1, 1, 1, 1, 1, 1, 1, 1, 1, 1, 1, 1, 1, 1, 1, 1, 1, 1, 1, 1, 1, 1, 1, 1, 1, 1, 1, 1, 1, 1, 1, 1, 1, 1, 1, 1, 1, 1, 1, 1, 1, 1, 1, 1, 1, 1, 1, 1, 1, 1, 1, 1, 1, 1, 1, 1, 1, 1, 1, 1, 1, 1, 1, 1, 1, 1, 1, 1, 1, 1, 1, 1, 1, 1, 1, 1, 1, 1, 1, 1, 1, 1, 1, 1, 1, 1, 1, 1, 1, 1, 1, 1, 1, 1, 1, 1, 1, 4 ),
 ( 0.000000000000000000, 0.002600033395298661284, 0.005208813367820810773, 0.007813200023264601363, 0.01041635779573905213, 0.01302082523971277370, 0.01562491580351430334, 0.01822918961192645723, 0.02083333155136493989, 0.02343746137460561707, 0.02604174567981391505, 0.02864576082122225614, 0.03125012338981237453, 0.03385410379569547823, 0.03645843966640821554, 0.03906250599122108869, 0.04166672065998115043, 0.04427093656960304907, 0.04687500111868234121, 0.04947933663890847350, 0.05208331727515622817, 0.05468767913406928638, 0.05729168951085979872, 0.05989597295159828499, 0.06250011041458469752, 0.06510424634142775169, 0.06770853038940542745, 0.07031253939703428768, 0.07291690072920921362, 0.07552088074063932621, 0.07812521459448035221, 0.08072927904253822395, 0.08333349217322323643, 0.08593770650149938628, 0.08854176936806532061, 0.09114610329512429221, 0.09375008230893774885, 0.09635444258075796797, 0.09895845137230636912, 0.1015627332241899466, 0.1041668691376404637, 0.1067710034717011397, 0.1093752859901425123, 0.1119792934252105548, 0.1145836532378000650, 0.1171876317139315254, 0.1197919640503514460, 0.1223960270027875247, 0.1250002386107842423, 0.1276044514713231270, 0.1302085128224930721, 0.1328128452953424854, 0.1354168228245230532, 0.1380211816480703679, 0.1406251889951717071, 0.1432294693974442978, 0.1458336039016293884, 0.1484377367829480265, 0.1510420179109137340, 0.1536460239143070949, 0.1562503823458506746, 0.1588543594276481397, 0.1614586903853630351, 0.1640627519827278502, 0.1666669622076225599, 0.1692711737400035832, 0.1718752337163205746, 0.1744795648736557347, 0.1770835410591554138, 0.1796878985729436218, 0.1822919046164021839, 0.1848961837081005144, 0.1875003169431251615, 0.1901044485118078553, 0.1927087283883223978, 0.1953127331008320255, 0.1979170902898210183, 0.2005210661182068033, 0.2031253958358791578, 0.2057294562186703923, 0.2083336651999991573, 0.2109378755437518183, 0.2135419342857080849, 0.2161462642661750033, 0.2187502392488957503, 0.2213545955913898966, 0.2239586004719608947, 0.2265628783920732026, 0.2291670104979939837, 0.2317711408940984485, 0.2343754196581391558, 0.2369794232205082452, 0.2395837793053874898, 0.2421877540212369617, 0.2447920826374832270, 0.2473961419461526701, 0.2500003498234057431, 0.2526045591180144934, 0.2552086167660569949, 0.2578129457082574683, 0.2604169196290564980, 0.2630212749386780513, 0.2656252787970727613, 0.2682295556845439854, 0.2708336868013750398, 0.2734378161649161920, 0.2760420939554183439, 0.2786460965083475960, 0.2812504516275206035, 0.2838544253716674404, 0.2864587530250631842, 0.2890628114000217685, 0.2916670183126490179, 0.2942712266975582858, 0.2968752833920936807, 0.2994796114345903981, 0.3020835844342854570, 0.3046879388494173613, 0.3072919418263086455, 0.3098962178200457829, 0.3125003480877632800, 0.3151044765587182606, 0.3177087535145803887, 0.3203127551987332566, 0.3229171094905676220, 0.3255210824038090589, 0.3281254092328941829, 0.3307294668145174810, 0.3333336729019333866, 0.3359378805165532667, 0.3385419363979534357, 0.3411462636792753078, 0.3437502358986498918, 0.3463545895576419231, 0.3489585917936692261, 0.3515628670325462446, 0.3541669965910940188, 0.3567711243094072171, 0.3593754005694961839, 0.3619794015255044517, 0.3645837551283364619, 0.3671877273514386752, 0.3697920534947228832, 0.3723961104233561858, 0.3750003158249449187, 0.3776045228086560845, 0.3802085780172632101, 0.3828129046759103926, 0.3854168762557192984, 0.3880212292968930887, 0.3906252309326675998, 0.3932295055555311003, 0.3958336345448258409, 0.3984377616504144459, 0.4010420373535708016, 0.4036460377220391638, 0.4062503907741795706, 0.4088543624478828686, 0.4114586880438503846, 0.4140627444598136697, 0.4166669493149349202, 0.4192711558070936761, 0.4218752104832254046, 0.4244795366576747386, 0.4270835077386489487, 0.4296878603003031483, 0.4322918614764136302, 0.4348961356220873986, 0.4375002641820237570, 0.4401043908147829753, 0.4427086660998260093, 0.4453126660213379551, 0.4479170186610768045, 0.4505209899261007900, 0.4531253151132156320, 0.4557293711568096706, 0.4583335756048029785, 0.4609377817447468106, 0.4635418360287018591, 0.4661461618574116450, 0.4687501325802634344, 0.4713544848006788190, 0.4739584856576960492, 0.4765627594649867738, 0.4791668877354426925, 0.4817710140352507997, 0.4843752890409837031, 0.4869792886561065681, 0.4895836410217184742, 0.4921876120187673176, 0.4947919369354787933, 0.4973959927469893683, 0.5000001969271801183, 0.5026044028542325792, 0.5052084568862954539, 0.5078127825077110025, 0.5104167530131399344, 0.5130211050305848453, 0.5156251057090676104, 0.5182293793167697116, 0.5208335074376115870, 0.5234376335443351458, 0.5260419084095501185, 0.5286459078588399141, 0.5312502600885893322, 0.5338542309583571566, 0.5364585557431046370, 0.5390626114628084276, 0.5416668155145124564, 0.5442710213679887721, 0.5468750752884355970, 0.5494794008409938924, 0.5520833712696913143, 0.5546877232224267651, 0.5572917238629264691, 0.5598959974098275394, 0.5625001255209155504, 0.5651042515744146844, 0.5677085264378984863, 0.5703125258619060611, 0.5729168780940517847, 0.5755208489772277725, 0.5781251737684461878, 0.5807292295366155432, 0.5833334335991446906, 0.5859376395183565345, 0.5885416934674594369, 0.5911460190895951872, 0.5937499895822500040, 0.5963543416085342885, 0.5989583423516006144, 0.6015626159764864145, 0.6041667442176794633, 0.6067708703578130747, 0.6093751453583519107, 0.6119791448976270587, 0.6145834972704286026, 0.6171874683077025470, 0.6197917932438269384, 0.6223958492007358734, 0.6250000534134032559, 0.6276042595376638555, 0.6302083136556971832, 0.6328126394858472059, 0.6354166101831504321, 0.6380209624212449526, 0.6406249634074311361, 0.6432292372490908683, 0.6458333657602520761, 0.6484374921268833969, 0.6510417674032679125, 0.6536457671983656459, 0.6562501198500874100, 0.6588540911821543222, 0.6614584164016259482, 0.6640624726875546946, 0.6666666771896793131, 0.6692708836583093346, 0.6718749380855545406, 0.6744792642621626477, 0.6770832353048136243, 0.6796875878929879988, 0.6822915892628557133, 0.6848958634600870177, 0.6874999923810890534, 0.6901041191140900866, 0.6927083948051209195, 0.6953123949966061312, 0.6979167480655225075, 0.7005207198330885010, 0.7031250454743595002, 0.7057291022295995031, 0.7083333071605121267, 0.7109375141128444486, 0.7135415689895947544, 0.7161458956511181917, 0.7187498671798290273, 0.7213542202563657524, 0.7239582221504904380, 0.7265624968421051655, 0.7291666263128349090, 0.7317707535520923123, 0.7343750297965853102, 0.7369790305250381035, 0.7395833841494394711, 0.7421873564932268685, 0.7447916826947649227, 0.7473957400596251688, 0.7499999455586733310, 0.7526041531340577073, 0.7552082086006238759, 0.7578125358855373195, 0.7604165080410384414, 0.7630208617442386654, 0.7656248643032155243, 0.7682291396280439555, 0.7708332697884082707, 0.7734373976738285750, 0.7760416746106194585, 0.7786456760166404756, 0.7812500303348380859, 0.7838540033955903041, 0.7864583302958847444, 0.7890623884106959807, 0.7916665946172487534, 0.7942708029550582527, 0.7968748591517740287, 0.7994791871985751364, 0.8020831601216208417, 0.8046875145898089166, 0.8072915179542569097, 0.8098957940511537501, 0.8124999250410844809, 0.8151040537125986418, 0.8177083314805486669, 0.8203123337047645292, 0.8229166888550945025, 0.8255206627735817149, 0.8281249905111484066, 0.8307290495162685806, 0.8333332565697225691, 0.8359374658093579047, 0.8385415228765847884, 0.8411458518237998616, 0.8437498256551729803, 0.8463541810267020127, 0.8489581853372698550, 0.8515624623451190089, 0.8541665943045783083, 0.8567707239021479237, 0.8593750026401490993, 0.8619790058232168484, 0.8645833619440471685, 0.8671873368610717447, 0.8697916655744575287, 0.8723957256102774505, 0.8749999336500613456, 0.8776041439309557601, 0.8802082020090884473, 0.8828125319952765393, 0.8854165068757942070, 0.8880208632890512765, 0.8906248686864229880, 0.8932291467441429988, 0.8958332798131283248, 0.8984374104767501867, 0.9010416903237299380, 0.9036456946063434748, 0.9062500518360779855, 0.9088540278924787108, 0.9114583577202677311, 0.9140624189272162914, 0.9166666280927961985, 0.9192708395544209043, 0.9218748987838942810, 0.9244792299476556341, 0.9270832060181642964, 0.9296875636115721209, 0.9322915702365133228, 0.9348958494830461596, 0.9374999838014769216, 0.9401041156712998115, 0.9427083967663798525, 0.9453124022892170908, 0.9479167607665550666, 0.9505207380999710631, 0.9531250691809918241, 0.9557291317261836783, 0.9583333421310490374, 0.9609375547886240820, 0.9635416155522130710, 0.9661459483928183101, 0.9687499245033458495, 0.9713542829945021051, 0.9739582954330652242, 0.9765625745907361432, 0.9791667024412501474, 0.9817708385604039245, 0.9843751096149007118, 0.9869791944699233266, 0.9895836584107432499, 0.9921868132917668337, 0.9947911946869415489, 0.9973999724172807335, 1.000000000000000000 ),
 .UNSPECIFIED. ) ;
#105718=CARTESIAN_POINT ( 'NONE',  ( 0.9794701899953797142, -0.05759512415488829418, -2.206297691287119722 ) ) ;
#105719=CARTESIAN_POINT ( 'NONE',  ( 3.989755448363790258, 1.635235102580555155, 1.563706588500752837 ) ) ;
#105721=CARTESIAN_POINT ( 'NONE',  ( 3.920002888225936566, -1.806327840557620412, 0.1390898763422818984 ) ) ;
#105722=CARTESIAN_POINT ( 'NONE',  ( 4.540194369826378029, 0.7389084316076138803, 1.767693002002197034 ) ) ;
#105723=CARTESIAN_POINT ( 'NONE',  ( 4.932118098221458524, 1.189261692661430114, 1.694535115018414917 ) ) ;
#105726=CARTESIAN_POINT ( 'NONE',  ( 2.606273030088624765, -0.7529636864501542126, -1.822200628222752972 ) ) ;
#105727=CARTESIAN_POINT ( 'NONE',  ( 1.571183270939533694, 0.1444824169965253369, -1.921038573443895059 ) ) ;
#105728=CARTESIAN_POINT ( 'NONE',  ( 4.012460596634464416, 1.323225596166040186, -1.322536486416127977 ) ) ;
#105729=CARTESIAN_POINT ( 'NONE',  ( 2.983396891919448013, -0.1703749763015352803, -2.301462837838092135 ) ) ;
#105730=CARTESIAN_POINT ( 'NONE',  ( 4.140933978860473985, -0.1807793374023874688, -1.852226635870577898 ) ) ;
#105736=CARTESIAN_POINT ( 'NONE',  ( 0.6453166446471610973, -1.805311040884694185, 1.084365637629558954 ) ) ;
#105743=CARTESIAN_POINT ( 'NONE',  ( 1.898838059644195386, -2.080654286433290867, -0.4088066060855889972 ) ) ;
#105745=CARTESIAN_POINT ( 'NONE',  ( 0.9670638486888746277, -1.589497524861957611, 1.246053474203263178 ) ) ;
#105750=CARTESIAN_POINT ( 'NONE',  ( 0.7202740732663616141, -1.155732025818452913, -1.826486478054230256 ) ) ;
#105753=CARTESIAN_POINT ( 'NONE',  ( 6.925078400183556582, 1.261064080992575498, 2.068696352333323052 ) ) ;
#105757=CARTESIAN_POINT ( 'NONE',  ( 6.034388706570055660, 0.6371486477873434806, 1.913263546360920220 ) ) ;
#105760=CARTESIAN_POINT ( 'NONE',  ( 0.02921319935947005314, -2.001080581411585513, 0.8940957790435491992 ) ) ;
#105762=CARTESIAN_POINT ( 'NONE',  ( 0.2689492781585648418, -1.474829822998312778, 1.715830925988118816 ) ) ;
#105766=CARTESIAN_POINT ( 'NONE',  ( 1.124461781556247431, 0.3751114458506888405, 1.878329865892948813 ) ) ;
#105770=CARTESIAN_POINT ( 'NONE',  ( 2.613528241349000858, -1.706151288242565567, 0.2525731233022251443 ) ) ;
#105772=CARTESIAN_POINT ( 'NONE',  ( 2.512676673363742452, 1.578732364194649573, 0.7999210992828114097 ) ) ;
#105773=CARTESIAN_POINT ( 'NONE',  ( 2.947904902976675068, -1.353543519239216897, -1.490266562291961749 ) ) ;
#105775=CARTESIAN_POINT ( 'NONE',  ( 5.544034191846948900, 0.8990280053539388971, -2.015528879820461583 ) ) ;
#105778=CARTESIAN_POINT ( 'NONE',  ( 4.025652601906283046, -0.3410878217046057204, 1.990599050954243054 ) ) ;
#105780=CARTESIAN_POINT ( 'NONE',  ( 4.160867320283115234, 0.5667376361006767338, 2.043264482828925033 ) ) ;
#105781=CARTESIAN_POINT ( 'NONE',  ( 4.235953958900400274, 2.015913684659226490, -0.05231418598541925924 ) ) ;
#105782=CARTESIAN_POINT ( 'NONE',  ( 4.201270403262004294, 1.615401881959299235, -0.8201500932763347018 ) ) ;
#105786=CARTESIAN_POINT ( 'NONE',  ( 1.463515404423965105, 1.843522461416190250, -0.3164952454337774390 ) ) ;
#105788=CARTESIAN_POINT ( 'NONE',  ( 6.234996492879100849, 1.692908850720629799, 0.6451080659017217611 ) ) ;
#105799=CARTESIAN_POINT ( 'NONE',  ( 4.166350089634453191, 2.120059694336435374, -0.05518752902338577848 ) ) ;
#105802=CARTESIAN_POINT ( 'NONE',  ( 5.571542166969843279, 1.900665388187183114, -0.5230325980125193341 ) ) ;
#105804=CARTESIAN_POINT ( 'NONE',  ( 1.090090997392887173, 1.202455520763350272, 1.614487003566661638 ) ) ;
#105806=CARTESIAN_POINT ( 'NONE',  ( 0.2107725088618967457, 2.027540257690120029, 0.6097772466436711669 ) ) ;
#105808=CARTESIAN_POINT ( 'NONE',  ( 1.785682506433339478, -1.950172559450613852, 0.6955597780969878796 ) ) ;
#105811=CARTESIAN_POINT ( 'NONE',  ( 4.259774723613071856, 0.9852665271268057356, 1.843911019796584450 ) ) ;
#105814=CARTESIAN_POINT ( 'NONE',  ( 2.783998052563033010, -0.9402290988879957734, 1.564698673013890984 ) ) ;
#105815=CARTESIAN_POINT ( 'NONE',  ( 2.121461778293322276, -0.3959642608444019496, 1.767488790605805438 ) ) ;
#105819=CARTESIAN_POINT ( 'NONE',  ( 3.979664642534729513, 2.078844338038158934, -0.7408291028327751437 ) ) ;
#105822=CARTESIAN_POINT ( 'NONE',  ( 3.000541214264150547, -1.884352459892328024, -0.3246530749497905655 ) ) ;
#105824=CARTESIAN_POINT ( 'NONE',  ( 6.830528382861658088, -1.277203763263988101, 1.630111558092485868 ) ) ;
#105826=CARTESIAN_POINT ( 'NONE',  ( 5.952700804540857149, -1.878875186057769486, -1.127905468421293689 ) ) ;
#105833=CARTESIAN_POINT ( 'NONE',  ( -0.2409995289980246258, 2.020898751655671788, -2.415740196953279462 ) ) ;
#105836=CARTESIAN_POINT ( 'NONE',  ( 5.366107254901440804, -2.060797467674013284, 0.1973761227843511823 ) ) ;
#105837=CARTESIAN_POINT ( 'NONE',  ( 4.494702926938664689, -0.4234472454235098104, -1.879237243589318318 ) ) ;
#105838=CARTESIAN_POINT ( 'NONE',  ( 0.5972800738224989248, -0.2930464221381040013, 1.994874516246990748 ) ) ;
#105842=CARTESIAN_POINT ( 'NONE',  ( 1.535386672163775668, -1.589036399888818618, -1.509351277865833563 ) ) ;
#105843=CARTESIAN_POINT ( 'NONE',  ( 5.250558533952181861, 0.5335417292645014964, 1.745990657226546894 ) ) ;
#105852=CARTESIAN_POINT ( 'NONE',  ( 2.893917256732419396, -0.5369380550670297403, -1.761199466696103499 ) ) ;
#105853=CARTESIAN_POINT ( 'NONE',  ( -0.02280469861281903335, -1.799075986276091887, -0.9034098368623093567 ) ) ;
#105854=CARTESIAN_POINT ( 'NONE',  ( 2.109147326763362695, 0.8800818102412102384, -2.123382460422203355 ) ) ;
#105856=CARTESIAN_POINT ( 'NONE',  ( 6.385602409055195494, -1.848352663145738095, 0.6577735930803210174 ) ) ;
#105859=CARTESIAN_POINT ( 'NONE',  ( 3.076317393561965208, 0.8638369986560844316, 1.706277067364105893 ) ) ;
#105861=CARTESIAN_POINT ( 'NONE',  ( 0.3970419974134197783, 0.3524218036512065111, 2.039982198586967943 ) ) ;
#105863=CARTESIAN_POINT ( 'NONE',  ( 2.876600747729184615, -0.1562720264073799992, -2.084980456524800019 ) ) ;
#105864=CARTESIAN_POINT ( 'NONE',  ( 0.9888773766892227091, 1.651582696977689890, -0.8784067438419729257 ) ) ;
#105865=CARTESIAN_POINT ( 'NONE',  ( 2.389999771189327937, -0.002812746694069029330, 2.016288306988550438 ) ) ;
#105869=CARTESIAN_POINT ( 'NONE',  ( 3.192619200838729743, 1.373927285412982036, 1.068286041690246657 ) ) ;
#105873=CARTESIAN_POINT ( 'NONE',  ( 2.543205433794017978, -1.277680944696883092, -1.158960206811429750 ) ) ;
#105874=CARTESIAN_POINT ( 'NONE',  ( 2.665787806004877414, 1.174844384069907655, 1.849873475113596566 ) ) ;
#105875=CARTESIAN_POINT ( 'NONE',  ( 0.03525962724756306205, -1.394606873943932346, 1.030409205853829668 ) ) ;
#105876=CARTESIAN_POINT ( 'NONE',  ( 5.004599478379411437, -0.7411955310945415043, -2.078817424605138964 ) ) ;
#105879=CARTESIAN_POINT ( 'NONE',  ( 3.133805249272236804, 2.063032676455050396, -0.6766426178266419234 ) ) ;
#105880=CARTESIAN_POINT ( 'NONE',  ( 2.174178736149934732, -1.123764393468742684, 1.438770255985911684 ) ) ;
#105882=CARTESIAN_POINT ( 'NONE',  ( 4.030539441936417333, 0.5683090829115284848, 2.039553408600587758 ) ) ;
#105883=CARTESIAN_POINT ( 'NONE',  ( 6.539320575229228716, 1.281788455817688188, 2.013036689384885225 ) ) ;
#105885=CARTESIAN_POINT ( 'NONE',  ( 5.056304237002312796, -1.661761009075436002, 1.579303468685322009 ) ) ;
#105889=CARTESIAN_POINT ( 'NONE',  ( 0.01256502854718108061, -2.120115106878577294, -0.04748564598491820943 ) ) ;
#105895=AXIS2_PLACEMENT_3D ( 'NONE', #172290, #207963, #72635 ) ;
#105896=ORIENTED_EDGE ( 'NONE', *, *, #123967, .F. ) ;
#105897=CARTESIAN_POINT ( 'NONE',  ( 5.221327349844218091, 1.987046161919112430, 0.3419379449052239450 ) ) ;
#105899=CARTESIAN_POINT ( 'NONE',  ( 3.467685518289661317, -0.4070155273973393717, 2.021854410566482407 ) ) ;
#105901=CARTESIAN_POINT ( 'NONE',  ( -0.1408020194050510487, 6.947782644136224484, -2.695327183700791274 ) ) ;
#105905=CARTESIAN_POINT ( 'NONE',  ( 6.140607899229072686, -1.853288307406484758, 1.169240172944140621 ) ) ;
#105906=CARTESIAN_POINT ( 'NONE',  ( 3.340470361411255418, 0.4872029778183216697, -1.956561305313428978 ) ) ;
#105907=CARTESIAN_POINT ( 'NONE',  ( 3.579498943475650563, -0.9044721095569520086, 1.603693017070174864 ) ) ;
#105911=CARTESIAN_POINT ( 'NONE',  ( 0.7797844759148920835, -0.9637546898726162548, 1.430169641563599159 ) ) ;
#105912=CARTESIAN_POINT ( 'NONE',  ( 0.2121463357745425049, 2.202340261784305753, 0.6586529460593565366 ) ) ;
#105914=CARTESIAN_POINT ( 'NONE',  ( 6.596538519236475828, -0.5955016034951933213, -2.182694285642503562 ) ) ;
#105915=CARTESIAN_POINT ( 'NONE',  ( 1.699976503534783356, -0.7083771898081425711, 1.983499743616623956 ) ) ;
#105925=CARTESIAN_POINT ( 'NONE',  ( 2.162495577681341707, 2.120227376586072854, 0.04728746717985036346 ) ) ;
#105926=CARTESIAN_POINT ( 'NONE',  ( 4.148835382215973588, 2.178989060337086503, 0.4312644480095380040 ) ) ;
#105927=CARTESIAN_POINT ( 'NONE',  ( 2.133021248740565756, -1.956732443736847182, 0.9868821405488172882 ) ) ;
#105929=CARTESIAN_POINT ( 'NONE',  ( 6.883263157960364254, 2.447565407927353220, 2.329071302269662080 ) ) ;
#105931=CARTESIAN_POINT ( 'NONE',  ( 5.019951445752288244, 1.940773837913706057, -0.2859759768028962146 ) ) ;
#105932=DIRECTION ( 'NONE',  ( 1.040834085586084257E-15, 1.000000000000000000, -4.622230424712076367E-32 ) ) ;
#105934=CARTESIAN_POINT ( 'NONE',  ( 6.610000000000018083, 6.039292104641935666, 2.314898989754467618 ) ) ;
#105937=CARTESIAN_POINT ( 'NONE',  ( 4.131183091185314460, 1.940096312829143299, 0.8565103500411813675 ) ) ;
#105940=CARTESIAN_POINT ( 'NONE',  ( 5.752838164830007983, -1.706859214253673152, 1.326403591387192771 ) ) ;
#105942=CARTESIAN_POINT ( 'NONE',  ( 5.319803798718575116, 1.092037692397327620, -1.482314076171886708 ) ) ;
#105945=CARTESIAN_POINT ( 'NONE',  ( 0.01074006189176902708, -1.707493591921129372, 0.3360247309564004525 ) ) ;
#105946=CARTESIAN_POINT ( 'NONE',  ( 6.727182134110222478, 0.005875948494733079785, 1.810970247402940547 ) ) ;
#105949=CARTESIAN_POINT ( 'NONE',  ( 4.487301133948972343, 1.932317252032596633, -0.9692046190768679459 ) ) ;
#105952=CARTESIAN_POINT ( 'NONE',  ( 6.397814513887354337, 0.1948139983735352188, 2.006652364629394114 ) ) ;
#105954=CARTESIAN_POINT ( 'NONE',  ( 3.028364643526501698, 1.202066397148596977, -1.796461956351296019 ) ) ;
#105955=CARTESIAN_POINT ( 'NONE',  ( 4.376219360443936779, -1.137518282590570751, 1.609873005976544924 ) ) ;
#105956=CARTESIAN_POINT ( 'NONE',  ( 4.147546876296400065, -0.1688817038796013026, -1.725555368340276008 ) ) ;
#105957=CARTESIAN_POINT ( 'NONE',  ( 0.3104468679729632807, 1.506874830639578056, -1.591553791636945991 ) ) ;
#105958=CARTESIAN_POINT ( 'NONE',  ( 1.290513193724596164, -1.035378025537621927, 2.062353807931560645 ) ) ;
#105959=CARTESIAN_POINT ( 'NONE',  ( 3.532544388643095612, 2.009728383178956523, 0.4550750861811359571 ) ) ;
#105960=CARTESIAN_POINT ( 'NONE',  ( 5.794467663293456638, 1.585267558806532362, -1.121583357746269050 ) ) ;
#105970=CARTESIAN_POINT ( 'NONE',  ( 3.012930935654754450, 1.599341701681813444, -1.520756135150652222 ) ) ;
#105973=CARTESIAN_POINT ( 'NONE',  ( 1.252544054828262476, -0.4453625992760417707, -1.806759803163625167 ) ) ;
#105974=CARTESIAN_POINT ( 'NONE',  ( -0.02900071798683095947, 1.997299723774683455, -2.587491137808914488 ) ) ;
#105979=CARTESIAN_POINT ( 'NONE',  ( 6.140549721451361798, -1.552764191669778304, 0.9890077265983505672 ) ) ;
#105981=CARTESIAN_POINT ( 'NONE',  ( 2.254824865002862389, -1.593768082018555354, 1.306595953347834849 ) ) ;
#105989=CARTESIAN_POINT ( 'NONE',  ( 0.5497720567373615141, 0.6472090466588500401, -1.956683156177397853 ) ) ;
#105991=CARTESIAN_POINT ( 'NONE',  ( 5.126429434416579056, 0.1410513515392505246, 1.835921608166577013 ) ) ;
#105995=CARTESIAN_POINT ( 'NONE',  ( 4.635508124736155366, -2.018492079602551392, 0.8926152185086615454 ) ) ;
#105996=CARTESIAN_POINT ( 'NONE',  ( 6.889870058830950938, -0.9756824853745720283, 2.038933460117636542 ) ) ;
#105998=CARTESIAN_POINT ( 'NONE',  ( 0.5801457039020865292, 0.9447208859736742070, 1.662703529197881558 ) ) ;
#105999=CARTESIAN_POINT ( 'NONE',  ( 1.024625454658374624, 0.3981145430279106057, 1.976669095394629982 ) ) ;
#106001=CARTESIAN_POINT ( 'NONE',  ( 1.388484499181727561, -0.05552238045265603383, 2.297868740670248044 ) ) ;
#106002=CARTESIAN_POINT ( 'NONE',  ( 6.754772315933175619, -1.444328698515121800, 1.188528157999017454 ) ) ;
#106005=CARTESIAN_POINT ( 'NONE',  ( 1.322894217037654085, -0.04941562205608432401, 1.870173573632450958 ) ) ;
#106006=CARTESIAN_POINT ( 'NONE',  ( 2.307827663788959871, -1.164988201124015577, -1.645758576239789051 ) ) ;
#106008=CARTESIAN_POINT ( 'NONE',  ( 6.639320575229257670, 4.691717626494606996, 2.665852771288126366 ) ) ;
#106010=CARTESIAN_POINT ( 'NONE',  ( 4.793641967770590817, 1.559994068796449529, 1.415095702743226047 ) ) ;
#106014=B_SPLINE_CURVE_WITH_KNOTS ( 'NONE', 3,
 ( #54958, #146352, #196146, #33629, #213425, #65047, #131204, #212364, #179895, #164701, #30452 ),
 .UNSPECIFIED., .F., .F.,
 ( 4, 1, 1, 1, 1, 1, 1, 1, 4 ),
 ( 0.000000000000000000, 0.2256085737580844630, 0.3975982043691296264, 0.5251069566405043298, 0.6172860083021659561, 0.6832860984239963464, 0.7321959383537668398, 0.7728624839797392232, 1.000000000000000000 ),
 .UNSPECIFIED. ) ;
#106016=CARTESIAN_POINT ( 'NONE',  ( 3.972919405334675691, -1.493746422221740699, 1.359666112553897355 ) ) ;
#106018=CARTESIAN_POINT ( 'NONE',  ( 6.303195905902406970, -1.744534168554587872, 1.100284471152054300 ) ) ;
#106020=CARTESIAN_POINT ( 'NONE',  ( 4.763041337456088264, -1.928505312680216743, -0.9765951867335492809 ) ) ;
#106025=CARTESIAN_POINT ( 'NONE',  ( 2.348295082997472250, -0.9299805079447539535, 1.962071136543291683 ) ) ;
#106028=CARTESIAN_POINT ( 'NONE',  ( 1.417261839328866513, -1.023339270300478221, -1.530466495063505628 ) ) ;
#106030=CARTESIAN_POINT ( 'NONE',  ( 3.105210138592546798, -0.4252477525170209605, 2.149737936336936883 ) ) ;
#106031=CARTESIAN_POINT ( 'NONE',  ( 6.983263157960330147, 2.017328405816510628, 2.456467998350126525 ) ) ;
#106032=CARTESIAN_POINT ( 'NONE',  ( 4.206154751832458238, -2.256696944984788011, 0.1629611055770207317 ) ) ;
#106038=CARTESIAN_POINT ( 'NONE',  ( 5.219873587733063758, -0.9469346145933134062, -1.494860035008038324 ) ) ;
#106040=CARTESIAN_POINT ( 'NONE',  ( 2.397617287051221791, 1.627147360716905800, 1.336933552532795222 ) ) ;
#106043=CARTESIAN_POINT ( 'NONE',  ( 1.082395645157930852, 1.176005852300557653, -1.579744537442813401 ) ) ;
#106045=CARTESIAN_POINT ( 'NONE',  ( 0.3968290921660848070, 0.3316028935436679537, 1.933473477243151439 ) ) ;
#106046=CARTESIAN_POINT ( 'NONE',  ( 5.379120748016958053, -1.641329381114923658, -0.7670206631310432233 ) ) ;
#106050=CARTESIAN_POINT ( 'NONE',  ( 5.049604242677836474, 0.5861553263475408615, -1.776501995420045610 ) ) ;
#106052=CARTESIAN_POINT ( 'NONE',  ( 4.821179601816666604, -1.846891146645711412, -0.9356023351853595127 ) ) ;
#106063=CARTESIAN_POINT ( 'NONE',  ( 5.389097038490845648, 0.1425914310585977562, 1.956722230749983193 ) ) ;
#106065=CARTESIAN_POINT ( 'NONE',  ( 1.915388525686153143, 0.6297767875703685903, 1.915307412907449436 ) ) ;
#106067=CARTESIAN_POINT ( 'NONE',  ( 0.1346727191937693857, 0.3808678606769915209, 2.158067550307264604 ) ) ;
#106069=CARTESIAN_POINT ( 'NONE',  ( 2.266681450017640653, -1.708379500633325998, -0.7622673669660309237 ) ) ;
#106071=CARTESIAN_POINT ( 'NONE',  ( 3.674091251731440355, 1.997487462777279621, -0.2507888908306437625 ) ) ;
#106074=CARTESIAN_POINT ( 'NONE',  ( 3.234098929720787385, 2.117403153491578927, -0.002560228748609005411 ) ) ;
#106075=CARTESIAN_POINT ( 'NONE',  ( 6.825078400183575589, -0.005632053428735600553, 2.144262460745151255 ) ) ;
#106076=CARTESIAN_POINT ( 'NONE',  ( 5.178213324540339002, -1.104578422852561914, -1.750899486206449751 ) ) ;
#106078=CARTESIAN_POINT ( 'NONE',  ( 0.8727377898805768197, -0.05501089605610678251, -2.090203850258448792 ) ) ;
#106079=CARTESIAN_POINT ( 'NONE',  ( 6.720655732516649827, 0.5759399164693942419, 2.126764875236677454 ) ) ;
#106080=CARTESIAN_POINT ( 'NONE',  ( 0.07661050522433668353, 0.008287133257128471639, -1.710863442170395432 ) ) ;
#106088=CARTESIAN_POINT ( 'NONE',  ( 6.199862383955294654, 1.322219258337012704, 1.381733411008022383 ) ) ;
#106096=EDGE_CURVE ( 'NONE', #95583, #68014, #127461, .T. ) ;
#106097=CARTESIAN_POINT ( 'NONE',  ( 6.603150281434943203, -0.1430492952050037847, 1.984088717376513822 ) ) ;
#106100=CARTESIAN_POINT ( 'NONE',  ( 0.1399997263886020860, 0.7221123407896400392, -2.083281383436136558 ) ) ;
#106103=CARTESIAN_POINT ( 'NONE',  ( 3.625798818847306038, 1.922417080405220968, -0.4270903664440502956 ) ) ;
#106104=CARTESIAN_POINT ( 'NONE',  ( 4.534779904478015489, -1.617806963314952773, 1.203370736114671269 ) ) ;
#106108=CARTESIAN_POINT ( 'NONE',  ( 4.664136352776428573, -1.432711980460563250, 1.658340198327029613 ) ) ;
#106110=CARTESIAN_POINT ( 'NONE',  ( 3.293886989636186868, -0.7820812614263569218, 1.760672275598859748 ) ) ;
#106112=CARTESIAN_POINT ( 'NONE',  ( -0.02988540731103071432, 7.629137130509069387, -2.326318838967501357 ) ) ;
#106113=CARTESIAN_POINT ( 'NONE',  ( 0.1331565106231363538, 2.033293680964400885, -2.362282156872722805 ) ) ;
#106120=CARTESIAN_POINT ( 'NONE',  ( 6.603072989126265391, -0.3962418105841297722, 1.804722624154910360 ) ) ;
#106121=CARTESIAN_POINT ( 'NONE',  ( 2.736979112881072762, 1.896321534115693819, 0.6760404272549996874 ) ) ;
#106122=CARTESIAN_POINT ( 'NONE',  ( 4.956595877991936128, 1.698763664877179780, 1.548309420705455741 ) ) ;
#106124=CARTESIAN_POINT ( 'NONE',  ( 3.221387034570993624, 0.2776250501920934921, -1.840009301959115051 ) ) ;
#106126=CARTESIAN_POINT ( 'NONE',  ( 0.02755585400013305097, 7.629137130509076492, -2.789001785468494976 ) ) ;
#106127=CARTESIAN_POINT ( 'NONE',  ( 6.539320575229249144, 0.007148032025052972194, 1.896977914940492393 ) ) ;
#106130=CARTESIAN_POINT ( 'NONE',  ( 6.480031082513550089, -2.050496881725831777, -0.4073240614407472315 ) ) ;
#106135=CARTESIAN_POINT ( 'NONE',  ( 6.709587848829112744, -0.3662258548819911086, 1.691549535187387932 ) ) ;
#106137=CARTESIAN_POINT ( 'NONE',  ( 2.320625381698769640, 0.8157257908444032202, -1.530271591396751729 ) ) ;
#106142=CARTESIAN_POINT ( 'NONE',  ( 6.948074912775242140, -0.9353680688231647000, 1.957065181168372581 ) ) ;
#106143=CARTESIAN_POINT ( 'NONE',  ( 5.883392091387671385, 1.685093539698417242, -0.7030590484573000509 ) ) ;
#106144=CARTESIAN_POINT ( 'NONE',  ( 3.256644689873238629, -0.5649923015349536115, -1.878667693404307171 ) ) ;
#106148=CARTESIAN_POINT ( 'NONE',  ( 3.528090983593739516, -2.088826311502915090, 0.3641918842257965139 ) ) ;
#106151=CARTESIAN_POINT ( 'NONE',  ( 1.709917326824461181, 0.6048241955843024487, -1.979901091156407666 ) ) ;
#106154=CARTESIAN_POINT ( 'NONE',  ( 4.987093027905733500, -2.091254775410257061, -0.7492775906185499268 ) ) ;
#106156=CARTESIAN_POINT ( 'NONE',  ( 1.530362799304554100, -1.938799508460651522, 1.234721073783265233 ) ) ;
#106158=CARTESIAN_POINT ( 'NONE',  ( 6.368047018367568590, -2.047660648193879496, 0.2468551644246498589 ) ) ;
#106162=CARTESIAN_POINT ( 'NONE',  ( 6.163598723784101452, 0.9525508894225950263, 1.575581956637741587 ) ) ;
#106164=CARTESIAN_POINT ( 'NONE',  ( 2.900541297466651347, -1.884798985816903860, -0.3226963764228693576 ) ) ;
#106165=FACE_OUTER_BOUND ( 'NONE', #156477, .T. ) ;
#106166=CARTESIAN_POINT ( 'NONE',  ( 3.891373129206575410, 1.249378432800802852, 1.189308452707043884 ) ) ;
#106167=CARTESIAN_POINT ( 'NONE',  ( 2.676970549635893537, 1.727063564601112100, -1.040793759654296213 ) ) ;
#106168=CARTESIAN_POINT ( 'NONE',  ( 4.412867445986612402, -1.413514171388057239, -1.812631114537610166 ) ) ;
#106169=( BOUNDED_CURVE ( )  B_SPLINE_CURVE ( 3, ( #124109, #24352, #88319, #156528 ),
 .UNSPECIFIED., .F., .T. ) 
 B_SPLINE_CURVE_WITH_KNOTS ( ( 4, 4 ),
 ( 0.000000000000000000, 0.5000000000000005551 ),
 .UNSPECIFIED. ) 
 CURVE ( )  GEOMETRIC_REPRESENTATION_ITEM ( )  RATIONAL_B_SPLINE_CURVE ( ( 1.000000000000000222, 0.3333333333333327042, 0.3333333333333334259, 1.000000000000000888 ) ) 
 REPRESENTATION_ITEM ( '' )  );
#106170=CARTESIAN_POINT ( 'NONE',  ( 3.708526512723071544, -0.9128432734063509635, -2.070237398927244676 ) ) ;
#106171=CARTESIAN_POINT ( 'NONE',  ( 5.953767555512091469, 0.6130212357637642162, -2.014879775860946687 ) ) ;
#106173=CARTESIAN_POINT ( 'NONE',  ( 5.044116495868207650, 1.765035602982415242, 0.1300806658623629153 ) ) ;
#106176=CARTESIAN_POINT ( 'NONE',  ( 1.096115288130569798, -2.292435215939184534, 0.004638672314880368241 ) ) ;
#106177=CARTESIAN_POINT ( 'NONE',  ( 5.683513393433289096, -0.8240744568873883402, 1.646495476055845231 ) ) ;
#106180=CARTESIAN_POINT ( 'NONE',  ( 6.281208295753298643, 1.508423295503196648, 1.589913042345507455 ) ) ;
#106184=CARTESIAN_POINT ( 'NONE',  ( 5.775854211382815073, -2.020734006234246927, 0.4499205674863211990 ) ) ;
#106185=CARTESIAN_POINT ( 'NONE',  ( 0.5324358445358172709, 0.5899921999869184308, 1.928256190492839028 ) ) ;
#106187=CARTESIAN_POINT ( 'NONE',  ( 4.301339506872517759, 1.548173799611574530, 1.146357790588454106 ) ) ;
#106190=CARTESIAN_POINT ( 'NONE',  ( 1.723182734256373916, 1.642088205692782132, -1.496221191757711066 ) ) ;
#106198=CARTESIAN_POINT ( 'NONE',  ( 1.715213470010600538, -1.680963409367957295, -1.011360081469035999 ) ) ;
#106202=CARTESIAN_POINT ( 'NONE',  ( 6.215287892896892430, -1.681934637451238279, -1.009743211781432670 ) ) ;
#106206=CARTESIAN_POINT ( 'NONE',  ( 0.3216218905449366172, -0.1073394912241855820, 2.260102045549317928 ) ) ;
#106210=CARTESIAN_POINT ( 'NONE',  ( 1.405301488743180061, -0.4598193086536165319, 1.813012767170335993 ) ) ;
#106211=CARTESIAN_POINT ( 'NONE',  ( 0.5274301605363295176, -1.488642097782297835, 0.8892331099567828412 ) ) ;
#106213=CARTESIAN_POINT ( 'NONE',  ( 4.669572502782517454, 1.262004115398765780, 1.791526714441132873 ) ) ;
#106214=CARTESIAN_POINT ( 'NONE',  ( 4.014917937017292715, 1.634369553669342778, -1.629294119824703069 ) ) ;
#106215=CARTESIAN_POINT ( 'NONE',  ( 0.3212574623711033639, -0.1015677953285927942, 2.058520922655207031 ) ) ;
#106216=CARTESIAN_POINT ( 'NONE',  ( 2.677597413788167735, -0.9980636400313472878, 1.665709379616100883 ) ) ;
#106219=CARTESIAN_POINT ( 'NONE',  ( 5.660427296577901224, 2.118236611397010805, 0.1021076702828054988 ) ) ;
#106221=CARTESIAN_POINT ( 'NONE',  ( 4.026017654026761150, -1.753031021560845559, 0.9963007555989014108 ) ) ;
#106225=CARTESIAN_POINT ( 'NONE',  ( 0.5744775230259161480, -1.718042477583326066, -0.6180270036199516648 ) ) ;
#106230=CARTESIAN_POINT ( 'NONE',  ( 5.102442524761234388, -0.6923759778164092493, -1.941246359495584883 ) ) ;
#106232=ADVANCED_FACE ( 'NONE', ( #114632 ), #81465, .T. ) ;
#106235=CARTESIAN_POINT ( 'NONE',  ( 6.235022398275627431, 1.885252722396244085, 0.7250032809389771460 ) ) ;
#106236=CARTESIAN_POINT ( 'NONE',  ( 6.059279899546098136, -1.878006040282210298, 1.186031488430500769 ) ) ;
#106240=CARTESIAN_POINT ( 'NONE',  ( 4.364173291480280881, 0.9696465702416400267, 1.818514982836361593 ) ) ;
#106241=CARTESIAN_POINT ( 'NONE',  ( 3.481092415823695774, -2.014232707597499505, -0.09613569647320965861 ) ) ;
#106250=CARTESIAN_POINT ( 'NONE',  ( 4.218124927476913477, -1.674631575811252215, -1.122325875776951420 ) ) ;
#106251=CARTESIAN_POINT ( 'NONE',  ( 3.345483972246702020, 1.841320589717788447, -0.001054884335952021917 ) ) ;
#106253=CARTESIAN_POINT ( 'NONE',  ( 1.524504908422112726, -1.285150704446396341, -1.916548379014111791 ) ) ;
#106255=CARTESIAN_POINT ( 'NONE',  ( 3.620547430246877862, 1.374377816306590727, -1.668374205817772182 ) ) ;
#106259=CARTESIAN_POINT ( 'NONE',  ( 3.181363629901075463, -1.130666556857576444, -2.000962643106804606 ) ) ;
#106261=CARTESIAN_POINT ( 'NONE',  ( 2.746779440450992649, -1.556306552617524597, 1.037596984913228937 ) ) ;
#106263=CARTESIAN_POINT ( 'NONE',  ( 6.526250059115050739, 1.135311405967744935, -1.611567521105742751 ) ) ;
#106267=CARTESIAN_POINT ( 'NONE',  ( 1.401302286655212948, 1.802556353783949517, -1.272968949304439379 ) ) ;
#106273=CARTESIAN_POINT ( 'NONE',  ( 6.227413254736037906, -1.856526228437559434, 0.6636957074077839414 ) ) ;
#106274=CARTESIAN_POINT ( 'NONE',  ( 6.059233210108489587, -1.975957287588899769, -1.191867793525339669 ) ) ;
#106275=CARTESIAN_POINT ( 'NONE',  ( 0.3265133270617843197, -1.284392789319420913, 1.483054880892266114 ) ) ;
#106276=CARTESIAN_POINT ( 'NONE',  ( 3.080982041725123910, 1.940567726598545040, 0.6991345639211270502 ) ) ;
#106283=CARTESIAN_POINT ( 'NONE',  ( 5.371592247264787900, -0.3238957681546798528, 2.146784808600268324 ) ) ;
#106285=CARTESIAN_POINT ( 'NONE',  ( 5.161589042655139181, 0.9124512986629171873, 1.599201395118980740 ) ) ;
#106289=CARTESIAN_POINT ( 'NONE',  ( 0.6845637836509765872, -0.2226890396202323152, -1.857165095135074218 ) ) ;
#106290=CARTESIAN_POINT ( 'NONE',  ( 0.4568015506021270156, 0.8674211623492070755, 2.089700042804636837 ) ) ;
#106296=CARTESIAN_POINT ( 'NONE',  ( 2.307162891426073337, -0.3907249415124186553, 1.725993255813297989 ) ) ;
#106297=CARTESIAN_POINT ( 'NONE',  ( 6.199863759850236633, 1.389832719217662049, 1.456544111691231658 ) ) ;
#106299=CARTESIAN_POINT ( 'NONE',  ( 3.409697593026795204, -1.143712931967875601, -1.536527803759838662 ) ) ;
#106300=CARTESIAN_POINT ( 'NONE',  ( 4.017982430692658369, 1.954955499905395522, -0.2386041268068790633 ) ) ;
#106301=CARTESIAN_POINT ( 'NONE',  ( 6.504167520383483669, -0.8605252283936345448, 1.825738368183300153 ) ) ;
#106303=CARTESIAN_POINT ( 'NONE',  ( 2.588565208901713266, -0.3177388942022137397, -1.843305967786903032 ) ) ;
#106304=CARTESIAN_POINT ( 'NONE',  ( 6.111878173048258311, -1.710926958338830017, 0.2183984861162356628 ) ) ;
#106306=CARTESIAN_POINT ( 'NONE',  ( 2.403190426070573871, 1.771669130372434564, -1.315670724662293178 ) ) ;
#106309=CARTESIAN_POINT ( 'NONE',  ( 6.197705743426439540, -1.420020466879829302, -1.353909852041992767 ) ) ;
#106316=CARTESIAN_POINT ( 'NONE',  ( 2.031770498437397876, 1.981864486777328294, -0.5989037013024376410 ) ) ;
#106320=CARTESIAN_POINT ( 'NONE',  ( 0.9791725360285336022, -1.826886329348556881, -0.8614179918085950183 ) ) ;
#106323=CARTESIAN_POINT ( 'NONE',  ( 0.07459516483345089710, 7.629137130509094256, -2.355503875070711572 ) ) ;
#106325=CARTESIAN_POINT ( 'NONE',  ( 5.782577320554741718, -1.967585831723076772, 0.4389650999883643046 ) ) ;
#106326=CARTESIAN_POINT ( 'NONE',  ( 5.665228803577522676, 1.767359255132592066, -0.7397141715129780248 ) ) ;
#106327=CARTESIAN_POINT ( 'NONE',  ( 6.639320575229223031, 6.036153810275548537, 2.598155902862766542 ) ) ;
#106328=CARTESIAN_POINT ( 'NONE',  ( 4.019203527901527018, -2.096847714747759106, 0.6372333828079318474 ) ) ;
#106332=CARTESIAN_POINT ( 'NONE',  ( 2.425908952446104827, -1.891012092455180760, 0.2844710172774585488 ) ) ;
#106336=CARTESIAN_POINT ( 'NONE',  ( -0.1351500440973339712, -0.1486198258836557429, -1.983738523497140305 ) ) ;
#106338=CARTESIAN_POINT ( 'NONE',  ( 6.128506746050899068, 0.2130254606748181456, 2.181202035047181020 ) ) ;
#106340=CARTESIAN_POINT ( 'NONE',  ( 2.484998412088899489, 1.578176246201369093, -0.6962595882179720697 ) ) ;
#106342=CARTESIAN_POINT ( 'NONE',  ( 5.959260761812961604, -1.790568634313693730, 1.135864312162476297 ) ) ;
#106346=CARTESIAN_POINT ( 'NONE',  ( 0.4319881149899909567, 1.126445828788334991, 1.606065282034954578 ) ) ;
#106353=CARTESIAN_POINT ( 'NONE',  ( 2.578518618993036693, -1.248033014721174228, 1.313194663545588003 ) ) ;
#106357=CARTESIAN_POINT ( 'NONE',  ( 4.002463340116116264, -1.792309675113772371, -0.2618007260343068743 ) ) ;
#106361=CARTESIAN_POINT ( 'NONE',  ( 4.984723811273123140, 1.780707155018296239, 0.5408319247705763999 ) ) ;
#106363=CARTESIAN_POINT ( 'NONE',  ( 2.249496223418820939, 1.878159554852454338, -0.3759676508649934523 ) ) ;
#106364=CARTESIAN_POINT ( 'NONE',  ( 1.166719304534512558, -1.648536928579244165, -0.7845717211837843763 ) ) ;
#106374=CARTESIAN_POINT ( 'NONE',  ( 1.218821504741087969, -0.04963993015681333193, 2.090216850290891326 ) ) ;
#106375=CARTESIAN_POINT ( 'NONE',  ( 0.07680821025393690105, 0.005952109439256307241, -1.810863387344714193 ) ) ;
#106377=CARTESIAN_POINT ( 'NONE',  ( 2.977373796215292856, 1.734057503958493118, -0.5710112477543202170 ) ) ;
#106378=CARTESIAN_POINT ( 'NONE',  ( 3.071135375186518690, -2.039199700013223815, -0.8442704067812345503 ) ) ;
#106380=CARTESIAN_POINT ( 'NONE',  ( 1.125099709691119276, 1.687896996356451629, 0.8989547360247207575 ) ) ;
#106381=CARTESIAN_POINT ( 'NONE',  ( 1.117558341675929157, 0.3875481960372212931, -1.930861576554385062 ) ) ;
#106382=CARTESIAN_POINT ( 'NONE',  ( 4.247558953154553230, 1.941557341479711152, -0.05109960196620494388 ) ) ;
#106386=CARTESIAN_POINT ( 'NONE',  ( 6.895359103435129811, -1.662453150013998515, 0.8363214020891978073 ) ) ;
#106391=CARTESIAN_POINT ( 'NONE',  ( 2.771223791512751333, 2.080116120148074010, -0.6901165687889164735 ) ) ;
#106395=CARTESIAN_POINT ( 'NONE',  ( 3.721172816245840842, -0.1328194893376876962, 1.820914920514608459 ) ) ;
#106399=CARTESIAN_POINT ( 'NONE',  ( -0.02968770228140017037, 2.049257630910449990, -2.243713227073070637 ) ) ;
#106400=CARTESIAN_POINT ( 'NONE',  ( 4.733189744967194024, -1.710186631362722531, 0.7584244158565585092 ) ) ;
#106402=CARTESIAN_POINT ( 'NONE',  ( 1.752441099931791868, 0.6037874858934308975, 1.829501483119711169 ) ) ;
#106404=CARTESIAN_POINT ( 'NONE',  ( 6.332860960579021814, -1.861707940517230764, -0.6185968553879470644 ) ) ;
#106410=CARTESIAN_POINT ( 'NONE',  ( -0.1349523647116790404, -0.1509472049114955194, -2.083628827036696052 ) ) ;
#106414=CARTESIAN_POINT ( 'NONE',  ( 5.049704560591026237, 1.530381825397047812, 1.394388655583590042 ) ) ;
#106415=CARTESIAN_POINT ( 'NONE',  ( 0.9426144736941791669, -1.451487892885485742, -1.132780452900377099 ) ) ;
#106417=CARTESIAN_POINT ( 'NONE',  ( 4.764420831138592938, 2.145307606383870969, -0.8259888504972175971 ) ) ;
#106421=CARTESIAN_POINT ( 'NONE',  ( 0.7094041017953250927, -0.3309814517665210509, 2.268137058596159328 ) ) ;
#106424=CARTESIAN_POINT ( 'NONE',  ( 4.663973314478016441, -1.267186161278991419, 1.471619509450792229 ) ) ;
#106428=CARTESIAN_POINT ( 'NONE',  ( 6.328373294368253354, -0.9077179077918960948, -1.683272687665722467 ) ) ;
#106429=CARTESIAN_POINT ( 'NONE',  ( 1.013767525470328001, -0.7718518339048777710, -1.542633921862639701 ) ) ;
#106430=CARTESIAN_POINT ( 'NONE',  ( 5.858611323429600226, -1.916351766245901977, -0.6279953093112633500 ) ) ;
#106434=CARTESIAN_POINT ( 'NONE',  ( 3.064484987736408872, -1.931880230092865025, -0.7996142226951181708 ) ) ;
#106435=CARTESIAN_POINT ( 'NONE',  ( 0.8481071238514601429, 0.5083433500535933236, 1.695271877703796504 ) ) ;
#106438=CARTESIAN_POINT ( 'NONE',  ( 4.084120828622629595, -2.267077656855093881, -0.3380819097023191055 ) ) ;
#106439=CARTESIAN_POINT ( 'NONE',  ( 2.325747778006927557, 1.687818050649522617, 0.4237310505307323449 ) ) ;
#106441=CARTESIAN_POINT ( 'NONE',  ( 2.830460552442021438, -1.048868820301660953, -1.842999677239331113 ) ) ;
#106443=CARTESIAN_POINT ( 'NONE',  ( 2.407222047678575283, 0.3756278383273171095, 1.692465640204628974 ) ) ;
#106445=CARTESIAN_POINT ( 'NONE',  ( 1.451354471725987860, 1.406072211568440755, 1.219298000798328507 ) ) ;
#106446=CARTESIAN_POINT ( 'NONE',  ( 2.488948079679761172, 2.105553563057678712, 0.5292575070172370610 ) ) ;
#106448=CARTESIAN_POINT ( 'NONE',  ( 3.907435596788138010, -1.928258004016227378, 0.5899861904685861358 ) ) ;
#106449=CARTESIAN_POINT ( 'NONE',  ( 1.875000000000001776, 2.052068128417950721, -1.077215146005767577E-13 ) ) ;
#106451=CARTESIAN_POINT ( 'NONE',  ( 0.4637318561061140043, 1.905900585730261110, -0.2794304195078872732 ) ) ;
#106453=CARTESIAN_POINT ( 'NONE',  ( 4.043395766388809598, 0.1113883285390921962, 2.218758960698932192 ) ) ;
#106459=CARTESIAN_POINT ( 'NONE',  ( 0.6630925397578091296, 0.6502370396846578471, 2.123993688044391259 ) ) ;
#106460=CARTESIAN_POINT ( 'NONE',  ( 4.598074495912657156, 0.8407358649686400565, -1.772743347989129692 ) ) ;
#106462=CARTESIAN_POINT ( 'NONE',  ( 5.431070396044226811, 0.1588226897794122738, 2.256881284257936215 ) ) ;
#106464=CARTESIAN_POINT ( 'NONE',  ( 3.473143217414649708, 1.863520296645693186, 0.8845801619412340111 ) ) ;
#106468=CARTESIAN_POINT ( 'NONE',  ( 5.026551685794930613, 1.789549103570491573, 0.5443708928771497924 ) ) ;
#106469=CARTESIAN_POINT ( 'NONE',  ( 3.217127751380299383, 1.692560603008624875, 0.3766165182450386117 ) ) ;
#106470=CARTESIAN_POINT ( 'NONE',  ( 2.928976884739741493, -1.170936322307249089, -1.287801759770091925 ) ) ;
#106471=CARTESIAN_POINT ( 'NONE',  ( 0.3809655214361170050, -0.2885804254640594868, -2.274098033663536356 ) ) ;
#106472=CARTESIAN_POINT ( 'NONE',  ( 0.7806487521475922176, -1.224371414366259847, 1.835764474286231129 ) ) ;
#106473=CARTESIAN_POINT ( 'NONE',  ( 5.144118995967028596, 0.6083014027435985627, 2.000272865920887266 ) ) ;
#106474=CARTESIAN_POINT ( 'NONE',  ( 6.087830645824786835, -1.932811661901209010, -0.1881662411436606785 ) ) ;
#106478=CARTESIAN_POINT ( 'NONE',  ( 0.4225002777262388265, -1.427939226333583500, -1.423959630194884696 ) ) ;
#106479=CARTESIAN_POINT ( 'NONE',  ( 1.055114822555893728, 0.4192091730233596381, 2.078585086915801128 ) ) ;
#106485=CARTESIAN_POINT ( 'NONE',  ( 4.459475772512963232, 0.3974328844052883447, -1.781742007231662983 ) ) ;
#106492=CARTESIAN_POINT ( 'NONE',  ( 1.793229165239007994, -0.1032543025433537293, -2.017296481459893709 ) ) ;
#106493=CARTESIAN_POINT ( 'NONE',  ( 5.877994779194309238, 1.310017027744770246, 1.775731318763192013 ) ) ;
#106495=CARTESIAN_POINT ( 'NONE',  ( 2.606119654932341767, 1.860434991719280173, 0.05107381154999082046 ) ) ;
#106500=CARTESIAN_POINT ( 'NONE',  ( 4.582524934692378871, -1.771534430979417429, -0.4408631061849078714 ) ) ;
#106505=CARTESIAN_POINT ( 'NONE',  ( 0.4207071466195873022, 0.6554624660736629860, 1.605403739708724631 ) ) ;
#106506=CARTESIAN_POINT ( 'NONE',  ( 0.1810874682179625661, -0.8250252819957092365, 1.532327275369157915 ) ) ;
#106507=CARTESIAN_POINT ( 'NONE',  ( 5.725286558339668375, -0.06233732282829743815, 2.307013574275817547 ) ) ;
#106509=CARTESIAN_POINT ( 'NONE',  ( 6.661405305706385782, 0.3767857563467743032, -2.128362917677539379 ) ) ;
#106511=CARTESIAN_POINT ( 'NONE',  ( 5.677245700908649439, -1.026343684741271023, -2.056567161392281129 ) ) ;
#106514=CARTESIAN_POINT ( 'NONE',  ( 5.489076674590072535, 1.649195787720953987, -0.8828566466120502110 ) ) ;
#106516=CARTESIAN_POINT ( 'NONE',  ( 3.164218664783400747, 1.912571728330178855, -0.004505864839042527346 ) ) ;
#106518=CARTESIAN_POINT ( 'NONE',  ( 5.567066847960510323, -1.993696164035433371, -0.9465883713010987410 ) ) ;
#106519=CARTESIAN_POINT ( 'NONE',  ( 4.557876730116875663, 1.221875164117897539, 1.729014733294547801 ) ) ;
#106524=CARTESIAN_POINT ( 'NONE',  ( 5.883467998083113493, 0.1561420574479575329, -2.114776682634044391 ) ) ;
#106525=CARTESIAN_POINT ( 'NONE',  ( 1.870602726103831381, 1.187374005633199836, 1.978520242944050711 ) ) ;
#106526=CARTESIAN_POINT ( 'NONE',  ( 3.930091730393743710, 1.087902980620155891, 1.632394305395828304 ) ) ;
#106528=CARTESIAN_POINT ( 'NONE',  ( 6.016483441405136467, 0.8307744727026479259, 1.888021813390627246 ) ) ;
#106532=CARTESIAN_POINT ( 'NONE',  ( 5.436732529336289588, -1.586671906620169104, 1.244382051841623538 ) ) ;
#106536=CARTESIAN_POINT ( 'NONE',  ( 1.622189073652591240, 2.139406107190901185, -0.3685050674664645531 ) ) ;
#106538=CARTESIAN_POINT ( 'NONE',  ( 0.1938080739139167730, 1.976361990896974508, -0.7691651810952588875 ) ) ;
#106543=CARTESIAN_POINT ( 'NONE',  ( 0.9837496482606482573, 1.382075509872608299, 1.528818673835147024 ) ) ;
#106548=CARTESIAN_POINT ( 'NONE',  ( 3.176317266091326807, 0.8619891151622931513, 1.707069686517001195 ) ) ;
#106550=CARTESIAN_POINT ( 'NONE',  ( 4.961649905909814251, 1.750258134581949232, -0.2615843724830448913 ) ) ;
#106553=CARTESIAN_POINT ( 'NONE',  ( 0.2986855335190057859, -0.2218818089524568216, -1.797891974444510765 ) ) ;
#106555=CARTESIAN_POINT ( 'NONE',  ( 6.116788041597909675, 0.1929307199614685164, 1.905880049602140636 ) ) ;
#106556=CARTESIAN_POINT ( 'NONE',  ( 0.4849360239999983557, 1.980737741294085419, 0.6024896509310638804 ) ) ;
#106559=CARTESIAN_POINT ( 'NONE',  ( 5.998880656844745474, 1.528293836345222312, -1.078463600801618405 ) ) ;
#106560=CARTESIAN_POINT ( 'NONE',  ( 2.666400811807769777, -1.259032629953384719, 1.322343945743660543 ) ) ;
#106562=CARTESIAN_POINT ( 'NONE',  ( 6.059228469117068805, -1.890744221452178353, -1.137928576693452820 ) ) ;
#106565=CARTESIAN_POINT ( 'NONE',  ( 2.840340301219072217, -1.062657783794159538, 1.767763702702547679 ) ) ;
#106569=CARTESIAN_POINT ( 'NONE',  ( 0.6499751493908960676, 0.6786997614584532323, -2.052318101833712660 ) ) ;
#106570=CARTESIAN_POINT ( 'NONE',  ( 6.408651866624735405, 0.6456447432892989946, 1.967203394946090977 ) ) ;
#106573=CARTESIAN_POINT ( 'NONE',  ( 4.059979352932830743, 2.145800628424157974, -0.2601280725000321148 ) ) ;
#106574=CARTESIAN_POINT ( 'NONE',  ( 4.723309930327257433, 1.758355855194023487, 0.9934411112178792580 ) ) ;
#106575=CARTESIAN_POINT ( 'NONE',  ( 2.084357000244409175, 1.132115006494602394, -1.602057852124554316 ) ) ;
#106582=CARTESIAN_POINT ( 'NONE',  ( 2.852750215419812108, -1.865046845876184189, -0.7672916333427428626 ) ) ;
#106585=CARTESIAN_POINT ( 'NONE',  ( 5.660397963661894849, 1.910509065610028090, 0.08734628876111423523 ) ) ;
#106590=CARTESIAN_POINT ( 'NONE',  ( 3.866814677988283044, -0.2004539179165897023, -2.006445418776988010 ) ) ;
#106594=CARTESIAN_POINT ( 'NONE',  ( 6.370102249521607973, 0.8915232854993185851, 1.476320845237573787 ) ) ;
#106598=CARTESIAN_POINT ( 'NONE',  ( 4.147608549738549755, 0.6325110726591242072, -1.760471310998643624 ) ) ;
#106600=CARTESIAN_POINT ( 'NONE',  ( 1.674760025662187735, 1.393346669028448392, -1.531324272915953744 ) ) ;
#106604=CARTESIAN_POINT ( 'NONE',  ( -0.05311194370935175268, -1.802413661875476913, -0.9041393574176490588 ) ) ;
#106605=CARTESIAN_POINT ( 'NONE',  ( 6.633470331352866900, -0.1302952867699505302, 1.781688180685939926 ) ) ;
#106613=CARTESIAN_POINT ( 'NONE',  ( 6.380494711820015930, -0.5163536399260219012, -1.844617532318414632 ) ) ;
#106619=CARTESIAN_POINT ( 'NONE',  ( 3.379894511112140787, 1.369989894601089775, 1.672159933133889442 ) ) ;
#106623=CARTESIAN_POINT ( 'NONE',  ( 0.9144942500491149984, -2.120778211678171488, 0.005759991200282586418 ) ) ;
#106624=CARTESIAN_POINT ( 'NONE',  ( 5.666980381186065507, -1.651371415153819688, -0.7785968546244539379 ) ) ;
#106626=CARTESIAN_POINT ( 'NONE',  ( 1.141796867408477967, 0.8028701493673767731, -1.800646566474963572 ) ) ;
#106627=CARTESIAN_POINT ( 'NONE',  ( 3.550944491985886575, 0.2853618425060593378, 1.890879049853078087 ) ) ;
#106630=CARTESIAN_POINT ( 'NONE',  ( 5.230891393285493685, -1.853837313009810028, -0.6654804215649990917 ) ) ;
#106631=CARTESIAN_POINT ( 'NONE',  ( 0.6560686395847237229, -1.407132438187887136, 1.338565165000434876 ) ) ;
#106637=CARTESIAN_POINT ( 'NONE',  ( 3.879479457080482696, 0.2311173251203814394, -1.898182577502210977 ) ) ;
#106639=CARTESIAN_POINT ( 'NONE',  ( 1.255210933454937283, -1.738917431694649185, 1.358592805172780693 ) ) ;
#106641=CARTESIAN_POINT ( 'NONE',  ( 6.639320575229259447, 0.002292789353198348111, 1.996863816985874118 ) ) ;
#106645=CARTESIAN_POINT ( 'NONE',  ( 2.277862540309500083, -2.008769142935047380, 0.5008063122204224893 ) ) ;
#106649=CARTESIAN_POINT ( 'NONE',  ( 0.1280963075596490419, -1.331634228802502928, -1.703589906866372017 ) ) ;
#106656=CARTESIAN_POINT ( 'NONE',  ( 6.825078400183548055, 3.702925343214446663, 2.370119418288775925 ) ) ;
#106658=CARTESIAN_POINT ( 'NONE',  ( 5.221237796217499394, 1.709784868986977902, 0.2885349091684140665 ) ) ;
#106661=CARTESIAN_POINT ( 'NONE',  ( 2.008725816923035978, 0.6454906730102347723, 1.967154155859623055 ) ) ;
#106662=CARTESIAN_POINT ( 'NONE',  ( 3.374719764411674205, -0.4154235484931252942, -2.075916080105549177 ) ) ;
#106667=CARTESIAN_POINT ( 'NONE',  ( 1.533974946755271240, 1.168952700103634390, 1.584878304665905180 ) ) ;
#106670=CARTESIAN_POINT ( 'NONE',  ( 4.207168913946373934, -0.3938425722496830539, 2.258028373892074558 ) ) ;
#106671=CARTESIAN_POINT ( 'NONE',  ( 1.945663734523142230, 0.6997465788082489757, -1.686465609443507763 ) ) ;
#106672=ADVANCED_FACE ( 'NONE', ( #29999 ), #103601, .F. ) ;
#106676=CARTESIAN_POINT ( 'NONE',  ( 2.531496316177814787, -0.1932786158439051827, 2.003878288502713101 ) ) ;
#106677=CARTESIAN_POINT ( 'NONE',  ( 3.045700443693433179, 1.383923128670875746, 1.390673908496591782 ) ) ;
#106680=CARTESIAN_POINT ( 'NONE',  ( 0.1751657365761339624, 7.629137130509054288, -2.644001943226172102 ) ) ;
#106681=CARTESIAN_POINT ( 'NONE',  ( 5.876921326125680523, 1.932075295558054240, -0.7991432938223922422 ) ) ;
#106682=CARTESIAN_POINT ( 'NONE',  ( 4.082668839255446436, -0.1736907016443404450, -1.761279006307460371 ) ) ;
#106684=CARTESIAN_POINT ( 'NONE',  ( 1.078377591563362436, -2.138745004354754897, -0.4770250503970187572 ) ) ;
#106685=CARTESIAN_POINT ( 'NONE',  ( 5.613164593121685364, -1.696513092703657799, 0.3873091720919922265 ) ) ;
#106688=CARTESIAN_POINT ( 'NONE',  ( 5.854147224351119227, 0.1731004610599009841, -2.292201554650086237 ) ) ;
#106689=CARTESIAN_POINT ( 'NONE',  ( 0.1333692844072559558, 0.7140749627707367875, -2.136770008611441618 ) ) ;
#106690=CARTESIAN_POINT ( 'NONE',  ( 5.395702507230883072, 0.1292110896585068891, 1.729053200853872596 ) ) ;
#106691=CARTESIAN_POINT ( 'NONE',  ( 1.612255294781844706, -2.189918024983358080, 0.2725913246661854084 ) ) ;
#106692=CARTESIAN_POINT ( 'NONE',  ( 5.723135995274492238, -1.960344405425541670, -0.9336216343173405763 ) ) ;
#106694=CARTESIAN_POINT ( 'NONE',  ( 0.09316046741510237983, 1.845552173327277501, 1.037660268145562004 ) ) ;
#106695=CARTESIAN_POINT ( 'NONE',  ( 4.500000000000003553, -2.561000571632643674E-13, -2.052068128417943171 ) ) ;
#106696=CARTESIAN_POINT ( 'NONE',  ( 6.827182134110200806, 2.035520418778674845, 2.394189263408800450 ) ) ;
#106697=CARTESIAN_POINT ( 'NONE',  ( 4.875960570263176308, 1.108828003875685475, 1.575097709652195643 ) ) ;
#106698=CARTESIAN_POINT ( 'NONE',  ( 1.717743135698499124, 1.849103211704594463, 1.230578002476825583 ) ) ;
#106704=CARTESIAN_POINT ( 'NONE',  ( 3.370003599138057471, 0.5381768412672756074, -2.155016279732512974 ) ) ;
#106710=CARTESIAN_POINT ( 'NONE',  ( 2.127577483945505055, 0.4445034925110411539, 1.966644524931899563 ) ) ;
#106712=CARTESIAN_POINT ( 'NONE',  ( 0.3036763228623740041, -1.592034637876770908, -1.310935287704196206 ) ) ;
#106715=CARTESIAN_POINT ( 'NONE',  ( 6.620655732516682157, 0.01042156863441953685, 1.726407961933309476 ) ) ;
#106718=CARTESIAN_POINT ( 'NONE',  ( 1.000807349803897628, 1.442299932730039869, 1.025250199436118503 ) ) ;
#106719=CARTESIAN_POINT ( 'NONE',  ( 0.4752326960846975923, -2.001511663014220677, -0.2440270837566413387 ) ) ;
#106720=CARTESIAN_POINT ( 'NONE',  ( 0.4504185290156897947, -1.555054577268409899, -0.9855837367087336709 ) ) ;
#106721=CARTESIAN_POINT ( 'NONE',  ( 4.142302782979132125, 0.6112592793995803575, 2.209291399377455889 ) ) ;
#106722=CARTESIAN_POINT ( 'NONE',  ( 2.044624030687072214, -1.478315374303545315, -1.097237131862264903 ) ) ;
#106725=CARTESIAN_POINT ( 'NONE',  ( 3.487140482124751362, 1.650829432287181264, -0.7796944959364560113 ) ) ;
#106726=CARTESIAN_POINT ( 'NONE',  ( 4.026017654026761150, -1.753031021560845559, 0.9963007555989014108 ) ) ;
#106728=CARTESIAN_POINT ( 'NONE',  ( 3.626065245518626412, -1.345661663401491293, -1.818709669598504997 ) ) ;
#106730=CARTESIAN_POINT ( 'NONE',  ( 5.807678370005410429, -0.5150985282868367765, 2.041858835689168927 ) ) ;
#106732=CARTESIAN_POINT ( 'NONE',  ( 2.066927875543830950, 1.535623996113824496, -1.388825173883188713 ) ) ;
#106735=CARTESIAN_POINT ( 'NONE',  ( 5.391314312714450274, -0.05227466736787074464, -2.120015263102632552 ) ) ;
#106737=CARTESIAN_POINT ( 'NONE',  ( 0.8383531591091289981, 1.897801360490163569, 0.3304300003270659314 ) ) ;
#106745=CARTESIAN_POINT ( 'NONE',  ( 1.002519415922138002, -0.9925456330053865628, 1.987394366727333717 ) ) ;
#106746=CARTESIAN_POINT ( 'NONE',  ( 2.608543117039106463, -0.8048738574607334773, -1.946287526097515430 ) ) ;
#106749=CARTESIAN_POINT ( 'NONE',  ( 5.770303593930925956, -0.8350939829899912681, -1.663081984830430793 ) ) ;
#106754=CARTESIAN_POINT ( 'NONE',  ( -0.06985027309261250539, -2.078401542846250116, 0.4200961532789050379 ) ) ;
#106757=CARTESIAN_POINT ( 'NONE',  ( 3.016010921186715432, 1.952665002612500533, -0.1895750030070641190 ) ) ;
#106758=CARTESIAN_POINT ( 'NONE',  ( 2.272554088390315030, -1.330374092946192688, 1.703740541667747133 ) ) ;
#106762=CARTESIAN_POINT ( 'NONE',  ( 3.714586447349605081, -0.1257948980903991487, 1.735838019273880928 ) ) ;
#106766=CARTESIAN_POINT ( 'NONE',  ( 0.9366540776252421097, 2.129889809250965271, 0.3686189752144660714 ) ) ;
#106767=CARTESIAN_POINT ( 'NONE',  ( 2.513045873335068237, 2.015604327017831654, 0.05229110803010171560 ) ) ;
#106770=GEOMETRIC_CURVE_SET ( 'NONE', ( #168733, #3369, #103896, #127391 ) ) ;
#106771=CARTESIAN_POINT ( 'NONE',  ( 2.465646028844501902, 1.933766160897397057, -0.3828895411656701997 ) ) ;
#106772=CARTESIAN_POINT ( 'NONE',  ( 6.539320575229249144, 0.007148032025052972194, 1.896977914940492393 ) ) ;
#106778=CARTESIAN_POINT ( 'NONE',  ( 2.350265711909118593, 0.9499565981557709371, -1.782299418695271198 ) ) ;
#106780=CARTESIAN_POINT ( 'NONE',  ( 6.088978940744814494, -0.3304744056438710387, -2.283700556900492451 ) ) ;
#106782=CARTESIAN_POINT ( 'NONE',  ( 2.694135368495911731, 0.9291169126603683326, -1.727816930623335967 ) ) ;
#106784=CARTESIAN_POINT ( 'NONE',  ( 0.6334356698059574464, 0.5880228326464317368, 1.928751028484784191 ) ) ;
#106786=CARTESIAN_POINT ( 'NONE',  ( 2.694651208505644213, 1.530237149716510370, -1.463602791221560118 ) ) ;
#106789=CARTESIAN_POINT ( 'NONE',  ( 1.745803608711377075, 0.5764907460206626366, 1.748616612666432868 ) ) ;
#106793=CARTESIAN_POINT ( 'NONE',  ( 4.394861267144759331, -2.057662932662501110, -0.5123870273424437904 ) ) ;
#106794=CARTESIAN_POINT ( 'NONE',  ( 0.2339851986729903077, 0.3116528534230639247, 1.814411239467295101 ) ) ;
#106798=CARTESIAN_POINT ( 'NONE',  ( 4.903620131156614548, -0.5536938069644473659, 1.984910608926907960 ) ) ;
#106800=CARTESIAN_POINT ( 'NONE',  ( 1.891909123491273492, -0.4922293657834125313, -1.774144672653771293 ) ) ;
#106805=CARTESIAN_POINT ( 'NONE',  ( 0.5752038918783763943, -2.079344756725898691, -0.7397341299467049547 ) ) ;
#106806=CARTESIAN_POINT ( 'NONE',  ( 3.743696771605113494, -1.710248914368957873, -1.481124664604586583 ) ) ;
#106808=CARTESIAN_POINT ( 'NONE',  ( 3.164119808340008611, 1.811767227632065325, -0.004774541488360150264 ) ) ;
#106809=CARTESIAN_POINT ( 'NONE',  ( 3.327253086410830729, -1.454009962414861912, -1.247479002808443704 ) ) ;
#106810=CARTESIAN_POINT ( 'NONE',  ( 4.000488093070094564, 2.060113009926473726, 0.2059288336104248551 ) ) ;
#106812=CARTESIAN_POINT ( 'NONE',  ( 2.483225996990960027, 1.803144932609510143, -0.7974705804912070040 ) ) ;
#106813=CARTESIAN_POINT ( 'NONE',  ( 0.5867820057828515568, -0.2326963965399355405, -1.912219011898611765 ) ) ;
#106814=CARTESIAN_POINT ( 'NONE',  ( 4.100366707588389836, -0.5864361863821172527, -1.776433678864146382 ) ) ;
#106816=CARTESIAN_POINT ( 'NONE',  ( 2.245130213409586961, 0.5076759487793567338, 2.251015715305480391 ) ) ;
#106817=CARTESIAN_POINT ( 'NONE',  ( 4.211269073929763351, -1.546465011353677532, -1.035020834652039090 ) ) ;
#106823=CARTESIAN_POINT ( 'NONE',  ( 0.4695305163736606668, 0.2040741594158005934, -2.096154701512464413 ) ) ;
#106827=CARTESIAN_POINT ( 'NONE',  ( 6.854756222516504849, -1.675677847961650313, 1.365199464886861946 ) ) ;
#106828=CARTESIAN_POINT ( 'NONE',  ( 2.478903650112133317, -1.459102030866548994, 1.539066919819010781 ) ) ;
#106830=CARTESIAN_POINT ( 'NONE',  ( 0.4748752182902976071, -1.459934291025711373, 1.395986992609834276 ) ) ;
#106834=CARTESIAN_POINT ( 'NONE',  ( 1.353037089713942320, -1.704917477850418805, 1.328741451194020762 ) ) ;
#106836=CARTESIAN_POINT ( 'NONE',  ( 6.925078400183550364, 4.696033252921790968, 2.518291795588607052 ) ) ;
#106839=CARTESIAN_POINT ( 'NONE',  ( 6.122279814772176643, 1.995267444086584296, 0.2910868170948808786 ) ) ;
#106841=CARTESIAN_POINT ( 'NONE',  ( 0.08191350661116909848, -1.027414926483052326, 1.935800647029708443 ) ) ;
#106843=CARTESIAN_POINT ( 'NONE',  ( 0.7083710243460902278, -2.251296572208848712, 0.2248925466769024495 ) ) ;
#106847=CARTESIAN_POINT ( 'NONE',  ( 1.177184062793021679, 1.451467631357589383, 1.250241458713635456 ) ) ;
#106851=CARTESIAN_POINT ( 'NONE',  ( 2.648709078547459850, -1.434216206362935564, 0.9578970732360950757 ) ) ;
#106854=CARTESIAN_POINT ( 'NONE',  ( 0.4382651835369972826, 0.2938455168926180638, 1.745004787994571593 ) ) ;
#106856=CARTESIAN_POINT ( 'NONE',  ( 2.051433223282957297, -1.797157160989469427, 0.9072355583341712437 ) ) ;
#106859=CARTESIAN_POINT ( 'NONE',  ( 4.085166796624926100, -0.2132991444873769959, -2.196430506890618695 ) ) ;
#106863=CARTESIAN_POINT ( 'NONE',  ( 4.371814246616528621, 0.4635510597098577712, -2.069045912693792566 ) ) ;
#106864=CARTESIAN_POINT ( 'NONE',  ( 3.972279928656559100, -1.994873972748755442, -0.2930500606010341125 ) ) ;
#106865=CARTESIAN_POINT ( 'NONE',  ( 3.216879062660949362, 1.425012358211204422, -1.118398921490076026 ) ) ;
#106869=CARTESIAN_POINT ( 'NONE',  ( 1.709613803025863188, -1.856884215550944850, 0.2259493607114013147 ) ) ;
#106871=CARTESIAN_POINT ( 'NONE',  ( 5.813091150998386247, 1.612263477354998864, 0.8566026058636074803 ) ) ;
#106878=B_SPLINE_CURVE_WITH_KNOTS ( 'NONE', 3,
 ( #160527, #77137, #12132, #210328, #179983, #79278, #15319, #191935, #208192, #195168, #161611, #64099, #97680, #95560, #80341, #30542, #31604, #112916, #96622, #43599, #143258, #61966, #196233, #128122, #162676, #163738, #78204, #45735, #145395, #109718, #209247, #178927, #111853, #29469, #13201, #211393, #175723, #63022, #193011, #176778, #14246, #129190, #146441, #94489, #212454, #59825, #125978, #44665, #60891, #110778, #93421, #159458, #127051, #28394, #194082, #52111, #134460, #182084, #81407, #213512, #34774, #83527, #149610, #18525, #1192, #66183, #200464, #49974, #100846, #69394, #48918, #118237, #181038, #147490, #115039, #33715, #132329, #99792, #198334, #197278, #166932, #36909, #84603, #19594, #150691, #116093, #131291, #165859, #184222, #17444, #119300, #2253, #67256, #32654, #68329, #35844, #85667, #199397, #101923, #183170, #117, #102991, #133391, #169049, #98732, #51043, #117166, #65133, #164790, #167989, #151753, #3324, #135501, #201524, #16382, #53172, #185286, #82461, #148551, #205810, #55311, #173343, #136571, #23854, #21698, #89962, #20647, #186357, #120382, #24923, #37993, #22775, #88892, #172267, #154946, #5451, #73685, #203660, #188499, #8678, #202592, #42277, #74760, #140862, #104065, #139783, #86736, #54244, #108391, #91028, #57441, #190619, #156013, #157089, #40131, #71530, #70456, #137641, #123602, #105145, #58507, #170111, #39059, #6530, #72608, #171185, #189567, #107319, #121460, #41212, #87809, #138708, #204724, #152805, #56375, #122538, #153882, #187430, #206876, #106241, #7600, #124662, #4384, #211134, #9747, #94233, #210066, #158154, #13996, #145128, #208995, #46537, #75821, #128918, #96365, #192749, #43344, #44406, #28138, #146182, #111589, #110526, #59563, #80081, #25992, #212197, #141929, #177599, #60631, #77950, #160271, #176526, #62758, #61706, #193824, #11873, #66721, #112658, #194899, #207942, #144071, #127874, #29211, #125723, #109464, #79012, #45473, #95301, #161350, #12931, #191683, #178667, #10802, #126794, #30279, #132864, #50515, #162419, #198868, #174415, #142997, #76876, #175471, #92100, #27057, #93164, #159201, #199945, #186900, #118773, #4919, #19062, #154419, #68868, #70996, #134988, #69930, #202054, #200998, #203138, #169595, #170657, #21177, #54780, #20126, #101392, #103535, #5997, #119847, #117716, #185825, #116638, #67788, #1731, #120927, #133938, #184757, #36384, #53714, #102462, #167466, #100327, #37456, #87280, #153349, #38532, #138178, #104610, #22244, #51592, #137109, #182633, #150163, #204188, #88354, #72068, #34255, #166394, #17985, #136042, #85140, #84075, #183706, #35314, #52643, #86212, #151227, #168528, #152284, #3857, #2796, #92645, #142466, #40681, #10285, #56914, #173894, #124141, #55844, #190103, #140332, #91577, #122000, #143544, #59040, #57978, #26537, #75299, #158687, #105697, #41756, #157629, #39594, #110003, #76359, #90497, #208474, #171724, #60110, #192226, #74239, #106784, #126269, #9227, #43889, #156560, #206351, #155482, #176016, #187966, #27608, #23323, #125198, #8155, #25469, #107868, #141414, #172812, #207421, #93708, #191161, #159748, #11346, #77427, #89431, #42828, #7065, #123087, #108934, #73138, #174955, #139243, #205274, #24384, #189044, #161899, #97971, #13486, #162962, #80638, #79561, #145680, #178144, #49209, #48161, #81692, #113204 ),
 .UNSPECIFIED., .F., .F.,
 ( 4, 1, 1, 1, 1, 1, 1, 1, 1, 1, 1, 1, 1, 1, 1, 1, 1, 1, 1, 1, 1, 1, 1, 1, 1, 1, 1, 1, 1, 1, 1, 1, 1, 1, 1, 1, 1, 1, 1, 1, 1, 1, 1, 1, 1, 1, 1, 1, 1, 1, 1, 1, 1, 1, 1, 1, 1, 1, 1, 1, 1, 1, 1, 1, 1, 1, 1, 1, 1, 1, 1, 1, 1, 1, 1, 1, 1, 1, 1, 1, 1, 1, 1, 1, 1, 1, 1, 1, 1, 1, 1, 1, 1, 1, 1, 1, 1, 1, 1, 1, 1, 1, 1, 1, 1, 1, 1, 1, 1, 1, 1, 1, 1, 1, 1, 1, 1, 1, 1, 1, 1, 1, 1, 1, 1, 1, 1, 1, 1, 1, 1, 1, 1, 1, 1, 1, 1, 1, 1, 1, 1, 1, 1, 1, 1, 1, 1, 1, 1, 1, 1, 1, 1, 1, 1, 1, 1, 1, 1, 1, 1, 1, 1, 1, 1, 1, 1, 1, 1, 1, 1, 1, 1, 1, 1, 1, 1, 1, 1, 1, 1, 1, 1, 1, 1, 1, 1, 1, 1, 1, 1, 1, 1, 1, 1, 1, 1, 1, 1, 1, 1, 1, 1, 1, 1, 1, 1, 1, 1, 1, 1, 1, 1, 1, 1, 1, 1, 1, 1, 1, 1, 1, 1, 1, 1, 1, 1, 1, 1, 1, 1, 1, 1, 1, 1, 1, 1, 1, 1, 1, 1, 1, 1, 1, 1, 1, 1, 1, 1, 1, 1, 1, 1, 1, 1, 1, 1, 1, 1, 1, 1, 1, 1, 1, 1, 1, 1, 1, 1, 1, 1, 1, 1, 1, 1, 1, 1, 1, 1, 1, 1, 1, 1, 1, 1, 1, 1, 1, 1, 1, 1, 1, 1, 1, 1, 1, 1, 1, 1, 1, 1, 1, 1, 1, 1, 1, 1, 1, 1, 1, 1, 1, 1, 1, 1, 1, 1, 1, 1, 1, 1, 1, 1, 1, 1, 1, 1, 1, 1, 1, 1, 1, 1, 1, 1, 1, 1, 1, 1, 1, 1, 1, 1, 1, 1, 1, 1, 1, 1, 1, 1, 1, 1, 1, 1, 1, 1, 1, 1, 1, 1, 1, 1, 1, 1, 1, 1, 1, 1, 1, 1, 1, 1, 1, 1, 1, 1, 1, 1, 1, 1, 1, 1, 1, 4 ),
 ( 0.000000000000000000, 0.002600033395298661284, 0.005208813367820810773, 0.007813200023264601363, 0.01041635779573905213, 0.01302082523971277370, 0.01562491580351430334, 0.01822918961192645723, 0.02083333155136493989, 0.02343746137460561707, 0.02604174567981391505, 0.02864576082122225614, 0.03125012338981237453, 0.03385410379569547823, 0.03645843966640821554, 0.03906250599122108869, 0.04166672065998115043, 0.04427093656960304907, 0.04687500111868234121, 0.04947933663890847350, 0.05208331727515622817, 0.05468767913406928638, 0.05729168951085979872, 0.05989597295159828499, 0.06250011041458469752, 0.06510424634142775169, 0.06770853038940542745, 0.07031253939703428768, 0.07291690072920921362, 0.07552088074063932621, 0.07812521459448035221, 0.08072927904253822395, 0.08333349217322323643, 0.08593770650149938628, 0.08854176936806532061, 0.09114610329512429221, 0.09375008230893774885, 0.09635444258075796797, 0.09895845137230636912, 0.1015627332241899466, 0.1041668691376404637, 0.1067710034717011397, 0.1093752859901425123, 0.1119792934252105548, 0.1145836532378000650, 0.1171876317139315254, 0.1197919640503514460, 0.1223960270027875247, 0.1250002386107842423, 0.1276044514713231270, 0.1302085128224930721, 0.1328128452953424854, 0.1354168228245230532, 0.1380211816480703679, 0.1406251889951717071, 0.1432294693974442978, 0.1458336039016293884, 0.1484377367829480265, 0.1510420179109137340, 0.1536460239143070949, 0.1562503823458506746, 0.1588543594276481397, 0.1614586903853630351, 0.1640627519827278502, 0.1666669622076225599, 0.1692711737400035832, 0.1718752337163205746, 0.1744795648736557347, 0.1770835410591554138, 0.1796878985729436218, 0.1822919046164021839, 0.1848961837081005144, 0.1875003169431251615, 0.1901044485118078553, 0.1927087283883223978, 0.1953127331008320255, 0.1979170902898210183, 0.2005210661182068033, 0.2031253958358791578, 0.2057294562186703923, 0.2083336651999991573, 0.2109378755437518183, 0.2135419342857080849, 0.2161462642661750033, 0.2187502392488957503, 0.2213545955913898966, 0.2239586004719608947, 0.2265628783920732026, 0.2291670104979939837, 0.2317711408940984485, 0.2343754196581391558, 0.2369794232205082452, 0.2395837793053874898, 0.2421877540212369617, 0.2447920826374832270, 0.2473961419461526701, 0.2500003498234057431, 0.2526045591180144934, 0.2552086167660569949, 0.2578129457082574683, 0.2604169196290564980, 0.2630212749386780513, 0.2656252787970727613, 0.2682295556845439854, 0.2708336868013750398, 0.2734378161649161920, 0.2760420939554183439, 0.2786460965083475960, 0.2812504516275206035, 0.2838544253716674404, 0.2864587530250631842, 0.2890628114000217685, 0.2916670183126490179, 0.2942712266975582858, 0.2968752833920936807, 0.2994796114345903981, 0.3020835844342854570, 0.3046879388494173613, 0.3072919418263086455, 0.3098962178200457829, 0.3125003480877632800, 0.3151044765587182606, 0.3177087535145803887, 0.3203127551987332566, 0.3229171094905676220, 0.3255210824038090589, 0.3281254092328941829, 0.3307294668145174810, 0.3333336729019333866, 0.3359378805165532667, 0.3385419363979534357, 0.3411462636792753078, 0.3437502358986498918, 0.3463545895576419231, 0.3489585917936692261, 0.3515628670325462446, 0.3541669965910940188, 0.3567711243094072171, 0.3593754005694961839, 0.3619794015255044517, 0.3645837551283364619, 0.3671877273514386752, 0.3697920534947228832, 0.3723961104233561858, 0.3750003158249449187, 0.3776045228086560845, 0.3802085780172632101, 0.3828129046759103926, 0.3854168762557192984, 0.3880212292968930887, 0.3906252309326675998, 0.3932295055555311003, 0.3958336345448258409, 0.3984377616504144459, 0.4010420373535708016, 0.4036460377220391638, 0.4062503907741795706, 0.4088543624478828686, 0.4114586880438503846, 0.4140627444598136697, 0.4166669493149349202, 0.4192711558070936761, 0.4218752104832254046, 0.4244795366576747386, 0.4270835077386489487, 0.4296878603003031483, 0.4322918614764136302, 0.4348961356220873986, 0.4375002641820237570, 0.4401043908147829753, 0.4427086660998260093, 0.4453126660213379551, 0.4479170186610768045, 0.4505209899261007900, 0.4531253151132156320, 0.4557293711568096706, 0.4583335756048029785, 0.4609377817447468106, 0.4635418360287018591, 0.4661461618574116450, 0.4687501325802634344, 0.4713544848006788190, 0.4739584856576960492, 0.4765627594649867738, 0.4791668877354426925, 0.4817710140352507997, 0.4843752890409837031, 0.4869792886561065681, 0.4895836410217184742, 0.4921876120187673176, 0.4947919369354787933, 0.4973959927469893683, 0.5000001969271801183, 0.5026044028542325792, 0.5052084568862954539, 0.5078127825077110025, 0.5104167530131399344, 0.5130211050305848453, 0.5156251057090676104, 0.5182293793167697116, 0.5208335074376115870, 0.5234376335443351458, 0.5260419084095501185, 0.5286459078588399141, 0.5312502600885893322, 0.5338542309583571566, 0.5364585557431046370, 0.5390626114628084276, 0.5416668155145124564, 0.5442710213679887721, 0.5468750752884355970, 0.5494794008409938924, 0.5520833712696913143, 0.5546877232224267651, 0.5572917238629264691, 0.5598959974098275394, 0.5625001255209155504, 0.5651042515744146844, 0.5677085264378984863, 0.5703125258619060611, 0.5729168780940517847, 0.5755208489772277725, 0.5781251737684461878, 0.5807292295366155432, 0.5833334335991446906, 0.5859376395183565345, 0.5885416934674594369, 0.5911460190895951872, 0.5937499895822500040, 0.5963543416085342885, 0.5989583423516006144, 0.6015626159764864145, 0.6041667442176794633, 0.6067708703578130747, 0.6093751453583519107, 0.6119791448976270587, 0.6145834972704286026, 0.6171874683077025470, 0.6197917932438269384, 0.6223958492007358734, 0.6250000534134032559, 0.6276042595376638555, 0.6302083136556971832, 0.6328126394858472059, 0.6354166101831504321, 0.6380209624212449526, 0.6406249634074311361, 0.6432292372490908683, 0.6458333657602520761, 0.6484374921268833969, 0.6510417674032679125, 0.6536457671983656459, 0.6562501198500874100, 0.6588540911821543222, 0.6614584164016259482, 0.6640624726875546946, 0.6666666771896793131, 0.6692708836583093346, 0.6718749380855545406, 0.6744792642621626477, 0.6770832353048136243, 0.6796875878929879988, 0.6822915892628557133, 0.6848958634600870177, 0.6874999923810890534, 0.6901041191140900866, 0.6927083948051209195, 0.6953123949966061312, 0.6979167480655225075, 0.7005207198330885010, 0.7031250454743595002, 0.7057291022295995031, 0.7083333071605121267, 0.7109375141128444486, 0.7135415689895947544, 0.7161458956511181917, 0.7187498671798290273, 0.7213542202563657524, 0.7239582221504904380, 0.7265624968421051655, 0.7291666263128349090, 0.7317707535520923123, 0.7343750297965853102, 0.7369790305250381035, 0.7395833841494394711, 0.7421873564932268685, 0.7447916826947649227, 0.7473957400596251688, 0.7499999455586733310, 0.7526041531340577073, 0.7552082086006238759, 0.7578125358855373195, 0.7604165080410384414, 0.7630208617442386654, 0.7656248643032155243, 0.7682291396280439555, 0.7708332697884082707, 0.7734373976738285750, 0.7760416746106194585, 0.7786456760166404756, 0.7812500303348380859, 0.7838540033955903041, 0.7864583302958847444, 0.7890623884106959807, 0.7916665946172487534, 0.7942708029550582527, 0.7968748591517740287, 0.7994791871985751364, 0.8020831601216208417, 0.8046875145898089166, 0.8072915179542569097, 0.8098957940511537501, 0.8124999250410844809, 0.8151040537125986418, 0.8177083314805486669, 0.8203123337047645292, 0.8229166888550945025, 0.8255206627735817149, 0.8281249905111484066, 0.8307290495162685806, 0.8333332565697225691, 0.8359374658093579047, 0.8385415228765847884, 0.8411458518237998616, 0.8437498256551729803, 0.8463541810267020127, 0.8489581853372698550, 0.8515624623451190089, 0.8541665943045783083, 0.8567707239021479237, 0.8593750026401490993, 0.8619790058232168484, 0.8645833619440471685, 0.8671873368610717447, 0.8697916655744575287, 0.8723957256102774505, 0.8749999336500613456, 0.8776041439309557601, 0.8802082020090884473, 0.8828125319952765393, 0.8854165068757942070, 0.8880208632890512765, 0.8906248686864229880, 0.8932291467441429988, 0.8958332798131283248, 0.8984374104767501867, 0.9010416903237299380, 0.9036456946063434748, 0.9062500518360779855, 0.9088540278924787108, 0.9114583577202677311, 0.9140624189272162914, 0.9166666280927961985, 0.9192708395544209043, 0.9218748987838942810, 0.9244792299476556341, 0.9270832060181642964, 0.9296875636115721209, 0.9322915702365133228, 0.9348958494830461596, 0.9374999838014769216, 0.9401041156712998115, 0.9427083967663798525, 0.9453124022892170908, 0.9479167607665550666, 0.9505207380999710631, 0.9531250691809918241, 0.9557291317261836783, 0.9583333421310490374, 0.9609375547886240820, 0.9635416155522130710, 0.9661459483928183101, 0.9687499245033458495, 0.9713542829945021051, 0.9739582954330652242, 0.9765625745907361432, 0.9791667024412501474, 0.9817708385604039245, 0.9843751096149007118, 0.9869791944699233266, 0.9895836584107432499, 0.9921868132917668337, 0.9947911946869415489, 0.9973999724172807335, 1.000000000000000000 ),
 .UNSPECIFIED. ) ;
#106883=CARTESIAN_POINT ( 'NONE',  ( 3.885109016898562029, -1.979880364965879380, -0.7601140796509860964 ) ) ;
#106884=CARTESIAN_POINT ( 'NONE',  ( -0.02948999725182251466, 1.364966664109868555, -2.179895196203474050 ) ) ;
#106886=CARTESIAN_POINT ( 'NONE',  ( 5.167239647397361857, 0.1962102620695851674, -1.961592271633934903 ) ) ;
#106889=CARTESIAN_POINT ( 'NONE',  ( 0.4216853220532343904, -1.500587716210170841, -1.493872543894637417 ) ) ;
#106891=CARTESIAN_POINT ( 'NONE',  ( 1.012269475826784060, 2.068064858651061932, -0.09981174449213289779 ) ) ;
#106896=CARTESIAN_POINT ( 'NONE',  ( 3.416043810090535260, 1.326132273491455349, -1.616208110139333742 ) ) ;
#106899=CARTESIAN_POINT ( 'NONE',  ( 2.432394421669949569, 1.770131964307398498, 0.4459858026567494194 ) ) ;
#106900=CARTESIAN_POINT ( 'NONE',  ( 1.734716041023535160, 1.690356777636679686, 0.6517371015684128022 ) ) ;
#106902=CARTESIAN_POINT ( 'NONE',  ( 5.654950187766193181, -1.741821662664808645, 1.355018943897445149 ) ) ;
#106905=CARTESIAN_POINT ( 'NONE',  ( 3.856632026064894525, 0.7917978285330304900, 2.060012427959257764 ) ) ;
#106909=CARTESIAN_POINT ( 'NONE',  ( 2.807167725247063483, 1.639017566557477990, -0.9848878580655600068 ) ) ;
#106911=CARTESIAN_POINT ( 'NONE',  ( 4.932118098221458524, 1.189261692661430114, 1.694535115018414917 ) ) ;
#106914=CARTESIAN_POINT ( 'NONE',  ( 6.321842903100939104, 1.263506803105146847, -1.790488031206059372 ) ) ;
#106915=VERTEX_POINT ( 'NONE', #79287 ) ;
#106924=CARTESIAN_POINT ( 'NONE',  ( 5.295788417638883416, -1.460108768623759712, -1.467927865959644862 ) ) ;
#106925=CARTESIAN_POINT ( 'NONE',  ( 4.301339506872517759, 1.548173799611574530, 1.146357790588454106 ) ) ;
#106926=CARTESIAN_POINT ( 'NONE',  ( 0.03478015955125923070, -1.617804660175032661, 1.203375172262765913 ) ) ;
#106931=CARTESIAN_POINT ( 'NONE',  ( 0.7971425760184660536, 1.793611693402120455, 1.258865353619270433 ) ) ;
#106932=CARTESIAN_POINT ( 'NONE',  ( 4.916531288042031989, 1.256637652550334883, -1.324621001416517840 ) ) ;
#106940=CARTESIAN_POINT ( 'NONE',  ( 2.770863647982471534, 1.747605724785822767, -0.5798694457997202178 ) ) ;
#106941=CARTESIAN_POINT ( 'NONE',  ( 5.994395146102541538, -1.073393154543872852, 1.702996195706570681 ) ) ;
#106942=CARTESIAN_POINT ( 'NONE',  ( 1.740083653633100580, -2.182622149841602521, -0.7203450084119922270 ) ) ;
#106943=CARTESIAN_POINT ( 'NONE',  ( 6.631700630569578259, 1.878258136613653040, -0.5663492180864730940 ) ) ;
#106949=CARTESIAN_POINT ( 'NONE',  ( 2.612926333352751929, -0.2020284733853395243, 2.080942194061443651 ) ) ;
#106950=CARTESIAN_POINT ( 'NONE',  ( 1.270139834521961886, -1.189467451172643964, 1.443775233441677130 ) ) ;
#106951=CARTESIAN_POINT ( 'NONE',  ( 1.563827143785265328, 1.649830188709809686, -1.158509706484150970 ) ) ;
#106954=CARTESIAN_POINT ( 'NONE',  ( 2.401564422585287684, -0.6675299454344629790, -1.607540830017651023 ) ) ;
#106958=CARTESIAN_POINT ( 'NONE',  ( 2.420142186669431705, 1.127438667474765621, -1.305497878543178336 ) ) ;
#106959=CARTESIAN_POINT ( 'NONE',  ( 2.384552795368581890, -0.3778730364575392797, -2.158588602542845347 ) ) ;
#106960=CARTESIAN_POINT ( 'NONE',  ( 5.197975494389605267, -0.7968864405506062010, 2.058166701804148957 ) ) ;
#106963=CARTESIAN_POINT ( 'NONE',  ( 2.887734989934476193, -2.027295339332426227, 0.7774125151447373039 ) ) ;
#106964=CARTESIAN_POINT ( 'NONE',  ( 0.5569169099325711469, -1.540613122784354916, -0.9793164655157863274 ) ) ;
#106965=CARTESIAN_POINT ( 'NONE',  ( 4.329393036353162749, -1.639139883998712799, -1.340335314225228780 ) ) ;
#106966=CARTESIAN_POINT ( 'NONE',  ( 6.539320575229279342, 6.038407674219216759, 2.491644695858772796 ) ) ;
#106968=CARTESIAN_POINT ( 'NONE',  ( 4.792671637142519536, 1.906707348304257366, -1.272296631038958070 ) ) ;
#106970=CARTESIAN_POINT ( 'NONE',  ( 6.827182134110238998, -0.009824402486291110986, 2.288967694407703313 ) ) ;
#106972=CARTESIAN_POINT ( 'NONE',  ( 0.8211285067932658777, 1.603129840700336706, -1.388046135824993366 ) ) ;
#106978=CARTESIAN_POINT ( 'NONE',  ( 4.746720300533005421, 1.994071680685698400, -0.2986252114312442640 ) ) ;
#106980=CARTESIAN_POINT ( 'NONE',  ( 3.731348124473393479, 0.05553323764710679095, -2.061997793915891553 ) ) ;
#106982=CARTESIAN_POINT ( 'NONE',  ( -0.1409997244346088141, 4.088373444016307978, -2.555100908668860082 ) ) ;
#106986=CARTESIAN_POINT ( 'NONE',  ( 5.648420989521034663, -1.729380818958951460, 1.345873388983606533 ) ) ;
#106987=CARTESIAN_POINT ( 'NONE',  ( 3.533827422916273164, -1.646839391163470223, 1.163268690995450383 ) ) ;
#106988=CARTESIAN_POINT ( 'NONE',  ( 3.544333174469185721, -1.503253232081468216, 1.062929765333266108 ) ) ;
#106990=CARTESIAN_POINT ( 'NONE',  ( 6.510779352739587189, 1.350450193652263930, -1.228632259304612839 ) ) ;
#106991=CARTESIAN_POINT ( 'NONE',  ( 0.2296305240335142495, 2.293118238291039113, 0.1608910274224564507 ) ) ;
#106993=CARTESIAN_POINT ( 'NONE',  ( 6.297788943421148922, -0.7692995465161235336, 2.127847719713715335 ) ) ;
#106994=CARTESIAN_POINT ( 'NONE',  ( 2.350341522438728514, 2.105628791459000393, 0.05071553880554508648 ) ) ;
#107003=CARTESIAN_POINT ( 'NONE',  ( 4.131244869123442243, 2.031816273447330623, 0.8983479855831574268 ) ) ;
#107004=CARTESIAN_POINT ( 'NONE',  ( 2.660326705311684581, -1.510451929809487170, 1.587989696798755235 ) ) ;
#107005=CARTESIAN_POINT ( 'NONE',  ( 0.6982365061397632910, -0.7907169553198112322, 2.060542492664858560 ) ) ;
#107008=CARTESIAN_POINT ( 'NONE',  ( 4.844172697165038066, -0.9265620464425131653, 1.729294158640543699 ) ) ;
#107012=CARTESIAN_POINT ( 'NONE',  ( 6.610000000000006537, 0.002781820520842553934, 2.000159646111852929 ) ) ;
#107015=CARTESIAN_POINT ( 'NONE',  ( 3.322626870553476941, -0.8629183168706102691, -1.937285153019531414 ) ) ;
#107017=CARTESIAN_POINT ( 'NONE',  ( 5.770447993230207295, -1.374857387916775364, 1.668144713590607120 ) ) ;
#107018=CARTESIAN_POINT ( 'NONE',  ( 3.579498943475650563, -0.9044721095569520086, 1.603693017070174864 ) ) ;
#107021=CARTESIAN_POINT ( 'NONE',  ( 6.650362500428334656, -1.339898832705511911, 1.110426912289312451 ) ) ;
#107022=CARTESIAN_POINT ( 'NONE',  ( 6.827182134110219458, 2.993868409037139688, 2.165198344177218903 ) ) ;
#107025=CARTESIAN_POINT ( 'NONE',  ( 4.030267251519312310, 1.158562084521784108, -1.824840551714689507 ) ) ;
#107028=CARTESIAN_POINT ( 'NONE',  ( 5.360703810585087048, -0.7282664037663032497, 1.880147357087233129 ) ) ;
#107030=CARTESIAN_POINT ( 'NONE',  ( 3.292016909520224743, -0.8776455207864016783, 1.975710135277891633 ) ) ;
#107031=CARTESIAN_POINT ( 'NONE',  ( 3.180892574772069992, -0.1416633064414400678, -1.966302885814166013 ) ) ;
#107033=CARTESIAN_POINT ( 'NONE',  ( 0.5875216112017033199, -0.2866185507822028855, -2.289643093864159429 ) ) ;
#107034=CARTESIAN_POINT ( 'NONE',  ( 3.233719155016498092, -1.381502681103630392, -1.529336839808728365 ) ) ;
#107035=CARTESIAN_POINT ( 'NONE',  ( 5.372584366608633921, -0.05174306282297027465, -1.941541108160367513 ) ) ;
#107042=CARTESIAN_POINT ( 'NONE',  ( 2.362605853119781774, 0.9431403173822919817, 1.995201469058570432 ) ) ;
#107045=CARTESIAN_POINT ( 'NONE',  ( 0.4966286816309881114, 0.3102001241638470685, 1.834739031104109408 ) ) ;
#107047=CARTESIAN_POINT ( 'NONE',  ( -0.02919842301646497981, 2.009414862388910983, -2.487882213790572283 ) ) ;
#107052=CARTESIAN_POINT ( 'NONE',  ( 5.806566994037906326, 1.625791660643903791, 0.8640615347050364381 ) ) ;
#107054=CARTESIAN_POINT ( 'NONE',  ( 1.938423425814293388, 2.038317423364948588, 0.3033609537064930750 ) ) ;
#107061=ADVANCED_FACE ( 'NONE', ( #47886 ), #52363, .F. ) ;
#107062=CARTESIAN_POINT ( 'NONE',  ( 1.200152769736504421, -2.061077815970461025, -0.0008511993763692102862 ) ) ;
#107064=CARTESIAN_POINT ( 'NONE',  ( 4.528748383445759806, -1.681502307688139908, 0.7506017836093890061 ) ) ;
#107067=CARTESIAN_POINT ( 'NONE',  ( -0.2409995289980246813, 5.721856934700204178, -2.594540323675114113 ) ) ;
#107069=CARTESIAN_POINT ( 'NONE',  ( 4.793709216081707858, 1.633822259641436903, 1.483752339651790653 ) ) ;
#107070=CARTESIAN_POINT ( 'NONE',  ( 0.7554163591718568993, -1.825703804718967316, -1.157005318491082901 ) ) ;
#107071=CARTESIAN_POINT ( 'NONE',  ( 3.696500153570709379, 1.422608671726926177, -1.429447704489300364 ) ) ;
#107074=CARTESIAN_POINT ( 'NONE',  ( -0.1229892814952095459, -1.709044814581164973, -0.8582256167319823881 ) ) ;
#107075=CARTESIAN_POINT ( 'NONE',  ( 1.077361674225948418, 1.530160568918725872, 1.313541346884481209 ) ) ;
#107079=CARTESIAN_POINT ( 'NONE',  ( 0.07536363704235481131, 0.6997989235110781969, -2.226667633679416447 ) ) ;
#107081=CARTESIAN_POINT ( 'NONE',  ( 6.516268831907007453, -1.911747763583053317, 0.05203757306279645223 ) ) ;
#107083=CARTESIAN_POINT ( 'NONE',  ( 0.2857447052702493662, -0.8859512962964136706, 1.647562673099879138 ) ) ;
#107084=CARTESIAN_POINT ( 'NONE',  ( 2.729704159269104924, 0.7212915320151757070, -1.883313052590728454 ) ) ;
#107088=CARTESIAN_POINT ( 'NONE',  ( 4.319037722229518650, 1.925386421186209507, 0.8538897750212376403 ) ) ;
#107093=CARTESIAN_POINT ( 'NONE',  ( 4.447524238883529435, -1.845004865869297905, 0.8223427699834483517 ) ) ;
#107096=CARTESIAN_POINT ( 'NONE',  ( 4.833375328034618335, -1.978455579520097762, 0.8711445904842631816 ) ) ;
#107102=CARTESIAN_POINT ( 'NONE',  ( 1.715514515588032030, -1.861668902569445283, -1.117036959414873465 ) ) ;
#107105=CARTESIAN_POINT ( 'NONE',  ( 0.9953642579336658969, -1.841430844361633845, 2.783310008858119066E-05 ) ) ;
#107107=CARTESIAN_POINT ( 'NONE',  ( 3.263397454411249399, 2.137687552337414587, -0.4822058812353549606 ) ) ;
#107109=CARTESIAN_POINT ( 'NONE',  ( 3.538171838403024516, 1.019457259465136101, -2.019903332531754803 ) ) ;
#107115=CARTESIAN_POINT ( 'NONE',  ( 3.831107792978345472, -1.636083747181043879, 0.6751729126634566924 ) ) ;
#107118=CARTESIAN_POINT ( 'NONE',  ( 1.325372091284286569, -0.05194335737490791277, 2.105495032795675847 ) ) ;
#107121=CARTESIAN_POINT ( 'NONE',  ( 0.9593497616274889728, 1.608103478905052119, 1.136861374779022604 ) ) ;
#107124=CARTESIAN_POINT ( 'NONE',  ( 5.396671993488243224, -1.769204348786549641, -0.3888369506312178703 ) ) ;
#107128=CARTESIAN_POINT ( 'NONE',  ( 4.627732503263369601, -1.150995203733524930, -1.474563928533303869 ) ) ;
#107131=CARTESIAN_POINT ( 'NONE',  ( 4.979381509686323426, -0.1069728651886258930, 2.067640925720988232 ) ) ;
#107141=CARTESIAN_POINT ( 'NONE',  ( 3.402741375674179114, 0.4741672551989496998, 1.903589013717405853 ) ) ;
#107142=CARTESIAN_POINT ( 'NONE',  ( 1.581407437776818581, 1.356094323556347181, -1.492024998029889860 ) ) ;
#107146=CARTESIAN_POINT ( 'NONE',  ( 2.090876104454452378, 1.629797177321444579, -0.9178172146045021629 ) ) ;
#107148=CARTESIAN_POINT ( 'NONE',  ( 3.656497369231588745, 2.003880934342232578, 0.1932520657266077191 ) ) ;
#107150=CARTESIAN_POINT ( 'NONE',  ( 2.829822700998831486, 0.7593016614581545864, -1.976571788296621834 ) ) ;
#107152=CARTESIAN_POINT ( 'NONE',  ( 4.492674960910642667, 2.029786422369950216, 0.4070406814440513665 ) ) ;
#107154=CARTESIAN_POINT ( 'NONE',  ( 0.04657986452102218927, -1.676603903080859492, 1.248863468804935151 ) ) ;
#107155=CARTESIAN_POINT ( 'NONE',  ( 6.720655732516655156, 7.629137130509086262, 2.673739711112704143 ) ) ;
#107156=CARTESIAN_POINT ( 'NONE',  ( 5.104447739783800841, -0.6163660037172628003, -1.718524672285254740 ) ) ;
#107164=CARTESIAN_POINT ( 'NONE',  ( 5.813130153884224605, 1.560705751063670377, -1.104717755519408984 ) ) ;
#107173=CARTESIAN_POINT ( 'NONE',  ( 5.343375128634678006, 0.3905785925618041610, -1.978055652833633271 ) ) ;
#107179=CARTESIAN_POINT ( 'NONE',  ( 2.360148646665951144, -1.969129416856093551, 0.04326586078102003657 ) ) ;
#107180=CARTESIAN_POINT ( 'NONE',  ( 4.903922820734956112, -1.081083478763317007, -1.701937824264573518 ) ) ;
#107182=CARTESIAN_POINT ( 'NONE',  ( 6.727182134110202938, 2.016807574165893513, 2.492494991173601182 ) ) ;
#107184=CARTESIAN_POINT ( 'NONE',  ( 5.050807487124363782, -1.850163549229045579, -1.174163402404400092 ) ) ;
#107186=CARTESIAN_POINT ( 'NONE',  ( 2.995051018759773420, 1.652986441767102743, -0.9890191681132395329 ) ) ;
#107189=CARTESIAN_POINT ( 'NONE',  ( -0.02244404828157658613, -0.004869073801674199918, -2.189079685368473527 ) ) ;
#107196=CARTESIAN_POINT ( 'NONE',  ( 5.987831981441136264, -1.833028718050220940, -0.1737628300680846560 ) ) ;
#107197=CARTESIAN_POINT ( 'NONE',  ( 3.317044347720001785, 1.585670248135360838, -1.240117154037506886 ) ) ;
#107198=CARTESIAN_POINT ( 'NONE',  ( 5.114793989753786185, 0.7273159113986256141, -2.180329384352611033 ) ) ;
#107200=CARTESIAN_POINT ( 'NONE',  ( 3.467479172597370596, -0.3673618142193516012, 1.824136687861827921 ) ) ;
#107207=CARTESIAN_POINT ( 'NONE',  ( 5.899963319545262763, -0.7533809947482277281, -1.950465142816688813 ) ) ;
#107214=CARTESIAN_POINT ( 'NONE',  ( 5.971300253285758863, 0.1196647562241616447, -1.720808320142935610 ) ) ;
#107216=CARTESIAN_POINT ( 'NONE',  ( 1.336079928753497681, 0.5043104442001166143, -1.659204044645303355 ) ) ;
#107220=CARTESIAN_POINT ( 'NONE',  ( 5.664936021742177807, 1.649023742746661192, -1.412335049966114253 ) ) ;
#107221=CARTESIAN_POINT ( 'NONE',  ( 4.635264976507449397, -1.668059998867366778, 0.7425182445051290436 ) ) ;
#107222=CARTESIAN_POINT ( 'NONE',  ( 2.324987154519737143, -1.791562868964852395, -0.7996954790665600221 ) ) ;
#107227=CARTESIAN_POINT ( 'NONE',  ( 3.774183692772983267, 2.104302197123971485, -0.2610650231627819062 ) ) ;
#107233=CARTESIAN_POINT ( 'NONE',  ( 2.131770371054972912, 1.982354287819853456, -0.5969549857752221023 ) ) ;
#107236=CARTESIAN_POINT ( 'NONE',  ( 3.721504678736448302, 1.905620783811642571, 1.141157194635911365 ) ) ;
#107238=CARTESIAN_POINT ( 'NONE',  ( 2.233388324916096845, 2.298236692437699791, 0.05235245155727624722 ) ) ;
#107240=CARTESIAN_POINT ( 'NONE',  ( 6.977413162628444354, -0.1478290182607009950, 2.029965231729473185 ) ) ;
#107246=CARTESIAN_POINT ( 'NONE',  ( -0.2106725631050176684, -0.004273297132624876912, -2.003483006309703995 ) ) ;
#107247=CARTESIAN_POINT ( 'NONE',  ( 3.381609400508314600, 1.093566088711795281, 1.333772831174476758 ) ) ;
#107248=CARTESIAN_POINT ( 'NONE',  ( 2.272673044126482189, -0.3494851828299733176, -1.985868527484459856 ) ) ;
#107249=CARTESIAN_POINT ( 'NONE',  ( 2.514614159817552430, -2.143548176638510938, 0.8305585572774812908 ) ) ;
#107250=CARTESIAN_POINT ( 'NONE',  ( 3.849113346294403382, -1.852342442990447813, 1.298737409825992062 ) ) ;
#107251=CARTESIAN_POINT ( 'NONE',  ( 5.725249284967181218, -0.05305106314347144553, 2.105570132020935237 ) ) ;
#107254=CARTESIAN_POINT ( 'NONE',  ( 3.426767255637660270, 0.04027588734063606429, 1.769438255327019593 ) ) ;
#107256=CARTESIAN_POINT ( 'NONE',  ( 0.07670252363861564115, -2.225146658028719582, -0.5502862128906602646 ) ) ;
#107257=CARTESIAN_POINT ( 'NONE',  ( 5.296754776809613041, 1.507285696749562476, 1.057021923447129197 ) ) ;
#107259=CARTESIAN_POINT ( 'NONE',  ( 5.525378525699438548, -1.388074942811763357, -1.695776126864618316 ) ) ;
#107262=CARTESIAN_POINT ( 'NONE',  ( 5.600075274486990828, 0.8424382930321882013, -1.891409743246947217 ) ) ;
#107263=CARTESIAN_POINT ( 'NONE',  ( -0.1706859984542466180, -1.561801110730935971, -1.275320528755889526 ) ) ;
#107265=CARTESIAN_POINT ( 'NONE',  ( 4.459546661884671970, 0.4205705884572363829, -1.879884317620848178 ) ) ;
#107268=CARTESIAN_POINT ( 'NONE',  ( 0.3697636260225238836, -1.880949819439242443, -1.181558314010826116 ) ) ;
#107278=CARTESIAN_POINT ( 'NONE',  ( 0.9417639971489067952, 1.314929008279978495, 1.456166070238865018 ) ) ;
#107281=CARTESIAN_POINT ( 'NONE',  ( 5.371523934717264304, -0.2895824386080196322, 1.940264742196501802 ) ) ;
#107284=CARTESIAN_POINT ( 'NONE',  ( 6.543834100630380846, 0.8322713294773576020, -1.995267709627518427 ) ) ;
#107288=CARTESIAN_POINT ( 'NONE',  ( 1.844777716111935861, -1.582881869529973562, 0.9963996312925410548 ) ) ;
#107289=CARTESIAN_POINT ( 'NONE',  ( 0.05276861106134726059, -1.135576942788417254, 1.310739833803043819 ) ) ;
#107291=CARTESIAN_POINT ( 'NONE',  ( 4.405938146338868933, -0.9375679901368579872, -1.981035393479456008 ) ) ;
#107292=CARTESIAN_POINT ( 'NONE',  ( 4.102763937057193999, -0.7201832649769298600, -2.192400882750038971 ) ) ;
#107293=CARTESIAN_POINT ( 'NONE',  ( 6.678986887005352813, -0.09631167155637165855, -2.058642716137318640 ) ) ;
#107294=CARTESIAN_POINT ( 'NONE',  ( 2.361185668158103379, 1.904436331314839137, -0.3790439726399745246 ) ) ;
#107297=CARTESIAN_POINT ( 'NONE',  ( 5.625269520628737752, 1.871107552910089122, 0.9978724776121964402 ) ) ;
#107299=CARTESIAN_POINT ( 'NONE',  ( 3.516250148862578584, -1.862017090670412767, 0.7743150488077471527 ) ) ;
#107303=CARTESIAN_POINT ( 'NONE',  ( 1.277666653898035021, 1.085793613588705853, 1.467558327050644484 ) ) ;
#107308=CARTESIAN_POINT ( 'NONE',  ( 5.998915433584960155, 1.686223865786851128, -1.184587077384538167 ) ) ;
#107313=CARTESIAN_POINT ( 'NONE',  ( 4.055335607603890224, -1.756228124781366917, 0.9972510931155349478 ) ) ;
#107314=CARTESIAN_POINT ( 'NONE',  ( 5.180443790456886077, 1.093758630767979412, 1.933306047416243567 ) ) ;
#107318=CARTESIAN_POINT ( 'NONE',  ( 4.452062314400541787, 2.060485596604546110, -0.04854883430290175134 ) ) ;
#107319=CARTESIAN_POINT ( 'NONE',  ( 3.692029868468839737, 1.730865839653324079, 1.034166058993556181 ) ) ;
#107326=CARTESIAN_POINT ( 'NONE',  ( 3.550157523342875709, 1.823840110401256931, -0.8594984857327039318 ) ) ;
#107327=CARTESIAN_POINT ( 'NONE',  ( 2.800538183361205302, 1.555518290611109800, 0.9846574483025125613 ) ) ;
#107329=CARTESIAN_POINT ( 'NONE',  ( 0.5929126122562259349, -2.290994082922478636, -0.2767204673215419852 ) ) ;
#107331=CARTESIAN_POINT ( 'NONE',  ( 3.515052679271633895, 1.952536648612019921, 0.9277410485990513767 ) ) ;
#107336=CARTESIAN_POINT ( 'NONE',  ( 2.952824900933643804, 1.623659768481898302, 1.626969957801235989 ) ) ;
#107338=CARTESIAN_POINT ( 'NONE',  ( 2.219420098953532428, -1.815089452277141691, 0.4520615115926190919 ) ) ;
#107339=CARTESIAN_POINT ( 'NONE',  ( 5.577018171352951192, -0.04780089932613153236, -1.971040553531088868 ) ) ;
#107343=CARTESIAN_POINT ( 'NONE',  ( 0.9267433102794273569, 1.311770220233858586, -1.774563083084364834 ) ) ;
#107348=CARTESIAN_POINT ( 'NONE',  ( 6.280149219824591178, -1.055055557545642175, 1.665224566959803143 ) ) ;
#107349=CARTESIAN_POINT ( 'NONE',  ( 6.112023189137078205, -2.291079414021851779, 0.2760875835842706016 ) ) ;
#107350=CARTESIAN_POINT ( 'NONE',  ( 6.672303541529164050, -0.8785034406106060345, -1.640621795851913367 ) ) ;
#107351=CARTESIAN_POINT ( 'NONE',  ( 3.291897078901334428, -1.381674118267547602, -1.531590470265832726 ) ) ;
#107359=CARTESIAN_POINT ( 'NONE',  ( 5.898927382237683759, 0.4177183949424836396, 2.130464630886391486 ) ) ;
#107363=CARTESIAN_POINT ( 'NONE',  ( 5.442854017605395889, -1.455216020186438364, -1.127989967910733915 ) ) ;
#107365=CARTESIAN_POINT ( 'NONE',  ( 6.620655732516632419, 1.270823175217004941, 2.040803978124502205 ) ) ;
#107368=CARTESIAN_POINT ( 'NONE',  ( 6.579017896966585788, -0.1030185651522512180, -2.260299859776133236 ) ) ;
#107373=CARTESIAN_POINT ( 'NONE',  ( 0.4867802866235851345, -1.800715477623024086, -0.6440170976053718466 ) ) ;
#107374=CARTESIAN_POINT ( 'NONE',  ( 1.410649291501327118, 1.558696297929580199, 0.8383436984091273692 ) ) ;
#107375=CARTESIAN_POINT ( 'NONE',  ( 0.02974158317493520720, -1.875378228685410376, 0.3729384364157954379 ) ) ;
#107376=CARTESIAN_POINT ( 'NONE',  ( 4.753012104044548991, -1.692955597047377747, 1.252381512178860401 ) ) ;
#107378=CARTESIAN_POINT ( 'NONE',  ( 3.778834734487185099, 1.616410871901182711, -1.027684692424314594 ) ) ;
#107379=CARTESIAN_POINT ( 'NONE',  ( -0.02244404828157393894, 7.629137130509076492, -2.789100637983292774 ) ) ;
#107381=CARTESIAN_POINT ( 'NONE',  ( 4.457443581450992731, 1.580467340599530424, 1.175029403372893855 ) ) ;
#107382=CARTESIAN_POINT ( 'NONE',  ( 6.170177014438331220, 2.014108787598484440, -0.1525786406279260876 ) ) ;
#107384=CARTESIAN_POINT ( 'NONE',  ( 2.887410755087606695, 1.321643875934110479, 1.324118206929347563 ) ) ;
#107385=CARTESIAN_POINT ( 'NONE',  ( 5.496639145235802104, -0.4250261254647030307, -1.671567591930831043 ) ) ;
#107387=CARTESIAN_POINT ( 'NONE',  ( 2.596532132193625664, -2.201043451360765957, -0.1612727490639675743 ) ) ;
#107391=CARTESIAN_POINT ( 'NONE',  ( 6.637165056451467038, -0.09505199798197358496, -1.959668910398344233 ) ) ;
#107398=CARTESIAN_POINT ( 'NONE',  ( 1.539598694730393680, 1.913698299121506352, -0.7905179490511196061 ) ) ;
#107402=CARTESIAN_POINT ( 'NONE',  ( 6.569000932001921811, -1.639521903533578850, 1.344440124909966450 ) ) ;
#107408=CARTESIAN_POINT ( 'NONE',  ( 5.888046020683161075, -0.05228737891407529703, 2.015604419750731680 ) ) ;
#107409=CARTESIAN_POINT ( 'NONE',  ( 4.891753643660703865, -1.905893201010636195, 0.1940691045876908327 ) ) ;
#107410=CARTESIAN_POINT ( 'NONE',  ( 6.639320575229256782, 3.693993153770461113, 2.517469677323687538 ) ) ;
#107411=CARTESIAN_POINT ( 'NONE',  ( 2.859115728684503477, 0.3189004193784421015, -2.168101852914063876 ) ) ;
#107413=CARTESIAN_POINT ( 'NONE',  ( 1.880979024232478425, -1.749874716401520036, -0.7718601483891265325 ) ) ;
#107416=CARTESIAN_POINT ( 'NONE',  ( 6.521125090989952078, -1.891168486443073116, 0.9521521135891182208 ) ) ;
#107418=CARTESIAN_POINT ( 'NONE',  ( 5.829655996829377962, 1.081331853127937448, -1.906115348727636549 ) ) ;
#107420=CARTESIAN_POINT ( 'NONE',  ( 2.731144534912807842, -1.610196803864067938, 0.6186328129335681991 ) ) ;
#107433=CARTESIAN_POINT ( 'NONE',  ( 2.842218536208180435, 1.004546245467073717, -1.507189720918320486 ) ) ;
#107437=CARTESIAN_POINT ( 'NONE',  ( 3.967288593341521175, -1.508176260789632739, -1.003069782103764185 ) ) ;
#107442=CARTESIAN_POINT ( 'NONE',  ( 5.547250370032299038, 1.641257983771953866, -0.8773172063531119447 ) ) ;
#107444=CARTESIAN_POINT ( 'NONE',  ( 3.022943291168778579, -1.688106736905025995, 0.9054777632113325536 ) ) ;
#107445=CARTESIAN_POINT ( 'NONE',  ( 0.9381830591699467092, 1.797733097909786304, 0.3167546781352030272 ) ) ;
#107453=CARTESIAN_POINT ( 'NONE',  ( 5.717622241336643540, 0.3879015478767386949, -1.930678852912662391 ) ) ;
#107457=CARTESIAN_POINT ( 'NONE',  ( 1.464907584622468173, 0.1521959979720881595, -2.085151142678423497 ) ) ;
#107458=CARTESIAN_POINT ( 'NONE',  ( 5.983413252614310451, 1.779745538724048171, -0.7376744472527080321 ) ) ;
#107460=CARTESIAN_POINT ( 'NONE',  ( 2.889462524698828361, 1.289687736819044472, 1.292329967842877014 ) ) ;
#107461=CARTESIAN_POINT ( 'NONE',  ( 2.895379187063460869, 1.892502543702856865, -1.135010264495312837 ) ) ;
#107463=CARTESIAN_POINT ( 'NONE',  ( 0.7207899753199145110, 1.446443371814851941, -1.251069288267861346 ) ) ;
#107465=CARTESIAN_POINT ( 'NONE',  ( 1.152721088564850671, -0.4753370964276568134, -1.911210599630641882 ) ) ;
#107466=CARTESIAN_POINT ( 'NONE',  ( 2.999484396081523396, -1.939716604588328508, 0.09806999327347488971 ) ) ;
#107470=CARTESIAN_POINT ( 'NONE',  ( 6.244940914744545601, -0.2718465296328761438, -1.840820509183779263 ) ) ;
#107476=CARTESIAN_POINT ( 'NONE',  ( 2.138457411672203712, 0.4836887423533155483, 2.137355272389021899 ) ) ;
#107481=CARTESIAN_POINT ( 'NONE',  ( 2.420285107995377327, 1.192830232448302441, -1.382225081888274643 ) ) ;
#107482=CARTESIAN_POINT ( 'NONE',  ( 5.893767612163585135, -2.000732204962274441, 0.2516274335107801519 ) ) ;
#107485=CARTESIAN_POINT ( 'NONE',  ( 6.925078400183550364, 2.979478345347878587, 2.309228228758605450 ) ) ;
#107487=CARTESIAN_POINT ( 'NONE',  ( 2.033698780422585006, -1.258094322230184581, -1.459052628860134648 ) ) ;
#107488=CARTESIAN_POINT ( 'NONE',  ( 5.647302737930705696, 1.731814717071546772, -0.9215059220915235993 ) ) ;
#107496=CARTESIAN_POINT ( 'NONE',  ( 5.278213287142951238, -1.102824678039602269, -1.751873656341627505 ) ) ;
#107498=CARTESIAN_POINT ( 'NONE',  ( 5.643294731490863470, 0.9288382957042642385, 2.102849567203187053 ) ) ;
#107502=CARTESIAN_POINT ( 'NONE',  ( -0.01123377539814351088, -0.5141151231248282105, -2.242550872947962404 ) ) ;
#107505=CARTESIAN_POINT ( 'NONE',  ( 4.611236491138351212, -1.904185011576609465, 0.3803074441277309314 ) ) ;
#107508=CARTESIAN_POINT ( 'NONE',  ( 6.047114369478562956, 0.1942372860762129894, 1.902532258075719351 ) ) ;
#107509=CARTESIAN_POINT ( 'NONE',  ( 6.581054485068423610, -0.09077197429533871709, -1.722499283940544634 ) ) ;
#107510=CARTESIAN_POINT ( 'NONE',  ( 6.192592252150040721, 1.490973663936447480, -1.357864438797616868 ) ) ;
#107514=CARTESIAN_POINT ( 'NONE',  ( 1.113355907768112774, -2.039295093617380594, 0.4597149659458180104 ) ) ;
#107515=CARTESIAN_POINT ( 'NONE',  ( 1.340303658288226396, 0.3404796732740902887, 1.736595688552546424 ) ) ;
#107518=CARTESIAN_POINT ( 'NONE',  ( 4.048992419199006321, -1.904907007256863904, -1.274792539085588539 ) ) ;
#107519=CARTESIAN_POINT ( 'NONE',  ( 2.536699030922508591, -1.289252169270055370, -1.169197435003018315 ) ) ;
#107520=STYLED_ITEM ( 'NONE', ( #124267 ), #168834 ) ;
#107521=CARTESIAN_POINT ( 'NONE',  ( 2.319350913329641717, -1.342983818224493531, 1.096632721805221200 ) ) ;
#107523=CARTESIAN_POINT ( 'NONE',  ( 1.732617751151921404, -1.765751579927745007, -0.5880843478397956847 ) ) ;
#107524=CARTESIAN_POINT ( 'NONE',  ( 2.893231026729268685, 0.2635377995367886861, 2.155045766152231757 ) ) ;
#107526=CARTESIAN_POINT ( 'NONE',  ( 3.784388871581423786, -0.6371526190629381858, -1.913262240507591416 ) ) ;
#107527=CARTESIAN_POINT ( 'NONE',  ( 1.812500000000001554, 1.451031289061194052, 1.451031289061046170 ) ) ;
#107530=CARTESIAN_POINT ( 'NONE',  ( 0.7625677631861004224, -1.397537113076696036, 1.326088851308028449 ) ) ;
#107532=CARTESIAN_POINT ( 'NONE',  ( 4.887093103977882436, -2.092044318328468488, -0.7474293538695072625 ) ) ;
#107534=CARTESIAN_POINT ( 'NONE',  ( -0.2108831679770959699, 2.036692374882024037, -2.313561348563981657 ) ) ;
#107538=CARTESIAN_POINT ( 'NONE',  ( 0.06548277170575435291, -1.780103896928236118, 1.328506668625312859 ) ) ;
#107539=CARTESIAN_POINT ( 'NONE',  ( 5.090269282739749102, 1.010147525469132557, -1.681691772506640481 ) ) ;
#107543=CARTESIAN_POINT ( 'NONE',  ( 5.940765808339826037, 0.4328084161881738945, 2.220481174026817772 ) ) ;
#107545=CARTESIAN_POINT ( 'NONE',  ( 2.734894939886590937, -1.973151212864039605, -0.6010335745895727388 ) ) ;
#107547=ORIENTED_EDGE ( 'NONE', *, *, #21794, .F. ) ;
#107550=CARTESIAN_POINT ( 'NONE',  ( 4.270664716992385479, -1.744513905240049567, -0.6754176267826096369 ) ) ;
#107551=CARTESIAN_POINT ( 'NONE',  ( 3.304998880318401167, 1.097559245703746855, -1.342624595404175780 ) ) ;
#107552=CARTESIAN_POINT ( 'NONE',  ( 1.680815414582544243, 1.200268842161634097, 1.260572391871515263 ) ) ;
#107553=CARTESIAN_POINT ( 'NONE',  ( 1.013678699313476095, -2.235087565253154107, 0.5086484811528817485 ) ) ;
#107554=CARTESIAN_POINT ( 'NONE',  ( 0.5521677985501523001, 0.6901698128830742185, -2.096122547012829962 ) ) ;
#107555=CARTESIAN_POINT ( 'NONE',  ( 4.581631739359020017, -0.9839878911236143999, 1.844693108308750551 ) ) ;
#107556=CARTESIAN_POINT ( 'NONE',  ( 5.982362851901904754, -0.2873240852911072007, -1.920464370370161600 ) ) ;
#107559=CARTESIAN_POINT ( 'NONE',  ( 0.1588275700346117869, 1.163271727376416376, 1.646837250247008777 ) ) ;
#107560=CARTESIAN_POINT ( 'NONE',  ( 0.0004480315400831600455, -0.9938866557669153723, 1.873244595478529728 ) ) ;
#107565=CARTESIAN_POINT ( 'NONE',  ( 4.406759617291758246, 1.409692282476209924, -1.160130723419292353 ) ) ;
#107566=CARTESIAN_POINT ( 'NONE',  ( 1.835297179245497068, 0.2165863673247066801, 2.196102686035047213 ) ) ;
#107573=CARTESIAN_POINT ( 'NONE',  ( 1.336200995665462354, -1.125576746034629094, -1.676869184967361814 ) ) ;
#107576=CARTESIAN_POINT ( 'NONE',  ( 2.799463494909336880, -1.375353214051901807, -1.253764128285854706 ) ) ;
#107583=CARTESIAN_POINT ( 'NONE',  ( 3.404746562951189937, 1.438594061741470753, -1.123979961188771304 ) ) ;
#107587=CARTESIAN_POINT ( 'NONE',  ( 0.1745346383498986020, -0.7352478164647980874, -1.569626033853884106 ) ) ;
#107588=CARTESIAN_POINT ( 'NONE',  ( 6.509700743154069436, -0.8726169035938921015, -1.621212818125779220 ) ) ;
#107590=CARTESIAN_POINT ( 'NONE',  ( 4.776155900897590456, 1.325808183606682622, 1.888659687595494407 ) ) ;
#107592=CARTESIAN_POINT ( 'NONE',  ( 0.6497718435918962143, 0.6490781098625525436, -1.955935974237718256 ) ) ;
#107595=CARTESIAN_POINT ( 'NONE',  ( 6.081499288503829703, 1.550124037452194958, -1.697122508851423905 ) ) ;
#107598=CARTESIAN_POINT ( 'NONE',  ( 5.225416543158964977, -1.776039340814106637, 0.5876355328483380269 ) ) ;
#107600=CARTESIAN_POINT ( 'NONE',  ( 1.880979024232478425, -1.749874716401520036, -0.7718601483891265325 ) ) ;
#107602=CARTESIAN_POINT ( 'NONE',  ( 4.758537496233657293, 0.8426522330295079799, 2.039869969286691731 ) ) ;
#107603=CARTESIAN_POINT ( 'NONE',  ( 4.768830992622041798, -0.2625661012465319022, -2.100967800990781509 ) ) ;
#107605=CARTESIAN_POINT ( 'NONE',  ( 6.883263157960369583, 7.629137130509070275, 2.546189081643289942 ) ) ;
#107608=CARTESIAN_POINT ( 'NONE',  ( 2.116686800396328838, -1.088458544310743736, -2.034734824932447506 ) ) ;
#107609=CARTESIAN_POINT ( 'NONE',  ( 3.209375601822930690, -1.602329130913646926, -1.131729396966949963 ) ) ;
#107611=CARTESIAN_POINT ( 'NONE',  ( 6.860222192644392258, -2.062229998417430377, 0.04471529749722201463 ) ) ;
#107615=CARTESIAN_POINT ( 'NONE',  ( 5.384000029850495750, -2.016708404008683786, 0.004832792792668073358 ) ) ;
#107617=CARTESIAN_POINT ( 'NONE',  ( -0.1608832656953863849, 7.629137130509072939, -2.497055476982701361 ) ) ;
#107620=CARTESIAN_POINT ( 'NONE',  ( 1.868283874303029446, -2.155004017527381244, 0.2628641719419066991 ) ) ;
#107625=CARTESIAN_POINT ( 'NONE',  ( 0.9485937975238111219, 0.5957422345228384764, 1.972812641012058776 ) ) ;
#107626=CARTESIAN_POINT ( 'NONE',  ( -0.02224634325196857970, 4.078913133451218087, -2.843768138527980049 ) ) ;
#107627=CARTESIAN_POINT ( 'NONE',  ( 6.727182134110207379, 6.038252846411742425, 2.505853901327475874 ) ) ;
#107630=CARTESIAN_POINT ( 'NONE',  ( 3.756429630051653756, 1.903336793139897010, 0.1845653119916731144 ) ) ;
#107632=CARTESIAN_POINT ( 'NONE',  ( 5.049538948550310380, 0.5532318831848512808, -1.681206329525422483 ) ) ;
#107636=CARTESIAN_POINT ( 'NONE',  ( 6.239839116978105338, 1.910102730490463641, -0.1462054744419109820 ) ) ;
#107638=CARTESIAN_POINT ( 'NONE',  ( 0.9595327444568906294, 1.691550050060253829, 1.193477315110213599 ) ) ;
#107640=CARTESIAN_POINT ( 'NONE',  ( 6.508674657442179878, 1.384610780642284711, -1.258058027910214927 ) ) ;
#107641=CARTESIAN_POINT ( 'NONE',  ( 2.596107596775329540, -1.820790993511243849, -0.1344670722737417168 ) ) ;
#107642=CARTESIAN_POINT ( 'NONE',  ( 6.006501602161061548, -0.7906231143557163055, -2.060575041408031272 ) ) ;
#107645=CARTESIAN_POINT ( 'NONE',  ( 2.752447824977616087, -2.056971473714273468, -0.1544007921008266060 ) ) ;
#107651=CARTESIAN_POINT ( 'NONE',  ( 0.7554163591718568993, -1.825703804718967316, -1.157005318491082901 ) ) ;
#107654=CARTESIAN_POINT ( 'NONE',  ( 5.406714943436663035, 0.5975561702324573288, 1.982271326387271770 ) ) ;
#107656=CARTESIAN_POINT ( 'NONE',  ( 3.374459016379764087, -1.290570702369205014, 1.733878788530067938 ) ) ;
#107658=CARTESIAN_POINT ( 'NONE',  ( 2.649087060217536926, 0.2492969965636695762, 2.004170148778378735 ) ) ;
#107659=CARTESIAN_POINT ( 'NONE',  ( 2.189831975649577878, -1.279155337443920404, -1.487614327915102841 ) ) ;
#107666=CARTESIAN_POINT ( 'NONE',  ( 1.551970632248239612, 1.040795554343958429, 1.727062486439542965 ) ) ;
#107668=CARTESIAN_POINT ( 'NONE',  ( 6.462441986028243157, -2.002789442531027309, -0.8901952361822994542 ) ) ;
#107670=CARTESIAN_POINT ( 'NONE',  ( 5.467032840998240495, -1.503656711810175350, 1.181500457595338505 ) ) ;
#107674=CARTESIAN_POINT ( 'NONE',  ( 3.005482631727268039, -1.942536929278560365, 0.5405117225928540714 ) ) ;
#107677=CARTESIAN_POINT ( 'NONE',  ( -0.005825499538506145533, -0.3671160670182890273, -1.691004160741523155 ) ) ;
#107682=CARTESIAN_POINT ( 'NONE',  ( 4.217926093758464390, -0.9595593063399066036, -1.605508702137818045 ) ) ;
#107684=CARTESIAN_POINT ( 'NONE',  ( 1.622023338512183832, 2.040292009219225378, -0.3499636251925800079 ) ) ;
#107688=CARTESIAN_POINT ( 'NONE',  ( 0.03478015955125923070, -1.617804660175032661, 1.203375172262765913 ) ) ;
#107689=CARTESIAN_POINT ( 'NONE',  ( 0.01741795466771427214, -0.4834593703179098645, 1.745828368453090418 ) ) ;
#107695=CARTESIAN_POINT ( 'NONE',  ( 1.170277241841523264, -0.8789641444944886750, -1.754005360843587047 ) ) ;
#107697=CARTESIAN_POINT ( 'NONE',  ( 6.222283718431360633, 1.895538691748376081, 0.2756032664797089526 ) ) ;
#107704=CARTESIAN_POINT ( 'NONE',  ( 2.782270202741622178, -1.112240752214749273, 1.853481441253836071 ) ) ;
#107708=CARTESIAN_POINT ( 'NONE',  ( 5.877927443470423619, 1.089437568142386015, 1.464738158297604453 ) ) ;
#107710=CARTESIAN_POINT ( 'NONE',  ( 1.546097919708361079, 1.968910558940571320, 0.1009371868440200049 ) ) ;
#107711=CARTESIAN_POINT ( 'NONE',  ( 3.691585721427274258, 1.799035686688513325, -0.6489376663148455071 ) ) ;
#107714=CARTESIAN_POINT ( 'NONE',  ( 5.512145389550558328, 1.967385609537531277, -0.09471018678799088264 ) ) ;
#107716=CARTESIAN_POINT ( 'NONE',  ( 6.444875487053635332, -1.562622460104126310, -1.153009275138028089 ) ) ;
#107720=CARTESIAN_POINT ( 'NONE',  ( 6.521762860236213655, -0.4636855090699961712, 2.076960040381255812 ) ) ;
#107723=CARTESIAN_POINT ( 'NONE',  ( 3.404848115249804685, -0.3755933644018424888, -1.874856250562627391 ) ) ;
#107725=CARTESIAN_POINT ( 'NONE',  ( 0.8509352111321017986, 0.6423128672003556305, 2.111239891224323983 ) ) ;
#107727=CARTESIAN_POINT ( 'NONE',  ( -0.04057498839846879202, -1.478066481919372510, -1.213044814162365981 ) ) ;
#107730=CARTESIAN_POINT ( 'NONE',  ( 6.234959169399230561, 0.1841439077357870380, 1.816378869960999509 ) ) ;
#107731=CARTESIAN_POINT ( 'NONE',  ( 2.488806849732328796, 2.007603858877416769, 0.5053560088097222014 ) ) ;
#107736=CARTESIAN_POINT ( 'NONE',  ( 6.754772315933175619, -1.444328698515121800, 1.188528157999017454 ) ) ;
#107742=CARTESIAN_POINT ( 'NONE',  ( 6.777182134110200096, 7.629137130509069387, 2.789055895399249696 ) ) ;
#107744=CARTESIAN_POINT ( 'NONE',  ( 6.825078400183556049, 7.053092130845653784, 2.453807127456457238 ) ) ;
#107746=CARTESIAN_POINT ( 'NONE',  ( 5.361839092321889488, -0.05056905708066515570, -1.733610765856267388 ) ) ;
#107748=CARTESIAN_POINT ( 'NONE',  ( 2.500909639826456754, 0.4493149015136475022, 2.020762751476639529 ) ) ;
#107749=CARTESIAN_POINT ( 'NONE',  ( 3.691103677939993499, 1.816986910410453682, 1.086596289330623799 ) ) ;
#107752=CARTESIAN_POINT ( 'NONE',  ( 1.358185265713553136, -1.969629313231166856, -0.005369267927731942967 ) ) ;
#107756=CARTESIAN_POINT ( 'NONE',  ( 3.310744302307960574, 2.072215845705066339, 0.9802597712869900448 ) ) ;
#107757=CARTESIAN_POINT ( 'NONE',  ( 1.383131112650197281, 1.687622997524572677, -0.6969523973551354779 ) ) ;
#107761=CARTESIAN_POINT ( 'NONE',  ( 3.111590725901419940, 1.589763268213672420, 1.235112918372171187 ) ) ;
#107762=CARTESIAN_POINT ( 'NONE',  ( 3.801568999928582659, -1.482573837031101016, -1.284759613706359271 ) ) ;
#107766=CARTESIAN_POINT ( 'NONE',  ( 5.630836714711354496, -1.890471120482087652, 0.8929869209393003215 ) ) ;
#107767=CARTESIAN_POINT ( 'NONE',  ( 4.662845455860040289, -1.581648675543185334, -0.7943582009959786472 ) ) ;
#107769=CARTESIAN_POINT ( 'NONE',  ( 0.6213436022244859247, -2.079703760468250451, 0.6910661131078955632 ) ) ;
#107770=CARTESIAN_POINT ( 'NONE',  ( 5.595574051893665413, -1.740516469239574704, 0.006108698158355239591 ) ) ;
#107773=CARTESIAN_POINT ( 'NONE',  ( 6.381448165025822128, -0.6081200552338487109, -2.216719476268604438 ) ) ;
#107775=CARTESIAN_POINT ( 'NONE',  ( 5.079290571759123019, 1.194821443462086963, -1.256652284620445759 ) ) ;
#107776=CARTESIAN_POINT ( 'NONE',  ( 6.004372733575126020, 2.168386774327632160, 0.1126981005201161401 ) ) ;
#107778=CARTESIAN_POINT ( 'NONE',  ( -0.04742653102243841318, -1.377616979729365809, 1.608019283586498371 ) ) ;
#107779=CARTESIAN_POINT ( 'NONE',  ( 3.156250000000002665, -1.895863743164019288, 0.7852924748301466362 ) ) ;
#107780=CARTESIAN_POINT ( 'NONE',  ( 6.827182134110224787, 2.015384445464900587, 2.492173930675382731 ) ) ;
#107781=CARTESIAN_POINT ( 'NONE',  ( 4.331023931135844940, 0.09395156538319178463, 1.924209479612617235 ) ) ;
#107783=CARTESIAN_POINT ( 'NONE',  ( 1.278328015487300462, 2.187630646761177466, -0.3845124374818161828 ) ) ;
#107788=CARTESIAN_POINT ( 'NONE',  ( 2.315342353584739055, 1.782219222887641674, -1.325647956807120220 ) ) ;
#107790=CARTESIAN_POINT ( 'NONE',  ( -0.02900071798685523866, 4.082342745036794618, -2.728474045032194262 ) ) ;
#107795=CARTESIAN_POINT ( 'NONE',  ( 0.8971115437808926396, -0.9091470795906559932, -1.799921601489597123 ) ) ;
#107797=CARTESIAN_POINT ( 'NONE',  ( 0.2333540202161610289, 0.003568502611739353923, -2.045944795905803471 ) ) ;
#107801=CARTESIAN_POINT ( 'NONE',  ( 0.9304724923206836307, 0.1222484634449630542, 1.765570801851876537 ) ) ;
#107802=CARTESIAN_POINT ( 'NONE',  ( 0.4049229342097167006, -1.081068455937021611, -1.701946057285643743 ) ) ;
#107803=CARTESIAN_POINT ( 'NONE',  ( 5.477983384163819025, -1.699738153848131983, -0.3734572171999461232 ) ) ;
#107804=CARTESIAN_POINT ( 'NONE',  ( 4.019262574452024062, -2.193609252165360513, 0.6655472109698862271 ) ) ;
#107806=CARTESIAN_POINT ( 'NONE',  ( 2.589598559577494186, -1.836209955096680613, -0.1354230481333124070 ) ) ;
#107808=CARTESIAN_POINT ( 'NONE',  ( 2.854317205943053271, 0.6132515345431620579, 1.719634925709014439 ) ) ;
#107809=CARTESIAN_POINT ( 'NONE',  ( 3.902970337090125863, -1.038992709432768891, -1.728002613881730598 ) ) ;
#107811=CARTESIAN_POINT ( 'NONE',  ( 2.518781164845237175, 1.478067295746248400, -1.713045486838754794 ) ) ;
#107813=CARTESIAN_POINT ( 'NONE',  ( 5.508848719172433128, 1.596710022150628294, -1.373279487321391379 ) ) ;
#107815=CARTESIAN_POINT ( 'NONE',  ( 2.717306809760032138, -1.800131872397674471, -1.022606600864908399 ) ) ;
#107818=CARTESIAN_POINT ( 'NONE',  ( 4.424552244980545446, -0.9075887007226298708, -1.916591080935086788 ) ) ;
#107821=CARTESIAN_POINT ( 'NONE',  ( 0.5219392174641559468, -1.029590632097213687, -1.628125521969860712 ) ) ;
#107828=CARTESIAN_POINT ( 'NONE',  ( 0.7389115964958146154, 1.317144317036992973, -1.788695212975628168 ) ) ;
#107829=CARTESIAN_POINT ( 'NONE',  ( 2.256984296129550760, -1.628445616851754263, 1.335386477757320778 ) ) ;
#107832=CARTESIAN_POINT ( 'NONE',  ( 6.719592977537645062, 0.3186052404706584129, -1.833303987817246794 ) ) ;
#107837=CARTESIAN_POINT ( 'NONE',  ( 0.2113915902133572944, 1.759560880827226947, -1.183302968686468226 ) ) ;
#107839=CARTESIAN_POINT ( 'NONE',  ( 3.525789274851616639, 1.914599547803575330, -0.4273510147508317591 ) ) ;
#107840=CARTESIAN_POINT ( 'NONE',  ( 2.219795081190904629, -2.096929600374438429, 0.5247480557022954351 ) ) ;
#107844=CARTESIAN_POINT ( 'NONE',  ( 3.152039231231161587, -1.317153252834550425, 1.137565551706197775 ) ) ;
#107851=CARTESIAN_POINT ( 'NONE',  ( 2.038435264984053585, 1.930122609968443204, -0.5825652091262025767 ) ) ;
#107852=CARTESIAN_POINT ( 'NONE',  ( 6.825078400183554272, 2.951006455646578264, 2.596623860847916188 ) ) ;
#107854=CARTESIAN_POINT ( 'NONE',  ( 1.885558555406470660, 1.358073900086468333, 1.429321910850362753 ) ) ;
#107862=CARTESIAN_POINT ( 'NONE',  ( 1.945969044768879552, -1.321035068824018222, -1.527795347589502972 ) ) ;
#107864=CARTESIAN_POINT ( 'NONE',  ( 5.368347952151684588, 1.131674353116480569, 2.010972138180310065 ) ) ;
#107865=CARTESIAN_POINT ( 'NONE',  ( 6.848121815800094936, -0.8396676627679277027, 1.771385694100804375 ) ) ;
#107866=CARTESIAN_POINT ( 'NONE',  ( 2.676550354755039773, 1.285117694784821518, -1.482265789204496143 ) ) ;
#107868=CARTESIAN_POINT ( 'NONE',  ( 0.3873425458618061645, -0.6819987885887255352, -1.897696807414723574 ) ) ;
#107870=CARTESIAN_POINT ( 'NONE',  ( 1.850927149041701192, -1.938055702826226190, -0.8530577433697658085 ) ) ;
#107874=CARTESIAN_POINT ( 'NONE',  ( 2.396224210035051261, 1.478860665732561808, -1.096489538662905217 ) ) ;
#107878=CARTESIAN_POINT ( 'NONE',  ( 3.217144136595586179, 1.669276650691432495, -1.307696563879121365 ) ) ;
#107879=CARTESIAN_POINT ( 'NONE',  ( 0.6031360380127914755, -1.832534659106283659, 0.1778487281504093076 ) ) ;
#107883=CARTESIAN_POINT ( 'NONE',  ( 4.534483719690214798, 2.020231433191475467, 0.4058933888440272031 ) ) ;
#107885=CARTESIAN_POINT ( 'NONE',  ( 1.135996871135702024, 0.3593859243370273182, 1.805655672011026391 ) ) ;
#107891=CARTESIAN_POINT ( 'NONE',  ( 1.559489335033688251, -1.894147805384650995, -1.132260830144316888 ) ) ;
#107892=CARTESIAN_POINT ( 'NONE',  ( 3.462467831702148668, 1.013738371934786331, 2.022624228200241348 ) ) ;
#107895=CARTESIAN_POINT ( 'NONE',  ( 3.392628153686805259, -1.747241832701627473, -0.4783254123041839057 ) ) ;
#107897=CARTESIAN_POINT ( 'NONE',  ( 2.782342135839787289, -0.5608490805640730104, -1.831745072482870107 ) ) ;
#107898=CARTESIAN_POINT ( 'NONE',  ( 4.422371208857902580, 0.9731212702417373350, 1.827393648576709717 ) ) ;
#107900=CARTESIAN_POINT ( 'NONE',  ( 2.412907133309648788, 1.760172955399338823, 0.8881188249313717309 ) ) ;
#107901=CARTESIAN_POINT ( 'NONE',  ( 1.254767684091241620, -1.520462189517374219, 1.182783339890740359 ) ) ;
#107902=CARTESIAN_POINT ( 'NONE',  ( 3.379631771358857950, 1.185797501207178861, 1.446808710765794315 ) ) ;
#107903=CARTESIAN_POINT ( 'NONE',  ( 2.772455145383013519, 1.235390390761299306, 1.949004725048721243 ) ) ;
#107904=CARTESIAN_POINT ( 'NONE',  ( 3.965176940185519250, 1.595341564286660629, 0.9581005465538834365 ) ) ;
#107909=CARTESIAN_POINT ( 'NONE',  ( 0.06524607375175436874, -1.882416456675739092, -0.9446200181052357703 ) ) ;
#107914=CARTESIAN_POINT ( 'NONE',  ( 2.057031522680652369, 0.4693188842763912905, 2.067847215655476134 ) ) ;
#107915=CARTESIAN_POINT ( 'NONE',  ( 0.1936255187755825669, 1.883021768735486434, -0.7310382463305180600 ) ) ;
#107918=ADVANCED_FACE ( 'NONE', ( #48313 ), #178245, .F. ) ;
#107920=CARTESIAN_POINT ( 'NONE',  ( 0.8081717762262634608, -2.151237856378166224, 0.2110218573620133986 ) ) ;
#107922=CARTESIAN_POINT ( 'NONE',  ( 6.925078400183593885, 7.629137130509070275, 2.455651831298297338 ) ) ;
#107925=CARTESIAN_POINT ( 'NONE',  ( 5.296111364736042937, -0.9110065213352031011, -1.799124599017036585 ) ) ;
#107929=CARTESIAN_POINT ( 'NONE',  ( 0.3392369075362114961, 0.3904986559340599128, 2.228413801644222758 ) ) ;
#107933=CARTESIAN_POINT ( 'NONE',  ( 0.2631137269465182449, 1.787087189245086583, -0.6902753917677264539 ) ) ;
#107937=CARTESIAN_POINT ( 'NONE',  ( 3.263966975432155415, 0.7763617936313322865, 1.540355606630551710 ) ) ;
#107940=CARTESIAN_POINT ( 'NONE',  ( 0.7722622890447777833, -1.663610408097391691, -0.6040080933595278756 ) ) ;
#107941=CARTESIAN_POINT ( 'NONE',  ( 2.244791168117025837, 1.953224514136771006, 0.4868699220301163089 ) ) ;
#107942=CARTESIAN_POINT ( 'NONE',  ( 4.489439581592091777, 1.972811803287272348, -0.9889974963176446643 ) ) ;
#107945=CARTESIAN_POINT ( 'NONE',  ( 3.826904873358004888, 1.498484187726952799, -1.500593194838243605 ) ) ;
#107946=CARTESIAN_POINT ( 'NONE',  ( 3.198842376697589085, 1.824128004127192559, 0.8596145101084637918 ) ) ;
#107947=CARTESIAN_POINT ( 'NONE',  ( 3.199259029290311140, 1.635763741490828593, -0.7788767334107206119 ) ) ;
#107951=CARTESIAN_POINT ( 'NONE',  ( 1.006479672118578916, 1.419055151971573059, -1.218976214888117804 ) ) ;
#107953=CARTESIAN_POINT ( 'NONE',  ( 6.041596546049881944, -1.325759876995153075, -1.255439798616593716 ) ) ;
#107955=CARTESIAN_POINT ( 'NONE',  ( 2.026450851813020648, 0.4238854151232730461, 1.868046764376835922 ) ) ;
#107963=CARTESIAN_POINT ( 'NONE',  ( 3.586284538990120119, 1.181046903802232206, 1.761068336431830472 ) ) ;
#107964=CARTESIAN_POINT ( 'NONE',  ( -0.02988540731099428513, 0.2551080090007939449, -1.761437810625957834 ) ) ;
#107966=CARTESIAN_POINT ( 'NONE',  ( 4.850830000233872674, -1.585153962374891812, 1.171817952366477344 ) ) ;
#107967=CARTESIAN_POINT ( 'NONE',  ( 0.1760394598168211200, 1.990691791301450575, -0.2996127288820998325 ) ) ;
#107969=CARTESIAN_POINT ( 'NONE',  ( 0.1052747227462194346, -0.09900681772390507174, 2.115024835901352596 ) ) ;
#107971=CARTESIAN_POINT ( 'NONE',  ( 1.838419004579601834, -1.109345826794335688, 1.747895861591180156 ) ) ;
#107975=CARTESIAN_POINT ( 'NONE',  ( 3.820331522234471144, 1.985175722263971654, 0.6558375257153716831 ) ) ;
#107979=CARTESIAN_POINT ( 'NONE',  ( 0.9963917123081984517, -1.767100618702711179, -0.3976972079893052459 ) ) ;
#107981=CARTESIAN_POINT ( 'NONE',  ( 5.672569038193632451, -1.402732290180560337, 1.703733612381942653 ) ) ;
#107984=CARTESIAN_POINT ( 'NONE',  ( 4.050008041959299199, 0.7462531942188170841, -2.076888956485785975 ) ) ;
#107987=CARTESIAN_POINT ( 'NONE',  ( 3.106014470790594562, -0.7728303494197851231, 1.749331318715248385 ) ) ;
#107989=CARTESIAN_POINT ( 'NONE',  ( 5.811005889236001032, -1.634438611397070806, 1.270752202701043609 ) ) ;
#107990=CARTESIAN_POINT ( 'NONE',  ( -1.786765180256111307E-13, 7.629137130509076492, -2.599999999999921929 ) ) ;
#107991=CARTESIAN_POINT ( 'NONE',  ( 3.239309987758617115, -1.907233169736745060, 1.017530501952010447 ) ) ;
#107992=CARTESIAN_POINT ( 'NONE',  ( 6.480031355044912900, -2.148842909532014289, -0.4297212958329286736 ) ) ;
#108002=CARTESIAN_POINT ( 'NONE',  ( 5.559458666840932928, 1.689222788819956245, 1.196583256836199149 ) ) ;
#108003=CARTESIAN_POINT ( 'NONE',  ( 4.037660154168158932, -1.329308714249255452, -1.394617731102282709 ) ) ;
#108004=CARTESIAN_POINT ( 'NONE',  ( 0.2281389574181335589, 2.011207032379238591, 0.1455110067964115739 ) ) ;
#108008=CARTESIAN_POINT ( 'NONE',  ( 0.4983068789779531160, -0.7420642642406435341, -2.062120472104383317 ) ) ;
#108009=CARTESIAN_POINT ( 'NONE',  ( 4.775911370473768791, 1.053640644303525331, 1.490772598166143048 ) ) ;
#108016=CARTESIAN_POINT ( 'NONE',  ( 2.806014743833367131, 1.331929863061011465, -1.271513748034671654 ) ) ;
#108017=CARTESIAN_POINT ( 'NONE',  ( 5.695569903961543723, 1.858472494656268958, -0.7744561248179144819 ) ) ;
#108018=CARTESIAN_POINT ( 'NONE',  ( 0.6854589470919645322, -1.231871052372325526, -1.940221060253940699 ) ) ;
#108019=CARTESIAN_POINT ( 'NONE',  ( 6.438335799692933570, -1.052282694883142078, 1.655480336553965648 ) ) ;
#108025=CARTESIAN_POINT ( 'NONE',  ( 2.806283438348840420, 1.512464495701435929, -1.443730951476623670 ) ) ;
#108026=CARTESIAN_POINT ( 'NONE',  ( 1.006479672118578916, 1.419055151971573059, -1.218976214888117804 ) ) ;
#108027=CARTESIAN_POINT ( 'NONE',  ( 2.038435264984053585, 1.930122609968443204, -0.5825652091262025767 ) ) ;
#108031=CARTESIAN_POINT ( 'NONE',  ( 2.612550116648149512, -0.1684838578246611873, 1.732238525843646570 ) ) ;
#108035=CARTESIAN_POINT ( 'NONE',  ( 2.719059632816126282, -0.1691219839104734501, 1.716555610488319505 ) ) ;
#108036=CARTESIAN_POINT ( 'NONE',  ( 3.122796855005858241, 0.05607861761174406934, 2.191015320347329709 ) ) ;
#108037=CARTESIAN_POINT ( 'NONE',  ( 4.723365791888975096, -0.1103408873950258995, 2.204240794804641190 ) ) ;
#108040=CARTESIAN_POINT ( 'NONE',  ( 1.973704989461112946, -0.2689809023317759618, 2.154309762211854107 ) ) ;
#108041=CARTESIAN_POINT ( 'NONE',  ( 1.101864800459760207, -1.825872481749410525, -0.002338443969775172437 ) ) ;
#108042=CARTESIAN_POINT ( 'NONE',  ( 3.555961197718297218, 1.179765190368966321, 1.758020836099948747 ) ) ;
#108045=ORIENTED_EDGE ( 'NONE', *, *, #95054, .F. ) ;
#108046=CARTESIAN_POINT ( 'NONE',  ( 3.755682109644884026, 2.274985096322924338, -0.2814536430481278662 ) ) ;
#108050=CARTESIAN_POINT ( 'NONE',  ( 5.654997643673960184, 0.4312606369310955645, 2.178877383265501066 ) ) ;
#108057=CARTESIAN_POINT ( 'NONE',  ( 4.219375079941334761, 1.978050461189932552, 0.3905991720301109082 ) ) ;
#108059=CARTESIAN_POINT ( 'NONE',  ( 2.975492196776472031, -0.2068670369150918398, 2.052202205628439913 ) ) ;
#108063=CARTESIAN_POINT ( 'NONE',  ( 6.527279143455773536, -1.428284688129980440, -1.662137905815167294 ) ) ;
#108064=CARTESIAN_POINT ( 'NONE',  ( 3.568982563115063567, -0.9913999084223242830, 1.755768870528086056 ) ) ;
#108065=CARTESIAN_POINT ( 'NONE',  ( 2.964219115174483665, -1.702287218311925310, -0.7022057971969236645 ) ) ;
#108067=CARTESIAN_POINT ( 'NONE',  ( 6.211906940382025510, -1.811394037990306627, 0.2264786762415857968 ) ) ;
#108069=CARTESIAN_POINT ( 'NONE',  ( 0.2282871097136250915, -1.394050316402313916, -1.782836666206646603 ) ) ;
#108070=CARTESIAN_POINT ( 'NONE',  ( 2.139418596640904280, -1.880839966478216052, 0.9477614987608102837 ) ) ;
#108080=CARTESIAN_POINT ( 'NONE',  ( 3.603960747418310184, 1.611073206568460758, 1.529666071269941474 ) ) ;
#108081=CARTESIAN_POINT ( 'NONE',  ( 0.7795418844130063141, 1.474435645617519164, 1.621430000501473900 ) ) ;
#108082=CARTESIAN_POINT ( 'NONE',  ( 0.7860941533469123499, 1.484900681275106438, 1.632775826992872492 ) ) ;
#108084=CARTESIAN_POINT ( 'NONE',  ( 4.826587731031282580, -1.282962940432516907, 1.484285152025546672 ) ) ;
#108092=CARTESIAN_POINT ( 'NONE',  ( 3.533539421053989660, -0.1523460092780377639, 2.115156586662121363 ) ) ;
#108094=CARTESIAN_POINT ( 'NONE',  ( 5.559502693676295237, 0.4258712887980077300, -2.119171757835013548 ) ) ;
#108095=CARTESIAN_POINT ( 'NONE',  ( 4.282634502089007533, 1.642705626968201216, -0.8318752211165169053 ) ) ;
#108096=CARTESIAN_POINT ( 'NONE',  ( 5.454314652423888354, -1.275559214091715354, 1.561879324423600668 ) ) ;
#108099=CARTESIAN_POINT ( 'NONE',  ( 0.1865103356883268948, 1.287481616103260063, 1.171338548376497535 ) ) ;
#108100=CARTESIAN_POINT ( 'NONE',  ( 6.827182134110164391, 0.5838490905608649806, 1.963161153048794905 ) ) ;
#108103=CARTESIAN_POINT ( 'NONE',  ( 4.364260218091946975, 1.016419123106377276, 1.907829002176253175 ) ) ;
#108105=CARTESIAN_POINT ( 'NONE',  ( 5.343124974464078747, -1.122324884721880078, 1.674632237393176792 ) ) ;
#108108=CARTESIAN_POINT ( 'NONE',  ( 3.590839768554392908, -0.4196827604958653923, -2.120402733634827452 ) ) ;
#108109=CARTESIAN_POINT ( 'NONE',  ( 3.690661264905565009, -0.3812834177611671982, -1.933973196684968920 ) ) ;
#108110=CARTESIAN_POINT ( 'NONE',  ( -0.07626876867936756288, -1.353788312843669406, -1.724171373301164767 ) ) ;
#108111=CARTESIAN_POINT ( 'NONE',  ( 1.220229771213819481, -2.250799921053967090, 0.5081616799173671595 ) ) ;
#108112=CARTESIAN_POINT ( 'NONE',  ( 3.708323652925065161, -0.8317495340520587588, -1.885651027073296904 ) ) ;
#108113=CARTESIAN_POINT ( 'NONE',  ( 5.987830644705256056, -1.933104919717167025, -0.1861817195589876295 ) ) ;
#108117=CARTESIAN_POINT ( 'NONE',  ( 6.889999999999967706, 0.005249217920031542736, 1.719840535937327441 ) ) ;
#108122=CARTESIAN_POINT ( 'NONE',  ( 2.837189949676882428, 0.2689455771197127310, 2.190246129917215789 ) ) ;
#108124=CARTESIAN_POINT ( 'NONE',  ( 6.280128941539553367, -1.086961472313338284, -1.632890767417946032 ) ) ;
#108125=CARTESIAN_POINT ( 'NONE',  ( 6.539320575229230492, 2.428701779328062749, 2.485127258459709054 ) ) ;
#108129=FACE_OUTER_BOUND ( 'NONE', #28388, .T. ) ;
#108130=CARTESIAN_POINT ( 'NONE',  ( 4.892441406782114477, 1.528958278715689234, -1.025397978904031060 ) ) ;
#108132=CARTESIAN_POINT ( 'NONE',  ( 2.448182087220668102, 2.060414928722671402, 0.05179878229087316738 ) ) ;
#108136=CARTESIAN_POINT ( 'NONE',  ( 6.469000917296717112, -1.638331675554663747, 1.346054232038436105 ) ) ;
#108139=CARTESIAN_POINT ( 'NONE',  ( 0.8134386948647929216, -0.3029782207385351422, 2.038374528180360912 ) ) ;
#108142=CARTESIAN_POINT ( 'NONE',  ( 4.511176471348508521, -1.804767551675333204, 0.3638508048048467169 ) ) ;
#108149=CARTESIAN_POINT ( 'NONE',  ( 4.565167970240332274, -1.970479184476851886, -0.9938812724585781577 ) ) ;
#108150=CARTESIAN_POINT ( 'NONE',  ( 6.837213258907510749, -2.025504081721161143, 1.008097451810068268 ) ) ;
#108152=CARTESIAN_POINT ( 'NONE',  ( 0.4570967503451648373, -1.639016809899789040, 0.9851245988263114262 ) ) ;
#108153=CARTESIAN_POINT ( 'NONE',  ( 0.09298292169932984019, 1.756857073293972116, 0.9896806593640145033 ) ) ;
#108155=CARTESIAN_POINT ( 'NONE',  ( 0.07536363704235479744, 6.947016338497881804, -2.739277465201896078 ) ) ;
#108156=CARTESIAN_POINT ( 'NONE',  ( 5.760397938718036848, 1.910310778393434106, 0.08934430699411573251 ) ) ;
#108157=CARTESIAN_POINT ( 'NONE',  ( 0.5845639792326964290, -0.2246964894469481722, -1.857040431621145959 ) ) ;
#108158=CARTESIAN_POINT ( 'NONE',  ( 2.518767860054324625, 0.2516336668320385828, 2.000731427934741902 ) ) ;
#108160=CARTESIAN_POINT ( 'NONE',  ( 4.477239461409222798, 0.0005595100435150377523, -2.106257355078521964 ) ) ;
#108166=CARTESIAN_POINT ( 'NONE',  ( 4.236585392707596043, 1.239412559483305198, -1.594744479876673005 ) ) ;
#108170=CARTESIAN_POINT ( 'NONE',  ( 4.323607124742586016, -2.069909602744592014, 0.6229453038564189971 ) ) ;
#108176=CARTESIAN_POINT ( 'NONE',  ( 2.436178610684522461, 1.334241001675811500, 1.712780914784496122 ) ) ;
#108179=CARTESIAN_POINT ( 'NONE',  ( 0.8898994657863326108, -0.4472179738511591895, -1.785967584704901912 ) ) ;
#108181=CARTESIAN_POINT ( 'NONE',  ( 3.316156725143477146, 1.388770557483296697, -1.695381604771596606 ) ) ;
#108182=CARTESIAN_POINT ( 'NONE',  ( 6.983263157960383438, 0.5812290088160886325, 2.006563525967783868 ) ) ;
#108183=CARTESIAN_POINT ( 'NONE',  ( 3.995213114784367026, 1.913063998889670714, -1.207689374757703771 ) ) ;
#108185=CARTESIAN_POINT ( 'NONE',  ( 4.505092375653735992, -0.09411930587044713137, 2.014432893821124004 ) ) ;
#108190=CARTESIAN_POINT ( 'NONE',  ( 4.147515422935190266, 0.5979684684156804098, -1.665763606213203518 ) ) ;
#108193=CARTESIAN_POINT ( 'NONE',  ( 0.5168062790325059774, 1.452128344422070283, -1.525477944039640432 ) ) ;
#108197=CARTESIAN_POINT ( 'NONE',  ( 1.117558341675929157, 0.3875481960372212931, -1.930861576554385062 ) ) ;
#108199=CARTESIAN_POINT ( 'NONE',  ( 5.835564593388588683, 0.5826401998472263699, -1.930423629703325705 ) ) ;
#108203=CARTESIAN_POINT ( 'NONE',  ( 4.399188623838041323, 1.502396186649012311, 1.114296746780506497 ) ) ;
#108206=CARTESIAN_POINT ( 'NONE',  ( 4.329010850845236291, -1.929826300244817272, -0.7499136367685383942 ) ) ;
#108215=CARTESIAN_POINT ( 'NONE',  ( 4.176187491914356897, -1.006606191838583131, -1.683785057063936552 ) ) ;
#108216=CARTESIAN_POINT ( 'NONE',  ( 2.108749758911751204, 0.7741990562295970602, -1.861730988020185329 ) ) ;
#108218=CARTESIAN_POINT ( 'NONE',  ( 6.639320575229278099, 1.279659970127836388, 2.012538313910294807 ) ) ;
#108219=CARTESIAN_POINT ( 'NONE',  ( 1.510794437334112672, 1.647127454408814362, 0.8865631655482277829 ) ) ;
#108221=CARTESIAN_POINT ( 'NONE',  ( 2.478773383088346716, -1.385198452255667290, 1.461135165768602029 ) ) ;
#108223=CARTESIAN_POINT ( 'NONE',  ( 3.023186137256496764, -1.865899319694108272, 1.000581237753160879 ) ) ;
#108225=CARTESIAN_POINT ( 'NONE',  ( 4.404779037558821386, 0.5491149005726041477, 1.996164414091922135 ) ) ;
#108227=CARTESIAN_POINT ( 'NONE',  ( 0.3278234441896179518, 1.071198113070050972, -1.795324408978350439 ) ) ;
#108229=CARTESIAN_POINT ( 'NONE',  ( 5.596661130663158623, -0.4455768995972574364, -1.770251349769519367 ) ) ;
#108237=CARTESIAN_POINT ( 'NONE',  ( 6.551426578739074635, -1.705833205818767295, 0.8644478841580638395 ) ) ;
#108242=CARTESIAN_POINT ( 'NONE',  ( 6.933263157960373846, 7.629137130509066722, 2.546189081643289942 ) ) ;
#108246=CARTESIAN_POINT ( 'NONE',  ( 5.360953910674266965, -0.05231296482399727665, -2.015913715532565043 ) ) ;
#108248=( LENGTH_UNIT ( ) NAMED_UNIT ( * ) SI_UNIT ( .MILLI., .METRE. ) );
#108254=CARTESIAN_POINT ( 'NONE',  ( 1.903111606826495938, -1.666530434877494304, 1.049136497343281738 ) ) ;
#108255=CARTESIAN_POINT ( 'NONE',  ( 3.954703970953522774, -1.882481274494081980, -0.7231244775810635739 ) ) ;
#108257=CARTESIAN_POINT ( 'NONE',  ( 6.827182134110196365, 7.629137130509086262, 2.889055895399252005 ) ) ;
#108258=CARTESIAN_POINT ( 'NONE',  ( 3.943468035136340255, 0.7389761752502190806, -2.063229655756371628 ) ) ;
#108260=CARTESIAN_POINT ( 'NONE',  ( 2.467692127658027701, 1.889608252265186694, -0.3738381972786026797 ) ) ;
#108262=CARTESIAN_POINT ( 'NONE',  ( 0.1329588055935396196, 2.886534925058126699, -2.334852352984605695 ) ) ;
#108270=CARTESIAN_POINT ( 'NONE',  ( 5.583513413114173041, -0.8223277247318347971, 1.647484189299788682 ) ) ;
#108271=CARTESIAN_POINT ( 'NONE',  ( 3.158842756365538129, 0.4911626674463653863, 1.952128870646198555 ) ) ;
#108272=CARTESIAN_POINT ( 'NONE',  ( 4.130415602100383943, 0.2865403768554532493, -2.280420282979139124 ) ) ;
#108273=CARTESIAN_POINT ( 'NONE',  ( -0.1290005225502675879, -0.006633637972621592160, -2.173875058097324064 ) ) ;
#108274=CARTESIAN_POINT ( 'NONE',  ( 3.678407310798579299, 1.183884816018574426, -1.435758196845798418 ) ) ;
#108280=CARTESIAN_POINT ( 'NONE',  ( 5.653879428721274358, 0.8482012749469816093, 1.911158475179574046 ) ) ;
#108287=CARTESIAN_POINT ( 'NONE',  ( 6.111878173048258311, -1.710926958338830017, 0.2183984861162356628 ) ) ;
#108289=CARTESIAN_POINT ( 'NONE',  ( 1.054805789555151696, -1.101345310128332367, 1.339526040370845772 ) ) ;
#108292=CARTESIAN_POINT ( 'NONE',  ( 6.086835205273840366, 2.090220906010348045, 0.5866831100012849243 ) ) ;
#108293=CARTESIAN_POINT ( 'NONE',  ( 4.266095019097836172, 0.8626762044917112293, 1.609013669381313294 ) ) ;
#108294=CARTESIAN_POINT ( 'NONE',  ( 2.676550354755039773, 1.285117694784821518, -1.482265789204496143 ) ) ;
#108298=CARTESIAN_POINT ( 'NONE',  ( 3.387459763963754700, 0.05019612904376415108, -2.120051327867578550 ) ) ;
#108303=CARTESIAN_POINT ( 'NONE',  ( 0.7607008448355723207, -0.6940761377024067258, -1.950597895851911456 ) ) ;
#108306=CARTESIAN_POINT ( 'NONE',  ( 3.668779877082572138, 0.8004024921177651519, 2.072244876181651652 ) ) ;
#108308=CARTESIAN_POINT ( 'NONE',  ( 1.846706770127172881, 0.3881029198684777803, -2.265567138619323018 ) ) ;
#108310=CARTESIAN_POINT ( 'NONE',  ( 6.684441936803141360, 1.192331456891123187, -1.682829884528406428 ) ) ;
#108316=CARTESIAN_POINT ( 'NONE',  ( -0.2102771530458458771, 0.2260464284578807270, -2.237246294970319127 ) ) ;
#108317=CARTESIAN_POINT ( 'NONE',  ( 3.047548298876975537, 0.6224300751757807504, -1.608722921838340092 ) ) ;
#108318=CARTESIAN_POINT ( 'NONE',  ( 2.219935720625454412, 0.9462983093676997637, -1.780669029686342331 ) ) ;
#108319=( BOUNDED_SURFACE ( )  B_SPLINE_SURFACE ( 3, 3, ( 
 ( #108273, #174294, #10681, #192630, #126665, #61579, #211008, #160152, #79953, #161220 ),
 ( #110403, #60505, #206756, #44282, #76752, #207818, #75701, #78880, #93042, #42158 ),
 ( #176407, #94111, #58387, #62631, #208875, #95171, #109344, #124543, #12807, #128791 ),
 ( #9624, #145003, #194772, #175354, #26934, #29087, #96237, #142873, #159084, #91979 ),
 ( #162287, #25869, #46409, #28013, #112525, #11749, #190500, #158037, #77824, #141815 ),
 ( #178538, #143945, #209941, #127747, #193704, #30148, #45348, #59446, #125603, #191563 ),
 ( #43227, #111467, #177473, #13875, #48544, #47489, #147114, #148174, #19209, #196904 ) ),
 .UNSPECIFIED., .T., .F., .T. ) 
 B_SPLINE_SURFACE_WITH_KNOTS ( ( 4, 3, 4 ),
 ( 4, 1, 1, 1, 1, 1, 1, 4 ),
 ( 0.000000000000000000, 0.5000000000000000000, 1.000000000000000000 ),
 ( 0.000000000000000000, 0.09123828766142533242, 0.1830323254715014447, 0.2554767746403809325, 0.3605042187413262100, 0.5206858269973231312, 0.7335850107976985557, 1.000000000000000000 ),
 .UNSPECIFIED. ) 
 GEOMETRIC_REPRESENTATION_ITEM ( )  RATIONAL_B_SPLINE_SURFACE ( (
 ( 1.000000000000000000, 1.000000000000000000, 1.000000000000000000, 0.9999999999999997780, 1.000000000000000000, 1.000000000000000000, 1.000000000000000222, 1.000000000000000000, 1.000000000000000000, 1.000000000000000000),
 ( 0.3333333333333333703, 0.3333333333333333703, 0.3333333333333334259, 0.3333333333333332593, 0.3333333333333333703, 0.3333333333333333703, 0.3333333333333334814, 0.3333333333333333703, 0.3333333333333333703, 0.3333333333333333703),
 ( 0.3333333333333333703, 0.3333333333333333703, 0.3333333333333334259, 0.3333333333333332593, 0.3333333333333333703, 0.3333333333333333703, 0.3333333333333334814, 0.3333333333333333703, 0.3333333333333333703, 0.3333333333333333703),
 ( 1.000000000000000000, 1.000000000000000000, 1.000000000000000000, 0.9999999999999997780, 1.000000000000000000, 1.000000000000000000, 1.000000000000000222, 1.000000000000000000, 1.000000000000000000, 1.000000000000000000),
 ( 0.3333333333333333703, 0.3333333333333333703, 0.3333333333333334259, 0.3333333333333332593, 0.3333333333333333703, 0.3333333333333333703, 0.3333333333333334814, 0.3333333333333333703, 0.3333333333333333703, 0.3333333333333333703),
 ( 0.3333333333333333703, 0.3333333333333333703, 0.3333333333333334259, 0.3333333333333332593, 0.3333333333333333703, 0.3333333333333333703, 0.3333333333333334814, 0.3333333333333333703, 0.3333333333333333703, 0.3333333333333333703),
 ( 1.000000000000000000, 1.000000000000000000, 1.000000000000000000, 0.9999999999999997780, 1.000000000000000000, 1.000000000000000000, 1.000000000000000222, 1.000000000000000000, 1.000000000000000000, 1.000000000000000000) ) ) 
 REPRESENTATION_ITEM ( '' )  SURFACE ( )  );
#108320=CARTESIAN_POINT ( 'NONE',  ( 2.497091698460200071, -2.273154071007321697, 0.3411551791231131059 ) ) ;
#108321=CARTESIAN_POINT ( 'NONE',  ( 3.743696771605113494, -1.710248914368957873, -1.481124664604586583 ) ) ;
#108322=CARTESIAN_POINT ( 'NONE',  ( 4.934254457356054502, 1.083321712992061814, -1.805932085151832789 ) ) ;
#108324=CARTESIAN_POINT ( 'NONE',  ( 3.883871017828253613, -0.8741022562178245581, 1.538735937109585672 ) ) ;
#108326=CARTESIAN_POINT ( 'NONE',  ( 5.882448709439383805, -0.3326909364035086081, -2.268010969791500742 ) ) ;
#108327=CARTESIAN_POINT ( 'NONE',  ( 5.208873985248447802, -0.2666229848188906848, 1.821608446441948193 ) ) ;
#108331=CARTESIAN_POINT ( 'NONE',  ( 5.015667846030231303, -1.170523448010954315, -1.852474865436819274 ) ) ;
#108334=CARTESIAN_POINT ( 'NONE',  ( 5.863751307568212390, -0.5067217619753560109, 2.007263066363853987 ) ) ;
#108338=CARTESIAN_POINT ( 'NONE',  ( 3.598194957300792307, -1.924334687528261201, -0.09379112422614949152 ) ) ;
#108341=CARTESIAN_POINT ( 'NONE',  ( 0.03578803411239706023, -0.1004787818888741302, 2.219253419324648036 ) ) ;
#108348=CARTESIAN_POINT ( 'NONE',  ( 0.8362905744919849615, -1.092891352686057527, 1.629061181365853539 ) ) ;
#108351=CARTESIAN_POINT ( 'NONE',  ( 6.127397123722368555, 0.1457569626216181913, -1.956525209266091192 ) ) ;
#108354=CARTESIAN_POINT ( 'NONE',  ( 0.08136044664198981147, -0.1580758092474404408, -2.227059435111256924 ) ) ;
#108358=CARTESIAN_POINT ( 'NONE',  ( 0.4209003391736841349, -0.09842406703440903515, 1.868101828653282226 ) ) ;
#108359=CARTESIAN_POINT ( 'NONE',  ( 5.659468189498653601, -0.4240490459222304165, -1.681042783800198448 ) ) ;
#108361=CARTESIAN_POINT ( 'NONE',  ( 3.316156725143477146, 1.388770557483296697, -1.695381604771596606 ) ) ;
#108362=CARTESIAN_POINT ( 'NONE',  ( 4.243447643126375013, -2.009724547103900250, 1.133870999951855696 ) ) ;
#108363=CARTESIAN_POINT ( 'NONE',  ( 0.3915709625425906615, 1.526647161510179318, 1.384594130533061129 ) ) ;
#108364=CARTESIAN_POINT ( 'NONE',  ( 2.747912338643729413, 0.6545661140590716132, 1.828431812057261352 ) ) ;
#108368=CARTESIAN_POINT ( 'NONE',  ( 4.728832233812888752, 1.460412846248357210, -1.537820402542383169 ) ) ;
#108370=CARTESIAN_POINT ( 'NONE',  ( 3.164685561777963230, 1.281361203394768111, 1.556908733426412450 ) ) ;
#108374=CARTESIAN_POINT ( 'NONE',  ( 1.207329354700342305, -0.4456725867950651621, 1.770335049871730071 ) ) ;
#108379=CARTESIAN_POINT ( 'NONE',  ( 5.278222320829740077, -1.146742738506721704, 1.712165125756033968 ) ) ;
#108383=CARTESIAN_POINT ( 'NONE',  ( 4.565106334443884251, -1.620744288901782904, 1.204869856736161537 ) ) ;
#108384=CARTESIAN_POINT ( 'NONE',  ( 5.321006124507968060, 1.683121437214535554, -1.449644825538060733 ) ) ;
#108390=CARTESIAN_POINT ( 'NONE',  ( 4.469639075930389893, 1.999461767218065678, -0.4989166988303375683 ) ) ;
#108391=CARTESIAN_POINT ( 'NONE',  ( 4.026017654026761150, -1.753031021560845559, 0.9963007555989014108 ) ) ;
#108398=CARTESIAN_POINT ( 'NONE',  ( 2.970077202574809228, 1.701686883299750264, 1.080900613174784475 ) ) ;
#108399=CARTESIAN_POINT ( 'NONE',  ( 2.114959233223293822, -1.785989328681826027, 0.4467204754193611627 ) ) ;
#108400=CARTESIAN_POINT ( 'NONE',  ( 1.331197006551400497, 2.225188506942116895, 0.6113326355875832174 ) ) ;
#108402=CARTESIAN_POINT ( 'NONE',  ( 3.655696586050953378, 0.5291108212043382775, -2.095698868369605616 ) ) ;
#108405=CARTESIAN_POINT ( 'NONE',  ( 3.146212962842390937, -0.1666923573656608759, -2.292372948102610053 ) ) ;
#108409=CARTESIAN_POINT ( 'NONE',  ( 1.270139834521961886, -1.189467451172643964, 1.443775233441677130 ) ) ;
#108411=CARTESIAN_POINT ( 'NONE',  ( 5.137557537983609812, -1.393591726081166771, -1.394729141857486532 ) ) ;
#108415=CARTESIAN_POINT ( 'NONE',  ( 0.7860941533469123499, 1.484900681275106438, 1.632775826992872492 ) ) ;
#108420=CARTESIAN_POINT ( 'NONE',  ( 6.539320575229258026, 4.689551739520863904, 2.765837357486185866 ) ) ;
#108421=CARTESIAN_POINT ( 'NONE',  ( 5.084826545086224669, -0.2406546161831616404, -1.956650619579934469 ) ) ;
#108422=CARTESIAN_POINT ( 'NONE',  ( 5.637451635233869496, -2.088540497258955408, 0.9818693799023417990 ) ) ;
#108423=CARTESIAN_POINT ( 'NONE',  ( 6.144940932578938586, -0.2738450275633330100, -1.840644705263774217 ) ) ;
#108425=CARTESIAN_POINT ( 'NONE',  ( 3.327062588944328603, -1.903923626093235955, -0.7937240881994469532 ) ) ;
#108433=CARTESIAN_POINT ( 'NONE',  ( 5.740740459546420205, -2.117024774779395102, -0.4812451790989195621 ) ) ;
#108435=CARTESIAN_POINT ( 'NONE',  ( 4.581507094455529838, -0.8636776874328588871, 1.626104626046148249 ) ) ;
#108437=CARTESIAN_POINT ( 'NONE',  ( 6.620655732516668834, 7.629137130509086262, 2.526260288887293814 ) ) ;
#108438=FACE_OUTER_BOUND ( 'NONE', #60816, .T. ) ;
#108440=CARTESIAN_POINT ( 'NONE',  ( 0.4392367245290337840, 0.3885019757292383913, 2.228643277672849976 ) ) ;
#108445=CARTESIAN_POINT ( 'NONE',  ( 0.08246951281144777879, -1.249137507218839094, 1.448023666807837895 ) ) ;
#108446=CARTESIAN_POINT ( 'NONE',  ( 0.2679308956112765872, -1.161373500300251216, 1.335597826242039154 ) ) ;
#108447=CARTESIAN_POINT ( 'NONE',  ( 5.742843059509288750, 1.940770921862687182, 0.5345600180575919014 ) ) ;
#108450=CARTESIAN_POINT ( 'NONE',  ( 4.383879424978657902, 1.373869114255725776, 1.596202613037283502 ) ) ;
#108451=CARTESIAN_POINT ( 'NONE',  ( 3.638217106272136903, 0.6927189700525613336, 1.786146362908203944 ) ) ;
#108453=CARTESIAN_POINT ( 'NONE',  ( 3.930098287398839041, 1.092129198686382141, 1.638800773490353802 ) ) ;
#108454=CARTESIAN_POINT ( 'NONE',  ( 5.677991919488574624, 1.989193807575660555, -0.3493085226990484959 ) ) ;
#108455=CARTESIAN_POINT ( 'NONE',  ( 3.133525119713890472, -1.255248497922526463, -1.387151338369890574 ) ) ;
#108456=CARTESIAN_POINT ( 'NONE',  ( 5.197747934024010696, -0.6158827634895787106, 1.611369335837910644 ) ) ;
#108457=CARTESIAN_POINT ( 'NONE',  ( 0.7910927259777954523, -0.04954035392716604758, -1.911929172785244102 ) ) ;
#108459=CARTESIAN_POINT ( 'NONE',  ( 2.860232119962682784, 2.196193069775736362, -0.2169517147150926140 ) ) ;
#108462=CARTESIAN_POINT ( 'NONE',  ( 0.1509074155349584279, -0.4535863444464246497, -2.019966333402842817 ) ) ;
#108468=CARTESIAN_POINT ( 'NONE',  ( 2.260293373024503616, -2.069953001785612479, 0.04851313490940312168 ) ) ;
#108472=CARTESIAN_POINT ( 'NONE',  ( 6.463548717370299457, -1.702720583769131490, -1.263627255760652046 ) ) ;
#108477=CARTESIAN_POINT ( 'NONE',  ( 5.149767453795408123, -0.2439937967673235231, -2.001204641050558397 ) ) ;
#108478=CARTESIAN_POINT ( 'NONE',  ( 5.085127819360848456, 1.569905733240322343, 1.097627489654330990 ) ) ;
#108480=CARTESIAN_POINT ( 'NONE',  ( 2.595491417077447238, -0.6846416945752286098, 2.081959150545972914 ) ) ;
#108483=CARTESIAN_POINT ( 'NONE',  ( 5.537363252524067470, -0.04518311473342268708, 2.012845415592057208 ) ) ;
#108484=CARTESIAN_POINT ( 'NONE',  ( 1.212987991671743204, 1.561712320281399835, -1.103468303573502673 ) ) ;
#108487=CARTESIAN_POINT ( 'NONE',  ( -0.05311194370935175268, -1.802413661875476913, -0.9041393574176490588 ) ) ;
#108489=CARTESIAN_POINT ( 'NONE',  ( 3.685174051874222201, 1.515783366363635531, 1.440268600269165589 ) ) ;
#108491=CARTESIAN_POINT ( 'NONE',  ( 2.203723468020501119, -1.724507683567375826, 0.03868650182545228799 ) ) ;
#108493=CARTESIAN_POINT ( 'NONE',  ( 6.222909436229170588, 1.570324008046734221, -1.425282903188800798 ) ) ;
#108501=CARTESIAN_POINT ( 'NONE',  ( 3.299258901807587741, 1.636513117289538188, -0.7770104639905143218 ) ) ;
#108506=CARTESIAN_POINT ( 'NONE',  ( 3.844242791777858770, 0.9658850817777319131, -1.532267982868290579 ) ) ;
#108507=CARTESIAN_POINT ( 'NONE',  ( 6.539320575229232269, 1.262224698349242669, 2.111181586620724637 ) ) ;
#108509=CARTESIAN_POINT ( 'NONE',  ( 3.578407426278474190, 1.182412371022481645, -1.437126236693661241 ) ) ;
#108510=CARTESIAN_POINT ( 'NONE',  ( 1.669406806874464300, 1.322410700044797327, 1.386144426805105523 ) ) ;
#108511=CARTESIAN_POINT ( 'NONE',  ( 1.483130931141176889, 1.688290157389197077, -0.6950536248920418103 ) ) ;
#108518=CARTESIAN_POINT ( 'NONE',  ( 5.295741323871941297, -1.389945570378407380, -1.395530913269894091 ) ) ;
#108521=CARTESIAN_POINT ( 'NONE',  ( 6.509741685903361663, -1.029359178063901092, -1.934661654277470166 ) ) ;
#108522=CARTESIAN_POINT ( 'NONE',  ( 5.139640169905585587, -1.362188071541370116, -1.362388069303143823 ) ) ;
#108524=CARTESIAN_POINT ( 'NONE',  ( 0.9381830591699467092, 1.797733097909786304, 0.3167546781352030272 ) ) ;
#108525=CARTESIAN_POINT ( 'NONE',  ( 1.787996309160574837, 1.523479866092191548, 1.596893430481533649 ) ) ;
#108527=CARTESIAN_POINT ( 'NONE',  ( 0.9844543725016400293, -1.211084316286781037, 1.480072698922259455 ) ) ;
#108529=CARTESIAN_POINT ( 'NONE',  ( 0.6605274321102487800, -0.6603073245880388686, -1.855717402334137622 ) ) ;
#108530=CARTESIAN_POINT ( 'NONE',  ( 2.595178948467924851, -0.6067665810922833192, 1.844924317596825070 ) ) ;
#108534=CARTESIAN_POINT ( 'NONE',  ( 6.666864641256595725, 1.379314998728842445, -1.249469950728621326 ) ) ;
#108539=CARTESIAN_POINT ( 'NONE',  ( 2.823975127348025804, 1.215230906543849354, -1.823574674616668556 ) ) ;
#108543=CARTESIAN_POINT ( 'NONE',  ( 2.807047293222181494, 1.542382716246639474, 0.9765254425028799812 ) ) ;
#108548=CARTESIAN_POINT ( 'NONE',  ( 1.383290355582541542, 1.780271273866357529, -0.7366933121468289825 ) ) ;
#108549=CARTESIAN_POINT ( 'NONE',  ( 5.717619619964247946, 0.3862620380215216476, -1.923179868201368548 ) ) ;
#108554=CARTESIAN_POINT ( 'NONE',  ( 4.775033345069852331, 2.044829088842615494, -0.7888500489584143738 ) ) ;
#108559=CARTESIAN_POINT ( 'NONE',  ( 5.541872263726007830, 1.386227983376321582, 1.537841262885197846 ) ) ;
#108563=CARTESIAN_POINT ( 'NONE',  ( 5.063244923127927954, -1.278613472530117035, 1.910113253385301801 ) ) ;
#108567=CARTESIAN_POINT ( 'NONE',  ( 0.5336625369133874974, -1.625122730996070297, -1.616870241932764074 ) ) ;
#108570=CARTESIAN_POINT ( 'NONE',  ( 4.910071578948462800, 1.337895470842176193, -1.407775065355970412 ) ) ;
#108575=CARTESIAN_POINT ( 'NONE',  ( 4.728717205193702533, 1.314622909153417174, -1.389140896021365368 ) ) ;
#108576=CARTESIAN_POINT ( 'NONE',  ( 6.194358799569198659, -1.717016665659231167, -0.1635641229304989064 ) ) ;
#108577=CARTESIAN_POINT ( 'NONE',  ( 5.348842313791752900, -1.825074749614737701, -0.8578464102408298597 ) ) ;
#108581=CARTESIAN_POINT ( 'NONE',  ( 1.605537313848971026, -2.074692111233501723, 0.2571424261670462452 ) ) ;
#108582=CARTESIAN_POINT ( 'NONE',  ( 6.837169251635001999, -1.579311124772398767, 0.7986344709578310219 ) ) ;
#108583=CARTESIAN_POINT ( 'NONE',  ( 5.502577337681268332, -1.966645332631598908, 0.4444998760482973821 ) ) ;
#108585=CARTESIAN_POINT ( 'NONE',  ( 3.310744302307960574, 2.072215845705066339, 0.9802597712869900448 ) ) ;
#108586=CARTESIAN_POINT ( 'NONE',  ( 2.290578643201816256, 1.344622755191619445, 1.104862870798990260 ) ) ;
#108587=CARTESIAN_POINT ( 'NONE',  ( 3.058948843759463188, 0.5191580478346514704, 2.055925682384197373 ) ) ;
#108589=CARTESIAN_POINT ( 'NONE',  ( 1.686441086386183619, -0.9581320880991549549, -1.444804011637023322 ) ) ;
#108591=CARTESIAN_POINT ( 'NONE',  ( 1.943593235818155351, 1.280450557881509299, 1.350794863662147627 ) ) ;
#108592=CARTESIAN_POINT ( 'NONE',  ( 2.875608777474625732, -0.2152533142569280078, 2.160498500671267585 ) ) ;
#108593=CARTESIAN_POINT ( 'NONE',  ( 3.503138892209650024, -0.1435209762444041581, 2.011451614702438828 ) ) ;
#108594=CARTESIAN_POINT ( 'NONE',  ( 5.187500000000002665, -1.451031289060905172, 1.451031289061322838 ) ) ;
#108596=CARTESIAN_POINT ( 'NONE',  ( 1.008667890995796457, 1.460797969510800876, -1.255919511179462322 ) ) ;
#108598=CARTESIAN_POINT ( 'NONE',  ( 3.146955363149469331, 2.168125099964354874, 0.4830323043785512138 ) ) ;
#108604=CARTESIAN_POINT ( 'NONE',  ( 5.941669428368816952, -2.091911387875099670, 0.7476460515099275783 ) ) ;
#108605=CARTESIAN_POINT ( 'NONE',  ( 5.213317179658601752, -1.656387821537348426, -1.051046178410528942 ) ) ;
#108609=CARTESIAN_POINT ( 'NONE',  ( 6.028679731477588177, 2.178036183261321757, 0.6118574502519974478 ) ) ;
#108611=CARTESIAN_POINT ( 'NONE',  ( 2.576693429754982390, 1.349077690114818040, -1.560390594356737104 ) ) ;
#108616=CARTESIAN_POINT ( 'NONE',  ( 4.094877388769967652, 1.581529129216452612, -0.9985332613470513374 ) ) ;
#108617=CARTESIAN_POINT ( 'NONE',  ( 2.935853622122220674, -1.419245300609776272, -0.9961633832534546595 ) ) ;
#108618=CARTESIAN_POINT ( 'NONE',  ( -0.02329727741511803188, -2.225753042794619496, -0.5483686822410521744 ) ) ;
#108619=CARTESIAN_POINT ( 'NONE',  ( 1.378255502416312117, 1.315327575222959622, 1.771799650011764538 ) ) ;
#108620=CARTESIAN_POINT ( 'NONE',  ( 4.282818888323718376, 1.866831796845986435, -0.9415434926851961039 ) ) ;
#108621=CARTESIAN_POINT ( 'NONE',  ( 5.806574285656749268, 1.713600856677459205, 0.9136399477176879724 ) ) ;
#108623=CARTESIAN_POINT ( 'NONE',  ( 0.3749999999841767684, 2.052068128807281955, -2.222409888604170519E-14 ) ) ;
#108624=CARTESIAN_POINT ( 'NONE',  ( 0.6685925339881376717, 1.356301626434471164, 1.492253803477984642 ) ) ;
#108625=ADVANCED_FACE ( 'NONE', ( #81155 ), #150418, .F. ) ;
#108628=CARTESIAN_POINT ( 'NONE',  ( 6.610000000000006537, 0.002781820520842553934, 2.000159646111852929 ) ) ;
#108632=CARTESIAN_POINT ( 'NONE',  ( 3.844227010333609584, 1.817057058749595777, 0.1772887374331885701 ) ) ;
#108633=CARTESIAN_POINT ( 'NONE',  ( 2.661379449941482012, -1.919611247835448342, -1.088434722066232485 ) ) ;
#108638=CARTESIAN_POINT ( 'NONE',  ( 1.476825778181306559, -1.425320297365587408, 1.431352559222300203 ) ) ;
#108642=CARTESIAN_POINT ( 'NONE',  ( 2.588518228195731741, 1.803668244214111871, 0.4575444346353977898 ) ) ;
#108649=CARTESIAN_POINT ( 'NONE',  ( 4.178209475066913647, -1.049361115903378883, 1.493786327181771068 ) ) ;
#108653=CARTESIAN_POINT ( 'NONE',  ( 0.6843859445029027988, -0.9204285295532282918, -1.469136994349945047 ) ) ;
#108654=CARTESIAN_POINT ( 'NONE',  ( 5.753808258465379133, 0.7501079416377672837, 1.681592913607635964 ) ) ;
#108655=CARTESIAN_POINT ( 'NONE',  ( 4.723409996707597536, -0.1167165639803491167, 2.304856601038312913 ) ) ;
#108657=CARTESIAN_POINT ( 'NONE',  ( 0.3861014259941424887, -0.9735654513510684227, 1.816333823429964411 ) ) ;
#108659=CARTESIAN_POINT ( 'NONE',  ( 5.554211264220430877, 2.030576384096828502, -1.076727444025220803 ) ) ;
#108662=CARTESIAN_POINT ( 'NONE',  ( 5.207814216083940018, -1.861544245658670604, 0.1842191830812092979 ) ) ;
#108663=CARTESIAN_POINT ( 'NONE',  ( 2.338023529656753752, -1.104205016203146705, -1.561194055274425452 ) ) ;
#108665=CARTESIAN_POINT ( 'NONE',  ( 4.037865812933420173, -1.521084700717803884, -1.599171214764223636 ) ) ;
#108666=CARTESIAN_POINT ( 'NONE',  ( 4.311780797230674089, -1.305379566919599332, -1.666953740739559819 ) ) ;
#108670=CARTESIAN_POINT ( 'NONE',  ( -0.2108831679770926115, 5.723481173670196043, -2.491210874135452613 ) ) ;
#108673=CARTESIAN_POINT ( 'NONE',  ( 1.958496456072187142, 2.301298802517747877, -0.1708829291464097622 ) ) ;
#108674=CARTESIAN_POINT ( 'NONE',  ( 2.014041202081144011, 1.956828179156915315, -0.1411808619533050091 ) ) ;
#108676=CARTESIAN_POINT ( 'NONE',  ( 6.491093265613332441, 0.1965012520625461223, 2.053163312798581774 ) ) ;
#108678=CARTESIAN_POINT ( 'NONE',  ( 4.153529959351897283, 1.954779968807466295, -0.4946301968136583849 ) ) ;
#108681=CARTESIAN_POINT ( 'NONE',  ( 4.329314735043091389, -1.561880650076686861, -1.275557594027726394 ) ) ;
#108683=DIRECTION ( 'NONE',  ( -0.9999980456341538426, 0.000000000000000000, -0.001977050295941298105 ) ) ;
#108686=CARTESIAN_POINT ( 'NONE',  ( 1.692468234204123734, 1.072632775294654062, -1.887553939074837261 ) ) ;
#108691=CARTESIAN_POINT ( 'NONE',  ( 2.547943918863291302, 1.870051909910470878, 0.05015897750767356333 ) ) ;
#108692=CARTESIAN_POINT ( 'NONE',  ( 0.3157904346527000139, -2.021491663516309156, 0.3995350904514202162 ) ) ;
#108693=CARTESIAN_POINT ( 'NONE',  ( -0.02244404828157658613, 5.719765766439059540, -2.783169749654360814 ) ) ;
#108694=CARTESIAN_POINT ( 'NONE',  ( 6.727182134110222478, 0.005875948494733079785, 1.810970247402940547 ) ) ;
#108698=CARTESIAN_POINT ( 'NONE',  ( 3.492734469894549498, -1.843672829398452784, -0.5074192597756198575 ) ) ;
#108699=CARTESIAN_POINT ( 'NONE',  ( 3.766244448481158802, -1.188900867318806176, 1.311211162958977328 ) ) ;
#108700=CARTESIAN_POINT ( 'NONE',  ( 1.488763880571321030, -1.816176428755595706, -0.5988469716494760897 ) ) ;
#108703=CARTESIAN_POINT ( 'NONE',  ( -0.1708952380198276444, -1.482394133889615828, -1.213259445456981167 ) ) ;
#108705=CARTESIAN_POINT ( 'NONE',  ( 0.6431357727456864515, -0.2518013131528433757, -2.054909676291870380 ) ) ;
#108707=CARTESIAN_POINT ( 'NONE',  ( 5.787941465827733722, -0.8397648285632768328, 1.671655200917811168 ) ) ;
#108708=CARTESIAN_POINT ( 'NONE',  ( 1.963248404482214049, 0.3131683437365209710, -1.798463397695612809 ) ) ;
#108710=CARTESIAN_POINT ( 'NONE',  ( 5.338574060078519423, 2.173733305800494175, 0.3801736985692484305 ) ) ;
#108713=CARTESIAN_POINT ( 'NONE',  ( 3.244635591053147916, -2.031700879476082466, -0.3553325473293292847 ) ) ;
#108721=CARTESIAN_POINT ( 'NONE',  ( 5.107906530550561541, 0.6527686194882609261, -1.964817160181751010 ) ) ;
#108724=CARTESIAN_POINT ( 'NONE',  ( 2.073706595668877384, 2.069181010895416950, -0.6253580070983978390 ) ) ;
#108726=CARTESIAN_POINT ( 'NONE',  ( 3.545573561795499540, -1.865266050240913520, 0.7750044584247675061 ) ) ;
#108727=CARTESIAN_POINT ( 'NONE',  ( 2.014041202081144011, 1.956828179156915315, -0.1411808619533050091 ) ) ;
#108728=CARTESIAN_POINT ( 'NONE',  ( 6.720655732516679137, 3.688991442244013097, 2.587785764416630219 ) ) ;
#108733=CARTESIAN_POINT ( 'NONE',  ( 1.639861632979456418, 2.010800986640928656, -0.1531718788195315928 ) ) ;
#108735=CARTESIAN_POINT ( 'NONE',  ( 6.233935805145816467, 2.167428969419796125, 0.3234103439683775894 ) ) ;
#108737=CARTESIAN_POINT ( 'NONE',  ( 5.765855477156511810, 0.5488314196105298359, -1.831976909803390896 ) ) ;
#108741=CARTESIAN_POINT ( 'NONE',  ( 3.058220425488000327, -1.198843740453523266, 1.621196181159669347 ) ) ;
#108744=CARTESIAN_POINT ( 'NONE',  ( 5.684504558281781250, -1.683600953293447944, -0.3737579273616030706 ) ) ;
#108748=CARTESIAN_POINT ( 'NONE',  ( 4.692568346783878575, -0.4079999995015987091, -1.825350503840660110 ) ) ;
#108751=CARTESIAN_POINT ( 'NONE',  ( 0.7607008448355724317, -0.6940761377024067258, -1.950597895851911456 ) ) ;
#108756=CARTESIAN_POINT ( 'NONE',  ( -0.01774202353897573470, -1.183624524064251116, 1.371566177806067932 ) ) ;
#108761=CARTESIAN_POINT ( 'NONE',  ( 0.9241798626423223251, 0.9638202082158978667, 1.708698881219716137 ) ) ;
#108763=CARTESIAN_POINT ( 'NONE',  ( 5.114804650195723390, 0.1453347504645576271, 1.910168102697987313 ) ) ;
#108771=CARTESIAN_POINT ( 'NONE',  ( 2.606508400632711719, -0.8264410288459265175, -1.997682696722333562 ) ) ;
#108775=CARTESIAN_POINT ( 'NONE',  ( 4.893472065931465664, 1.353474861756031267, 1.225258530246610134 ) ) ;
#108777=CARTESIAN_POINT ( 'NONE',  ( 1.176956626245349247, -0.04423564266526488348, -1.971012800895243888 ) ) ;
#108778=CARTESIAN_POINT ( 'NONE',  ( 3.797043250571481732, -0.1924442655423033721, -1.902711443722324258 ) ) ;
#108781=CARTESIAN_POINT ( 'NONE',  ( 4.721133488271325618, -1.758435714881977141, -0.8873337903104687729 ) ) ;
#108783=CARTESIAN_POINT ( 'NONE',  ( 5.935097076209718381, -1.409686562828060152, -1.336055723097711256 ) ) ;
#108787=CARTESIAN_POINT ( 'NONE',  ( 6.240501835383900797, 1.219778281852833546, -1.734492557903525523 ) ) ;
#108789=CARTESIAN_POINT ( 'NONE',  ( 3.440010667329951310, -1.141173813254949820, -1.534285795567114974 ) ) ;
#108792=CARTESIAN_POINT ( 'NONE',  ( 0.07755575628183573877, -0.002876890934064984216, -2.188974970840869005 ) ) ;
#108794=CARTESIAN_POINT ( 'NONE',  ( 5.180342516426402533, 0.9943292982247069478, 1.750330089345548679 ) ) ;
#108796=CARTESIAN_POINT ( 'NONE',  ( 5.795480788678070816, 1.385457615097264394, 1.189071861804301466 ) ) ;
#108797=CARTESIAN_POINT ( 'NONE',  ( 1.609917502266303480, 0.6029389078928657497, -1.980602105166151095 ) ) ;
#108799=( BOUNDED_SURFACE ( )  B_SPLINE_SURFACE ( 3, 3, ( 
 ( #197022, #126784, #193815, #10792, #208986, #192740, #186891, #139232, #56904, #170647 ),
 ( #22233, #154409, #180773, #101383, #103525, #19053, #203128, #88345, #54771, #3847 ),
 ( #205263, #35306, #120918, #55835, #38523, #85132, #121991, #118762, #36374, #151219 ),
 ( #68859, #20117, #136031, #153338, #5988, #204179, #187957, #200988, #171715, #184747 ),
 ( #23314, #169584, #21167, #52634, #155472, #102452, #168518, #86202, #202044, #72884 ),
 ( #25209, #91313, #193041, #157370, #8964, #43629, #141154, #124941, #77162, #190903 ),
 ( #138991, #205012, #42567, #44695, #176807, #188781, #109744, #108670, #27346, #28423 ) ),
 .UNSPECIFIED., .T., .F., .T. ) 
 B_SPLINE_SURFACE_WITH_KNOTS ( ( 4, 3, 4 ),
 ( 4, 1, 1, 1, 1, 1, 1, 4 ),
 ( 0.000000000000000000, 0.5000000000000000000, 1.000000000000000000 ),
 ( 0.000000000000000000, 0.09705918685507786137, 0.1907419858981972138, 0.2602182418918835838, 0.3625179829595637226, 0.5215049497019805802, 0.7338397267804015467, 1.000000000000000000 ),
 .UNSPECIFIED. ) 
 GEOMETRIC_REPRESENTATION_ITEM ( )  RATIONAL_B_SPLINE_SURFACE ( (
 ( 1.000000000000000000, 1.000000000000000000, 1.000000000000000000, 1.000000000000000222, 1.000000000000000222, 0.9999999999999994449, 1.000000000000000444, 0.9999999999999997780, 1.000000000000000000, 1.000000000000000000),
 ( 0.3333333333333333703, 0.3333333333333333703, 0.3333333333333333703, 0.3333333333333334259, 0.3333333333333333703, 0.3333333333333332038, 0.3333333333333335369, 0.3333333333333332038, 0.3333333333333333703, 0.3333333333333333703),
 ( 0.3333333333333333703, 0.3333333333333333703, 0.3333333333333333703, 0.3333333333333334259, 0.3333333333333333703, 0.3333333333333332038, 0.3333333333333335369, 0.3333333333333332038, 0.3333333333333333703, 0.3333333333333333703),
 ( 1.000000000000000000, 1.000000000000000000, 1.000000000000000000, 1.000000000000000222, 1.000000000000000222, 0.9999999999999994449, 1.000000000000000444, 0.9999999999999997780, 1.000000000000000000, 1.000000000000000000),
 ( 0.3333333333333333703, 0.3333333333333333703, 0.3333333333333333703, 0.3333333333333334259, 0.3333333333333333703, 0.3333333333333332038, 0.3333333333333335369, 0.3333333333333332038, 0.3333333333333333703, 0.3333333333333333703),
 ( 0.3333333333333333703, 0.3333333333333333703, 0.3333333333333333703, 0.3333333333333334259, 0.3333333333333333703, 0.3333333333333332038, 0.3333333333333335369, 0.3333333333333332038, 0.3333333333333333703, 0.3333333333333333703),
 ( 1.000000000000000000, 1.000000000000000000, 1.000000000000000000, 1.000000000000000222, 1.000000000000000222, 0.9999999999999994449, 1.000000000000000444, 0.9999999999999997780, 1.000000000000000000, 1.000000000000000000) ) ) 
 REPRESENTATION_ITEM ( '' )  SURFACE ( )  );
#108804=B_SPLINE_CURVE_WITH_KNOTS ( 'NONE', 3,
 ( #134349, #200352, #114929, #199289, #35734, #184113, #119187, #101809, #4273, #50934, #183055 ),
 .UNSPECIFIED., .F., .F.,
 ( 4, 1, 1, 1, 1, 1, 1, 1, 4 ),
 ( 0.000000000000000000, 0.2254494161556361009, 0.3971188491599597081, 0.5240836380151728813, 0.6154273167216615104, 0.6803253696226415626, 0.7282602231486813293, 0.7688932809586735972, 1.000000000000000000 ),
 .UNSPECIFIED. ) ;
#108809=CARTESIAN_POINT ( 'NONE',  ( 6.925078400183553029, 0.5781763343528348864, 2.007479843201316783 ) ) ;
#108811=CARTESIAN_POINT ( 'NONE',  ( 4.377415392590312315, -0.3859441149459389431, -1.690453949067998840 ) ) ;
#108812=CLOSED_SHELL ( 'NONE', ( #195089, #116761, #41587, #102962, #28510, #128210, #159385, #17251 ) ) ;
#108814=CARTESIAN_POINT ( 'NONE',  ( 2.237250781069185734, -0.09733102107959036575, -2.068066387140480522 ) ) ;
#108815=CARTESIAN_POINT ( 'NONE',  ( 3.445011857661818944, -1.868279436719679110, -0.9960484452814029055 ) ) ;
#108818=CARTESIAN_POINT ( 'NONE',  ( 1.815228950277411712, -1.686530385472130744, -1.016810816036699316 ) ) ;
#108822=CARTESIAN_POINT ( 'NONE',  ( 3.732637569912560682, 0.3354268113090127512, 2.267480163388153169 ) ) ;
#108823=CARTESIAN_POINT ( 'NONE',  ( 2.051128252772801641, -1.465761996925790900, -1.088229512710245261 ) ) ;
#108827=CARTESIAN_POINT ( 'NONE',  ( 2.566654749391559687, 0.6821283815301434350, 1.894225559998161668 ) ) ;
#108828=CARTESIAN_POINT ( 'NONE',  ( 2.623818369222921554, 1.924856029493416276, -0.3778354045670463401 ) ) ;
#108831=CARTESIAN_POINT ( 'NONE',  ( 0.07536363704233049743, 0.2309889609098912111, -2.177957698420322163 ) ) ;
#108832=CARTESIAN_POINT ( 'NONE',  ( 5.525362607580523111, -1.325732906064909677, -1.616523167544873241 ) ) ;
#108833=CARTESIAN_POINT ( 'NONE',  ( 3.098275772329066591, -0.5124342443764763333, -1.694037474313156988 ) ) ;
#108835=CARTESIAN_POINT ( 'NONE',  ( 6.667932745306283771, -1.416340830354723135, 1.803254352984103859 ) ) ;
#108836=CARTESIAN_POINT ( 'NONE',  ( 6.070193552946823168, -1.654735283430305515, -0.5392940629580407208 ) ) ;
#108838=CARTESIAN_POINT ( 'NONE',  ( 6.504485943970635731, -2.231000991611901352, 0.5533298437200293574 ) ) ;
#108839=CARTESIAN_POINT ( 'NONE',  ( 0.1333692844072585093, 7.629137130509075604, -2.653547345224527287 ) ) ;
#108840=CARTESIAN_POINT ( 'NONE',  ( 5.325445489366991580, -1.254443461812755789, 1.197174301038748334 ) ) ;
#108841=CARTESIAN_POINT ( 'NONE',  ( 5.477072320546296780, 2.003985016195033886, 0.8359633449262526828 ) ) ;
#108843=CARTESIAN_POINT ( 'NONE',  ( -0.2408018239684434625, -0.007136184528846663787, -2.100252307185761058 ) ) ;
#108844=CARTESIAN_POINT ( 'NONE',  ( 5.718750000000003553, -0.7852924748296825630, 1.895863743164203141 ) ) ;
#108846=CARTESIAN_POINT ( 'NONE',  ( 3.873980538081963854, 1.069312750484844088, 1.602167800089354222 ) ) ;
#108848=CARTESIAN_POINT ( 'NONE',  ( 6.275645185405086757, 0.3810096023663198661, -2.188332947720336819 ) ) ;
#108853=CARTESIAN_POINT ( 'NONE',  ( 2.139591745018020408, 0.003451857093505344976, 2.221473417793240923 ) ) ;
#108859=CARTESIAN_POINT ( 'NONE',  ( 0.2818752512256904597, 1.674885806461807958, -1.122501178855893400 ) ) ;
#108861=CARTESIAN_POINT ( 'NONE',  ( 5.846154128119951388, -0.9308047640707247661, 1.840808156992862932 ) ) ;
#108868=CARTESIAN_POINT ( 'NONE',  ( 0.9832602892492541269, 1.182927327958797070, 1.316506037215345426 ) ) ;
#108870=CARTESIAN_POINT ( 'NONE',  ( 0.1939827082095749167, 1.755770691208278889, 0.9913967135185000057 ) ) ;
#108871=CARTESIAN_POINT ( 'NONE',  ( 6.128409194715155550, 0.1798751216713200540, 1.731140798666473968 ) ) ;
#108872=CARTESIAN_POINT ( 'NONE',  ( 3.632637656275085281, 0.3374270351050281946, 2.267304333945507011 ) ) ;
#108874=CARTESIAN_POINT ( 'NONE',  ( 2.571990918753517708, -1.761868631437716548, -0.5344257538507578564 ) ) ;
#108877=CARTESIAN_POINT ( 'NONE',  ( 2.889462524698828361, 1.289687736819044472, 1.292329967842877014 ) ) ;
#108878=CARTESIAN_POINT ( 'NONE',  ( 3.797500137148449362, 1.423962148579031917, -1.427936706820939872 ) ) ;
#108880=CARTESIAN_POINT ( 'NONE',  ( 2.694485044408474916, -2.256396476877442492, -0.1672753843019215703 ) ) ;
#108882=CARTESIAN_POINT ( 'NONE',  ( 5.491282870796595716, 1.858858430755592428, -0.9897807336930256605 ) ) ;
#108885=CARTESIAN_POINT ( 'NONE',  ( 2.594261239525695206, 0.9781076984213372683, -1.824767828009652426 ) ) ;
#108888=CARTESIAN_POINT ( 'NONE',  ( 4.196021508500130004, 1.385991406618786836, 1.604897850144955340 ) ) ;
#108890=CARTESIAN_POINT ( 'NONE',  ( 1.031717895469780988, -1.221320771479022627, -1.489887157414800267 ) ) ;
#108896=CARTESIAN_POINT ( 'NONE',  ( 5.818629517237746462, -0.7649446623404360102, -1.977987144599784086 ) ) ;
#108897=CARTESIAN_POINT ( 'NONE',  ( 1.676933785844336944, -1.999498008410249383, -0.6612845060171600453 ) ) ;
#108900=CARTESIAN_POINT ( 'NONE',  ( 6.244940914744545601, -0.2718465296328761438, -1.840820509183779263 ) ) ;
#108908=CARTESIAN_POINT ( 'NONE',  ( 3.508209890309890167, 1.962046631884439174, 0.002529298861464468473 ) ) ;
#108909=CARTESIAN_POINT ( 'NONE',  ( 0.5148121308554790554, 1.489681748880047563, -1.566682057046255849 ) ) ;
#108914=CARTESIAN_POINT ( 'NONE',  ( 2.607021377293942344, -1.721407032317923802, 0.2550150930856145970 ) ) ;
#108917=CARTESIAN_POINT ( 'NONE',  ( 1.809922493048341297, -1.704678386728165185, 1.076150803433255865 ) ) ;
#108918=CARTESIAN_POINT ( 'NONE',  ( 6.825078400183511640, 3.679815135839346496, 2.758192972206894744 ) ) ;
#108920=CARTESIAN_POINT ( 'NONE',  ( 2.131653300961271924, -1.286245803994587877, -1.494167145092902160 ) ) ;
#108922=CARTESIAN_POINT ( 'NONE',  ( 5.590081826628392925, 1.144292256163012667, 1.532101299821154949 ) ) ;
#108928=CARTESIAN_POINT ( 'NONE',  ( 0.9791725360285336022, -1.826886329348556881, -0.8614179918085950183 ) ) ;
#108930=CARTESIAN_POINT ( 'NONE',  ( 5.649573025266686699, -1.814708426832438048, -1.425321367006604056 ) ) ;
#108931=CARTESIAN_POINT ( 'NONE',  ( 6.777797683793751915, -1.903277019102869616, 0.4755351429900215310 ) ) ;
#108932=CARTESIAN_POINT ( 'NONE',  ( 2.729291793292155432, 0.1011638768560127188, -1.959297240552673181 ) ) ;
#108934=CARTESIAN_POINT ( 'NONE',  ( 0.1588275700346117869, 1.163271727376416376, 1.646837250247008777 ) ) ;
#108936=CARTESIAN_POINT ( 'NONE',  ( 0.7786901736592425349, -0.5205582433389954744, -2.052224243718490992 ) ) ;
#108939=CARTESIAN_POINT ( 'NONE',  ( 1.904012794591736668, 1.364881752761820222, -1.235849761865935870 ) ) ;
#108942=CARTESIAN_POINT ( 'NONE',  ( 3.129257641292593650, 1.918792544363761454, 0.9031103230835100248 ) ) ;
#108947=CARTESIAN_POINT ( 'NONE',  ( 3.919256602636957076, -0.1552153454438681413, 2.055015938418188526 ) ) ;
#108949=CARTESIAN_POINT ( 'NONE',  ( 1.417261839328866513, -1.023339270300478221, -1.530466495063505628 ) ) ;
#108954=CARTESIAN_POINT ( 'NONE',  ( 1.577102763248950046, -2.096353118739826993, -0.6898709473643764856 ) ) ;
#108955=CARTESIAN_POINT ( 'NONE',  ( 2.355063576532693936, -1.750152493129919717, 1.433722681173225100 ) ) ;
#108957=CARTESIAN_POINT ( 'NONE',  ( 1.968756957844201239, -1.398423508019512651, 1.151565528817798834 ) ) ;
#108958=CARTESIAN_POINT ( 'NONE',  ( 2.553800400642152635, 1.028702656226655465, 1.615903109786074099 ) ) ;
#108959=CARTESIAN_POINT ( 'NONE',  ( 4.580570967453869713, 1.276285970795057345, -1.630082184409971324 ) ) ;
#108961=CARTESIAN_POINT ( 'NONE',  ( 2.975414797803474176, 1.872564425654202225, -0.6168198417838985925 ) ) ;
#108962=CARTESIAN_POINT ( 'NONE',  ( 6.516243422921982109, -0.9108434941001318785, -1.697579817862464147 ) ) ;
#108963=CARTESIAN_POINT ( 'NONE',  ( 4.451927283622527654, 1.870250842541102410, -0.04591718433973044494 ) ) ;
#108964=CARTESIAN_POINT ( 'NONE',  ( 1.805729983942544026, 1.920404770136320716, 1.279379207282659969 ) ) ;
#108966=CARTESIAN_POINT ( 'NONE',  ( 3.701460696238024539, -1.407827198975480032, -1.217257945129922803 ) ) ;
#108973=CARTESIAN_POINT ( 'NONE',  ( 0.5398470734442856189, -1.490880511344143011, -1.487817205855391789 ) ) ;
#108975=CARTESIAN_POINT ( 'NONE',  ( 5.905597126736788383, -0.5315564325061740147, 2.095088507090197893 ) ) ;
#108976=CARTESIAN_POINT ( 'NONE',  ( 2.514065211524143084, -0.6609878990531635745, 2.015050547854141172 ) ) ;
#108977=CARTESIAN_POINT ( 'NONE',  ( 6.217445935018812264, 1.680332259792745475, 1.120195391490413472 ) ) ;
#108980=CARTESIAN_POINT ( 'NONE',  ( 1.265152180075890254, -1.953616520262021039, -0.9254636565915741464 ) ) ;
#108982=CARTESIAN_POINT ( 'NONE',  ( 6.825078400183573812, 7.629137130509070275, 2.455651831298297338 ) ) ;
#108985=CARTESIAN_POINT ( 'NONE',  ( 5.278529876733943915, -0.4946281652532491524, -1.954780475499573900 ) ) ;
#108989=CARTESIAN_POINT ( 'NONE',  ( 6.350466702034289312, 0.6732396885240909956, 2.054270918568662729 ) ) ;
#108994=CARTESIAN_POINT ( 'NONE',  ( 6.222279831957801655, 1.994873610751910942, 0.2930524845206964879 ) ) ;
#108996=CARTESIAN_POINT ( 'NONE',  ( 6.883263157960358924, 7.052235917045241997, 2.651962373728885325 ) ) ;
#108998=CARTESIAN_POINT ( 'NONE',  ( 2.771755371404661439, 0.9226176164769549493, 1.457180633135872094 ) ) ;
#109002=CARTESIAN_POINT ( 'NONE',  ( 1.123854678948147834, 1.060202766368176786, -1.416847970540972668 ) ) ;
#109003=CARTESIAN_POINT ( 'NONE',  ( 2.473293533796361299, -1.752518403998115426, -0.9904139345979168230 ) ) ;
#109005=CARTESIAN_POINT ( 'NONE',  ( 4.155453238874762256, -1.833011353516471154, -1.228491751752130545 ) ) ;
#109009=CARTESIAN_POINT ( 'NONE',  ( 2.877707679121459083, 0.3088738507561124558, -2.097740099398600400 ) ) ;
#109010=CARTESIAN_POINT ( 'NONE',  ( 2.407827563459669307, -1.163288551851604513, -1.646826728940099738 ) ) ;
#109011=CARTESIAN_POINT ( 'NONE',  ( 3.814574336081223649, -0.5739048956562255999, -1.718320587032542202 ) ) ;
#109017=CARTESIAN_POINT ( 'NONE',  ( 6.586557105272873969, -1.791547847876047594, -0.3505316570680468979 ) ) ;
#109019=CARTESIAN_POINT ( 'NONE',  ( 1.534256617913127174, 0.6047330867673149646, 1.817800723622571057 ) ) ;
#109028=CARTESIAN_POINT ( 'NONE',  ( 2.619513681940002670, 1.793805257907291395, 1.130712135851599687 ) ) ;
#109029=CARTESIAN_POINT ( 'NONE',  ( -0.1298852118744100725, 7.629137130509058728, -2.326516543997098729 ) ) ;
#109031=CARTESIAN_POINT ( 'NONE',  ( 4.956303624527079066, 0.7517850369052423432, 1.822569506419220220 ) ) ;
#109032=CARTESIAN_POINT ( 'NONE',  ( 6.275647926998929371, 0.3200337115364471074, -1.885262484646982095 ) ) ;
#109034=CARTESIAN_POINT ( 'NONE',  ( 6.192584684491233560, 1.567513771475435247, -1.423521977300482577 ) ) ;
#109036=CARTESIAN_POINT ( 'NONE',  ( 1.891162872569674080, 0.2007839719405465906, 2.060584128686280714 ) ) ;
#109037=CARTESIAN_POINT ( 'NONE',  ( 3.187375889530741802, -0.7864489302777454283, 1.775747734548535961 ) ) ;
#109041=CARTESIAN_POINT ( 'NONE',  ( 3.257844248621785788, 0.9402718649541740303, 1.867333078124802315 ) ) ;
#109044=CARTESIAN_POINT ( 'NONE',  ( 0.6096459265214678735, -0.6533943968328138618, 1.689718745909152053 ) ) ;
#109045=ORIENTED_EDGE ( 'NONE', *, *, #81110, .T. ) ;
#109046=CARTESIAN_POINT ( 'NONE',  ( 5.848300530743933301, 2.204158087718602221, 0.1119919437090263481 ) ) ;
#109048=CARTESIAN_POINT ( 'NONE',  ( 3.329339556154627289, 0.05228039400686017302, 2.206313527657398854 ) ) ;
#109051=CARTESIAN_POINT ( 'NONE',  ( 3.422422624566554994, -0.7774026117220147469, -1.747318718686732275 ) ) ;
#109053=CARTESIAN_POINT ( 'NONE',  ( 5.389151899530504330, 0.1487064154041470299, 2.065066873896327593 ) ) ;
#109056=CARTESIAN_POINT ( 'NONE',  ( 3.081113354808207916, -0.1575343947536785305, -2.156009052512488200 ) ) ;
#109057=CARTESIAN_POINT ( 'NONE',  ( 5.126606437771586755, 0.1607948393855564151, 2.185736094377451089 ) ) ;
#109069=CARTESIAN_POINT ( 'NONE',  ( 5.489151832033660305, 0.1466973765328460355, 2.065091666743318122 ) ) ;
#109070=CARTESIAN_POINT ( 'NONE',  ( 4.072816532378962684, -1.798017144868354178, -0.6922151418781684606 ) ) ;
#109071=CARTESIAN_POINT ( 'NONE',  ( 0.4566579290818244541, -1.899626807963299635, -0.6766942018802262204 ) ) ;
#109075=CARTESIAN_POINT ( 'NONE',  ( 5.172688686914132639, 1.361056241693802349, -1.423677202773800721 ) ) ;
#109076=CARTESIAN_POINT ( 'NONE',  ( 6.720655732516684466, -0.007268404184076341853, 2.273772995263834140 ) ) ;
#109077=CARTESIAN_POINT ( 'NONE',  ( 4.793472150574508817, 1.354911484294840429, 1.223852735664505698 ) ) ;
#109079=EDGE_CURVE ( 'NONE', #40760, #63091, #71722, .T. ) ;
#109085=CARTESIAN_POINT ( 'NONE',  ( 2.788419073117563762, 1.577926727847511312, -0.9486480243563880643 ) ) ;
#109086=CARTESIAN_POINT ( 'NONE',  ( 5.959245303985257536, -1.698412939339728700, 1.080668751846917797 ) ) ;
#109087=CARTESIAN_POINT ( 'NONE',  ( 0.5272844384777974902, 2.272924705895418285, -0.3403917945235325204 ) ) ;
#109088=CARTESIAN_POINT ( 'NONE',  ( 5.242999579849755953, -0.2363135928187160284, -1.947375393322479109 ) ) ;
#109092=CARTESIAN_POINT ( 'NONE',  ( 0.7485892145711986467, -2.054541080789675789, -0.2550698046258002005 ) ) ;
#109094=CARTESIAN_POINT ( 'NONE',  ( 1.610996488345920907, -0.2524672473064055733, 2.075362222853482930 ) ) ;
#109095=CARTESIAN_POINT ( 'NONE',  ( 0.4966798268824790252, 1.557709316500059726, -1.035497600327957235 ) ) ;
#109096=CARTESIAN_POINT ( 'NONE',  ( 1.423203639035979906, 0.8144988626696235690, 1.844428818423976546 ) ) ;
#109097=EDGE_LOOP ( 'NONE', ( #150170, #159202 ) ) ;
#109100=CARTESIAN_POINT ( 'NONE',  ( 1.909305195714078307, -0.8207579233160157139, -1.534770245041901182 ) ) ;
#109104=CARTESIAN_POINT ( 'NONE',  ( 2.666273504311657661, -1.189765394598929937, 1.249106299861786118 ) ) ;
#109105=CARTESIAN_POINT ( 'NONE',  ( 2.859115728684503477, 0.3189004193784421015, -2.168101852914063876 ) ) ;
#109106=CARTESIAN_POINT ( 'NONE',  ( 4.793709216081707858, 1.633822259641436903, 1.483752339651790653 ) ) ;
#109108=CARTESIAN_POINT ( 'NONE',  ( 2.237404288245536943, -0.1031769000767470690, -2.168708286310920386 ) ) ;
#109109=CARTESIAN_POINT ( 'NONE',  ( 1.523764310407935030, -1.012771255265769943, -1.518815351243132383 ) ) ;
#109110=CARTESIAN_POINT ( 'NONE',  ( 3.749298086285374865, 0.2552367968642406115, -2.101811201404654827 ) ) ;
#109114=CARTESIAN_POINT ( 'NONE',  ( 3.650172380179962150, 0.8259502761284505112, 2.138564905064809896 ) ) ;
#109118=CARTESIAN_POINT ( 'NONE',  ( 6.358078514681034576, 0.8530912398192547208, -2.051143523256500067 ) ) ;
#109126=CARTESIAN_POINT ( 'NONE',  ( 4.447888798048591497, -1.802416534049579910, -0.9041112711936499791 ) ) ;
#109128=CARTESIAN_POINT ( 'NONE',  ( 3.784078317859154605, -1.224626257592566159, -1.659553996539532283 ) ) ;
#109134=CARTESIAN_POINT ( 'NONE',  ( 6.580031370938625557, -2.148343778048496411, -0.4316624935760752790 ) ) ;
#109135=CARTESIAN_POINT ( 'NONE',  ( 4.026017654026761150, -1.753031021560845559, 0.9963007555989014108 ) ) ;
#109136=CARTESIAN_POINT ( 'NONE',  ( 2.454439063956286304, -1.602943312447857593, -0.9057913635923324769 ) ) ;
#109138=CARTESIAN_POINT ( 'NONE',  ( 6.176747059734421619, -1.734417727105644680, -0.5698399933231483860 ) ) ;
#109139=CARTESIAN_POINT ( 'NONE',  ( -0.1219072497536327904, -0.5225375287686329084, -2.247936139081475382 ) ) ;
#109141=CARTESIAN_POINT ( 'NONE',  ( 6.139586942761116717, -1.633760600410700592, -1.565427815648293031 ) ) ;
#109143=CARTESIAN_POINT ( 'NONE',  ( 1.823018060162405085, 1.965545597939293954, 0.7568914254860066304 ) ) ;
#109153=CARTESIAN_POINT ( 'NONE',  ( 2.021885665735908333, -0.4598567139443253682, 2.069992740399699382 ) ) ;
#109154=CARTESIAN_POINT ( 'NONE',  ( 3.305138010220570521, -0.4367349056570711263, -2.177900917948209614 ) ) ;
#109155=CARTESIAN_POINT ( 'NONE',  ( 0.1357705729100426029, -2.015811560716780360, 0.8986578214904348272 ) ) ;
#109158=CARTESIAN_POINT ( 'NONE',  ( 4.703538834289092030, -1.515240342570793430, -1.246145567450624991 ) ) ;
#109166=CARTESIAN_POINT ( 'NONE',  ( 3.849942018323779358, -1.464806807754112539, -1.533599281611098597 ) ) ;
#109168=CARTESIAN_POINT ( 'NONE',  ( 4.452137864729129646, 2.161286467946467837, -0.05003489268536746859 ) ) ;
#109169=CARTESIAN_POINT ( 'NONE',  ( 4.317794123949899365, 1.129187743159822288, -1.454283868005897151 ) ) ;
#109172=CARTESIAN_POINT ( 'NONE',  ( 6.281193118957388855, 1.205677877666534892, 1.255287683557136491 ) ) ;
#109173=CARTESIAN_POINT ( 'NONE',  ( 6.727182134110203826, 0.5859025467632031914, 1.963451964196837984 ) ) ;
#109176=CARTESIAN_POINT ( 'NONE',  ( 3.713887418366210280, -2.130098009959373151, 0.3673708613747132534 ) ) ;
#109178=CARTESIAN_POINT ( 'NONE',  ( 5.677111188754776272, -0.9039728708103295096, -1.802140534545144890 ) ) ;
#109180=CARTESIAN_POINT ( 'NONE',  ( 3.854492016355787420, 0.7758605394001509836, 2.017853709245204463 ) ) ;
#109181=CARTESIAN_POINT ( 'NONE',  ( 3.321511454083085457, -1.900871985879136528, 0.5222822307265824193 ) ) ;
#109184=CARTESIAN_POINT ( 'NONE',  ( 1.308152564336163115, -0.5581994038030186900, 2.238931160296030232 ) ) ;
#109185=CARTESIAN_POINT ( 'NONE',  ( 2.038423305949757847, 2.037923218716758633, 0.3053300769366319445 ) ) ;
#109186=CARTESIAN_POINT ( 'NONE',  ( 4.739756017840593749, 1.937102985688110568, 0.1393878014490906314 ) ) ;
#109196=CARTESIAN_POINT ( 'NONE',  ( 1.958336283151569157, 2.200835622443702011, -0.1624582802550941507 ) ) ;
#109198=CARTESIAN_POINT ( 'NONE',  ( 6.895372015613538075, -1.753720159772365284, 0.8792710811909019153 ) ) ;
#109199=CARTESIAN_POINT ( 'NONE',  ( -0.02919842301648319441, 0.2290444945237135044, -2.107092690553781456 ) ) ;
#109201=CARTESIAN_POINT ( 'NONE',  ( 0.1749903794560644099, 4.092791488633133135, -2.510332109122221045 ) ) ;
#109203=CARTESIAN_POINT ( 'NONE',  ( 5.876868881424701208, 1.699447150514224125, -0.7087742222662285485 ) ) ;
#109209=CARTESIAN_POINT ( 'NONE',  ( 6.275647701495586261, 0.3610785225884837746, -2.089460823871174266 ) ) ;
#109213=CARTESIAN_POINT ( 'NONE',  ( 0.3915709625425906615, 1.526647161510179318, 1.384594130533061129 ) ) ;
#109215=CARTESIAN_POINT ( 'NONE',  ( 1.398636348511049565, 0.3583461405318502102, 1.826042456754966681 ) ) ;
#109216=CARTESIAN_POINT ( 'NONE',  ( 4.317794123949899365, 1.129187743159822288, -1.454283868005897151 ) ) ;
#109223=CARTESIAN_POINT ( 'NONE',  ( 4.811249113497881424, 1.919052844561389692, 1.089612025192594258 ) ) ;
#109224=CARTESIAN_POINT ( 'NONE',  ( 6.186863813140405455, -0.3229369685709322924, -2.239133911541963506 ) ) ;
#109226=CARTESIAN_POINT ( 'NONE',  ( -0.08783152977152529350, -1.912005390248720627, -0.04503566501021933483 ) ) ;
#109227=CARTESIAN_POINT ( 'NONE',  ( 6.139839150192680783, 1.910077931696544384, -0.1482136438759658337 ) ) ;
#109229=CARTESIAN_POINT ( 'NONE',  ( 0.07536363704230969462, 1.333366039338843789, -2.397125032416930424 ) ) ;
#109230=CARTESIAN_POINT ( 'NONE',  ( 5.777967262743825216, 1.883199444611630469, -0.3313529498064629042 ) ) ;
#109232=CARTESIAN_POINT ( 'NONE',  ( 1.217418975555501826, -1.825842229346545498, 0.4062821374252246764 ) ) ;
#109233=CARTESIAN_POINT ( 'NONE',  ( 2.378138974734815392, -2.011451771401792321, -0.1435188914247695346 ) ) ;
#109235=CARTESIAN_POINT ( 'NONE',  ( 4.143269384990833970, -1.832638288540566318, 1.037631460274644812 ) ) ;
#109240=CARTESIAN_POINT ( 'NONE',  ( 2.689718276569666333, 1.916506935140523726, -0.6377304922457660563 ) ) ;
#109245=CARTESIAN_POINT ( 'NONE',  ( 4.253314833958360630, -1.794556715717060769, -1.204719293387515267 ) ) ;
#109251=CARTESIAN_POINT ( 'NONE',  ( 2.471331864234734610, 1.938535094165691142, 0.9779774689679074928 ) ) ;
#109254=CARTESIAN_POINT ( 'NONE',  ( 0.9426144736941791669, -1.451487892885485742, -1.132780452900377099 ) ) ;
#109256=CARTESIAN_POINT ( 'NONE',  ( 1.575987392057216940, -1.168677030305173004, 1.853764812240476623 ) ) ;
#109258=CARTESIAN_POINT ( 'NONE',  ( 3.221791447092836602, -2.180992460559240786, 0.6016781482265749492 ) ) ;
#109264=CARTESIAN_POINT ( 'NONE',  ( 4.393649985211129483, -0.6784793013954493190, 1.634714195790587077 ) ) ;
#109266=CARTESIAN_POINT ( 'NONE',  ( 0.5343771797220103759, 1.082321145649869587, -1.806417116151628477 ) ) ;
#109270=CARTESIAN_POINT ( 'NONE',  ( 6.064077406165095496, -1.076301619396256237, 1.704949653848472302 ) ) ;
#109275=CARTESIAN_POINT ( 'NONE',  ( 3.977312496258199825, 1.761605600429091201, -0.6297503393934977822 ) ) ;
#109276=CARTESIAN_POINT ( 'NONE',  ( 3.907136544319700810, -1.695332804699274387, 1.187946514627869821 ) ) ;
#109284=CARTESIAN_POINT ( 'NONE',  ( 3.771884902471400292, -1.933230903833718539, 0.3329965046865584477 ) ) ;
#109285=CARTESIAN_POINT ( 'NONE',  ( 2.548203688163702463, 1.844428314090811538, -0.8144999995377337765 ) ) ;
#109288=CARTESIAN_POINT ( 'NONE',  ( 0.6142526126209290060, 1.294576594435635108, -1.350420462534522859 ) ) ;
#109290=CARTESIAN_POINT ( 'NONE',  ( 2.883067256526872235, -1.861736025891271407, -0.7665772676846579481 ) ) ;
#109292=CARTESIAN_POINT ( 'NONE',  ( 3.462624114536147157, -2.041159069107215007, -0.5622701121768166610 ) ) ;
#109294=CARTESIAN_POINT ( 'NONE',  ( 4.949704645232674061, 1.531818663031824013, 1.392983054852282132 ) ) ;
#109296=CARTESIAN_POINT ( 'NONE',  ( 0.5563344311030217204, -1.511574431613523117, 1.444666882759609194 ) ) ;
#109298=CARTESIAN_POINT ( 'NONE',  ( 5.174738384962677351, -1.719472664011096219, -0.6136495084824307167 ) ) ;
#109305=CARTESIAN_POINT ( 'NONE',  ( 6.305323439471717251, 1.661359358424657318, -0.9468341723649562613 ) ) ;
#109320=CARTESIAN_POINT ( 'NONE',  ( -0.1399997263889819765, 0.7174702203470960660, -2.082715917450683740 ) ) ;
#109325=CARTESIAN_POINT ( 'NONE',  ( 2.535944157116743369, 1.207843060446149197, 1.555523554018751309 ) ) ;
#109326=CARTESIAN_POINT ( 'NONE',  ( 3.216422893352603563, 1.967893637826668263, 0.4390085219014849827 ) ) ;
#109328=CARTESIAN_POINT ( 'NONE',  ( 6.827182134110219458, 3.682144966263278363, 2.702925436647874324 ) ) ;
#109329=CARTESIAN_POINT ( 'NONE',  ( 3.222796723461582413, 0.05406831605479084368, 2.190948157972896659 ) ) ;
#109331=CARTESIAN_POINT ( 'NONE',  ( 1.834862671528534994, 0.1865727292883790633, 1.917327306167202261 ) ) ;
#109334=CARTESIAN_POINT ( 'NONE',  ( 0.2333540202161402677, 0.7093705336200817335, -2.128223931541360248 ) ) ;
#109341=CARTESIAN_POINT ( 'NONE',  ( 5.495603940606402560, -1.841430844871448258, 0.006098274996368944698 ) ) ;
#109342=CARTESIAN_POINT ( 'NONE',  ( 2.684242053459008570, 1.078846248543659403, 1.699430804756915547 ) ) ;
#109343=CARTESIAN_POINT ( 'NONE',  ( 4.148081960540086932, -0.2207414774363871957, -2.287749835899715034 ) ) ;
#109344=CARTESIAN_POINT ( 'NONE',  ( -0.02880301295722554472, 4.079423595021631321, -2.828475351696632778 ) ) ;
#109345=CARTESIAN_POINT ( 'NONE',  ( 3.379601846096703888, -1.794663673993960540, 0.4920686967917423105 ) ) ;
#109347=CARTESIAN_POINT ( 'NONE',  ( -0.1290005225502918740, 6.946858002156244716, -2.769053915224591211 ) ) ;
#109348=CARTESIAN_POINT ( 'NONE',  ( 6.310809538426106258, -0.5167911955388967415, -1.841158844219364044 ) ) ;
#109351=CARTESIAN_POINT ( 'NONE',  ( 5.442948297640814559, -1.648798800320664615, -1.285478093666903687 ) ) ;
#109355=CARTESIAN_POINT ( 'NONE',  ( 5.672382752830540831, -1.089361703149527072, 1.337344134918318606 ) ) ;
#109357=CARTESIAN_POINT ( 'NONE',  ( 1.213026639236804316, 1.670944716536880259, 0.4636423645143650241 ) ) ;
#109362=CARTESIAN_POINT ( 'NONE',  ( 5.946172770594575496, -0.9833217254726284162, 1.935730195829394429 ) ) ;
#109363=CARTESIAN_POINT ( 'NONE',  ( 4.090329635444483358, -1.806102819543849769, -0.2658631594732660530 ) ) ;
#109364=CARTESIAN_POINT ( 'NONE',  ( 2.026150138982992566, 1.004015975608811173, 1.685199498757394831 ) ) ;
#109368=CARTESIAN_POINT ( 'NONE',  ( 2.420699464796825850, -0.8139657014685426351, -1.958238820914718792 ) ) ;
#109373=CARTESIAN_POINT ( 'NONE',  ( 0.6200890622066607127, 2.048230590617374336, -0.3001980380039070972 ) ) ;
#109376=CARTESIAN_POINT ( 'NONE',  ( 3.229344874888330441, 2.008827177783510720, 0.9482931344305007837 ) ) ;
#109378=CARTESIAN_POINT ( 'NONE',  ( 0.7394344266866456072, 2.295659475925112769, -0.1205738325454289578 ) ) ;
#109380=CARTESIAN_POINT ( 'NONE',  ( 6.508646177561060675, 0.6413444998595011493, 1.960425241914983907 ) ) ;
#109384=CARTESIAN_POINT ( 'NONE',  ( 0.2329586101569527945, 7.629137130509077380, -2.445728209250570107 ) ) ;
#109385=CARTESIAN_POINT ( 'NONE',  ( 6.058133912487986272, -1.297239342979487509, 1.306937132449899508 ) ) ;
#109388=CARTESIAN_POINT ( 'NONE',  ( -0.2104748580754408904, 1.337026610731705700, -2.356057411969681326 ) ) ;
#109389=CARTESIAN_POINT ( 'NONE',  ( 3.029983902540707152, 0.9595516922606081023, -1.432977992855663185 ) ) ;
#109390=CARTESIAN_POINT ( 'NONE',  ( 1.710173085450257702, 1.157096902994741772, -1.651345047625000229 ) ) ;
#109391=CARTESIAN_POINT ( 'NONE',  ( 2.918861131495727790, -1.545587104802835565, -1.701642145805809303 ) ) ;
#109392=CARTESIAN_POINT ( 'NONE',  ( 2.390224264847177871, -0.9692217175977213550, 2.044435098530998474 ) ) ;
#109393=CARTESIAN_POINT ( 'NONE',  ( 4.916683514525310272, 1.453009998446822992, -1.524801812277425839 ) ) ;
#109396=CARTESIAN_POINT ( 'NONE',  ( 3.303702144000867591, -1.767878013958000150, 0.08340844992380143375 ) ) ;
#109398=CARTESIAN_POINT ( 'NONE',  ( 6.128533286225700039, 0.2205342988230532264, 2.281768524910554596 ) ) ;
#109399=CARTESIAN_POINT ( 'NONE',  ( 4.839718430358881385, 1.836437689789902628, 0.1323948491315785347 ) ) ;
#109403=CARTESIAN_POINT ( 'NONE',  ( 4.857479518068650748, 2.167902099161696849, -0.3196092617779102696 ) ) ;
#109406=CARTESIAN_POINT ( 'NONE',  ( 4.984861949208964305, 1.980195279717174905, 0.6042863919064264122 ) ) ;
#109410=CARTESIAN_POINT ( 'NONE',  ( 3.123571566491334384, -1.856553849623356234, 0.5141669907481066781 ) ) ;
#109413=CARTESIAN_POINT ( 'NONE',  ( -0.1047794747230318818, -2.156939676625940994, -0.5310815526072456549 ) ) ;
#109421=CARTESIAN_POINT ( 'NONE',  ( 1.855835942623608181, -0.6640040153468586004, 1.846199708051485588 ) ) ;
#109424=CARTESIAN_POINT ( 'NONE',  ( 6.021922112293466967, 1.933069186966931863, -0.3339256516061983038 ) ) ;
#109427=CARTESIAN_POINT ( 'NONE',  ( 6.754756207809571755, -1.674487575904315406, 1.366813541845832924 ) ) ;
#109431=CARTESIAN_POINT ( 'NONE',  ( 6.678986255646885972, -0.09454399199107686724, -1.969188304806670287 ) ) ;
#109432=CARTESIAN_POINT ( 'NONE',  ( 6.573613466494099278, 1.281508381366827765, -1.168108599551227478 ) ) ;
#109434=CARTESIAN_POINT ( 'NONE',  ( 2.736070936638954176, 2.175344985778558726, 0.2654339622269741295 ) ) ;
#109435=CARTESIAN_POINT ( 'NONE',  ( 4.753107839025799031, -1.856540859070819005, 1.370308287008913606 ) ) ;
#109436=CARTESIAN_POINT ( 'NONE',  ( 6.098915436037096960, 1.687290577560787375, -1.182889608693861394 ) ) ;
#109437=CARTESIAN_POINT ( 'NONE',  ( 1.816251609031571457, 1.811968324836669142, 0.6989759121980871903 ) ) ;
#109441=CARTESIAN_POINT ( 'NONE',  ( 5.607717026683647354, 1.607092460389969446, 1.383685132418293495 ) ) ;
#109442=CARTESIAN_POINT ( 'NONE',  ( 2.672500184003968382, 1.427937546361924381, 1.423961308954827754 ) ) ;
#109453=CARTESIAN_POINT ( 'NONE',  ( 5.823136237661057812, -0.05295972098229295016, 2.060385759621866431 ) ) ;
#109458=CARTESIAN_POINT ( 'NONE',  ( 5.110023566311792997, -0.7249756751233800145, 1.885263354437803240 ) ) ;
#109463=CARTESIAN_POINT ( 'NONE',  ( 3.959881651031765593, 2.045548025627259126, -0.2503382637644557263 ) ) ;
#109464=CARTESIAN_POINT ( 'NONE',  ( 2.690077459517980163, 1.704938782060089864, 1.076316768488336351 ) ) ;
#109465=ORIENTED_EDGE ( 'NONE', *, *, #15404, .F. ) ;
#109470=CARTESIAN_POINT ( 'NONE',  ( 2.565779641467882399, 1.620934753846922982, -1.198676126143098486 ) ) ;
#109471=CARTESIAN_POINT ( 'NONE',  ( 1.991909005812149358, -0.4902695928585449892, -1.774584731258487036 ) ) ;
#109472=CARTESIAN_POINT ( 'NONE',  ( 0.8038796212130067120, 1.889748380504801650, 1.324265523043531845 ) ) ;
#109474=CARTESIAN_POINT ( 'NONE',  ( 3.936934155531632396, 0.3128429973590241553, 2.138701728237289768 ) ) ;
#109477=CARTESIAN_POINT ( 'NONE',  ( 3.585630231873372598, 1.460649136416993121, -1.774545834528557409 ) ) ;
#109481=CARTESIAN_POINT ( 'NONE',  ( 0.8306673739700667358, 0.1335802410974036292, 1.865940672528036304 ) ) ;
#109482=CARTESIAN_POINT ( 'NONE',  ( 5.752796013432011080, -1.554615333184097059, 1.212288997074702834 ) ) ;
#109487=CARTESIAN_POINT ( 'NONE',  ( 0.9618826090718561872, 0.4271145061440981272, -2.164990749644220447 ) ) ;
#109491=CARTESIAN_POINT ( 'NONE',  ( 6.539320575229230492, 2.428701779328062749, 2.485127258459709054 ) ) ;
#109492=CARTESIAN_POINT ( 'NONE',  ( 5.243030984088811408, -1.691212405323471835, 1.012918505260449464 ) ) ;
#109493=CARTESIAN_POINT ( 'NONE',  ( 4.037936217472848810, -1.589972691411502659, -1.672771819537349325 ) ) ;
#109494=CARTESIAN_POINT ( 'NONE',  ( 3.397386871994355850, -1.821155587584430302, 0.9682287363927607471 ) ) ;
#109501=CARTESIAN_POINT ( 'NONE',  ( 5.002462566363424123, 2.165002515946230499, 0.1647018997421762776 ) ) ;
#109503=CARTESIAN_POINT ( 'NONE',  ( 3.684953445348177148, 1.336164438771630714, 1.267087564277062484 ) ) ;
#109506=CARTESIAN_POINT ( 'NONE',  ( 5.390230798962840630, -0.5317533105795355652, -2.125930911514521959 ) ) ;
#109508=CARTESIAN_POINT ( 'NONE',  ( 0.7555949320777423095, -1.911880202960547948, -1.209378468041100607 ) ) ;
#109514=CARTESIAN_POINT ( 'NONE',  ( 0.4613126893583847643, 1.751520745650859912, -0.2531317886874852041 ) ) ;
#109516=CARTESIAN_POINT ( 'NONE',  ( 5.233069312805943341, 1.860886824452904653, 0.7683393057746935595 ) ) ;
#109518=CARTESIAN_POINT ( 'NONE',  ( 4.559663772078708988, 0.4639327178320976630, -2.054050964449795291 ) ) ;
#109519=CARTESIAN_POINT ( 'NONE',  ( 2.970226572681373689, -1.887729772399210804, -0.3245638568863758455 ) ) ;
#109521=CARTESIAN_POINT ( 'NONE',  ( 4.387129405986627262, 0.09430581837475923712, 1.967405897498993195 ) ) ;
#109522=CARTESIAN_POINT ( 'NONE',  ( 5.748308766347858700, 0.9917722086787251756, -1.759414076857076514 ) ) ;
#109524=CARTESIAN_POINT ( 'NONE',  ( 1.551402291579254022, 0.5461136009352780540, -1.789155053659279071 ) ) ;
#109525=CARTESIAN_POINT ( 'NONE',  ( 4.652814366283819503, -1.382804000779764619, 1.030830748262304253 ) ) ;
#109526=CARTESIAN_POINT ( 'NONE',  ( 1.582132296805271787, 0.9858968508435607125, 1.638552900098678045 ) ) ;
#109528=CARTESIAN_POINT ( 'NONE',  ( 1.858336453454629611, 2.200810804183956026, -0.1644699235988852648 ) ) ;
#109532=CARTESIAN_POINT ( 'NONE',  ( 6.320756440275016708, -1.388331291134708767, 1.386421665916007795 ) ) ;
#109541=CARTESIAN_POINT ( 'NONE',  ( 2.084514231050747401, 1.193861083872927109, -1.691280048542340708 ) ) ;
#109546=CARTESIAN_POINT ( 'NONE',  ( 0.3287785284849250034, 1.391158174000119097, -1.464406657780653820 ) ) ;
#109551=CARTESIAN_POINT ( 'NONE',  ( 5.958361200765043719, 1.524811557412728114, 1.319025083221535333 ) ) ;
#109552=CARTESIAN_POINT ( 'NONE',  ( 4.944510238519550072, -1.383032091829504928, 1.325833103116050626 ) ) ;
#109554=CARTESIAN_POINT ( 'NONE',  ( 2.613028500285840661, -0.2118117899099076218, 2.181281865515646068 ) ) ;
#109557=CARTESIAN_POINT ( 'NONE',  ( 5.713144883995101786, 1.643398218655172105, -1.162588118691459949 ) ) ;
#109558=CARTESIAN_POINT ( 'NONE',  ( 1.793074957647671663, -0.09724762972821224261, -1.910064080951429100 ) ) ;
#109561=CARTESIAN_POINT ( 'NONE',  ( 0.06993570063764525946, -0.9480199632962028611, 1.779638758220257522 ) ) ;
#109563=CARTESIAN_POINT ( 'NONE',  ( 3.896100387133538234, -0.6578992572023834029, -1.984587938432079257 ) ) ;
#109565=CARTESIAN_POINT ( 'NONE',  ( 1.904884197260014567, 1.431573929998239958, 0.9616530215695131556 ) ) ;
#109567=CARTESIAN_POINT ( 'NONE',  ( 6.521762860236213655, -0.4636855090699961712, 2.076960040381255812 ) ) ;
#109570=CARTESIAN_POINT ( 'NONE',  ( 0.4671467121175364445, 1.705069321186868159, 0.9702857188121425391 ) ) ;
#109575=CARTESIAN_POINT ( 'NONE',  ( 2.982852160962686128, -1.674641624487639424, -0.6911452858660637188 ) ) ;
#109580=CARTESIAN_POINT ( 'NONE',  ( 4.248556108744420357, 1.777317977963272178, 0.3491261437693141123 ) ) ;
#109581=CARTESIAN_POINT ( 'NONE',  ( 6.539320575229287336, 7.629137130509086262, 2.596737603865982624 ) ) ;
#109584=CARTESIAN_POINT ( 'NONE',  ( 3.982723974049819482, 1.766592268715084790, 0.5855280163863920695 ) ) ;
#109585=CARTESIAN_POINT ( 'NONE',  ( 1.370553398973891390, -0.2825970708170088552, -1.894525755544463008 ) ) ;
#109586=CARTESIAN_POINT ( 'NONE',  ( 0.6920833903016985200, -1.811158644599793810, -0.2285449354127722099 ) ) ;
#109594=CARTESIAN_POINT ( 'NONE',  ( 5.840667653085179545, -1.920577060998058583, -0.4351772876184378247 ) ) ;
#109598=CARTESIAN_POINT ( 'NONE',  ( 0.5157159539815784344, -1.120044586405210207, -1.765097889335610404 ) ) ;
#109600=CARTESIAN_POINT ( 'NONE',  ( 5.579104889113781773, -0.04751220352695872257, -1.925958990430853612 ) ) ;
#109602=CARTESIAN_POINT ( 'NONE',  ( 1.131563826228650038, -1.154680578942975044, -1.414029504508321100 ) ) ;
#109603=CARTESIAN_POINT ( 'NONE',  ( 2.491098823239074278, -0.3784457004711218042, -2.174036671264235387 ) ) ;
#109607=CARTESIAN_POINT ( 'NONE',  ( 6.842638217859555283, -1.930751226189564962, -0.3875045943893626887 ) ) ;
#109608=CARTESIAN_POINT ( 'NONE',  ( 2.981904208038600679, -1.913756795454506721, -0.3294587723015156011 ) ) ;
#109611=CARTESIAN_POINT ( 'NONE',  ( 0.5091384654962345380, 2.010518347751136137, 0.1511200514899835312 ) ) ;
#109613=CARTESIAN_POINT ( 'NONE',  ( 6.948144928891270666, -0.7966579434352799582, 1.680504273975716334 ) ) ;
#109619=CARTESIAN_POINT ( 'NONE',  ( 2.911879292414458309, -1.082406496695037301, -1.905547650945007776 ) ) ;
#109623=CARTESIAN_POINT ( 'NONE',  ( 2.385134503015675200, 1.669401249834654433, -0.7394980648879890817 ) ) ;
#109630=CARTESIAN_POINT ( 'NONE',  ( 0.9614038661405551744, 0.3767496340168969837, -1.889141571593662805 ) ) ;
#109631=CARTESIAN_POINT ( 'NONE',  ( 5.242999579849755953, -0.2363135928187160284, -1.947375393322479109 ) ) ;
#109635=CARTESIAN_POINT ( 'NONE',  ( 4.652002595327206613, 0.8389548150543740812, 2.024815518666116088 ) ) ;
#109639=CARTESIAN_POINT ( 'NONE',  ( 3.590741003927795827, 2.018730135711533258, 0.4582614309688318177 ) ) ;
#109643=CARTESIAN_POINT ( 'NONE',  ( 3.920743334446879835, -1.585418671752996334, -1.664648107385821030 ) ) ;
#109649=CARTESIAN_POINT ( 'NONE',  ( 4.453030731839799472, 0.4239971928432215154, -1.894948383050964580 ) ) ;
#109654=CARTESIAN_POINT ( 'NONE',  ( 5.238497809344139000, 1.134185964801931679, -1.539638564045166857 ) ) ;
#109655=CARTESIAN_POINT ( 'NONE',  ( 5.983370841356476788, 1.591773204597257463, -0.6646525218769030463 ) ) ;
#109656=CARTESIAN_POINT ( 'NONE',  ( 4.118375227313908482, 1.978554835517082555, 0.3886342876525810119 ) ) ;
#109660=CARTESIAN_POINT ( 'NONE',  ( 1.236401392562349155, 0.4093969531599008227, 2.049976805931138735 ) ) ;
#109661=CARTESIAN_POINT ( 'NONE',  ( 0.1625042017948316320, -1.577765994087614310, -0.8020051908347087810 ) ) ;
#109662=CARTESIAN_POINT ( 'NONE',  ( 5.994767569012836361, -2.000857541758268354, 0.2496038112331094849 ) ) ;
#109664=CARTESIAN_POINT ( 'NONE',  ( 3.416269409239420352, 1.454353297360365449, -1.771818544839237175 ) ) ;
#109665=CARTESIAN_POINT ( 'NONE',  ( 1.675334203684273771, -0.9328193774022232043, 1.469000774227617434 ) ) ;
#109667=CARTESIAN_POINT ( 'NONE',  ( 0.6140417155099803237, 0.5521904297083098934, -1.643632271941943612 ) ) ;
#109669=CARTESIAN_POINT ( 'NONE',  ( 2.136937089482681795, -0.08731620468203694918, -1.859122327218107218 ) ) ;
#109670=CARTESIAN_POINT ( 'NONE',  ( 2.102231420249685456, 0.8322404413585123839, -2.005527090382641653 ) ) ;
#109671=CARTESIAN_POINT ( 'NONE',  ( 3.010954138651841916, 0.05432569772663429358, 2.015980714967258614 ) ) ;
#109672=CARTESIAN_POINT ( 'NONE',  ( 3.968750000000002665, 0.7852924748297764879, -1.895863743164168724 ) ) ;
#109674=CARTESIAN_POINT ( 'NONE',  ( 6.621714856310891406, -1.867994803139013005, 0.4708039761674199797 ) ) ;
#109676=CARTESIAN_POINT ( 'NONE',  ( 3.340272282456987263, -1.325889367010645969, -1.782164031402436954 ) ) ;
#109681=CARTESIAN_POINT ( 'NONE',  ( 0.03034698492793227315, -2.177136498186870384, 0.4399771670399817425 ) ) ;
#109682=CARTESIAN_POINT ( 'NONE',  ( 4.510177812457000002, 1.961482754637720927, -0.04604004567236585910 ) ) ;
#109686=CARTESIAN_POINT ( 'NONE',  ( 5.589262808440923713, 1.998987879104210608, -1.059483486058722779 ) ) ;
#109687=CARTESIAN_POINT ( 'NONE',  ( 2.594246270321644676, 0.9746516854327008650, -1.817902028900773459 ) ) ;
#109691=CARTESIAN_POINT ( 'NONE',  ( 3.971829172498120286, 1.036919360001643531, 1.556626693588740062 ) ) ;
#109692=CARTESIAN_POINT ( 'NONE',  ( 2.144752260294139568, 0.7423094788623717522, 1.567400511497107018 ) ) ;
#109693=CARTESIAN_POINT ( 'NONE',  ( 6.005464345382193869, -2.175231771021503668, 0.2666438670960933344 ) ) ;
#109694=CARTESIAN_POINT ( 'NONE',  ( 1.044295067165665669, 0.8929887407379886177, -2.018210024696056148 ) ) ;
#109695=CARTESIAN_POINT ( 'NONE',  ( 3.625982885822197410, -1.285997354380935098, -1.737435825693343094 ) ) ;
#109696=CARTESIAN_POINT ( 'NONE',  ( 6.052673674419667194, -1.666704710846309112, -0.9964068823852706425 ) ) ;
#109705=CARTESIAN_POINT ( 'NONE',  ( 3.738726038629454074, 0.2694068579384528150, 1.805578518607708016 ) ) ;
#109707=CARTESIAN_POINT ( 'NONE',  ( 1.975870009618452050, 2.111717515986545113, -0.6407313945460398896 ) ) ;
#109712=CARTESIAN_POINT ( 'NONE',  ( 0.8967469923133252196, -1.971478154887895684, -0.4383870506769834141 ) ) ;
#109713=CARTESIAN_POINT ( 'NONE',  ( 0.9617728337494994006, -1.673954878106189703, -1.301583125534570673 ) ) ;
#109716=CARTESIAN_POINT ( 'NONE',  ( 2.412761291957177701, -1.442071615443579091, 1.176286876380010726 ) ) ;
#109718=CARTESIAN_POINT ( 'NONE',  ( 6.117814597332064785, 0.2004318333163370436, 2.006446488866588496 ) ) ;
#109721=CARTESIAN_POINT ( 'NONE',  ( 3.879382553896340013, 1.718498013671100777, -0.6167319420108534622 ) ) ;
#109726=CARTESIAN_POINT ( 'NONE',  ( 6.485703859413265882, 1.880147802650249611, 0.7282652505391642439 ) ) ;
#109727=CARTESIAN_POINT ( 'NONE',  ( 6.369096972855497363, 1.760372669148374758, -0.5393517311068628528 ) ) ;
#109729=CARTESIAN_POINT ( 'NONE',  ( 4.196143101376831552, -0.8852276965729001246, 2.131346054819768909 ) ) ;
#109731=CARTESIAN_POINT ( 'NONE',  ( 6.749309733681256418, -1.731629633356733589, -1.293610171197785652 ) ) ;
#109733=CARTESIAN_POINT ( 'NONE',  ( 1.892034919678585281, -0.5197426219408564085, -1.871140422112322232 ) ) ;
#109734=CARTESIAN_POINT ( 'NONE',  ( 5.255319057710332586, -2.280117823540278366, -0.2889680969316887893 ) ) ;
#109737=CARTESIAN_POINT ( 'NONE',  ( 4.082764389539480732, -0.1829629792115642917, -1.861669828791753467 ) ) ;
#109738=CARTESIAN_POINT ( 'NONE',  ( 2.373185085050379506, -1.665764800640230803, -0.9392108107411781814 ) ) ;
#109741=CARTESIAN_POINT ( 'NONE',  ( 4.108205984530819421, -2.201057848371779535, 0.1611738814469021175 ) ) ;
#109743=CARTESIAN_POINT ( 'NONE',  ( 6.983263157960398537, 3.691045885609476773, 2.560325512483021981 ) ) ;
#109744=CARTESIAN_POINT ( 'NONE',  ( -0.2108831679770924727, 4.091978752061476321, -2.452067053820900622 ) ) ;
#109747=CARTESIAN_POINT ( 'NONE',  ( 1.880087831454971603, -1.058004756265405799, 1.663231189906771990 ) ) ;
#109748=CARTESIAN_POINT ( 'NONE',  ( 2.520946605012349018, 1.507388781920895759, -1.747272692061818011 ) ) ;
#109749=CARTESIAN_POINT ( 'NONE',  ( 2.875390130891414042, -0.1950805366632331617, 1.952157403750237163 ) ) ;
#109751=CARTESIAN_POINT ( 'NONE',  ( 6.244999159755385776, -0.2970413431409227312, -2.040939473721150144 ) ) ;
#109753=CARTESIAN_POINT ( 'NONE',  ( 3.889861467948489082, -2.010801299972611478, 0.1531677096566556595 ) ) ;
#109760=CARTESIAN_POINT ( 'NONE',  ( 2.430757386254971841, -1.338474561058100143, 1.709278666203792652 ) ) ;
#109765=CARTESIAN_POINT ( 'NONE',  ( 2.881944908259078453, -0.9649329312324153030, 1.602325162460143559 ) ) ;
#109766=CARTESIAN_POINT ( 'NONE',  ( 6.134075720976177593, 1.071308383804179476, -1.877395391766012445 ) ) ;
#109769=CARTESIAN_POINT ( 'NONE',  ( 6.727182134110203826, 7.053687134213418197, 2.309100590371661710 ) ) ;
#109772=CARTESIAN_POINT ( 'NONE',  ( 1.805181101471531546, 1.663141274854248230, -0.9436981260437929953 ) ) ;
#109773=CARTESIAN_POINT ( 'NONE',  ( 3.959615635602866668, 1.756445048235187212, -0.2166398133998989062 ) ) ;
#109774=CARTESIAN_POINT ( 'NONE',  ( 2.068876254944008508, -1.477226179422253871, 1.214308343151893510 ) ) ;
#109776=CARTESIAN_POINT ( 'NONE',  ( 0.1279635871501626776, 1.910768599467532081, 0.1380287717926073077 ) ) ;
#109778=CARTESIAN_POINT ( 'NONE',  ( 1.328672132201724532, -1.314895749051579132, 1.599177317581280455 ) ) ;
#109781=CARTESIAN_POINT ( 'NONE',  ( 5.225416543158964977, -1.776039340814106637, 0.5876355328483380269 ) ) ;
#109782=CARTESIAN_POINT ( 'NONE',  ( 1.347985785199314668, 1.823511463271022093, 0.09156768404049858701 ) ) ;
#109783=CARTESIAN_POINT ( 'NONE',  ( 5.531908139154323223, -1.397534428995873546, -1.707979418440738195 ) ) ;
#109786=CARTESIAN_POINT ( 'NONE',  ( 2.734894939886590937, -1.973151212864039605, -0.6010335745895727388 ) ) ;
#109792=CARTESIAN_POINT ( 'NONE',  ( 0.5796411875719498230, 2.017120475678677582, -0.7774783797904263327 ) ) ;
#109796=CARTESIAN_POINT ( 'NONE',  ( 5.371561628297467195, -0.3073141173523045167, 2.047320497149993646 ) ) ;
#109798=CARTESIAN_POINT ( 'NONE',  ( 2.987745815084281276, 1.526290923294726820, 1.530918043534036599 ) ) ;
#109800=CARTESIAN_POINT ( 'NONE',  ( 3.633467297704314980, -0.1462457305761339643, 2.014424004083538833 ) ) ;
#109801=CARTESIAN_POINT ( 'NONE',  ( 6.720655732516649827, 0.5547967289194677409, 2.325046546815363602 ) ) ;
#109805=CARTESIAN_POINT ( 'NONE',  ( 1.780482797753998092, -0.5424726148271253878, -1.942096288550937411 ) ) ;
#109807=CARTESIAN_POINT ( 'NONE',  ( 6.444889499930222421, -1.758869480593090673, -1.307235502039267860 ) ) ;
#109809=CARTESIAN_POINT ( 'NONE',  ( 4.535362393419643645, -0.08824616237496610283, 1.910463848342446980 ) ) ;
#109813=CARTESIAN_POINT ( 'NONE',  ( 3.567982607561688280, -0.9913820634350967165, 1.755780237201590488 ) ) ;
#109815=CARTESIAN_POINT ( 'NONE',  ( 5.649328262929842914, -1.362134112713381029, -1.057878908126141715 ) ) ;
#109819=CARTESIAN_POINT ( 'NONE',  ( 3.954256261376987602, 0.6707706173689140794, 1.746330409709492937 ) ) ;
#109822=CARTESIAN_POINT ( 'NONE',  ( 0.9716355300813659390, -0.3074278181635254903, 2.047203142020392441 ) ) ;
#109825=CARTESIAN_POINT ( 'NONE',  ( 6.445981706654077215, -1.189238676736432465, -1.366527308926633211 ) ) ;
#109828=CARTESIAN_POINT ( 'NONE',  ( 0.2635251908490592876, 0.5682291949154983923, -1.720254828205844966 ) ) ;
#109833=CARTESIAN_POINT ( 'NONE',  ( 0.8538673084422104820, -0.7095216264049221122, 1.829241926910141203 ) ) ;
#109835=CARTESIAN_POINT ( 'NONE',  ( 4.868704338522531039, -0.2386889102116992178, -1.900620109961237203 ) ) ;
#109840=CARTESIAN_POINT ( 'NONE',  ( 1.920999885407469243, 2.016935458891587096, 0.7782144962657986387 ) ) ;
#109844=CARTESIAN_POINT ( 'NONE',  ( 4.875911338656576888, 1.051942333337583468, 1.491839654383666947 ) ) ;
#109847=CARTESIAN_POINT ( 'NONE',  ( 0.7726555735236986244, -1.854786837065467653, -0.6681536526091761408 ) ) ;
#109848=CARTESIAN_POINT ( 'NONE',  ( 3.867365959033176814, -1.592763314076732106, -1.058159689705892692 ) ) ;
#109851=CARTESIAN_POINT ( 'NONE',  ( 3.666418788940009943, -0.7958718277518551654, -1.801768233320384605 ) ) ;
#109853=CARTESIAN_POINT ( 'NONE',  ( 5.864781425808283544, 0.1387459415673809593, -1.937151248970377271 ) ) ;
#109857=CARTESIAN_POINT ( 'NONE',  ( 6.504144398916748671, -0.9053081408615070158, 1.915699539216948688 ) ) ;
#109859=CARTESIAN_POINT ( 'NONE',  ( 4.283787348595206268, 1.854039900284172315, -0.4678174759695231666 ) ) ;
#109862=FILL_AREA_STYLE_COLOUR ( '', #23612 ) ;
#109863=CARTESIAN_POINT ( 'NONE',  ( 5.110025693318159590, -0.7223781944584523051, 1.879196401790662607 ) ) ;
#109865=CARTESIAN_POINT ( 'NONE',  ( 6.656878040733529289, -1.407521694628325770, 1.162499734694094844 ) ) ;
#109866=CARTESIAN_POINT ( 'NONE',  ( 5.630092293170263495, 2.014432788975322630, 0.09412139267171715229 ) ) ;
#109868=CARTESIAN_POINT ( 'NONE',  ( 1.398975865466948632, 0.4019745351953528112, 2.030794141931663521 ) ) ;
#109879=SURFACE_STYLE_FILL_AREA ( #192100 ) ;
#109881=CARTESIAN_POINT ( 'NONE',  ( 4.043420308529748652, -1.281227996783333989, 1.168826672502675912 ) ) ;
#109883=CARTESIAN_POINT ( 'NONE',  ( 2.975506508543227291, -0.2074491501150333705, 2.059866449969804503 ) ) ;
#109884=CARTESIAN_POINT ( 'NONE',  ( 3.058335788041772307, -1.258934183635691095, 1.702155058717010672 ) ) ;
#109887=CARTESIAN_POINT ( 'NONE',  ( 0.5144232481557647896, 0.7485027850700550767, 1.821871385004094845 ) ) ;
#109892=CARTESIAN_POINT ( 'NONE',  ( 3.627152717534872561, -2.118219197452147373, 0.8765883884584676489 ) ) ;
#109893=CARTESIAN_POINT ( 'NONE',  ( 1.101864800459760207, -1.825872481749410525, -0.002338443969775172437 ) ) ;
#109895=CARTESIAN_POINT ( 'NONE',  ( 3.779479514802902340, 0.2291398179169491789, -1.898525689255560422 ) ) ;
#109899=CARTESIAN_POINT ( 'NONE',  ( 1.933841784273998332, -1.951746473714164321, 0.4931059669559466063 ) ) ;
#109900=CARTESIAN_POINT ( 'NONE',  ( 2.008577182894935476, 0.6104510041588117053, 1.864461945915835583 ) ) ;
#109905=CARTESIAN_POINT ( 'NONE',  ( 4.470703160837229184, 0.0002547659985942945528, -2.090823719324691687 ) ) ;
#109906=CARTESIAN_POINT ( 'NONE',  ( 3.625649997064513297, -1.053871202854910871, -1.421704988934450409 ) ) ;
#109908=CARTESIAN_POINT ( 'NONE',  ( 5.982448691606671254, -0.3306924304021444661, -2.268186543139012024 ) ) ;
#109909=CARTESIAN_POINT ( 'NONE',  ( 5.138483783005516337, -1.490010379379594241, 0.8989716238894971401 ) ) ;
#109912=CARTESIAN_POINT ( 'NONE',  ( 5.378194026956880869, -0.2521426391564468572, 1.715267145961799411 ) ) ;
#109913=CARTESIAN_POINT ( 'NONE',  ( 6.180164126497881938, -1.200935631872475540, -1.808625420649534021 ) ) ;
#109915=CARTESIAN_POINT ( 'NONE',  ( 6.403528931544730796, -1.954801056786956259, 0.4946215565981848528 ) ) ;
#109916=CARTESIAN_POINT ( 'NONE',  ( 5.218750000000002665, -0.7852924748297095414, 1.895863743164193371 ) ) ;
#109918=CARTESIAN_POINT ( 'NONE',  ( 3.557566385928968788, 0.4691178692100838599, -1.868274323828737371 ) ) ;
#109920=CARTESIAN_POINT ( 'NONE',  ( 0.6455721646590365514, 0.1693206843514388493, 2.214916916779915201 ) ) ;
#109925=CARTESIAN_POINT ( 'NONE',  ( 2.069254833283964867, -1.714886923611224745, 1.411838272681579687 ) ) ;
#109932=CARTESIAN_POINT ( 'NONE',  ( 0.6510177983308338412, 0.9963039324867200008, 1.753029211773032392 ) ) ;
#109934=CARTESIAN_POINT ( 'NONE',  ( 5.424308963177657539, 1.013736099364664911, 1.796294033555500658 ) ) ;
#109939=CARTESIAN_POINT ( 'NONE',  ( 0.1921619543209041325, -0.3744425218715953796, -1.735604558297418443 ) ) ;
#109940=CARTESIAN_POINT ( 'NONE',  ( 6.416678112323896954, -1.140949303232444478, -1.306061676789990855 ) ) ;
#109941=CARTESIAN_POINT ( 'NONE',  ( 5.794438198198100132, 1.417746085458403638, -1.009241466377588603 ) ) ;
#109942=CARTESIAN_POINT ( 'NONE',  ( 2.613130667218881431, -0.2215951064345271782, 2.281621536969838271 ) ) ;
#109944=CARTESIAN_POINT ( 'NONE',  ( 2.501689010688646242, -0.7045654096689784041, -1.701190496055771550 ) ) ;
#109947=CARTESIAN_POINT ( 'NONE',  ( 2.608196206841297826, -0.6965810133783244540, -1.687657492251873226 ) ) ;
#109948=CARTESIAN_POINT ( 'NONE',  ( 4.254529844270301453, 1.955172953530256219, -0.4926405443339901269 ) ) ;
#109951=CARTESIAN_POINT ( 'NONE',  ( 5.649480931864863109, -1.658039504894607719, -1.298324887859639842 ) ) ;
#109954=CARTESIAN_POINT ( 'NONE',  ( 2.189971326302230903, -1.350648006375281929, -1.569233719104834890 ) ) ;
#109957=CARTESIAN_POINT ( 'NONE',  ( 4.705793326368500118, 1.571798730262342181, 1.423547657546264000 ) ) ;
#109959=CARTESIAN_POINT ( 'NONE',  ( 1.295397306693826467, 1.458444760659328265, 1.258811869801695682 ) ) ;
#109966=CARTESIAN_POINT ( 'NONE',  ( 5.730757696090861941, 1.422813033107739988, -1.572628729999878905 ) ) ;
#109967=CARTESIAN_POINT ( 'NONE',  ( 1.993330679213504153, 1.832751758872013914, -1.037179240317965823 ) ) ;
#109970=CARTESIAN_POINT ( 'NONE',  ( 5.910971410920907942, -1.467885462018687415, 1.143791174867914373 ) ) ;
#109974=AXIS2_PLACEMENT_3D ( 'NONE', #126834, #29252, #94273 ) ;
#109979=CARTESIAN_POINT ( 'NONE',  ( 2.242563829109287088, -1.923402688547710904, -0.3857071251459272543 ) ) ;
#109980=CARTESIAN_POINT ( 'NONE',  ( 1.376082401959723089, 1.288024388040419632, 1.735935173841046675 ) ) ;
#109984=CARTESIAN_POINT ( 'NONE',  ( 2.934579196337202323, 0.9245653808827180020, 1.466514439666162684 ) ) ;
#109985=CARTESIAN_POINT ( 'NONE',  ( 2.026944798790380364, -1.135751832872053058, -1.318713242574782507 ) ) ;
#109991=CARTESIAN_POINT ( 'NONE',  ( 1.182427310604698079, -1.922956083944601158, -0.4339701177692931178 ) ) ;
#109992=CARTESIAN_POINT ( 'NONE',  ( 5.291234991620994421, -0.05314252713351996088, -1.911838368980276925 ) ) ;
#109997=CARTESIAN_POINT ( 'NONE',  ( 1.102219918440990876, -0.9059408578524772437, 1.805149201161629025 ) ) ;
#109999=CARTESIAN_POINT ( 'NONE',  ( 5.895647473559280982, 1.742329625737188525, 1.513132890121783536 ) ) ;
#110000=CARTESIAN_POINT ( 'NONE',  ( 5.371523934717264304, -0.2895824386080196322, 1.940264742196501802 ) ) ;
#110001=CARTESIAN_POINT ( 'NONE',  ( 3.537899350542179189, 1.241011212050652901, 1.519374649786103149 ) ) ;
#110003=CARTESIAN_POINT ( 'NONE',  ( 0.7740648250077889481, 1.777010169924503558, -0.9530137779002674225 ) ) ;
#110005=CARTESIAN_POINT ( 'NONE',  ( 1.675176079212177260, 1.839371217556123650, -1.048680071690030413 ) ) ;
#110008=CARTESIAN_POINT ( 'NONE',  ( 2.273173984786102775, 1.132353773513800510, 1.451651336590239927 ) ) ;
#110011=CARTESIAN_POINT ( 'NONE',  ( 3.269896953881154644, 0.5115095171020591636, -2.057881918134551125 ) ) ;
#110015=CARTESIAN_POINT ( 'NONE',  ( 3.163408073613428684, 0.3057118896435347954, -2.037866251177067323 ) ) ;
#110017=CARTESIAN_POINT ( 'NONE',  ( 0.02850758872123548837, -1.683968158181762043, 0.7450552726024004535 ) ) ;
#110021=CARTESIAN_POINT ( 'NONE',  ( 0.2939702064862387276, 1.638257335637434364, 1.478849500172851217 ) ) ;
#110022=CARTESIAN_POINT ( 'NONE',  ( 2.478104529052836291, 1.390129537188329101, 1.784895063601476428 ) ) ;
#110024=CARTESIAN_POINT ( 'NONE',  ( 2.671877653990344381, 1.802496804585513868, -0.1814095246875074008 ) ) ;
#110025=CARTESIAN_POINT ( 'NONE',  ( 3.239363768214057249, 0.4605203156026844158, -1.859431460922003509 ) ) ;
#110026=CARTESIAN_POINT ( 'NONE',  ( 3.912603064140641074, 0.7423916865902054907, 1.932869565047180549 ) ) ;
#110029=CARTESIAN_POINT ( 'NONE',  ( 3.010573890873136094, 1.429054271512670615, -1.358355385302984164 ) ) ;
#110031=CARTESIAN_POINT ( 'NONE',  ( 6.709608095207008738, -0.4227469423600908605, 1.886647698053174116 ) ) ;
#110032=CARTESIAN_POINT ( 'NONE',  ( 2.711613914024712191, -1.850561042518297672, 0.2725550856255419818 ) ) ;
#110033=CARTESIAN_POINT ( 'NONE',  ( 2.069360784497351613, -2.110879405061675929, -0.9329422106417961658 ) ) ;
#110035=CARTESIAN_POINT ( 'NONE',  ( 2.681907113330802339, -1.068898278170841598, -1.523273593526828673 ) ) ;
#110037=CARTESIAN_POINT ( 'NONE',  ( 6.408646180098039657, 0.6432782940990633413, 1.959889192978042205 ) ) ;
#110041=CARTESIAN_POINT ( 'NONE',  ( 0.6101635361662772761, -2.095732242510168764, 0.2083838208960953620 ) ) ;
#110043=CARTESIAN_POINT ( 'NONE',  ( 5.817692603468245238, -2.110333850551704415, 0.4673072906974176655 ) ) ;
#110044=CARTESIAN_POINT ( 'NONE',  ( 6.639320575229294086, 0.002105643433562148347, 2.003388605011639179 ) ) ;
#110050=CARTESIAN_POINT ( 'NONE',  ( -0.2409995289980038091, -0.004801160710915519658, -2.000252362011435636 ) ) ;
#110051=CARTESIAN_POINT ( 'NONE',  ( 4.346888830327386266, -1.803415170841724979, -0.9023466997552240798 ) ) ;
#110055=CARTESIAN_POINT ( 'NONE',  ( 5.612251347527116963, -0.9680786960581324596, -1.932885698521320528 ) ) ;
#110060=CARTESIAN_POINT ( 'NONE',  ( 6.415638736316127577, -1.319241173714128745, -1.525034172108488573 ) ) ;
#110062=CARTESIAN_POINT ( 'NONE',  ( 6.883263157960367806, 2.959656548886806515, 2.506466465954690914 ) ) ;
#110064=CARTESIAN_POINT ( 'NONE',  ( 1.664246808422519486, -1.221613929703774915, 1.218001262086549907 ) ) ;
#110068=CARTESIAN_POINT ( 'NONE',  ( 1.282078435845935616, -1.724974465617232999, -0.3947418589646100040 ) ) ;
#110069=CARTESIAN_POINT ( 'NONE',  ( 2.209637070578834628, 1.557646164037255643, 1.275278917823706948 ) ) ;
#110070=CARTESIAN_POINT ( 'NONE',  ( 4.225739626866775289, -2.112672615930260900, 0.6375689414055001336 ) ) ;
#110072=CARTESIAN_POINT ( 'NONE',  ( 5.401315523140023167, -1.865749354952720207, 1.109950958716971803 ) ) ;
#110076=CARTESIAN_POINT ( 'NONE',  ( 3.281995766809755466, 2.068381274212594878, -0.4664580258975092875 ) ) ;
#110077=CARTESIAN_POINT ( 'NONE',  ( 3.005482631727268039, -1.942536929278560365, 0.5405117225928540714 ) ) ;
#110078=CARTESIAN_POINT ( 'NONE',  ( 3.357467859903106255, -1.375039365347962450, -1.179588011891503418 ) ) ;
#110084=CARTESIAN_POINT ( 'NONE',  ( 6.129513044595952032, -1.717388127611047421, 0.6198453807191862674 ) ) ;
#110086=CARTESIAN_POINT ( 'NONE',  ( 1.200237320533149799, 1.284028115529710190, -1.421911532115504029 ) ) ;
#110088=AXIS2_PLACEMENT_3D ( 'NONE', #204051, #202998, #186763 ) ;
#110094=CARTESIAN_POINT ( 'NONE',  ( 5.752838164830007983, -1.706859214253673152, 1.326403591387192771 ) ) ;
#110097=CARTESIAN_POINT ( 'NONE',  ( 3.498385214435925317, -1.041973313016024472, 1.846846941210858351 ) ) ;
#110098=CARTESIAN_POINT ( 'NONE',  ( -0.1296875068448125057, 1.390030859318210688, -2.083197486262199138 ) ) ;
#110100=CARTESIAN_POINT ( 'NONE',  ( 4.165272970243100836, 0.2446167658484849627, -1.956081580383911778 ) ) ;
#110101=CARTESIAN_POINT ( 'NONE',  ( 6.170165192347925931, 1.906784905861274693, -0.1475879885542986936 ) ) ;
#110103=CARTESIAN_POINT ( 'NONE',  ( 5.700440484604645697, 1.420036636931173657, -1.570746850784213056 ) ) ;
#110105=CARTESIAN_POINT ( 'NONE',  ( 0.2388460773940295212, -2.007853281042128568, -0.5044432775610437902 ) ) ;
#110106=CARTESIAN_POINT ( 'NONE',  ( 2.888542945859973177, 1.665235949713929076, -0.9988640340363763581 ) ) ;
#110107=VERTEX_POINT ( 'NONE', #156581 ) ;
#110108=DIRECTION ( 'NONE',  ( -1.000000000000000000, 0.000000000000000000, 0.000000000000000000 ) ) ;
#110110=CARTESIAN_POINT ( 'NONE',  ( 4.136730066327800159, -1.819077861029708032, 1.030257495502053589 ) ) ;
#110113=CARTESIAN_POINT ( 'NONE',  ( 0.3283783949157508819, 1.250606878306897984, -1.310747381600821049 ) ) ;
#110115=CARTESIAN_POINT ( 'NONE',  ( 5.285833163787800437, 1.479997892162683071, 1.637210856327932618 ) ) ;
#110117=CARTESIAN_POINT ( 'NONE',  ( 3.223846859376262142, -2.127229092858519799, 0.5869343725257711863 ) ) ;
#110120=CARTESIAN_POINT ( 'NONE',  ( 1.699719973799845185, 1.319605273547658220, 1.384218846220357291 ) ) ;
#110122=CARTESIAN_POINT ( 'NONE',  ( 5.283670394142272464, -1.967056725255760474, 0.6460906113585005439 ) ) ;
#110124=CARTESIAN_POINT ( 'NONE',  ( 2.307699607974790901, -0.4742087202370263155, 2.108885336910087283 ) ) ;
#110125=CARTESIAN_POINT ( 'NONE',  ( 4.985950990042907094, -2.174969566330759996, -0.2684501861200879747 ) ) ;
#110136=CARTESIAN_POINT ( 'NONE',  ( 5.981320602565292965, -0.05662044862421274777, 2.069665677200482445 ) ) ;
#110137=CARTESIAN_POINT ( 'NONE',  ( 4.670489471188726149, -1.257041717089462773, 1.459967279689990960 ) ) ;
#110138=CARTESIAN_POINT ( 'NONE',  ( -0.1234324464992678227, -0.4448297287729073846, -1.973926538189611835 ) ) ;
#110141=CARTESIAN_POINT ( 'NONE',  ( 4.715651637508523564, 0.4355733895117944177, -1.920488317121961108 ) ) ;
#110142=CARTESIAN_POINT ( 'NONE',  ( -0.01142137120296871262, -0.4863542539808898280, -2.144715426241408984 ) ) ;
#110143=CARTESIAN_POINT ( 'NONE',  ( 4.195794211080963620, -0.6966935528937776567, 1.687730213881050600 ) ) ;
#110149=CARTESIAN_POINT ( 'NONE',  ( 2.946635061770470632, -1.506786691049965432, -1.057933238436038925 ) ) ;
#110150=CARTESIAN_POINT ( 'NONE',  ( 5.625249212676971311, 1.777412282398885823, 0.9453524948108845694 ) ) ;
#110151=CARTESIAN_POINT ( 'NONE',  ( 0.6326644773376333131, 0.2229630159884201934, -2.287572974657641645 ) ) ;
#110152=CARTESIAN_POINT ( 'NONE',  ( 5.858247074779933783, -1.961936380223072263, -0.003592477671530979431 ) ) ;
#110156=CARTESIAN_POINT ( 'NONE',  ( 0.2212536527127808295, -1.848710500310095872, -0.9322282823912150240 ) ) ;
#110159=CARTESIAN_POINT ( 'NONE',  ( 1.083664105429899216, -0.9366695517310281716, 1.869248094466950949 ) ) ;
#110160=CARTESIAN_POINT ( 'NONE',  ( 0.3384655940862451029, 0.3152513238553408814, 1.843739016257638141 ) ) ;
#110163=CARTESIAN_POINT ( 'NONE',  ( -0.2104748580754426390, 2.865278511227668634, -2.591885361450113834 ) ) ;
#110164=CARTESIAN_POINT ( 'NONE',  ( 1.715945410011958217, 1.623988859063689949, 0.6264298892959454523 ) ) ;
#110169=CARTESIAN_POINT ( 'NONE',  ( 2.789346554370454534, 1.219787599184172233, 1.219827592095571456 ) ) ;
#110170=CARTESIAN_POINT ( 'NONE',  ( 2.261505105119133052, 2.148611799745976381, -0.4309092228176118478 ) ) ;
#110171=CARTESIAN_POINT ( 'NONE',  ( 4.776106669258010307, 1.268914099295117781, 1.805409367619143390 ) ) ;
#110173=CARTESIAN_POINT ( 'NONE',  ( 2.413135165516873126, -1.680682958684741823, 1.374403011902309402 ) ) ;
#110174=CARTESIAN_POINT ( 'NONE',  ( 0.6272434487209905818, -1.734552980249819631, 0.5698080454362154379 ) ) ;
#110175=CARTESIAN_POINT ( 'NONE',  ( 3.204427616716760685, 1.339657272674670718, -1.639694800048612899 ) ) ;
#110176=CARTESIAN_POINT ( 'NONE',  ( 6.639320575229255894, 7.053084031878349869, 2.494893166485531388 ) ) ;
#110177=ORIENTED_EDGE ( 'NONE', *, *, #63333, .T. ) ;
#110179=CARTESIAN_POINT ( 'NONE',  ( 4.072042370276293788, -1.319783315292190284, 1.874172932857321339 ) ) ;
#110182=CARTESIAN_POINT ( 'NONE',  ( 5.778047442595251937, 2.188849720005956900, -0.3775064732549227586 ) ) ;
#110189=CARTESIAN_POINT ( 'NONE',  ( 3.920546200773936896, -1.392545040883992336, -1.458557299768625581 ) ) ;
#110191=CARTESIAN_POINT ( 'NONE',  ( 1.657159287258206604, 1.688608613550081516, -1.184165042645689558 ) ) ;
#110196=CARTESIAN_POINT ( 'NONE',  ( 5.191441776010862874, -0.7909675746368143301, 2.043907961996515699 ) ) ;
#110197=CARTESIAN_POINT ( 'NONE',  ( 2.672500184003968382, 1.427937546361924381, 1.423961308954827754 ) ) ;
#110198=CARTESIAN_POINT ( 'NONE',  ( 1.821575194732877545, 1.059174331173462935, -1.505913648122420900 ) ) ;
#110200=CARTESIAN_POINT ( 'NONE',  ( 0.1117072452763347851, -0.7311285168369995313, -1.561089762993218999 ) ) ;
#110203=CARTESIAN_POINT ( 'NONE',  ( 5.313438862022389131, -0.3376633510823018880, 2.237075724153537504 ) ) ;
#110205=CARTESIAN_POINT ( 'NONE',  ( 1.471456325463766479, 0.1532790705911575568, -2.100547924479207129 ) ) ;
#110217=CARTESIAN_POINT ( 'NONE',  ( 1.810938747355747447, -0.5704394276861005642, -2.042344090522000055 ) ) ;
#110218=CARTESIAN_POINT ( 'NONE',  ( 3.146955363149469331, 2.168125099964354874, 0.4830323043785512138 ) ) ;
#110219=CARTESIAN_POINT ( 'NONE',  ( -0.02244404828157658613, -0.004869073801674199918, -2.189079685368473527 ) ) ;
#110222=CARTESIAN_POINT ( 'NONE',  ( 4.404711838702720428, 0.5211615849865286476, 1.891323523724611766 ) ) ;
#110230=CARTESIAN_POINT ( 'NONE',  ( 2.935903058640790597, -2.042584291827519660, 0.5695675404085094318 ) ) ;
#110232=CARTESIAN_POINT ( 'NONE',  ( 4.153314892778156242, -1.795761387672462961, -1.203114871582221079 ) ) ;
#110233=CARTESIAN_POINT ( 'NONE',  ( 3.614658571667620279, -0.1319153736358945894, 1.836568937333193485 ) ) ;
#110236=CARTESIAN_POINT ( 'NONE',  ( 5.454937174282652457, 0.3337844340769695606, -1.707832357695503234 ) ) ;
#110240=CARTESIAN_POINT ( 'NONE',  ( 3.098656953246520906, -0.6260995091542166380, -2.069055637940686143 ) ) ;
#110241=CARTESIAN_POINT ( 'NONE',  ( 5.659529772124847646, -0.4871306767523299608, -1.956261131662299535 ) ) ;
#110244=CARTESIAN_POINT ( 'NONE',  ( 2.536181837661064087, 1.019768383293401248, -1.906060392209196763 ) ) ;
#110245=CARTESIAN_POINT ( 'NONE',  ( 3.901606001822624403, -0.5752225463674947026, 1.885544661340606165 ) ) ;
#110246=CARTESIAN_POINT ( 'NONE',  ( 0.1874131419884322858, 1.628132678060219884, 1.467219630700428157 ) ) ;
#110247=CARTESIAN_POINT ( 'NONE',  ( 4.897963269493502025, -0.6577025220009655726, -1.827417481390420928 ) ) ;
#110256=CARTESIAN_POINT ( 'NONE',  ( 2.415298318263587873, 1.970979330149217335, 0.9926799514654092160 ) ) ;
#110258=CARTESIAN_POINT ( 'NONE',  ( 6.737165023268617325, -0.09304339776683606678, -1.959646862056351857 ) ) ;
#110264=CARTESIAN_POINT ( 'NONE',  ( 5.120983416928425846, -1.747193932927636029, 0.5808180576658967809 ) ) ;
#110269=CARTESIAN_POINT ( 'NONE',  ( 6.433838290133602200, -2.056603270127650429, 0.5165238393732355382 ) ) ;
#110272=CARTESIAN_POINT ( 'NONE',  ( 6.169226111886771946, 0.1559856310293654957, -2.054958193847939096 ) ) ;
#110274=CARTESIAN_POINT ( 'NONE',  ( 2.383057912469242812, -0.003606268183664260163, 1.861241884763777499 ) ) ;
#110275=CARTESIAN_POINT ( 'NONE',  ( 4.229911503591711863, 1.806553461410321582, 0.3548724298726435022 ) ) ;
#110281=CARTESIAN_POINT ( 'NONE',  ( 4.283934280384479543, 1.440456688004333019, 1.672026782002330458 ) ) ;
#110282=CARTESIAN_POINT ( 'NONE',  ( 5.870491743106223126, -1.441790217864300283, 1.743476569090945061 ) ) ;
#110284=CARTESIAN_POINT ( 'NONE',  ( 5.959207022242491547, -1.525490245149653701, 0.9768169865009832531 ) ) ;
#110285=CARTESIAN_POINT ( 'NONE',  ( 6.333208386676280277, -1.543085173044305591, -1.135110930932172746 ) ) ;
#110288=CARTESIAN_POINT ( 'NONE',  ( 6.403191318657627029, 1.556466930477506505, 1.037356966126230517 ) ) ;
#110289=CARTESIAN_POINT ( 'NONE',  ( 5.953752735127215701, -1.388294428863137586, -1.315342447896154843 ) ) ;
#110291=CARTESIAN_POINT ( 'NONE',  ( 1.111929834214450796, -0.8377583890188080584, -1.672643128629976772 ) ) ;
#110292=CARTESIAN_POINT ( 'NONE',  ( 0.8312679839070147292, -1.592664559859976237, -1.236796411087807801 ) ) ;
#110295=CARTESIAN_POINT ( 'NONE',  ( 4.459663826605764214, 0.4620033958209149305, -2.054602365452788071 ) ) ;
#110300=CARTESIAN_POINT ( 'NONE',  ( 3.375264624815476289, -1.783316433176849625, -0.9482593927577113169 ) ) ;
#110303=CARTESIAN_POINT ( 'NONE',  ( 4.868538603872567982, -1.416007186031362330, 1.633285015310452115 ) ) ;
#110304=CARTESIAN_POINT ( 'NONE',  ( 6.620655732516627090, 7.629137130509076492, 2.426260288887295502 ) ) ;
#110309=CARTESIAN_POINT ( 'NONE',  ( 0.4499840099862363330, 1.609255455985519445, 1.457649523623653298 ) ) ;
#110312=CARTESIAN_POINT ( 'NONE',  ( 0.9602180038516641147, -1.664555262390180257, -0.7873027242753791732 ) ) ;
#110314=CARTESIAN_POINT ( 'NONE',  ( 1.804482060849887270, 1.621174160030929068, -1.474864209862189579 ) ) ;
#110316=CARTESIAN_POINT ( 'NONE',  ( 2.378104638162964246, 1.391771292293322082, 1.783738300129237508 ) ) ;
#110323=CARTESIAN_POINT ( 'NONE',  ( 4.639784515242838303, 0.7573303825321504590, -1.599664492173937358 ) ) ;
#110326=CARTESIAN_POINT ( 'NONE',  ( 0.6750070354940709283, -1.982970624965023410, -0.7094951434080811747 ) ) ;
#110332=CARTESIAN_POINT ( 'NONE',  ( 5.958611281643053204, -1.915606116362132072, -0.6298603123368745615 ) ) ;
#110333=CARTESIAN_POINT ( 'NONE',  ( 5.045072953846708508, 0.1408599011454790551, 1.806194821104394777 ) ) ;
#110336=CARTESIAN_POINT ( 'NONE',  ( 3.238977024203249400, -1.650389259550872456, 0.8806316622528218563 ) ) ;
#110337=CARTESIAN_POINT ( 'NONE',  ( 4.856339096887199780, -2.069677458173447171, -0.05615216265978521804 ) ) ;
#110346=CARTESIAN_POINT ( 'NONE',  ( 3.648837080137564470, -0.3802854374791163616, -1.924481129451253603 ) ) ;
#110347=CARTESIAN_POINT ( 'NONE',  ( 1.177110994959302825, -0.9039684864705423983, -1.802142742073430171 ) ) ;
#110350=CARTESIAN_POINT ( 'NONE',  ( 0.9834252619641962179, 1.251819791611600285, 1.390119989509101650 ) ) ;
#110352=CARTESIAN_POINT ( 'NONE',  ( 2.970950383256478755, -1.521771678934441097, 1.318087423592265717 ) ) ;
#110354=CARTESIAN_POINT ( 'NONE',  ( 3.339577153505444151, 0.5119293057267596536, -2.054306502313862470 ) ) ;
#110355=CARTESIAN_POINT ( 'NONE',  ( 6.825078400183551608, 0.5660753733540256905, 2.196387875007102419 ) ) ;
#110356=CARTESIAN_POINT ( 'NONE',  ( 5.441872305809390298, 1.387781221417656141, 1.536568222347669987 ) ) ;
#110358=CARTESIAN_POINT ( 'NONE',  ( 6.615180898807764720, -2.028213694748048024, 0.5066274125750843682 ) ) ;
#110360=CARTESIAN_POINT ( 'NONE',  ( 5.051681782491273864, 0.5714109786712183725, -1.733901259708306331 ) ) ;
#110363=CARTESIAN_POINT ( 'NONE',  ( 6.639320575229281651, -0.0007625845807879281287, 2.103388539994067497 ) ) ;
#110365=CARTESIAN_POINT ( 'NONE',  ( 6.721690211428396289, -2.142211831252617493, 0.5295551626897446740 ) ) ;
#110367=CARTESIAN_POINT ( 'NONE',  ( 4.969353466749234727, -1.617520173792227567, -1.019718193788564209 ) ) ;
#110377=CARTESIAN_POINT ( 'NONE',  ( -0.02299388927992032997, 5.724334336916190757, -2.505015335112478425 ) ) ;
#110384=CARTESIAN_POINT ( 'NONE',  ( 2.395301122324170695, -1.761490415372953589, 0.8809153588016715997 ) ) ;
#110385=CARTESIAN_POINT ( 'NONE',  ( 3.532827515057835654, -1.646827434736859441, 1.163287548526056980 ) ) ;
#110388=CARTESIAN_POINT ( 'NONE',  ( 6.827182134110205247, 2.955377424523279117, 2.541486622063714673 ) ) ;
#110389=CARTESIAN_POINT ( 'NONE',  ( 3.398540877415173966, 1.727514402264049620, -1.348270469230819391 ) ) ;
#110391=CARTESIAN_POINT ( 'NONE',  ( 1.782126058915745936, -1.032679515686143024, 1.626040290554785717 ) ) ;
#110394=CARTESIAN_POINT ( 'NONE',  ( 0.2333540202161610289, 0.003568502611739353923, -2.045944795905803471 ) ) ;
#110400=CARTESIAN_POINT ( 'NONE',  ( 6.321814700078944860, 1.054209175812788502, -1.509406368332133930 ) ) ;
#110401=CARTESIAN_POINT ( 'NONE',  ( 2.649090073008007362, 0.2487567141898557876, 1.997615136964459470 ) ) ;
#110402=CARTESIAN_POINT ( 'NONE',  ( 4.745672437882476835, -2.227950070917711134, -0.5642311211754289513 ) ) ;
#110403=CARTESIAN_POINT ( 'NONE',  ( -0.1288028175206907822, -0.008968661790493319408, -2.273875003271645934 ) ) ;
#110404=CARTESIAN_POINT ( 'NONE',  ( 1.709564315929460232, 0.5465817987246027743, -1.778839887662834185 ) ) ;
#110407=CARTESIAN_POINT ( 'NONE',  ( 5.449440537890920311, -1.726199344983204265, 0.8234401749890255529 ) ) ;
#110411=CARTESIAN_POINT ( 'NONE',  ( 5.003505698738024421, -2.080571448108500476, 0.2061593518874194064 ) ) ;
#110412=CARTESIAN_POINT ( 'NONE',  ( 3.906994808788874174, 1.604092888448312326, 0.9621832354540849064 ) ) ;
#110417=CARTESIAN_POINT ( 'NONE',  ( 5.760297821273290708, 0.7050700890500715134, 1.574392225784694066 ) ) ;
#110419=CARTESIAN_POINT ( 'NONE',  ( 1.670155932360503970, 1.196126419257515838, 1.255837360413303738 ) ) ;
#110421=CARTESIAN_POINT ( 'NONE',  ( 6.539320575229233157, 0.001224430076711413356, 2.103502572931112091 ) ) ;
#110422=CARTESIAN_POINT ( 'NONE',  ( 6.315638730379727228, -1.320822524126588515, -1.523799118890494020 ) ) ;
#110423=CARTESIAN_POINT ( 'NONE',  ( 6.157114316693172995, 1.779627781583184909, -1.243356570269833483 ) ) ;
#110424=CARTESIAN_POINT ( 'NONE',  ( 4.898959864523320107, 1.516061528642864253, -1.016892643307308441 ) ) ;
#110425=CARTESIAN_POINT ( 'NONE',  ( 2.061309051315598051, 1.628117514333087934, 1.094105149622534467 ) ) ;
#110426=CARTESIAN_POINT ( 'NONE',  ( 0.2283145101530216492, 2.111890517744571927, 0.1509969543822299032 ) ) ;
#110429=CARTESIAN_POINT ( 'NONE',  ( 2.561320117580662803, -1.761587792986643475, 1.180070990429403555 ) ) ;
#110434=CARTESIAN_POINT ( 'NONE',  ( 6.983263157960363010, -0.009046620988246899253, 2.153544821522495489 ) ) ;
#110437=CARTESIAN_POINT ( 'NONE',  ( 3.809420206217276395, 1.876102094647231988, -1.189034995700769981 ) ) ;
#110439=CARTESIAN_POINT ( 'NONE',  ( 1.214008909562364069, 2.217199183031343779, 0.6065299581617057401 ) ) ;
#110441=CARTESIAN_POINT ( 'NONE',  ( 5.225460488781804358, 0.2076664479006613828, -2.052122333454815539 ) ) ;
#110444=CARTESIAN_POINT ( 'NONE',  ( 0.2329586101569320611, 0.7537478099126624365, -1.931748487665209124 ) ) ;
#110445=CARTESIAN_POINT ( 'NONE',  ( 5.882333747326812023, -0.2767177626767613474, -1.820229446528654371 ) ) ;
#110448=CARTESIAN_POINT ( 'NONE',  ( -0.1104750535120025690, -0.004616138082884356161, -2.103378236956428893 ) ) ;
#110449=CARTESIAN_POINT ( 'NONE',  ( 2.432253191915220825, 1.672178088080849223, 0.4220979471536658867 ) ) ;
#110450=CARTESIAN_POINT ( 'NONE',  ( 1.217982839071569012, 0.9896824804975332679, -1.756856037137773940 ) ) ;
#110451=CARTESIAN_POINT ( 'NONE',  ( 3.041888879667261403, -1.739239095176773775, 1.503071639953108773 ) ) ;
#110452=CARTESIAN_POINT ( 'NONE',  ( 2.847247395794590297, -1.882567391055539385, 1.254484791939513899 ) ) ;
#110453=CARTESIAN_POINT ( 'NONE',  ( 5.391282926306558032, 1.858022621660906371, -0.9916069233004040084 ) ) ;
#110455=CARTESIAN_POINT ( 'NONE',  ( 3.356489944714312834, -1.342140201951192102, 1.153657164820639958 ) ) ;
#110457=CARTESIAN_POINT ( 'NONE',  ( 6.005493137707444973, -2.275576565988911337, 0.2767016799969032603 ) ) ;
#110458=CARTESIAN_POINT ( 'NONE',  ( 4.576008823784957436, -1.786506429242448624, -0.4446734633927542091 ) ) ;
#110463=CARTESIAN_POINT ( 'NONE',  ( 4.681673494351117348, -1.034495392153191418, 1.931897795048514554 ) ) ;
#110466=CARTESIAN_POINT ( 'NONE',  ( 4.949704645232674061, 1.531818663031824013, 1.392983054852282132 ) ) ;
#110469=CARTESIAN_POINT ( 'NONE',  ( 3.510301166856438115, -0.7815644168660453861, -1.761018089871415393 ) ) ;
#110472=CARTESIAN_POINT ( 'NONE',  ( 0.0006278483607258588750, -1.039594266688011137, 1.963129682597685166 ) ) ;
#110479=AXIS2_PLACEMENT_3D ( 'NONE', #104661, #185874, #154474 ) ;
#110482=CARTESIAN_POINT ( 'NONE',  ( 1.099968687278202406, 0.7983322178258808188, -1.792280776234014050 ) ) ;
#110485=CARTESIAN_POINT ( 'NONE',  ( 5.928642344448160628, 2.082074431819755045, 0.5810635428650026135 ) ) ;
#110486=CARTESIAN_POINT ( 'NONE',  ( 5.406682003534418079, 0.5678430586343993225, 1.877905798087247335 ) ) ;
#110489=CARTESIAN_POINT ( 'NONE',  ( 5.735289742212391850, -1.956171686333206816, 0.9202595734885756773 ) ) ;
#110493=CARTESIAN_POINT ( 'NONE',  ( 6.608667082420285332, 1.462428336960637676, -1.322156044359092064 ) ) ;
#110494=CARTESIAN_POINT ( 'NONE',  ( 6.134130222960958889, 0.1235499018571624141, -1.729521282446895070 ) ) ;
#110496=CARTESIAN_POINT ( 'NONE',  ( 2.525153347276567484, -2.043736813514348771, 0.7916865192442237298 ) ) ;
#110497=CARTESIAN_POINT ( 'NONE',  ( 4.401628477801726724, 1.850755835686506590, 1.378093606121533199 ) ) ;
#110498=CARTESIAN_POINT ( 'NONE',  ( 5.378222296270031677, -1.148346438381561363, 1.710960936357192264 ) ) ;
#110499=CARTESIAN_POINT ( 'NONE',  ( 1.570153368812776229, -1.843976851262040029, -0.6092462720258711162 ) ) ;
#110502=CARTESIAN_POINT ( 'NONE',  ( 5.045234882716379765, 0.1584239314957915090, 2.114765283346302205 ) ) ;
#110503=CARTESIAN_POINT ( 'NONE',  ( 2.180314765559120183, 1.560501322096979449, 1.277041908422072991 ) ) ;
#110505=CARTESIAN_POINT ( 'NONE',  ( 5.210101597250164751, -2.196594437182074255, 0.2116553293704941940 ) ) ;
#110508=CARTESIAN_POINT ( 'NONE',  ( 0.08226035653636187828, -1.769965142718381124, -0.4472663993063328847 ) ) ;
#110514=CARTESIAN_POINT ( 'NONE',  ( 4.750885258907265651, -1.656392207783722315, 1.226022070186979063 ) ) ;
#110519=CARTESIAN_POINT ( 'NONE',  ( 4.688151973431080144, 1.164670015804763370, 1.649827500200540253 ) ) ;
#110525=CARTESIAN_POINT ( 'NONE',  ( 4.082927109850850833, -0.2000173336921743650, -2.051146848037002979 ) ) ;
#110526=CARTESIAN_POINT ( 'NONE',  ( 3.094375128876575065, -0.3905979561782264575, 1.978050703236901686 ) ) ;
#110528=CARTESIAN_POINT ( 'NONE',  ( 6.727182134110194944, 2.413774403037728167, 2.569658639860139093 ) ) ;
#110532=CARTESIAN_POINT ( 'NONE',  ( 2.864611068004913275, -0.6351033500862738324, 1.913510180259501592 ) ) ;
#110533=CARTESIAN_POINT ( 'NONE',  ( 2.079791654855645877, -1.805462111169679584, -0.3597937517794968509 ) ) ;
#110534=CARTESIAN_POINT ( 'NONE',  ( 0.7687468715882056491, 1.142267183891092053, 2.005099294460314319 ) ) ;
#110537=CARTESIAN_POINT ( 'NONE',  ( 2.513140823169751847, 1.929641211675875878, 0.9743453106897670413 ) ) ;
#110541=CARTESIAN_POINT ( 'NONE',  ( 1.498681428038322050, 1.531199225506232553, -1.074333469806128427 ) ) ;
#110542=CARTESIAN_POINT ( 'NONE',  ( 5.612177202991157188, -0.8859793764278474093, -1.761228054870385806 ) ) ;
#110546=CARTESIAN_POINT ( 'NONE',  ( 0.3115100037339203487, 1.922317768103290803, 1.083863418116323807 ) ) ;
#110547=CARTESIAN_POINT ( 'NONE',  ( 6.777786256569462431, -2.009253640576996514, 0.4989836931604470505 ) ) ;
#110550=CARTESIAN_POINT ( 'NONE',  ( 6.639320575229251453, 6.034321252505787214, 2.798156424428144717 ) ) ;
#110551=CARTESIAN_POINT ( 'NONE',  ( 5.383651750111712708, 1.323420565077202182, 1.461416689776244615 ) ) ;
#110552=CARTESIAN_POINT ( 'NONE',  ( 6.293224362130668936, -0.1031327824093461465, -2.017302584901353946 ) ) ;
#110554=CARTESIAN_POINT ( 'NONE',  ( 4.301628547034565209, 1.852045629758605649, 1.376555262909467947 ) ) ;
#110556=CARTESIAN_POINT ( 'NONE',  ( 1.463816541924748638, -0.5049463793320208005, 1.999668334691290683 ) ) ;
#110563=CARTESIAN_POINT ( 'NONE',  ( 4.826735082517537023, -1.421624449711873295, 1.641102681368050487 ) ) ;
#110565=CARTESIAN_POINT ( 'NONE',  ( 4.423293856316495187, -1.136390847421838490, -1.448631019334602144 ) ) ;
#110568=CARTESIAN_POINT ( 'NONE',  ( 5.812113132715003516, 1.472855484078567700, -1.623034594306454137 ) ) ;
#110570=CARTESIAN_POINT ( 'NONE',  ( 6.051720714260678591, 0.6634699467917944959, -2.163057363297292035 ) ) ;
#110577=CARTESIAN_POINT ( 'NONE',  ( 0.5492016079408028606, 0.5613503750152969429, -1.678537049539428727 ) ) ;
#110578=CARTESIAN_POINT ( 'NONE',  ( 5.725249205227378013, 1.776381904961796154, 0.9470739834369249488 ) ) ;
#110580=CARTESIAN_POINT ( 'NONE',  ( 3.944438254296574797, 2.095630017474863660, 0.2083849179023259668 ) ) ;
#110581=CARTESIAN_POINT ( 'NONE',  ( 1.933070621186453897, -1.539717990624125621, -1.139454883405303098 ) ) ;
#110583=CARTESIAN_POINT ( 'NONE',  ( 2.963290904843593587, 1.662405373943407261, 1.055889934586044188 ) ) ;
#110584=CARTESIAN_POINT ( 'NONE',  ( 5.291273337336410698, -0.05367003302336400411, -2.019259759236047280 ) ) ;
#110585=CARTESIAN_POINT ( 'NONE',  ( 2.184254540302111636, -1.834043650784190405, -0.3674020703766100460 ) ) ;
#110586=CARTESIAN_POINT ( 'NONE',  ( 4.582452686631489414, -1.674003568303910949, -0.4152789331205719026 ) ) ;
#110587=CARTESIAN_POINT ( 'NONE',  ( 1.634869402278725348, 1.785593253932623803, 0.6852637533772619749 ) ) ;
#110589=CARTESIAN_POINT ( 'NONE',  ( 1.471597369358583318, 0.1596246592955492538, -2.201166978212334424 ) ) ;
#110600=CARTESIAN_POINT ( 'NONE',  ( 1.943885480841448965, 1.426152643941134501, 1.501071833787496645 ) ) ;
#110605=CARTESIAN_POINT ( 'NONE',  ( -0.02277885239688070759, -1.805142470748948513, -0.9059449988992168690 ) ) ;
#110611=CARTESIAN_POINT ( 'NONE',  ( 4.868517441940229951, -0.5404072756688070855, 1.942244311778835497 ) ) ;
#110612=CARTESIAN_POINT ( 'NONE',  ( 5.278507882932355955, -0.4720989235634742154, -1.856488224439522439 ) ) ;
#110614=CARTESIAN_POINT ( 'NONE',  ( 2.894263506066748093, -0.6386881658498286818, -2.096408367471907841 ) ) ;
#110615=CARTESIAN_POINT ( 'NONE',  ( 0.2335667940002684184, 0.001055507091213009818, -2.153566573614831281 ) ) ;
#110617=CARTESIAN_POINT ( 'NONE',  ( 5.554944837187737683, 0.3969321943368699368, 1.973527061375530023 ) ) ;
#110620=CARTESIAN_POINT ( 'NONE',  ( 6.345324880664913181, 0.3618513607092630480, -2.085922816363374288 ) ) ;
#110622=CARTESIAN_POINT ( 'NONE',  ( 3.140259756110568734, 0.5104685904834010968, 2.027328384984484533 ) ) ;
#110624=CARTESIAN_POINT ( 'NONE',  ( 1.535739282219195978, 0.8544175402723229729, -1.498188246372294863 ) ) ;
#110626=CARTESIAN_POINT ( 'NONE',  ( 6.170199167347634628, 2.114832956739281400, -0.1575216572810705096 ) ) ;
#110633=CARTESIAN_POINT ( 'NONE',  ( 1.769862606763368706, 1.806619053477545700, -0.1335387089566111574 ) ) ;
#110639=CARTESIAN_POINT ( 'NONE',  ( 3.141053669680595739, 0.04696373034178760036, 1.811039086309898627 ) ) ;
#110644=CARTESIAN_POINT ( 'NONE',  ( 3.596024570820981037, 0.8385914878215626755, -1.661501840750801540 ) ) ;
#110645=CARTESIAN_POINT ( 'NONE',  ( 1.651812010259229968, 0.9862763539280462455, 1.642055979085883299 ) ) ;
#110646=CARTESIAN_POINT ( 'NONE',  ( 0.5338675855391886715, 0.9430634504648884864, -1.562995807167219642 ) ) ;
#110653=CARTESIAN_POINT ( 'NONE',  ( 5.489095164188675824, 0.1408790922432824055, 1.964433151921646470 ) ) ;
#110656=CARTESIAN_POINT ( 'NONE',  ( 0.2872076490801517279, 1.550519377178682268, 1.402564467939530823 ) ) ;
#110658=CARTESIAN_POINT ( 'NONE',  ( 5.051747076446268636, 0.6043308924107357871, -1.829198057362067198 ) ) ;
#110660=CARTESIAN_POINT ( 'NONE',  ( 0.8678470384533981674, 0.8956018474440343713, 1.590720368640268001 ) ) ;
#110661=CARTESIAN_POINT ( 'NONE',  ( 2.245003380770736801, 0.4850519687749441644, 2.152760086278446394 ) ) ;
#110664=CARTESIAN_POINT ( 'NONE',  ( 0.4847283499135228713, 1.883623918205453718, 0.5753430019505183513 ) ) ;
#110665=CARTESIAN_POINT ( 'NONE',  ( 2.331498104393217474, 0.9136196428927362279, -1.713718834741830177 ) ) ;
#110667=CARTESIAN_POINT ( 'NONE',  ( 0.8079699768257715409, -1.730602710733687877, 1.034004433739174500 ) ) ;
#110669=CARTESIAN_POINT ( 'NONE',  ( 5.823074758751579871, -1.681767765412798710, -0.7970822532109583802 ) ) ;
#110675=CARTESIAN_POINT ( 'NONE',  ( 1.804482060849887270, 1.621174160030929068, -1.474864209862189579 ) ) ;
#110679=CARTESIAN_POINT ( 'NONE',  ( 2.560947663861262491, -1.588335953301520220, -0.9000364273514869229 ) ) ;
#110687=CARTESIAN_POINT ( 'NONE',  ( 1.506341009219732907, -0.6927896466909737594, -1.797792356224122923 ) ) ;
#110688=CARTESIAN_POINT ( 'NONE',  ( 5.119951393648711324, 1.940949770148656661, -0.2839766199017114690 ) ) ;
#110691=CARTESIAN_POINT ( 'NONE',  ( 4.845371438081495619, 0.6875289519675978900, -2.081009137124201658 ) ) ;
#110693=CARTESIAN_POINT ( 'NONE',  ( 3.555589372526322123, 1.629040189086952362, 1.277421477176057474 ) ) ;
#110696=CARTESIAN_POINT ( 'NONE',  ( 3.709890859234076466, 2.183183022688690578, 0.7197655052363950423 ) ) ;
#110703=CARTESIAN_POINT ( 'NONE',  ( 4.119036135373352003, -1.858019016064060169, 0.5647323716678387395 ) ) ;
#110707=CARTESIAN_POINT ( 'NONE',  ( 4.992401499097729456, -1.057410677138232780, 1.593263788312593743 ) ) ;
#110708=CARTESIAN_POINT ( 'NONE',  ( 6.457991230880992362, 1.719707694194565484, -0.1327171722449934921 ) ) ;
#110709=CARTESIAN_POINT ( 'NONE',  ( 4.698454014923811428, 1.387101836239763131, -1.463925544105355803 ) ) ;
#110711=CARTESIAN_POINT ( 'NONE',  ( 2.315298440750997777, 1.971968782506158924, 0.9909306302095726160 ) ) ;
#110714=CARTESIAN_POINT ( 'NONE',  ( 1.886780952650327636, 1.818441039422484806, -1.031378756152110610 ) ) ;
#110715=CARTESIAN_POINT ( 'NONE',  ( 0.4437791967034719343, 1.764639887404760188, 0.1366099650685937694 ) ) ;
#110716=CARTESIAN_POINT ( 'NONE',  ( 6.100232455412330168, -0.2440331339308223768, 2.001510902166554473 ) ) ;
#110718=CARTESIAN_POINT ( 'NONE',  ( 3.521668038933927658, -1.364967583988693889, -1.841414078927001041 ) ) ;
#110719=CARTESIAN_POINT ( 'NONE',  ( 0.6029369919973374126, -1.732405018438128552, 0.1659646143751663805 ) ) ;
#110721=CARTESIAN_POINT ( 'NONE',  ( 2.812858766682566181, -0.6196351552101020399, -2.028021595557969015 ) ) ;
#110723=CARTESIAN_POINT ( 'NONE',  ( 1.317307599089176939, -1.370793471230176808, 1.061547382435957587 ) ) ;
#110726=CARTESIAN_POINT ( 'NONE',  ( 1.205810543264747681, -1.711434635494583967, -1.335908126413299923 ) ) ;
#110727=CARTESIAN_POINT ( 'NONE',  ( 3.626185617424378282, 2.007256095728218614, 0.1928357053486499662 ) ) ;
#110728=CARTESIAN_POINT ( 'NONE',  ( 5.281250000000004441, 0.7852924748302615443, 1.895863743163964665 ) ) ;
#110730=CARTESIAN_POINT ( 'NONE',  ( 6.358035567807713839, 1.921127907539350810, -0.1446545421508997620 ) ) ;
#110732=CARTESIAN_POINT ( 'NONE',  ( 3.182088186068011915, 2.166492470972399165, -0.4902054615175278629 ) ) ;
#110738=CARTESIAN_POINT ( 'NONE',  ( 5.759256982813394821, 1.713166593665109705, -0.3060214249656545982 ) ) ;
#110739=CARTESIAN_POINT ( 'NONE',  ( 4.141029529442549872, -0.1900441490861082827, -1.952618137025011746 ) ) ;
#110745=CARTESIAN_POINT ( 'NONE',  ( 6.274757189715042927, -2.145364790639526564, -0.7184590933012062752 ) ) ;
#110746=CARTESIAN_POINT ( 'NONE',  ( 1.996602216506689453, 2.039906831610329263, 0.3049752315822819027 ) ) ;
#110750=CARTESIAN_POINT ( 'NONE',  ( 3.866346082213562685, -1.258301477641217803, 1.384200088751494251 ) ) ;
#110751=CARTESIAN_POINT ( 'NONE',  ( 2.109626794357027268, 0.001117226762978317921, 1.734343004219033757 ) ) ;
#110752=CARTESIAN_POINT ( 'NONE',  ( 6.374583145400191775, -0.1054333438532777389, -2.189162923280890904 ) ) ;
#110753=CARTESIAN_POINT ( 'NONE',  ( 1.307976841356368602, -0.5351398426680589182, 2.140771676462468687 ) ) ;
#110754=CARTESIAN_POINT ( 'NONE',  ( 4.276362541559985075, -1.246951984143488623, 1.765614359104182629 ) ) ;
#110755=CARTESIAN_POINT ( 'NONE',  ( 5.121012332258009891, -1.843477085030984286, 0.6107378676363499626 ) ) ;
#110756=CARTESIAN_POINT ( 'NONE',  ( 6.678970768140332304, -0.09217866350584583146, -1.868372134486769420 ) ) ;
#110757=CARTESIAN_POINT ( 'NONE',  ( 0.01034996896555614825, -0.2601230917365888740, -1.999999999999999556 ) ) ;
#110759=CARTESIAN_POINT ( 'NONE',  ( 6.825078400183575589, -0.005632053428735600553, 2.144262460745151255 ) ) ;
#110760=CARTESIAN_POINT ( 'NONE',  ( 5.801407773674092105, 1.352156682446105984, -1.496049708713815374 ) ) ;
#110764=CARTESIAN_POINT ( 'NONE',  ( 3.211362085483655981, -0.3553965070040401852, 1.790585553824732390 ) ) ;
#110765=CARTESIAN_POINT ( 'NONE',  ( 2.274722540679521288, -1.357913018379176995, 1.739418515187239223 ) ) ;
#110770=CARTESIAN_POINT ( 'NONE',  ( 1.160422406460089428, 2.017671146822976880, 0.09473317391113857122 ) ) ;
#110771=CARTESIAN_POINT ( 'NONE',  ( 0.9441710812277158693, -1.348169866081018853, -1.636719737310005973 ) ) ;
#110775=CARTESIAN_POINT ( 'NONE',  ( 2.289708051090312058, -1.211253549455925338, -1.412920978024762908 ) ) ;
#110777=CARTESIAN_POINT ( 'NONE',  ( 0.3038912542124502236, -0.5749842496362895794, 2.083749421223294540 ) ) ;
#110778=CARTESIAN_POINT ( 'NONE',  ( 5.766250055133458119, 1.862018000461727052, -0.7743128548072516493 ) ) ;
#110781=CARTESIAN_POINT ( 'NONE',  ( 3.967279163243800255, 0.2216459979678051528, -1.812115712870238537 ) ) ;
#110786=CARTESIAN_POINT ( 'NONE',  ( 5.993517489292202960, 1.942244631591660164, 0.5404061186519912852 ) ) ;
#110787=CARTESIAN_POINT ( 'NONE',  ( 6.263598714517844890, 0.9507720431706818687, 1.576509192756641697 ) ) ;
#110789=CARTESIAN_POINT ( 'NONE',  ( 4.213705752388523962, -0.3967513169967327724, 2.273188601971836142 ) ) ;
#110791=CARTESIAN_POINT ( 'NONE',  ( 5.413408226029434722, -0.3230527293765028674, 2.137217106551466905 ) ) ;
#110793=CARTESIAN_POINT ( 'NONE',  ( 2.542442122522000414, -1.613304532933591995, 1.080848972723145618 ) ) ;
#110794=CARTESIAN_POINT ( 'NONE',  ( 4.728017916497640805, -2.050086588643835750, -1.039272215941482225 ) ) ;
#110796=CARTESIAN_POINT ( 'NONE',  ( 4.610133579271312954, -0.8000244862099057386, -1.691074300901610261 ) ) ;
#110798=CARTESIAN_POINT ( 'NONE',  ( 2.021601768330282045, -0.4154675118966509317, 1.866563793090275203 ) ) ;
#110801=CARTESIAN_POINT ( 'NONE',  ( 3.914836437932368796, 1.561248537261412883, -1.560010120355350471 ) ) ;
#110805=CARTESIAN_POINT ( 'NONE',  ( 1.458210469330342374, 0.7952313087857125762, 1.804010633499957272 ) ) ;
#110806=CARTESIAN_POINT ( 'NONE',  ( 1.765117381242779615, -1.630797578202509701, 1.632866094832433834 ) ) ;
#110807=CARTESIAN_POINT ( 'NONE',  ( 2.787496613063783713, -1.831585881375777713, 0.7034878451678548972 ) ) ;
#110810=CARTESIAN_POINT ( 'NONE',  ( 5.928601196466630086, -1.312702821215183002, 1.590880328853358394 ) ) ;
#110817=CARTESIAN_POINT ( 'NONE',  ( 1.973704989461112946, -0.2689809023317759618, 2.154309762211854107 ) ) ;
#110821=CARTESIAN_POINT ( 'NONE',  ( 2.811613793402362393, -1.850737340378521223, 0.2705540153197931730 ) ) ;
#110822=CARTESIAN_POINT ( 'NONE',  ( 0.2103215893997134323, -0.8792329509940269849, -1.862182962916396844 ) ) ;
#110823=CARTESIAN_POINT ( 'NONE',  ( 6.727182134110222478, 3.706444386917655986, 2.325533714637216143 ) ) ;
#110827=CARTESIAN_POINT ( 'NONE',  ( 1.717294761138322690, 1.590556852780611097, 1.061263400373997134 ) ) ;
#110830=CARTESIAN_POINT ( 'NONE',  ( 4.451851733873055217, 1.769451340447548038, -0.04442182319205205399 ) ) ;
#110831=CARTESIAN_POINT ( 'NONE',  ( 2.332540574144434053, 1.247770424613745543, -1.449200414897835687 ) ) ;
#110834=CARTESIAN_POINT ( 'NONE',  ( 6.609000000000045283, 0.005669918681758949128, 1.900160851458796651 ) ) ;
#110836=CARTESIAN_POINT ( 'NONE',  ( 0.9771079587245214970, 1.912259438035465386, 0.7939916666956441382 ) ) ;
#110838=CARTESIAN_POINT ( 'NONE',  ( 4.961713530105988923, 1.850188064717460223, -0.2750520410098392654 ) ) ;
#110839=CARTESIAN_POINT ( 'NONE',  ( 2.015964598666186269, -0.8597642540715648707, -1.610575774528985704 ) ) ;
#110840=CARTESIAN_POINT ( 'NONE',  ( 4.371826309796801979, 2.140994599346605742, -0.5347268394074317088 ) ) ;
#110843=CARTESIAN_POINT ( 'NONE',  ( 2.488800817111187946, 2.000174138640842258, 0.5034198422354563274 ) ) ;
#110850=CARTESIAN_POINT ( 'NONE',  ( 5.934052368846653991, 1.230181698326970885, 1.665117723180092213 ) ) ;
#110852=CARTESIAN_POINT ( 'NONE',  ( 2.829541668879275829, -2.018026287816252040, 0.7751260729957699658 ) ) ;
#110854=CARTESIAN_POINT ( 'NONE',  ( 3.387372106552827944, 0.04729818973902254198, -2.019286085025721267 ) ) ;
#110863=CARTESIAN_POINT ( 'NONE',  ( 0.8136858238772455287, -1.282993010278702606, -1.555696519147983459 ) ) ;
#110865=CARTESIAN_POINT ( 'NONE',  ( 5.899973326018036701, -0.7874313895239596350, -2.045375389432432467 ) ) ;
#110868=CARTESIAN_POINT ( 'NONE',  ( 5.080287894202283994, 0.9478536798121822704, 1.660923459347658282 ) ) ;
#110872=CARTESIAN_POINT ( 'NONE',  ( 3.216422893352603563, 1.967893637826668263, 0.4390085219014849827 ) ) ;
#110875=CARTESIAN_POINT ( 'NONE',  ( 5.455954713372185516, 1.722626330383254745, -0.08824682005538657392 ) ) ;
#110880=CARTESIAN_POINT ( 'NONE',  ( 1.551716534671506498, 1.565040117424065347, 1.355267069636761912 ) ) ;
#110883=CARTESIAN_POINT ( 'NONE',  ( 5.777939495331589015, 1.783485896618082878, -0.3162516061415173718 ) ) ;
#110886=CARTESIAN_POINT ( 'NONE',  ( 0.4745106373920011666, -1.311730567922615665, 1.249698552857400946 ) ) ;
#110889=CARTESIAN_POINT ( 'NONE',  ( 2.888834398507355239, 1.879202789969806497, -1.127179367409691935 ) ) ;
#110891=CARTESIAN_POINT ( 'NONE',  ( 0.7132427667453158371, -1.655377960257615966, -1.052639099659122390 ) ) ;
#110893=CARTESIAN_POINT ( 'NONE',  ( 4.569893716599374933, -0.8992288252529623271, 1.691407037985042772 ) ) ;
#110901=CARTESIAN_POINT ( 'NONE',  ( 1.991316529349271836, 1.880942973025516940, -1.065213018539921563 ) ) ;
#110904=CARTESIAN_POINT ( 'NONE',  ( 1.553431815599433108, 0.5335803070953272220, -1.745854899344486233 ) ) ;
#110905=CARTESIAN_POINT ( 'NONE',  ( 0.01804983835817890528, -0.5593552815991027494, 2.045460531183339814 ) ) ;
#110906=CARTESIAN_POINT ( 'NONE',  ( 4.805575371506604299, -0.4859443722219913830, 1.759630929660048526 ) ) ;
#110908=CARTESIAN_POINT ( 'NONE',  ( 3.463059065379545221, -1.560675823418774533, 1.104941681961457256 ) ) ;
#110910=CARTESIAN_POINT ( 'NONE',  ( 3.719166427026363131, -1.735901824557140927, -0.9304994270666072653 ) ) ;
#110912=CARTESIAN_POINT ( 'NONE',  ( 6.356980358691139088, 0.3275572002108660952, -1.914087848568704731 ) ) ;
#110916=CARTESIAN_POINT ( 'NONE',  ( 5.941668366282724101, -1.996146358238064522, 0.7160658055916299114 ) ) ;
#110918=CARTESIAN_POINT ( 'NONE',  ( 3.773993364719562926, 1.897484654492180400, -0.2369724479281897500 ) ) ;
#110924=CARTESIAN_POINT ( 'NONE',  ( 5.268231569329090647, 2.010679013512342017, -0.1011730594673541789 ) ) ;
#110926=CARTESIAN_POINT ( 'NONE',  ( 6.076747101522134820, -1.735163100867884500, -0.5679748894881069265 ) ) ;
#110927=CARTESIAN_POINT ( 'NONE',  ( 0.6782873735513492708, -1.106163567672680204, -1.749894625276714688 ) ) ;
#110931=CARTESIAN_POINT ( 'NONE',  ( 6.438356904408193415, 1.850619875698428674, 0.2722718653145329015 ) ) ;
#110933=( NAMED_UNIT ( * ) SI_UNIT ( $, .STERADIAN. ) SOLID_ANGLE_UNIT ( ) );
#110940=CARTESIAN_POINT ( 'NONE',  ( 3.568775204899740316, -0.8506723435033979319, 1.511049830170706931 ) ) ;
#110942=CARTESIAN_POINT ( 'NONE',  ( 0.7607008448355723207, -0.6940761377024067258, -1.950597895851911456 ) ) ;
#110943=CARTESIAN_POINT ( 'NONE',  ( 3.814152603263697650, 1.130891212129871093, -1.789721717560237790 ) ) ;
#110947=CARTESIAN_POINT ( 'NONE',  ( 0.5847281401991512029, 1.882922653073782815, 0.5772291209212175866 ) ) ;
#110952=CARTESIAN_POINT ( 'NONE',  ( 3.381108394495379699, 2.072348265612040219, -0.9799971971852624586 ) ) ;
#110953=CARTESIAN_POINT ( 'NONE',  ( 1.172165686010542496, -1.159919637379997814, 1.409874495853599141 ) ) ;
#110954=CARTESIAN_POINT ( 'NONE',  ( 3.357576282340120066, -1.451192137084562628, -1.245647637661301044 ) ) ;
#110958=CARTESIAN_POINT ( 'NONE',  ( 1.599859548348059324, 1.391279381849828800, 1.455310581225319311 ) ) ;
#110959=CARTESIAN_POINT ( 'NONE',  ( 1.973419848571813073, -0.2453196125269933581, 1.946320556625024345 ) ) ;
#110962=CARTESIAN_POINT ( 'NONE',  ( 4.716787809154822320, -0.1028738300157816532, 2.088225860312553195 ) ) ;
#110963=CARTESIAN_POINT ( 'NONE',  ( 3.977242411272710942, 1.666424048269627534, -0.5965368118019414023 ) ) ;
#110966=CARTESIAN_POINT ( 'NONE',  ( -0.02900071798685524560, -0.004641455105012376459, -2.173770343569726649 ) ) ;
#110967=CARTESIAN_POINT ( 'NONE',  ( 3.925522983587381276, 0.9287783018587884021, -1.471562914255954757 ) ) ;
#110971=CARTESIAN_POINT ( 'NONE',  ( 4.182719533963025427, -0.8905394866418876454, -1.487461311242815443 ) ) ;
#110973=CARTESIAN_POINT ( 'NONE',  ( 4.563029256048502624, 1.681186374793992355, -1.373936881898863982 ) ) ;
#110975=CARTESIAN_POINT ( 'NONE',  ( 6.333220217719927270, -1.622483202430196725, -1.197309987464048486 ) ) ;
#110976=CARTESIAN_POINT ( 'NONE',  ( 5.125000000000002665, -2.052068128417943171, 3.046444613966958600E-13 ) ) ;
#110977=DIRECTION ( 'NONE',  ( -0.9999980456341538426, 0.000000000000000000, -0.001977050295941262543 ) ) ;
#110978=CARTESIAN_POINT ( 'NONE',  ( 3.223571483072392940, -1.856993652095505487, 0.5122080487700955143 ) ) ;
#110980=CARTESIAN_POINT ( 'NONE',  ( 0.3291711827644402399, 1.527175228150777331, -1.613279532339807476 ) ) ;
#110981=ORIENTED_EDGE ( 'NONE', *, *, #212871, .T. ) ;
#110982=CARTESIAN_POINT ( 'NONE',  ( -0.1411974294641968053, 0.7397609206469482057, -1.984549174418163808 ) ) ;
#110985=EDGE_CURVE ( 'NONE', #120459, #60268, #23208, .T. ) ;
#110986=CARTESIAN_POINT ( 'NONE',  ( 2.930584098205230248, -1.096850167032170420, -1.931549987457868989 ) ) ;
#110992=CARTESIAN_POINT ( 'NONE',  ( 0.9674229098759130618, -1.967888300253183953, -0.4390273639364171698 ) ) ;
#110994=CARTESIAN_POINT ( 'NONE',  ( 5.178211798877670802, -1.100624681205965461, -1.744318484351764509 ) ) ;
#110999=CARTESIAN_POINT ( 'NONE',  ( 0.2976568962721929390, -1.769157359987379996, -0.05240849467303894393 ) ) ;
#111000=CARTESIAN_POINT ( 'NONE',  ( 5.572856105055380205, -0.7716597722284452843, 1.553080519226685885 ) ) ;
#111001=CARTESIAN_POINT ( 'NONE',  ( 5.425286103790146974, -1.110369212591550747, -1.340227399214832360 ) ) ;
#111003=CARTESIAN_POINT ( 'NONE',  ( 2.964700083287651999, -2.118976988643240578, -0.8750470330559836363 ) ) ;
#111005=CARTESIAN_POINT ( 'NONE',  ( 2.466542765887615563, 0.09048117372523720170, -1.839033023284454060 ) ) ;
#111008=CARTESIAN_POINT ( 'NONE',  ( 2.309345278970798887, -0.4025885200794159235, 1.780468244869021222 ) ) ;
#111009=CARTESIAN_POINT ( 'NONE',  ( 2.233046271152541618, 2.016033844848092560, 0.04667593304989729741 ) ) ;
#111012=CARTESIAN_POINT ( 'NONE',  ( 4.243269300766455920, -1.833519874744583111, 1.035826785333898270 ) ) ;
#111015=CARTESIAN_POINT ( 'NONE',  ( 2.488806849732328796, 2.007603858877416769, 0.5053560088097220904 ) ) ;
#111018=CARTESIAN_POINT ( 'NONE',  ( 5.092489908381383934, -1.177591669451777179, 1.763244422785560150 ) ) ;
#111019=CARTESIAN_POINT ( 'NONE',  ( 6.410779360540267646, 1.349177972556347971, -1.230185023894624141 ) ) ;
#111026=CARTESIAN_POINT ( 'NONE',  ( 5.976833544478475702, -1.498421880457675215, 1.500811427713820478 ) ) ;
#111027=CARTESIAN_POINT ( 'NONE',  ( 0.9738169395155724661, 2.029595412481857153, -0.5617393031529455127 ) ) ;
#111030=CARTESIAN_POINT ( 'NONE',  ( 6.614093472281312280, 1.855988364702824800, -0.1360997465041282051 ) ) ;
#111038=CARTESIAN_POINT ( 'NONE',  ( 2.471086628630547288, 1.751123931924388089, 0.8847596551376719631 ) ) ;
#111039=CARTESIAN_POINT ( 'NONE',  ( 1.024558638192473170, 1.287004556549703693, -1.736669753874709343 ) ) ;
#111043=CARTESIAN_POINT ( 'NONE',  ( 2.688496201417677867, -0.9952141288376895600, -1.419535560660119655 ) ) ;
#111044=CARTESIAN_POINT ( 'NONE',  ( 2.466429552724667129, 0.08583113499382444278, -1.738331801394930043 ) ) ;
#111047=CARTESIAN_POINT ( 'NONE',  ( 2.354842093047845530, -0.8645933883619570937, 1.821462535208747457 ) ) ;
#111048=CARTESIAN_POINT ( 'NONE',  ( 6.925078400183552141, 7.052169149086129352, 2.642497803771151954 ) ) ;
#111051=CARTESIAN_POINT ( 'NONE',  ( 0.7605432175010603535, -1.429589592961340028, 1.357792370201470256 ) ) ;
#111052=CARTESIAN_POINT ( 'NONE',  ( 5.484596585704371918, -1.208295678440996390, 1.482354609825987435 ) ) ;
#111057=CARTESIAN_POINT ( 'NONE',  ( 1.383469627199322538, 0.1461868815116218467, -2.014428406654201531 ) ) ;
#111059=CARTESIAN_POINT ( 'NONE',  ( 4.700386263483860461, -2.306923794945021200, -0.06181454844297362694 ) ) ;
#111060=CARTESIAN_POINT ( 'NONE',  ( 6.144970055084349347, -0.2864424343173576082, -1.940704187532462210 ) ) ;
#111062=CARTESIAN_POINT ( 'NONE',  ( 3.203904402660478379, 0.7104733393662396868, -1.828749470067204896 ) ) ;
#111066=CARTESIAN_POINT ( 'NONE',  ( 1.165409582065090266, 1.953992404094638591, -0.8159742408818432269 ) ) ;
#111069=CARTESIAN_POINT ( 'NONE',  ( 1.464538624043790316, 0.1369371521719800755, -1.836096087760468398 ) ) ;
#111072=CARTESIAN_POINT ( 'NONE',  ( 2.443736651115399283, -1.977012053918187906, 0.7674769708189137507 ) ) ;
#111077=CARTESIAN_POINT ( 'NONE',  ( 3.567699708620798216, 2.011335548252995764, -0.4479969848151729162 ) ) ;
#111084=CARTESIAN_POINT ( 'NONE',  ( 2.706632988724329891, -0.8634771713065221288, -2.091333714195188431 ) ) ;
#111086=CARTESIAN_POINT ( 'NONE',  ( 2.320317256442219644, -0.6965147209693119956, -1.672536871252501500 ) ) ;
#111087=CARTESIAN_POINT ( 'NONE',  ( 3.362411380332845035, -1.847649188899632255, -0.5059680389012406465 ) ) ;
#111088=CARTESIAN_POINT ( 'NONE',  ( 4.668459276380106715, -0.8822503692092443783, -1.873099891353036561 ) ) ;
#111090=STYLED_ITEM ( 'NONE', ( #18640 ), #164931 ) ;
#111091=CARTESIAN_POINT ( 'NONE',  ( 1.727351915365995083, -1.857048012799527248, 0.6622322079550806428 ) ) ;
#111092=CARTESIAN_POINT ( 'NONE',  ( 6.375613808387889492, 1.842787572768100457, -0.5617375553943514399 ) ) ;
#111093=CARTESIAN_POINT ( 'NONE',  ( 2.887410755087606695, 1.321643875934110479, 1.324118206929347563 ) ) ;
#111094=CARTESIAN_POINT ( 'NONE',  ( 2.315413608375629817, 2.062204878978285194, 1.035883635760030508 ) ) ;
#111096=CARTESIAN_POINT ( 'NONE',  ( 2.840123846975282973, -0.9592540151425684725, 1.594648687322928859 ) ) ;
#111098=CARTESIAN_POINT ( 'NONE',  ( 6.285603487943992818, -1.943538462464271088, 0.6912672899390749359 ) ) ;
#111102=CARTESIAN_POINT ( 'NONE',  ( 6.616252143301227129, -0.9890948110137095517, -1.859226117534703571 ) ) ;
#111104=CARTESIAN_POINT ( 'NONE',  ( 6.362596528949501895, -1.533591692085239266, 1.523617273982772247 ) ) ;
#111105=CARTESIAN_POINT ( 'NONE',  ( 6.305333282589566934, 1.756257216537491450, -0.9971998561906397773 ) ) ;
#111114=CARTESIAN_POINT ( 'NONE',  ( 5.225796113160614986, 0.8128206588041908542, -1.845625551132886288 ) ) ;
#111115=CARTESIAN_POINT ( 'NONE',  ( 2.975796278104340331, -0.8128168404246680634, 1.845627246706407210 ) ) ;
#111120=CARTESIAN_POINT ( 'NONE',  ( 6.245025451202089073, -1.828886558906620774, 1.152162773130911644 ) ) ;
#111125=CARTESIAN_POINT ( 'NONE',  ( 0.1400564425528905699, 0.7337865575636399740, 1.769695213874568962 ) ) ;
#111128=CARTESIAN_POINT ( 'NONE',  ( 1.787319861506628804, 1.187891131197996497, 1.250883549239764081 ) ) ;
#111132=CARTESIAN_POINT ( 'NONE',  ( 0.4734442463095941411, 1.011852719971978232, 1.451749726636430093 ) ) ;
#111134=CARTESIAN_POINT ( 'NONE',  ( 2.104154084628720334, -0.8588668247239000797, 1.820802598171267439 ) ) ;
#111136=CARTESIAN_POINT ( 'NONE',  ( 3.926972183325681875, 2.094573593246536802, 0.6948772193901550098 ) ) ;
#111139=CARTESIAN_POINT ( 'NONE',  ( 5.805598453987085072, -1.706804643700374102, -1.341652511797826186 ) ) ;
#111140=VERTEX_POINT ( 'NONE', #187472 ) ;
#111144=CARTESIAN_POINT ( 'NONE',  ( 3.422626747576805961, -0.8610355553571764631, -1.937992358232228041 ) ) ;
#111145=CARTESIAN_POINT ( 'NONE',  ( 2.724232643812212196, 2.001515029240468646, 0.2440086781289458329 ) ) ;
#111146=CARTESIAN_POINT ( 'NONE',  ( 3.269578866965703767, 0.4354455071775619190, -1.758352452871074334 ) ) ;
#111149=VERTEX_POINT ( 'NONE', #40170 ) ;
#111150=CARTESIAN_POINT ( 'NONE',  ( 0.3209005354254980680, -0.09642172165634513292, 1.868300368337752815 ) ) ;
#111154=CARTESIAN_POINT ( 'NONE',  ( 1.938566325679047297, -1.478098309594473525, 1.218629399928832013 ) ) ;
#111160=CARTESIAN_POINT ( 'NONE',  ( 5.366167234668930419, 1.061923416652654550, 1.882811416686725359 ) ) ;
#111163=CARTESIAN_POINT ( 'NONE',  ( 2.689816194747224110, 2.012238202079220439, -0.6693303307304664385 ) ) ;
#111164=CARTESIAN_POINT ( 'NONE',  ( -0.1296875068448125057, 7.629137130509072939, -2.426516348560475933 ) ) ;
#111166=CARTESIAN_POINT ( 'NONE',  ( 4.552002736099131752, 1.970983365533407694, -0.04540313215006633318 ) ) ;
#111167=CARTESIAN_POINT ( 'NONE',  ( 0.01783784634934187929, -0.5327901187049766119, 1.941387642157591742 ) ) ;
#111169=CARTESIAN_POINT ( 'NONE',  ( 6.087133394233009476, 1.761630753581880704, 1.174362570269470218 ) ) ;
#111171=CARTESIAN_POINT ( 'NONE',  ( 0.5200892513525963157, 2.048054262204841880, -0.3022008342252607838 ) ) ;
#111172=CARTESIAN_POINT ( 'NONE',  ( 2.976435162280165247, -0.1435924003432750840, -1.936700533151126891 ) ) ;
#111176=CARTESIAN_POINT ( 'NONE',  ( 3.714856679239968873, -0.1534820204720024339, 2.085054752100850894 ) ) ;
#111179=CARTESIAN_POINT ( 'NONE',  ( 0.01197859805690624189, -1.811022649853447630, -0.04676520365421397291 ) ) ;
#111180=ORIENTED_EDGE ( 'NONE', *, *, #178838, .T. ) ;
#111181=CARTESIAN_POINT ( 'NONE',  ( 5.865903189996043210, 2.174886565178067777, -0.3735607071253947975 ) ) ;
#111183=CARTESIAN_POINT ( 'NONE',  ( 3.118423654462946892, -1.086285162511631652, -1.920806481261853493 ) ) ;
#111185=CARTESIAN_POINT ( 'NONE',  ( 1.682132150489405564, 0.9841149911452107268, 1.639481845682550398 ) ) ;
#111187=CARTESIAN_POINT ( 'NONE',  ( 5.072747062355987602, 1.430223858385268665, -1.497173470029027120 ) ) ;
#111189=CARTESIAN_POINT ( 'NONE',  ( 2.711983997553393699, -2.138339778157403615, 0.3160903847422363300 ) ) ;
#111190=CARTESIAN_POINT ( 'NONE',  ( 4.775033345069852331, 2.044829088842615494, -0.7888500489584143738 ) ) ;
#111198=CARTESIAN_POINT ( 'NONE',  ( 0.2642963535325442703, 1.880433764241522088, -0.7283817610406128074 ) ) ;
#111202=CARTESIAN_POINT ( 'NONE',  ( 4.539934223682924319, 1.348354173984022575, 1.571082123823979826 ) ) ;
#111203=CARTESIAN_POINT ( 'NONE',  ( 2.912629423498619197, 1.395154039405178903, -1.328744637545350882 ) ) ;
#111204=CARTESIAN_POINT ( 'NONE',  ( 0.1578276607246929530, 1.163290555716024244, 1.646825313395771762 ) ) ;
#111208=CARTESIAN_POINT ( 'NONE',  ( 4.205875300247041260, 0.6677108253347485700, -1.852911535531636789 ) ) ;
#111209=CARTESIAN_POINT ( 'NONE',  ( 0.3225714733509216781, 2.098294765757203528, 0.6321472216322538973 ) ) ;
#111210=CARTESIAN_POINT ( 'NONE',  ( 3.650846181029033133, -1.491723252493650786, 1.052289205326198074 ) ) ;
#111217=CARTESIAN_POINT ( 'NONE',  ( 1.487592393518050837, -1.832424703912252317, -0.1798031890194173865 ) ) ;
#111218=CARTESIAN_POINT ( 'NONE',  ( 5.607686816480834224, 1.527379804643314687, 1.311666717936723403 ) ) ;
#111219=CARTESIAN_POINT ( 'NONE',  ( 0.4921457485732755321, 2.200376924867069484, 0.6639341530902067579 ) ) ;
#111220=CARTESIAN_POINT ( 'NONE',  ( 5.014483083204026137, 0.7471541359172824137, 1.814103259000845458 ) ) ;
#111226=CARTESIAN_POINT ( 'NONE',  ( 1.980132433977495499, -2.051005990652774447, -0.4047881525126810209 ) ) ;
#111227=CARTESIAN_POINT ( 'NONE',  ( 6.420749384593221087, 1.653102913324438816, 0.6326092773807339142 ) ) ;
#111229=CARTESIAN_POINT ( 'NONE',  ( -0.1104750535120251204, 2.866086309876151539, -2.591737134608104842 ) ) ;
#111230=CARTESIAN_POINT ( 'NONE',  ( 1.504977638028012432, -1.727349551440153119, 0.2125612633746311042 ) ) ;
#111234=CARTESIAN_POINT ( 'NONE',  ( 1.347838067242516313, 1.722766431120416941, 0.08778956860019770936 ) ) ;
#111235=CARTESIAN_POINT ( 'NONE',  ( 1.523247060345904291, -2.062048068855956373, 0.7425582295156886170 ) ) ;
#111236=CARTESIAN_POINT ( 'NONE',  ( 3.721466898765386500, -0.1629207441977159332, 2.200919931280575170 ) ) ;
#111238=CARTESIAN_POINT ( 'NONE',  ( 2.149520630032801805, 1.890536112741852959, -1.067247343769129442 ) ) ;
#111239=CARTESIAN_POINT ( 'NONE',  ( 0.7678472254676466102, 0.8974085622692473674, 1.589837017038860045 ) ) ;
#111240=CARTESIAN_POINT ( 'NONE',  ( 3.942653875399897423, -1.566338124119817987, 1.424821879184964946 ) ) ;
#111241=CARTESIAN_POINT ( 'NONE',  ( 6.539320575229250920, 3.702490941164796379, 2.411252750440337156 ) ) ;
#111243=CARTESIAN_POINT ( 'NONE',  ( 3.966586032518903959, -2.139059804502403850, -0.8247178969851276520 ) ) ;
#111245=CARTESIAN_POINT ( 'NONE',  ( 0.07755575628181145265, 0.6932613274447991802, -2.271134039238668301 ) ) ;
#111249=CARTESIAN_POINT ( 'NONE',  ( 6.199871938995108245, 1.529590366309235172, 1.610960538716522006 ) ) ;
#111255=CARTESIAN_POINT ( 'NONE',  ( 4.430314669760617718, -1.560499787156752971, -1.277043788614096176 ) ) ;
#111257=CARTESIAN_POINT ( 'NONE',  ( 2.430602512062591369, -1.272252061732727091, 1.623331442124707591 ) ) ;
#111262=CARTESIAN_POINT ( 'NONE',  ( 5.525378525699438548, -1.388074942811763357, -1.695776126864618316 ) ) ;
#111263=CARTESIAN_POINT ( 'NONE',  ( 2.250625165576759290, 1.976955744075848065, -0.3961026872240576702 ) ) ;
#111264=CARTESIAN_POINT ( 'NONE',  ( 2.577489280727011778, -0.9446877197298314544, 1.580272903027237774 ) ) ;
#111268=CARTESIAN_POINT ( 'NONE',  ( 5.649374308873757577, -1.440485763676568443, -1.121356984487072328 ) ) ;
#111269=CARTESIAN_POINT ( 'NONE',  ( 6.029922689959810178, -1.701949372586025744, 1.081063231324945528 ) ) ;
#111271=CARTESIAN_POINT ( 'NONE',  ( 5.208033936170274103, -2.252144374781993363, 0.2163938657309023850 ) ) ;
#111273=CARTESIAN_POINT ( 'NONE',  ( 1.014449334229026611, -0.9484566428747326361, -1.880489036503508959 ) ) ;
#111282=CARTESIAN_POINT ( 'NONE',  ( 1.951583061186522583, -1.892041120407188304, 0.9578705467366486204 ) ) ;
#111283=CARTESIAN_POINT ( 'NONE',  ( 2.953626239309721679, -1.957189270898977762, 1.050815160798105552 ) ) ;
#111287=CARTESIAN_POINT ( 'NONE',  ( 3.912515228517557286, 0.7039278570535618673, 1.831416474553926310 ) ) ;
#111296=CARTESIAN_POINT ( 'NONE',  ( 3.639029512587122372, 2.014767915268770082, 0.6618469929612482705 ) ) ;
#111298=CARTESIAN_POINT ( 'NONE',  ( 4.768538688506021472, -1.414568798902924307, 1.634688457493836289 ) ) ;
#111299=CARTESIAN_POINT ( 'NONE',  ( 3.825598141381767903, 0.9817388958630569595, -1.557492293685861284 ) ) ;
#111303=CARTESIAN_POINT ( 'NONE',  ( 5.806559702419027857, 1.537982464610265332, 0.8144831216923865691 ) ) ;
#111307=CARTESIAN_POINT ( 'NONE',  ( 3.432649856329002880, 2.108609624295390006, 0.4754391814798044069 ) ) ;
#111308=CARTESIAN_POINT ( 'NONE',  ( 5.483749906247235906, 1.861732415968733401, 0.7741956105717237024 ) ) ;
#111310=CARTESIAN_POINT ( 'NONE',  ( 2.518638242371186386, 1.412657066830936392, -1.636333507658905173 ) ) ;
#111311=CARTESIAN_POINT ( 'NONE',  ( 3.233620971007169942, -1.321289716990686980, -1.463211747571713461 ) ) ;
#111312=CARTESIAN_POINT ( 'NONE',  ( 0.2225716830646235489, 2.098996182288978218, 0.6302611576235671587 ) ) ;
#111313=CARTESIAN_POINT ( 'NONE',  ( 4.792492878049551486, 1.612589784423448025, -1.081918670939057137 ) ) ;
#111322=CARTESIAN_POINT ( 'NONE',  ( 2.221956617217385244, -2.140583525707707935, 0.5359638216213060691 ) ) ;
#111325=CARTESIAN_POINT ( 'NONE',  ( 6.385602409055195494, -1.848352663145738095, 0.6577735930803210174 ) ) ;
#111329=CARTESIAN_POINT ( 'NONE',  ( 0.07479286986305369589, 0.2526433113205875935, -1.890777245541554574 ) ) ;
#111330=CARTESIAN_POINT ( 'NONE',  ( 4.857273802806507668, 1.820629801081237620, -0.2732171615176108848 ) ) ;
#111335=CARTESIAN_POINT ( 'NONE',  ( 5.801066647469003357, -0.3129311994157328303, -2.097281602037828208 ) ) ;
#111338=CARTESIAN_POINT ( 'NONE',  ( 6.081337768261708909, 1.905808788339557802, -0.7845383490599889820 ) ) ;
#111340=CARTESIAN_POINT ( 'NONE',  ( 1.820531350174507512, -1.319122485308525716, 1.313071031887176998 ) ) ;
#111341=CARTESIAN_POINT ( 'NONE',  ( 3.227900028218867234, 1.797025815167479390, 0.4004103908350764573 ) ) ;
#111347=CARTESIAN_POINT ( 'NONE',  ( 3.879664727460280904, 2.078262106501146622, -0.7427522710690689367 ) ) ;
#111348=CARTESIAN_POINT ( 'NONE',  ( 5.554102117330329769, 2.260170762534471578, -0.1031424389980051676 ) ) ;
#111350=CARTESIAN_POINT ( 'NONE',  ( 5.590068458682615038, 1.086043493620889144, 1.449778898616445488 ) ) ;
#111351=CARTESIAN_POINT ( 'NONE',  ( 6.280494692369203769, -0.5183099952858164494, -1.844178102243919870 ) ) ;
#111353=CARTESIAN_POINT ( 'NONE',  ( 5.647288160985431738, -1.475499438119257878, -1.149758287351684949 ) ) ;
#111354=CARTESIAN_POINT ( 'NONE',  ( 6.059226159983991167, -1.612925389857391645, 1.026989893868179404 ) ) ;
#111357=CARTESIAN_POINT ( 'NONE',  ( 0.5318453760667535279, 0.9654296485097979552, -1.602142582367314549 ) ) ;
#111358=CARTESIAN_POINT ( 'NONE',  ( 1.217982839071569012, 0.9896824804975331569, -1.756856037137774162 ) ) ;
#111360=CARTESIAN_POINT ( 'NONE',  ( 3.791714260247856849, 1.525338472785308097, 1.452445685796518227 ) ) ;
#111365=CARTESIAN_POINT ( 'NONE',  ( 3.076430314242516229, 0.9118049750012310328, 1.802366903320629765 ) ) ;
#111369=CARTESIAN_POINT ( 'NONE',  ( 3.233815116076131257, -1.449111151313630996, -1.604113057997895053 ) ) ;
#111375=CARTESIAN_POINT ( 'NONE',  ( 1.205810543264747681, -1.711434635494583967, -1.335908126413299923 ) ) ;
#111380=CARTESIAN_POINT ( 'NONE',  ( 1.822082775007987543, 1.258534617508931586, -1.793986466278547853 ) ) ;
#111381=CARTESIAN_POINT ( 'NONE',  ( 6.883263157960391787, 1.253787318140922480, 2.167784446185747171 ) ) ;
#111382=CARTESIAN_POINT ( 'NONE',  ( 2.044175283654376951, 0.8654258166664110519, -2.090645895884978955 ) ) ;
#111390=CARTESIAN_POINT ( 'NONE',  ( 4.358513420383302694, -1.312205524322278549, 1.187683162289454142 ) ) ;
#111392=CARTESIAN_POINT ( 'NONE',  ( 0.7453164640696362531, -1.806240154289909139, 1.082582905463305378 ) ) ;
#111395=CARTESIAN_POINT ( 'NONE',  ( 6.116814581292481456, 0.2004514801264325186, 2.006445662566976651 ) ) ;
#111398=CARTESIAN_POINT ( 'NONE',  ( 3.291731440620565330, -0.7593194595177065187, 1.709801165022284408 ) ) ;
#111399=CARTESIAN_POINT ( 'NONE',  ( 3.696198088285786998, 0.9351842759567146057, -1.847102243037239910 ) ) ;
#111405=CARTESIAN_POINT ( 'NONE',  ( 6.192270064542984898, -2.150811787302907785, -0.2168040374768212541 ) ) ;
#111407=CARTESIAN_POINT ( 'NONE',  ( 3.473055881322492322, 1.772541284497713976, 0.8411618914155660764 ) ) ;
#111408=CARTESIAN_POINT ( 'NONE',  ( 0.4739822347885510601, 1.752760637641921360, 0.9961516927870716076 ) ) ;
#111412=CARTESIAN_POINT ( 'NONE',  ( 0.7724589312842686795, -1.759198622581410021, -0.6360808729843556719 ) ) ;
#111414=CARTESIAN_POINT ( 'NONE',  ( 3.058842833410029272, 0.4931317667464900634, 1.951740033431844434 ) ) ;
#111416=CARTESIAN_POINT ( 'NONE',  ( 1.827892122045454260, 0.8069190765337170834, -1.957623834376254646 ) ) ;
#111418=CARTESIAN_POINT ( 'NONE',  ( 3.930184216435282707, 1.147649575447948100, 1.722966636330313550 ) ) ;
#111420=CARTESIAN_POINT ( 'NONE',  ( 0.5036076356924833464, -2.080315145378656805, 0.2087293992604210557 ) ) ;
#111422=CARTESIAN_POINT ( 'NONE',  ( 5.877927443470423619, 1.089437568142386015, 1.464738158297604453 ) ) ;
#111427=CARTESIAN_POINT ( 'NONE',  ( 5.948300505803369553, 2.203960110721484789, 0.1139900122707343255 ) ) ;
#111429=CARTESIAN_POINT ( 'NONE',  ( 4.793567869993575314, 1.782951692925707654, -0.6917526515820491273 ) ) ;
#111440=CARTESIAN_POINT ( 'NONE',  ( 4.358574879328508622, -1.387578095181252413, 1.254630796652965730 ) ) ;
#111447=CARTESIAN_POINT ( 'NONE',  ( 2.324999910687207461, -1.798643183423669134, -0.8027048682860711271 ) ) ;
#111448=CARTESIAN_POINT ( 'NONE',  ( 3.374625213368151133, -0.3961236654455925765, -1.976952669325626299 ) ) ;
#111451=CARTESIAN_POINT ( 'NONE',  ( 6.827182134110194589, 2.412578537245218424, 2.569476350730160785 ) ) ;
#111453=CARTESIAN_POINT ( 'NONE',  ( 3.697391623616069101, -0.6365095100077067247, 2.096977347260075231 ) ) ;
#111455=CARTESIAN_POINT ( 'NONE',  ( 2.010648722831087198, 1.429088002864507212, -1.291968487218410511 ) ) ;
#111457=CARTESIAN_POINT ( 'NONE',  ( 0.2333540202161506205, 0.2466631755442013352, -2.080888922837381916 ) ) ;
#111464=CARTESIAN_POINT ( 'NONE',  ( 4.704558828624370470, 1.604442792107749760, 0.9031527321438773681 ) ) ;
#111465=CARTESIAN_POINT ( 'NONE',  ( 1.506495127224609876, -2.003582159550582276, -0.1952931609562995052 ) ) ;
#111466=CARTESIAN_POINT ( 'NONE',  ( 3.849189735728062001, -1.136876111170448178, 1.997481460179703960 ) ) ;
#111467=CARTESIAN_POINT ( 'NONE',  ( -0.1290005225502398323, 0.2247172878383028038, -2.207197350255707402 ) ) ;
#111468=CARTESIAN_POINT ( 'NONE',  ( 2.377597188713850507, -1.806433865756534640, 0.4466691629738496760 ) ) ;
#111471=CARTESIAN_POINT ( 'NONE',  ( 5.554919272666569263, 0.3793472168572444292, 1.874222000232607765 ) ) ;
#111474=CARTESIAN_POINT ( 'NONE',  ( 4.774988821994140764, 1.950233014344885385, -0.7539837885136254636 ) ) ;
#111475=CARTESIAN_POINT ( 'NONE',  ( 3.063207453921251489, 0.2760179531714930246, -1.850060308400132358 ) ) ;
#111478=CARTESIAN_POINT ( 'NONE',  ( 5.602095939246814815, -1.725068444894608310, 0.006287883723511687381 ) ) ;
#111480=CARTESIAN_POINT ( 'NONE',  ( 1.037308000539336694, -1.367553460919969543, 1.066146521862390673 ) ) ;
#111484=CARTESIAN_POINT ( 'NONE',  ( 5.752828983992735346, -0.5200050086436918129, -2.107789999013423454 ) ) ;
#111485=CARTESIAN_POINT ( 'NONE',  ( 4.301258635363705451, 1.467727663998198429, 1.085573330547324744 ) ) ;
#111486=CARTESIAN_POINT ( 'NONE',  ( 2.219515905360454067, 0.3404028402014187549, -1.931851785523025944 ) ) ;
#111487=CARTESIAN_POINT ( 'NONE',  ( 0.01740989766754827417, -1.933669582450600499, 0.8627405663345076858 ) ) ;
#111492=CARTESIAN_POINT ( 'NONE',  ( 2.666775373343560407, 0.7166976873529752323, 1.995817185486338019 ) ) ;
#111497=CARTESIAN_POINT ( 'NONE',  ( 1.006788857090525013, 0.5974033793386055446, 1.982218910981221827 ) ) ;
#111500=CARTESIAN_POINT ( 'NONE',  ( 3.405137934272496558, -0.4347481476216079055, -2.178183672434565565 ) ) ;
#111502=CARTESIAN_POINT ( 'NONE',  ( 0.3526649539562948243, 0.2173941373411722999, -2.288394520000771148 ) ) ;
#111504=CARTESIAN_POINT ( 'NONE',  ( 6.121949867982135807, 2.033011618171334245, -0.3470327977990442792 ) ) ;
#111507=CARTESIAN_POINT ( 'NONE',  ( 0.2329586101569892376, 6.948071080078905837, -2.440796105365902857 ) ) ;
#111508=CARTESIAN_POINT ( 'NONE',  ( 5.108874002337426390, -0.2646564886703614006, 1.822002613180016883 ) ) ;
#111511=CARTESIAN_POINT ( 'NONE',  ( 3.170621359714973941, -1.593115903276512757, -0.6614109595024783017 ) ) ;
#111512=CARTESIAN_POINT ( 'NONE',  ( 0.7961116948485976730, -0.9110139862544311962, -1.799120828532501326 ) ) ;
#111513=CARTESIAN_POINT ( 'NONE',  ( 3.094664012895144367, -0.4461126415513679833, 2.254854857015383462 ) ) ;
#111515=CARTESIAN_POINT ( 'NONE',  ( 2.935161367736533133, 0.2740405928264351143, 2.245665650516134093 ) ) ;
#111516=CARTESIAN_POINT ( 'NONE',  ( 5.549480973255512595, -1.659368771798474196, -1.296820645603852018 ) ) ;
#111518=CARTESIAN_POINT ( 'NONE',  ( 4.129968326689526847, 0.9481555284369269643, -1.494110371635357648 ) ) ;
#111521=CARTESIAN_POINT ( 'NONE',  ( 6.251568577072929678, 2.286574220100371591, -0.1642174239346057829 ) ) ;
#111522=CARTESIAN_POINT ( 'NONE',  ( 4.242028835625204053, 0.4931972713904734795, 1.773778790588397491 ) ) ;
#111527=CARTESIAN_POINT ( 'NONE',  ( 5.050807487124363782, -1.850163549229045579, -1.174163402404400092 ) ) ;
#111532=CARTESIAN_POINT ( 'NONE',  ( 3.193887106011963350, -0.7802878698427909709, 1.761581285093082982 ) ) ;
#111535=CARTESIAN_POINT ( 'NONE',  ( 0.2994921435493704820, -0.2801620449621230469, -2.203647339609093869 ) ) ;
#111543=CARTESIAN_POINT ( 'NONE',  ( 2.507021497916587460, -1.721230695331811722, 0.2570161617474544524 ) ) ;
#111545=CARTESIAN_POINT ( 'NONE',  ( 0.5374593765826127800, 1.831924746014142791, -0.7026076897959919743 ) ) ;
#111547=CARTESIAN_POINT ( 'NONE',  ( 5.946190753372003535, 2.158995856162956084, 0.1107517376499680406 ) ) ;
#111550=CARTESIAN_POINT ( 'NONE',  ( 5.225516498768126183, -2.053876642077703707, 0.6744380372525200507 ) ) ;
#111551=CARTESIAN_POINT ( 'NONE',  ( -0.2104748580754166321, -0.006608320950486632102, -2.103482951484026309 ) ) ;
#111554=CARTESIAN_POINT ( 'NONE',  ( 0.7900579835180140398, -1.855660487967484951, -0.2351621623290362506 ) ) ;
#111555=CARTESIAN_POINT ( 'NONE',  ( 5.747320757027973848, -1.692087196126054849, -0.3772414270737846631 ) ) ;
#111557=CARTESIAN_POINT ( 'NONE',  ( 2.876726420669137863, -0.1638259704515396820, -2.185508879517850112 ) ) ;
#111558=CARTESIAN_POINT ( 'NONE',  ( 2.995503060082918889, 1.979820613015465858, -1.185208598768563881 ) ) ;
#111560=CARTESIAN_POINT ( 'NONE',  ( 5.905559377550752664, -0.5051061836833131702, 1.997775138168448761 ) ) ;
#111561=CARTESIAN_POINT ( 'NONE',  ( 1.148265734048327769, -1.531264750074516234, 1.194210492925862344 ) ) ;
#111565=CARTESIAN_POINT ( 'NONE',  ( 4.113620189327307664, 1.705085180707970771, 1.260635662952174663 ) ) ;
#111567=CARTESIAN_POINT ( 'NONE',  ( 2.268204128460939550, 1.842446992372799963, -0.8197738674571022344 ) ) ;
#111569=CARTESIAN_POINT ( 'NONE',  ( 5.983472182158235952, 2.041168445429199618, -0.8392293214988936212 ) ) ;
#111572=DIRECTION ( 'NONE',  ( -1.000000000000000000, 0.000000000000000000, 0.000000000000000000 ) ) ;
#111575=CARTESIAN_POINT ( 'NONE',  ( 6.825078400183577365, 2.023440267519378999, 2.448151054272352578 ) ) ;
#111578=CARTESIAN_POINT ( 'NONE',  ( 4.786040499707863383, -0.9732044846940243188, 1.816634495032407814 ) ) ;
#111583=CARTESIAN_POINT ( 'NONE',  ( 4.072919328976184694, -1.495020084728536203, 1.358112258667160344 ) ) ;
#111588=CARTESIAN_POINT ( 'NONE',  ( 2.711851390082948399, -2.038666671984638690, 0.3009093235433103475 ) ) ;
#111589=CARTESIAN_POINT ( 'NONE',  ( 3.111954093273407551, 0.05229746705895028935, 2.015912966248374349 ) ) ;
#111595=ORIENTED_EDGE ( 'NONE', *, *, #144753, .F. ) ;
#111596=CARTESIAN_POINT ( 'NONE',  ( 3.409529676982744562, 0.4871283372531940992, 1.956261718130556382 ) ) ;
#111597=CARTESIAN_POINT ( 'NONE',  ( 2.906014618889842360, 1.333239036598636407, -1.269987479889053139 ) ) ;
#111599=CARTESIAN_POINT ( 'NONE',  ( 6.516270054225981490, -1.036149114087565382, -1.948532232987249424 ) ) ;
#111601=CARTESIAN_POINT ( 'NONE',  ( 2.372553944209778720, -1.331880425775422205, 1.702409713178254069 ) ) ;
#111603=CARTESIAN_POINT ( 'NONE',  ( 2.706789001878449508, -1.702045039646230107, -1.544681222897727357 ) ) ;
#111606=CARTESIAN_POINT ( 'NONE',  ( 1.322894217037654085, -0.04941562205608432401, 1.870173573632450958 ) ) ;
#111608=CARTESIAN_POINT ( 'NONE',  ( 5.735224789204648843, -1.782488891340678894, 0.8425237689327728097 ) ) ;
#111612=CARTESIAN_POINT ( 'NONE',  ( 0.6455096168876961471, -1.890800792967793686, 1.137844069391671820 ) ) ;
#111613=CARTESIAN_POINT ( 'NONE',  ( 6.109843426155951107, 0.6047356833836557977, -1.980059631771100781 ) ) ;
#111616=CARTESIAN_POINT ( 'NONE',  ( 6.539320575229255361, 7.051987793746187450, 2.801414728815339039 ) ) ;
#111617=CARTESIAN_POINT ( 'NONE',  ( 5.313337694394675736, -0.2901137614541632881, 1.949896409304814116 ) ) ;
#111618=CARTESIAN_POINT ( 'NONE',  ( 6.345964425358009642, -1.322526734765665513, -1.526637064097993157 ) ) ;
#111620=CARTESIAN_POINT ( 'NONE',  ( 4.741030679083562127, 0.3911436318500530751, 2.274166950501448348 ) ) ;
#111621=CARTESIAN_POINT ( 'NONE',  ( 1.832955167792608364, -1.957230265441430417, -0.6508311760726466222 ) ) ;
#111628=CARTESIAN_POINT ( 'NONE',  ( 3.807220332926362083, -1.777014928589750076, 1.247251757893479640 ) ) ;
#111630=CARTESIAN_POINT ( 'NONE',  ( 4.388128076750056117, -0.4078595375654435751, -1.795341762384855544 ) ) ;
#111633=CARTESIAN_POINT ( 'NONE',  ( 6.720655732516647163, 2.082321177337285167, 2.135279995619132620 ) ) ;
#111634=CARTESIAN_POINT ( 'NONE',  ( 5.425378541715013547, -1.389685604419872655, -1.694579525865948844 ) ) ;
#111636=CARTESIAN_POINT ( 'NONE',  ( 5.717715967963762580, -2.208827357630326560, 0.4893477075747532101 ) ) ;
#111642=CARTESIAN_POINT ( 'NONE',  ( 0.9008075156715513732, 1.443549170786810443, 1.023676300919857507 ) ) ;
#111643=CARTESIAN_POINT ( 'NONE',  ( 4.793612393603923216, 1.877549684267119101, -0.7266104139797191497 ) ) ;
#111645=CARTESIAN_POINT ( 'NONE',  ( 4.190527447551747109, -2.082725220463335081, -0.3111483248238402499 ) ) ;
#111646=CARTESIAN_POINT ( 'NONE',  ( 1.985809494836645817, -1.915157380443854418, 0.04907906824581054206 ) ) ;
#111648=CARTESIAN_POINT ( 'NONE',  ( 3.244544899158372520, -1.939951241085198896, -0.3392403660903812734 ) ) ;
#111649=CARTESIAN_POINT ( 'NONE',  ( 5.080334495226257907, 0.9990293545295618749, 1.755361416599170443 ) ) ;
#111650=CARTESIAN_POINT ( 'NONE',  ( 2.026040307571222332, 1.079255042350239391, -1.527726335390042767 ) ) ;
#111651=CARTESIAN_POINT ( 'NONE',  ( 5.426277463695272196, 1.022757762066462961, -1.388784613272223689 ) ) ;
#111652=CARTESIAN_POINT ( 'NONE',  ( 1.845825534506392085, -1.251752223804462272, -1.445855903880132631 ) ) ;
#111654=CARTESIAN_POINT ( 'NONE',  ( 1.577102763248950046, -2.096353118739826993, -0.6898709473643764856 ) ) ;
#111665=CARTESIAN_POINT ( 'NONE',  ( 0.5552397518338060278, 1.722184604005328357, -1.148819969904082861 ) ) ;
#111670=CARTESIAN_POINT ( 'NONE',  ( 6.428397668822618094, -0.9990526908794925554, -1.870407359624715937 ) ) ;
#111673=CARTESIAN_POINT ( 'NONE',  ( 0.07479286986305544449, 6.948552162806721277, -2.450557996216149892 ) ) ;
#111675=CARTESIAN_POINT ( 'NONE',  ( 4.253279712585047001, -1.993766238088546361, -0.2985801555873274227 ) ) ;
#111676=CARTESIAN_POINT ( 'NONE',  ( 4.329236433732988942, -1.484621416154695117, -1.210779873830228670 ) ) ;
#111678=CARTESIAN_POINT ( 'NONE',  ( 2.384552795368581890, -0.3778730364575392797, -2.158588602542845347 ) ) ;
#111681=CARTESIAN_POINT ( 'NONE',  ( 5.010025764882303001, -0.7205479882510434919, 1.880027049715059073 ) ) ;
#111684=CARTESIAN_POINT ( 'NONE',  ( 5.730101960677154160, 2.114805460001396575, 0.1033778851832044821 ) ) ;
#111686=CARTESIAN_POINT ( 'NONE',  ( 3.878531184313998015, -0.2068018975109634505, -2.080507369234054771 ) ) ;
#111688=CARTESIAN_POINT ( 'NONE',  ( 1.447837905203141373, 1.722567860661971206, 0.08979103728979326293 ) ) ;
#111690=CARTESIAN_POINT ( 'NONE',  ( 4.781546299372162245, 0.2051969522943071500, -2.110614603223801122 ) ) ;
#111700=CARTESIAN_POINT ( 'NONE',  ( 1.787489318380721448, 1.733277665728020001, -0.5263807565755849183 ) ) ;
#111705=CARTESIAN_POINT ( 'NONE',  ( 3.123486050149349769, -0.3508677868355335461, 1.776971544703136452 ) ) ;
#111706=CARTESIAN_POINT ( 'NONE',  ( 6.639320575229236354, 1.260096212659385984, 2.110683211146132443 ) ) ;
#111710=CARTESIAN_POINT ( 'NONE',  ( 4.369486748645814878, -0.3193033414996570007, 1.833288415851072273 ) ) ;
#111711=CARTESIAN_POINT ( 'NONE',  ( 1.159628707424670280, 1.142309718407741093, 1.537566464135895261 ) ) ;
#111712=CARTESIAN_POINT ( 'NONE',  ( 6.704134009050578769, -1.925936059460537697, 0.04828832120675958378 ) ) ;
#111719=CARTESIAN_POINT ( 'NONE',  ( 6.315293006042116630, -1.687366247620238457, -1.015419155273014740 ) ) ;
#111722=CARTESIAN_POINT ( 'NONE',  ( 0.3575176574102476579, 2.067590324638542310, -0.3087094068163088179 ) ) ;
#111723=CARTESIAN_POINT ( 'NONE',  ( 4.840804290916858932, 0.3290424097142484738, 1.897927756555679801 ) ) ;
#111725=CARTESIAN_POINT ( 'NONE',  ( 1.201864610381056853, -1.825762228264395048, -0.004348209057210283834 ) ) ;
#111726=CARTESIAN_POINT ( 'NONE',  ( 1.981372325807278623, -0.1102420082176903682, -2.204251428397439483 ) ) ;
#111728=CARTESIAN_POINT ( 'NONE',  ( 0.2637284958507991606, 0.5978344860198721022, -1.816641584731902626 ) ) ;
#111730=CARTESIAN_POINT ( 'NONE',  ( 0.3441184698094986727, -0.9315698024882634876, 1.735327799219071210 ) ) ;
#111731=CARTESIAN_POINT ( 'NONE',  ( 2.718228044968384882, 1.829540209339441503, 0.6518440813585175686 ) ) ;
#111733=ORIENTED_EDGE ( 'NONE', *, *, #191590, .T. ) ;
#111734=CARTESIAN_POINT ( 'NONE',  ( 1.352888501574830205, -0.9090079681693465918, 1.799646022210943386 ) ) ;
#111736=CARTESIAN_POINT ( 'NONE',  ( 5.278104476702146108, -0.9935453584285673934, -1.573305019461817444 ) ) ;
#111742=CARTESIAN_POINT ( 'NONE',  ( 1.663894474538109236, 1.130263417742288112, 1.877492182091732076 ) ) ;
#111746=CARTESIAN_POINT ( 'NONE',  ( 3.264084022359412529, 0.8216391472936382945, 1.630427331384458833 ) ) ;
#111753=CARTESIAN_POINT ( 'NONE',  ( 0.8559318490590170914, 1.924348548886562815, -0.09362981192203097269 ) ) ;
#111754=CARTESIAN_POINT ( 'NONE',  ( 5.752778578519474273, -0.4731148833870613690, -1.903749215227706015 ) ) ;
#111758=CARTESIAN_POINT ( 'NONE',  ( 5.179302069984247581, 1.471482994053765925, 1.624232740060495228 ) ) ;
#111760=CARTESIAN_POINT ( 'NONE',  ( 4.082924941702062327, 1.964217522864346810, 0.6541895251909736198 ) ) ;
#111764=CARTESIAN_POINT ( 'NONE',  ( 4.535913861531776448, -1.846855032230051208, 1.368429651993019025 ) ) ;
#111771=CARTESIAN_POINT ( 'NONE',  ( 3.609261671491706736, -1.913043583297647565, 0.3329670706836064809 ) ) ;
#111776=CARTESIAN_POINT ( 'NONE',  ( 4.904515063324526025, -1.898637117948184017, -0.2282459111111398431 ) ) ;
#111778=CARTESIAN_POINT ( 'NONE',  ( 5.807552366672524613, -0.4147409827905921831, 1.674012740457442305 ) ) ;
#111779=CARTESIAN_POINT ( 'NONE',  ( 4.294157853547872605, -0.8666056138363427142, -1.820986994602633802 ) ) ;
#111781=CARTESIAN_POINT ( 'NONE',  ( 2.280145854635793334, 1.358931147977986420, 1.738775483816151768 ) ) ;
#111784=CARTESIAN_POINT ( 'NONE',  ( 1.834041477103361739, 2.068079971995392619, 0.3053845110000241170 ) ) ;
#111785=CARTESIAN_POINT ( 'NONE',  ( 6.731742716130249882, -1.158518921844574834, -1.337957499386055682 ) ) ;
#111786=CARTESIAN_POINT ( 'NONE',  ( 5.414685466650038137, -1.281359335986744341, -1.556910257834144051 ) ) ;
#111788=CARTESIAN_POINT ( 'NONE',  ( 2.924086828919622238, 1.272802903806929953, -1.906236438263966271 ) ) ;
#111789=CARTESIAN_POINT ( 'NONE',  ( 1.622608716997505418, -1.639457832600412113, 0.5842430463761526527 ) ) ;
#111792=CARTESIAN_POINT ( 'NONE',  ( 0.8601780606121096628, -0.6315397308106798224, 1.614934579331471998 ) ) ;
#111795=CARTESIAN_POINT ( 'NONE',  ( 1.082764339582122481, 1.293380948865870073, -1.743738868014677035 ) ) ;
#111796=CARTESIAN_POINT ( 'NONE',  ( 1.921111612355221654, -1.799121770747251547, 0.9110121207814986244 ) ) ;
#111797=CARTESIAN_POINT ( 'NONE',  ( 3.781250000000002665, 0.7852924748301846058, 1.895863743164001081 ) ) ;
#111799=CARTESIAN_POINT ( 'NONE',  ( 0.1824732010112985747, -1.867734037610004449, -0.4713708115406111676 ) ) ;
#111801=CARTESIAN_POINT ( 'NONE',  ( 3.885193193976806292, -2.073655658835142024, -0.7971110592776513570 ) ) ;
#111808=CARTESIAN_POINT ( 'NONE',  ( 5.776847720190436242, 1.604795045139913556, -0.6741588622883755155 ) ) ;
#111809=CARTESIAN_POINT ( 'NONE',  ( 3.771884902471400292, -1.933230903833718539, 0.3329965046865584477 ) ) ;
#111813=CARTESIAN_POINT ( 'NONE',  ( 4.868612525405347391, -1.482742447731852709, 1.708856814797095725 ) ) ;
#111816=AXIS2_PLACEMENT_3D ( 'NONE', #63200, #148722, #127228 ) ;
#111817=CARTESIAN_POINT ( 'NONE',  ( 1.803259461591859347, -1.743671650923955374, 1.101644963814436329 ) ) ;
#111822=CARTESIAN_POINT ( 'NONE',  ( 3.954256261376987602, 0.6707706173689140794, 1.746330409709492937 ) ) ;
#111823=CARTESIAN_POINT ( 'NONE',  ( 2.426026400502009128, -1.286032909179233297, -1.163566193670103832 ) ) ;
#111824=CARTESIAN_POINT ( 'NONE',  ( 6.110890996357365879, -0.2699588104537915534, 2.174781792473476472 ) ) ;
#111825=CARTESIAN_POINT ( 'NONE',  ( 0.4291286860223576527, 2.112415399404877547, 0.6383354507134838540 ) ) ;
#111826=CARTESIAN_POINT ( 'NONE',  ( 4.487301133948972343, 1.932317252032596633, -0.9692046190768679459 ) ) ;
#111827=CARTESIAN_POINT ( 'NONE',  ( 4.962805208576138938, 0.1888075513713943498, -1.932747541012701964 ) ) ;
#111830=CARTESIAN_POINT ( 'NONE',  ( 6.450466390465378730, 0.5869013949594548141, 1.776180802621520005 ) ) ;
#111833=CARTESIAN_POINT ( 'NONE',  ( 0.08834397731360790762, 1.226219587655341448, 1.729930300845914815 ) ) ;
#111836=CARTESIAN_POINT ( 'NONE',  ( 5.608046130584797950, -0.04667949407829303371, 2.016033753796213635 ) ) ;
#111840=CARTESIAN_POINT ( 'NONE',  ( 3.000428103051573814, -0.5303778429210231904, -1.746945217264872507 ) ) ;
#111841=CARTESIAN_POINT ( 'NONE',  ( 2.538337413235943973, 1.040872164564849767, -1.945885072647230318 ) ) ;
#111846=CARTESIAN_POINT ( 'NONE',  ( 1.494405286683021306, -1.076835855708496936, 1.708581493997686662 ) ) ;
#111847=CARTESIAN_POINT ( 'NONE',  ( 1.348456458401224412, 1.042098076042829780, -1.846665823592225975 ) ) ;
#111850=CARTESIAN_POINT ( 'NONE',  ( 2.043593076603223757, 1.278923709890807503, 1.352104710524345554 ) ) ;
#111852=CARTESIAN_POINT ( 'NONE',  ( 5.893449486436047380, 1.558864155394885875, 1.348126965055055804 ) ) ;
#111853=CARTESIAN_POINT ( 'NONE',  ( 6.065077313367789102, -1.076319894221990259, 1.704936797084610101 ) ) ;
#111854=ORIENTED_EDGE ( 'NONE', *, *, #91211, .F. ) ;
#111857=CARTESIAN_POINT ( 'NONE',  ( 4.494645072041675071, -0.4025399330690944133, -1.780595394402582077 ) ) ;
#111861=CARTESIAN_POINT ( 'NONE',  ( 6.538435458278026857, 1.930121188254026787, -0.5825698962980339068 ) ) ;
#111862=CARTESIAN_POINT ( 'NONE',  ( 5.314338895140062746, 1.702579029208791450, 0.7012131971957940024 ) ) ;
#111863=CARTESIAN_POINT ( 'NONE',  ( 0.07680821025394035662, 2.052785608010514018, -2.228496998325917744 ) ) ;
#111864=CARTESIAN_POINT ( 'NONE',  ( 4.600386337014011673, -2.307077041318765342, -0.05981084109947519545 ) ) ;
#111866=CARTESIAN_POINT ( 'NONE',  ( 5.817692603468245238, -2.110333850551704415, 0.4673072906974176655 ) ) ;
#111868=CARTESIAN_POINT ( 'NONE',  ( 1.452572125225624955, -1.666495805118956897, -0.9969474394922008820 ) ) ;
#111870=CARTESIAN_POINT ( 'NONE',  ( 4.657739267062822819, -0.4975208956916782332, -2.243777209869437517 ) ) ;
#111873=CARTESIAN_POINT ( 'NONE',  ( 4.961713530105988923, 1.850188064717460223, -0.2750520410098392654 ) ) ;
#111875=CARTESIAN_POINT ( 'NONE',  ( 1.951281838316549777, -1.706683157587106425, 0.8630329916254894096 ) ) ;
#111878=CARTESIAN_POINT ( 'NONE',  ( 3.985166894971280183, -0.2153072539897090687, -2.196357064762343825 ) ) ;
#111879=CARTESIAN_POINT ( 'NONE',  ( 6.883263157960333167, 4.698395927207251077, 2.408847447403542841 ) ) ;
#111884=CARTESIAN_POINT ( 'NONE',  ( 1.423050710548888542, -0.05258038247234024520, 1.970828066091591557 ) ) ;
#111885=CARTESIAN_POINT ( 'NONE',  ( 1.202667248822903989, -2.307758714249080079, 0.002725711325006137473 ) ) ;
#111886=CARTESIAN_POINT ( 'NONE',  ( 2.822649888979886335, -1.354935067541668259, 1.419045635080482093 ) ) ;
#111888=CARTESIAN_POINT ( 'NONE',  ( 4.891499300893256574, -1.887858789894794054, 0.8311416006015391877 ) ) ;
#111895=CARTESIAN_POINT ( 'NONE',  ( 1.112457285868488910, 2.168641027238225938, -0.1045176843600063021 ) ) ;
#111900=CARTESIAN_POINT ( 'NONE',  ( 2.336979506217982117, -1.672866993182718698, 0.8370366242000035761 ) ) ;
#111901=CARTESIAN_POINT ( 'NONE',  ( 6.679002375395027613, -0.09866081283815136826, -2.159460157733564145 ) ) ;
#111902=CARTESIAN_POINT ( 'NONE',  ( 0.07755575628183573877, 1.996246338214379801, -2.602582295553407032 ) ) ;
#111903=SURFACE_STYLE_USAGE ( .BOTH. , #62020 ) ;
#111906=CARTESIAN_POINT ( 'NONE',  ( 2.402860538037488780, -0.3286879766849961082, -1.883663324302800257 ) ) ;
#111908=CARTESIAN_POINT ( 'NONE',  ( 3.889309559433737906, 1.281865973830035754, 1.220554204183731173 ) ) ;
#111909=CARTESIAN_POINT ( 'NONE',  ( 2.314975094136799694, 1.534822137071165660, -1.140449143091977646 ) ) ;
#111913=CARTESIAN_POINT ( 'NONE',  ( 5.642171489992906075, 0.7808347329528000369, 1.749441798972359408 ) ) ;
#111915=CARTESIAN_POINT ( 'NONE',  ( 6.391062254520311292, 0.1913994329204322109, 1.960204640275018395 ) ) ;
#111918=CARTESIAN_POINT ( 'NONE',  ( 4.979306205331720747, 1.745251617482036943, -0.6738592683939447214 ) ) ;
#111919=CARTESIAN_POINT ( 'NONE',  ( 1.681982107312831154, -0.9779208310041755947, 1.541497997293653555 ) ) ;
#111921=CARTESIAN_POINT ( 'NONE',  ( 4.688207069967821106, -1.042061291317699423, 1.945354640606362873 ) ) ;
#111924=CARTESIAN_POINT ( 'NONE',  ( 1.891156856157749866, 0.2001100897341882012, 2.052929594394680812 ) ) ;
#111931=CARTESIAN_POINT ( 'NONE',  ( 5.512195382060368409, 2.068158883198469855, -0.09793725168850964113 ) ) ;
#111933=CARTESIAN_POINT ( 'NONE',  ( 2.565889408427945995, 2.120439650033152379, -0.4189318973958494619 ) ) ;
#111935=CARTESIAN_POINT ( 'NONE',  ( 3.369790118769320664, 0.4886731666619185677, -1.959541563195909220 ) ) ;
#111936=CARTESIAN_POINT ( 'NONE',  ( 6.620655732516651071, 1.241313378043694238, 2.288056600130850882 ) ) ;
#111942=CARTESIAN_POINT ( 'NONE',  ( 1.428923106112218067, -1.700960256238340573, 1.082842518468102089 ) ) ;
#111943=CARTESIAN_POINT ( 'NONE',  ( 6.497619750234602698, -2.191128968173004843, 0.05151875470104508997 ) ) ;
#111945=CARTESIAN_POINT ( 'NONE',  ( 4.482611839828003930, -1.244964735940889522, 1.451779576051547282 ) ) ;
#111949=CARTESIAN_POINT ( 'NONE',  ( 2.249625261780491936, 1.976952429928409805, -0.3961248688731587309 ) ) ;
#111952=CARTESIAN_POINT ( 'NONE',  ( 4.981344092214620822, 1.608381032133517019, -0.6233497484429885160 ) ) ;
#111957=CARTESIAN_POINT ( 'NONE',  ( 1.481394567461959300, -0.05474761849930119550, 2.069712792878583230 ) ) ;
#111959=CARTESIAN_POINT ( 'NONE',  ( 6.760220206081136496, -2.069995208266177666, 0.04663682477341199450 ) ) ;
#111961=CARTESIAN_POINT ( 'NONE',  ( 4.705596528438695358, 1.345619282010660500, 1.212945642518966416 ) ) ;
#111964=CARTESIAN_POINT ( 'NONE',  ( 6.305303276254960565, 1.572402219250234268, -0.8993151100721032964 ) ) ;
#111967=CARTESIAN_POINT ( 'NONE',  ( 3.152458698460915532, -1.659165413833121550, 1.431739491984926671 ) ) ;
#111970=CARTESIAN_POINT ( 'NONE',  ( 0.9066075625437097774, 0.5660373911110065936, 1.878450800843839419 ) ) ;
#111973=CARTESIAN_POINT ( 'NONE',  ( 4.464398116780900594, -1.859039872360370937, -0.4615888831297955686 ) ) ;
#111981=CARTESIAN_POINT ( 'NONE',  ( 2.395597313961893349, 1.670541196947441742, 1.371929806955954234 ) ) ;
#111984=CARTESIAN_POINT ( 'NONE',  ( 1.817148636465517164, -0.2269042555285011864, 1.811363274943120771 ) ) ;
#111985=CARTESIAN_POINT ( 'NONE',  ( 0.0004480315400831600455, -0.9938866557669153723, 1.873244595478529728 ) ) ;
#111986=CARTESIAN_POINT ( 'NONE',  ( 4.137589658204786858, -1.258905094989382967, -1.322318538811013466 ) ) ;
#111990=CARTESIAN_POINT ( 'NONE',  ( 3.350016042381760872, -0.8005406348832925234, 1.799716665148870964 ) ) ;
#111992=CARTESIAN_POINT ( 'NONE',  ( 6.550339418841141459, -1.498220820903242601, 1.235316290203094081 ) ) ;
#111996=CARTESIAN_POINT ( 'NONE',  ( 5.308877466510794285, -0.5174029350529658622, -2.056363676157816123 ) ) ;
#111998=CARTESIAN_POINT ( 'NONE',  ( 3.106014470790594562, -0.7728303494197851231, 1.749331318715248385 ) ) ;
#112003=CARTESIAN_POINT ( 'NONE',  ( 4.758451920691616266, 2.007841679651333422, 0.1459793341078066131 ) ) ;
#112005=CARTESIAN_POINT ( 'NONE',  ( 6.358013415952256331, 1.820405254634300363, -0.1396899356524081148 ) ) ;
#112006=CARTESIAN_POINT ( 'NONE',  ( 1.012269475826784060, 2.068064858651061932, -0.09981174449213289779 ) ) ;
#112010=CARTESIAN_POINT ( 'NONE',  ( 6.385618529757402406, 1.291587659170100766, 1.353439767483602285 ) ) ;
#112015=PRESENTATION_STYLE_ASSIGNMENT (( #27482 ) ) ;
#112017=CARTESIAN_POINT ( 'NONE',  ( 4.219182763733449804, 1.701723821253621427, 0.3326838626578206282 ) ) ;
#112019=CARTESIAN_POINT ( 'NONE',  ( 1.534126288888465917, 1.230018689141991306, 1.665114864061276734 ) ) ;
#112020=CARTESIAN_POINT ( 'NONE',  ( 2.847379581703746609, 0.3079039886237054935, -2.094596350150164987 ) ) ;
#112024=CARTESIAN_POINT ( 'NONE',  ( 0.9363041846261275225, -1.098647377812447923, 1.634312829373037568 ) ) ;
#112029=CARTESIAN_POINT ( 'NONE',  ( 3.135043019019596144, -2.021410203770683367, 1.080917199049796107 ) ) ;
#112030=CARTESIAN_POINT ( 'NONE',  ( 0.8908993799596062191, 1.611356928563783208, -0.8583080905386344384 ) ) ;
#112031=CARTESIAN_POINT ( 'NONE',  ( 3.498220628606643956, -0.9384276995785534314, 1.666209768436441419 ) ) ;
#112036=CARTESIAN_POINT ( 'NONE',  ( 2.285404485177256362, 0.09469097253389560653, -2.011075120970148511 ) ) ;
#112037=CARTESIAN_POINT ( 'NONE',  ( 2.641395077882053410, 1.795597516233004232, -0.7905247784146393064 ) ) ;
#112042=CARTESIAN_POINT ( 'NONE',  ( 4.822261998019022222, 2.000437409348213347, 0.6074620046824655839 ) ) ;
#112043=CARTESIAN_POINT ( 'NONE',  ( 3.414700241993049001, 1.599697164860384380, 0.7574896018788888075 ) ) ;
#112046=CARTESIAN_POINT ( 'NONE',  ( 6.632792736454030447, -2.050728487082712270, 1.024446431767987331 ) ) ;
#112047=CARTESIAN_POINT ( 'NONE',  ( 4.945099085969404840, 0.5415675326034079529, -1.653987846916603610 ) ) ;
#112049=CARTESIAN_POINT ( 'NONE',  ( 4.147546876296400065, -0.1688817038796013026, -1.725555368340276008 ) ) ;
#112051=CARTESIAN_POINT ( 'NONE',  ( 4.756392321286846858, -2.170573799849393470, -0.05792142139850359195 ) ) ;
#112053=CARTESIAN_POINT ( 'NONE',  ( 5.630092293170263495, 2.014432788975322630, 0.09412139267171715229 ) ) ;
#112054=CARTESIAN_POINT ( 'NONE',  ( 5.375000000000002665, 2.052068128417941395, -3.059081846666863488E-13 ) ) ;
#112056=CARTESIAN_POINT ( 'NONE',  ( 3.258729403965909821, -1.459781800624770032, 1.257100956980856443 ) ) ;
#112058=CARTESIAN_POINT ( 'NONE',  ( 6.521772982575972044, -0.4919494239215887466, 2.174507958589830370 ) ) ;
#112060=CARTESIAN_POINT ( 'NONE',  ( 6.883263157960369583, 7.629137130509070275, 2.546189081643289942 ) ) ;
#112063=CARTESIAN_POINT ( 'NONE',  ( 3.088771134150660735, -1.321542420002120855, 1.785288483701172657 ) ) ;
#112068=CARTESIAN_POINT ( 'NONE',  ( 0.5103889644224939293, -1.913802852362625151, 0.6352017490645140985 ) ) ;
#112070=CARTESIAN_POINT ( 'NONE',  ( 5.617653825673187384, 0.4058615334493093085, -2.022196393678155957 ) ) ;
#112076=CARTESIAN_POINT ( 'NONE',  ( 6.731728662460410462, -1.222180481402233898, -1.416172877279207931 ) ) ;
#112077=CARTESIAN_POINT ( 'NONE',  ( 5.660742353926829118, 1.040242247344788762, 1.387327330804826619 ) ) ;
#112078=CARTESIAN_POINT ( 'NONE',  ( 5.108843383178156117, -0.2480618215125965365, 1.722539690991312877 ) ) ;
#112079=CARTESIAN_POINT ( 'NONE',  ( 3.298623631688667235, 1.806097335442503393, -1.411605728516792002 ) ) ;
#112081=CARTESIAN_POINT ( 'NONE',  ( 0.9723034553027898319, -0.04304006056080753040, -1.840805954149108858 ) ) ;
#112085=CARTESIAN_POINT ( 'NONE',  ( 1.571042225754931465, 0.1381101175703668971, -1.820421783975199048 ) ) ;
#112086=CARTESIAN_POINT ( 'NONE',  ( 3.059220373557011818, -1.198860207862334049, 1.621182619130703051 ) ) ;
#112087=CARTESIAN_POINT ( 'NONE',  ( 0.9201892814816802213, 1.302667801055312990, -1.762099327409505811 ) ) ;
#112089=CARTESIAN_POINT ( 'NONE',  ( 4.647555896809190124, -1.626162052001564717, -1.338137134695188468 ) ) ;
#112092=CARTESIAN_POINT ( 'NONE',  ( 1.785682506433339478, -1.950172559450613852, 0.6955597780969878796 ) ) ;
#112095=CARTESIAN_POINT ( 'NONE',  ( 4.811248821985151913, 1.762591750878339081, -1.178568461981117643 ) ) ;
#112096=CARTESIAN_POINT ( 'NONE',  ( 0.1176308287326099516, -1.889623933557175617, 0.3742946393059803367 ) ) ;
#112103=CARTESIAN_POINT ( 'NONE',  ( -0.05205951232617207075, -2.027416208471942038, 0.9083432681902519068 ) ) ;
#112104=CARTESIAN_POINT ( 'NONE',  ( 1.008971530259877403, 1.594680585555088292, -1.375637761830387440 ) ) ;
#112107=CARTESIAN_POINT ( 'NONE',  ( 5.401151054173385369, -1.597185415876556158, 0.9547389691558528790 ) ) ;
#112114=CARTESIAN_POINT ( 'NONE',  ( 2.014041202081144011, 1.956828179156915315, -0.1411808619533050091 ) ) ;
#112115=CARTESIAN_POINT ( 'NONE',  ( 1.094844843509492183, -0.5259716649698794599, -2.096624219460433647 ) ) ;
#112119=CARTESIAN_POINT ( 'NONE',  ( 2.547823072707461112, 1.587006686370129316, -0.6987220570618419835 ) ) ;
#112120=CARTESIAN_POINT ( 'NONE',  ( 2.659766076405935653, -1.200293992427956757, 1.260412480424155435 ) ) ;
#112123=CARTESIAN_POINT ( 'NONE',  ( 0.7376574009502723239, -1.897405874265755354, -0.6818954202830117550 ) ) ;
#112124=CARTESIAN_POINT ( 'NONE',  ( 6.825078400183550720, 0.5766433668599518780, 2.097246334241170906 ) ) ;
#112127=CARTESIAN_POINT ( 'NONE',  ( 1.358210660854881402, 0.7971155783631430625, 1.803302576489584697 ) ) ;
#112129=CARTESIAN_POINT ( 'NONE',  ( 6.011958326525193463, -0.6379227081053112647, 1.803018720113582773 ) ) ;
#112134=CARTESIAN_POINT ( 'NONE',  ( 0.8561247329088355063, 0.8163843618401511737, -1.847503835822896789 ) ) ;
#112136=CARTESIAN_POINT ( 'NONE',  ( 4.524672722398297431, 1.423327999681742062, -1.816260527432728811 ) ) ;
#112137=CARTESIAN_POINT ( 'NONE',  ( 5.775826483351648832, -1.914393393812302113, 0.4282712878391075062 ) ) ;
#112138=CARTESIAN_POINT ( 'NONE',  ( 2.166782468979636000, 1.457124453068344039, -1.313723524322525815 ) ) ;
#112142=CARTESIAN_POINT ( 'NONE',  ( 1.411481693167576434, -1.991701369327549154, 0.7188087792022596068 ) ) ;
#112146=CARTESIAN_POINT ( 'NONE',  ( 0.9547317490294878750, 0.3612830171869831353, -1.805165878648997912 ) ) ;
#112150=CARTESIAN_POINT ( 'NONE',  ( 2.777707764728345907, 0.3069055913166895966, -2.098134212408508059 ) ) ;
#112154=CARTESIAN_POINT ( 'NONE',  ( 3.198563317047153465, -0.5950029230564283234, -1.973035911149529698 ) ) ;
#112156=PLANE ( 'NONE',  #86226 ) ;
#112158=CARTESIAN_POINT ( 'NONE',  ( 0.07775346131142897577, 0.6705917366217004627, -2.369298483346020667 ) ) ;
#112160=CARTESIAN_POINT ( 'NONE',  ( 0.1005910224048736229, -2.206496634663042133, -0.04943112074598519229 ) ) ;
#112161=CARTESIAN_POINT ( 'NONE',  ( 2.513255990918183524, 2.019876067157271748, 1.019300669498679479 ) ) ;
#112163=CARTESIAN_POINT ( 'NONE',  ( 2.337905319157699502, -1.045887089798164915, -1.478944033197209462 ) ) ;
#112164=CARTESIAN_POINT ( 'NONE',  ( 2.061615604755413500, 1.182011660234401962, 1.507458768284040129 ) ) ;
#112165=CARTESIAN_POINT ( 'NONE',  ( 3.051297593704501043, 1.777051743073382761, -1.062048545217339823 ) ) ;
#112167=CARTESIAN_POINT ( 'NONE',  ( 1.920718329235811872, 1.838843090712917405, 0.7113003943867537426 ) ) ;
#112168=CARTESIAN_POINT ( 'NONE',  ( 6.604134034941783860, -1.926004669841055339, 0.05029594667986003048 ) ) ;
#112169=CARTESIAN_POINT ( 'NONE',  ( 2.430351462470367707, 1.813921419787648315, 0.4566771774890953095 ) ) ;
#112170=CARTESIAN_POINT ( 'NONE',  ( 1.629934303081633340, -2.171740791250169611, 0.7807429155501348639 ) ) ;
#112172=CARTESIAN_POINT ( 'NONE',  ( 2.435812105726247623, 1.142245297582837882, 1.469210208790121763 ) ) ;
#112174=CARTESIAN_POINT ( 'NONE',  ( 5.881316448893678661, -0.05433346072863074611, 2.062130925675903725 ) ) ;
#112179=CARTESIAN_POINT ( 'NONE',  ( 6.159223736743516753, -1.804415119744419149, -1.085654967431331164 ) ) ;
#112181=CARTESIAN_POINT ( 'NONE',  ( 6.221977808853903724, -1.195094089922192016, -1.800988070004491792 ) ) ;
#112182=CARTESIAN_POINT ( 'NONE',  ( 5.988927272769587695, -1.918439801222410201, -0.6316595152702029203 ) ) ;
#112186=CARTESIAN_POINT ( 'NONE',  ( 6.825078400183548055, 3.702925343214446663, 2.370119418288775925 ) ) ;
#112189=CARTESIAN_POINT ( 'NONE',  ( 5.120327457147888950, 1.987497208294352280, 0.3399611521368098854 ) ) ;
#112194=CARTESIAN_POINT ( 'NONE',  ( 5.700121470611750674, -2.161883445634639411, -0.004416275431240455560 ) ) ;
#112198=CARTESIAN_POINT ( 'NONE',  ( 0.2982578006338062471, 1.320465477219048722, -1.388022668363431356 ) ) ;
#112200=CARTESIAN_POINT ( 'NONE',  ( 6.539320575229251808, 7.629137130509035636, 2.803262396134009737 ) ) ;
#112201=CARTESIAN_POINT ( 'NONE',  ( 1.980655567072008072, -0.08268669962357808045, -1.723028944404185303 ) ) ;
#112205=CARTESIAN_POINT ( 'NONE',  ( 6.749288224047839790, -1.502610544577225982, -1.113804566994440970 ) ) ;
#112206=CARTESIAN_POINT ( 'NONE',  ( 0.3814940398445298420, 0.1953205766255173559, -2.003579427208526553 ) ) ;
#112208=CARTESIAN_POINT ( 'NONE',  ( 3.592985822966657583, -0.4282699184722462693, -2.164648485658649868 ) ) ;
#112209=CARTESIAN_POINT ( 'NONE',  ( 5.454042025912737124, -0.7881617977381920603, 2.023119649181570168 ) ) ;
#112212=CARTESIAN_POINT ( 'NONE',  ( 3.756581929197760683, 2.110411401290826383, 0.2062832702387565331 ) ) ;
#112213=CARTESIAN_POINT ( 'NONE',  ( 2.478138860811992306, -2.011206848916185397, -0.1455134472309257965 ) ) ;
#112214=CARTESIAN_POINT ( 'NONE',  ( 1.933590839544163664, -1.756428034162808904, 0.4429697619106263695 ) ) ;
#112219=CARTESIAN_POINT ( 'NONE',  ( 0.6724591444495706671, -1.759989063064151038, -0.6342292696241008665 ) ) ;
#112223=CARTESIAN_POINT ( 'NONE',  ( 1.797909001537282503, -0.9065369449853509787, -1.687681949719927577 ) ) ;
#112229=CARTESIAN_POINT ( 'NONE',  ( 5.717692609583751029, -2.109997883074541392, 0.4692839721026839661 ) ) ;
#112232=CARTESIAN_POINT ( 'NONE',  ( 2.953504815971871533, -1.868289524550557523, 1.003269902519102086 ) ) ;
#112235=CARTESIAN_POINT ( 'NONE',  ( 3.989495051124877456, 1.425666444934305499, 1.361731899605103768 ) ) ;
#112236=CARTESIAN_POINT ( 'NONE',  ( 5.361546783204238942, -1.511448857895525855, -1.171587532507123441 ) ) ;
#112239=CARTESIAN_POINT ( 'NONE',  ( 0.7485892145711986467, -2.054541080789675789, -0.2550698046258002005 ) ) ;
#112240=CARTESIAN_POINT ( 'NONE',  ( 2.765492612253204641, 1.039303555060458351, 1.640259502831205918 ) ) ;
#112244=CARTESIAN_POINT ( 'NONE',  ( 2.748082359423655419, 0.7051493092682534769, 1.968258087557398284 ) ) ;
#112247=CARTESIAN_POINT ( 'NONE',  ( 0.9085206565882588681, -0.4392767353821840914, -1.757246876086359988 ) ) ;
#112249=CARTESIAN_POINT ( 'NONE',  ( 4.037865812933420173, -1.521084700717803884, -1.599171214764223636 ) ) ;
#112250=CARTESIAN_POINT ( 'NONE',  ( 3.469938103458301448, 2.153457811087633011, -0.4814610123115290463 ) ) ;
#112253=CARTESIAN_POINT ( 'NONE',  ( 2.244649938279310142, 1.855272219182309668, 0.4629769397326845004 ) ) ;
#112255=CARTESIAN_POINT ( 'NONE',  ( 4.018080225218490398, 2.055083638104511223, -0.2504045000601487492 ) ) ;
#112257=CARTESIAN_POINT ( 'NONE',  ( 2.641676655999642076, -1.601130012699041982, -1.452526871000489495 ) ) ;
#112258=CARTESIAN_POINT ( 'NONE',  ( 5.161759341795384870, 1.079763445194487970, 1.907048802792680631 ) ) ;
#112266=CARTESIAN_POINT ( 'NONE',  ( 0.7916389524552720491, 1.525042296397002284, -1.319230309296010928 ) ) ;
#112268=CARTESIAN_POINT ( 'NONE',  ( 4.434477146351770926, -1.196200190851111733, 1.689492296227593116 ) ) ;
#112269=CARTESIAN_POINT ( 'NONE',  ( 3.387250987759330645, 1.741285041988534621, -0.8245012487104221854 ) ) ;
#112270=CARTESIAN_POINT ( 'NONE',  ( 6.204719021523306566, 1.975628225290576356, 0.7617523325972180848 ) ) ;
#112273=CARTESIAN_POINT ( 'NONE',  ( 3.450015926008513478, -0.8023341227383492535, 1.798807795796441678 ) ) ;
#112274=CARTESIAN_POINT ( 'NONE',  ( 5.789115795541526666, 1.732349586671273922, 1.501262892615047750 ) ) ;
#112275=CARTESIAN_POINT ( 'NONE',  ( 4.564971734551386717, -1.632036996880025903, -0.8184370388232551363 ) ) ;
#112282=CARTESIAN_POINT ( 'NONE',  ( 1.065666191918061445, -1.167978014494171823, 1.423405568861766168 ) ) ;
#112283=CARTESIAN_POINT ( 'NONE',  ( 5.097907127711155617, 1.355137859109056819, 1.488956579698009763 ) ) ;
#112284=CARTESIAN_POINT ( 'NONE',  ( 1.423680875022467873, 0.9325134783980688624, 2.100857314651356500 ) ) ;
#112285=CARTESIAN_POINT ( 'NONE',  ( 5.137533780887935997, 1.831872034461759835, -0.7024582609849658876 ) ) ;
#112290=CARTESIAN_POINT ( 'NONE',  ( 1.470382607095675143, -1.986325758040393685, -0.6527442681472686026 ) ) ;
#112291=CARTESIAN_POINT ( 'NONE',  ( 6.772329494929559601, -1.084452473627237845, 1.399072979944876449 ) ) ;
#112293=CARTESIAN_POINT ( 'NONE',  ( -0.1102773484823937195, 1.312263477441493187, -2.452793124480449283 ) ) ;
#112294=CARTESIAN_POINT ( 'NONE',  ( 1.311604768886602157, 1.169564267535606605, -1.289085965974474668 ) ) ;
#112298=CARTESIAN_POINT ( 'NONE',  ( 1.945521746005531627, 0.6619316864419527713, -1.593019548489343240 ) ) ;
#112299=CARTESIAN_POINT ( 'NONE',  ( 1.699035084177059174, 1.824418957995146195, 1.213967346723361596 ) ) ;
#112301=CARTESIAN_POINT ( 'NONE',  ( -0.05262932013434371004, -1.547529252455181581, -0.7825623337873451879 ) ) ;
#112302=CARTESIAN_POINT ( 'NONE',  ( 4.020313978404310262, -1.133593497508533110, -1.893353337301090233 ) ) ;
#112304=CARTESIAN_POINT ( 'NONE',  ( 0.8136159317379263456, -1.833160233796997218, -1.162963494187698510 ) ) ;
#112305=CARTESIAN_POINT ( 'NONE',  ( 0.1877650043593872553, -0.8638833939697135866, 1.608357707688967242 ) ) ;
#112306=CARTESIAN_POINT ( 'NONE',  ( 3.098929814713128561, 1.916056983672033587, 0.9012583305440853287 ) ) ;
#112308=CARTESIAN_POINT ( 'NONE',  ( 6.639320575229258559, 7.629137130509072051, 2.496737603865983424 ) ) ;
#112310=CARTESIAN_POINT ( 'NONE',  ( 3.298623631688667235, 1.806097335442503393, -1.411605728516792002 ) ) ;
#112314=CARTESIAN_POINT ( 'NONE',  ( 5.707756388377941192, 1.680692789272177468, 1.452518960167401341 ) ) ;
#112320=CARTESIAN_POINT ( 'NONE',  ( 4.500625067706437221, -1.976956227568788638, 0.3961002554062897918 ) ) ;
#112322=CARTESIAN_POINT ( 'NONE',  ( 2.536046341495324707, 1.265347977242038402, 1.628790341535201636 ) ) ;
#112328=CARTESIAN_POINT ( 'NONE',  ( 5.068408068084750973, -2.062719301109996461, -0.7404068969242217912 ) ) ;
#112329=CARTESIAN_POINT ( 'NONE',  ( 2.567029916978436077, -1.034165006014248211, 1.730866473406714068 ) ) ;
#112330=CARTESIAN_POINT ( 'NONE',  ( 1.856743374925871715, 0.3135980649527739250, -1.814175028193690808 ) ) ;
#112335=CARTESIAN_POINT ( 'NONE',  ( 5.280226139177822908, -1.012770463184736736, 1.518683248463777113 ) ) ;
#112336=CARTESIAN_POINT ( 'NONE',  ( 6.012342310302175363, -1.897698807000438359, 0.6819931642896917001 ) ) ;
#112338=CARTESIAN_POINT ( 'NONE',  ( 5.664971525351325532, -2.042639428312309935, -0.9732368426803981176 ) ) ;
#112340=CARTESIAN_POINT ( 'NONE',  ( 1.278104297367024467, 1.255928009607910623, 1.690453460462447044 ) ) ;
#112350=CARTESIAN_POINT ( 'NONE',  ( 3.023905552101690208, -0.4295200811062405699, 2.179336035515607950 ) ) ;
#112354=CARTESIAN_POINT ( 'NONE',  ( 3.666413850373055006, -0.7928392042928497085, -1.794698522912529182 ) ) ;
#112360=CARTESIAN_POINT ( 'NONE',  ( 2.338272602237463360, -1.224740070204191289, -1.730971256048131401 ) ) ;
#112362=CARTESIAN_POINT ( 'NONE',  ( 4.276362541559985075, -1.246951984143488623, 1.765614359104182629 ) ) ;
#112363=CARTESIAN_POINT ( 'NONE',  ( 2.313779677144182312, 1.201330555204615180, -1.395457044143719072 ) ) ;
#112367=CARTESIAN_POINT ( 'NONE',  ( 5.929613673486688441, 0.8517357041802063877, -1.517590187452934281 ) ) ;
#112368=CARTESIAN_POINT ( 'NONE',  ( 6.727182134110222478, 0.005875948494733079785, 1.810970247402940547 ) ) ;
#112371=CARTESIAN_POINT ( 'NONE',  ( 3.573254463033649131, 0.05508235185803719847, -2.161170636208443963 ) ) ;
#112372=CARTESIAN_POINT ( 'NONE',  ( 4.569685373303983944, 1.560260980002409870, -1.276848140101802365 ) ) ;
#112374=CARTESIAN_POINT ( 'NONE',  ( 2.184651956524386041, -2.119909832212972578, -0.4221607449544013679 ) ) ;
#112375=CARTESIAN_POINT ( 'NONE',  ( 2.635955087654485940, 0.9327151613215716175, -1.736774642614127284 ) ) ;
#112377=CARTESIAN_POINT ( 'NONE',  ( 4.616706917144582256, -0.09184519841067168011, 1.939997386343417896 ) ) ;
#112386=CARTESIAN_POINT ( 'NONE',  ( 1.518904762042364354, 1.481482853740143657, -1.635709697223409531 ) ) ;
#112388=CARTESIAN_POINT ( 'NONE',  ( 5.840667439708360220, -1.913134005453724251, -0.4332900713753874977 ) ) ;
#112392=CARTESIAN_POINT ( 'NONE',  ( 0.1749903794560566384, 0.2522965209616668814, -1.990827758811020809 ) ) ;
#112393=CARTESIAN_POINT ( 'NONE',  ( 3.872867692073681756, 1.733033312621637068, -0.6219614626309655225 ) ) ;
#112399=CARTESIAN_POINT ( 'NONE',  ( 6.222909436229170588, 1.570324008046734221, -1.425282903188800798 ) ) ;
#112403=CARTESIAN_POINT ( 'NONE',  ( 6.837187436585446143, -1.842956594435873896, 0.9222261209423606720 ) ) ;
#112405=CARTESIAN_POINT ( 'NONE',  ( 1.609564491371988426, 0.5446964562696824386, -1.779540750359181800 ) ) ;
#112406=CARTESIAN_POINT ( 'NONE',  ( 3.860763913883006992, 0.2215400755124704024, -1.827792592973469743 ) ) ;
#112411=CARTESIAN_POINT ( 'NONE',  ( 3.282038605231399231, 1.400092287458438722, 1.705885466304429166 ) ) ;
#112412=CARTESIAN_POINT ( 'NONE',  ( 6.432949606591497727, 0.2122621168692347127, 2.252429721023613496 ) ) ;
#112414=CARTESIAN_POINT ( 'NONE',  ( 5.836161222118039227, -1.013825144121174526, -1.501122385605196952 ) ) ;
#112415=CARTESIAN_POINT ( 'NONE',  ( 6.503150280507321135, -0.1381757461387123076, 1.884094533524976578 ) ) ;
#112417=CARTESIAN_POINT ( 'NONE',  ( 6.139502064137229986, -1.356240498024411600, -1.288626068300227523 ) ) ;
#112418=CARTESIAN_POINT ( 'NONE',  ( 6.162542460989155479, -0.6707643300355231597, -1.736165932305182125 ) ) ;
#112421=CARTESIAN_POINT ( 'NONE',  ( 6.702016551492756768, -1.769339222028827319, 0.04870252428828580893 ) ) ;
#112422=CARTESIAN_POINT ( 'NONE',  ( 1.200408080392855181, 1.350732740426639822, -1.497504596960941958 ) ) ;
#112424=CARTESIAN_POINT ( 'NONE',  ( 3.088603512095712045, -2.074978072712420296, -0.3595722787458465186 ) ) ;
#112429=CARTESIAN_POINT ( 'NONE',  ( 2.584245202030683419, 1.084020786718616680, 1.704056320703779992 ) ) ;
#112432=CARTESIAN_POINT ( 'NONE',  ( 3.128364550451453230, 1.203671540783244565, -1.795256801906938815 ) ) ;
#112437=CARTESIAN_POINT ( 'NONE',  ( 0.9421113726552653445, 1.458074577165750396, 1.608915699534870569 ) ) ;
#112441=CARTESIAN_POINT ( 'NONE',  ( 2.630644284709309666, 0.2711686948545319886, 2.174668582101045633 ) ) ;
#112443=CARTESIAN_POINT ( 'NONE',  ( 2.712116605023757288, -2.238012884330255581, 0.3312714459411686962 ) ) ;
#112450=CARTESIAN_POINT ( 'NONE',  ( 3.163107763524728444, 0.2631224511941733790, -1.749944513356870734 ) ) ;
#112452=CARTESIAN_POINT ( 'NONE',  ( 6.387735258934439386, 1.517164627179751646, 1.602757196154185770 ) ) ;
#112456=CARTESIAN_POINT ( 'NONE',  ( 6.046499952770106212, -1.423952032562772807, 1.427948417171531759 ) ) ;
#112459=CARTESIAN_POINT ( 'NONE',  ( 3.713615009860570471, -1.843089489661838831, 0.3189824552965599413 ) ) ;
#112461=CARTESIAN_POINT ( 'NONE',  ( 2.834898843300116766, -1.979765732921334731, -0.6052725283285932401 ) ) ;
#112469=CARTESIAN_POINT ( 'NONE',  ( 3.350005920730843911, -0.7974703105717847462, 1.792663495558038056 ) ) ;
#112470=CARTESIAN_POINT ( 'NONE',  ( 0.7024996975148189993, -1.423740904080775138, -1.427721366232127753 ) ) ;
#112475=CARTESIAN_POINT ( 'NONE',  ( 1.106479506788549116, 1.420293003395491693, -1.217391549091076275 ) ) ;
#112477=CARTESIAN_POINT ( 'NONE',  ( 3.357684704777043283, -1.527344908821237635, -1.311707263431096671 ) ) ;
#112479=CARTESIAN_POINT ( 'NONE',  ( 2.056417290815291121, -1.299724242359597826, 1.671285701813587821 ) ) ;
#112481=CARTESIAN_POINT ( 'NONE',  ( 3.719242722441223226, -1.824546119899137731, -0.9785211796824041519 ) ) ;
#112483=CARTESIAN_POINT ( 'NONE',  ( 5.542948256250054051, -1.647469546829454234, -1.286982348046373570 ) ) ;
#112485=CARTESIAN_POINT ( 'NONE',  ( 4.717693524642503355, -1.790169364231732674, 0.3569235582787863570 ) ) ;
#112489=CARTESIAN_POINT ( 'NONE',  ( 6.809632187368197087, -0.4906261968062891055, 2.159508175712351541 ) ) ;
#112491=CARTESIAN_POINT ( 'NONE',  ( 5.320932177894995618, 1.445329238430465013, -1.252218921613167169 ) ) ;
#112497=CARTESIAN_POINT ( 'NONE',  ( 0.7316835000789992938, 1.813914744281470925, 0.3150931809976220133 ) ) ;
#112500=CARTESIAN_POINT ( 'NONE',  ( 5.026551685794929725, 1.789549103570491351, 0.5443708928771497924 ) ) ;
#112501=CARTESIAN_POINT ( 'NONE',  ( -0.02319159430949970999, 4.096340798889516854, -2.366022381217198767 ) ) ;
#112507=CARTESIAN_POINT ( 'NONE',  ( 1.551539110526085619, 1.487754399324931365, 1.290523904849065095 ) ) ;
#112508=CARTESIAN_POINT ( 'NONE',  ( 3.814077502958601595, 1.076299547611740293, -1.704950967544152984 ) ) ;
#112511=CARTESIAN_POINT ( 'NONE',  ( 3.662233025353780480, -1.472007171213615351, 1.623636439255560227 ) ) ;
#112522=CARTESIAN_POINT ( 'NONE',  ( 4.897927690869709139, -0.6253142351902387652, -1.731941863025769246 ) ) ;
#112523=CARTESIAN_POINT ( 'NONE',  ( 2.068995670861985658, -1.554830924100785161, 1.278664071131753843 ) ) ;
#112524=CARTESIAN_POINT ( 'NONE',  ( 4.657739267062822819, -0.4975208956916782332, -2.243777209869437517 ) ) ;
#112525=CARTESIAN_POINT ( 'NONE',  ( -0.02919842301646497981, 2.009414862388910983, -2.487882213790572283 ) ) ;
#112526=CARTESIAN_POINT ( 'NONE',  ( 2.623689330893996363, 1.826062842344724269, -0.3576783775682371158 ) ) ;
#112529=CARTESIAN_POINT ( 'NONE',  ( 5.256085721135645095, 0.7693902824621422498, -1.750971482026221437 ) ) ;
#112533=CARTESIAN_POINT ( 'NONE',  ( 5.284749326355624888, 1.843379893440146633, -0.9865243283948360586 ) ) ;
#112534=CARTESIAN_POINT ( 'NONE',  ( 3.572993900519233712, 0.04689164532409998559, -1.870237235490713079 ) ) ;
#112536=CARTESIAN_POINT ( 'NONE',  ( 5.407694413872749628, -0.8332299576223768378, -1.642021276980778932 ) ) ;
#112539=CARTESIAN_POINT ( 'NONE',  ( 5.303229652072571021, 1.413297086782526302, 0.9885393367406664078 ) ) ;
#112542=CARTESIAN_POINT ( 'NONE',  ( 0.6329805529394582075, 0.5017471949167272571, 1.659931108299773639 ) ) ;
#112546=CARTESIAN_POINT ( 'NONE',  ( 4.821225769315531373, -1.936335391968559527, -0.9821231961690338741 ) ) ;
#112547=CARTESIAN_POINT ( 'NONE',  ( 3.826616632296374831, 1.734130841282412128, 0.5711148077138239465 ) ) ;
#112548=CARTESIAN_POINT ( 'NONE',  ( 1.164813196467245904, 1.489159823276710926, -1.277213275948145599 ) ) ;
#112549=CARTESIAN_POINT ( 'NONE',  ( 6.227753904044541322, 0.8083430201051154951, -1.957153335705215103 ) ) ;
#112550=CARTESIAN_POINT ( 'NONE',  ( 0.3930492761001015967, 1.902410075555853064, -1.278529456123769892 ) ) ;
#112554=CARTESIAN_POINT ( 'NONE',  ( 2.948016456289838771, -1.425740979638410399, -1.569777838261996017 ) ) ;
#112559=CARTESIAN_POINT ( 'NONE',  ( 0.5321919801732944988, 1.189095644551215525, 1.694524325727378322 ) ) ;
#112560=CARTESIAN_POINT ( 'NONE',  ( 6.983263157960361234, 4.694303448529787204, 2.516403841208918912 ) ) ;
#112564=CARTESIAN_POINT ( 'NONE',  ( 2.420824200137431603, -0.8528996238171372424, -2.051222908810364842 ) ) ;
#112566=CARTESIAN_POINT ( 'NONE',  ( 0.2472849680876147149, 2.272430822888141133, -0.3459996173978163725 ) ) ;
#112568=CARTESIAN_POINT ( 'NONE',  ( 5.840703832811390050, -2.011083492259890360, -0.4572853040550031167 ) ) ;
#112573=CARTESIAN_POINT ( 'NONE',  ( 0.2331563151865729544, 6.948071805571808035, -2.540803835148666145 ) ) ;
#112574=CARTESIAN_POINT ( 'NONE',  ( 5.653808312887880660, 0.7519890275384639722, 1.680886247995525773 ) ) ;
#112576=CARTESIAN_POINT ( 'NONE',  ( 2.379564082050821483, 1.058669913282745956, 1.361546577445968964 ) ) ;
#112577=CARTESIAN_POINT ( 'NONE',  ( 1.059780186608853203, 1.205045252304644210, 1.616690996016925563 ) ) ;
#112578=CARTESIAN_POINT ( 'NONE',  ( 2.110373620506571957, 0.004507209458638748376, 2.298851035670963050 ) ) ;
#112580=CARTESIAN_POINT ( 'NONE',  ( 2.126610404160976575, 1.303795175273964269, -1.848758590024823123 ) ) ;
#112581=CARTESIAN_POINT ( 'NONE',  ( 3.598352328373265685, -2.103663943315597251, -0.1031874809700270568 ) ) ;
#112583=CARTESIAN_POINT ( 'NONE',  ( 2.301682877085888368, -1.769492147959438322, 0.03813942612425345879 ) ) ;
#112587=CARTESIAN_POINT ( 'NONE',  ( 5.794527259016318155, 1.876155144389481721, -1.316939630280162365 ) ) ;
#112588=CARTESIAN_POINT ( 'NONE',  ( 4.048646477676579813, -1.531818510360350327, -1.021117339664041834 ) ) ;
#112592=CARTESIAN_POINT ( 'NONE',  ( 4.576244502665470115, -2.125281509430646754, -0.5339713055512520512 ) ) ;
#112597=CARTESIAN_POINT ( 'NONE',  ( 2.666528119303875233, -1.328299865307873695, 1.395581591625531193 ) ) ;
#112601=CARTESIAN_POINT ( 'NONE',  ( 5.273731010124149243, 0.4114677744767555878, -2.080124947408354963 ) ) ;
#112606=CARTESIAN_POINT ( 'NONE',  ( 5.987831981441137152, -1.833028718050220940, -0.1737628300680846560 ) ) ;
#112610=CARTESIAN_POINT ( 'NONE',  ( 1.874151978141885833, -0.08570891532005876778, -1.738468184182701881 ) ) ;
#112611=CARTESIAN_POINT ( 'NONE',  ( 0.3089402658475807195, -1.578002999302514642, 1.165503548361209063 ) ) ;
#112614=CARTESIAN_POINT ( 'NONE',  ( 6.051685545382852638, 0.6321331830463626789, -2.067208725892249799 ) ) ;
#112619=CARTESIAN_POINT ( 'NONE',  ( 5.981359018292748075, 1.999130597612966742, -0.8229454869796914984 ) ) ;
#112623=CARTESIAN_POINT ( 'NONE',  ( 6.819606788702130551, -1.912791534441590668, 0.4766558377571166183 ) ) ;
#112624=CARTESIAN_POINT ( 'NONE',  ( 6.362590153729421161, -0.5805357501837383749, 1.633877867761362124 ) ) ;
#112626=CARTESIAN_POINT ( 'NONE',  ( 3.527062600443749307, -2.024233912922444478, 0.8403589366152917073 ) ) ;
#112627=CARTESIAN_POINT ( 'NONE',  ( 3.259088711995949517, -1.748676463734340603, 1.505793948229345869 ) ) ;
#112628=CARTESIAN_POINT ( 'NONE',  ( 6.204382384804184802, -0.7375479284208189545, -1.924474620761642996 ) ) ;
#112629=CARTESIAN_POINT ( 'NONE',  ( 1.605311038211139740, -1.927294583035423114, 0.2376585312828301821 ) ) ;
#112634=CARTESIAN_POINT ( 'NONE',  ( 3.779626292077961747, 0.2561244552635975058, -2.104982076983111572 ) ) ;
#112636=CARTESIAN_POINT ( 'NONE',  ( 2.654922836763852878, 1.081066371885472277, 1.701947380796410059 ) ) ;
#112638=CARTESIAN_POINT ( 'NONE',  ( 4.489439581592091777, 1.972811803287272348, -0.9889974963176446643 ) ) ;
#112641=CARTESIAN_POINT ( 'NONE',  ( 0.01192831195480706721, -0.7772932952810689411, -1.650495136788888040 ) ) ;
#112644=CARTESIAN_POINT ( 'NONE',  ( 6.825078400183555161, 2.003297025668087983, 2.546134486959560572 ) ) ;
#112647=CARTESIAN_POINT ( 'NONE',  ( 4.610263661134276880, -0.8792652907330700263, -1.864042625929088759 ) ) ;
#112652=CARTESIAN_POINT ( 'NONE',  ( 2.877608074518396286, 0.2940240112025078179, -1.998017427383149913 ) ) ;
#112657=CARTESIAN_POINT ( 'NONE',  ( 3.555589940775650604, 0.5024415226424256975, -1.998565159594118068 ) ) ;
#112658=CARTESIAN_POINT ( 'NONE',  ( 2.813125141109920069, 1.117832431973438734, -1.678005364621336426 ) ) ;
#112663=CARTESIAN_POINT ( 'NONE',  ( 0.8668490835730925381, 1.774987751554598869, -0.4888055736953432207 ) ) ;
#112664=CARTESIAN_POINT ( 'NONE',  ( 0.01296380302724577452, -0.9916191462571806170, -2.081274906121612034 ) ) ;
#112666=CARTESIAN_POINT ( 'NONE',  ( 2.688937055384226671, -0.3666181952855402382, -2.130111032054008646 ) ) ;
#112668=CARTESIAN_POINT ( 'NONE',  ( 4.487589638097394307, -0.5612149057237262317, 2.041579019078069379 ) ) ;
#112669=CARTESIAN_POINT ( 'NONE',  ( 2.847332689139534523, -1.183592279326161290, 1.970102427710369808 ) ) ;
#112671=CARTESIAN_POINT ( 'NONE',  ( 1.182252951876180180, -1.824241171369020531, -0.4133900166373091767 ) ) ;
#112672=CARTESIAN_POINT ( 'NONE',  ( 4.469576204829595945, 1.912561584401346604, -0.4778803491252373026 ) ) ;
#112673=CARTESIAN_POINT ( 'NONE',  ( 4.135954056172497673, 2.015980767636461835, -0.05432360925018697717 ) ) ;
#112677=CARTESIAN_POINT ( 'NONE',  ( 6.428360055892773595, 1.214212339677790409, -1.720619796903441578 ) ) ;
#112678=CARTESIAN_POINT ( 'NONE',  ( 6.250451049865752395, -2.060019788584551481, -0.2068627631737207651 ) ) ;
#112681=CARTESIAN_POINT ( 'NONE',  ( 6.539320575229274901, 4.692178491785949923, 2.665866134390063813 ) ) ;
#112682=CARTESIAN_POINT ( 'NONE',  ( 4.733256667524862848, -1.802829663221987788, 0.7981805449851049339 ) ) ;
#112683=CARTESIAN_POINT ( 'NONE',  ( 6.011974661143067777, -0.6766988549865710079, 1.903214300750865506 ) ) ;
#112685=CARTESIAN_POINT ( 'NONE',  ( 4.987122935671228774, -0.2785958505117277495, -2.290767236937583995 ) ) ;
#112686=CARTESIAN_POINT ( 'NONE',  ( 1.622013285028017338, 2.032735996446675131, -0.3486163383695956575 ) ) ;
#112693=CARTESIAN_POINT ( 'NONE',  ( 4.563029256048502624, 1.681186374793992355, -1.373936881898863982 ) ) ;
#112696=CARTESIAN_POINT ( 'NONE',  ( 3.561895345837225779, -1.234009368583251387, 1.366721199326895952 ) ) ;
#112699=CARTESIAN_POINT ( 'NONE',  ( 5.935146830689759234, -1.586316731616247200, -1.512381816529739353 ) ) ;
#112701=CARTESIAN_POINT ( 'NONE',  ( 5.594667793837476033, -0.5436135106791986082, -2.196135934016548052 ) ) ;
#112707=CARTESIAN_POINT ( 'NONE',  ( 0.4964904254905980197, 1.474999729349553590, -0.9777959528048956184 ) ) ;
#112708=CARTESIAN_POINT ( 'NONE',  ( 5.777995030156034773, 1.982912992605226465, -0.3464542934713372158 ) ) ;
#112709=CARTESIAN_POINT ( 'NONE',  ( 3.821394775679032740, -0.1568257194812898159, 2.100186923160925812 ) ) ;
#112710=CARTESIAN_POINT ( 'NONE',  ( 2.354979200267411255, 0.09147625538302081583, -1.913532508166473800 ) ) ;
#112712=CARTESIAN_POINT ( 'NONE',  ( 3.139063269091638908, -0.1420806666206550495, -1.964468959564101613 ) ) ;
#112713=CARTESIAN_POINT ( 'NONE',  ( 5.959241620951676310, -1.704104911329520800, 1.083944116985413819 ) ) ;
#112714=CARTESIAN_POINT ( 'NONE',  ( 1.902992089709685031, 1.553661375375714471, 1.041555772207984676 ) ) ;
#112715=CARTESIAN_POINT ( 'NONE',  ( 2.312880826517309085, -1.518475810973318074, 1.242258525517292433 ) ) ;
#112716=CARTESIAN_POINT ( 'NONE',  ( 3.896855043588220546, 1.455827857355775246, -0.9247512240674607975 ) ) ;
#112717=CARTESIAN_POINT ( 'NONE',  ( 0.8614045922798494459, -1.509235727096858826, -1.174430983434850972 ) ) ;
#112719=CARTESIAN_POINT ( 'NONE',  ( 1.700138637298425737, -0.7412910010123253679, 2.078789392164873906 ) ) ;
#112730=CARTESIAN_POINT ( 'NONE',  ( 0.3442982867475213871, -0.9772804826688463731, 1.825211318103404867 ) ) ;
#112736=CARTESIAN_POINT ( 'NONE',  ( 5.760427271636393343, 2.118038551301495875, 0.1041057254967461404 ) ) ;
#112740=CARTESIAN_POINT ( 'NONE',  ( 5.898874287966751950, 0.3812104124719677412, 1.924297140916144233 ) ) ;
#112742=CARTESIAN_POINT ( 'NONE',  ( 3.831407535526813124, -1.356092489331266027, 1.492026659919619025 ) ) ;
#112743=CARTESIAN_POINT ( 'NONE',  ( 3.608511690770484837, 1.820787697044351505, 0.5958877267112758780 ) ) ;
#112744=CARTESIAN_POINT ( 'NONE',  ( 1.681448347407452193, 1.514353137444489406, 1.584415833815432162 ) ) ;
#112746=CARTESIAN_POINT ( 'NONE',  ( 0.1394461523056788055, 0.009327122704651916868, -1.719853553173174010 ) ) ;
#112748=CARTESIAN_POINT ( 'NONE',  ( 5.027594669734884114, -0.2912581947275821315, 1.991892893239319617 ) ) ;
#112751=CARTESIAN_POINT ( 'NONE',  ( 5.747700551816460113, 2.085811977426319519, -0.3625847027708250514 ) ) ;
#112753=CARTESIAN_POINT ( 'NONE',  ( 2.911755628046075906, -1.032623549580795608, -1.817877418097467501 ) ) ;
#112755=CARTESIAN_POINT ( 'NONE',  ( 1.359898630301906053, 0.6939498547450100308, 1.579201994853156821 ) ) ;
#112757=CARTESIAN_POINT ( 'NONE',  ( 5.853796514643677007, -1.537196951383312804, -1.461068456062891041 ) ) ;
#112766=CARTESIAN_POINT ( 'NONE',  ( 2.068756839025966521, -1.399621434743709703, 1.149952615172030512 ) ) ;
#112773=CARTESIAN_POINT ( 'NONE',  ( 2.174188805400371294, 0.7754062184415695391, 1.637274071133995035 ) ) ;
#112774=CARTESIAN_POINT ( 'NONE',  ( 6.539320575229291777, 2.092415259949731432, 2.107292781797183601 ) ) ;
#112777=CARTESIAN_POINT ( 'NONE',  ( 4.510102262511601623, 1.860682779278443277, -0.04454786357706643635 ) ) ;
#112778=CARTESIAN_POINT ( 'NONE',  ( 0.7728743906838764222, 1.688931763573727540, -0.9039392725495792869 ) ) ;
#112779=CARTESIAN_POINT ( 'NONE',  ( 0.3756504392133250825, 1.046533627790873000, 1.495644344755318045 ) ) ;
#112786=CARTESIAN_POINT ( 'NONE',  ( 4.680490344776488065, 1.214988973509235848, -1.549875580164503663 ) ) ;
#112789=CARTESIAN_POINT ( 'NONE',  ( 6.650331627364351128, -1.696677047125955795, 1.386650686450926484 ) ) ;
#112790=CARTESIAN_POINT ( 'NONE',  ( 5.842784322950494769, 0.3761301977728331858, 1.889152344147272178 ) ) ;
#112793=CARTESIAN_POINT ( 'NONE',  ( 2.139570144280181108, -1.970530345926827742, 0.9937953903183870397 ) ) ;
#112795=CARTESIAN_POINT ( 'NONE',  ( 0.3164790345465406385, -0.6463921985436006379, -1.799943259716822341 ) ) ;
#112798=CARTESIAN_POINT ( 'NONE',  ( 0.1390025477998011738, -0.1451226239368992033, -1.937570863154890688 ) ) ;
#112799=CARTESIAN_POINT ( 'NONE',  ( 1.786567547031367775, 1.688677558619257058, -0.9590575663266877049 ) ) ;
#112801=CARTESIAN_POINT ( 'NONE',  ( 0.8255457999647041190, -1.462224166115761337, 1.388270745661695837 ) ) ;
#112803=CARTESIAN_POINT ( 'NONE',  ( 5.242936282186112962, -0.2253732266207208457, -1.847139840844784775 ) ) ;
#112806=CARTESIAN_POINT ( 'NONE',  ( 6.509000000000014552, 2.444259026362519904, 2.383015625331697862 ) ) ;
#112810=CARTESIAN_POINT ( 'NONE',  ( 1.839652601550560096, 0.8350199954420146620, -2.026445374841173930 ) ) ;
#112814=CARTESIAN_POINT ( 'NONE',  ( 2.086296903703276140, -1.790263230197926436, -0.3570169370194844483 ) ) ;
#112817=CARTESIAN_POINT ( 'NONE',  ( 6.509000000000015440, 0.001920477310516938412, 2.100274754360692331 ) ) ;
#112819=CARTESIAN_POINT ( 'NONE',  ( 0.7328819429333592872, 0.1407736501095498138, 1.921419779381093207 ) ) ;
#112820=CARTESIAN_POINT ( 'NONE',  ( 3.924618397835403893, -1.320764108826902428, 1.450678906977073579 ) ) ;
#112823=CARTESIAN_POINT ( 'NONE',  ( 4.915667883426772633, -1.172277214026868464, -1.851500752446763709 ) ) ;
#112825=CARTESIAN_POINT ( 'NONE',  ( 3.871986384844767315, -2.040452582458017083, 0.3490408808229996662 ) ) ;
#112829=CARTESIAN_POINT ( 'NONE',  ( 4.483195000112350392, -2.298113444969139607, -0.05724751674645797012 ) ) ;
#112834=CARTESIAN_POINT ( 'NONE',  ( 6.620655732516651071, 7.053049904137934867, 2.524417197114035005 ) ) ;
#112836=CARTESIAN_POINT ( 'NONE',  ( 3.328005318368632892, 1.894807597966931878, 0.4246257584521081485 ) ) ;
#112839=CARTESIAN_POINT ( 'NONE',  ( 4.816621285000030284, -0.6497861859515661198, -1.798733151862880186 ) ) ;
#112841=CARTESIAN_POINT ( 'NONE',  ( 5.631808906544129911, -1.097478420741523575, -1.330571920265137376 ) ) ;
#112842=CARTESIAN_POINT ( 'NONE',  ( 4.522672878804367969, 0.3494810548456111499, 1.985869246038343583 ) ) ;
#112843=CARTESIAN_POINT ( 'NONE',  ( 5.098365541279441082, -0.3395090112114571013, 2.273368781073564993 ) ) ;
#112845=CARTESIAN_POINT ( 'NONE',  ( 1.049787907720298286, -1.741764784136769162, -1.355102641770723704 ) ) ;
#112848=CARTESIAN_POINT ( 'NONE',  ( 5.782415762239879520, -1.726843194930051562, -0.3863986657466413899 ) ) ;
#112849=CARTESIAN_POINT ( 'NONE',  ( 6.205703963786828758, 1.882472927010571118, 0.7231429968634556227 ) ) ;
#112852=CARTESIAN_POINT ( 'NONE',  ( 2.554944377107245757, -1.995129818168206226, -1.128553997664314412 ) ) ;
#112853=CARTESIAN_POINT ( 'NONE',  ( 1.253398004092287854, 0.7024035357156286352, 1.592479786115083229 ) ) ;
#112855=CARTESIAN_POINT ( 'NONE',  ( 1.176590053548575598, -0.7728590343649595074, -1.552129106697144989 ) ) ;
#112858=CARTESIAN_POINT ( 'NONE',  ( 1.346384888165049754, -0.9767783691352300846, 1.939140577548441380 ) ) ;
#112859=CARTESIAN_POINT ( 'NONE',  ( 1.938685741270998797, -1.555697844595272716, 1.282991390469834458 ) ) ;
#112860=CARTESIAN_POINT ( 'NONE',  ( 4.031250000000002665, -0.7852924748301974844, -1.895863743163994863 ) ) ;
#112862=CARTESIAN_POINT ( 'NONE',  ( 6.674445239480702341, -1.183187502913226608, 1.521125075997560527 ) ) ;
#112864=CARTESIAN_POINT ( 'NONE',  ( 3.762163318865581640, 0.7457541186767223662, -2.092641825391368560 ) ) ;
#112871=CARTESIAN_POINT ( 'NONE',  ( 5.161534370633450663, 0.8641669074914829496, 1.510678848428636201 ) ) ;
#112872=CARTESIAN_POINT ( 'NONE',  ( 3.437899435096212208, 1.242623406730450686, 1.518177208742684803 ) ) ;
#112876=CARTESIAN_POINT ( 'NONE',  ( 4.358826825731692445, -1.680320932299755210, 1.515136896344573270 ) ) ;
#112878=CARTESIAN_POINT ( 'NONE',  ( 1.891156856157749866, 0.2001100897341882012, 2.052929594394680812 ) ) ;
#112882=CARTESIAN_POINT ( 'NONE',  ( 2.255063695347800934, -1.748954272965432155, 1.435335380440343256 ) ) ;
#112885=CARTESIAN_POINT ( 'NONE',  ( 3.391731324245280010, -0.7611128710301139355, 1.708892184765831157 ) ) ;
#112886=CARTESIAN_POINT ( 'NONE',  ( 2.004178618920505972, -1.681731546479984463, 0.4224366712483189623 ) ) ;
#112887=CARTESIAN_POINT ( 'NONE',  ( 6.356982542327763497, 0.3766756592470664744, -2.158781491689326426 ) ) ;
#112888=CARTESIAN_POINT ( 'NONE',  ( 0.2709337360254741034, -1.439471777561899035, 1.672717458380864608 ) ) ;
#112889=CARTESIAN_POINT ( 'NONE',  ( 3.872077330825273389, 1.198917189070296541, 1.798566189592496034 ) ) ;
#112890=CARTESIAN_POINT ( 'NONE',  ( 4.646391893561965247, -1.558859349912258718, 1.157878524630775230 ) ) ;
#112892=CARTESIAN_POINT ( 'NONE',  ( 6.468025801952650866, 0.9617254617904011926, 1.604207369834034669 ) ) ;
#112898=CARTESIAN_POINT ( 'NONE',  ( 5.485000066852382616, -2.016597020608828839, 0.002808655738886777897 ) ) ;
#112902=CARTESIAN_POINT ( 'NONE',  ( 3.527797039230845311, -1.088449851438414218, -1.465592618984489670 ) ) ;
#112905=VERTEX_POINT ( 'NONE', #171712 ) ;
#112909=CARTESIAN_POINT ( 'NONE',  ( 6.340491327343366734, 1.161156619345372842, -1.652315300818160582 ) ) ;
#112910=CARTESIAN_POINT ( 'NONE',  ( 0.8562900302464396818, 0.8558255631127342777, -1.940287777186230578 ) ) ;
#112913=CARTESIAN_POINT ( 'NONE',  ( 2.324856365976185391, -1.699136111967664453, -0.7594513203179918959 ) ) ;
#112915=CARTESIAN_POINT ( 'NONE',  ( 6.297740734744428970, -0.6968897171561654336, 1.939616516419547132 ) ) ;
#112916=CARTESIAN_POINT ( 'NONE',  ( 6.328750030911493241, 0.7691242348151774433, -1.864167186630163009 ) ) ;
#112924=CARTESIAN_POINT ( 'NONE',  ( 6.046249930811113060, 1.863882344683247094, -0.7690052245405626374 ) ) ;
#112925=CARTESIAN_POINT ( 'NONE',  ( 4.242028835625204053, 0.4931972713904734795, 1.773778790588397491 ) ) ;
#112926=CARTESIAN_POINT ( 'NONE',  ( -0.02299388927992032997, 5.724334336916190757, -2.505015335112478425 ) ) ;
#112927=CARTESIAN_POINT ( 'NONE',  ( 3.493080449939501619, -0.4495562565045966852, -2.263328358674908003 ) ) ;
#112929=CARTESIAN_POINT ( 'NONE',  ( 6.257120919624137301, -1.850417449585840313, -1.117149918570578437 ) ) ;
#112931=CARTESIAN_POINT ( 'NONE',  ( 0.8373251867893832801, 0.7858318893144546902, -1.776134337346139125 ) ) ;
#112935=CARTESIAN_POINT ( 'NONE',  ( 4.763194794223141848, -2.297684049645591919, -0.06285783202429616467 ) ) ;
#112938=CARTESIAN_POINT ( 'NONE',  ( 4.856247981345184428, 0.7163626499266174674, 1.728251504774950709 ) ) ;
#112939=CARTESIAN_POINT ( 'NONE',  ( 0.7383556378116812313, 1.137082172773289379, -1.537495029474859276 ) ) ;
#112942=CARTESIAN_POINT ( 'NONE',  ( 2.614145488985010424, -2.182733025630137824, 0.3247920039054427721 ) ) ;
#112943=CARTESIAN_POINT ( 'NONE',  ( 6.883263157960335832, 7.629137130509051623, 2.446189081643288521 ) ) ;
#112949=CARTESIAN_POINT ( 'NONE',  ( 1.721884408201577399, -1.091793429770457458, -1.641225607529321229 ) ) ;
#112950=CARTESIAN_POINT ( 'NONE',  ( 1.237850453945861906, -2.084960033126967982, 0.9891342380793988198 ) ) ;
#112951=CARTESIAN_POINT ( 'NONE',  ( 2.084357000244409175, 1.132115006494602394, -1.602057852124554316 ) ) ;
#112952=CARTESIAN_POINT ( 'NONE',  ( 5.348506707712929575, -2.046340616697607473, -0.2579891923277094490 ) ) ;
#112959=CARTESIAN_POINT ( 'NONE',  ( 0.9366657375849207767, -1.207674400081097721, 1.803990093267322736 ) ) ;
#112964=CARTESIAN_POINT ( 'NONE',  ( 2.723731132150861711, -1.073666234122659713, -1.531540996774889640 ) ) ;
#112965=CARTESIAN_POINT ( 'NONE',  ( 6.397764797294555272, -0.7349420381566433846, 2.032942830986879557 ) ) ;
#112966=CARTESIAN_POINT ( 'NONE',  ( 0.07735805125220260314, 1.351236195817316466, -2.344668200922094492 ) ) ;
#112967=CARTESIAN_POINT ( 'NONE',  ( 6.827182134110201694, 1.288579688585177685, 1.926502426867699569 ) ) ;
#112969=CARTESIAN_POINT ( 'NONE',  ( 2.438023429326571456, -1.102505324871098757, -1.562262158393577405 ) ) ;
#112970=CARTESIAN_POINT ( 'NONE',  ( 4.205725695155067889, -1.765064932122958785, 0.1306522685067777467 ) ) ;
#112971=CARTESIAN_POINT ( 'NONE',  ( 1.541514448083292965, -1.800223203088219481, 0.6453159242577054533 ) ) ;
#112974=CARTESIAN_POINT ( 'NONE',  ( 5.273012193977356432, 1.687281682853270848, -0.9070163062135666587 ) ) ;
#112975=CARTESIAN_POINT ( 'NONE',  ( 0.2739938332866619364, -2.030697503880642518, 0.4024348779970430834 ) ) ;
#112977=CARTESIAN_POINT ( 'NONE',  ( 1.969135536805465492, -1.636093909763213228, 1.349083368969570262 ) ) ;
#112979=CARTESIAN_POINT ( 'NONE',  ( 4.645289301550183936, -1.446173438076237217, -1.186536486241091204 ) ) ;
#112980=CARTESIAN_POINT ( 'NONE',  ( 1.400715809426569702, 1.493624456287694358, -1.049586478250638999 ) ) ;
#112982=CARTESIAN_POINT ( 'NONE',  ( 4.758537496233657293, 0.8426522330295079799, 2.039869969286691731 ) ) ;
#112986=CARTESIAN_POINT ( 'NONE',  ( 2.418490130824833440, 0.8798743164511336756, 1.865715637115851866 ) ) ;
#112992=CARTESIAN_POINT ( 'NONE',  ( 4.018080225218490398, 2.055083638104511223, -0.2504045000601487492 ) ) ;
#112994=CARTESIAN_POINT ( 'NONE',  ( 2.653791512158054200, 0.5793167894731532375, -2.082426382048585101 ) ) ;
#112996=CARTESIAN_POINT ( 'NONE',  ( 2.578776193315842846, -1.391201028639722281, 1.464365899026105700 ) ) ;
#113004=CARTESIAN_POINT ( 'NONE',  ( 0.6203277878081385754, 1.987498645412737908, 0.3399528957561820386 ) ) ;
#113005=B_SPLINE_CURVE_WITH_KNOTS ( 'NONE', 3,
 ( #41271, #206935, #9802, #75877, #190678, #141984, #42337, #176584, #8740, #107379 ),
 .UNSPECIFIED., .F., .F.,
 ( 4, 1, 1, 1, 1, 1, 1, 4 ),
 ( 0.000000000000000000, 0.09090790722575105287, 0.1825853934691276381, 0.2551728700554835028, 0.3603391217242263855, 0.5205903519787860034, 0.7335386666926504429, 0.9999999999999998890 ),
 .UNSPECIFIED. ) ;
#113006=CARTESIAN_POINT ( 'NONE',  ( 4.880524338131243312, -0.2681524694418159216, -2.175044001020635331 ) ) ;
#113009=CARTESIAN_POINT ( 'NONE',  ( 4.869353489999923568, -1.618680692612521455, -1.018082601613921723 ) ) ;
#113013=CARTESIAN_POINT ( 'NONE',  ( 2.267204043252795120, 1.842440753109304330, -0.8197907266209791821 ) ) ;
#113016=CARTESIAN_POINT ( 'NONE',  ( 5.491107761985050573, 1.519353413045966494, -0.8162815091526542943 ) ) ;
#113017=CARTESIAN_POINT ( 'NONE',  ( 0.1405533004714097089, -0.003749010675423158478, -2.279853246149381452 ) ) ;
#113023=CARTESIAN_POINT ( 'NONE',  ( 1.024380955673375393, 1.017105081308821379, 1.803069775380027995 ) ) ;
#113025=VERTEX_POINT ( 'NONE', #4907 ) ;
#113026=CARTESIAN_POINT ( 'NONE',  ( 5.109926359719781708, -0.6467658019376655298, 1.692270648455761917 ) ) ;
#113030=CARTESIAN_POINT ( 'NONE',  ( 5.760388245948376174, 1.809740711040405348, 0.08207984589548086851 ) ) ;
#113033=CARTESIAN_POINT ( 'NONE',  ( 3.170069416559752273, -1.305109287949431929, 1.760291797049506446 ) ) ;
#113036=CARTESIAN_POINT ( 'NONE',  ( 0.9593383959572501229, 1.601786533887459507, 1.132500672181527168 ) ) ;
#113038=CARTESIAN_POINT ( 'NONE',  ( 5.396063265741290138, -0.8654563178034151427, -1.709049623916969018 ) ) ;
#113040=ADVANCED_FACE ( 'NONE', ( #5984 ), #90952, .T. ) ;
#113044=CARTESIAN_POINT ( 'NONE',  ( 2.184651956524386041, -2.119909832212972578, -0.4221607449544013679 ) ) ;
#113047=CARTESIAN_POINT ( 'NONE',  ( 2.098414945899258033, -0.4839449910110822373, -1.760204267430766301 ) ) ;
#113049=CARTESIAN_POINT ( 'NONE',  ( 4.928627555176230857, 1.747287423663802075, 0.5288322122747670662 ) ) ;
#113051=CARTESIAN_POINT ( 'NONE',  ( 2.672007700615218528, 1.902801012812182169, -0.1915479950082218386 ) ) ;
#113053=CARTESIAN_POINT ( 'NONE',  ( 3.947672784279113500, 1.424866277981166052, 1.359976495918001627 ) ) ;
#113055=CARTESIAN_POINT ( 'NONE',  ( 4.827648274430585751, 0.9952931021880854212, -1.667489682845281207 ) ) ;
#113059=CARTESIAN_POINT ( 'NONE',  ( 4.851869265964163347, -1.501451181749386743, -1.497782127133556518 ) ) ;
#113061=CARTESIAN_POINT ( 'NONE',  ( 2.666550042863625958, 0.6461651886627232111, 1.799920402468312197 ) ) ;
#113066=CARTESIAN_POINT ( 'NONE',  ( 5.443998933236983362, -1.278728028966215957, -1.554778559382914871 ) ) ;
#113068=CARTESIAN_POINT ( 'NONE',  ( 5.092344371507952161, -1.812320225013038133, -0.2200062734805732223 ) ) ;
#113069=CARTESIAN_POINT ( 'NONE',  ( 1.047426762419433777, 1.826728496382063582, -0.9743617655595809834 ) ) ;
#113073=CARTESIAN_POINT ( 'NONE',  ( 6.174654088403855212, -1.776896415251895789, -0.5849557326117056366 ) ) ;
#113082=CARTESIAN_POINT ( 'NONE',  ( 1.235311698660218838, -0.04697018572753957483, -2.069874154031334790 ) ) ;
#113083=CARTESIAN_POINT ( 'NONE',  ( 2.425544100157220662, -1.571072031863307572, -1.419494070558358967 ) ) ;
#113086=CARTESIAN_POINT ( 'NONE',  ( 0.4089589639980686919, -1.585120765669449261, 1.168626392425928584 ) ) ;
#113091=CARTESIAN_POINT ( 'NONE',  ( 2.660454013544113927, -1.579728858233371946, 1.661220326946882375 ) ) ;
#113092=CARTESIAN_POINT ( 'NONE',  ( 0.8205984872286451459, 1.685833220154912881, 0.7012733028506010768 ) ) ;
#113093=CARTESIAN_POINT ( 'NONE',  ( 1.898553772666348394, -1.876154101037771582, -0.3696338911259658411 ) ) ;
#113097=CARTESIAN_POINT ( 'NONE',  ( 1.476815932985692026, -1.420704281710112316, 1.426639689446000281 ) ) ;
#113098=CARTESIAN_POINT ( 'NONE',  ( 2.360140415366944744, -1.961439503465340239, 0.04308618615556784187 ) ) ;
#113102=CARTESIAN_POINT ( 'NONE',  ( 4.576172254314175625, -2.027756842407653082, -0.5083681234262329429 ) ) ;
#113103=CARTESIAN_POINT ( 'NONE',  ( 3.994789325776046507, 1.495029845459275863, -0.9468837749658890468 ) ) ;
#113107=CARTESIAN_POINT ( 'NONE',  ( 6.597627758599571735, -2.291905675289906519, 0.04924309260747637695 ) ) ;
#113108=CARTESIAN_POINT ( 'NONE',  ( 4.347407756490777153, 1.739891706657967552, -0.04609750694275702165 ) ) ;
#113111=CARTESIAN_POINT ( 'NONE',  ( 4.956219290344169970, 1.285291309562084816, 1.163873732738918587 ) ) ;
#113112=CARTESIAN_POINT ( 'NONE',  ( 4.721225823269111110, -1.937324205527543253, -0.9803755122778281539 ) ) ;
#113114=CARTESIAN_POINT ( 'NONE',  ( 5.788296071918774821, -0.7303023681345042206, -1.879805717804765353 ) ) ;
#113115=CARTESIAN_POINT ( 'NONE',  ( 5.000000000000003553, -2.717005030479747438E-13, -2.052068128417942727 ) ) ;
#113117=CARTESIAN_POINT ( 'NONE',  ( 2.713793335149127905, -1.905670363949378165, 0.2809714450454863233 ) ) ;
#113119=CARTESIAN_POINT ( 'NONE',  ( 6.504121277450023442, -0.9500910533294173455, 2.005660710250598555 ) ) ;
#113121=CARTESIAN_POINT ( 'NONE',  ( 6.883263157960393563, 4.695771316066229772, 2.508818740863460572 ) ) ;
#113124=CARTESIAN_POINT ( 'NONE',  ( 1.383751715516433833, 0.1588885597470449385, -2.215665637441687430 ) ) ;
#113125=CARTESIAN_POINT ( 'NONE',  ( 6.760214184729610665, -1.961454122871961747, 0.04698431645466792650 ) ) ;
#113131=CARTESIAN_POINT ( 'NONE',  ( 5.020015070024019366, 2.040704184028362178, -0.2994381943521097766 ) ) ;
#113136=CARTESIAN_POINT ( 'NONE',  ( 6.661405586796748324, 0.3194099797865917467, -1.842918054787325843 ) ) ;
#113137=CARTESIAN_POINT ( 'NONE',  ( 6.029869095562110815, -1.459853974539515153, 0.9356793305193217281 ) ) ;
#113138=CARTESIAN_POINT ( 'NONE',  ( 4.054071295385909934, -1.286197829845928675, 1.172710138673456415 ) ) ;
#113140=CARTESIAN_POINT ( 'NONE',  ( 2.929518028021148357, -1.541346711875633435, -1.696969020646617476 ) ) ;
#113142=CARTESIAN_POINT ( 'NONE',  ( 1.095364067855080448, -1.841320589428995236, -0.001981933617903330457 ) ) ;
#113146=CARTESIAN_POINT ( 'NONE',  ( 2.344514592193002400, 0.3973361102717865023, 1.781653928021959432 ) ) ;
#113147=CARTESIAN_POINT ( 'NONE',  ( 3.076796235938107138, -0.8146265060355701859, 1.844709937164576097 ) ) ;
#113148=CARTESIAN_POINT ( 'NONE',  ( 1.711130781365449716, -0.2659051965858104660, 2.175189728913041964 ) ) ;
#113150=CARTESIAN_POINT ( 'NONE',  ( 4.260836881943074417, -1.562014524604074861, 1.412707936923715879 ) ) ;
#113154=CARTESIAN_POINT ( 'NONE',  ( 1.873570696236816158, -0.2555354716398828274, 2.054483085851127377 ) ) ;
#113157=CARTESIAN_POINT ( 'NONE',  ( 3.106218681870171139, -0.8574772492565513327, 1.939554460742904274 ) ) ;
#113159=CARTESIAN_POINT ( 'NONE',  ( 6.674438497507635404, -1.118711561685633349, 1.443368817030561635 ) ) ;
#113166=CARTESIAN_POINT ( 'NONE',  ( 5.994406619193555663, -1.133004004027007294, 1.792352430775605798 ) ) ;
#113167=CARTESIAN_POINT ( 'NONE',  ( 1.518734001684220347, 1.414770742371696644, -1.560122519311944345 ) ) ;
#113170=CARTESIAN_POINT ( 'NONE',  ( 5.330833089851809703, -1.751472900985746373, -0.6291486930528921162 ) ) ;
#113172=( BOUNDED_SURFACE ( )  B_SPLINE_SURFACE ( 3, 3, ( 
 ( #196333, #97782, #45832, #17541, #47977, #210428, #46903, #32757, #164889, #161712 ),
 ( #79377, #64203, #180084, #145496, #65235, #63128, #16483, #66287, #131385, #129292 ),
 ( #113017, #197381, #115141, #96728, #162777, #14355, #82564, #51143, #150791, #120486 ),
 ( #121558, #1293, #200562, #135602, #71628, #2354, #19693, #137741, #149713, #70553 ),
 ( #134559, #20744, #184321, #68430, #21799, #202697, #4482, #69495, #54347, #136672 ),
 ( #55404, #18625, #186458, #53272, #87907, #199499, #35946, #34869, #86839, #3428 ),
 ( #169151, #52209, #117267, #118336, #183265, #201623, #203761, #100943, #38095, #67351 ) ),
 .UNSPECIFIED., .T., .F., .T. ) 
 B_SPLINE_SURFACE_WITH_KNOTS ( ( 4, 3, 4 ),
 ( 4, 1, 1, 1, 1, 1, 1, 4 ),
 ( 0.000000000000000000, 0.5000000000000000000, 1.000000000000000000 ),
 ( 0.000000000000000000, 0.09487947018404768729, 0.1878442364269655440, 0.2584026419818104547, 0.3617053504666527530, 0.5211417612611924932, 0.7337075935910832847, 1.000000000000000000 ),
 .UNSPECIFIED. ) 
 GEOMETRIC_REPRESENTATION_ITEM ( )  RATIONAL_B_SPLINE_SURFACE ( (
 ( 1.000000000000000000, 1.000000000000000000, 1.000000000000000000, 0.9999999999999996669, 1.000000000000000222, 1.000000000000000000, 1.000000000000000222, 0.9999999999999997780, 1.000000000000000000, 1.000000000000000000),
 ( 0.3333333333333333703, 0.3333333333333333703, 0.3333333333333334259, 0.3333333333333332593, 0.3333333333333334814, 0.3333333333333333148, 0.3333333333333334259, 0.3333333333333333148, 0.3333333333333333703, 0.3333333333333333703),
 ( 0.3333333333333333703, 0.3333333333333333703, 0.3333333333333334259, 0.3333333333333332593, 0.3333333333333334814, 0.3333333333333333148, 0.3333333333333334259, 0.3333333333333333148, 0.3333333333333333703, 0.3333333333333333703),
 ( 1.000000000000000000, 1.000000000000000000, 1.000000000000000000, 0.9999999999999996669, 1.000000000000000222, 1.000000000000000000, 1.000000000000000222, 0.9999999999999997780, 1.000000000000000000, 1.000000000000000000),
 ( 0.3333333333333333703, 0.3333333333333333703, 0.3333333333333334259, 0.3333333333333332593, 0.3333333333333334814, 0.3333333333333333148, 0.3333333333333334259, 0.3333333333333333148, 0.3333333333333333703, 0.3333333333333333703),
 ( 0.3333333333333333703, 0.3333333333333333703, 0.3333333333333334259, 0.3333333333333332593, 0.3333333333333334814, 0.3333333333333333148, 0.3333333333333334259, 0.3333333333333333148, 0.3333333333333333703, 0.3333333333333333703),
 ( 1.000000000000000000, 1.000000000000000000, 1.000000000000000000, 0.9999999999999996669, 1.000000000000000222, 1.000000000000000000, 1.000000000000000222, 0.9999999999999997780, 1.000000000000000000, 1.000000000000000000) ) ) 
 REPRESENTATION_ITEM ( '' )  SURFACE ( )  );
#113177=CARTESIAN_POINT ( 'NONE',  ( 2.734756269166933151, -1.876540383875524576, -0.5722209215143353456 ) ) ;
#113178=CARTESIAN_POINT ( 'NONE',  ( 1.428841412761387986, 2.083414371474631377, 0.5762002773818803991 ) ) ;
#113182=CARTESIAN_POINT ( 'NONE',  ( 2.618122797784384836, 0.4666061159355525678, -1.669766330342295158 ) ) ;
#113183=CARTESIAN_POINT ( 'NONE',  ( 2.835604015501072439, 1.727201357243525637, 0.2126739171897980840 ) ) ;
#113184=CARTESIAN_POINT ( 'NONE',  ( 6.463506322211490129, 0.4017315814064837953, -2.272322137143814480 ) ) ;
#113187=CARTESIAN_POINT ( 'NONE',  ( 3.022786435837477637, 1.939216523002813997, 0.6976457746366692136 ) ) ;
#113188=CARTESIAN_POINT ( 'NONE',  ( 0.6321852052597470850, 0.2004073784105386835, -2.006138679842318862 ) ) ;
#113189=CARTESIAN_POINT ( 'NONE',  ( 6.925078400183521055, 4.691537398408025972, 2.606905763235977336 ) ) ;
#113191=CARTESIAN_POINT ( 'NONE',  ( 1.217580299722145210, -1.923910348332603881, 0.4297500124877791650 ) ) ;
#113193=CARTESIAN_POINT ( 'NONE',  ( 5.361546783204238942, -1.511448857895525855, -1.171587532507123441 ) ) ;
#113198=CARTESIAN_POINT ( 'NONE',  ( 1.365885014167470546, 0.5842608817006667010, -1.933330045775418116 ) ) ;
#113200=CARTESIAN_POINT ( 'NONE',  ( 4.876155869083551586, 1.324110019830313734, 1.889726917317616328 ) ) ;
#113201=CARTESIAN_POINT ( 'NONE',  ( 5.494571831323358246, 1.932540981948445147, 0.3370517209014682325 ) ) ;
#113202=CARTESIAN_POINT ( 'NONE',  ( 1.586688997538304058, 1.889165970957426444, 0.5283831072378852856 ) ) ;
#113204=CARTESIAN_POINT ( 'NONE',  ( -0.1399997263889594112, -0.002789056014654289761, -2.000146600338557956 ) ) ;
#113205=ORIENTED_EDGE ( 'NONE', *, *, #137027, .T. ) ;
#113206=CARTESIAN_POINT ( 'NONE',  ( 1.095081093118466908, 1.870138624552514006, 0.9927810678921239473 ) ) ;
#113209=CARTESIAN_POINT ( 'NONE',  ( 0.9898993202219902310, -0.4452471680344311511, -1.786356756097874587 ) ) ;
#113211=CARTESIAN_POINT ( 'NONE',  ( 4.258752264053907055, -0.6753675163390076008, -2.063452119831588494 ) ) ;
#113213=CARTESIAN_POINT ( 'NONE',  ( 1.582450481569739331, 1.094613367649547309, 1.816135667671102016 ) ) ;
#113217=CARTESIAN_POINT ( 'NONE',  ( 2.952472966291960876, 0.6911811108033919515, 1.941568756818631725 ) ) ;
#113219=CARTESIAN_POINT ( 'NONE',  ( 0.5207438388301621757, -1.748553680932497745, 0.5769860859521497298 ) ) ;
#113221=CARTESIAN_POINT ( 'NONE',  ( 0.07755575628181145265, 7.629137130509078268, -2.788902932953695846 ) ) ;
#113224=CARTESIAN_POINT ( 'NONE',  ( 0.3818278861203865393, 2.057605126571937060, -0.7983354260262252033 ) ) ;
#113225=CARTESIAN_POINT ( 'NONE',  ( 2.900009951539525677, -0.7123764238676842941, 2.147366075387107553 ) ) ;
#113227=CARTESIAN_POINT ( 'NONE',  ( 2.250024469429566132, 0.8508988043372580634, -1.599271047475413932 ) ) ;
#113229=CARTESIAN_POINT ( 'NONE',  ( 1.815515222670351259, -1.254507992466627808, -1.447865379607627512 ) ) ;
#113230=CARTESIAN_POINT ( 'NONE',  ( 3.508316276398337319, 2.070544812355082254, 0.002818362966339192730 ) ) ;
#113233=CARTESIAN_POINT ( 'NONE',  ( 1.323050886902911616, -0.05057411593789931659, 1.970981584096524575 ) ) ;
#113234=CARTESIAN_POINT ( 'NONE',  ( 6.656866507323381477, -1.487278495449697147, 1.224136630395280534 ) ) ;
#113235=CARTESIAN_POINT ( 'NONE',  ( 2.729206520949432946, -1.746158693253213379, 0.6715030345267187784 ) ) ;
#113236=CARTESIAN_POINT ( 'NONE',  ( 0.9092882892361430214, 1.744143012382966207, -1.511207573902007884 ) ) ;
#113238=CARTESIAN_POINT ( 'NONE',  ( 2.400643840759258740, 0.4042734059873221986, 1.816444493264858906 ) ) ;
#113240=CARTESIAN_POINT ( 'NONE',  ( 5.125460521936802571, 0.2056810312900352600, -2.052415479088207650 ) ) ;
#113244=CARTESIAN_POINT ( 'NONE',  ( 6.563511373971260277, 0.3638278135829931537, -2.074131770586047363 ) ) ;
#113246=CARTESIAN_POINT ( 'NONE',  ( 6.345025448074324892, -1.829860219143174982, 1.150409744987097804 ) ) ;
#113247=CARTESIAN_POINT ( 'NONE',  ( 6.586581121665559202, -1.240835222743674526, 1.594039115436784337 ) ) ;
#113253=CARTESIAN_POINT ( 'NONE',  ( 6.925078400183578786, 2.094238355957972253, 2.065574651578235610 ) ) ;
#113256=CARTESIAN_POINT ( 'NONE',  ( 4.839077477813122918, -1.706110771555340744, -1.074664961451990308 ) ) ;
#113261=CARTESIAN_POINT ( 'NONE',  ( 5.506754051192107369, 1.639644015412666800, -1.408845030788405506 ) ) ;
#113267=CARTESIAN_POINT ( 'NONE',  ( 5.519157712072518152, -1.821736412749059397, 0.8647389720048551665 ) ) ;
#113269=CARTESIAN_POINT ( 'NONE',  ( 1.927930615940620873, 0.9947386370207593753, -1.408936266059911624 ) ) ;
#113274=CARTESIAN_POINT ( 'NONE',  ( 6.819622122755134797, -1.814287395386984691, 0.4549875680220638596 ) ) ;
#113275=CARTESIAN_POINT ( 'NONE',  ( 0.4693897461072121802, -1.701762708260607715, -1.075143862628368474 ) ) ;
#113277=CARTESIAN_POINT ( 'NONE',  ( 2.837189949676882428, 0.2689455771197127310, 2.190246129917215789 ) ) ;
#113278=CARTESIAN_POINT ( 'NONE',  ( 5.243124948155760912, -0.2588677773407067617, -2.155501751117256948 ) ) ;
#113282=CARTESIAN_POINT ( 'NONE',  ( 3.615986862044855421, -0.6139777315949943581, 2.029667854546577388 ) ) ;
#113283=CARTESIAN_POINT ( 'NONE',  ( 1.687125285987755019, 1.678019391100945779, 1.117813378161469418 ) ) ;
#113284=CARTESIAN_POINT ( 'NONE',  ( 2.601584773815317497, 1.283861566028346779, 1.278364218381728090 ) ) ;
#113285=ORIENTED_EDGE ( 'NONE', *, *, #168663, .F. ) ;
#113289=CARTESIAN_POINT ( 'NONE',  ( 1.305720528479116682, -1.067273574023764438, -1.590657944389769707 ) ) ;
#113290=CARTESIAN_POINT ( 'NONE',  ( 0.07479286986305370977, 0.004866263145587856019, -1.855573292446038414 ) ) ;
#113297=CARTESIAN_POINT ( 'NONE',  ( 4.979442225389012933, 2.018306902694905425, -0.7746836383674888804 ) ) ;
#113301=CARTESIAN_POINT ( 'NONE',  ( 1.389100911873580646, -2.015333191458138273, -0.6601287711371638389 ) ) ;
#113302=CARTESIAN_POINT ( 'NONE',  ( -0.1298852118744100725, 6.948705093303869873, -2.321530996463050389 ) ) ;
#113304=CARTESIAN_POINT ( 'NONE',  ( 3.831288253049653481, -1.822718488796180925, 0.7514253593702052703 ) ) ;
#113305=CARTESIAN_POINT ( 'NONE',  ( 5.590081826628392925, 1.144292256163012667, 1.532101299821154949 ) ) ;
#113309=CARTESIAN_POINT ( 'NONE',  ( 0.1333692844072559280, 0.001398348041498076455, -2.053671342968105051 ) ) ;
#113310=CARTESIAN_POINT ( 'NONE',  ( 2.361185668158103379, 1.904436331314839137, -0.3790439726399745246 ) ) ;
#113315=CARTESIAN_POINT ( 'NONE',  ( 2.959016038526005143, 0.3060221511422682727, -2.067984839732572855 ) ) ;
#113318=CARTESIAN_POINT ( 'NONE',  ( 5.988906256519173077, -1.817303134770717588, -0.5954205699960082310 ) ) ;
#113320=CARTESIAN_POINT ( 'NONE',  ( 4.600333186373093852, -2.206333364838486411, -0.05604163552313382035 ) ) ;
#113321=CARTESIAN_POINT ( 'NONE',  ( 2.661379449941482012, -1.919611247835448342, -1.088434722066232485 ) ) ;
#113324=CARTESIAN_POINT ( 'NONE',  ( 1.611815888142430264, -0.6431676737995162263, 1.801018335096972400 ) ) ;
#113327=CARTESIAN_POINT ( 'NONE',  ( 4.439934286204096914, 1.349936692791346093, 1.569845735447549906 ) ) ;
#113329=CARTESIAN_POINT ( 'NONE',  ( 2.061604318190731533, 0.3698614785779800185, -2.129673623264888960 ) ) ;
#113330=CARTESIAN_POINT ( 'NONE',  ( 4.212563348414651188, 2.004022095860341413, 0.8874167208733558798 ) ) ;
#113338=CARTESIAN_POINT ( 'NONE',  ( 0.1236729436712938751, 0.3474707636354073537, 1.986100063511665237 ) ) ;
#113341=CARTESIAN_POINT ( 'NONE',  ( 4.768459183169745152, -0.8803848081004579385, -1.873848736155204087 ) ) ;
#113342=CARTESIAN_POINT ( 'NONE',  ( 3.158729500758109765, -1.458545141725621219, 1.258684350631077642 ) ) ;
#113343=CARTESIAN_POINT ( 'NONE',  ( 5.607064690329227830, -0.05131010805739347896, 2.116756054987908531 ) ) ;
#113346=CARTESIAN_POINT ( 'NONE',  ( 4.117982337901913148, 1.955079553045156127, -0.2365992483164043592 ) ) ;
#113347=CARTESIAN_POINT ( 'NONE',  ( 6.421853422025334268, 1.325270252340422061, -1.870170258788282247 ) ) ;
#113348=CARTESIAN_POINT ( 'NONE',  ( 4.301258635363705451, 1.467727663998198206, 1.085573330547324744 ) ) ;
#113354=CARTESIAN_POINT ( 'NONE',  ( 1.294213439101927321, 1.504999338701202394, -1.060447551955064016 ) ) ;
#113355=CARTESIAN_POINT ( 'NONE',  ( 4.834244255588106221, -1.080646305101562232, -1.698427166264226518 ) ) ;
#113356=CARTESIAN_POINT ( 'NONE',  ( 6.047535252586548893, -1.628406021067085874, 1.622660289872903006 ) ) ;
#113357=CARTESIAN_POINT ( 'NONE',  ( 5.576992410575341452, 1.811172876804711507, 0.7542287045681006497 ) ) ;
#113362=CARTESIAN_POINT ( 'NONE',  ( 1.382492367555522295, -0.3100735531622924035, -2.067509394536557021 ) ) ;
#113363=CARTESIAN_POINT ( 'NONE',  ( 0.4439547499465161251, 1.865322535695708606, 0.1421067652795371117 ) ) ;
#113365=CARTESIAN_POINT ( 'NONE',  ( 5.683525053321154985, -0.8713906080477454852, 1.735537339962249792 ) ) ;
#113366=CARTESIAN_POINT ( 'NONE',  ( -0.2104748580754408904, 1.337026610731705700, -2.356057411969681326 ) ) ;
#113367=CARTESIAN_POINT ( 'NONE',  ( 0.3798832434597871344, -0.2101876225509922147, -1.727645577085941353 ) ) ;
#113370=CARTESIAN_POINT ( 'NONE',  ( 1.418105696869888410, 1.160834107949513472, -1.275986549933407543 ) ) ;
#113371=CARTESIAN_POINT ( 'NONE',  ( 1.224469250947546328, 2.113408192816915943, 0.5798510048089372537 ) ) ;
#113372=CARTESIAN_POINT ( 'NONE',  ( 3.739080281021701868, 0.3231575147602770426, 2.182976880621155136 ) ) ;
#113375=CARTESIAN_POINT ( 'NONE',  ( 1.428853742479018862, -1.379120938454091227, 1.676725645940212894 ) ) ;
#113377=CARTESIAN_POINT ( 'NONE',  ( 1.727892286414894674, 0.8051050731917328562, -1.958494560251317740 ) ) ;
#113378=CARTESIAN_POINT ( 'NONE',  ( 6.639320575229263888, 6.039109382135522175, 2.391643382086404923 ) ) ;
#113380=CARTESIAN_POINT ( 'NONE',  ( 2.683473709500754367, 1.623236604230539282, 1.618912294457574674 ) ) ;
#113383=CARTESIAN_POINT ( 'NONE',  ( 4.547657996348432263, -2.031006315926532135, 0.8999586162586125093 ) ) ;
#113389=CARTESIAN_POINT ( 'NONE',  ( 2.602185585689294367, -0.1948409242511044692, 2.006959980107574371 ) ) ;
#113391=CARTESIAN_POINT ( 'NONE',  ( 1.955997896808071568, -0.6987562721488985717, 1.940702610317937671 ) ) ;
#113397=CARTESIAN_POINT ( 'NONE',  ( 4.716832014018703667, -0.1092502567305031480, 2.188841582221649595 ) ) ;
#113398=CARTESIAN_POINT ( 'NONE',  ( 2.004529941291322448, -1.955172360644286789, 0.4926429297785542283 ) ) ;
#113399=CARTESIAN_POINT ( 'NONE',  ( 2.524749765808989466, -1.717266272480859834, 0.6646640004178904215 ) ) ;
#113404=CARTESIAN_POINT ( 'NONE',  ( 4.946237996787820279, 1.820793779319082706, 0.1331645236858983172 ) ) ;
#113405=CARTESIAN_POINT ( 'NONE',  ( 5.555314621531947772, -1.277044735018734833, 1.560499014526220307 ) ) ;
#113407=CARTESIAN_POINT ( 'NONE',  ( 5.489262863951156923, 1.998152018339900415, -1.061309651537506227 ) ) ;
#113409=CARTESIAN_POINT ( 'NONE',  ( 0.6804681372492230595, -1.168251705716750299, 1.752132397912719242 ) ) ;
#113419=CARTESIAN_POINT ( 'NONE',  ( 1.723052270212792836, 1.567896913533245229, -1.427966198690698851 ) ) ;
#113420=CARTESIAN_POINT ( 'NONE',  ( 2.971146563671855034, -1.679565462486251048, 1.453923022682623856 ) ) ;
#113424=CARTESIAN_POINT ( 'NONE',  ( 2.805073129645048624, -1.632656238785214597, 1.087510969322850629 ) ) ;
#113430=CARTESIAN_POINT ( 'NONE',  ( 1.969135536805465492, -1.636093909763213228, 1.349083368969570262 ) ) ;
#113432=CARTESIAN_POINT ( 'NONE',  ( 4.891577088959510711, 1.599438101461609918, 1.454397306527709155 ) ) ;
#113433=CARTESIAN_POINT ( 'NONE',  ( 2.788419073117563762, 1.577926727847511312, -0.9486480243563880643 ) ) ;
#113436=CARTESIAN_POINT ( 'NONE',  ( 5.472502228039195060, -0.04848951148075366507, -1.739831344048385908 ) ) ;
#113440=CARTESIAN_POINT ( 'NONE',  ( 2.606508400632711719, -0.8264410288459265175, -1.997682696722333784 ) ) ;
#113442=CARTESIAN_POINT ( 'NONE',  ( 4.446638634790680555, 1.314796391739967207, 1.528506369862133285 ) ) ;
#113444=CARTESIAN_POINT ( 'NONE',  ( 1.991316529349271836, 1.880942973025516940, -1.065213018539921563 ) ) ;
#113445=CARTESIAN_POINT ( 'NONE',  ( 3.040257615459122320, 1.956033444698499268, 0.2450028794991568337 ) ) ;
#113448=CARTESIAN_POINT ( 'NONE',  ( 4.862805241732807815, 0.1868221656222105176, -1.933040885264789122 ) ) ;
#113457=CARTESIAN_POINT ( 'NONE',  ( 1.097021799178355739, -0.5375665728563282508, -2.140183485690804410 ) ) ;
#113459=CARTESIAN_POINT ( 'NONE',  ( 4.715648799723409113, 0.4337510919622395988, -1.913030730064477769 ) ) ;
#113465=CARTESIAN_POINT ( 'NONE',  ( 3.749809578975582536, 0.6641696684822319119, 1.717346325712478583 ) ) ;
#113470=CARTESIAN_POINT ( 'NONE',  ( 5.502226937873657242, -0.9515977829631333540, 1.895136135177949877 ) ) ;
#113473=CARTESIAN_POINT ( 'NONE',  ( 6.327427223165448922, -1.941958050844143413, 0.6900897555163245656 ) ) ;
#113475=CARTESIAN_POINT ( 'NONE',  ( 1.539268068193447858, 1.721329529071988107, -0.7080023387807417024 ) ) ;
#113476=CARTESIAN_POINT ( 'NONE',  ( 4.001369526190221571, -1.836035423186295201, 0.1395379388276704880 ) ) ;
#113481=CARTESIAN_POINT ( 'NONE',  ( 3.176612885197922953, -1.314426786483071208, 1.772596291930063739 ) ) ;
#113482=CARTESIAN_POINT ( 'NONE',  ( 5.483742561420515749, 1.513553928502100465, 1.681752807289581986 ) ) ;
#113484=CARTESIAN_POINT ( 'NONE',  ( 6.029554192727712980, -0.2124046070472781211, 1.799012333733180702 ) ) ;
#113485=CARTESIAN_POINT ( 'NONE',  ( 5.524599559428126305, 0.3805214045222211627, 1.877366190154891701 ) ) ;
#113487=CARTESIAN_POINT ( 'NONE',  ( 6.385618529757402406, 1.291587659170100766, 1.353439767483602285 ) ) ;
#113488=CARTESIAN_POINT ( 'NONE',  ( 5.775803124993572624, -1.815561990025884143, 0.4082129570420859888 ) ) ;
#113490=CARTESIAN_POINT ( 'NONE',  ( 6.754783849477350444, -1.364574176550734208, 1.126888093558385817 ) ) ;
#113493=CARTESIAN_POINT ( 'NONE',  ( 1.622280145275534435, 1.995268681201247452, 0.2910785328335343536 ) ) ;
#113495=CARTESIAN_POINT ( 'NONE',  ( 2.403073576612833939, 1.690916729301103594, -1.255302274246564043 ) ) ;
#113499=CARTESIAN_POINT ( 'NONE',  ( 3.287372214357705325, 0.04529362468645367623, -2.019439401957975111 ) ) ;
#113502=EDGE_CURVE ( 'NONE', #21324, #41604, #205103, .T. ) ;
#113503=CARTESIAN_POINT ( 'NONE',  ( 3.216266648612066792, -1.062311135343798618, -1.882447817163131587 ) ) ;
#113508=CARTESIAN_POINT ( 'NONE',  ( 0.7839114044838908502, -2.061656150924387365, 0.6811309647984428173 ) ) ;
#113512=CARTESIAN_POINT ( 'NONE',  ( 1.857222401600963302, 0.3706860215506869172, -2.159823580554325329 ) ) ;
#113514=CARTESIAN_POINT ( 'NONE',  ( 2.870297354751516039, 1.209492683862042339, 1.911920897162355582 ) ) ;
#113522=CARTESIAN_POINT ( 'NONE',  ( 2.846658922380195911, -1.473647421164023141, 0.9796213258056789552 ) ) ;
#113525=CARTESIAN_POINT ( 'NONE',  ( 6.809632187368197087, -0.4906261968062891055, 2.159508175712351541 ) ) ;
#113528=CARTESIAN_POINT ( 'NONE',  ( 5.202749988929913805, 1.864175517894875789, 0.7691070904374335271 ) ) ;
#113531=CARTESIAN_POINT ( 'NONE',  ( 3.432352559540859271, 1.824792983844251371, 0.4109263881779609551 ) ) ;
#113532=CARTESIAN_POINT ( 'NONE',  ( 2.922783962489564846, -1.430918204188264875, 1.496350883549990129 ) ) ;
#113539=CARTESIAN_POINT ( 'NONE',  ( 1.336036003918249948, -1.064896177285217016, -1.588262137521757822 ) ) ;
#113540=CARTESIAN_POINT ( 'NONE',  ( 2.541395235131336694, 1.794889867694851260, -0.7924082849640816661 ) ) ;
#113541=ADVANCED_FACE ( 'NONE', ( #14428 ), #79450, .T. ) ;
#113542=CARTESIAN_POINT ( 'NONE',  ( 1.423203639035979906, 0.8144988626696235690, 1.844428818423976546 ) ) ;
#113546=CARTESIAN_POINT ( 'NONE',  ( 6.309841845984305309, -1.956726702252456596, 0.2390368442499128110 ) ) ;
#113548=CARTESIAN_POINT ( 'NONE',  ( 2.302991897352596684, -0.3483681713834784199, -1.982697776695659053 ) ) ;
#113550=CARTESIAN_POINT ( 'NONE',  ( 2.407945773967453462, -1.221608841751795405, -1.729074501506906225 ) ) ;
#113552=CARTESIAN_POINT ( 'NONE',  ( 4.264170421968140445, -2.065031762457261610, 0.1491743435546449281 ) ) ;
#113554=CARTESIAN_POINT ( 'NONE',  ( 5.560518711993346130, -1.889693770910952253, -0.8946095687128383656 ) ) ;
#113556=CARTESIAN_POINT ( 'NONE',  ( 4.330939430599492823, 0.08983702179986638447, 1.823481399301421169 ) ) ;
#113559=CARTESIAN_POINT ( 'NONE',  ( 6.890000000000015667, 0.5768591945385994624, 2.052260346930290247 ) ) ;
#113561=CARTESIAN_POINT ( 'NONE',  ( 6.176841753231244958, -2.093540797633717254, -0.6980159708611932690 ) ) ;
#113564=CARTESIAN_POINT ( 'NONE',  ( 5.022078740994724733, -1.902695638548990820, 0.1913334245251183119 ) ) ;
#113571=CARTESIAN_POINT ( 'NONE',  ( 0.8723036553972833840, -0.04505207493780279820, -1.840872848514919280 ) ) ;
#113575=CARTESIAN_POINT ( 'NONE',  ( 5.167206475355686557, 0.1846639555213614448, -1.861428779493356167 ) ) ;
#113582=CARTESIAN_POINT ( 'NONE',  ( 1.621857603371698708, 1.941177911247515375, -0.3314221829187612989 ) ) ;
#113583=CARTESIAN_POINT ( 'NONE',  ( 2.302361438560030393, 1.314982760645909465, -1.528754769246756018 ) ) ;
#113587=CARTESIAN_POINT ( 'NONE',  ( 2.765787700092982693, 1.173089151190203294, 1.850848517565194751 ) ) ;
#113596=CARTESIAN_POINT ( 'NONE',  ( 4.476008884455379366, -1.787108923542475525, -0.4427587100873929815 ) ) ;
#113597=CARTESIAN_POINT ( 'NONE',  ( 2.350245942676463695, 0.9471468416194218642, -1.776342852653712168 ) ) ;
#113598=CARTESIAN_POINT ( 'NONE',  ( 3.093437905492165907, 1.279035344561373355, -1.909460003155829311 ) ) ;
#113600=CARTESIAN_POINT ( 'NONE',  ( 2.166652004499136197, 1.382927810177040584, -1.245475062859234372 ) ) ;
#113602=CARTESIAN_POINT ( 'NONE',  ( 6.152599605923961157, 1.892562589925715466, 0.2737767527046449101 ) ) ;
#113605=CARTESIAN_POINT ( 'NONE',  ( 4.757415945720180339, 2.067795187486476394, -0.3081579728113920669 ) ) ;
#113606=CARTESIAN_POINT ( 'NONE',  ( 3.291731440620565330, -0.7593194595177065187, 1.709801165022284408 ) ) ;
#113608=CARTESIAN_POINT ( 'NONE',  ( 5.776868925826902590, 1.698781319366513998, -0.7106697882480541573 ) ) ;
#113612=CARTESIAN_POINT ( 'NONE',  ( 5.268053373232242542, 0.8548693298336268453, 1.498049451945895116 ) ) ;
#113619=CARTESIAN_POINT ( 'NONE',  ( 4.293918747171243666, -1.492831977124044363, -1.576629974643141363 ) ) ;
#113620=CARTESIAN_POINT ( 'NONE',  ( 3.475057130574196407, 0.04366187338752242769, -1.825333387291371512 ) ) ;
#113621=CARTESIAN_POINT ( 'NONE',  ( 1.129655866247070595, 1.892139549451707037, -0.5178372573612435303 ) ) ;
#113622=CARTESIAN_POINT ( 'NONE',  ( 5.753141757616087482, 0.1533694674813860792, -2.111807561841658742 ) ) ;
#113623=CARTESIAN_POINT ( 'NONE',  ( 5.355124402800013783, 0.4497703203518633175, -2.247661708361737620 ) ) ;
#113627=CARTESIAN_POINT ( 'NONE',  ( 2.332823983099761911, 1.383068002389773454, -1.607457772141835717 ) ) ;
#113632=CARTESIAN_POINT ( 'NONE',  ( 6.227409518260961896, 0.1680337313966096258, -2.164657318592048352 ) ) ;
#113633=CARTESIAN_POINT ( 'NONE',  ( 6.983263157960355016, 2.444413620957446742, 2.336241774956763884 ) ) ;
#113635=CARTESIAN_POINT ( 'NONE',  ( 2.789914007569836318, 2.108506539658880907, -0.6989939510357189301 ) ) ;
#113637=CARTESIAN_POINT ( 'NONE',  ( 0.1066027571702803795, -0.1042336552941041522, 2.296444677329109840 ) ) ;
#113639=CARTESIAN_POINT ( 'NONE',  ( 5.612196365462351011, 2.060443358388251323, -0.09580443939274756182 ) ) ;
#113644=CARTESIAN_POINT ( 'NONE',  ( 0.1333542156527140476, 0.7077123155428012291, -2.127987941987404596 ) ) ;
#113645=CARTESIAN_POINT ( 'NONE',  ( 6.005383971424570255, -1.826508537601937432, 0.2321369796495567073 ) ) ;
#113649=CARTESIAN_POINT ( 'NONE',  ( 1.553258647468837461, 0.5056154618373939202, -1.648988316134043286 ) ) ;
#113650=CARTESIAN_POINT ( 'NONE',  ( 1.464077725791514517, -1.074659653367866952, 1.706114136832518779 ) ) ;
#113651=CARTESIAN_POINT ( 'NONE',  ( 1.741309990946012132, 2.292119649597070374, -0.1747640694012199680 ) ) ;
#113653=CARTESIAN_POINT ( 'NONE',  ( 1.933286576697599513, 0.2207578219815004572, 2.251582216785783075 ) ) ;
#113654=CARTESIAN_POINT ( 'NONE',  ( 4.670599442626208742, -1.376304852316366789, 1.594240983682773782 ) ) ;
#113656=CARTESIAN_POINT ( 'NONE',  ( 2.125891686596991903, 1.023501848097716493, -1.443529828085978739 ) ) ;
#113662=CARTESIAN_POINT ( 'NONE',  ( 6.504121277450023442, -0.9500910533294173455, 2.005660710250598555 ) ) ;
#113663=CARTESIAN_POINT ( 'NONE',  ( 3.029421956395737858, -1.472182739719897215, -1.623467934892895759 ) ) ;
#113670=CARTESIAN_POINT ( 'NONE',  ( 5.941668366282724101, -1.996146358238064522, 0.7160658055916299114 ) ) ;
#113680=CARTESIAN_POINT ( 'NONE',  ( 2.313636755748917473, 1.135937956827288042, -1.318730690005095241 ) ) ;
#113682=( GEOMETRIC_REPRESENTATION_CONTEXT ( 3 ) GLOBAL_UNCERTAINTY_ASSIGNED_CONTEXT ( ( #48658 ) ) GLOBAL_UNIT_ASSIGNED_CONTEXT ( ( #131175, #2, #117047 ) ) REPRESENTATION_CONTEXT ( 'NONE', 'WORKASPACE' ) );
#113686=CARTESIAN_POINT ( 'NONE',  ( 6.789893189004300389, -0.9291300992274166282, 1.949920244826188309 ) ) ;
#113691=CARTESIAN_POINT ( 'NONE',  ( 6.069229152942410721, 0.1638285306290178100, -2.155560115052157055 ) ) ;
#113695=CARTESIAN_POINT ( 'NONE',  ( 5.835224730271552751, -1.783237572924928127, 0.8406590917669158891 ) ) ;
#113696=CARTESIAN_POINT ( 'NONE',  ( 4.903498277369322977, 0.2971982615034232111, 1.707963748468165122 ) ) ;
#113698=CARTESIAN_POINT ( 'NONE',  ( 2.507599501126521524, -2.167277876680247850, 0.3246147914140809498 ) ) ;
#113699=CARTESIAN_POINT ( 'NONE',  ( 3.698509654486553000, -2.304784958540738060, -0.1161927354758583580 ) ) ;
#113700=CARTESIAN_POINT ( 'NONE',  ( 6.327427223165448922, -1.941958050844143413, 0.6900897555163245656 ) ) ;
#113701=CARTESIAN_POINT ( 'NONE',  ( 1.622886899410342254, -1.828648197406743670, 0.6539591521299585875 ) ) ;
#113705=CARTESIAN_POINT ( 'NONE',  ( 3.885109016898561585, -1.979880364965879380, -0.7601140796509860964 ) ) ;
#113707=CARTESIAN_POINT ( 'NONE',  ( 2.039685609654022347, -1.556907966322677472, 1.281362143053674130 ) ) ;
#113709=CARTESIAN_POINT ( 'NONE',  ( 4.805825877545530922, -0.5924843665619135002, 2.125676689404366826 ) ) ;
#113712=CARTESIAN_POINT ( 'NONE',  ( -0.005637892868452093476, -0.3948761927005627337, -1.788892068844874395 ) ) ;
#113718=CARTESIAN_POINT ( 'NONE',  ( 4.803620198249330286, -0.5517947341296326469, 1.985563166520041278 ) ) ;
#113723=CARTESIAN_POINT ( 'NONE',  ( 3.527994226718012438, -1.989412488823691483, 0.3473740275561196245 ) ) ;
#113727=CARTESIAN_POINT ( 'NONE',  ( 3.450122203709057533, 2.061077815303002936, 0.001625369314967386580 ) ) ;
#113730=CARTESIAN_POINT ( 'NONE',  ( -0.2409995289980246813, 5.721856934700204178, -2.594540323675114113 ) ) ;
#113731=CARTESIAN_POINT ( 'NONE',  ( 1.728195974063054141, 0.1793598003074353686, 1.832383557197496460 ) ) ;
#113732=CARTESIAN_POINT ( 'NONE',  ( 6.621690180768193379, -2.141820631849135292, 0.5315211216728524812 ) ) ;
#113734=CARTESIAN_POINT ( 'NONE',  ( 2.460438939752377152, 0.9218109643280818499, 1.955300211207489758 ) ) ;
#113736=CARTESIAN_POINT ( 'NONE',  ( 1.446500318503377125, -1.422605717829699801, 1.429450658469958668 ) ) ;
#113737=CARTESIAN_POINT ( 'NONE',  ( 2.513387927098627905, 2.297807174607501057, 0.05796762653747893068 ) ) ;
#113741=CARTESIAN_POINT ( 'NONE',  ( 5.049669536805332370, 0.6190787695102616395, -1.871797661314599015 ) ) ;
#113742=CARTESIAN_POINT ( 'NONE',  ( 4.100796195634116792, 1.845626398921360822, 0.8128187495666516771 ) ) ;
#113746=CARTESIAN_POINT ( 'NONE',  ( 6.674446291637649686, -1.297315479741867117, 1.659578660624160706 ) ) ;
#113748=CARTESIAN_POINT ( 'NONE',  ( 6.883263157960362477, -0.004191378316371896506, 2.053658919477070910 ) ) ;
#113752=CARTESIAN_POINT ( 'NONE',  ( 4.276219423538512032, -1.135946514926335915, 1.611120745738093385 ) ) ;
#113753=CARTESIAN_POINT ( 'NONE',  ( 6.469012451414649867, -1.558587985773008278, 1.284399031846704009 ) ) ;
#113755=CARTESIAN_POINT ( 'NONE',  ( 4.494930827260392725, -0.5027447494639860626, -2.252120713733107404 ) ) ;
#113756=CARTESIAN_POINT ( 'NONE',  ( 2.465751394709358113, -0.4561089685623443968, 2.011347002571160836 ) ) ;
#113764=CARTESIAN_POINT ( 'NONE',  ( 3.736941271748619009, -2.091586689864731063, -0.5821943698010292323 ) ) ;
#113767=CARTESIAN_POINT ( 'NONE',  ( 2.735704033801298785, 1.827604811068459956, 0.2230458208379028362 ) ) ;
#113769=CARTESIAN_POINT ( 'NONE',  ( 5.829655996829377962, 1.081331853127937448, -1.906115348727636549 ) ) ;
#113771=CARTESIAN_POINT ( 'NONE',  ( 5.559536883401111851, 0.4474127746876849221, -2.217688626266269392 ) ) ;
#113776=CARTESIAN_POINT ( 'NONE',  ( 6.538360807962172672, 1.750891970090788119, 0.2567797125347607845 ) ) ;
#113778=CARTESIAN_POINT ( 'NONE',  ( 4.494793336055456834, -1.953237823851183164, -0.4868166104980836684 ) ) ;
#113780=CARTESIAN_POINT ( 'NONE',  ( 3.294068349240862226, -0.8549715976811816942, 1.924793576080959578 ) ) ;
#113781=CARTESIAN_POINT ( 'NONE',  ( 2.249496223418820939, 1.878159554852454338, -0.3759676508649934523 ) ) ;
#113783=CARTESIAN_POINT ( 'NONE',  ( 2.805082309988204514, -1.639025760435019130, 1.091792480472515647 ) ) ;
#113784=CARTESIAN_POINT ( 'NONE',  ( 1.147088892781012781, -1.472398045354219365, -1.153743250124287689 ) ) ;
#113785=CARTESIAN_POINT ( 'NONE',  ( 1.609737659951641309, 0.5726723138891121057, -1.876404140693301414 ) ) ;
#113786=CARTESIAN_POINT ( 'NONE',  ( 3.545241905100663615, -1.307145164029408502, -1.125523404956897178 ) ) ;
#113787=CARTESIAN_POINT ( 'NONE',  ( 0.2461629937395051204, 0.9812432698282257393, -1.641294572782559413 ) ) ;
#113789=CARTESIAN_POINT ( 'NONE',  ( 1.102499568101540817, -2.207063161980229005, 0.003256074490760872773 ) ) ;
#113792=CARTESIAN_POINT ( 'NONE',  ( 6.596569749568344854, -0.5012203084251048990, -1.802199723311518786 ) ) ;
#113797=CARTESIAN_POINT ( 'NONE',  ( 0.9946828900261883710, 2.039433816042154124, 0.3556643922909968891 ) ) ;
#113802=CARTESIAN_POINT ( 'NONE',  ( 5.356147330077114077, 0.8591290142025626020, -1.938821108677920346 ) ) ;
#113808=CARTESIAN_POINT ( 'NONE',  ( 6.760214184729610665, -1.961454122871961747, 0.04698431645466792650 ) ) ;
#113811=CARTESIAN_POINT ( 'NONE',  ( 4.727888646976695419, -1.799647678597478206, -0.9090046787488814672 ) ) ;
#113812=CARTESIAN_POINT ( 'NONE',  ( 4.188635153834672664, 1.476993813991718918, -1.219978962091677221 ) ) ;
#113814=CARTESIAN_POINT ( 'NONE',  ( 2.015410700679621137, -2.124826835150806392, 0.5361769018528695918 ) ) ;
#113816=CARTESIAN_POINT ( 'NONE',  ( 3.356579238971897805, -1.418645411611328067, 1.219307012350186126 ) ) ;
#113821=CARTESIAN_POINT ( 'NONE',  ( 5.413701396201449079, -1.343708383727526101, -1.636158592728423455 ) ) ;
#113823=CARTESIAN_POINT ( 'NONE',  ( 2.841443172333203204, 0.7501175549536406306, -1.951742197369815912 ) ) ;
#113825=CARTESIAN_POINT ( 'NONE',  ( 1.184105695005283287, -1.681391461502951046, -0.3836232258775870152 ) ) ;
#113837=ORIENTED_EDGE ( 'NONE', *, *, #45569, .T. ) ;
#113839=CARTESIAN_POINT ( 'NONE',  ( 1.980848084912645524, -1.656539610615878955, -0.7334085510423118404 ) ) ;
#113843=CARTESIAN_POINT ( 'NONE',  ( 6.539320575229250032, 4.701774335136183147, 2.359470009949143243 ) ) ;
#113848=CARTESIAN_POINT ( 'NONE',  ( 3.138934141195717675, -0.1340819638860979157, -1.856265897873999426 ) ) ;
#113850=CARTESIAN_POINT ( 'NONE',  ( 0.9662486314009374189, -1.869180826568194398, -0.4184218257623931181 ) ) ;
#113851=CARTESIAN_POINT ( 'NONE',  ( 6.739296538182359519, -1.720230304288400625, 0.8672215684524892110 ) ) ;
#113858=CARTESIAN_POINT ( 'NONE',  ( 4.768383308330760961, -0.8382467442454040185, -1.782262242837754807 ) ) ;
#113859=CARTESIAN_POINT ( 'NONE',  ( 1.946092837771850492, -1.387361170020007695, -1.603719225630481970 ) ) ;
#113863=CARTESIAN_POINT ( 'NONE',  ( 5.525378525699438548, -1.388074942811763357, -1.695776126864618316 ) ) ;
#113864=CARTESIAN_POINT ( 'NONE',  ( 4.700175447307747945, -1.925963193209312418, -0.04779502591981815707 ) ) ;
#113866=CARTESIAN_POINT ( 'NONE',  ( 0.5162701059127188241, 1.262803565755654001, -1.318596375272471199 ) ) ;
#113867=CARTESIAN_POINT ( 'NONE',  ( 1.243116305521356990, 0.4334984505205765060, 2.163720904216937857 ) ) ;
#113869=CARTESIAN_POINT ( 'NONE',  ( 0.01762790050853849447, -0.5081247445114078776, 1.843608005305336528 ) ) ;
#113873=CARTESIAN_POINT ( 'NONE',  ( 6.508657463561863921, 0.6146053541861602465, 1.871187945041019152 ) ) ;
#113874=CARTESIAN_POINT ( 'NONE',  ( 2.032666248472639214, -1.733752323498815029, 0.8752225562490000277 ) ) ;
#113875=CARTESIAN_POINT ( 'NONE',  ( 6.345094440775825184, -1.237889906630392334, 1.936425090000978289 ) ) ;
#113877=CARTESIAN_POINT ( 'NONE',  ( 5.735155330654303718, -0.04388460642621531960, -1.860581820771879835 ) ) ;
#113883=CARTESIAN_POINT ( 'NONE',  ( 1.048660896456204528, -1.724490848714568259, 1.352309724062021878 ) ) ;
#113888=CARTESIAN_POINT ( 'NONE',  ( 1.857752496991037061, 1.820901040755190214, -0.1330985588276211995 ) ) ;
#113891=CARTESIAN_POINT ( 'NONE',  ( 6.609000000000018638, 2.976782768882420438, 2.353557172130323227 ) ) ;
#113894=CARTESIAN_POINT ( 'NONE',  ( 6.621730190220365131, -1.769489810573118049, 0.4491385735008179836 ) ) ;
#113895=CARTESIAN_POINT ( 'NONE',  ( 4.205873059901494848, 0.6649649114027419428, -1.845726756006949909 ) ) ;
#113899=CARTESIAN_POINT ( 'NONE',  ( 4.388337494309430653, -0.4807229498768311182, -2.138019847805587403 ) ) ;
#113901=CARTESIAN_POINT ( 'NONE',  ( 4.258688845354158481, -0.6446009455991276171, -1.967446834807617284 ) ) ;
#113905=CARTESIAN_POINT ( 'NONE',  ( 4.061395409788411293, -1.323216277904919691, 1.879509618897465817 ) ) ;
#113909=CARTESIAN_POINT ( 'NONE',  ( 6.620655732516644854, 2.103946135090263514, 2.037628900882877847 ) ) ;
#113911=CARTESIAN_POINT ( 'NONE',  ( 3.679572934066538181, -0.9564393601015194202, 1.690012426612282681 ) ) ;
#113914=CARTESIAN_POINT ( 'NONE',  ( 3.656429697474584017, 1.903630103707624865, 0.1825790434749063051 ) ) ;
#113916=CARTESIAN_POINT ( 'NONE',  ( 5.719686907728898539, -1.681737053624256628, 0.3821217278023018582 ) ) ;
#113917=CARTESIAN_POINT ( 'NONE',  ( 4.030482632556767975, 0.5424685788828055300, 1.942097399793737411 ) ) ;
#113918=CARTESIAN_POINT ( 'NONE',  ( 4.606216143772843274, -0.1140155944862955434, 2.295953707746749117 ) ) ;
#113920=CARTESIAN_POINT ( 'NONE',  ( 1.155211076828046579, -1.737760091701185505, 1.360235214042208263 ) ) ;
#113923=CARTESIAN_POINT ( 'NONE',  ( 5.993352163831329626, 1.341162022463908032, 1.154712335393495160 ) ) ;
#113925=CARTESIAN_POINT ( 'NONE',  ( 1.641004737452517626, -1.934627630680013199, 1.229243952562808939 ) ) ;
#113926=CARTESIAN_POINT ( 'NONE',  ( 1.235833198037468827, 0.3363826672934740469, 1.707315539672292104 ) ) ;
#113928=CARTESIAN_POINT ( 'NONE',  ( 0.7019813383442319310, -1.220362748482771487, -1.231932065070516558 ) ) ;
#113931=CARTESIAN_POINT ( 'NONE',  ( 1.100314673101766338, 0.8801652113111978482, -1.984954624234806175 ) ) ;
#113932=CARTESIAN_POINT ( 'NONE',  ( 2.114470590943520634, 1.957170936680457052, 0.4852650170619755565 ) ) ;
#113934=CARTESIAN_POINT ( 'NONE',  ( 0.1648913374791864117, -1.719061530832368234, -0.8695707864920312335 ) ) ;
#113937=CARTESIAN_POINT ( 'NONE',  ( 1.828696429707490578, -1.052382519090878654, -1.956348917980913260 ) ) ;
#113943=CARTESIAN_POINT ( 'NONE',  ( 5.583501753226309816, -0.7750115735715494836, 1.558442325393385897 ) ) ;
#113944=CARTESIAN_POINT ( 'NONE',  ( 3.560947883890089649, 1.548132398191165882, -1.204989647596923730 ) ) ;
#113949=CARTESIAN_POINT ( 'NONE',  ( 5.149841461411730492, 0.7164311094934887603, -2.146032026599023812 ) ) ;
#113950=CARTESIAN_POINT ( 'NONE',  ( 1.275913394178169957, -2.012872700982801355, 0.4499014461352250360 ) ) ;
#113952=CARTESIAN_POINT ( 'NONE',  ( 1.991474686832030994, 1.968180706754483644, -1.115757519136374221 ) ) ;
#113955=CARTESIAN_POINT ( 'NONE',  ( 2.864352374448192240, -1.292745417840788003, 1.352161534859085412 ) ) ;
#113956=CARTESIAN_POINT ( 'NONE',  ( 1.336079928753497681, 0.5043104442001166143, -1.659204044645303355 ) ) ;
#113957=CARTESIAN_POINT ( 'NONE',  ( 5.249643141573060667, 2.189086832579402842, -0.1069518675670885766 ) ) ;
#113958=CARTESIAN_POINT ( 'NONE',  ( 6.598638948628339662, -0.6063221841578874116, -2.226463007350306444 ) ) ;
#113959=CARTESIAN_POINT ( 'NONE',  ( 4.223607183596161718, -2.069420184152844566, 0.6248923283326962563 ) ) ;
#113960=CARTESIAN_POINT ( 'NONE',  ( 4.206929537583108392, -0.3307808895044571651, 1.913420690662092305 ) ) ;
#113962=CARTESIAN_POINT ( 'NONE',  ( 6.362560269511371658, -1.322780316340057549, 1.322825847358683138 ) ) ;
#113963=CARTESIAN_POINT ( 'NONE',  ( 1.843750000000001332, 1.895863743164127868, 0.7852924748298895086 ) ) ;
#113969=CARTESIAN_POINT ( 'NONE',  ( 5.537732479266092689, -1.587839044716709669, 1.242724925242834066 ) ) ;
#113973=CARTESIAN_POINT ( 'NONE',  ( 3.686012862905340803, -0.8985999850123352894, 1.589152278004740237 ) ) ;
#113980=CARTESIAN_POINT ( 'NONE',  ( 6.463536886191197262, -1.623326069159360063, -1.201424211086026261 ) ) ;
#113981=CARTESIAN_POINT ( 'NONE',  ( 0.6102159345307588412, -0.7594153588383574238, 1.980023364433493693 ) ) ;
#113986=CARTESIAN_POINT ( 'NONE',  ( 6.754767742037871336, -1.594745458351163103, 1.305156173170081813 ) ) ;
#113997=CARTESIAN_POINT ( 'NONE',  ( 5.747422657745248742, -1.966344092054626680, -0.4444320411668146731 ) ) ;
#113998=CARTESIAN_POINT ( 'NONE',  ( 5.226429366918344144, 0.1390423275269437320, 1.835946739075666745 ) ) ;
#114000=CARTESIAN_POINT ( 'NONE',  ( 3.036059619770274498, -1.550059391276232601, -1.709768245815939780 ) ) ;
#114002=CARTESIAN_POINT ( 'NONE',  ( 6.028642311625867833, 2.081422104948245533, 0.5829617784755269927 ) ) ;
#114004=CARTESIAN_POINT ( 'NONE',  ( 1.048265877425518688, -1.530107816300673829, 1.195853197770081255 ) ) ;
#114008=CARTESIAN_POINT ( 'NONE',  ( 4.640180047935675844, 0.006009439367033602396, -2.298542322207643984 ) ) ;
#114011=CARTESIAN_POINT ( 'NONE',  ( 4.240975883383619305, -1.627667033997456381, 0.9218181776217827528 ) ) ;
#114012=CARTESIAN_POINT ( 'NONE',  ( 0.9668906521006037647, -1.505869814250645478, 1.178657042999963878 ) ) ;
#114015=CARTESIAN_POINT ( 'NONE',  ( 2.561379550486083012, -1.920685204893451292, -1.086737900330703166 ) ) ;
#114021=CARTESIAN_POINT ( 'NONE',  ( 1.510939727685528311, 1.736590689682067756, 0.9330581202648262629 ) ) ;
#114022=CARTESIAN_POINT ( 'NONE',  ( 1.220229771213819481, -2.250799921053967090, 0.5081616799173671595 ) ) ;
#114023=CARTESIAN_POINT ( 'NONE',  ( 1.926150285298435572, 1.005797860886543660, 1.684270608208485065 ) ) ;
#114024=CARTESIAN_POINT ( 'NONE',  ( 5.453991371731997440, -0.7473993133914544895, 1.922551457666883401 ) ) ;
#114033=CARTESIAN_POINT ( 'NONE',  ( 0.3390589225593713674, -2.105617620008819468, -0.5285623031292383533 ) ) ;
#114035=CARTESIAN_POINT ( 'NONE',  ( 6.374545129912787544, -0.09763137639631430664, -1.838803627010993313 ) ) ;
#114038=CARTESIAN_POINT ( 'NONE',  ( 1.229531971273215341, -1.182229855178434930, -1.449605969065965949 ) ) ;
#114040=CARTESIAN_POINT ( 'NONE',  ( 5.554052124568397808, 2.159397089200214559, -0.09991998142631913771 ) ) ;
#114044=CARTESIAN_POINT ( 'NONE',  ( 1.928230879603441750, -0.9027140558476205445, -1.685813393195116694 ) ) ;
#114045=CARTESIAN_POINT ( 'NONE',  ( 3.555294528146099697, 0.4307136429906773256, -1.716485385381610662 ) ) ;
#114046=CARTESIAN_POINT ( 'NONE',  ( 0.9789966485893276671, -1.729064073676725544, -0.8170501332188941923 ) ) ;
#114048=CARTESIAN_POINT ( 'NONE',  ( 4.974201611368001430, -1.901669438865726924, -0.2299391999119395624 ) ) ;
#114050=CARTESIAN_POINT ( 'NONE',  ( 6.232857221494619182, -1.869652508273983882, -0.6194465747909986275 ) ) ;
#114052=CARTESIAN_POINT ( 'NONE',  ( 1.230900525853476868, 1.420129835883350955, -1.575055732827963295 ) ) ;
#114054=CARTESIAN_POINT ( 'NONE',  ( 4.574985519202336981, -0.0001439422951596270033, -1.870836309977530920 ) ) ;
#114055=CARTESIAN_POINT ( 'NONE',  ( 0.1526014871912773629, -1.468541917219987836, 1.084465738218153064 ) ) ;
#114057=CARTESIAN_POINT ( 'NONE',  ( 5.039771180630152614, -1.558841386063321455, -1.562417271110942307 ) ) ;
#114061=CARTESIAN_POINT ( 'NONE',  ( 1.592308366680051490, 1.018618965756763473, -1.793563681512408525 ) ) ;
#114069=CARTESIAN_POINT ( 'NONE',  ( 3.754400092289136737, -2.067862582909282487, -0.1045053291982081939 ) ) ;
#114071=CARTESIAN_POINT ( 'NONE',  ( 1.106953007505812492, 1.637591863572019690, -1.411084338363017832 ) ) ;
#114073=CARTESIAN_POINT ( 'NONE',  ( 2.156904581142269350, 0.4447176379400120672, 1.969927323211942083 ) ) ;
#114076=EDGE_LOOP ( 'NONE', ( #753, #183229, #61253, #90057 ) ) ;
#114081=CARTESIAN_POINT ( 'NONE',  ( 0.2511858651975951151, 0.1928294586405615574, -2.007256720055437871 ) ) ;
#114082=CARTESIAN_POINT ( 'NONE',  ( 5.091441847573507040, -0.7891374179831471825, 2.044738775321436997 ) ) ;
#114084=CARTESIAN_POINT ( 'NONE',  ( 4.781465250580236415, 0.1816826923375300662, -1.903719681147630016 ) ) ;
#114088=CARTESIAN_POINT ( 'NONE',  ( 2.724232643812212196, 2.001515029240468646, 0.2440086781289458329 ) ) ;
#114090=CARTESIAN_POINT ( 'NONE',  ( 0.02941885139840036759, -2.092310700284722103, 0.9370380844745775928 ) ) ;
#114092=CARTESIAN_POINT ( 'NONE',  ( 4.102375631063598149, -0.5418327121037533889, -1.637530703111476305 ) ) ;
#114097=PLANE ( 'NONE',  #54555 ) ;
#114099=CARTESIAN_POINT ( 'NONE',  ( 5.356058406599743194, 0.7285399314688314476, -1.658701577940960847 ) ) ;
#114104=CARTESIAN_POINT ( 'NONE',  ( 5.707607943424125807, 1.375951858612366019, 1.178334608346263579 ) ) ;
#114107=CARTESIAN_POINT ( 'NONE',  ( 3.275498427308475069, 1.390425696708731396, 1.693851754907250928 ) ) ;
#114108=CARTESIAN_POINT ( 'NONE',  ( 5.758217292028081857, -1.861241882002647285, 0.0004304118630827496474 ) ) ;
#114110=CARTESIAN_POINT ( 'NONE',  ( 3.919475720687201736, -1.323675617205988475, -1.384941642318695987 ) ) ;
#114118=CARTESIAN_POINT ( 'NONE',  ( 0.3214396764580421118, -0.1044536432763705502, 2.159311484102262479 ) ) ;
#114121=CARTESIAN_POINT ( 'NONE',  ( 2.520284954824199453, 1.194270260598716771, -1.380820861806408617 ) ) ;
#114123=CARTESIAN_POINT ( 'NONE',  ( 4.014527796464135712, 1.291161025869846712, -1.290856679043244970 ) ) ;
#114126=CARTESIAN_POINT ( 'NONE',  ( 3.684007040126308752, -1.171275171843730867, -1.583282632743492790 ) ) ;
#114128=CARTESIAN_POINT ( 'NONE',  ( 4.634287131779754709, 0.3355949523314147309, 1.912704035658734592 ) ) ;
#114132=CARTESIAN_POINT ( 'NONE',  ( 5.502226937873657242, -0.9515977829631333540, 1.895136135177949877 ) ) ;
#114134=CARTESIAN_POINT ( 'NONE',  ( 2.596233987490266681, -0.9813665562012074961, 1.641104690102652919 ) ) ;
#114139=CARTESIAN_POINT ( 'NONE',  ( 4.600248117428091810, -0.9470982757478171310, 1.776368884175743235 ) ) ;
#114141=CARTESIAN_POINT ( 'NONE',  ( 4.934128534657983067, 0.9357288403324083292, -1.567518238613223813 ) ) ;
#114142=CARTESIAN_POINT ( 'NONE',  ( 0.3442982867475213871, -0.9772804826688463731, 1.825211318103404867 ) ) ;
#114146=CARTESIAN_POINT ( 'NONE',  ( 6.069203928793593050, 0.1358119448514639727, -1.865795782587629681 ) ) ;
#114156=CARTESIAN_POINT ( 'NONE',  ( 0.9892257793299992219, 0.1485654903058269416, 2.064951490685583924 ) ) ;
#114157=CARTESIAN_POINT ( 'NONE',  ( 1.880608475893473353, -0.5680388087716014001, -2.039528425668888811 ) ) ;
#114160=CARTESIAN_POINT ( 'NONE',  ( 0.7780955915308949145, -1.048793665676364562, -1.666747765972796946 ) ) ;
#114165=CARTESIAN_POINT ( 'NONE',  ( 2.502247188656173016, -0.8787990176886916194, -2.117303525603573267 ) ) ;
#114166=CARTESIAN_POINT ( 'NONE',  ( 1.066719475142904994, -1.649486405746130258, -0.7827983987617056494 ) ) ;
#114167=CARTESIAN_POINT ( 'NONE',  ( 2.056764645581514728, 0.4224895836346024280, 1.864965418913032913 ) ) ;
#114170=CARTESIAN_POINT ( 'NONE',  ( 1.371341259694250247, -1.728764894987804057, -1.031425992479652720 ) ) ;
#114171=CARTESIAN_POINT ( 'NONE',  ( 1.129655866247070595, 1.892139549451707037, -0.5178372573612434193 ) ) ;
#114175=CARTESIAN_POINT ( 'NONE',  ( 4.347661206880347073, 2.090185315053775472, -0.05106478779118817091 ) ) ;
#114176=CARTESIAN_POINT ( 'NONE',  ( 2.008344819247428248, 1.313797796480600244, -1.186068062872788209 ) ) ;
#114179=CARTESIAN_POINT ( 'NONE',  ( 5.244168061255013669, 0.6613091839676830119, 2.194790591360805898 ) ) ;
#114180=CARTESIAN_POINT ( 'NONE',  ( 4.997892061590047952, -0.5910035050068825901, -1.637047790839076589 ) ) ;
#114182=CARTESIAN_POINT ( 'NONE',  ( 4.165211049733441584, -0.5436426828948260903, -1.646488866570811060 ) ) ;
#114183=CARTESIAN_POINT ( 'NONE',  ( 4.193918837840154623, -1.494357529231920889, -1.575321265833210305 ) ) ;
#114185=CARTESIAN_POINT ( 'NONE',  ( 6.122279814772176643, 1.995267444086584296, 0.2910868170948808786 ) ) ;
#114186=CARTESIAN_POINT ( 'NONE',  ( 1.156250000000000888, -1.895863743164063031, 0.7852924748300492697 ) ) ;
#114188=CARTESIAN_POINT ( 'NONE',  ( 3.750929837476246753, -1.575545889128293853, 1.108190883620339795 ) ) ;
#114190=CARTESIAN_POINT ( 'NONE',  ( 5.818639523836858451, -0.7989930759073891053, -2.072897825184773168 ) ) ;
#114192=CARTESIAN_POINT ( 'NONE',  ( 6.983263157960378997, 2.960795523694306652, 2.498903865360342369 ) ) ;
#114195=CARTESIAN_POINT ( 'NONE',  ( 1.278328015487300462, 2.187630646761177466, -0.3845124374818161828 ) ) ;
#114204=CARTESIAN_POINT ( 'NONE',  ( 4.475086314992714698, 1.884572246790953365, 0.8388810360253369236 ) ) ;
#114208=CARTESIAN_POINT ( 'NONE',  ( 0.5964902553294594290, 1.476022596236561846, -0.9760666246667221158 ) ) ;
#114209=CARTESIAN_POINT ( 'NONE',  ( 5.309090426574582189, 1.026673973311197585, -1.397408945856312590 ) ) ;
#114210=CARTESIAN_POINT ( 'NONE',  ( 4.651753270297207976, 0.6719488171132372845, 1.605710474869048499 ) ) ;
#114212=CARTESIAN_POINT ( 'NONE',  ( 2.806493257264990326, 1.658461721128750677, -1.582772817771603169 ) ) ;
#114214=CARTESIAN_POINT ( 'NONE',  ( 1.482094074889642288, -0.2687121449159133313, -1.821302815977184686 ) ) ;
#114216=CARTESIAN_POINT ( 'NONE',  ( 1.535882326342351334, 0.9031702520058831896, -1.586444745400449108 ) ) ;
#114217=CARTESIAN_POINT ( 'NONE',  ( 2.549454116737331244, -1.388485404012842261, 1.462446031800922253 ) ) ;
#114218=CARTESIAN_POINT ( 'NONE',  ( 1.500213180713722450, -0.7911926984936793472, -2.043816727864488314 ) ) ;
#114220=CARTESIAN_POINT ( 'NONE',  ( 4.788165231579453618, -0.9949995658048852443, 1.856088619770781989 ) ) ;
#114223=CARTESIAN_POINT ( 'NONE',  ( 1.240778115703184303, -2.019486815914430355, -0.4554155650244652853 ) ) ;
#114226=CARTESIAN_POINT ( 'NONE',  ( 3.229257539231108698, 1.917844101178723504, 0.9048822562475050679 ) ) ;
#114228=CARTESIAN_POINT ( 'NONE',  ( 6.709597972018079837, -0.3944863986210072060, 1.789098616620278470 ) ) ;
#114235=CARTESIAN_POINT ( 'NONE',  ( 3.041275741140234246, 0.05373089442234183638, 2.019258232931480546 ) ) ;
#114236=CARTESIAN_POINT ( 'NONE',  ( 0.6750070354940709283, -1.982970624965023410, -0.7094951434080811747 ) ) ;
#114239=CARTESIAN_POINT ( 'NONE',  ( 5.471493298581291853, -0.2749614684036653656, 1.840407035693031546 ) ) ;
#114245=CARTESIAN_POINT ( 'NONE',  ( 6.438362351209899082, 2.038089008908655853, 0.3048918457534201543 ) ) ;
#114250=CARTESIAN_POINT ( 'NONE',  ( 2.389626358114539162, -0.004507738041977306029, 1.734034291262590788 ) ) ;
#114251=CARTESIAN_POINT ( 'NONE',  ( 0.8666887897643248406, 1.678224016273874852, -0.4604494717724941233 ) ) ;
#114252=CARTESIAN_POINT ( 'NONE',  ( 0.2535066641492569883, -1.850528970283831010, 1.378429844982787422 ) ) ;
#114255=CARTESIAN_POINT ( 'NONE',  ( 2.284514177335088991, -2.020382039854185408, -0.4051362335234820478 ) ) ;
#114257=CARTESIAN_POINT ( 'NONE',  ( 1.722029606037442040, -1.727736752315935265, -1.038835718801443653 ) ) ;
#114260=CARTESIAN_POINT ( 'NONE',  ( 1.340630715518615679, 0.3825088487559283323, 1.933841885654476567 ) ) ;
#114261=CARTESIAN_POINT ( 'NONE',  ( 4.886922752366290368, -1.802716094696995786, -0.6387714794457154399 ) ) ;
#114264=CARTESIAN_POINT ( 'NONE',  ( 6.305322857734435793, 1.832379230283949667, 1.229636283518860118 ) ) ;
#114268=CARTESIAN_POINT ( 'NONE',  ( 0.5045642862554244878, -2.004696059604444081, -0.2448167134727705085 ) ) ;
#114269=CARTESIAN_POINT ( 'NONE',  ( 4.243447643126375013, -2.009724547103900250, 1.133870999951855696 ) ) ;
#114270=CARTESIAN_POINT ( 'NONE',  ( 6.268018250734934682, -1.947192974725008963, 0.2387856323943157166 ) ) ;
#114271=CARTESIAN_POINT ( 'NONE',  ( 1.498799732657706718, 0.3773721054241683248, 1.924948185394937283 ) ) ;
#114275=CARTESIAN_POINT ( 'NONE',  ( 0.1283146926199127957, 2.112135570198115708, 0.1490006669643220705 ) ) ;
#114278=CARTESIAN_POINT ( 'NONE',  ( 0.9195641160042143936, 1.098457714822091091, -1.477412082521646575 ) ) ;
#114280=CARTESIAN_POINT ( 'NONE',  ( 4.452125263715247527, -0.8365346480432279686, 2.003629037444945471 ) ) ;
#114283=CARTESIAN_POINT ( 'NONE',  ( 1.476976393720278002, -1.495863523836362896, 1.503369785937097136 ) ) ;
#114287=CARTESIAN_POINT ( 'NONE',  ( 2.864585088123726919, -1.423607738919046906, 1.490243374215278971 ) ) ;
#114289=CARTESIAN_POINT ( 'NONE',  ( 0.5382993156314471728, -1.579489783069366604, 0.9460463261394758128 ) ) ;
#114291=CARTESIAN_POINT ( 'NONE',  ( 0.07775346131144718342, 5.719027203068962173, -2.882954358279002260 ) ) ;
#114294=CARTESIAN_POINT ( 'NONE',  ( 1.458695031449417590, 0.9167444482420561425, 2.068505399879524642 ) ) ;
#114296=CARTESIAN_POINT ( 'NONE',  ( 1.160107992948592237, 1.809582681877516697, 0.08717244660690416647 ) ) ;
#114297=CARTESIAN_POINT ( 'NONE',  ( 2.325271742496349159, -1.422496398144998508, -1.283381434195222326 ) ) ;
#114298=CARTESIAN_POINT ( 'NONE',  ( 3.297389726143421740, -1.827171938055579536, 0.9735347560282039403 ) ) ;
#114300=CARTESIAN_POINT ( 'NONE',  ( 2.114083122616668309, -0.9278515453300213434, -1.739463596305758974 ) ) ;
#114301=CARTESIAN_POINT ( 'NONE',  ( 5.320897925068237555, 1.780805307305334040, 0.7354040419824976471 ) ) ;
#114303=CARTESIAN_POINT ( 'NONE',  ( 1.155362744787872931, -1.816424715318950112, 1.423309470994944537 ) ) ;
#114306=CARTESIAN_POINT ( 'NONE',  ( 4.984863162817260829, 1.972918577937707196, 0.6018043753471848945 ) ) ;
#114310=CARTESIAN_POINT ( 'NONE',  ( 6.018611168240656006, 1.417078199399327332, -1.558035186251781612 ) ) ;
#114312=CARTESIAN_POINT ( 'NONE',  ( 4.710339443014814442, -0.9195336665917231977, -1.956380038831563972 ) ) ;
#114313=CARTESIAN_POINT ( 'NONE',  ( 4.969401683643670076, -1.707372507963246022, -1.078548144515010909 ) ) ;
#114321=CARTESIAN_POINT ( 'NONE',  ( 4.118375227313908482, 1.978554835517082555, 0.3886342876525810119 ) ) ;
#114326=CARTESIAN_POINT ( 'NONE',  ( 5.348557406608104969, 0.6236849695623291057, 2.069784783864880851 ) ) ;
#114332=CARTESIAN_POINT ( 'NONE',  ( 5.325796065338770369, 0.8146125389149364571, -1.844717355016491478 ) ) ;
#114334=CARTESIAN_POINT ( 'NONE',  ( 1.699380632523245449, -0.5835770076011400631, 1.623301926564212794 ) ) ;
#114339=CARTESIAN_POINT ( 'NONE',  ( 6.520764494017629254, 1.745421825204738431, 0.6730592012400560264 ) ) ;
#114340=CARTESIAN_POINT ( 'NONE',  ( 0.7857919059152475016, 1.939557017834290020, -0.5388494671653855095 ) ) ;
#114342=CARTESIAN_POINT ( 'NONE',  ( 2.889901548669851383, 1.559680528474843841, 1.561422205034967314 ) ) ;
#114346=CARTESIAN_POINT ( 'NONE',  ( 1.981254353800803836, -1.939921095825656305, -0.8566514584813913480 ) ) ;
#114347=CARTESIAN_POINT ( 'NONE',  ( 1.388296234047466049, -0.7283980888908546669, -1.880428666220852696 ) ) ;
#114348=CARTESIAN_POINT ( 'NONE',  ( 2.373076535756658778, -1.577936908029322849, -0.8897043057118164677 ) ) ;
#114351=CIRCLE ( 'NONE', #86593, 0.04999999999999970440 ) ;
#114354=CARTESIAN_POINT ( 'NONE',  ( -0.1357414145864926924, -1.858833624763186032, -0.4630600859806994762 ) ) ;
#114362=CARTESIAN_POINT ( 'NONE',  ( 4.716029918043215474, 1.032482702726954527, -1.731993998903176957 ) ) ;
#114363=CARTESIAN_POINT ( 'NONE',  ( 4.698204674003193304, -2.161138953124014161, -0.05634304724232848394 ) ) ;
#114366=CARTESIAN_POINT ( 'NONE',  ( 2.057031522680652369, 0.4693188842763912905, 2.067847215655476578 ) ) ;
#114368=CARTESIAN_POINT ( 'NONE',  ( 3.005103179519866607, 1.663439489741199928, 1.057676205593648167 ) ) ;
#114371=CARTESIAN_POINT ( 'NONE',  ( 6.742638201966631328, -1.931250359857048515, -0.3855633916233728309 ) ) ;
#114372=CARTESIAN_POINT ( 'NONE',  ( 1.534995247775998939, -1.406442930887800813, -1.339296560326202146 ) ) ;
#114377=CARTESIAN_POINT ( 'NONE',  ( 2.220754083240178645, 0.001034992482759621978, 2.090823719040376893 ) ) ;
#114381=CARTESIAN_POINT ( 'NONE',  ( 6.428373272941257710, -0.9058926715965059939, -1.684108486221975953 ) ) ;
#114383=CARTESIAN_POINT ( 'NONE',  ( 4.354274438496381627, 2.206422198305586058, -0.05263853172451230661 ) ) ;
#114384=CARTESIAN_POINT ( 'NONE',  ( 1.975870009618452050, 2.111717515986545113, -0.6407313945460398896 ) ) ;
#114386=CARTESIAN_POINT ( 'NONE',  ( 0.9086806230526077721, -0.4651930584498394916, -1.854694524013176693 ) ) ;
#114389=CARTESIAN_POINT ( 'NONE',  ( 4.123533666479628046, 0.2564666318346648377, -2.054367117340555549 ) ) ;
#114391=CARTESIAN_POINT ( 'NONE',  ( 1.235488887756378551, -1.954010380348418119, 0.9248176494114216384 ) ) ;
#114392=CARTESIAN_POINT ( 'NONE',  ( 3.351304529449970371, 0.5305821810032870234, -2.126252377916526992 ) ) ;
#114398=CARTESIAN_POINT ( 'NONE',  ( 6.539718741795587320, -1.333554142906383744, 1.108523769342983689 ) ) ;
#114400=CARTESIAN_POINT ( 'NONE',  ( 4.504778988403771223, 0.5471568804141565545, 1.996604337080605474 ) ) ;
#114401=CARTESIAN_POINT ( 'NONE',  ( 2.930207584894477080, 1.069882305642521514, -1.601919868193351082 ) ) ;
#114402=CARTESIAN_POINT ( 'NONE',  ( 6.116841120987044356, 0.2079722402913257440, 2.107011275531808003 ) ) ;
#114405=CARTESIAN_POINT ( 'NONE',  ( 4.504722179138310523, 0.5213129852876841053, 1.899149332505256638 ) ) ;
#114406=CARTESIAN_POINT ( 'NONE',  ( 5.912145817070847187, 1.543564834742835234, -1.694840376948128391 ) ) ;
#114407=CARTESIAN_POINT ( 'NONE',  ( 3.932112477472641920, 0.9751300899686901058, -1.543267412809447681 ) ) ;
#114413=CARTESIAN_POINT ( 'NONE',  ( 5.045186288489547977, 0.1525188484602090777, 2.007510047055609093 ) ) ;
#114414=CARTESIAN_POINT ( 'NONE',  ( 6.504485943970635731, -2.231000991611901352, 0.5533298437200293574 ) ) ;
#114415=CARTESIAN_POINT ( 'NONE',  ( 4.909014596843685574, -1.577992517845404619, 1.165349624694256958 ) ) ;
#114420=CARTESIAN_POINT ( 'NONE',  ( 0.2926706434557576064, 1.735970642146159371, -1.164857044846574707 ) ) ;
#114421=CARTESIAN_POINT ( 'NONE',  ( 6.086734230332795370, -0.2636980280019511902, -1.749942407053702409 ) ) ;
#114423=CARTESIAN_POINT ( 'NONE',  ( 5.894467665742915585, 1.586334124781592969, -1.119885764912365467 ) ) ;
#114424=CARTESIAN_POINT ( 'NONE',  ( 1.834175572193702530, 2.167931929539984814, 0.3193665180123914094 ) ) ;
#114425=CARTESIAN_POINT ( 'NONE',  ( 0.5732861554464663278, -0.9687841611035786782, 1.445654263422226027 ) ) ;
#114428=CARTESIAN_POINT ( 'NONE',  ( 1.506044924156377807, -0.6181864485952697219, -1.610478869194363227 ) ) ;
#114429=( BOUNDED_CURVE ( )  B_SPLINE_CURVE ( 3, ( #185124, #81252, #83364, #149449 ),
 .UNSPECIFIED., .F., .T. ) 
 B_SPLINE_CURVE_WITH_KNOTS ( ( 4, 4 ),
 ( 0.000000000000000000, 0.5000000000000011102 ),
 .UNSPECIFIED. ) 
 CURVE ( )  GEOMETRIC_REPRESENTATION_ITEM ( )  RATIONAL_B_SPLINE_CURVE ( ( 1.000000000000000000, 0.3333333333333318715, 0.3333333333333333703, 1.000000000000001554 ) ) 
 REPRESENTATION_ITEM ( '' )  );
#114430=CARTESIAN_POINT ( 'NONE',  ( 1.382659466718983543, -0.3261178763579902218, -2.167053615394160637 ) ) ;
#114431=CARTESIAN_POINT ( 'NONE',  ( 4.037865812933420173, -1.521084700717803884, -1.599171214764223636 ) ) ;
#114432=CARTESIAN_POINT ( 'NONE',  ( 1.288188150525194642, -1.375441891341127265, -1.679832657438373511 ) ) ;
#114434=CARTESIAN_POINT ( 'NONE',  ( 2.712237125307418228, 1.172176456337461037, -1.763091465072692987 ) ) ;
#114437=CARTESIAN_POINT ( 'NONE',  ( 2.894357049080374278, -0.6678387144627718763, -2.192917219349885816 ) ) ;
#114441=CARTESIAN_POINT ( 'NONE',  ( 4.635507155980078231, -0.1095829440264598081, 2.218699120425669413 ) ) ;
#114450=CARTESIAN_POINT ( 'NONE',  ( 2.567029916978436077, -1.034165006014248211, 1.730866473406714068 ) ) ;
#114452=CARTESIAN_POINT ( 'NONE',  ( 2.694246160070143503, 0.9763755106866910394, -1.816870488346455037 ) ) ;
#114457=CARTESIAN_POINT ( 'NONE',  ( 4.541096662771787251, -1.693051203114638525, -1.391418086139440957 ) ) ;
#114458=CARTESIAN_POINT ( 'NONE',  ( 2.074842474778653134, -0.8596299393073093542, 1.824119475507138821 ) ) ;
#114459=CARTESIAN_POINT ( 'NONE',  ( 1.434833617064284805, -1.334073193498284793, -1.269287082821937362 ) ) ;
#114462=CARTESIAN_POINT ( 'NONE',  ( 4.875911338656576888, 1.051942333337583468, 1.491839654383666947 ) ) ;
#114463=CARTESIAN_POINT ( 'NONE',  ( 6.205703963786828758, 1.882472927010571118, 0.7231429968634556227 ) ) ;
#114465=CARTESIAN_POINT ( 'NONE',  ( 4.540055829149266309, 0.9713072833863345412, -2.043554373614121289 ) ) ;
#114467=CARTESIAN_POINT ( 'NONE',  ( 0.8914058518391498875, 1.856551077915175707, -0.9943519572734434986 ) ) ;
#114469=CARTESIAN_POINT ( 'NONE',  ( 5.230950013807261101, -1.948248037745937022, -0.7008574099531189594 ) ) ;
#114480=CARTESIAN_POINT ( 'NONE',  ( 1.582450481569739331, 1.094613367649547309, 1.816135667671102016 ) ) ;
#114481=CARTESIAN_POINT ( 'NONE',  ( 1.371645089906252446, -1.908569115047893394, -1.136440837462453723 ) ) ;
#114485=CARTESIAN_POINT ( 'NONE',  ( 3.121486724888074882, 0.2905151309811822569, -1.940125473959073421 ) ) ;
#114492=CARTESIAN_POINT ( 'NONE',  ( 2.426173717206762781, -2.096881089210366422, 0.3156149858808757203 ) ) ;
#114494=CARTESIAN_POINT ( 'NONE',  ( 5.283633159863808437, -1.863482887291990409, 0.6137318589548645953 ) ) ;
#114495=CARTESIAN_POINT ( 'NONE',  ( 3.344745324850742385, 0.5235245934552492653, 2.097234944377385002 ) ) ;
#114496=CARTESIAN_POINT ( 'NONE',  ( 3.280630368989821743, 1.663260157205956657, -0.7901080472864712156 ) ) ;
#114500=CARTESIAN_POINT ( 'NONE',  ( 4.452888953083543377, 0.3777208849818362579, -1.698664142626307383 ) ) ;
#114505=CARTESIAN_POINT ( 'NONE',  ( 2.518638242371186386, 1.412657066830936392, -1.636333507658905173 ) ) ;
#114506=CARTESIAN_POINT ( 'NONE',  ( 4.499374939222855474, 1.976653413780619761, 0.3960398538903551757 ) ) ;
#114508=CARTESIAN_POINT ( 'NONE',  ( 1.463986924769441478, 2.129665692569195024, -0.3698555562515608020 ) ) ;
#114509=CARTESIAN_POINT ( 'NONE',  ( 2.442595505675814405, 0.4281495253689853175, 1.924161874619955359 ) ) ;
#114511=CARTESIAN_POINT ( 'NONE',  ( 3.878411472391342318, -0.1936643080829789088, -1.932398009575059472 ) ) ;
#114521=CARTESIAN_POINT ( 'NONE',  ( 0.7806487521475922176, -1.224371414366259847, 1.835764474286231129 ) ) ;
#114523=CARTESIAN_POINT ( 'NONE',  ( 5.471523917629521172, -0.2915489554583711174, 1.939870717765689534 ) ) ;
#114527=CARTESIAN_POINT ( 'NONE',  ( 4.663899394030392997, -1.200468288914667614, 1.396033019000951336 ) ) ;
#114531=CARTESIAN_POINT ( 'NONE',  ( 4.693665235656380830, 1.977662049654808740, -0.7657889336421249693 ) ) ;
#114535=CARTESIAN_POINT ( 'NONE',  ( 6.608673410152685612, 1.530114183832030905, -1.380643333410998430 ) ) ;
#114537=CARTESIAN_POINT ( 'NONE',  ( 1.363465259770980209, -0.4569337200135030197, 1.803945581614458282 ) ) ;
#114538=CARTESIAN_POINT ( 'NONE',  ( 3.790429961727882713, 1.553415782126759792, -0.9881970032953185656 ) ) ;
#114545=CARTESIAN_POINT ( 'NONE',  ( 3.071135375186518690, -2.039199700013223815, -0.8442704067812344393 ) ) ;
#114546=CARTESIAN_POINT ( 'NONE',  ( 5.237693395785977479, -1.594672120175673946, -1.605097536805524916 ) ) ;
#114549=CARTESIAN_POINT ( 'NONE',  ( 5.994382934279598452, -0.9612500426990595592, 1.535330125949084135 ) ) ;
#114550=CARTESIAN_POINT ( 'NONE',  ( 5.243340954880816973, 0.3670949043641066889, -1.880036887305686966 ) ) ;
#114552=CARTESIAN_POINT ( 'NONE',  ( 5.787941465827733722, -0.8397648285632768328, 1.671655200917811168 ) ) ;
#114553=CARTESIAN_POINT ( 'NONE',  ( 6.127394093140170916, 0.1359088500606409067, -1.856169418941427729 ) ) ;
#114555=CARTESIAN_POINT ( 'NONE',  ( 6.297684251969362101, -0.5920937881782936119, 1.667988322058571393 ) ) ;
#114556=CARTESIAN_POINT ( 'NONE',  ( 1.112517963266421939, 1.944731545904467396, 0.5331650539944567946 ) ) ;
#114558=CARTESIAN_POINT ( 'NONE',  ( 2.596425589483622787, -2.100489730888196238, -0.1540555546653120389 ) ) ;
#114563=CARTESIAN_POINT ( 'NONE',  ( 2.320574876688247024, -0.7769297766534470906, -1.864587897788829718 ) ) ;
#114566=CARTESIAN_POINT ( 'NONE',  ( 3.374459016379764087, -1.290570702369205014, 1.733878788530068160 ) ) ;
#114567=CARTESIAN_POINT ( 'NONE',  ( 6.889999999999973035, 7.629137130509064946, 2.879999999999991456 ) ) ;
#114575=CARTESIAN_POINT ( 'NONE',  ( 1.259612756803454525, 2.158328104161820526, -0.3793702838810895095 ) ) ;
#114577=CARTESIAN_POINT ( 'NONE',  ( 2.167197484064213420, -2.068651741926224474, -0.9167319039211866416 ) ) ;
#114585=CARTESIAN_POINT ( 'NONE',  ( 3.391635040236582022, -0.7200671834438672203, 1.616821809559340517 ) ) ;
#114586=CARTESIAN_POINT ( 'NONE',  ( 3.158842756365538129, 0.4911626674463653863, 1.952128870646198555 ) ) ;
#114588=CARTESIAN_POINT ( 'NONE',  ( 6.791986947960565679, -0.9495855537378705691, 1.990061496475347802 ) ) ;
#114592=CARTESIAN_POINT ( 'NONE',  ( 4.605092316430917876, -0.09611821078869468848, 2.014234682242924457 ) ) ;
#114594=CARTESIAN_POINT ( 'NONE',  ( 2.342468781959532453, 0.4075140148256419792, 1.825566309089213579 ) ) ;
#114595=CARTESIAN_POINT ( 'NONE',  ( 3.520434184366732389, 0.9265386974339048232, 1.851387837889128640 ) ) ;
#114597=CARTESIAN_POINT ( 'NONE',  ( 1.863391182279940494, -1.538030936729195552, -1.136358088520472931 ) ) ;
#114602=CARTESIAN_POINT ( 'NONE',  ( 1.019614524654769872, -0.4619345408787678964, 1.855657206939323789 ) ) ;
#114603=CARTESIAN_POINT ( 'NONE',  ( 3.367582429956605061, -0.3852447139683997657, 1.923494667983568718 ) ) ;
#114604=CARTESIAN_POINT ( 'NONE',  ( 0.4212496859960760953, 0.7689994822442263178, 1.863884711849304487 ) ) ;
#114608=CARTESIAN_POINT ( 'NONE',  ( 6.608667082420285332, 1.462428336960637676, -1.322156044359092064 ) ) ;
#114610=CARTESIAN_POINT ( 'NONE',  ( 2.320566727126192053, -0.7743817983801875027, -1.858503283895854841 ) ) ;
#114612=CARTESIAN_POINT ( 'NONE',  ( 2.618900020153229757, 0.2622993368636802325, 2.100875384797147305 ) ) ;
#114614=CARTESIAN_POINT ( 'NONE',  ( 4.123533666479628046, 0.2564666318346648377, -2.054367117340555549 ) ) ;
#114616=CARTESIAN_POINT ( 'NONE',  ( 6.087849878328269071, -2.080457216024658607, -0.2059406971956292964 ) ) ;
#114618=CARTESIAN_POINT ( 'NONE',  ( 3.698116152863577977, -1.823479002399010396, -0.09026698595545472326 ) ) ;
#114624=CARTESIAN_POINT ( 'NONE',  ( 6.563508857876433567, 0.3837567690821128696, -2.173003994120882076 ) ) ;
#114627=CARTESIAN_POINT ( 'NONE',  ( 4.846305138012901637, 0.9798207982155520135, -1.642033262021398654 ) ) ;
#114632=FACE_OUTER_BOUND ( 'NONE', #132331, .T. ) ;
#114634=CARTESIAN_POINT ( 'NONE',  ( 0.2922019606856861018, 1.531309713818730822, -1.022077305420886040 ) ) ;
#114639=CARTESIAN_POINT ( 'NONE',  ( 5.044154037833219029, 1.865456107639616556, 0.1390639465682907416 ) ) ;
#114644=CARTESIAN_POINT ( 'NONE',  ( 0.7780955915308949145, -1.048793665676364562, -1.666747765972796946 ) ) ;
#114645=CARTESIAN_POINT ( 'NONE',  ( 2.144157856786413241, 0.8647422840215597262, 1.821734841475818101 ) ) ;
#114649=CARTESIAN_POINT ( 'NONE',  ( 2.027518650255655253, -1.432890729411402830, -1.658174735819065049 ) ) ;
#114659=CARTESIAN_POINT ( 'NONE',  ( 4.388128076750056117, -0.4078595375654435751, -1.795341762384855544 ) ) ;
#114660=CARTESIAN_POINT ( 'NONE',  ( 2.156891369321057628, 0.4431265858878992159, 1.963560470019373172 ) ) ;
#114661=CARTESIAN_POINT ( 'NONE',  ( 3.357065504480163387, -0.9345643552367989271, 2.099969358187879109 ) ) ;
#114663=CARTESIAN_POINT ( 'NONE',  ( 1.041598845562411890, 1.244476351500271472, 1.383831004058704961 ) ) ;
#114665=CARTESIAN_POINT ( 'NONE',  ( 6.983263157960365675, -0.006178392973848687020, 2.053544886540019210 ) ) ;
#114666=CARTESIAN_POINT ( 'NONE',  ( 5.748291730981218706, 0.9368611416523886515, -1.667099895225135686 ) ) ;
#114669=CARTESIAN_POINT ( 'NONE',  ( 5.038659576058011957, -1.792549807278142726, 1.075873411605046348 ) ) ;
#114670=CARTESIAN_POINT ( 'NONE',  ( 3.748781033766034998, -1.529746656882627454, 1.076398355447941491 ) ) ;
#114673=CARTESIAN_POINT ( 'NONE',  ( 5.337399561049260832, 0.7408347518493042516, -1.685818907712175019 ) ) ;
#114676=CARTESIAN_POINT ( 'NONE',  ( 5.619686913847246501, -1.681401280226066941, 0.3840984716911073349 ) ) ;
#114678=CARTESIAN_POINT ( 'NONE',  ( 0.6504783628028444342, 0.8526279987398683868, 1.509985294034902337 ) ) ;
#114681=( NAMED_UNIT ( * ) SI_UNIT ( $, .STERADIAN. ) SOLID_ANGLE_UNIT ( ) );
#114682=CARTESIAN_POINT ( 'NONE',  ( 4.944265959323273840, -1.029449158807031361, 1.911525048081736955 ) ) ;
#114683=CARTESIAN_POINT ( 'NONE',  ( 3.299243935302543118, 1.439784963707075649, 1.122460502641378755 ) ) ;
#114684=CARTESIAN_POINT ( 'NONE',  ( 0.6726124357511429341, 1.356994209013298036, -1.416925378234991095 ) ) ;
#114685=CARTESIAN_POINT ( 'NONE',  ( 5.384029865600029829, -2.117513407852515073, 0.002815966404249789501 ) ) ;
#114687=CARTESIAN_POINT ( 'NONE',  ( 5.706620831843001618, 2.020032061211772589, 1.083668233456626551 ) ) ;
#114690=CARTESIAN_POINT ( 'NONE',  ( 0.8738735914427527840, 0.4098651554323496926, -2.080331290949386513 ) ) ;
#114693=CARTESIAN_POINT ( 'NONE',  ( 6.614155491087242211, 2.165850671381476023, -0.1511765098734293433 ) ) ;
#114694=CARTESIAN_POINT ( 'NONE',  ( 6.883263157960364254, 4.694764272337425659, 2.516417202187768432 ) ) ;
#114696=CARTESIAN_POINT ( 'NONE',  ( 2.192296887966191488, 1.369148959659401754, 1.749082743080948799 ) ) ;
#114698=CARTESIAN_POINT ( 'NONE',  ( 6.223279759862190730, 1.994869330463379331, 0.2930738960792296233 ) ) ;
#114700=CARTESIAN_POINT ( 'NONE',  ( 5.629752743445687990, 1.989327071453067752, -0.5446528645957140480 ) ) ;
#114706=CARTESIAN_POINT ( 'NONE',  ( 4.792441439910442469, 1.527937338083688923, -1.027124420945781935 ) ) ;
#114710=CARTESIAN_POINT ( 'NONE',  ( 1.377515174558477273, 1.023066641755419282, 1.388426169202553018 ) ) ;
#114711=CARTESIAN_POINT ( 'NONE',  ( -0.1003747550864658999, -1.976661868047492998, 0.3981153667176607902 ) ) ;
#114712=CARTESIAN_POINT ( 'NONE',  ( 1.442429577410338615, -1.974492438002553918, -1.176823363874231587 ) ) ;
#114714=CARTESIAN_POINT ( 'NONE',  ( 1.353188757747030957, -1.783583821274600911, 1.391813662893444548 ) ) ;
#114715=CARTESIAN_POINT ( 'NONE',  ( 3.932330475907989342, 1.126754335618613379, -1.779114833428483866 ) ) ;
#114717=CARTESIAN_POINT ( 'NONE',  ( 2.424752316626857862, -0.004995123648579914352, 1.769921776121333945 ) ) ;
#114722=CARTESIAN_POINT ( 'NONE',  ( 5.414381242519362480, -2.221583670654456721, 0.0001252536179462138133 ) ) ;
#114723=CARTESIAN_POINT ( 'NONE',  ( 3.591891977137162684, -2.188917585555647527, -0.1077332384093188100 ) ) ;
#114727=CARTESIAN_POINT ( 'NONE',  ( 6.890000000000010338, 4.693995042360769254, 2.562605081426703180 ) ) ;
#114729=CARTESIAN_POINT ( 'NONE',  ( 5.642871316567687145, 2.044259226470702462, 0.5637153772257290640 ) ) ;
#114735=CARTESIAN_POINT ( 'NONE',  ( 6.198766299729112639, 1.534709720371667308, 1.016988835930050739 ) ) ;
#114738=CARTESIAN_POINT ( 'NONE',  ( 1.926944929849357280, -1.137335869680399902, -1.317475996949101669 ) ) ;
#114743=CARTESIAN_POINT ( 'NONE',  ( 6.473507614529132148, 2.070149491355821159, -0.6224772505839873959 ) ) ;
#114747=CARTESIAN_POINT ( 'NONE',  ( 5.436455051933180016, 2.129025116502227810, 0.3735886874452337691 ) ) ;
#114751=CARTESIAN_POINT ( 'NONE',  ( 6.327413238363588377, -1.857107522167710245, 0.6617740914907597194 ) ) ;
#114752=CARTESIAN_POINT ( 'NONE',  ( 4.622224120573574346, 0.3796314994632241646, -1.691551752166654543 ) ) ;
#114755=CARTESIAN_POINT ( 'NONE',  ( 1.628746693258641853, 0.2190750365392846177, 2.180598679842937759 ) ) ;
#114756=CARTESIAN_POINT ( 'NONE',  ( 2.890017657663559891, 1.631080081281432559, 1.632583592418336282 ) ) ;
#114757=CARTESIAN_POINT ( 'NONE',  ( 4.868464682339723737, -1.349271924330990080, 1.557713215823807174 ) ) ;
#114758=CARTESIAN_POINT ( 'NONE',  ( 1.218581363712217591, -0.04816221259190026777, 1.941509521754792855 ) ) ;
#114762=CARTESIAN_POINT ( 'NONE',  ( -0.1108833634136767443, 0.0002062650063822807356, -1.896853557917008271 ) ) ;
#114763=CARTESIAN_POINT ( 'NONE',  ( 4.025719079702368752, -0.3592959752154977204, 2.089770972018199835 ) ) ;
#114764=CARTESIAN_POINT ( 'NONE',  ( 0.9146856577476671912, -1.281363086869342194, -1.556907195799726917 ) ) ;
#114766=CARTESIAN_POINT ( 'NONE',  ( 4.401547605996741552, 1.770323140634282311, 1.317293360403009927 ) ) ;
#114773=CARTESIAN_POINT ( 'NONE',  ( 4.698151523293167209, -2.060395484190484794, -0.05257267949314303745 ) ) ;
#114777=CARTESIAN_POINT ( 'NONE',  ( 3.299477536675638145, 1.824990673169521793, -0.8654797531507262276 ) ) ;
#114782=CARTESIAN_POINT ( 'NONE',  ( 2.940362659251498645, 2.045167860313545916, 0.2535661900368457733 ) ) ;
#114785=CARTESIAN_POINT ( 'NONE',  ( -0.1411974294642202310, 0.2398548052158452348, -1.934266582396115819 ) ) ;
#114786=CARTESIAN_POINT ( 'NONE',  ( 1.183273638618479673, -0.8294958387620559037, 1.643756842616146630 ) ) ;
#114787=CARTESIAN_POINT ( 'NONE',  ( -0.004676085075996058368, -0.5178430341337829645, -2.257629771169813448 ) ) ;
#114789=CARTESIAN_POINT ( 'NONE',  ( 2.565889408427945995, 2.120439650033152379, -0.4189318973958494619 ) ) ;
#114791=CARTESIAN_POINT ( 'NONE',  ( 1.534389036647098692, 0.6371565916030231813, 1.913260934284975345 ) ) ;
#114793=CARTESIAN_POINT ( 'NONE',  ( 2.917634960997887994, 0.7719352619847442698, 2.165007881682521784 ) ) ;
#114795=CARTESIAN_POINT ( 'NONE',  ( 0.3911966820569385828, 1.383097094795827209, 1.259704262696823118 ) ) ;
#114796=CARTESIAN_POINT ( 'NONE',  ( 4.750830034454851969, -1.584041870840187327, 1.173487520707878096 ) ) ;
#114797=CARTESIAN_POINT ( 'NONE',  ( 4.259000112335223243, -0.004834882008357410665, -2.016708403958865414 ) ) ;
#114801=CARTESIAN_POINT ( 'NONE',  ( 6.410775461673044795, 1.561785836243877235, -1.413106494374539945 ) ) ;
#114802=CARTESIAN_POINT ( 'NONE',  ( 6.830528382861658088, -1.277203763263988101, 1.630111558092485868 ) ) ;
#114806=CARTESIAN_POINT ( 'NONE',  ( 4.763928514684708126, 0.6297656808758389513, -1.919195086291412888 ) ) ;
#114808=CARTESIAN_POINT ( 'NONE',  ( 3.510674805948321264, -0.9346715503392712954, -2.110115307156499753 ) ) ;
#114809=CARTESIAN_POINT ( 'NONE',  ( 2.289955638094377299, -1.343889277006144356, -1.564782475634781900 ) ) ;
#114816=CARTESIAN_POINT ( 'NONE',  ( 4.053319971960964274, 1.836175303466779374, -1.158372938815607656 ) ) ;
#114819=CARTESIAN_POINT ( 'NONE',  ( 2.858754248528099229, 0.2676582106064147593, -1.821554178878769470 ) ) ;
#114821=CARTESIAN_POINT ( 'NONE',  ( 3.878626735558046157, -0.2160506499642600997, -2.180900317982924275 ) ) ;
#114823=CARTESIAN_POINT ( 'NONE',  ( 5.946200445400964263, 2.259567648220105252, 0.1180026366056959042 ) ) ;
#114828=CARTESIAN_POINT ( 'NONE',  ( 6.749276393231373739, -1.423207027788903067, -1.051611706393209111 ) ) ;
#114830=CARTESIAN_POINT ( 'NONE',  ( 3.721343298090164620, 1.727675083452884897, 1.033047338021097383 ) ) ;
#114832=CARTESIAN_POINT ( 'NONE',  ( 3.452270085047473458, 2.106147100029008179, 0.001788861226008006461 ) ) ;
#114833=CARTESIAN_POINT ( 'NONE',  ( 1.792461972651203439, 1.418048008323580911, -1.288064678409290398 ) ) ;
#114836=CARTESIAN_POINT ( 'NONE',  ( 3.578522297727056767, 1.251517597477384447, -1.520772613757546354 ) ) ;
#114837=CARTESIAN_POINT ( 'NONE',  ( 0.8306673739700667358, 0.1335802410974036292, 1.865940672528036304 ) ) ;
#114838=CARTESIAN_POINT ( 'NONE',  ( 1.363640982571033611, -0.4799814350611387725, 1.902108589862220311 ) ) ;
#114839=CARTESIAN_POINT ( 'NONE',  ( 0.6153073421325053749, 1.564839666810373231, 1.099065937236625157 ) ) ;
#114843=CARTESIAN_POINT ( 'NONE',  ( 6.543822781336226413, 0.7137633992815132222, -1.729328153040734728 ) ) ;
#114846=CARTESIAN_POINT ( 'NONE',  ( 6.315297747118990834, -1.772576088781053327, -1.069364167438614732 ) ) ;
#114848=CARTESIAN_POINT ( 'NONE',  ( 0.7661813929631040576, -2.060537521029872643, 0.2012509062776293156 ) ) ;
#114853=CARTESIAN_POINT ( 'NONE',  ( 5.197945112634200449, 1.424400718755761908, 1.570990128125760554 ) ) ;
#114858=CARTESIAN_POINT ( 'NONE',  ( 6.689906388054261299, -1.280585065398877731, -1.486383542710856043 ) ) ;
#114860=CARTESIAN_POINT ( 'NONE',  ( 4.358749857130030492, -0.7741967591250037417, 1.861731939633674893 ) ) ;
#114861=CARTESIAN_POINT ( 'NONE',  ( 3.960093407954877520, -1.098340823217320184, 1.569403885630010320 ) ) ;
#114863=CARTESIAN_POINT ( 'NONE',  ( 1.452940684028160234, -1.882004992133184285, -1.122693704575933316 ) ) ;
#114864=CARTESIAN_POINT ( 'NONE',  ( 0.1333692844072559558, 0.7140749627707367875, -2.136770008611441618 ) ) ;
#114865=CARTESIAN_POINT ( 'NONE',  ( 2.952262541859524969, 0.6266372353985818489, 1.762611677789377440 ) ) ;
#114869=CARTESIAN_POINT ( 'NONE',  ( 5.765271170472290763, 1.955999355395316996, -0.8108409051663100220 ) ) ;
#114871=CARTESIAN_POINT ( 'NONE',  ( 1.804351596996961238, 1.546985077243122397, -1.406606537801007972 ) ) ;
#114873=CARTESIAN_POINT ( 'NONE',  ( 0.3051044079889728144, -0.4676614632079054701, 1.660094367756638434 ) ) ;
#114876=ADVANCED_FACE ( 'NONE', ( #183895 ), #172560, .F. ) ;
#114885=CARTESIAN_POINT ( 'NONE',  ( 1.207327558334120754, 1.371319684050668730, 1.183719584703796679 ) ) ;
#114894=ADVANCED_FACE ( 'NONE', ( #37653 ), #207318, .F. ) ;
#114895=CARTESIAN_POINT ( 'NONE',  ( 3.033498015644376267, 1.768043114356824930, -0.5812464218588138110 ) ) ;
#114897=CARTESIAN_POINT ( 'NONE',  ( 0.1928052069046156669, 1.667086954950956157, 0.9433992581227236274 ) ) ;
#114898=CARTESIAN_POINT ( 'NONE',  ( 6.282248997152713343, -1.030047846951231971, 1.627708832905690350 ) ) ;
#114899=CARTESIAN_POINT ( 'NONE',  ( 6.250451049865752395, -2.060019788584551481, -0.2068627631737207651 ) ) ;
#114905=CARTESIAN_POINT ( 'NONE',  ( 5.155114233317533490, 1.639596689546858777, -1.090739528099492928 ) ) ;
#114906=CARTESIAN_POINT ( 'NONE',  ( 1.840644454891388282, 1.218392294859267144, -1.735325642819861791 ) ) ;
#114910=CARTESIAN_POINT ( 'NONE',  ( 6.175747540105122724, -1.175446681380667213, 1.849350104233343783 ) ) ;
#114912=CARTESIAN_POINT ( 'NONE',  ( 4.137660063496669594, -1.327783069688622586, -1.395926297547624984 ) ) ;
#114914=CARTESIAN_POINT ( 'NONE',  ( 0.7096328715897933792, -1.817275359149352676, 0.1739118742359047065 ) ) ;
#114915=CARTESIAN_POINT ( 'NONE',  ( 0.6103625832605160673, -2.195865045534075133, 0.2202409711149767024 ) ) ;
#114920=CARTESIAN_POINT ( 'NONE',  ( 6.702011354250313246, 0.7569246535186587854, -1.818382958529676019 ) ) ;
#114921=CARTESIAN_POINT ( 'NONE',  ( 1.030689935155226555, -1.755017395645932066, 0.8318847510124205424 ) ) ;
#114922=CARTESIAN_POINT ( 'NONE',  ( 6.397888825007291835, 0.2158721846312293136, 2.288236095241158452 ) ) ;
#114924=CARTESIAN_POINT ( 'NONE',  ( 5.489040303513849750, 0.1347565666095333348, 1.856089258439092893 ) ) ;
#114927=CARTESIAN_POINT ( 'NONE',  ( 6.509000000000011887, 3.696273625755361447, 2.514342382328867753 ) ) ;
#114929=CARTESIAN_POINT ( 'NONE',  ( 6.720655732516701342, 6.039000170257122768, 2.421169367564251385 ) ) ;
#114930=CARTESIAN_POINT ( 'NONE',  ( 0.9080814035550346386, -0.9900877184637231210, -1.955254813705724404 ) ) ;
#114934=CARTESIAN_POINT ( 'NONE',  ( 1.383131112650197281, 1.687622997524572677, -0.6969523973551354779 ) ) ;
#114937=FACE_OUTER_BOUND ( 'NONE', #21798, .T. ) ;
#114939=CARTESIAN_POINT ( 'NONE',  ( 6.727182134110220701, 0.005875948494733078051, 1.810970247402940103 ) ) ;
#114940=CARTESIAN_POINT ( 'NONE',  ( 4.961744919065852244, -0.5270168765720646409, 1.889542207339139024 ) ) ;
#114943=CARTESIAN_POINT ( 'NONE',  ( 4.670628115925999246, 0.8122961462209904449, 1.958930372594757330 ) ) ;
#114944=CARTESIAN_POINT ( 'NONE',  ( 4.177398808104064720, 1.432170664236757540, 1.658919600136643524 ) ) ;
#114946=CARTESIAN_POINT ( 'NONE',  ( 3.221598570378156001, 0.3083542414583049784, -2.047064864394084971 ) ) ;
#114950=CARTESIAN_POINT ( 'NONE',  ( 2.602471654445730032, -0.2222675636014606049, 2.287907847288372043 ) ) ;
#114954=CARTESIAN_POINT ( 'NONE',  ( 6.720655732516660485, 7.629137130509104914, 2.326260288887294969 ) ) ;
#114956=CARTESIAN_POINT ( 'NONE',  ( 3.820204237656314561, 1.844379349147889480, 0.6080220579995837538 ) ) ;
#114959=ADVANCED_FACE ( 'NONE', ( #154088 ), #200343, .F. ) ;
#114960=CARTESIAN_POINT ( 'NONE',  ( 3.533378866418676711, -0.1359047358975660202, 1.907598245988059826 ) ) ;
#114962=CARTESIAN_POINT ( 'NONE',  ( 5.614166379062860202, -0.7790257685919326214, -1.538869111107727505 ) ) ;
#114963=CARTESIAN_POINT ( 'NONE',  ( 3.239470508323912146, 0.4852670486454255250, -1.957170429962351577 ) ) ;
#114964=CARTESIAN_POINT ( 'NONE',  ( 5.520273603857641653, -2.079230528169520031, 0.9805040003046764374 ) ) ;
#114966=CARTESIAN_POINT ( 'NONE',  ( 0.8212658843103730621, 2.040464674744349338, 0.8412164853940640175 ) ) ;
#114968=CARTESIAN_POINT ( 'NONE',  ( 5.764868906847371299, -1.600580677892119441, -0.7553990054774415430 ) ) ;
#114970=CARTESIAN_POINT ( 'NONE',  ( 1.711265200625663008, -0.2773638578843647950, 2.275360193931966535 ) ) ;
#114971=CARTESIAN_POINT ( 'NONE',  ( 1.165484214331854895, -1.106714608479087092, 1.343107696387570549 ) ) ;
#114978=CARTESIAN_POINT ( 'NONE',  ( 1.258521197368984268, -2.171350058325251187, -0.0004004535333074903960 ) ) ;
#114979=CARTESIAN_POINT ( 'NONE',  ( 2.009000277268524481, 0.004839059525654776373, 2.016708403978189956 ) ) ;
#114982=CARTESIAN_POINT ( 'NONE',  ( 5.830678075864223153, 1.857343136638961445, 0.5113247108688694365 ) ) ;
#114984=CARTESIAN_POINT ( 'NONE',  ( 2.461440635673370014, -1.844245817859784031, 1.238046099332066108 ) ) ;
#114992=CARTESIAN_POINT ( 'NONE',  ( 5.847135585344571673, 0.4968686550196474982, -1.668027988745724777 ) ) ;
#114993=CARTESIAN_POINT ( 'NONE',  ( 3.244534624505683418, -1.932379277470747558, -0.3379807920969243873 ) ) ;
#114997=CARTESIAN_POINT ( 'NONE',  ( 4.956464464747484477, 0.8595337117903809609, 2.092967149517725112 ) ) ;
#114998=CARTESIAN_POINT ( 'NONE',  ( 0.8013246507756426329, -1.769997244335961284, 1.058882903378530749 ) ) ;
#115002=CARTESIAN_POINT ( 'NONE',  ( 2.184789616947193203, -2.218938341775698042, -0.4411300470171536370 ) ) ;
#115005=CARTESIAN_POINT ( 'NONE',  ( 2.547943918863291302, 1.870051909910470878, 0.05015897750767356333 ) ) ;
#115006=CARTESIAN_POINT ( 'NONE',  ( 1.740413025836908156, 1.729532991921935325, -0.1275185469355680501 ) ) ;
#115008=CARTESIAN_POINT ( 'NONE',  ( 4.810206850810132551, 1.511280187219691928, -1.587364365194674498 ) ) ;
#115009=CARTESIAN_POINT ( 'NONE',  ( 6.352564483950959406, 0.7153834962906236994, 2.193980215933882150 ) ) ;
#115010=CARTESIAN_POINT ( 'NONE',  ( 1.516555680085801994, 1.384881227076775190, -1.526387457142893256 ) ) ;
#115011=CARTESIAN_POINT ( 'NONE',  ( 4.365135538708351248, 1.883338149218495516, -0.4730343525067778332 ) ) ;
#115014=CARTESIAN_POINT ( 'NONE',  ( 1.187500000000001110, -1.451031289061072815, 1.451031289061169183 ) ) ;
#115017=CARTESIAN_POINT ( 'NONE',  ( 6.239611212763971793, -1.913511330438378177, -0.6350998681113121380 ) ) ;
#115020=CARTESIAN_POINT ( 'NONE',  ( 6.012342310302175363, -1.897698807000438359, 0.6819931642896917001 ) ) ;
#115024=CARTESIAN_POINT ( 'NONE',  ( 2.367563199519676420, 1.790531440309536926, -0.3556685536310541518 ) ) ;
#115032=CARTESIAN_POINT ( 'NONE',  ( 0.05299788485858129838, 0.3494575625802974206, 1.989167885679890002 ) ) ;
#115033=CARTESIAN_POINT ( 'NONE',  ( 0.2762449081346768365, 2.096790360132039233, -0.3154013857558089495 ) ) ;
#115036=CIRCLE ( 'NONE', #49272, 0.04999999999999883010 ) ;
#115038=CARTESIAN_POINT ( 'NONE',  ( 6.174695665487812235, -1.956078286930991394, -0.6490473743868007128 ) ) ;
#115039=CARTESIAN_POINT ( 'NONE',  ( 5.326796142270829648, 0.8146286751641409474, -1.844708973168760924 ) ) ;
#115048=CARTESIAN_POINT ( 'NONE',  ( 4.692732413458527319, -1.238132498367884082, -1.591073831703953445 ) ) ;
#115049=CARTESIAN_POINT ( 'NONE',  ( 5.173706384855800700, -1.019854773079221344, 1.532662130498331887 ) ) ;
#115050=CARTESIAN_POINT ( 'NONE',  ( -0.02319159430949970999, 0.003959926571647092407, -1.810968101872318714 ) ) ;
#115051=CARTESIAN_POINT ( 'NONE',  ( 2.754834555525199846, 0.7783630933865728352, 2.172589714749242784 ) ) ;
#115053=CARTESIAN_POINT ( 'NONE',  ( 6.415313282229532454, -0.2716245656670859820, 2.144420208805633887 ) ) ;
#115054=CARTESIAN_POINT ( 'NONE',  ( 3.450407915430803385, -1.350735839785843773, 1.497501794165828626 ) ) ;
#115056=CARTESIAN_POINT ( 'NONE',  ( 0.9252163604592329449, -1.233020167302405490, -1.500395619358737553 ) ) ;
#115062=CARTESIAN_POINT ( 'NONE',  ( 3.977312496258199825, 1.761605600429091201, -0.6297503393934977822 ) ) ;
#115064=CARTESIAN_POINT ( 'NONE',  ( 1.793074957647671663, -0.09724762972821224261, -1.910064080951429100 ) ) ;
#115067=CARTESIAN_POINT ( 'NONE',  ( 3.035963658818414235, -1.482449291622448095, -1.634993338104336891 ) ) ;
#115068=CARTESIAN_POINT ( 'NONE',  ( 6.883263157960399781, 2.970623603138924818, 2.399364662246627589 ) ) ;
#115073=CARTESIAN_POINT ( 'NONE',  ( 0.8605430240068573378, -1.430899983082928761, 1.356264857227080567 ) ) ;
#115074=CARTESIAN_POINT ( 'NONE',  ( 1.466329616580586581, 2.273096917617071888, -0.3966160293069305731 ) ) ;
#115075=CARTESIAN_POINT ( 'NONE',  ( 1.504273306027693602, 1.959471947749168663, 0.09963418240711149898 ) ) ;
#115076=CARTESIAN_POINT ( 'NONE',  ( 5.559457797297955750, 1.683061182826322666, 1.192002683324727252 ) ) ;
#115083=CARTESIAN_POINT ( 'NONE',  ( 0.8487579731258857452, -2.154475699732544491, -0.2676485622446558299 ) ) ;
#115085=CARTESIAN_POINT ( 'NONE',  ( 6.022987620897008121, -1.731432113864934674, 0.6267441317700100933 ) ) ;
#115088=CARTESIAN_POINT ( 'NONE',  ( 1.493192106177696044, 1.412881632968411516, 1.225925835885120829 ) ) ;
#115089=CARTESIAN_POINT ( 'NONE',  ( 5.835289683280778128, -1.956920075724715602, 0.9183947573421016308 ) ) ;
#115091=CARTESIAN_POINT ( 'NONE',  ( 0.07755575628181145265, 6.946778278137147211, -2.783982195446454533 ) ) ;
#115093=CARTESIAN_POINT ( 'NONE',  ( 1.418461073652961257, -0.6892283116659430053, -1.783923526276688154 ) ) ;
#115095=CARTESIAN_POINT ( 'NONE',  ( 3.256490041505883504, -1.340903482672378466, 1.155240514129013407 ) ) ;
#115097=CARTESIAN_POINT ( 'NONE',  ( 0.8207898099904624711, 1.447681275506585541, -1.249484660484905030 ) ) ;
#115099=CARTESIAN_POINT ( 'NONE',  ( 5.220295459014530515, 1.888029131402849670, 0.3228437444452412763 ) ) ;
#115100=CARTESIAN_POINT ( 'NONE',  ( 6.144967554776202157, -0.2872888210109864060, -1.948340736549762697 ) ) ;
#115102=CARTESIAN_POINT ( 'NONE',  ( 1.213308285724056690, 1.730450836393576886, -1.225479750871574458 ) ) ;
#115104=CARTESIAN_POINT ( 'NONE',  ( 4.188257260935820625, -1.850246793840780279, -0.2747695030091561463 ) ) ;
#115105=CARTESIAN_POINT ( 'NONE',  ( 0.1350027811974127134, -1.670744041527939094, 0.7364786222084362954 ) ) ;
#115107=CARTESIAN_POINT ( 'NONE',  ( 4.459734715955371520, 0.4851516707722826061, -2.152740496749529608 ) ) ;
#115110=CARTESIAN_POINT ( 'NONE',  ( 1.908709741418318062, 0.6448079515158434694, 1.959386160279535494 ) ) ;
#115116=CARTESIAN_POINT ( 'NONE',  ( 0.1753634416057741618, 2.865130778691078461, -2.632309609290181651 ) ) ;
#115118=CARTESIAN_POINT ( 'NONE',  ( 4.105968538015460467, 0.7004154448949986289, -1.948405661837959713 ) ) ;
#115120=CARTESIAN_POINT ( 'NONE',  ( 1.019082891775088484, 1.996809913787592095, 0.8282600050937349856 ) ) ;
#115122=CARTESIAN_POINT ( 'NONE',  ( 2.209634141364385851, 1.562563088667227262, 1.279657157811086909 ) ) ;
#115129=CARTESIAN_POINT ( 'NONE',  ( 0.1457207355009884908, 1.993892511249679034, -0.3006540981884687214 ) ) ;
#115130=CARTESIAN_POINT ( 'NONE',  ( 4.441096743985088580, -1.694418930461354611, -1.389946530008886905 ) ) ;
#115132=CARTESIAN_POINT ( 'NONE',  ( 3.427896188528327226, -1.883279545317056547, 0.3315703044584616399 ) ) ;
#115136=CARTESIAN_POINT ( 'NONE',  ( 2.495720449669075247, -1.994069261235394741, 0.2986488809556055446 ) ) ;
#115138=CARTESIAN_POINT ( 'NONE',  ( 0.3281778771060560040, 1.171583119817346086, -1.970250653751925762 ) ) ;
#115140=CARTESIAN_POINT ( 'NONE',  ( 3.891373129206575410, 1.249378432800802852, 1.189308452707043884 ) ) ;
#115141=CARTESIAN_POINT ( 'NONE',  ( 0.1405533004714617507, 0.6596865332844923380, -2.358301179948574244 ) ) ;
#115145=CARTESIAN_POINT ( 'NONE',  ( 0.07536363704233400851, 2.864322694550157866, -2.632457840217194089 ) ) ;
#115150=CARTESIAN_POINT ( 'NONE',  ( 5.461500695664097904, -1.431772717462083566, -1.109608708211702099 ) ) ;
#115155=CARTESIAN_POINT ( 'NONE',  ( 5.690068458729246714, 1.084374654971603569, 1.450890516563392518 ) ) ;
#115158=CARTESIAN_POINT ( 'NONE',  ( 2.572451567087580493, -2.097416440861415321, -0.6350555677336399141 ) ) ;
#115160=CARTESIAN_POINT ( 'NONE',  ( 6.566864649055507819, 1.378042638564499489, -1.251022615016267103 ) ) ;
#115162=CARTESIAN_POINT ( 'NONE',  ( 4.235878408818731344, 1.915113449751761010, -0.05082400106456300831 ) ) ;
#115168=CARTESIAN_POINT ( 'NONE',  ( 5.419199134695255715, -1.912947687149676668, 0.9079543477103575455 ) ) ;
#115169=CARTESIAN_POINT ( 'NONE',  ( 1.200320640528436789, -2.161883444890321915, 0.0006282887012112879947 ) ) ;
#115172=CARTESIAN_POINT ( 'NONE',  ( 0.4811275135914867551, 1.705355465787803393, -0.6520327999673739550 ) ) ;
#115174=CARTESIAN_POINT ( 'NONE',  ( 3.030095697178539549, 1.015519584536026976, -1.516846343748608605 ) ) ;
#115178=CARTESIAN_POINT ( 'NONE',  ( 3.121499051359075239, 0.2915335129191589103, -1.947736612120597455 ) ) ;
#115180=CARTESIAN_POINT ( 'NONE',  ( 4.405766152992893758, -0.8336290453338083273, -1.754189941349618920 ) ) ;
#115183=CARTESIAN_POINT ( 'NONE',  ( 5.185831674374465905, 2.043064739972153543, -0.5678235988075125418 ) ) ;
#115185=CARTESIAN_POINT ( 'NONE',  ( 3.264218543254516103, 1.912461472423478970, -0.002497826895729581952 ) ) ;
#115191=CARTESIAN_POINT ( 'NONE',  ( 4.318997845537309033, 1.554796018123940193, -1.278706705004019506 ) ) ;
#115193=CARTESIAN_POINT ( 'NONE',  ( 4.793472150574508817, 1.354911484294840429, 1.223852735664505698 ) ) ;
#115194=CARTESIAN_POINT ( 'NONE',  ( 0.4497787391488928810, 1.533077660697563793, 1.391591089521776681 ) ) ;
#115198=CARTESIAN_POINT ( 'NONE',  ( 6.227412191919261986, -1.760757567598171480, 0.6321290105378990498 ) ) ;
#115208=CARTESIAN_POINT ( 'NONE',  ( 1.094682738308445202, 2.038987083759949304, 0.3576228084290478115 ) ) ;
#115209=CARTESIAN_POINT ( 'NONE',  ( 2.794651083563943761, 1.531546425470770245, -1.462076589042210495 ) ) ;
#115212=CARTESIAN_POINT ( 'NONE',  ( 6.104363016364067640, 2.067617457866403718, 0.1074407263862015016 ) ) ;
#115217=CARTESIAN_POINT ( 'NONE',  ( 2.713130565535960770, -0.2235823006870632790, 2.281328536464954038 ) ) ;
#115220=CARTESIAN_POINT ( 'NONE',  ( 2.759904966095374501, 0.6844231338998980618, -1.785916880244736715 ) ) ;
#115225=CARTESIAN_POINT ( 'NONE',  ( 0.2287712656204986261, 1.385237311202421662, -1.461098210751586857 ) ) ;
#115226=CARTESIAN_POINT ( 'NONE',  ( 1.199968502355329703, 0.8001272530510427083, -1.791371145023381128 ) ) ;
#115230=CARTESIAN_POINT ( 'NONE',  ( 4.119144422497845959, -2.000575632760223765, 0.6069725389450402186 ) ) ;
#115231=CARTESIAN_POINT ( 'NONE',  ( 2.324752472428833983, -0.002986221762550990942, 1.770032028303660576 ) ) ;
#115234=CARTESIAN_POINT ( 'NONE',  ( 4.769621702613293657, 1.317199799690757178, 1.875844486027035574 ) ) ;
#115235=CARTESIAN_POINT ( 'NONE',  ( 4.171615353782907931, -0.9995084519054014960, 1.424469360818179986 ) ) ;
#115238=CARTESIAN_POINT ( 'NONE',  ( 4.200348813226637112, -1.195399808894830773, -1.256130793262473455 ) ) ;
#115239=CARTESIAN_POINT ( 'NONE',  ( 5.125502745298136098, 0.2179265861129157655, -2.160231653469760982 ) ) ;
#115241=CARTESIAN_POINT ( 'NONE',  ( 5.225796113160614986, 0.8128206588041908542, -1.845625551132886288 ) ) ;
#115242=CARTESIAN_POINT ( 'NONE',  ( 6.750000000000005329, 3.748112931134527976E-13, 1.999999999999984901 ) ) ;
#115244=CARTESIAN_POINT ( 'NONE',  ( 2.661056112795460837, -1.675086148048400503, -0.9512456543366625272 ) ) ;
#115246=CARTESIAN_POINT ( 'NONE',  ( 5.203485844055394161, 1.958870149131001881, -1.047680120605886556 ) ) ;
#115248=CARTESIAN_POINT ( 'NONE',  ( 6.883263157960335832, 6.035928496661214560, 2.641088654967935323 ) ) ;
#115251=CARTESIAN_POINT ( 'NONE',  ( 6.619590441841330275, 0.3365870006281460047, -1.932621868259084330 ) ) ;
#115255=CARTESIAN_POINT ( 'NONE',  ( -0.08726289061519039436, -1.242903867559573161, -1.588418431006669351 ) ) ;
#115257=CARTESIAN_POINT ( 'NONE',  ( 4.773915743512389120, -2.023523412367009833, 0.3991901646795847913 ) ) ;
#115261=CARTESIAN_POINT ( 'NONE',  ( 5.676977070516882051, -0.04517083460114229565, -1.870152005306220611 ) ) ;
#115262=CARTESIAN_POINT ( 'NONE',  ( 4.852092609920839905, 0.1625460678297725725, -1.726498261149024271 ) ) ;
#115263=CARTESIAN_POINT ( 'NONE',  ( 4.388070221843799246, -0.3869516340575751001, -1.696700118790330558 ) ) ;
#115266=CARTESIAN_POINT ( 'NONE',  ( 2.138584244316643179, 0.5063124247480701445, 2.235611027800854078 ) ) ;
#115268=CARTESIAN_POINT ( 'NONE',  ( 5.232010533483211212, 2.060019964192044917, 0.3561100859283144460 ) ) ;
#115269=CARTESIAN_POINT ( 'NONE',  ( 1.235996726672627943, 0.3573974351761283752, 1.805938768738392319 ) ) ;
#115271=CARTESIAN_POINT ( 'NONE',  ( 2.865861461037176205, -0.1511401116795624278, -2.010826411938296143 ) ) ;
#115272=CARTESIAN_POINT ( 'NONE',  ( 1.465048628566959277, 0.1585425061045864503, -2.185770122351132994 ) ) ;
#115276=CARTESIAN_POINT ( 'NONE',  ( 1.732962091629593804, -1.965256999408044436, -0.6514315320021792921 ) ) ;
#115279=CARTESIAN_POINT ( 'NONE',  ( 3.967525559752110631, -1.763746451813380967, -1.176840329774282212 ) ) ;
#115281=CARTESIAN_POINT ( 'NONE',  ( 0.08247339995742437868, -1.868340020190910833, -0.4694531300831055742 ) ) ;
#115289=CARTESIAN_POINT ( 'NONE',  ( 3.058857861556500968, 0.4949273143410140574, 1.958058250343613693 ) ) ;
#115290=CARTESIAN_POINT ( 'NONE',  ( 1.483573828499670899, 1.945989852495342065, -0.8055925053903155719 ) ) ;
#115293=CARTESIAN_POINT ( 'NONE',  ( 4.803460451949028709, -1.436610920757129817, -1.182842806638328526 ) ) ;
#115299=CARTESIAN_POINT ( 'NONE',  ( 6.819229409281153842, -0.1590044787766713985, 2.026160355490718601 ) ) ;
#115304=CARTESIAN_POINT ( 'NONE',  ( 1.827078023146003760, -1.230200505038709036, 1.222094307470813934 ) ) ;
#115305=CARTESIAN_POINT ( 'NONE',  ( 1.569815774166925859, -1.651746245857487638, -0.5483857920917082351 ) ) ;
#115306=CARTESIAN_POINT ( 'NONE',  ( 6.235062949421072531, 0.2195253172713066969, 2.297251706954360095 ) ) ;
#115309=CARTESIAN_POINT ( 'NONE',  ( 2.143891142268034677, 0.7916089892260335104, -1.902880034897576733 ) ) ;
#115311=CARTESIAN_POINT ( 'NONE',  ( 1.106795812180675798, 0.8196504822069600182, -1.842164015508622521 ) ) ;
#115315=CARTESIAN_POINT ( 'NONE',  ( 6.684453402082996654, -1.835023323784425564, -0.3624468955198830722 ) ) ;
#115317=CARTESIAN_POINT ( 'NONE',  ( 4.746305163667582150, 0.9781546018433548983, -1.643150005489722787 ) ) ;
#115319=CARTESIAN_POINT ( 'NONE',  ( 5.813141826352885566, 1.944573597739504889, 1.043518232037063287 ) ) ;
#115323=CARTESIAN_POINT ( 'NONE',  ( 0.02995210924121824436, -1.980234168275105455, 0.3962368897427023806 ) ) ;
#115325=CARTESIAN_POINT ( 'NONE',  ( 4.507023749723728656, 1.786828103088284658, -1.460221407940938798 ) ) ;
#115326=CARTESIAN_POINT ( 'NONE',  ( 5.055110333045015558, 1.632132345252810035, -1.088295032039228172 ) ) ;
#115327=CARTESIAN_POINT ( 'NONE',  ( 2.360140415366944744, -1.961439503465340239, 0.04308618615556784187 ) ) ;
#115331=CARTESIAN_POINT ( 'NONE',  ( 0.04044418650436896329, 0.8167838292495681607, 1.953657075893009853 ) ) ;
#115334=CARTESIAN_POINT ( 'NONE',  ( 0.8492453639068753279, 1.839163117542693904, -0.08803940487626948919 ) ) ;
#115336=CARTESIAN_POINT ( 'NONE',  ( 4.698188964201695406, 0.9341788774818636787, -1.959971951513925781 ) ) ;
#115338=CARTESIAN_POINT ( 'NONE',  ( 2.215225606797793567, 1.700350911433265555, -1.266953333846132512 ) ) ;
#115342=CARTESIAN_POINT ( 'NONE',  ( 1.581398767000765426, 1.905217558097069386, -0.7859657096468860571 ) ) ;
#115343=AXIS2_PLACEMENT_3D ( 'NONE', #168336, #154221, #68672 ) ;
#115347=CARTESIAN_POINT ( 'NONE',  ( 0.07775346131142636674, 2.855377671833533970, -2.776861204146412021 ) ) ;
#115349=CARTESIAN_POINT ( 'NONE',  ( 5.408822929737922003, -0.4686924282312036061, -1.853821656156897868 ) ) ;
#115351=CARTESIAN_POINT ( 'NONE',  ( 1.968429645022830465, 1.162096202078844120, 1.940986467279571359 ) ) ;
#115353=CARTESIAN_POINT ( 'NONE',  ( 1.617148605665112537, 1.507408818846365017, 1.004416837792695194 ) ) ;
#115354=CARTESIAN_POINT ( 'NONE',  ( 1.938566325679047297, -1.478098309594473525, 1.218629399928832013 ) ) ;
#115355=CARTESIAN_POINT ( 'NONE',  ( 2.559107912120599071, 1.664280205102614429, -1.231313097332722872 ) ) ;
#115357=CARTESIAN_POINT ( 'NONE',  ( 1.094530253197498526, -0.4767503703589200392, -1.912843428949811075 ) ) ;
#115358=CARTESIAN_POINT ( 'NONE',  ( 5.602155610709171896, -1.926676517935271171, 0.002254597750208849581 ) ) ;
#115359=CARTESIAN_POINT ( 'NONE',  ( 1.208152727780729130, -0.5562822606778123902, 2.239534654701015981 ) ) ;
#115362=CARTESIAN_POINT ( 'NONE',  ( 5.758276963478038191, -2.062851381910678850, -0.003602753815758196875 ) ) ;
#115368=CARTESIAN_POINT ( 'NONE',  ( 0.04767123857605212733, -1.629476508726154016, -1.334019646271035198 ) ) ;
#115371=CARTESIAN_POINT ( 'NONE',  ( 4.973979902034267653, 1.240098594129716458, 1.770319513135506062 ) ) ;
#115372=CARTESIAN_POINT ( 'NONE',  ( 5.444012513273879250, -1.283034597847107161, -1.559753263307301463 ) ) ;
#115379=CARTESIAN_POINT ( 'NONE',  ( 3.696500153570709379, 1.422608671726926177, -1.429447704489300364 ) ) ;
#115384=CARTESIAN_POINT ( 'NONE',  ( 5.243122039519461097, -1.856066598825537373, 1.107904190987746063 ) ) ;
#115389=CARTESIAN_POINT ( 'NONE',  ( 5.466422796518627614, -1.967893101392578448, -0.4390109167287381542 ) ) ;
#115392=CARTESIAN_POINT ( 'NONE',  ( 0.4512176508754310866, 0.5462255407458499468, -1.636193974722987221 ) ) ;
#115397=CARTESIAN_POINT ( 'NONE',  ( 6.608674649642057197, 1.385883050205028333, -1.256505298338560062 ) ) ;
#115398=CARTESIAN_POINT ( 'NONE',  ( 0.4166524477783914437, -0.6801522605285510448, -1.894826352922045487 ) ) ;
#115400=CARTESIAN_POINT ( 'NONE',  ( 3.329339556154627289, 0.05228039400686017302, 2.206313527657398854 ) ) ;
#115404=CARTESIAN_POINT ( 'NONE',  ( 1.928540351845555056, -1.002238520345886785, -1.868699319572619366 ) ) ;
#115405=CARTESIAN_POINT ( 'NONE',  ( 1.581657880887325174, -0.6766953518495041342, 1.899626397962331126 ) ) ;
#115406=CARTESIAN_POINT ( 'NONE',  ( 2.513665319321151337, -0.5648568745635518251, 1.721363734954905356 ) ) ;
#115411=CARTESIAN_POINT ( 'NONE',  ( 0.4443725376216747236, -1.385435448976629180, 1.323305594895395343 ) ) ;
#115418=CARTESIAN_POINT ( 'NONE',  ( 4.223607183596161718, -2.069420184152844566, 0.6248923283326962563 ) ) ;
#115421=CARTESIAN_POINT ( 'NONE',  ( 2.232824136269210502, 1.381628265877183903, -1.608862310199298928 ) ) ;
#115423=CARTESIAN_POINT ( 'NONE',  ( 2.899638734157696796, -0.6216841358992927224, 1.870808799549168233 ) ) ;
#115426=CARTESIAN_POINT ( 'NONE',  ( 5.652785005015395825, -0.4769087673412530370, -1.910818445241519559 ) ) ;
#115427=CARTESIAN_POINT ( 'NONE',  ( 1.482261173788253394, -0.2847754331270537231, -1.920845095517382362 ) ) ;
#115432=CARTESIAN_POINT ( 'NONE',  ( 2.941443032221033427, 0.7519493320215028254, -1.950910760374990671 ) ) ;
#115436=CARTESIAN_POINT ( 'NONE',  ( 6.129550632656369125, -0.2293275368827427663, 1.898405681093485953 ) ) ;
#115438=CARTESIAN_POINT ( 'NONE',  ( 4.530015419921377351, -1.356323209173672106, -1.740806116466916187 ) ) ;
#115439=CARTESIAN_POINT ( 'NONE',  ( 1.905583573826599597, 1.834846665736546756, 1.225745012653912891 ) ) ;
#115441=CARTESIAN_POINT ( 'NONE',  ( 1.154776974461441341, 0.3738248154092556064, 1.875208037630435864 ) ) ;
#115445=CARTESIAN_POINT ( 'NONE',  ( 4.264170421968140445, -2.065031762457261610, 0.1491743435546449281 ) ) ;
#115449=CARTESIAN_POINT ( 'NONE',  ( 2.202237438260604030, -2.161223104231101644, 0.05255616829508147347 ) ) ;
#115450=CARTESIAN_POINT ( 'NONE',  ( 3.157961424266928052, 0.9873743524775533409, 1.956624655947765357 ) ) ;
#115456=PRODUCT_DEFINITION_CONTEXT ( 'detailed design', #60163, 'design' ) ;
#115457=CARTESIAN_POINT ( 'NONE',  ( 0.1060925565549031974, -0.09613213100253051313, 2.014232862735332308 ) ) ;
#115459=CARTESIAN_POINT ( 'NONE',  ( 4.223533608758993196, 0.2584441732129874603, -2.054024224480345939 ) ) ;
#115460=CARTESIAN_POINT ( 'NONE',  ( 5.800440434243619769, 1.421441630026821112, -1.569310636533404635 ) ) ;
#115463=CARTESIAN_POINT ( 'NONE',  ( 4.487129304207951641, 0.09229547738082846675, 1.967383831439367903 ) ) ;
#115464=CARTESIAN_POINT ( 'NONE',  ( 6.070342170859510667, -2.174803699615239783, -0.7246130948556377405 ) ) ;
#115465=CARTESIAN_POINT ( 'NONE',  ( 2.701551412915685457, -0.5726843992823158480, 1.733614832724015731 ) ) ;
#115471=CARTESIAN_POINT ( 'NONE',  ( 4.482685760555058074, -1.311686992106766203, 1.527362355471563182 ) ) ;
#115472=CARTESIAN_POINT ( 'NONE',  ( 4.522284091987982535, 0.9210895807079204634, 1.732038000912524689 ) ) ;
#115477=CARTESIAN_POINT ( 'NONE',  ( 0.2047783418026409563, 1.821168281471240435, 1.026754182986739927 ) ) ;
#115478=CARTESIAN_POINT ( 'NONE',  ( 6.034039731144309471, 0.8686908000094315518, -1.541921269980907949 ) ) ;
#115480=CARTESIAN_POINT ( 'NONE',  ( 1.781448188194576066, 1.512826363221421833, 1.585725795389548942 ) ) ;
#115481=CARTESIAN_POINT ( 'NONE',  ( 1.135833342500572440, 0.3383711564543417927, 1.707032442944929729 ) ) ;
#115483=CARTESIAN_POINT ( 'NONE',  ( 1.136830759877343722, -1.561040526032995590, 0.7340551814495520633 ) ) ;
#115484=CARTESIAN_POINT ( 'NONE',  ( 1.101424459656743071, -0.5276332240332289869, 2.126988402630063835 ) ) ;
#115485=CARTESIAN_POINT ( 'NONE',  ( 2.666872310945223923, -1.521158656661812714, 1.599105504226288499 ) ) ;
#115486=CARTESIAN_POINT ( 'NONE',  ( 0.9718041211803396529, -0.3205511010368928271, 2.147183668106082521 ) ) ;
#115488=CARTESIAN_POINT ( 'NONE',  ( 1.991562931776114542, -0.4585136385713373675, 2.066967827372573563 ) ) ;
#115489=CARTESIAN_POINT ( 'NONE',  ( 6.827182134110157286, 6.032625672350935275, 2.883942191975923830 ) ) ;
#115491=CARTESIAN_POINT ( 'NONE',  ( 2.419810632640221115, -1.322813552229468614, -1.872022261021451639 ) ) ;
#115495=CARTESIAN_POINT ( 'NONE',  ( 4.969482899335432968, -1.875980303166164376, -1.189202907730102732 ) ) ;
#115503=CARTESIAN_POINT ( 'NONE',  ( 3.340470361411255418, 0.4872029778183216697, -1.956561305313428978 ) ) ;
#115505=CARTESIAN_POINT ( 'NONE',  ( 1.516546868092843781, 0.8322427235708649285, 1.887369835301610621 ) ) ;
#115511=CARTESIAN_POINT ( 'NONE',  ( 3.961010909407122860, 0.2689195440248594027, -2.174814543647784593 ) ) ;
#115512=CARTESIAN_POINT ( 'NONE',  ( 1.195935645703485539, 1.779627574718087635, 0.9480385367472210500 ) ) ;
#115513=CARTESIAN_POINT ( 'NONE',  ( 0.8371598888798935656, 0.7463826720714299423, -1.683355135116317847 ) ) ;
#115515=CARTESIAN_POINT ( 'NONE',  ( 5.596661130663158623, -0.4455768995972574364, -1.770251349769519367 ) ) ;
#115516=CARTESIAN_POINT ( 'NONE',  ( 5.643203987388664800, 0.8197706014990979728, 1.842448445624145226 ) ) ;
#115518=CARTESIAN_POINT ( 'NONE',  ( 4.821284755203490313, -0.1158696699916968720, 2.259674544810440278 ) ) ;
#115520=CARTESIAN_POINT ( 'NONE',  ( 0.7156196601619690956, -0.3068708111382661974, 2.083463767009658962 ) ) ;
#115522=CARTESIAN_POINT ( 'NONE',  ( 4.316890830952234914, -1.536253448065309613, 1.388129241271539138 ) ) ;
#115532=CARTESIAN_POINT ( 'NONE',  ( 0.2465380642357860586, 1.084720387836759725, -1.822023332652397354 ) ) ;
#115533=CARTESIAN_POINT ( 'NONE',  ( 1.441950287000768771, -2.089521377041357653, 0.7543469697938051111 ) ) ;
#115537=CARTESIAN_POINT ( 'NONE',  ( 3.402741375674179114, 0.4741672551989496998, 1.903589013717405853 ) ) ;
#115543=CARTESIAN_POINT ( 'NONE',  ( 2.303126745213024851, -0.3670769733005623814, -2.088442229865586697 ) ) ;
#115545=CARTESIAN_POINT ( 'NONE',  ( 3.947668504265917644, 1.419370528949075005, 1.354593381527373186 ) ) ;
#115546=CARTESIAN_POINT ( 'NONE',  ( 3.696290335837215668, -2.159122111672501454, -0.1082323872379290647 ) ) ;
#115547=CARTESIAN_POINT ( 'NONE',  ( 3.157574601152390414, 0.8305207305269333151, 1.643389852989694200 ) ) ;
#115550=CARTESIAN_POINT ( 'NONE',  ( 5.120954501598782294, -1.650910780824323298, 0.5508982476954398244 ) ) ;
#115553=CARTESIAN_POINT ( 'NONE',  ( 6.620655732516647518, 0.007553340620044743381, 1.826407896915738238 ) ) ;
#115554=CARTESIAN_POINT ( 'NONE',  ( 1.745224485312408813, -1.826185749030174499, 1.156423465944363294 ) ) ;
#115555=CARTESIAN_POINT ( 'NONE',  ( 4.323592178502837058, -1.495822217463145476, 1.351947993609707632 ) ) ;
#115557=CARTESIAN_POINT ( 'NONE',  ( 1.516726440323381331, 1.451591637995581996, -1.601975981646540426 ) ) ;
#115559=CARTESIAN_POINT ( 'NONE',  ( 2.249238725404782091, -1.581088017263340806, -1.177247449022495118 ) ) ;
#115560=CARTESIAN_POINT ( 'NONE',  ( 6.509000000000010111, 6.037005099786168394, 2.594901386363585694 ) ) ;
#115561=CARTESIAN_POINT ( 'NONE',  ( 3.561997098397641448, -1.302002156301942604, 1.441148521680717387 ) ) ;
#115569=CARTESIAN_POINT ( 'NONE',  ( 1.149787729276055437, -1.740433383357189223, -1.356609624190791008 ) ) ;
#115571=CARTESIAN_POINT ( 'NONE',  ( 5.190269257085567745, 1.011813749630154691, -1.680575076195559792 ) ) ;
#115573=CARTESIAN_POINT ( 'NONE',  ( 3.362624215892480173, -2.041811681064845896, -0.5603701389207839112 ) ) ;
#115575=CARTESIAN_POINT ( 'NONE',  ( 0.1747926744264452492, 5.725295659261265158, -2.449351454080525681 ) ) ;
#115576=CARTESIAN_POINT ( 'NONE',  ( 4.136529068399773301, -1.600833271991594309, 0.9093273525555560788 ) ) ;
#115582=CARTESIAN_POINT ( 'NONE',  ( 5.220985865760717992, 1.604251394084664550, -1.386888226476624242 ) ) ;
#115583=CARTESIAN_POINT ( 'NONE',  ( -0.1104750535120025967, -0.004616138082884357029, -2.103378236956429337 ) ) ;
#115585=CARTESIAN_POINT ( 'NONE',  ( 5.413377607122367152, -0.3064755606005803434, 2.037752308911133348 ) ) ;
#115587=CARTESIAN_POINT ( 'NONE',  ( 1.187708300173949461, -1.176858333569561932, -1.441725857702576219 ) ) ;
#115588=CARTESIAN_POINT ( 'NONE',  ( 4.106863108761789505, -0.3106082297497716471, 1.814695527881895476 ) ) ;
#115594=CARTESIAN_POINT ( 'NONE',  ( 3.686314334879085663, -1.088174899301070253, 1.919869060924610293 ) ) ;
#115595=CARTESIAN_POINT ( 'NONE',  ( 4.394006599171666139, -0.8711832027283890056, 2.088141772348524050 ) ) ;
#115597=CARTESIAN_POINT ( 'NONE',  ( 4.464998409566146798, -1.450835031669978292, 1.084616504919968305 ) ) ;
#115598=CARTESIAN_POINT ( 'NONE',  ( 5.366386423658583205, -1.870495304593930097, -0.4130858509987145877 ) ) ;
#115599=CARTESIAN_POINT ( 'NONE',  ( 6.727182134110222478, 0.005875948494733079785, 1.810970247402940547 ) ) ;
#115600=CARTESIAN_POINT ( 'NONE',  ( 5.190257414508706368, -1.856628772771324210, -0.2281712211116558864 ) ) ;
#115601=CARTESIAN_POINT ( 'NONE',  ( 5.934019871859393724, 1.109147300373466871, 1.494279092885692606 ) ) ;
#115603=CARTESIAN_POINT ( 'NONE',  ( 6.051566426668148146, 0.5099629880620482059, -1.694758430261036564 ) ) ;
#115605=CARTESIAN_POINT ( 'NONE',  ( 0.2863426850727782136, -0.6839425765656822476, -1.897108587135355684 ) ) ;
#115607=CARTESIAN_POINT ( 'NONE',  ( 2.737057789242686390, 0.2582918889518608374, 2.090101187703028884 ) ) ;
#115612=CARTESIAN_POINT ( 'NONE',  ( 1.775654988352931563, 0.3410282263864356511, -1.990609417402624537 ) ) ;
#115615=CARTESIAN_POINT ( 'NONE',  ( 3.356853517036356038, -1.639235867460669072, 1.409173823127254366 ) ) ;
#115616=CARTESIAN_POINT ( 'NONE',  ( 6.889999999999965041, 7.051532193125384040, 2.878152852197481071 ) ) ;
#115623=CARTESIAN_POINT ( 'NONE',  ( 0.9080814035550346386, -0.9900877184637231210, -1.955254813705724404 ) ) ;
#115625=CARTESIAN_POINT ( 'NONE',  ( 1.798126127191189472, -0.7612548243747189192, 2.130717213291497547 ) ) ;
#115632=CARTESIAN_POINT ( 'NONE',  ( 3.215802288110910290, -0.8691132097216300867, -1.541513200001721540 ) ) ;
#115633=CARTESIAN_POINT ( 'NONE',  ( 6.071336392737415544, 0.1682094380959769098, -2.200428349287026908 ) ) ;
#115637=CARTESIAN_POINT ( 'NONE',  ( 4.763296089436113157, 1.880429982106451181, -0.7283946704290320540 ) ) ;
#115640=CARTESIAN_POINT ( 'NONE',  ( 2.289737743334671283, -0.8020533187339596859, 1.690132462187944107 ) ) ;
#115641=CARTESIAN_POINT ( 'NONE',  ( 3.485274717979901293, 0.04603381543630095940, 2.069897711131869933 ) ) ;
#115644=CARTESIAN_POINT ( 'NONE',  ( 1.880979024232478425, -1.749874716401520036, -0.7718601483891265325 ) ) ;
#115650=CARTESIAN_POINT ( 'NONE',  ( 0.8086807686161383568, -0.4671638426185490967, -1.854305266343849956 ) ) ;
#115653=CARTESIAN_POINT ( 'NONE',  ( 2.717183929654675811, -1.705535211757349456, -0.9694657131227711888 ) ) ;
#115659=CARTESIAN_POINT ( 'NONE',  ( 0.3857445262360514882, -0.8876765639535091346, 1.646530163845527195 ) ) ;
#115661=CARTESIAN_POINT ( 'NONE',  ( 1.705339411233731672, 1.749488060808137790, -0.9960635233151514667 ) ) ;
#115663=CARTESIAN_POINT ( 'NONE',  ( 0.9314518356654817310, -1.671823418590481447, -1.299033474062233351 ) ) ;
#115665=CARTESIAN_POINT ( 'NONE',  ( 3.227070907399377298, -1.911900318415656441, -0.7948586591664741352 ) ) ;
#115667=CARTESIAN_POINT ( 'NONE',  ( 5.771452434752829319, 1.244600244801373767, 1.679635579212119145 ) ) ;
#115669=CARTESIAN_POINT ( 'NONE',  ( 4.278209411971904075, -1.050932907216840295, 1.492538610026641122 ) ) ;
#115673=CARTESIAN_POINT ( 'NONE',  ( 5.245248717291847385, -1.895131572898335115, 1.130396782059706950 ) ) ;
#115677=CARTESIAN_POINT ( 'NONE',  ( 3.949791169003769475, -1.320912084567291034, -1.382976300589415342 ) ) ;
#115685=CARTESIAN_POINT ( 'NONE',  ( 0.06366010765614799061, -1.203631707120488947, 1.393476991864414760 ) ) ;
#115688=CARTESIAN_POINT ( 'NONE',  ( 5.272658424858247095, -1.760895560629770262, -0.6313210838888929644 ) ) ;
#115694=CARTESIAN_POINT ( 'NONE',  ( 1.217558188649459527, 0.3894938459214473125, -1.930362121600463610 ) ) ;
#115696=CARTESIAN_POINT ( 'NONE',  ( 1.862907868837269998, -0.1017702599966328891, -2.013986063733465226 ) ) ;
#115700=CARTESIAN_POINT ( 'NONE',  ( 2.589988673929614738, -2.185656584452956075, -0.1600571409424780822 ) ) ;
#115701=CARTESIAN_POINT ( 'NONE',  ( 6.340460056601358474, 1.806591233369018834, 0.2625940548972791611 ) ) ;
#115703=CARTESIAN_POINT ( 'NONE',  ( 6.825078400183573812, 7.629137130509070275, 2.455651831298297338 ) ) ;
#115711=CARTESIAN_POINT ( 'NONE',  ( 5.372543328820884589, -0.05112055865702340440, -1.840719716649619198 ) ) ;
#115712=CARTESIAN_POINT ( 'NONE',  ( 2.262359935378143394, 2.012689932058016495, 0.04726890441942610543 ) ) ;
#115713=CARTESIAN_POINT ( 'NONE',  ( 3.146212962842390937, -0.1666923573656608759, -2.292372948102610053 ) ) ;
#115715=CARTESIAN_POINT ( 'NONE',  ( 1.358004595412452664, -1.861131634099476573, -0.006961619045023344915 ) ) ;
#115719=CARTESIAN_POINT ( 'NONE',  ( 4.060738401289211374, 0.5150538496448524572, 1.841637258418599155 ) ) ;
#115722=CARTESIAN_POINT ( 'NONE',  ( 3.983990651536262195, -2.068283627568163308, -0.3046923749255076586 ) ) ;
#115723=CARTESIAN_POINT ( 'NONE',  ( 1.797508989346347619, -0.6330400025267440833, 1.760413054629046625 ) ) ;
#115726=CARTESIAN_POINT ( 'NONE',  ( 6.058133912487986272, -1.297239342979487509, 1.306937132449899508 ) ) ;
#115729=CARTESIAN_POINT ( 'NONE',  ( 4.775862138867135620, 0.9967549737653296216, 1.407514542897546850 ) ) ;
#115735=CARTESIAN_POINT ( 'NONE',  ( 5.207971749312423348, 0.6875717650507988665, -2.059362367386765591 ) ) ;
#115736=CARTESIAN_POINT ( 'NONE',  ( 3.650846181029033133, -1.491723252493650564, 1.052289205326197852 ) ) ;
#115737=CARTESIAN_POINT ( 'NONE',  ( 0.9714493606215730548, -0.2934177832072166758, 1.939591667560663035 ) ) ;
#115738=CARTESIAN_POINT ( 'NONE',  ( 5.313701412219064224, -1.345319185855331279, -1.634962184252206630 ) ) ;
#115739=CARTESIAN_POINT ( 'NONE',  ( 6.216396969532355321, 2.137338928125806614, 0.8291867496624371059 ) ) ;
#115743=CARTESIAN_POINT ( 'NONE',  ( 1.225412164737609055, 1.871785320780447792, 0.9964087003688710809 ) ) ;
#115747=CARTESIAN_POINT ( 'NONE',  ( 6.491115304390381979, 0.2044268322529273207, 2.161409909153473752 ) ) ;
#115748=CARTESIAN_POINT ( 'NONE',  ( 6.883263157960391787, 1.253787318140922480, 2.167784446185747171 ) ) ;
#115750=CARTESIAN_POINT ( 'NONE',  ( 2.842673000788879634, 1.232056068812878991, -1.848115600964394867 ) ) ;
#115752=CARTESIAN_POINT ( 'NONE',  ( 6.486953984781112403, -2.015912550161761629, 0.05229459904129707404 ) ) ;
#115754=CARTESIAN_POINT ( 'NONE',  ( 4.803617054199708747, -1.591134784341166508, -1.312391874486463550 ) ) ;
#115756=CARTESIAN_POINT ( 'NONE',  ( -0.2408018239684096284, -0.007136184528808932684, -2.100252307185761058 ) ) ;
#115760=CARTESIAN_POINT ( 'NONE',  ( 0.6739141125756157313, -1.159797070128726793, 1.739218980263528946 ) ) ;
#115761=CARTESIAN_POINT ( 'NONE',  ( 4.317794123949899365, 1.129187743159822288, -1.454283868005897151 ) ) ;
#115764=CARTESIAN_POINT ( 'NONE',  ( 2.221339967433374252, -1.673790515994465711, 0.4157018595009522310 ) ) ;
#115766=CARTESIAN_POINT ( 'NONE',  ( 1.776460590643181625, 1.997282851074515975, -1.137850514363091481 ) ) ;
#115768=CARTESIAN_POINT ( 'NONE',  ( 0.8258823708265795593, -2.148021843699068789, 0.7105549608077809109 ) ) ;
#115769=CARTESIAN_POINT ( 'NONE',  ( 4.319037722229518650, 1.925386421186209507, 0.8538897750212376403 ) ) ;
#115771=CARTESIAN_POINT ( 'NONE',  ( 2.723612921674794407, -1.015349471937683656, -1.449289906420585305 ) ) ;
#115779=CARTESIAN_POINT ( 'NONE',  ( 5.133148801814766848, 2.052693810517117079, 0.8496366593433544168 ) ) ;
#115780=CARTESIAN_POINT ( 'NONE',  ( 3.363397379774799134, 2.138023915923603635, -0.4802275100637617977 ) ) ;
#115783=CARTESIAN_POINT ( 'NONE',  ( 5.795592431653455279, 1.959276243578732091, -0.8114611383256833399 ) ) ;
#115786=CARTESIAN_POINT ( 'NONE',  ( 6.890000000000001457, 2.439643239904603966, 2.382311923195524095 ) ) ;
#115788=CARTESIAN_POINT ( 'NONE',  ( 5.361630242575341931, -1.673063676233761621, -1.302930760576012092 ) ) ;
#115792=FACE_OUTER_BOUND ( 'NONE', #89876, .T. ) ;
#115794=CARTESIAN_POINT ( 'NONE',  ( 6.427308110136687347, -1.208249125052461181, -1.389453836245766016 ) ) ;
#115798=CARTESIAN_POINT ( 'NONE',  ( 1.504977638028012432, -1.727349551440153119, 0.2125612633746311042 ) ) ;
#115800=CARTESIAN_POINT ( 'NONE',  ( 0.2913577194270203785, -1.795273245208812485, 0.7915465721433642132 ) ) ;
#115803=CARTESIAN_POINT ( 'NONE',  ( 4.733375416736937069, -1.977748744329570263, 0.8730265686548792647 ) ) ;
#115808=CARTESIAN_POINT ( 'NONE',  ( 4.750933126423753095, -1.738186171353903742, 1.284983810367075208 ) ) ;
#115812=CARTESIAN_POINT ( 'NONE',  ( 5.518811311470022574, 1.820418058502238035, 0.7569790930031635723 ) ) ;
#115813=CARTESIAN_POINT ( 'NONE',  ( 5.272643526055802887, -1.725312034932389382, 0.1713184177872198732 ) ) ;
#115816=CARTESIAN_POINT ( 'NONE',  ( 1.699035084177059174, 1.824418957995146195, 1.213967346723361596 ) ) ;
#115817=CARTESIAN_POINT ( 'NONE',  ( 3.751255533806226339, -1.888273344036644819, 1.326175916821286105 ) ) ;
#115818=CARTESIAN_POINT ( 'NONE',  ( 4.692684478349196553, -0.4476203070050369104, -2.011419953914685088 ) ) ;
#115819=CARTESIAN_POINT ( 'NONE',  ( 0.2341854262303414147, 0.3310631332954366290, 1.913375037591731775 ) ) ;
#115823=CARTESIAN_POINT ( 'NONE',  ( 4.342108446431157454, -1.306982937058022820, -1.669832246961988176 ) ) ;
#115825=CARTESIAN_POINT ( 'NONE',  ( 1.248672897702383988, 1.986100274556975354, -0.3474695496914689818 ) ) ;
#115827=CARTESIAN_POINT ( 'NONE',  ( 4.823365732668142947, -0.1123398232194070118, 2.204042774474362254 ) ) ;
#115830=CARTESIAN_POINT ( 'NONE',  ( 0.1399997263885795484, 5.723012109828673921, -2.593777676649943409 ) ) ;
#115837=CARTESIAN_POINT ( 'NONE',  ( 3.010674446437047624, 1.493694004556917365, -1.420165857245965668 ) ) ;
#115840=CARTESIAN_POINT ( 'NONE',  ( 3.264323853713008816, 2.019862492602925386, -0.002211735406987268802 ) ) ;
#115843=CARTESIAN_POINT ( 'NONE',  ( 3.256764320543267921, -1.561506546599530143, 1.345091337369247242 ) ) ;
#115846=CARTESIAN_POINT ( 'NONE',  ( -0.1409997244346087863, -0.002808977843308038246, -2.000147647483837776 ) ) ;
#115847=CARTESIAN_POINT ( 'NONE',  ( 1.569984571489828173, -1.747861548559765721, -0.5788160320587890650 ) ) ;
#115849=CARTESIAN_POINT ( 'NONE',  ( 6.691986956589398794, -0.9478133180038283978, 1.990996264204819122 ) ) ;
#115851=CARTESIAN_POINT ( 'NONE',  ( 1.142116303652768172, 0.8771353898661786719, -1.975824051420910221 ) ) ;
#115853=CARTESIAN_POINT ( 'NONE',  ( 2.202361591730035428, 1.313542931311746598, -1.530159205979222170 ) ) ;
#115856=CARTESIAN_POINT ( 'NONE',  ( 0.1626889888870358680, -1.668787113083155305, -0.8454427722031019332 ) ) ;
#115858=CARTESIAN_POINT ( 'NONE',  ( 4.434422825387909661, 1.933224968735423266, 0.3856102937377944295 ) ) ;
#115859=CARTESIAN_POINT ( 'NONE',  ( 4.979703994296570180, -0.7212954316567052881, 1.883311551353183511 ) ) ;
#115863=CARTESIAN_POINT ( 'NONE',  ( 6.568975480045090798, -1.924755568788787397, -0.8553139683228675461 ) ) ;
#115864=CARTESIAN_POINT ( 'NONE',  ( 4.844224204019831781, -0.9789346907586125024, 1.824324395707350943 ) ) ;
#115867=CARTESIAN_POINT ( 'NONE',  ( 6.639320575229283428, 0.5834889568891787892, 2.056715522164854981 ) ) ;
#115868=CARTESIAN_POINT ( 'NONE',  ( 5.097918204798724595, 1.359643563815411405, 1.493766824747685185 ) ) ;
#115870=CARTESIAN_POINT ( 'NONE',  ( 3.879734811474966794, 2.173438607767137043, -0.7759833549572618949 ) ) ;
#115872=CARTESIAN_POINT ( 'NONE',  ( 1.235300832636996970, -0.04672723545543105983, -2.062185333280424526 ) ) ;
#115879=CARTESIAN_POINT ( 'NONE',  ( 3.789651875377809898, -2.007375656734013969, 0.8277776116962390907 ) ) ;
#115883=CARTESIAN_POINT ( 'NONE',  ( 3.227900028218867234, 1.797025815167479390, 0.4004103908350764573 ) ) ;
#115885=CARTESIAN_POINT ( 'NONE',  ( 4.792620198997869174, 1.822056328612733145, -1.217503271791681163 ) ) ;
#115887=CARTESIAN_POINT ( 'NONE',  ( 5.190393989392352303, -2.244764952986468831, -0.2824595779603657486 ) ) ;
#115892=CARTESIAN_POINT ( 'NONE',  ( 6.274623264596165484, -1.681128386917314366, -0.5530667918781423387 ) ) ;
#115893=CARTESIAN_POINT ( 'NONE',  ( 3.791655721365494891, 1.894798488814054327, -0.6802303536831488806 ) ) ;
#115895=CARTESIAN_POINT ( 'NONE',  ( 3.118299990072324057, -1.036503014707575332, -1.833135815837197535 ) ) ;
#115896=CARTESIAN_POINT ( 'NONE',  ( 0.5619445578959707532, -1.063298924184744587, 1.593181094007071863 ) ) ;
#115898=CARTESIAN_POINT ( 'NONE',  ( 1.697640821309716497, -1.424308401971938975, -1.360563176039381261 ) ) ;
#115900=CARTESIAN_POINT ( 'NONE',  ( 1.006479672118578916, 1.419055151971573059, -1.218976214888117804 ) ) ;
#115901=CARTESIAN_POINT ( 'NONE',  ( 1.381223342121252085, -0.05156877537583307025, 1.961363007973878858 ) ) ;
#115902=CARTESIAN_POINT ( 'NONE',  ( 0.07037084582631887575, 0.7337836260858082715, 1.766209603411242668 ) ) ;
#115906=CARTESIAN_POINT ( 'NONE',  ( 5.682452175617663137, -1.825344843996518529, -0.4084625512627630406 ) ) ;
#115911=CARTESIAN_POINT ( 'NONE',  ( 0.9771079587245214970, 1.912259438035465386, 0.7939916666956441382 ) ) ;
#115916=CARTESIAN_POINT ( 'NONE',  ( 5.848313825214911610, 1.045240856298999432, -1.844880668361434939 ) ) ;
#115921=CARTESIAN_POINT ( 'NONE',  ( 5.846142468697441252, -0.8834969228576605715, 1.751761657833034613 ) ) ;
#115923=CARTESIAN_POINT ( 'NONE',  ( 2.776720060080526853, -1.994564479802892087, 0.2930246351905210211 ) ) ;
#115924=CARTESIAN_POINT ( 'NONE',  ( 4.171028900271775974, 1.708651049203385286, -0.8665242481073615055 ) ) ;
#115926=CARTESIAN_POINT ( 'NONE',  ( 1.558417602779540889, -1.546676288433556756, 1.552911753681482487 ) ) ;
#115928=CARTESIAN_POINT ( 'NONE',  ( 3.426877311086639288, 0.04264493303338459662, 1.870215716092846314 ) ) ;
#115932=CARTESIAN_POINT ( 'NONE',  ( 5.062167955004798436, -1.175237403299607797, 1.760913580352542862 ) ) ;
#115936=CARTESIAN_POINT ( 'NONE',  ( 2.419574211619343274, -1.206166186839405352, -1.707533215648052050 ) ) ;
#115937=CARTESIAN_POINT ( 'NONE',  ( 6.620655732516668834, 6.034240673559561507, 2.768629221164942145 ) ) ;
#115938=CARTESIAN_POINT ( 'NONE',  ( 1.307153468561640164, -0.4245502288011630543, 1.671566548543522268 ) ) ;
#115943=SURFACE_SIDE_STYLE ('',( #63933 ) ) ;
#115947=CARTESIAN_POINT ( 'NONE',  ( 0.7854713186128524649, 1.746033005210102962, -0.4821264535347525859 ) ) ;
#115956=ORIENTED_EDGE ( 'NONE', *, *, #37732, .F. ) ;
#115957=CARTESIAN_POINT ( 'NONE',  ( 2.734617598447198539, -1.779929554887052401, -0.5434082684390993956 ) ) ;
#115958=CARTESIAN_POINT ( 'NONE',  ( 0.3510145263703016716, 0.1867627727243931779, -1.906451055755745250 ) ) ;
#115959=CARTESIAN_POINT ( 'NONE',  ( 6.264670948233396430, -1.361836867979081545, 1.362739274238314868 ) ) ;
#115967=CARTESIAN_POINT ( 'NONE',  ( 5.032068834786890044, 1.130672129898707245, 1.612349476345806831 ) ) ;
#115969=CARTESIAN_POINT ( 'NONE',  ( 1.330900338397854155, 1.421537331630345014, -1.573617108223644312 ) ) ;
#115972=CARTESIAN_POINT ( 'NONE',  ( 6.351546390744762682, 2.185874319550953793, -0.1572705277706408500 ) ) ;
#115974=CARTESIAN_POINT ( 'NONE',  ( 3.891558735110557610, 1.394649387769153259, 1.329109640543422399 ) ) ;
#115977=CARTESIAN_POINT ( 'NONE',  ( 0.2701547006425785713, -1.196777392914155635, 1.378664180083796875 ) ) ;
#115978=CARTESIAN_POINT ( 'NONE',  ( 1.260703874955213744, 0.8971468365699288849, 2.016480257658866737 ) ) ;
#115981=PRESENTATION_STYLE_ASSIGNMENT (( #143399 ) ) ;
#115983=CARTESIAN_POINT ( 'NONE',  ( 6.737161338948785883, -0.09310609838950174855, -1.967343120315911298 ) ) ;
#115984=CARTESIAN_POINT ( 'NONE',  ( 1.909617033088998328, -0.9174269660217245770, -1.711723090954318405 ) ) ;
#115985=CARTESIAN_POINT ( 'NONE',  ( 6.186922437512073714, -1.269050685324083050, -1.916131536371464383 ) ) ;
#115987=CARTESIAN_POINT ( 'NONE',  ( 4.223391696059366929, 0.2311737859471388323, -1.846484453672825321 ) ) ;
#115992=CARTESIAN_POINT ( 'NONE',  ( -0.02351032182101517320, -2.127384168920816165, -0.5261613093957145937 ) ) ;
#115997=CARTESIAN_POINT ( 'NONE',  ( 1.699542765152612711, -0.6164703606487754728, 1.718597393154073671 ) ) ;
#115999=CARTESIAN_POINT ( 'NONE',  ( 3.797271647414564910, 1.222981480435406443, -1.229749918556479304 ) ) ;
#116004=CARTESIAN_POINT ( 'NONE',  ( 0.3109947909220554529, 1.675391530434092280, 0.9509023542121838313 ) ) ;
#116005=CARTESIAN_POINT ( 'NONE',  ( 4.750807836863311095, -0.4258335417525476729, -1.914832529679215023 ) ) ;
#116008=CARTESIAN_POINT ( 'NONE',  ( 5.110073233524446756, -0.7627883623938614965, 1.978724553277847464 ) ) ;
#116012=CARTESIAN_POINT ( 'NONE',  ( 2.659107809384615884, 1.665393510391148801, -1.229642267604726058 ) ) ;
#116016=CARTESIAN_POINT ( 'NONE',  ( 2.584987504963653038, -0.7174396784795608051, 2.183947998982360250 ) ) ;
#116024=CARTESIAN_POINT ( 'NONE',  ( 4.517770118113122457, -0.5046507728132009207, 1.844564425022446885 ) ) ;
#116026=CARTESIAN_POINT ( 'NONE',  ( 4.735197965344590365, -1.576124854778211626, 0.7008788178320748408 ) ) ;
#116027=CARTESIAN_POINT ( 'NONE',  ( 3.977750132953357998, -0.7672935630990398437, 1.865046046545227654 ) ) ;
#116028=CARTESIAN_POINT ( 'NONE',  ( 5.080843078579284189, -0.8290085517158821693, 2.144167039965215071 ) ) ;
#116029=CARTESIAN_POINT ( 'NONE',  ( 1.120068590173186163, -2.152398693614396397, 0.4866647226241942459 ) ) ;
#116031=CARTESIAN_POINT ( 'NONE',  ( 6.292257686217937795, -1.761477974832075244, -0.1709902323579186867 ) ) ;
#116033=CARTESIAN_POINT ( 'NONE',  ( 2.361634033267061561, 2.247686861432355077, -0.4490786020208848983 ) ) ;
#116034=CARTESIAN_POINT ( 'NONE',  ( 0.07555271646370392835, -1.686692104669092807, -0.4283695578703243245 ) ) ;
#116036=CARTESIAN_POINT ( 'NONE',  ( 6.474583112218436298, -0.1034247314782872212, -2.189140632845664403 ) ) ;
#116040=CARTESIAN_POINT ( 'NONE',  ( 0.3093308919281665959, -1.743438469055924145, 1.293836907758689758 ) ) ;
#116041=CARTESIAN_POINT ( 'NONE',  ( 1.798064920797682653, -0.9548589541341389042, -1.776165177175797583 ) ) ;
#116043=CARTESIAN_POINT ( 'NONE',  ( 5.268162717194916134, 0.9514403766726580169, 1.675093392909310142 ) ) ;
#116045=CARTESIAN_POINT ( 'NONE',  ( 2.531719857061366152, -0.2131849592692437734, 2.211133432850121761 ) ) ;
#116051=CARTESIAN_POINT ( 'NONE',  ( 4.300191697305631777, 1.341742100086223743, -1.108517911846224502 ) ) ;
#116052=CARTESIAN_POINT ( 'NONE',  ( 3.613678190204441254, 0.4790664972640528707, -1.902336835828049244 ) ) ;
#116057=CARTESIAN_POINT ( 'NONE',  ( 1.293506021254931193, -1.865543137965872678, 0.8802379953135958113 ) ) ;
#116060=CARTESIAN_POINT ( 'NONE',  ( 1.552057811931725428, 0.6552935188219483065, -2.165526471026494537 ) ) ;
#116063=CARTESIAN_POINT ( 'NONE',  ( 3.057714436724996876, 1.861869414292870006, -0.1796979844640861634 ) ) ;
#116064=CARTESIAN_POINT ( 'NONE',  ( 1.424001084297383146, -1.255706242181073851, -1.196294345734474129 ) ) ;
#116065=CARTESIAN_POINT ( 'NONE',  ( 5.232042516939362287, 2.159042084939459816, 0.3751777721049884273 ) ) ;
#116066=CARTESIAN_POINT ( 'NONE',  ( 6.212023164884419302, -2.291203086667678690, 0.2740844210103609568 ) ) ;
#116067=CARTESIAN_POINT ( 'NONE',  ( 1.604443549136617575, -0.7409017435648653782, -1.923293390451373819 ) ) ;
#116068=CARTESIAN_POINT ( 'NONE',  ( 3.855361883123554989, 1.927135149742021047, -0.2389370807101970084 ) ) ;
#116070=CARTESIAN_POINT ( 'NONE',  ( 6.116445839754358182, 1.256427234498383561, -1.385894902050835542 ) ) ;
#116071=CARTESIAN_POINT ( 'NONE',  ( 1.781250000000001332, 0.7852924748300815772, 1.895863743164048154 ) ) ;
#116073=CARTESIAN_POINT ( 'NONE',  ( 0.2273701076888709205, -1.544753302685021534, -0.7874640570253422789 ) ) ;
#116075=CARTESIAN_POINT ( 'NONE',  ( 4.166638809851969327, 1.319227567334404494, 1.525044649537968589 ) ) ;
#116079=CARTESIAN_POINT ( 'NONE',  ( 2.086296903703276140, -1.790263230197926436, -0.3570169370194844483 ) ) ;
#116087=CARTESIAN_POINT ( 'NONE',  ( -0.1755239516839811886, -0.8679694584908944632, -1.822324207963136988 ) ) ;
#116088=CARTESIAN_POINT ( 'NONE',  ( 6.305373609846285810, 1.934184411435871498, -1.092212275460135773 ) ) ;
#116092=CARTESIAN_POINT ( 'NONE',  ( 6.016494556629995216, 1.386029456380773572, -1.525348796181945854 ) ) ;
#116093=CARTESIAN_POINT ( 'NONE',  ( 5.133435478496918947, 0.5880181904946504279, 1.928752423557971829 ) ) ;
#116094=ORIENTED_EDGE ( 'NONE', *, *, #212871, .F. ) ;
#116102=CARTESIAN_POINT ( 'NONE',  ( 5.061874962716293780, 1.677747168027879709, -1.117663061872615771 ) ) ;
#116103=CARTESIAN_POINT ( 'NONE',  ( 4.417794048288587128, 1.130693009273657124, -1.452954439256304520 ) ) ;
#116104=CARTESIAN_POINT ( 'NONE',  ( 0.07680821025391955381, 7.629137130509078268, -2.410791881123967251 ) ) ;
#116105=CARTESIAN_POINT ( 'NONE',  ( 2.930630293717914725, 1.281480123180640529, -1.919000982882083095 ) ) ;
#116107=CARTESIAN_POINT ( 'NONE',  ( 4.692742333269261934, -0.4685372120167423660, -2.110058259655919422 ) ) ;
#116108=CARTESIAN_POINT ( 'NONE',  ( 3.485564796978508184, -0.5807542032013839339, 1.931124776463407189 ) ) ;
#116110=CARTESIAN_POINT ( 'NONE',  ( 1.610778572542032050, -0.2360344744354908597, 1.927585326284560585 ) ) ;
#116114=CARTESIAN_POINT ( 'NONE',  ( 4.095287530520356434, 1.233756528997317137, -1.939045446859017030 ) ) ;
#116118=CARTESIAN_POINT ( 'NONE',  ( 2.940157781200231746, 1.856316385841882965, 0.2306766016651334850 ) ) ;
#116120=CARTESIAN_POINT ( 'NONE',  ( 1.125099709691119276, 1.687896996356451629, 0.8989547360247207575 ) ) ;
#116124=CARTESIAN_POINT ( 'NONE',  ( 3.264504910713565078, 0.9923201075644829672, 1.971275125648555449 ) ) ;
#116130=CARTESIAN_POINT ( 'NONE',  ( 0.8781228960479293688, -1.098726114091676198, 1.636593336376483743 ) ) ;
#116131=CARTESIAN_POINT ( 'NONE',  ( 0.6226543773679366067, -1.237902357568532841, -1.947274881911696953 ) ) ;
#116132=CARTESIAN_POINT ( 'NONE',  ( 1.943732651021431224, 1.350599318427040840, 1.423195245143428433 ) ) ;
#116133=CARTESIAN_POINT ( 'NONE',  ( 4.961816841544592904, -0.5550570666568316325, 1.986392505239948036 ) ) ;
#116141=CARTESIAN_POINT ( 'NONE',  ( 0.9542540200799983774, -0.7831509020928304476, 2.025049046554725063 ) ) ;
#116143=CARTESIAN_POINT ( 'NONE',  ( 6.233933901472759942, 1.822226914158030286, 0.2631550708301691466 ) ) ;
#116146=CARTESIAN_POINT ( 'NONE',  ( 1.106479506788549116, 1.420293003395491693, -1.217391549091076275 ) ) ;
#116147=CARTESIAN_POINT ( 'NONE',  ( 5.325516461952285674, -2.054413220456321909, 0.6725034809518318779 ) ) ;
#116149=CARTESIAN_POINT ( 'NONE',  ( -0.02244404828160087226, 6.946777552644228138, -2.784171975256703124 ) ) ;
#116153=CARTESIAN_POINT ( 'NONE',  ( 1.541514448083292965, -1.800223203088219481, 0.6453159242577054533 ) ) ;
#116154=CARTESIAN_POINT ( 'NONE',  ( 2.869705036365962858, 0.9450794480442193946, 1.496173807068044148 ) ) ;
#116156=CARTESIAN_POINT ( 'NONE',  ( 1.014147342612067737, -1.912461472154961539, 0.0006945104691555297090 ) ) ;
#116158=CARTESIAN_POINT ( 'NONE',  ( 5.888286034446420736, -0.6943482264498787027, -1.785519067699488982 ) ) ;
#116160=CARTESIAN_POINT ( 'NONE',  ( 5.986760398725940568, 1.897641426698594813, 0.5270043353632068994 ) ) ;
#116161=CARTESIAN_POINT ( 'NONE',  ( 0.9848172835694012361, -1.340914915981223476, 1.642866500755429948 ) ) ;
#116163=CARTESIAN_POINT ( 'NONE',  ( 4.135518821028766112, -1.289757458839156934, -1.355179912160727085 ) ) ;
#116164=CARTESIAN_POINT ( 'NONE',  ( 0.2580658466875830337, 0.6954254843183353962, 1.688255465954719536 ) ) ;
#116166=CARTESIAN_POINT ( 'NONE',  ( 2.965657822035951963, 0.3232568108629539361, -2.182957019552448141 ) ) ;
#116169=CARTESIAN_POINT ( 'NONE',  ( 1.979039114045421988, 1.923815945824264073, 0.7444423131674202665 ) ) ;
#116174=MECHANICAL_DESIGN_GEOMETRIC_PRESENTATION_REPRESENTATION('',(#50392),#136840);
#116177=CARTESIAN_POINT ( 'NONE',  ( 4.316890830952234914, -1.536253448065309613, 1.388129241271539138 ) ) ;
#116179=CARTESIAN_POINT ( 'NONE',  ( 1.634274655659254005, 1.066924998833935989, -1.879885089102695250 ) ) ;
#116181=CARTESIAN_POINT ( 'NONE',  ( 2.543622981932230243, -1.883669348803659549, 0.7290701893776069253 ) ) ;
#116189=CARTESIAN_POINT ( 'NONE',  ( 6.509000000000050967, 0.007656933339270000430, 1.900274884395843022 ) ) ;
#116190=CARTESIAN_POINT ( 'NONE',  ( 6.639320575229294086, 2.013432609116216021, 2.506292271646192393 ) ) ;
#116191=CARTESIAN_POINT ( 'NONE',  ( 4.827760788416924242, 1.126602223531171898, -1.879657820484957664 ) ) ;
#116193=CARTESIAN_POINT ( 'NONE',  ( 3.252119977711815491, 0.8557668478980616777, -1.710280963351323846 ) ) ;
#116197=CARTESIAN_POINT ( 'NONE',  ( 1.827750133516142128, 0.7691037069590834774, -1.864176919362303675 ) ) ;
#116199=CARTESIAN_POINT ( 'NONE',  ( 0.6973257247198815234, 1.878305535369644064, 1.313909787900492843 ) ) ;
#116201=CARTESIAN_POINT ( 'NONE',  ( 3.908989539853875428, 1.479446464633243474, 0.8863536201247077528 ) ) ;
#116205=CARTESIAN_POINT ( 'NONE',  ( 1.275752070009423367, -1.914805681740685106, 0.4264308320794732432 ) ) ;
#116209=CARTESIAN_POINT ( 'NONE',  ( 0.07516593201273635838, 0.7223771927552320449, -2.128525933252373381 ) ) ;
#116211=CARTESIAN_POINT ( 'NONE',  ( 0.3915760470782835290, -1.894197279051227589, 0.8358220917567968922 ) ) ;
#116213=CARTESIAN_POINT ( 'NONE',  ( 4.758376837038695406, 1.806999933331495445, 0.1280191873242030876 ) ) ;
#116216=CARTESIAN_POINT ( 'NONE',  ( 5.619718922174004483, -0.4339147374951453084, 1.758609293272636487 ) ) ;
#116220=CARTESIAN_POINT ( 'NONE',  ( 6.461375281700972195, 1.547960615844719667, 1.032782510450443114 ) ) ;
#116222=CARTESIAN_POINT ( 'NONE',  ( 4.060093344861609665, -1.099912525845229583, 1.568156085375242093 ) ) ;
#116226=EDGE_CURVE ( 'NONE', #59934, #2638, #49884, .T. ) ;
#116228=CARTESIAN_POINT ( 'NONE',  ( 5.682842148387160286, 1.729519065878544426, -1.221158300678204300 ) ) ;
#116229=CARTESIAN_POINT ( 'NONE',  ( 0.9542513359644848592, 2.159166806557303531, -0.1069676271590186134 ) ) ;
#116232=CARTESIAN_POINT ( 'NONE',  ( 0.5514207423844892375, 0.5776932562693118944, -1.731835939664846613 ) ) ;
#116235=CARTESIAN_POINT ( 'NONE',  ( 3.786012796616508247, -0.9002957760516903107, 1.588078298607284111 ) ) ;
#116238=CARTESIAN_POINT ( 'NONE',  ( 2.717198260794476017, -1.712298780928861008, -0.9731099088599747260 ) ) ;
#116240=CARTESIAN_POINT ( 'NONE',  ( 4.388185931656235717, -0.4287674410733510744, -1.893983405979382306 ) ) ;
#116243=CARTESIAN_POINT ( 'NONE',  ( 4.869442314738527067, -1.792836814666173062, -1.132239877606910472 ) ) ;
#116245=CARTESIAN_POINT ( 'NONE',  ( 2.807167725247063483, 1.639017566557477990, -0.9848878580655600068 ) ) ;
#116253=CARTESIAN_POINT ( 'NONE',  ( 4.846238042176662653, 1.821038859956089606, 0.1311717439725426648 ) ) ;
#116258=CARTESIAN_POINT ( 'NONE',  ( 5.155093292349416600, -1.580716073637401076, -1.000049079914612449 ) ) ;
#116266=CARTESIAN_POINT ( 'NONE',  ( 0.3388458784313007066, -2.007247006727829852, -0.5063607812752639603 ) ) ;
#116267=( BOUNDED_SURFACE ( )  B_SPLINE_SURFACE ( 3, 3, ( 
 ( #2113, #183027, #201386, #200325, #153737, #133253, #187289, #101782, #166790, #199259 ),
 ( #119157, #21558, #167849, #19448, #85524, #5304, #20512, #55169, #137498, #121314 ),
 ( #185141, #4247, #151613, #53024, #3180, #86597, #69251, #36767, #102853, #168909 ),
 ( #152663, #39991, #106100, #191541, #126641, #26912, #76730, #172122, #205663, #155870 ),
 ( #204583, #159062, #122394, #175329, #60483, #9603, #207795, #188351, #75681, #140721 ),
 ( #89823, #192606, #24782, #154802, #141791, #59423, #57300, #10658, #189427, #23716 ),
 ( #104999, #7460, #109320, #171039, #74616, #6389, #73539, #139640, #90885, #8535 ) ),
 .UNSPECIFIED., .T., .F., .T. ) 
 B_SPLINE_SURFACE_WITH_KNOTS ( ( 4, 3, 4 ),
 ( 4, 1, 1, 1, 1, 1, 1, 4 ),
 ( 0.000000000000000000, 0.5000000000000000000, 1.000000000000000000 ),
 ( 0.000000000000000000, 0.09487947018404768729, 0.1878442364269655440, 0.2584026419818104547, 0.3617053504666527530, 0.5211417612611924932, 0.7337075935910832847, 1.000000000000000000 ),
 .UNSPECIFIED. ) 
 GEOMETRIC_REPRESENTATION_ITEM ( )  RATIONAL_B_SPLINE_SURFACE ( (
 ( 1.000000000000000000, 1.000000000000000000, 1.000000000000000000, 0.9999999999999996669, 1.000000000000000222, 1.000000000000000000, 1.000000000000000222, 0.9999999999999997780, 1.000000000000000000, 1.000000000000000000),
 ( 0.3333333333333333703, 0.3333333333333333703, 0.3333333333333334259, 0.3333333333333332593, 0.3333333333333334814, 0.3333333333333333148, 0.3333333333333334259, 0.3333333333333333148, 0.3333333333333333703, 0.3333333333333333703),
 ( 0.3333333333333333703, 0.3333333333333333703, 0.3333333333333334259, 0.3333333333333332593, 0.3333333333333334814, 0.3333333333333333148, 0.3333333333333334259, 0.3333333333333333148, 0.3333333333333333703, 0.3333333333333333703),
 ( 1.000000000000000000, 1.000000000000000000, 1.000000000000000000, 0.9999999999999996669, 1.000000000000000222, 1.000000000000000000, 1.000000000000000222, 0.9999999999999997780, 1.000000000000000000, 1.000000000000000000),
 ( 0.3333333333333333703, 0.3333333333333333703, 0.3333333333333334259, 0.3333333333333332593, 0.3333333333333334814, 0.3333333333333333148, 0.3333333333333334259, 0.3333333333333333148, 0.3333333333333333703, 0.3333333333333333703),
 ( 0.3333333333333333703, 0.3333333333333333703, 0.3333333333333334259, 0.3333333333333332593, 0.3333333333333334814, 0.3333333333333333148, 0.3333333333333334259, 0.3333333333333333148, 0.3333333333333333703, 0.3333333333333333703),
 ( 1.000000000000000000, 1.000000000000000000, 1.000000000000000000, 0.9999999999999996669, 1.000000000000000222, 1.000000000000000000, 1.000000000000000222, 0.9999999999999997780, 1.000000000000000000, 1.000000000000000000) ) ) 
 REPRESENTATION_ITEM ( '' )  SURFACE ( )  );
#116268=CARTESIAN_POINT ( 'NONE',  ( 2.777094422528699535, 1.814377389300044330, -1.091000554854235638 ) ) ;
#116272=CARTESIAN_POINT ( 'NONE',  ( 6.350451050988413115, -2.059726887988411637, -0.2088473404622398499 ) ) ;
#116276=CARTESIAN_POINT ( 'NONE',  ( 2.098001248608129199, -2.291667096838309270, 0.05881920129262825647 ) ) ;
#116277=CARTESIAN_POINT ( 'NONE',  ( 0.09986456629675066754, -1.825204794925545881, -0.04862044751281074939 ) ) ;
#116279=CARTESIAN_POINT ( 'NONE',  ( 2.179812656587180264, 1.874749209517186710, -0.3766967574026017229 ) ) ;
#116282=CARTESIAN_POINT ( 'NONE',  ( 0.1057268774627964369, 1.494660468187744229, 1.348908602934977496 ) ) ;
#116283=CARTESIAN_POINT ( 'NONE',  ( 1.094497266827038962, 1.931770780797737341, 0.3408682529649207926 ) ) ;
#116287=CARTESIAN_POINT ( 'NONE',  ( 3.785173937466048244, 1.514314676582936947, 1.441642292586094110 ) ) ;
#116288=CARTESIAN_POINT ( 'NONE',  ( 2.641160111863867233, -1.309778345111691999, -1.190485388269453049 ) ) ;
#116291=CARTESIAN_POINT ( 'NONE',  ( 5.103627735775233987, -2.281604237428825233, 0.2209099425345140144 ) ) ;
#116292=CARTESIAN_POINT ( 'NONE',  ( 2.782837888936703585, 1.230821076073612463, 1.230640916823136255 ) ) ;
#116295=CARTESIAN_POINT ( 'NONE',  ( 2.881899232214884865, -0.1729783253755692307, 1.725191050717300945 ) ) ;
#116296=CARTESIAN_POINT ( 'NONE',  ( 3.807220332926362083, -1.777014928589750076, 1.247251757893479640 ) ) ;
#116298=CARTESIAN_POINT ( 'NONE',  ( 5.173064673083394460, 1.776168143800487043, -0.9548534231369476544 ) ) ;
#116299=CARTESIAN_POINT ( 'NONE',  ( 0.1562501595635738816, -1.895867669153105339, 0.7852924748299968671 ) ) ;
#116302=CARTESIAN_POINT ( 'NONE',  ( 2.485270279442112429, 1.762041721199611333, -0.7789696210150058864 ) ) ;
#116304=CARTESIAN_POINT ( 'NONE',  ( 5.607756438734910809, 1.682095628590657643, 1.451081198120441229 ) ) ;
#116306=CARTESIAN_POINT ( 'NONE',  ( 6.983263157960398537, 3.691045885609476773, 2.560325512483021981 ) ) ;
#116310=CARTESIAN_POINT ( 'NONE',  ( 6.654749070045313353, -0.5220710138904552933, -1.891073168474053823 ) ) ;
#116316=CARTESIAN_POINT ( 'NONE',  ( 4.264169596968480747, -2.057349986699669397, 0.1488187104187361498 ) ) ;
#116320=CARTESIAN_POINT ( 'NONE',  ( 6.098880659294531270, 1.529360415809786433, -1.076766019972655197 ) ) ;
#116321=CARTESIAN_POINT ( 'NONE',  ( 4.377415392590312315, -0.3859441149459389431, -1.690453949067998840 ) ) ;
#116322=CARTESIAN_POINT ( 'NONE',  ( 3.948569229637605815, -1.449640539659799776, -0.9628182713226125511 ) ) ;
#116324=CARTESIAN_POINT ( 'NONE',  ( 1.541004877621090507, -1.933652123512133114, 1.230999918854805975 ) ) ;
#116326=CARTESIAN_POINT ( 'NONE',  ( 5.618719695961268634, -0.05021595884377753893, 2.090305304898040006 ) ) ;
#116327=CARTESIAN_POINT ( 'NONE',  ( 0.6031360380127914755, -1.832534659106283659, 0.1778487281504093076 ) ) ;
#116331=CARTESIAN_POINT ( 'NONE',  ( 1.494767762416524093, -2.000856930885573259, 0.2496086726550551249 ) ) ;
#116332=CARTESIAN_POINT ( 'NONE',  ( 0.5334774086375413393, -1.552487152004313087, -1.546944964277228607 ) ) ;
#116337=CARTESIAN_POINT ( 'NONE',  ( 3.000754678503589012, -2.089479603458433754, -0.3603616953608209661 ) ) ;
#116339=CARTESIAN_POINT ( 'NONE',  ( 5.619710272201024814, -1.780234218580947436, 0.4041525643716862848 ) ) ;
#116345=CARTESIAN_POINT ( 'NONE',  ( 3.814717077619066643, -0.6377016420256261808, -1.916516432535425363 ) ) ;
#116346=CARTESIAN_POINT ( 'NONE',  ( 6.440462174652990868, 2.181831651002089423, 0.3301269925025315799 ) ) ;
#116349=CARTESIAN_POINT ( 'NONE',  ( 4.363987150452108388, -1.856190122274929077, 0.1334137851533196695 ) ) ;
#116355=CARTESIAN_POINT ( 'NONE',  ( 6.245006310359877411, -1.742422335079217843, 1.100243706638550423 ) ) ;
#116359=CARTESIAN_POINT ( 'NONE',  ( 1.194254265631944367, -1.094737682603286189, -1.344534739289292569 ) ) ;
#116360=CARTESIAN_POINT ( 'NONE',  ( 1.657743431332364681, -1.232332549506355290, 1.229129442381997395 ) ) ;
#116361=CARTESIAN_POINT ( 'NONE',  ( 6.287736656369789401, 1.586309881779718323, 1.676255113901073512 ) ) ;
#116364=CARTESIAN_POINT ( 'NONE',  ( 1.511086176359067501, 1.816151333767004772, 0.9739060079534812564 ) ) ;
#116368=CARTESIAN_POINT ( 'NONE',  ( 6.397888825007291835, 0.2158721846312293136, 2.288236095241158452 ) ) ;
#116371=CARTESIAN_POINT ( 'NONE',  ( 6.368025811218641863, 0.9635043244729593059, 1.603280169136585220 ) ) ;
#116372=CARTESIAN_POINT ( 'NONE',  ( 4.166199421025416960, 1.911861072351704882, -0.05224187775455800542 ) ) ;
#116374=CARTESIAN_POINT ( 'NONE',  ( 6.621690180768193379, -2.141820631849135292, 0.5315211216728524812 ) ) ;
#116378=CARTESIAN_POINT ( 'NONE',  ( 6.498696114369957755, -2.079444522786470184, -0.4142970760486197612 ) ) ;
#116380=CARTESIAN_POINT ( 'NONE',  ( 3.013035845080668906, 1.672340031372629321, -1.590277441748239040 ) ) ;
#116381=CARTESIAN_POINT ( 'NONE',  ( 4.984793487045196869, 1.876812866478014596, 0.5713181500588762063 ) ) ;
#116382=CARTESIAN_POINT ( 'NONE',  ( 1.358172466202983042, -1.961936380284023063, -0.005482119489134959674 ) ) ;
#116386=CARTESIAN_POINT ( 'NONE',  ( 0.2162074652159052257, 1.082675745310441862, -1.819457589102360551 ) ) ;
#116388=CARTESIAN_POINT ( 'NONE',  ( 0.3746297210940018885, 1.718982886236510854, -0.6599183738737608440 ) ) ;
#116389=CARTESIAN_POINT ( 'NONE',  ( 4.083024739667787451, 2.059781850948108506, 0.6862965400120830672 ) ) ;
#116392=CARTESIAN_POINT ( 'NONE',  ( 2.197662576721173266, 1.936918166296027977, -0.8637449004969055544 ) ) ;
#116398=CARTESIAN_POINT ( 'NONE',  ( 2.196623993872096392, -0.5467073567838857118, -1.986887711889900432 ) ) ;
#116402=CARTESIAN_POINT ( 'NONE',  ( 0.07735805125225460321, 4.085280796943619563, -2.643583850410589964 ) ) ;
#116405=CARTESIAN_POINT ( 'NONE',  ( 4.318947422894989785, 1.476084237994702786, -1.215703867470045774 ) ) ;
#116407=CARTESIAN_POINT ( 'NONE',  ( 1.370828697373091432, -1.435183881573602216, 1.748884408748638597 ) ) ;
#116409=CARTESIAN_POINT ( 'NONE',  ( 0.9667389835759466754, -1.427192611269219924, 1.115597691851821116 ) ) ;
#116410=CARTESIAN_POINT ( 'NONE',  ( 1.481495926510235206, -0.6419399793253840469, 1.805124470068826037 ) ) ;
#116411=CARTESIAN_POINT ( 'NONE',  ( 3.262232429473245432, -2.068111870375147987, 0.09887451149894616043 ) ) ;
#116413=CARTESIAN_POINT ( 'NONE',  ( 0.7781230576423033840, -1.097119503657293382, 1.637799472441689996 ) ) ;
#116414=CARTESIAN_POINT ( 'NONE',  ( 5.514262516685338511, -0.8683059565382322820, -1.719797162412556535 ) ) ;
#116415=CARTESIAN_POINT ( 'NONE',  ( 0.6105616303546910206, -2.295997848557976617, 0.2320981213338509652 ) ) ;
#116418=CARTESIAN_POINT ( 'NONE',  ( 4.967260703730732807, 1.792967015482237469, 1.019669102033170516 ) ) ;
#116422=CARTESIAN_POINT ( 'NONE',  ( 5.684633084330723563, -2.053880889230023321, -0.4646916863456708735 ) ) ;
#116425=CARTESIAN_POINT ( 'NONE',  ( 4.341216920475977403, -1.883070171734081200, 1.061215411333437109 ) ) ;
#116426=CARTESIAN_POINT ( 'NONE',  ( 5.514321518048907578, -2.019862493962302441, 0.002152582845403941403 ) ) ;
#116433=CARTESIAN_POINT ( 'NONE',  ( 3.151577601795185757, 1.966304690962265234, -0.4465026806126579095 ) ) ;
#116437=CARTESIAN_POINT ( 'NONE',  ( 5.383715653711652394, 1.448795075966866852, 1.604530791579752202 ) ) ;
#116442=CARTESIAN_POINT ( 'NONE',  ( 5.290638740200859225, 1.525033539048275877, -1.319242139327673424 ) ) ;
#116444=CARTESIAN_POINT ( 'NONE',  ( 0.7852881911578631913, 1.155166132482473351, 1.281103752909551030 ) ) ;
#116449=CARTESIAN_POINT ( 'NONE',  ( 6.239502018287079288, -1.354773164471131164, -1.289998633004642237 ) ) ;
#116450=CARTESIAN_POINT ( 'NONE',  ( 0.5396978354115729015, -1.910900059352708125, 0.6334021227705748380 ) ) ;
#116457=CARTESIAN_POINT ( 'NONE',  ( 1.875790325896836919, 0.3594715711359474652, -2.089634487563592824 ) ) ;
#116458=CARTESIAN_POINT ( 'NONE',  ( 2.056267757160272325, -1.238304521155994209, 1.591332585091954854 ) ) ;
#116459=CARTESIAN_POINT ( 'NONE',  ( 2.003910543607852812, -0.7718314612508870853, 1.639047433122240660 ) ) ;
#116461=CARTESIAN_POINT ( 'NONE',  ( 6.455963997168007396, 2.156291961557708525, -0.1537611777119098633 ) ) ;
#116466=CARTESIAN_POINT ( 'NONE',  ( 0.2685667436414033160, -0.2372314691254543417, -1.900927335933370488 ) ) ;
#116475=CARTESIAN_POINT ( 'NONE',  ( 4.452137864729129646, 2.161286467946467837, -0.05003489268536746859 ) ) ;
#116478=CARTESIAN_POINT ( 'NONE',  ( 1.529697670087664108, -0.2543295609688834835, 2.105205558366497698 ) ) ;
#116479=CARTESIAN_POINT ( 'NONE',  ( 6.774438514930277933, -1.120217847261167243, 1.442041797927499980 ) ) ;
#116480=CARTESIAN_POINT ( 'NONE',  ( 2.969950176076568749, 1.051608646734447650, 1.667261953242512140 ) ) ;
#116481=CARTESIAN_POINT ( 'NONE',  ( 5.502191098127390489, -0.8541586074963626318, 1.711093258865265643 ) ) ;
#116485=CARTESIAN_POINT ( 'NONE',  ( 5.617622257330707747, 0.3859593044726419286, -1.931177630036359005 ) ) ;
#116486=CARTESIAN_POINT ( 'NONE',  ( 1.622886899410342254, -1.828648197406743670, 0.6539591521299585875 ) ) ;
#116494=CARTESIAN_POINT ( 'NONE',  ( 5.813130153884224605, 1.560705751063670377, -1.104717755519408984 ) ) ;
#116496=CARTESIAN_POINT ( 'NONE',  ( 4.512475528931441104, -0.9420208833846724916, -1.995868093903986118 ) ) ;
#116497=CARTESIAN_POINT ( 'NONE',  ( 1.712255133470397261, -2.190042126362458319, 0.2705847154940849153 ) ) ;
#116499=CARTESIAN_POINT ( 'NONE',  ( 0.5922591856823838929, -1.062013159134197693, 1.590055880637729402 ) ) ;
#116501=CARTESIAN_POINT ( 'NONE',  ( 3.631357695093720306, 0.05367941694835526301, -2.069842578854002468 ) ) ;
#116504=CARTESIAN_POINT ( 'NONE',  ( 1.463986924769441478, 2.129665692569195024, -0.3698555562515608020 ) ) ;
#116505=CARTESIAN_POINT ( 'NONE',  ( 3.931328349035985603, -1.512150646884598215, -1.586510368271301541 ) ) ;
#116511=CARTESIAN_POINT ( 'NONE',  ( 6.082590270738484683, -0.5753628732939282120, 1.636087478734444600 ) ) ;
#116514=CARTESIAN_POINT ( 'NONE',  ( 3.186448005867897670, 1.153939711166888982, -1.718631068965512210 ) ) ;
#116515=CARTESIAN_POINT ( 'NONE',  ( 5.167619242541076297, 1.422618751053092101, 1.568198848534626100 ) ) ;
#116518=CARTESIAN_POINT ( 'NONE',  ( 3.151173496672290852, 1.691593242058259783, -1.008282029756089493 ) ) ;
#116519=CARTESIAN_POINT ( 'NONE',  ( 5.666080500323320557, -1.458056995643598475, 1.768786637700834108 ) ) ;
#116520=CARTESIAN_POINT ( 'NONE',  ( 3.457459740917231628, 0.4424662778084071935, -1.771134634090239190 ) ) ;
#116527=CARTESIAN_POINT ( 'NONE',  ( 4.359639327901571271, -1.559048523801108477, -1.273764430229076483 ) ) ;
#116528=CARTESIAN_POINT ( 'NONE',  ( 3.889464431383614862, -1.814284039448841979, 0.7467176931179178023 ) ) ;
#116532=CARTESIAN_POINT ( 'NONE',  ( 0.1755611466353447780, 0.6788741266964171128, -2.325051092042058620 ) ) ;
#116533=CARTESIAN_POINT ( 'NONE',  ( 0.4508687890585044711, -1.768401812538191287, -1.115020903081758608 ) ) ;
#116534=CARTESIAN_POINT ( 'NONE',  ( 5.928513199909208886, 1.706640645603505257, 0.4684080695957025253 ) ) ;
#116536=CARTESIAN_POINT ( 'NONE',  ( 2.185716925580234449, -0.9354795820612994417, 1.981881815340847730 ) ) ;
#116537=CARTESIAN_POINT ( 'NONE',  ( 0.9424304438642245874, -1.370989592614113795, -1.072060877835380621 ) ) ;
#116539=CARTESIAN_POINT ( 'NONE',  ( 0.2331713839410576583, 0.005725554726919174046, -1.953566683266183102 ) ) ;
#116540=CARTESIAN_POINT ( 'NONE',  ( 0.6622201036875573488, -1.252624510564132931, 1.186060005986578014 ) ) ;
#116541=CARTESIAN_POINT ( 'NONE',  ( 0.9490539546192258147, 1.544862702020805223, 1.701928257493188434 ) ) ;
#116542=CARTESIAN_POINT ( 'NONE',  ( 0.7498831369015904746, 2.188782640433343474, -0.1130235578899463078 ) ) ;
#116543=CARTESIAN_POINT ( 'NONE',  ( 3.211752199052122503, -0.4303563718574507369, 2.164345902561148005 ) ) ;
#116544=CARTESIAN_POINT ( 'NONE',  ( 1.340952317110634118, -2.117647682651255803, -0.4779334406839957916 ) ) ;
#116545=CARTESIAN_POINT ( 'NONE',  ( 0.01192831195480706721, -0.7772932952810689411, -1.650495136788888040 ) ) ;
#116546=CARTESIAN_POINT ( 'NONE',  ( 2.606785607150950757, 1.995414689559615207, 0.7085744572869844271 ) ) ;
#116547=CARTESIAN_POINT ( 'NONE',  ( 6.727182134110202938, 2.016807574165893513, 2.492494991173601182 ) ) ;
#116548=CARTESIAN_POINT ( 'NONE',  ( 5.561526637868618117, 0.3756393653304244129, -1.889249976882242610 ) ) ;
#116550=CARTESIAN_POINT ( 'NONE',  ( 2.103457651957148844, -0.4980181218575702173, 2.237485198869753944 ) ) ;
#116554=CARTESIAN_POINT ( 'NONE',  ( 5.373765183877965868, 0.4349513647441177744, -2.178143251680577208 ) ) ;
#116562=CARTESIAN_POINT ( 'NONE',  ( 2.760388869050140137, 1.913803604375517109, -0.6351994527180188088 ) ) ;
#116564=CARTESIAN_POINT ( 'NONE',  ( 0.9364711893796459075, -1.149011738537804250, 1.712694122252313100 ) ) ;
#116568=CARTESIAN_POINT ( 'NONE',  ( 3.820431320580887302, 2.080737768064028437, 0.6879518193209921417 ) ) ;
#116569=CARTESIAN_POINT ( 'NONE',  ( 0.8795299900376440938, -0.4926441280813895762, -1.955172062459666904 ) ) ;
#116570=CARTESIAN_POINT ( 'NONE',  ( 1.557894219809667247, -1.301531972126177772, 1.302644501960325885 ) ) ;
#116571=CARTESIAN_POINT ( 'NONE',  ( 5.478174288590652807, -2.235914823156583964, -0.5050262530511948622 ) ) ;
#116572=CARTESIAN_POINT ( 'NONE',  ( 4.312339554033173705, 1.684294245562456993, 0.7440144950455057637 ) ) ;
#116575=CARTESIAN_POINT ( 'NONE',  ( 4.225493254642153751, -1.746956894163293361, 0.5300125199643389573 ) ) ;
#116576=CARTESIAN_POINT ( 'NONE',  ( 4.500625067706437221, -1.976956227568788638, 0.3961002554062897918 ) ) ;
#116578=CARTESIAN_POINT ( 'NONE',  ( 4.557670991828286056, 0.4998169670675355336, -2.206472437794388952 ) ) ;
#116580=CARTESIAN_POINT ( 'NONE',  ( 6.704139028598911310, -2.105588161048920437, 0.04759252156865538541 ) ) ;
#116582=CARTESIAN_POINT ( 'NONE',  ( 5.002425025097493538, 2.064580399062130311, 0.1557331365308264881 ) ) ;
#116587=CARTESIAN_POINT ( 'NONE',  ( 2.438006290551326671, 0.9082397578730906362, -1.698968261161729831 ) ) ;
#116590=CARTESIAN_POINT ( 'NONE',  ( 6.789911431267126041, -1.283970416288570116, -1.493486111907322389 ) ) ;
#116594=CARTESIAN_POINT ( 'NONE',  ( 1.283610819548046011, 0.1505422781087061845, -2.115291873224629082 ) ) ;
#116595=CARTESIAN_POINT ( 'NONE',  ( 1.178328164221422503, 2.187401300010451077, -0.3865082640040794493 ) ) ;
#116596=CARTESIAN_POINT ( 'NONE',  ( 2.819468948711697287, -0.2076110458819386551, 2.095707187103168945 ) ) ;
#116599=CARTESIAN_POINT ( 'NONE',  ( 2.734756269166933151, -1.876540383875524576, -0.5722209215143353456 ) ) ;
#116606=CARTESIAN_POINT ( 'NONE',  ( 2.004293344102888508, -0.9022931611136343344, 1.919180038594799687 ) ) ;
#116609=CARTESIAN_POINT ( 'NONE',  ( 4.598074495912658044, 0.8407358649686399454, -1.772743347989129692 ) ) ;
#116610=CARTESIAN_POINT ( 'NONE',  ( 3.186554565756247737, -2.129457467500107004, -0.3711038070777841202 ) ) ;
#116611=CARTESIAN_POINT ( 'NONE',  ( 2.630204301513817455, 0.2276190002089127917, 1.827071974840013491 ) ) ;
#116614=CARTESIAN_POINT ( 'NONE',  ( 4.224340698251967119, 0.08847545473529906668, 1.738206131172301161 ) ) ;
#116620=CARTESIAN_POINT ( 'NONE',  ( 2.272554088390315030, -1.330374092946192688, 1.703740541667747133 ) ) ;
#116621=CARTESIAN_POINT ( 'NONE',  ( 4.587267430073429963, 1.242536178122002344, -1.587594670648798445 ) ) ;
#116623=CARTESIAN_POINT ( 'NONE',  ( 1.393688021309073433, 1.637156065531343740, 1.411701162175371893 ) ) ;
#116624=CARTESIAN_POINT ( 'NONE',  ( 2.887526864075397715, 1.393042391738574137, 1.395278474455765805 ) ) ;
#116625=CARTESIAN_POINT ( 'NONE',  ( 6.509000000000053632, 2.033894086284238956, 2.405029747421689290 ) ) ;
#116626=CARTESIAN_POINT ( 'NONE',  ( 3.386211154777326815, -0.3816624740031882568, -1.904027918096486527 ) ) ;
#116634=CARTESIAN_POINT ( 'NONE',  ( 0.6576010401811819284, -1.865379905010958517, -1.178792301215730642 ) ) ;
#116637=CARTESIAN_POINT ( 'NONE',  ( 4.944172655442597986, -0.9282843415348587257, 1.728263438747809078 ) ) ;
#116638=CARTESIAN_POINT ( 'NONE',  ( 1.863907939170056149, -0.1017519224979606118, -2.013985838549677609 ) ) ;
#116640=CARTESIAN_POINT ( 'NONE',  ( 3.591103737854687061, 1.818103999434977025, 1.084929287856269742 ) ) ;
#116644=CARTESIAN_POINT ( 'NONE',  ( 4.224425198852012286, 0.09258891237720962009, 1.838934309869838968 ) ) ;
#116648=CARTESIAN_POINT ( 'NONE',  ( 4.816704082729271086, -0.7169179515637627009, -1.995842421597990413 ) ) ;
#116650=CARTESIAN_POINT ( 'NONE',  ( 5.009085904467641015, 1.791045569760267631, 1.019200576588958240 ) ) ;
#116652=CARTESIAN_POINT ( 'NONE',  ( 0.5372768211588532239, 1.738583335619352077, -0.6644854061606010331 ) ) ;
#116653=CARTESIAN_POINT ( 'NONE',  ( 2.823586671956069605, 1.020774559177588081, -1.532180179759069283 ) ) ;
#116658=CARTESIAN_POINT ( 'NONE',  ( 2.666872310945223923, -1.521158656661812714, 1.599105504226288499 ) ) ;
#116659=CARTESIAN_POINT ( 'NONE',  ( 4.587383588223284292, 2.023586100481920447, -1.011833202457941283 ) ) ;
#116661=CARTESIAN_POINT ( 'NONE',  ( 4.324329094900294379, -0.7804802743817635946, -1.635003121989448971 ) ) ;
#116662=CARTESIAN_POINT ( 'NONE',  ( 5.858580540861003882, -1.821332666672281553, -0.5942308157336049224 ) ) ;
#116664=CARTESIAN_POINT ( 'NONE',  ( 4.610133579271312954, -0.8000244862099057386, -1.691074300901610261 ) ) ;
#116665=CARTESIAN_POINT ( 'NONE',  ( 4.598021663640887269, 0.7965279161250311546, -1.682138884369558607 ) ) ;
#116667=CARTESIAN_POINT ( 'NONE',  ( 5.928513199909208886, 1.706640645603505257, 0.4684080695957025253 ) ) ;
#116668=CARTESIAN_POINT ( 'NONE',  ( 0.6906390985809904848, 1.523792322931913468, -1.320830384837400118 ) ) ;
#116670=CARTESIAN_POINT ( 'NONE',  ( 1.401149585966605882, 1.720815086091964652, -1.213930111015694369 ) ) ;
#116675=CARTESIAN_POINT ( 'NONE',  ( 2.144791408438687430, 1.960151896008819117, 0.4867283015469162644 ) ) ;
#116677=CARTESIAN_POINT ( 'NONE',  ( 6.620655732516649294, 2.985444497229528427, 2.280274006979409407 ) ) ;
#116680=CARTESIAN_POINT ( 'NONE',  ( 2.196749789412206333, -0.5742421066207163971, -2.083876772215712325 ) ) ;
#116681=CARTESIAN_POINT ( 'NONE',  ( 6.610000000000006537, 0.002781820520842553934, 2.000159646111852929 ) ) ;
#116686=CARTESIAN_POINT ( 'NONE',  ( 6.473846665049121540, -0.8576149079453172508, 1.823233050095712349 ) ) ;
#116689=CARTESIAN_POINT ( 'NONE',  ( 0.6971427418834205136, 1.794861059153027627, 1.257291590721874686 ) ) ;
#116691=CARTESIAN_POINT ( 'NONE',  ( 1.956323303678444425, 2.256377666735286169, -0.1672192238599319314 ) ) ;
#116698=CARTESIAN_POINT ( 'NONE',  ( 2.670886861492921316, 0.09125233944726543478, -1.767527270347787116 ) ) ;
#116700=CARTESIAN_POINT ( 'NONE',  ( 6.651417122894856426, -1.768357563224710605, -1.319949637914811458 ) ) ;
#116704=CARTESIAN_POINT ( 'NONE',  ( 5.167592292328679449, 1.356312711205298172, 1.492245250866150785 ) ) ;
#116705=CARTESIAN_POINT ( 'NONE',  ( 4.816585706611137496, -0.6173935602037239345, -1.703258737839604242 ) ) ;
#116707=CARTESIAN_POINT ( 'NONE',  ( 2.641296366799699147, -1.384790685969448099, -1.257831364775918503 ) ) ;
#116708=CARTESIAN_POINT ( 'NONE',  ( 2.219664259111033378, 0.3580842396277704176, -2.038906786875307020 ) ) ;
#116710=CARTESIAN_POINT ( 'NONE',  ( 2.302860652515530848, -0.3306829512400177862, -1.883434002855538081 ) ) ;
#116718=CARTESIAN_POINT ( 'NONE',  ( 1.609737659951641309, 0.5726723138891121057, -1.876404140693301414 ) ) ;
#116719=CARTESIAN_POINT ( 'NONE',  ( 0.1575669172422279607, -0.4392406603518673736, -1.974865693180789750 ) ) ;
#116721=CARTESIAN_POINT ( 'NONE',  ( 5.748313822965784858, 1.043546352714582071, -1.845953426139717246 ) ) ;
#116724=CARTESIAN_POINT ( 'NONE',  ( 6.731714608790520415, -1.285842040959904287, -1.494388255172361513 ) ) ;
#116726=CARTESIAN_POINT ( 'NONE',  ( 1.687745526430058263, 1.925312447093192825, -0.5882657090081342410 ) ) ;
#116728=CARTESIAN_POINT ( 'NONE',  ( 1.019337291899083064, -1.912195925978699140, 0.9092529662874779817 ) ) ;
#116731=CARTESIAN_POINT ( 'NONE',  ( 2.488806849732328796, 2.007603858877416769, 0.5053560088097220904 ) ) ;
#116735=CARTESIAN_POINT ( 'NONE',  ( 5.824191892830967276, 2.014527380540787505, 0.5587128073646082660 ) ) ;
#116737=CARTESIAN_POINT ( 'NONE',  ( 4.453998568579462969, 1.825179399820752169, -0.04523609120457571658 ) ) ;
#116738=CARTESIAN_POINT ( 'NONE',  ( 2.982852160962686128, -1.674641624487639424, -0.6911452858660637188 ) ) ;
#116743=CARTESIAN_POINT ( 'NONE',  ( 5.737410212107617369, -1.997324651315038002, 0.9386623957203034108 ) ) ;
#116746=CARTESIAN_POINT ( 'NONE',  ( 4.072844535355981677, -1.414876986328793329, 1.286614418101794444 ) ) ;
#116754=CARTESIAN_POINT ( 'NONE',  ( -0.006632162239710717895, -1.840811702136424088, -0.04651623371411393176 ) ) ;
#116757=CARTESIAN_POINT ( 'NONE',  ( 3.901501827272614964, -0.5455803081039903857, 1.789184164884791706 ) ) ;
#116761=ADVANCED_FACE ( 'NONE', ( #115792 ), #104871, .T. ) ;
#116764=CARTESIAN_POINT ( 'NONE',  ( 6.649288540346695697, 1.804226486660088558, -1.015068834323729297 ) ) ;
#116765=CARTESIAN_POINT ( 'NONE',  ( 2.249625261780491936, 1.976952429928409805, -0.3961248688731587309 ) ) ;
#116770=CARTESIAN_POINT ( 'NONE',  ( 2.449409141518565480, 0.5832169002529237201, -2.112351429719904861 ) ) ;
#116771=CARTESIAN_POINT ( 'NONE',  ( 6.041596546049881944, -1.325759876995153075, -1.255439798616593716 ) ) ;
#116779=CARTESIAN_POINT ( 'NONE',  ( 4.229911503591711863, 1.806553461410321582, 0.3548724298726435022 ) ) ;
#116780=CARTESIAN_POINT ( 'NONE',  ( 0.4166524477783914437, -0.6801522605285510448, -1.894826352922045487 ) ) ;
#116781=CARTESIAN_POINT ( 'NONE',  ( 2.882471369727876542, -0.2278316040762885242, 2.287086785078895179 ) ) ;
#116783=CARTESIAN_POINT ( 'NONE',  ( 1.463465096324652714, -0.4588509492367858766, 1.803342318195770178 ) ) ;
#116787=CARTESIAN_POINT ( 'NONE',  ( 4.957238921819991262, -1.637161358497842389, 0.9882132959125531357 ) ) ;
#116791=CARTESIAN_POINT ( 'NONE',  ( 3.825792374969799514, 1.116656699807290432, -1.767364921024146218 ) ) ;
#116792=CARTESIAN_POINT ( 'NONE',  ( 2.078771448894382701, -0.08914341469279044028, -1.868647664167771616 ) ) ;
#116795=CARTESIAN_POINT ( 'NONE',  ( 6.075717905342373548, -0.9791751913862613010, 1.559117742379905858 ) ) ;
#116798=CARTESIAN_POINT ( 'NONE',  ( 4.107791765966132047, -1.720061694268668395, 0.1296855704675456133 ) ) ;
#116800=CARTESIAN_POINT ( 'NONE',  ( 0.6681306116654138760, 1.163384174638517177, 1.286150249643343901 ) ) ;
#116803=CARTESIAN_POINT ( 'NONE',  ( 4.575155497752975364, 1.982410897724752319, 0.8856408146403412784 ) ) ;
#116804=CARTESIAN_POINT ( 'NONE',  ( 3.844227010333609584, 1.817057058749595777, 0.1772887374331885701 ) ) ;
#116805=CARTESIAN_POINT ( 'NONE',  ( 1.446067858876250112, -0.8869304882095051523, 1.749921244195346004 ) ) ;
#116806=CARTESIAN_POINT ( 'NONE',  ( 5.208266738515407113, 1.258803676730145371, -1.702402541353124077 ) ) ;
#116808=CARTESIAN_POINT ( 'NONE',  ( 5.812145867431055102, 1.542159960141289199, -1.696276722712148688 ) ) ;
#116811=CARTESIAN_POINT ( 'NONE',  ( 1.471502243059899850, -1.820439715282649251, -1.087164402369590555 ) ) ;
#116815=CARTESIAN_POINT ( 'NONE',  ( 6.086835205273840366, 2.090220906010348045, 0.5866831100012849243 ) ) ;
#116816=CARTESIAN_POINT ( 'NONE',  ( 6.983263157960365675, 2.037486384657179350, 2.358487060789053569 ) ) ;
#116818=CARTESIAN_POINT ( 'NONE',  ( 0.8564553275840697255, 0.8952667643853294832, -2.033071718549640305 ) ) ;
#116820=CARTESIAN_POINT ( 'NONE',  ( 6.047500043413473136, -1.423963828944514010, 1.427935028000301809 ) ) ;
#116822=CARTESIAN_POINT ( 'NONE',  ( 4.434473652564925317, -1.191674006009019404, 1.683292407194038054 ) ) ;
#116828=CARTESIAN_POINT ( 'NONE',  ( 0.05869050280414740001, -1.868530317513932504, -0.9378765995749788198 ) ) ;
#116829=CARTESIAN_POINT ( 'NONE',  ( 4.201796189063250253, 1.844709454618495670, 0.8146275914719460776 ) ) ;
#116830=CARTESIAN_POINT ( 'NONE',  ( 3.966218424140379728, -1.719484690100345325, -0.6589542199007536460 ) ) ;
#116834=CARTESIAN_POINT ( 'NONE',  ( 2.027930484333416050, 0.9963118489298377067, -1.407687550210996230 ) ) ;
#116835=CARTESIAN_POINT ( 'NONE',  ( 0.1984543448181053105, 1.387095780679182377, -1.463931301963219855 ) ) ;
#116836=CARTESIAN_POINT ( 'NONE',  ( 1.723655420059172050, 2.274453554295458702, 0.3322429970207661509 ) ) ;
#116838=CARTESIAN_POINT ( 'NONE',  ( 1.476233607035297490, 1.347422320225545089, 1.817282701917295240 ) ) ;
#116839=CARTESIAN_POINT ( 'NONE',  ( 3.703829026103040434, -0.6115302605771840705, 2.015330080423376913 ) ) ;
#116843=CARTESIAN_POINT ( 'NONE',  ( 6.156250000000002665, -1.895863743163982207, 0.7852924748303072855 ) ) ;
#116847=CARTESIAN_POINT ( 'NONE',  ( 4.887093103977882436, -2.092044318328468488, -0.7474293538695072625 ) ) ;
#116848=CARTESIAN_POINT ( 'NONE',  ( 3.310656966840678894, 1.981231107410564851, 0.9368519390955745152 ) ) ;
#116852=CARTESIAN_POINT ( 'NONE',  ( 6.610000000000010090, 4.687934210475516394, 2.842562027763709587 ) ) ;
#116855=CARTESIAN_POINT ( 'NONE',  ( 5.203433420164765622, 1.869144303625443371, -1.001675624404389620 ) ) ;
#116859=CARTESIAN_POINT ( 'NONE',  ( 6.403215362905616992, 1.794359850238020693, 1.205212418099836480 ) ) ;
#116861=CARTESIAN_POINT ( 'NONE',  ( 5.812015183962491172, 1.231757822100377320, -1.368757117762291253 ) ) ;
#116864=CARTESIAN_POINT ( 'NONE',  ( 0.6787880507331369717, 1.167388449615349044, 1.291009837513588998 ) ) ;
#116870=CARTESIAN_POINT ( 'NONE',  ( 5.331013795412237855, 0.1550192300789655642, 2.156197635354038411 ) ) ;
#116875=CARTESIAN_POINT ( 'NONE',  ( 4.838837662799537753, 0.3661284547709364734, 2.130314178654398205 ) ) ;
#116878=CARTESIAN_POINT ( 'NONE',  ( 6.046159394557358624, 1.968988722785993462, 0.09938198387684710200 ) ) ;
#116879=CARTESIAN_POINT ( 'NONE',  ( 5.589090328658773643, 1.030979737101325400, -1.393799353210682046 ) ) ;
#116881=CARTESIAN_POINT ( 'NONE',  ( 2.050558489324630251, -1.691691439650149897, 1.393213601605561180 ) ) ;
#116882=CARTESIAN_POINT ( 'NONE',  ( 2.714277975868684578, -2.282582259777651501, 0.3379699517906120110 ) ) ;
#116883=CARTESIAN_POINT ( 'NONE',  ( 5.290332094886032621, -2.044729594613464041, -0.2563108835951214970 ) ) ;
#116884=CARTESIAN_POINT ( 'NONE',  ( 0.4978614556471228081, -0.6533520819593687801, -1.828864621591755002 ) ) ;
#116888=CARTESIAN_POINT ( 'NONE',  ( 3.410498715577559015, -2.118327196165440185, -0.1003008382433126094 ) ) ;
#116890=CARTESIAN_POINT ( 'NONE',  ( 1.301407962653992501, 1.352153127569672098, -1.496052916918483522 ) ) ;
#116892=CARTESIAN_POINT ( 'NONE',  ( 4.366400497975233996, 1.037236317483503312, 1.947806255051434121 ) ) ;
#116894=CARTESIAN_POINT ( 'NONE',  ( 2.254548712976621516, -0.4907705908011159579, -1.795021142807408543 ) ) ;
#116899=DIRECTION ( 'NONE',  ( -0.9999980456341537316, 0.000000000000000000, -0.001977050295958555567 ) ) ;
#116902=CARTESIAN_POINT ( 'NONE',  ( 3.801680928091007772, -0.6000553829732765410, 1.971583879547859963 ) ) ;
#116905=CARTESIAN_POINT ( 'NONE',  ( 3.844402842710480162, 1.078523329768014349, -1.707388236230653611 ) ) ;
#116908=CARTESIAN_POINT ( 'NONE',  ( 1.885689728351304995, 1.420446345011391553, 1.493427266136108322 ) ) ;
#116912=CARTESIAN_POINT ( 'NONE',  ( -0.1408020194050510487, 6.947782644136224484, -2.695327183700791274 ) ) ;
#116914=CARTESIAN_POINT ( 'NONE',  ( 1.112948326906910035, -1.796673262952220629, 0.4014371099074555693 ) ) ;
#116915=CARTESIAN_POINT ( 'NONE',  ( 5.321004863918796346, 2.037934703285459115, 0.8473243778325880715 ) ) ;
#116917=CARTESIAN_POINT ( 'NONE',  ( 1.915512222264357467, -0.2666219456287990952, 2.145042957367573777 ) ) ;
#116919=CARTESIAN_POINT ( 'NONE',  ( 2.342982756445275427, -1.756855002775299379, -0.9896843009072553432 ) ) ;
#116922=CARTESIAN_POINT ( 'NONE',  ( 0.4439547499465161251, 1.865322535695708606, 0.1421067652795371117 ) ) ;
#116923=DIRECTION ( 'NONE',  ( -1.000000000000000000, 1.016547956922408957E-15, 1.479114432388267300E-31 ) ) ;
#116924=CARTESIAN_POINT ( 'NONE',  ( 4.030118584743531684, 1.055711351780568741, -1.664808796107832389 ) ) ;
#116925=CARTESIAN_POINT ( 'NONE',  ( 2.975796278104340331, -0.8128168404246680634, 1.845627246706407210 ) ) ;
#116930=CARTESIAN_POINT ( 'NONE',  ( 6.235009869002534622, 0.2045095422857303724, 2.096118580758222549 ) ) ;
#116931=CARTESIAN_POINT ( 'NONE',  ( 5.863751307568212390, -0.5067217619753560109, 2.007263066363853987 ) ) ;
#116934=CARTESIAN_POINT ( 'NONE',  ( 5.220965578766386450, 1.526617224004393369, -1.322549803791906786 ) ) ;
#116936=CARTESIAN_POINT ( 'NONE',  ( 0.5673240888519160974, 1.792687530798135143, 1.019967006830464706 ) ) ;
#116942=CARTESIAN_POINT ( 'NONE',  ( 6.727182134110195832, 0.008744176509076214548, 1.710970312420513784 ) ) ;
#116944=CARTESIAN_POINT ( 'NONE',  ( 2.981114689849233113, 2.043561189653697152, 0.7337040362941152916 ) ) ;
#116948=CARTESIAN_POINT ( 'NONE',  ( 2.981803241483144351, -1.814435276338403735, -0.3121031562058202424 ) ) ;
#116951=CARTESIAN_POINT ( 'NONE',  ( 4.616832073239669043, -0.1072513232249286408, 2.189039617437993357 ) ) ;
#116953=CARTESIAN_POINT ( 'NONE',  ( 5.401357799220028788, 1.846321421614788516, 1.307461012187713933 ) ) ;
#116960=CARTESIAN_POINT ( 'NONE',  ( 6.450471989241519211, 0.5578098333037047052, 1.679625245746432016 ) ) ;
#116961=CARTESIAN_POINT ( 'NONE',  ( 4.037747573665031453, -1.925786081212683465, 0.5863696817766034242 ) ) ;
#116963=CARTESIAN_POINT ( 'NONE',  ( 3.434694453818935678, 2.054221006159732354, 0.4631738978765443382 ) ) ;
#116964=CARTESIAN_POINT ( 'NONE',  ( 0.9838322988516207124, -1.915793139027978542, 0.001352086710114385869 ) ) ;
#116967=CARTESIAN_POINT ( 'NONE',  ( 2.172252323668334206, -0.9256296301539097549, -1.738465135635240522 ) ) ;
#116969=CARTESIAN_POINT ( 'NONE',  ( 0.2681426532152464959, -1.225442487749365483, 1.413462724991432218 ) ) ;
#116970=CARTESIAN_POINT ( 'NONE',  ( 0.9944974185457016169, 1.932217576897478528, 0.3389098420027157332 ) ) ;
#116971=CARTESIAN_POINT ( 'NONE',  ( 0.6504702201592416078, 1.884490048413577368, 0.3244712162126031085 ) ) ;
#116975=CARTESIAN_POINT ( 'NONE',  ( 5.594569530875261876, -0.4557361262383099465, -1.814172972432124498 ) ) ;
#116978=CARTESIAN_POINT ( 'NONE',  ( 6.139524545372063713, 1.915082402702467101, -0.7868883245659707981 ) ) ;
#116979=CARTESIAN_POINT ( 'NONE',  ( 0.2212536527127808295, -1.848710500310095872, -0.9322282823912150240 ) ) ;
#116986=CARTESIAN_POINT ( 'NONE',  ( 5.740667459973674447, -1.913685094937540132, -0.4313615418530327150 ) ) ;
#116988=CARTESIAN_POINT ( 'NONE',  ( 3.057970071934034362, 1.730601471501746147, -1.034006501934421784 ) ) ;
#116989=CARTESIAN_POINT ( 'NONE',  ( 4.206187189226945122, 1.174002167177927713, -1.513781418528682643 ) ) ;
#116991=CARTESIAN_POINT ( 'NONE',  ( 1.400213348495438437, -0.7931047570679079506, -2.043190674350242819 ) ) ;
#116992=CARTESIAN_POINT ( 'NONE',  ( 0.1333692844072559003, 2.872395615372814515, -2.542035612928101873 ) ) ;
#116993=CARTESIAN_POINT ( 'NONE',  ( 3.672993792711932048, 0.04889617625786558258, -1.870083761627352015 ) ) ;
#116997=CARTESIAN_POINT ( 'NONE',  ( 4.288735948182021751, 1.635604132441673020, -1.344385869115312770 ) ) ;
#117000=CARTESIAN_POINT ( 'NONE',  ( 6.250451049865752395, -2.060019788584551481, -0.2068627631737207651 ) ) ;
#117001=CARTESIAN_POINT ( 'NONE',  ( 2.050439074220523406, -1.614099552242785895, 1.328842424969446823 ) ) ;
#117002=CARTESIAN_POINT ( 'NONE',  ( 6.620655732516648406, 3.679503859435423241, 2.787618683092321969 ) ) ;
#117003=CARTESIAN_POINT ( 'NONE',  ( 0.9028307623185973796, 1.406233313734496448, 0.9983791803314099322 ) ) ;
#117013=CARTESIAN_POINT ( 'NONE',  ( 0.5042037957796470238, -1.797571035118279870, -0.2231917716723781087 ) ) ;
#117020=B_SPLINE_CURVE_WITH_KNOTS ( 'NONE', 3,
 ( #140625, #189328, #107079, #109229, #40969, #92928, #124427, #42042, #108155, #25752 ),
 .UNSPECIFIED., .F., .F.,
 ( 4, 1, 1, 1, 1, 1, 1, 4 ),
 ( 0.000000000000000000, 0.09183773654504942541, 0.1838067853904964410, 0.2558923657893393822, 0.3606054339151033017, 0.5206678126786191685, 0.7335446035554463728, 1.000000000000000000 ),
 .UNSPECIFIED. ) ;
#117021=CARTESIAN_POINT ( 'NONE',  ( 6.539320575229287336, 0.6031692783194403384, 1.851139666870088130 ) ) ;
#117026=CARTESIAN_POINT ( 'NONE',  ( 2.910441987356562787, 0.6243205138760847817, 1.753359951907756065 ) ) ;
#117027=CARTESIAN_POINT ( 'NONE',  ( 0.6498251619827577485, 0.9450094616851455465, 1.666218678892321226 ) ) ;
#117028=CARTESIAN_POINT ( 'NONE',  ( 0.06529689308308950224, -1.700389599856198863, 1.266735544122286283 ) ) ;
#117036=CARTESIAN_POINT ( 'NONE',  ( 4.469560827962531846, -0.3407972494764506810, 1.939574385640041809 ) ) ;
#117037=CARTESIAN_POINT ( 'NONE',  ( 1.172698094321134477, 0.8626872041959358084, 1.937259058979395432 ) ) ;
#117041=CARTESIAN_POINT ( 'NONE',  ( 5.964808794498537736, 0.1646014364122504459, -2.185315939793014639 ) ) ;
#117042=CARTESIAN_POINT ( 'NONE',  ( 4.612281621929555264, -0.8233390244782293754, -1.741700550419862825 ) ) ;
#117044=CARTESIAN_POINT ( 'NONE',  ( 0.07680821025393690105, 0.005952109439256307241, -1.810863387344714193 ) ) ;
#117045=CARTESIAN_POINT ( 'NONE',  ( 1.331021600797330118, 2.127646391749141941, 0.5858054460900484761 ) ) ;
#117047=( NAMED_UNIT ( * ) SI_UNIT ( $, .STERADIAN. ) SOLID_ANGLE_UNIT ( ) );
#117049=CARTESIAN_POINT ( 'NONE',  ( 5.770349169015823954, -0.8820018971720828826, -1.760941755123719421 ) ) ;
#117050=CARTESIAN_POINT ( 'NONE',  ( 1.329522225144257774, 0.9558622346672830394, -1.690450677827403103 ) ) ;
#117051=CARTESIAN_POINT ( 'NONE',  ( 0.1458495181914116201, -0.1430550213798176262, -1.983920851313693223 ) ) ;
#117053=CARTESIAN_POINT ( 'NONE',  ( 4.715577910371310466, 0.4106090485030155501, -1.814890118206938574 ) ) ;
#117059=CARTESIAN_POINT ( 'NONE',  ( 0.5565083568685527116, -1.583368386835169783, 1.515454571103365344 ) ) ;
#117063=CARTESIAN_POINT ( 'NONE',  ( 1.769861954154128725, 0.9373860217288846330, 1.566528536362868707 ) ) ;
#117066=CARTESIAN_POINT ( 'NONE',  ( 3.146783715800211212, 0.7824046571166408670, 1.547702628640304168 ) ) ;
#117067=CARTESIAN_POINT ( 'NONE',  ( 6.509000000000010111, 3.701365531483376881, 2.414445852726577080 ) ) ;
#117069=CARTESIAN_POINT ( 'NONE',  ( -0.005450286198350333053, -0.4226363183827580583, -1.886779976948229853 ) ) ;
#117070=CARTESIAN_POINT ( 'NONE',  ( 5.032062496497622384, 1.126290172248314514, 1.606047186625796819 ) ) ;
#117074=CARTESIAN_POINT ( 'NONE',  ( 4.336665864168765872, 1.303721989063952424, -1.672289659653345639 ) ) ;
#117078=CARTESIAN_POINT ( 'NONE',  ( 2.500909639826456754, 0.4493149015136475022, 2.020762751476639529 ) ) ;
#117082=CARTESIAN_POINT ( 'NONE',  ( 2.690384307321362467, 1.943607183752774636, 1.227106530010623864 ) ) ;
#117088=CARTESIAN_POINT ( 'NONE',  ( 0.07536363704235826688, -0.001874865094115066300, -2.144269471569634877 ) ) ;
#117089=CARTESIAN_POINT ( 'NONE',  ( 3.603681638446740720, 1.388520161702249567, 1.315275747533505069 ) ) ;
#117091=CARTESIAN_POINT ( 'NONE',  ( 5.104412161113025093, -0.5839786719442441321, -1.623048794067801781 ) ) ;
#117092=CARTESIAN_POINT ( 'NONE',  ( 3.063685658700274761, 1.282989771343697294, 1.555699169480361022 ) ) ;
#117093=CARTESIAN_POINT ( 'NONE',  ( 4.746898448635796797, 2.273877242543398403, -0.3363112362181965853 ) ) ;
#117095=CARTESIAN_POINT ( 'NONE',  ( 0.2763675079364875664, 1.274320874971252460, 1.801605125401319007 ) ) ;
#117097=CARTESIAN_POINT ( 'NONE',  ( 5.553870903591159092, 1.767663364219349553, -0.08767779694792036949 ) ) ;
#117099=CARTESIAN_POINT ( 'NONE',  ( 1.605870876717029549, -2.274517881136278508, 0.2841979012723067077 ) ) ;
#117100=CARTESIAN_POINT ( 'NONE',  ( 0.1107398820658512667, -1.707777377628461046, 0.3340355821882161069 ) ) ;
#117103=CARTESIAN_POINT ( 'NONE',  ( 6.527279143455773536, -1.428284688129980440, -1.662137905815167294 ) ) ;
#117107=CARTESIAN_POINT ( 'NONE',  ( 6.795378861676105053, -1.851214886592133846, 0.9271815693319698237 ) ) ;
#117108=CARTESIAN_POINT ( 'NONE',  ( 0.6730650033222317363, 1.776164188848127878, -0.9548607967814757291 ) ) ;
#117110=CARTESIAN_POINT ( 'NONE',  ( 5.092375307706883625, -1.912163826771107855, -0.2340926620403842862 ) ) ;
#117112=CARTESIAN_POINT ( 'NONE',  ( 1.793536179914383188, -0.1149406603053771958, -2.218580859979270681 ) ) ;
#117120=CARTESIAN_POINT ( 'NONE',  ( 4.247407853763897734, 1.739958666061100390, -0.04810691789801542495 ) ) ;
#117121=CARTESIAN_POINT ( 'NONE',  ( 2.260140581184489239, -1.961506502764579052, 0.04509734162668613960 ) ) ;
#117127=CARTESIAN_POINT ( 'NONE',  ( 0.5728089798012192535, 1.423622861147020302, -1.492835154123072883 ) ) ;
#117130=CARTESIAN_POINT ( 'NONE',  ( 0.9895999521203084903, 1.994116446801162290, -1.068836969126084835 ) ) ;
#117133=CARTESIAN_POINT ( 'NONE',  ( 2.090876104454452378, 1.629797177321444579, -0.9178172146045021629 ) ) ;
#117134=CARTESIAN_POINT ( 'NONE',  ( 0.9317525018172129192, -1.365947654462830618, -1.068275208499162909 ) ) ;
#117135=CARTESIAN_POINT ( 'NONE',  ( 5.829655996829377962, 1.081331853127937448, -1.906115348727636549 ) ) ;
#117136=CARTESIAN_POINT ( 'NONE',  ( 5.280430876874616430, -1.287285901688420608, 1.914989055045878352 ) ) ;
#117137=CARTESIAN_POINT ( 'NONE',  ( 0.9892191112199534286, 1.817966452439750968, -0.9706697534878678812 ) ) ;
#117138=CARTESIAN_POINT ( 'NONE',  ( 3.978411374042570170, -0.1916562231945718731, -1.932471992628071789 ) ) ;
#117141=CARTESIAN_POINT ( 'NONE',  ( 6.098880659294531270, 1.529360415809786433, -1.076766019972655197 ) ) ;
#117142=CARTESIAN_POINT ( 'NONE',  ( 0.6562500000000004441, -1.895863743164078130, 0.7852924748300215141 ) ) ;
#117146=CARTESIAN_POINT ( 'NONE',  ( 4.852185490356213826, 0.1948433276699329531, -2.006959737079899497 ) ) ;
#117151=CARTESIAN_POINT ( 'NONE',  ( 2.683998146737070378, -0.9385614705539682134, 1.565816405032012470 ) ) ;
#117160=CARTESIAN_POINT ( 'NONE',  ( -0.1403647893034008221, -1.563942476893056543, -1.277904792927646582 ) ) ;
#117161=CARTESIAN_POINT ( 'NONE',  ( 0.2410938523699951708, 2.030451451530786766, 0.6113826261911479154 ) ) ;
#117162=VERTEX_POINT ( 'NONE', #41621 ) ;
#117165=CARTESIAN_POINT ( 'NONE',  ( 5.594623806460828241, -0.4985412361782278201, -1.999555476978178703 ) ) ;
#117166=CARTESIAN_POINT ( 'NONE',  ( 4.764296165657141202, 1.880435471729305030, -0.7283773170061805802 ) ) ;
#117175=CARTESIAN_POINT ( 'NONE',  ( 4.973982425466109802, 1.752763018817087293, 0.9961474888594208377 ) ) ;
#117176=CARTESIAN_POINT ( 'NONE',  ( 4.804558796598876746, 1.603369264058150279, 0.9048477820690554729 ) ) ;
#117178=CARTESIAN_POINT ( 'NONE',  ( -0.02338929933909209696, 6.948787603726593431, -2.306014233525994772 ) ) ;
#117179=CARTESIAN_POINT ( 'NONE',  ( 2.842713172187049331, 2.290369893530233902, 0.2817356681584815004 ) ) ;
#117181=CARTESIAN_POINT ( 'NONE',  ( 4.868538603872567982, -1.416007186031362330, 1.633285015310452115 ) ) ;
#117183=CARTESIAN_POINT ( 'NONE',  ( 0.2572359396431650458, 1.920763697077633614, -0.2861409625158922165 ) ) ;
#117187=CARTESIAN_POINT ( 'NONE',  ( 3.309304339999539657, -0.3661640501408692794, 1.834289908569000538 ) ) ;
#117189=CARTESIAN_POINT ( 'NONE',  ( 1.371198541116287917, -1.641758494746584418, -0.9804709962101465504 ) ) ;
#117193=CARTESIAN_POINT ( 'NONE',  ( 3.106307083854151774, -2.204334110825040494, 0.1085914373066959593 ) ) ;
#117199=CARTESIAN_POINT ( 'NONE',  ( 0.8429695343807745989, -1.692941477971823483, 1.009804834249914851 ) ) ;
#117201=CARTESIAN_POINT ( 'NONE',  ( 6.481126831302748137, -0.1059855822947413234, -2.305399816445557359 ) ) ;
#117202=CARTESIAN_POINT ( 'NONE',  ( 1.328483007144948935, -1.247240240105648601, 1.514344512384787622 ) ) ;
#117203=CARTESIAN_POINT ( 'NONE',  ( 4.293840196874755044, -1.418639180022958080, -1.497458912744116022 ) ) ;
#117211=CARTESIAN_POINT ( 'NONE',  ( 6.865710891575433905, -0.4862813381408522817, 2.124062634707358566 ) ) ;
#117212=CARTESIAN_POINT ( 'NONE',  ( 6.480030769895370746, -1.807141314969593848, -0.3518929191878711338 ) ) ;
#117215=CARTESIAN_POINT ( 'NONE',  ( 1.897508810457830153, -0.6348907881138059484, 1.759622905829677508 ) ) ;
#117221=CARTESIAN_POINT ( 'NONE',  ( 1.453610327690219473, -1.385809040371610346, -1.317956379189986871 ) ) ;
#117222=CARTESIAN_POINT ( 'NONE',  ( 2.746659024021454787, -1.472625519509669134, 0.9813492100937453166 ) ) ;
#117223=CARTESIAN_POINT ( 'NONE',  ( 0.8910925258837493201, -0.04752833427993513604, -1.911862225341356858 ) ) ;
#117225=CARTESIAN_POINT ( 'NONE',  ( 3.954619794068328087, -1.788705220947036878, -0.6861305607534126105 ) ) ;
#117226=CARTESIAN_POINT ( 'NONE',  ( 5.969198390587827419, 1.736284540159404033, 0.9297856951416498816 ) ) ;
#117227=CARTESIAN_POINT ( 'NONE',  ( 1.072698285844303934, 0.8645715524648779349, 1.936551149067309741 ) ) ;
#117229=CARTESIAN_POINT ( 'NONE',  ( 4.170664822833985319, -1.745344833062393075, -0.6735866001992969476 ) ) ;
#117230=CARTESIAN_POINT ( 'NONE',  ( 0.4338677482375961070, 0.9413943332680120291, -1.564114433284753636 ) ) ;
#117232=CARTESIAN_POINT ( 'NONE',  ( 3.440233207309027375, 0.9924059104887033023, -1.971224004288201881 ) ) ;
#117235=CARTESIAN_POINT ( 'NONE',  ( 0.6431264911748921786, -0.2508561283167276557, -2.047287668789533832 ) ) ;
#117242=CARTESIAN_POINT ( 'NONE',  ( 4.299325596424930396, -1.802881993240162961, 1.017688063649782482 ) ) ;
#117244=CARTESIAN_POINT ( 'NONE',  ( 1.739762150092131643, -1.564342989677082629, -1.491970722459233123 ) ) ;
#117246=CARTESIAN_POINT ( 'NONE',  ( 1.524088222275731486, -2.004166515738073695, 0.2493262195080257204 ) ) ;
#117253=CARTESIAN_POINT ( 'NONE',  ( -0.1355283706049141557, -1.957205112593700003, -0.4852584411360050254 ) ) ;
#117254=CARTESIAN_POINT ( 'NONE',  ( 4.388337494309430653, -0.4807229498768311182, -2.138019847805587403 ) ) ;
#117257=CARTESIAN_POINT ( 'NONE',  ( 3.357576282340120066, -1.451192137084562628, -1.245647637661301044 ) ) ;
#117261=CARTESIAN_POINT ( 'NONE',  ( 1.071888921174158016, -0.9040910708146729924, 1.802427947461216373 ) ) ;
#117264=CARTESIAN_POINT ( 'NONE',  ( 0.8906306365582180584, -0.5635816346751547634, -2.221901885516941899 ) ) ;
#117266=CARTESIAN_POINT ( 'NONE',  ( 3.996854971928843092, 1.456802638785438475, -0.9229968019349673591 ) ) ;
#117267=CARTESIAN_POINT ( 'NONE',  ( -0.1399997263889819765, 0.7174702203470960660, -2.082715917450683740 ) ) ;
#117270=CARTESIAN_POINT ( 'NONE',  ( 1.715213470010600538, -1.680963409367957295, -1.011360081469035999 ) ) ;
#117273=CARTESIAN_POINT ( 'NONE',  ( 0.1751657365761547791, 2.016170943927285908, -2.458682602970231112 ) ) ;
#117277=CARTESIAN_POINT ( 'NONE',  ( 4.125510307337266980, -0.3055505145112321075, 1.785335377935037826 ) ) ;
#117281=CARTESIAN_POINT ( 'NONE',  ( 4.969312858920484466, -1.533218896822113653, -0.9643851972171797460 ) ) ;
#117284=FILL_AREA_STYLE_COLOUR ( '', #194040 ) ;
#117287=CARTESIAN_POINT ( 'NONE',  ( 5.969184020103408095, 1.641702931788184383, 0.8765767931452476125 ) ) ;
#117289=CARTESIAN_POINT ( 'NONE',  ( 4.271028807069753519, 1.709443138559762376, -0.8646770750302870123 ) ) ;
#117296=CARTESIAN_POINT ( 'NONE',  ( 0.9015118058452382677, 1.767791302423503685, 1.243857928393626633 ) ) ;
#117299=CARTESIAN_POINT ( 'NONE',  ( 0.3756504392133250825, 1.046533627790873000, 1.495644344755318045 ) ) ;
#117301=CARTESIAN_POINT ( 'NONE',  ( 3.100428009929767637, -0.5284298666012043899, -1.747434388548900541 ) ) ;
#117303=CARTESIAN_POINT ( 'NONE',  ( 1.951281838316549777, -1.706683157587106425, 0.8630329916254894096 ) ) ;
#117305=CARTESIAN_POINT ( 'NONE',  ( 2.172252323668334206, -0.9256296301539097549, -1.738465135635240522 ) ) ;
#117306=CARTESIAN_POINT ( 'NONE',  ( 4.757337479089009058, 1.920383491809660503, -0.2886861380682907430 ) ) ;
#117309=CARTESIAN_POINT ( 'NONE',  ( 3.656581996618038843, 2.110704406498860486, 0.2042969539849878724 ) ) ;
#117320=CARTESIAN_POINT ( 'NONE',  ( 4.477060521952030747, -0.002618581577289170060, -1.825872481161804561 ) ) ;
#117325=CARTESIAN_POINT ( 'NONE',  ( 5.823093596695693819, -0.04436734784114480107, 1.870300906237104988 ) ) ;
#117336=CARTESIAN_POINT ( 'NONE',  ( 0.6200890622066607127, 2.048230590617374336, -0.3001980380039070972 ) ) ;
#117337=CARTESIAN_POINT ( 'NONE',  ( 1.616979318382205433, 0.2114564432566454211, 2.106663336370690143 ) ) ;
#117340=CARTESIAN_POINT ( 'NONE',  ( 5.770397209236588942, -0.9257025293247715947, -1.851810055641222252 ) ) ;
#117341=CARTESIAN_POINT ( 'NONE',  ( 2.032514702046281485, -1.644074058028240692, 0.8291662819630771786 ) ) ;
#117346=CARTESIAN_POINT ( 'NONE',  ( 1.517954844142660464, -1.276539353255158105, -1.903739821206115623 ) ) ;
#117351=CARTESIAN_POINT ( 'NONE',  ( 0.1408853756387764278, 1.927792606564913136, 0.5802787064154624197 ) ) ;
#117352=CARTESIAN_POINT ( 'NONE',  ( 0.6374591745182572877, 1.832550977151351290, -0.7006947966294306829 ) ) ;
#117353=CARTESIAN_POINT ( 'NONE',  ( 6.491432910188612126, -0.4373703761123280964, 1.975813455233149218 ) ) ;
#117357=CARTESIAN_POINT ( 'NONE',  ( 4.101575158799015242, -2.085053422979638693, 0.1536182331017873492 ) ) ;
#117358=CARTESIAN_POINT ( 'NONE',  ( 2.078617942332625201, -0.08328603760934982780, -1.768007077409910588 ) ) ;
#117361=CARTESIAN_POINT ( 'NONE',  ( 5.296947879282962290, 1.871547875688117424, 1.323312301801358393 ) ) ;
#117362=CARTESIAN_POINT ( 'NONE',  ( 3.398151218454207090, 1.370964323331394397, -1.071876607410700677 ) ) ;
#117365=AXIS2_PLACEMENT_3D ( 'NONE', #58802, #41507, #171482 ) ;
#117367=CARTESIAN_POINT ( 'NONE',  ( 2.811537702714523856, -1.443443483380968173, 0.9601682615991720127 ) ) ;
#117368=CARTESIAN_POINT ( 'NONE',  ( 3.068971866484587530, 1.574395709666128296, -1.495330859492151943 ) ) ;
#117370=CARTESIAN_POINT ( 'NONE',  ( 5.067592334412735156, 1.357865985192594271, 1.490972259599515848 ) ) ;
#117371=CARTESIAN_POINT ( 'NONE',  ( 1.062500000000000888, -1.451031289061164742, -1.451031289061077922 ) ) ;
#117373=CARTESIAN_POINT ( 'NONE',  ( 1.870020283345479539, 0.9883514471830873171, 1.653387599232780447 ) ) ;
#117375=CARTESIAN_POINT ( 'NONE',  ( 5.994412725124051100, -1.189069957525538124, 1.876188141934010956 ) ) ;
#117377=CARTESIAN_POINT ( 'NONE',  ( -0.1110810684432622653, 2.888487728959455936, -2.285870655067727242 ) ) ;
#117382=CARTESIAN_POINT ( 'NONE',  ( 1.524421784905782618, -2.203991335649616357, 0.2763902372489163151 ) ) ;
#117383=CARTESIAN_POINT ( 'NONE',  ( 6.514115657861259123, 1.956686900881845714, -0.1430618042221123987 ) ) ;
#117387=CARTESIAN_POINT ( 'NONE',  ( 0.3159878724818787066, -2.119942686789745068, 0.4214050671751194410 ) ) ;
#117390=CARTESIAN_POINT ( 'NONE',  ( 4.457523014600942801, 1.654850327679569633, 1.231099151980449724 ) ) ;
#117394=CARTESIAN_POINT ( 'NONE',  ( 6.415307259278708152, -0.2288938695442776505, 1.856442058181500654 ) ) ;
#117395=CARTESIAN_POINT ( 'NONE',  ( 4.553154410594215662, -1.128159591824983377, 1.317121951208845454 ) ) ;
#117396=CARTESIAN_POINT ( 'NONE',  ( 4.845099162036492046, 0.5397016130457911176, -1.654733517006673482 ) ) ;
#117398=CARTESIAN_POINT ( 'NONE',  ( 2.033172958078794501, -2.045629734292064850, 1.034765616053961557 ) ) ;
#117400=CARTESIAN_POINT ( 'NONE',  ( 5.741762370215764300, 2.088391581209507741, 0.1015199779932918489 ) ) ;
#117401=CARTESIAN_POINT ( 'NONE',  ( 6.263619209540105537, 1.000520857970560895, 1.664240579554799648 ) ) ;
#117405=CARTESIAN_POINT ( 'NONE',  ( 1.231092510272915552, 2.014232830173094513, 0.09613330637052441840 ) ) ;
#117406=CARTESIAN_POINT ( 'NONE',  ( 0.4104466507391414387, 1.508250410577081979, -1.590083307377434974 ) ) ;
#117410=CARTESIAN_POINT ( 'NONE',  ( 3.492942606646631809, -2.044086983709763050, -0.5638711869686771072 ) ) ;
#117412=CARTESIAN_POINT ( 'NONE',  ( 5.356004772612798170, 1.823420152956479523, -0.09349780940721279243 ) ) ;
#117419=CARTESIAN_POINT ( 'NONE',  ( 3.463153198524880239, -1.648742896667846125, 1.166392943622736267 ) ) ;
#117420=CARTESIAN_POINT ( 'NONE',  ( 0.3586045525620683017, 0.8063113102214304329, 1.945692106844071789 ) ) ;
#117422=CARTESIAN_POINT ( 'NONE',  ( 4.522197165953073750, 0.8743044213657903407, 1.642730557785059053 ) ) ;
#117431=CARTESIAN_POINT ( 'NONE',  ( 2.038076752987047602, 1.660595340560795607, -0.4986328326925906773 ) ) ;
#117432=CARTESIAN_POINT ( 'NONE',  ( 0.9193797689642355664, 1.039780534333001771, -1.395406566618085709 ) ) ;
#117434=CARTESIAN_POINT ( 'NONE',  ( 0.4820102390354238375, 2.151571070674349606, -0.8345519191893053801 ) ) ;
#117437=CARTESIAN_POINT ( 'NONE',  ( 0.9134385407369073340, -0.3049482027854091837, 2.037980195292460550 ) ) ;
#117440=CARTESIAN_POINT ( 'NONE',  ( 0.3333609138582178111, -1.319029705771988858, 1.524807370920200356 ) ) ;
#117443=CARTESIAN_POINT ( 'NONE',  ( 6.719622092096638966, -1.813896567892055112, 0.4569536213836836169 ) ) ;
#117444=CARTESIAN_POINT ( 'NONE',  ( 4.271672842113056312, 0.4137096367802223784, -1.866957553337177611 ) ) ;
#117447=CARTESIAN_POINT ( 'NONE',  ( 5.988949835885216011, -0.3198878037087344306, -2.183464699167809275 ) ) ;
#117452=CARTESIAN_POINT ( 'NONE',  ( 6.569000932001921811, -1.639521903533578850, 1.344440124909966450 ) ) ;
#117454=CARTESIAN_POINT ( 'NONE',  ( 2.925200879784293218, 2.172439923367448067, 0.7784344579512092466 ) ) ;
#117455=CARTESIAN_POINT ( 'NONE',  ( 4.650807877244386823, -0.4278111053654386486, -1.914496481071884970 ) ) ;
#117456=CARTESIAN_POINT ( 'NONE',  ( 1.287862062775881666, -1.240280065097350448, -1.519972987346601023 ) ) ;
#117460=CARTESIAN_POINT ( 'NONE',  ( 0.3392563814038212500, -1.792290195912203954, -1.127034558586788249 ) ) ;
#117463=CARTESIAN_POINT ( 'NONE',  ( 4.030270078087188068, 1.201442806954319487, 1.808153907555063000 ) ) ;
#117465=CARTESIAN_POINT ( 'NONE',  ( 1.881254504445781794, -1.940830296247602949, -0.8548571619346673200 ) ) ;
#117471=CARTESIAN_POINT ( 'NONE',  ( 1.880222553438152033, -1.104958259108330898, 1.739320704499922154 ) ) ;
#117475=CARTESIAN_POINT ( 'NONE',  ( 0.07775346131144719730, 4.079442786094135798, -2.843586357576178614 ) ) ;
#117478=CARTESIAN_POINT ( 'NONE',  ( 5.039673278062164918, -1.814583965733532978, 0.6035816954967700987 ) ) ;
#117481=CARTESIAN_POINT ( 'NONE',  ( 2.056323133375201007, 2.256402538945650349, -0.1652075827990733270 ) ) ;
#117483=CARTESIAN_POINT ( 'NONE',  ( 1.845701740803426194, -1.185437281251604746, -1.369922693571566485 ) ) ;
#117484=CARTESIAN_POINT ( 'NONE',  ( 1.042033841529757421, 0.7795281806207611242, 1.750150644309953041 ) ) ;
#117485=CARTESIAN_POINT ( 'NONE',  ( 2.541538742049511246, 1.893869637037654208, -0.8368498079355383146 ) ) ;
#117487=CARTESIAN_POINT ( 'NONE',  ( 0.1980364362535640133, -1.970970528886636153, -0.05095907160383715551 ) ) ;
#117488=CARTESIAN_POINT ( 'NONE',  ( 6.041620323887018529, -1.397190737843529540, -1.326607404314980254 ) ) ;
#117489=CARTESIAN_POINT ( 'NONE',  ( 0.3293365701910222487, 2.210228212078951149, 0.6636047247109229108 ) ) ;
#117492=CARTESIAN_POINT ( 'NONE',  ( 4.738769042418014443, -1.999979230503599048, -0.5042011814720639418 ) ) ;
#117497=CARTESIAN_POINT ( 'NONE',  ( 5.649480931864863109, -1.658039504894607719, -1.298324887859639842 ) ) ;
#117499=CARTESIAN_POINT ( 'NONE',  ( 0.6081839208269465002, 0.6806018353129331677, -2.061787349250172596 ) ) ;
#117501=CARTESIAN_POINT ( 'NONE',  ( 5.167319818800252484, 0.2175342549677051207, -2.150644138106901693 ) ) ;
#117502=CARTESIAN_POINT ( 'NONE',  ( 4.899084735882781594, -0.2492385452713632155, -2.004177415419911679 ) ) ;
#117508=CARTESIAN_POINT ( 'NONE',  ( 4.065638850954083061, 1.320825628876612479, 1.523796413913918846 ) ) ;
#117512=CARTESIAN_POINT ( 'NONE',  ( 4.909125497034264818, 1.879091090907711425, 1.068517025386829467 ) ) ;
#117516=CARTESIAN_POINT ( 'NONE',  ( 5.730092268227672037, 2.014234620932173758, 0.09611943034040781875 ) ) ;
#117518=CARTESIAN_POINT ( 'NONE',  ( 0.6270765232691848379, -1.639361371195736439, 0.5365680580288884061 ) ) ;
#117523=CARTESIAN_POINT ( 'NONE',  ( 5.501189692264965458, 1.528658022856645315, 1.077728667985423661 ) ) ;
#117524=CARTESIAN_POINT ( 'NONE',  ( 6.011982430150495382, -0.6741147929612385514, 1.897138445369117354 ) ) ;
#117529=CARTESIAN_POINT ( 'NONE',  ( 2.350376503035214615, 0.9972050307137376723, -1.871358364749615033 ) ) ;
#117530=CARTESIAN_POINT ( 'NONE',  ( 1.775017769237042353, 1.753020666602569166, -0.9963212463810557917 ) ) ;
#117531=CARTESIAN_POINT ( 'NONE',  ( 1.652323331381430283, 1.792179557038487303, 0.2633440673391762576 ) ) ;
#117533=CARTESIAN_POINT ( 'NONE',  ( 6.719591497160966931, -2.098179372288328182, 0.5198544864785522579 ) ) ;
#117537=CARTESIAN_POINT ( 'NONE',  ( -0.08300117844089061059, -1.750507139949438296, 0.7787328797612643738 ) ) ;
#117545=CARTESIAN_POINT ( 'NONE',  ( 4.504844740329728481, 1.672958716126593082, -1.369014088531981255 ) ) ;
#117548=CARTESIAN_POINT ( 'NONE',  ( 1.582450481569739331, 1.094613367649547309, 1.816135667671102016 ) ) ;
#117550=CARTESIAN_POINT ( 'NONE',  ( 2.143765197515819843, 0.7580581125649475949, -1.819971111534921970 ) ) ;
#117551=CARTESIAN_POINT ( 'NONE',  ( 4.447458312869024155, -1.746245811230532130, 0.7801085911468002010 ) ) ;
#117554=CARTESIAN_POINT ( 'NONE',  ( 6.531706384513794816, 1.885137803977337656, -0.5704747015483744299 ) ) ;
#117555=CARTESIAN_POINT ( 'NONE',  ( 1.236160255307724665, 0.3784122030587311336, 1.904561997804487428 ) ) ;
#117562=CARTESIAN_POINT ( 'NONE',  ( 5.918603479541379109, -0.6925943527147163659, -1.782627650866043911 ) ) ;
#117564=CARTESIAN_POINT ( 'NONE',  ( 3.264504910713565078, 0.9923201075644829672, 1.971275125648555449 ) ) ;
#117566=CARTESIAN_POINT ( 'NONE',  ( 1.747397587315654865, -1.864034986486883261, 1.180896971623420999 ) ) ;
#117568=CARTESIAN_POINT ( 'NONE',  ( 0.7504700684401002242, 1.884043224930329385, 0.3264296256808990049 ) ) ;
#117571=CARTESIAN_POINT ( 'NONE',  ( 3.420434311836465291, 0.9283866757503268508, 1.850595421526677775 ) ) ;
#117575=CARTESIAN_POINT ( 'NONE',  ( 1.393688021309073433, 1.637156065531343740, 1.411701162175371893 ) ) ;
#117576=CARTESIAN_POINT ( 'NONE',  ( 3.948915171154475878, -1.822730400009948237, -1.216494452853926322 ) ) ;
#117586=CARTESIAN_POINT ( 'NONE',  ( 6.311143239517568837, 0.9901597221020401740, -1.423469027432751943 ) ) ;
#117588=CARTESIAN_POINT ( 'NONE',  ( 3.854399998794607818, -2.067664388167046674, -0.1065051105964970740 ) ) ;
#117589=CARTESIAN_POINT ( 'NONE',  ( 4.675474996081856460, 1.569897879423647336, 1.420792320860002178 ) ) ;
#117592=CARTESIAN_POINT ( 'NONE',  ( 2.623828205405827507, 1.932375918485039756, -0.3793698109293401344 ) ) ;
#117593=CARTESIAN_POINT ( 'NONE',  ( 0.5449873876890098945, 0.1430962203496731200, 1.907122450762772647 ) ) ;
#117594=CARTESIAN_POINT ( 'NONE',  ( 4.295090358266894448, 1.839821235612853600, 1.367129665020486273 ) ) ;
#117595=CARTESIAN_POINT ( 'NONE',  ( 2.807047293222181494, 1.542382716246639696, 0.9765254425028800922 ) ) ;
#117601=CARTESIAN_POINT ( 'NONE',  ( 4.271743731491533858, 0.4368499997736470797, -1.965098791395853750 ) ) ;
#117602=CARTESIAN_POINT ( 'NONE',  ( 4.082823661314609609, 1.861412734803047142, 0.6194944872321901386 ) ) ;
#117606=CARTESIAN_POINT ( 'NONE',  ( 0.6090670738765286973, -0.3027767823605455599, 2.068569423397928819 ) ) ;
#117607=CARTESIAN_POINT ( 'NONE',  ( 5.383597848809928088, 1.190821987996647513, 1.309499010278234898 ) ) ;
#117609=CARTESIAN_POINT ( 'NONE',  ( 2.220887445055406584, 0.001640320231081903845, 2.191629467496846839 ) ) ;
#117610=CARTESIAN_POINT ( 'NONE',  ( 0.1865103356883268948, 1.287481616103260063, 1.171338548376497535 ) ) ;
#117612=CARTESIAN_POINT ( 'NONE',  ( 0.1333692844072559280, 0.001398348041498076455, -2.053671342968105051 ) ) ;
#117613=CARTESIAN_POINT ( 'NONE',  ( 0.3985097114710112742, 1.437023721582047830, -0.9536953323180746844 ) ) ;
#117614=CARTESIAN_POINT ( 'NONE',  ( 1.124856824619735463, 0.4467566299657543816, -2.254411929275771609 ) ) ;
#117615=CARTESIAN_POINT ( 'NONE',  ( 0.9607770615731696662, -1.983481723135366304, -0.9323335341336475013 ) ) ;
#117616=CARTESIAN_POINT ( 'NONE',  ( 6.661516750719080449, -0.4673772157907078451, -1.669595843636323185 ) ) ;
#117617=CARTESIAN_POINT ( 'NONE',  ( 3.264504910713565078, 0.9923201075644829672, 1.971275125648555449 ) ) ;
#117618=CARTESIAN_POINT ( 'NONE',  ( 6.503150282362620160, -0.1410805869419759218, 1.984311032119711715 ) ) ;
#117621=CARTESIAN_POINT ( 'NONE',  ( 6.725048307591657171, -1.982231927674932948, -0.8863045971672071088 ) ) ;
#117623=CARTESIAN_POINT ( 'NONE',  ( 2.255205753237074617, 0.09875464746901543855, -2.115135400419057010 ) ) ;
#117624=CARTESIAN_POINT ( 'NONE',  ( 6.620655732516651071, 4.689394895873098434, 2.736297475404291024 ) ) ;
#117625=CARTESIAN_POINT ( 'NONE',  ( 5.086904980214876915, -0.2357887182157791250, -1.911833357141810241 ) ) ;
#117627=CARTESIAN_POINT ( 'NONE',  ( 2.226505721922732661, 2.224568380592424344, 0.5530147644091478742 ) ) ;
#117631=CARTESIAN_POINT ( 'NONE',  ( 4.319114520555938697, 1.717138752081597719, -1.409087234901666763 ) ) ;
#117638=CARTESIAN_POINT ( 'NONE',  ( 3.111954093273407107, 0.05229746705895028935, 2.015912966248374349 ) ) ;
#117640=CARTESIAN_POINT ( 'NONE',  ( 0.7782751772977951621, -1.100228457372550261, -1.744432094316533677 ) ) ;
#117645=CARTESIAN_POINT ( 'NONE',  ( 4.224703044441734612, 0.1064595904514322594, 2.188988589495489911 ) ) ;
#117646=CARTESIAN_POINT ( 'NONE',  ( 0.8971115437808926396, -0.9091470795906559932, -1.799921601489597123 ) ) ;
#117647=CARTESIAN_POINT ( 'NONE',  ( 1.153568636672014369, 0.7464410156945017194, 1.683350060182234209 ) ) ;
#117648=CARTESIAN_POINT ( 'NONE',  ( 4.862941710081361002, 0.2263591102839345448, -2.281146386033555462 ) ) ;
#117649=CARTESIAN_POINT ( 'NONE',  ( 3.046634964419430158, -1.505538468004435027, -1.059505732788845966 ) ) ;
#117653=CARTESIAN_POINT ( 'NONE',  ( 4.067279105520240634, 0.2236234833344897255, -1.811772463268163547 ) ) ;
#117654=CARTESIAN_POINT ( 'NONE',  ( 5.221327349844218091, 1.987046161919112430, 0.3419379449052239450 ) ) ;
#117656=CARTESIAN_POINT ( 'NONE',  ( 5.032209928657234599, 1.167594373104458461, -1.937845176762391874 ) ) ;
#117658=CARTESIAN_POINT ( 'NONE',  ( 6.668975466350578252, -1.923848446808050783, -0.8571054451525415008 ) ) ;
#117660=CARTESIAN_POINT ( 'NONE',  ( 4.176279081494421952, -1.061646348645030713, -1.777293304589353085 ) ) ;
#117663=PRODUCT_CONTEXT ( 'NONE', #122578, 'mechanical' ) ;
#117665=CARTESIAN_POINT ( 'NONE',  ( 2.104012753913253153, -1.926084867047285654, 0.04718631861246740111 ) ) ;
#117667=CARTESIAN_POINT ( 'NONE',  ( 6.877801621836153068, -1.911143888484008846, 0.4753377615324301253 ) ) ;
#117671=CARTESIAN_POINT ( 'NONE',  ( 1.301209403646291118, -0.3165094942152619772, -2.096747597609450953 ) ) ;
#117672=CARTESIAN_POINT ( 'NONE',  ( 1.969254952099579459, -1.713688747078499830, 1.413451004025434665 ) ) ;
#117673=CARTESIAN_POINT ( 'NONE',  ( 3.346800460960248191, 0.5101267414385314281, 2.043117269239830947 ) ) ;
#117677=CARTESIAN_POINT ( 'NONE',  ( 0.7482324461028444507, -1.846328264857381996, -0.2332022352751206007 ) ) ;
#117684=CARTESIAN_POINT ( 'NONE',  ( 1.107859837811319581, 1.609452232531217275, 1.380942675281403353 ) ) ;
#117687=CARTESIAN_POINT ( 'NONE',  ( 4.334394203492665909, -1.131343785558375226, 1.602600411086833931 ) ) ;
#117688=CARTESIAN_POINT ( 'NONE',  ( 3.239309987758617115, -1.907233169736745060, 1.017530501952010447 ) ) ;
#117689=CARTESIAN_POINT ( 'NONE',  ( 2.225889136967126536, 1.786374552192676823, 0.4457033907802817052 ) ) ;
#117692=CARTESIAN_POINT ( 'NONE',  ( 4.136439897933008147, -1.512742658674090857, 0.8602829033797516622 ) ) ;
#117696=CARTESIAN_POINT ( 'NONE',  ( 1.938557520917514987, 2.138169252768943984, 0.3173444169591658204 ) ) ;
#117698=CARTESIAN_POINT ( 'NONE',  ( 3.057970071934034362, 1.730601471501746147, -1.034006501934421784 ) ) ;
#117700=CARTESIAN_POINT ( 'NONE',  ( 0.8663662989462637132, 1.066309655776727539, 1.880320099339624296 ) ) ;
#117701=CARTESIAN_POINT ( 'NONE',  ( 3.221511537501456690, -1.900432112322864464, 0.5242411554721800870 ) ) ;
#117702=CARTESIAN_POINT ( 'NONE',  ( 6.609000000000047947, 2.072800852438889230, 2.208748404276588584 ) ) ;
#117703=CARTESIAN_POINT ( 'NONE',  ( 2.929168808825276749, -1.306124965484034117, -1.437377093338227496 ) ) ;
#117713=CARTESIAN_POINT ( 'NONE',  ( 0.2884678563945877738, -1.037960011796670523, 1.947446179978419512 ) ) ;
#117715=CARTESIAN_POINT ( 'NONE',  ( 5.594571816639393624, 1.932094781187740917, 0.3390067100078468232 ) ) ;
#117716=CARTESIAN_POINT ( 'NONE',  ( 1.899064777474347654, -0.9530127170578571727, -1.777010740487514173 ) ) ;
#117718=CARTESIAN_POINT ( 'NONE',  ( 4.030539441936417333, 0.5683090829115284848, 2.039553408600587758 ) ) ;
#117722=CARTESIAN_POINT ( 'NONE',  ( 3.011469152984513009, -0.9080073089506625061, -1.601583425259824001 ) ) ;
#117727=CARTESIAN_POINT ( 'NONE',  ( 5.484674493353773883, -1.343714522216314489, 1.640574901390474460 ) ) ;
#117730=CARTESIAN_POINT ( 'NONE',  ( 5.026665581557772100, 1.970771621317930045, 0.6023086073758465719 ) ) ;
#117732=CARTESIAN_POINT ( 'NONE',  ( 0.6954782174160825114, -1.312119466559122927, -1.320074052667360665 ) ) ;
#117733=CARTESIAN_POINT ( 'NONE',  ( 2.454439063956286304, -1.602943312447857593, -0.9057913635923324769 ) ) ;
#117737=CARTESIAN_POINT ( 'NONE',  ( 2.104404934925046877, -2.206339196854599116, 0.05594281105186085790 ) ) ;
#117738=CARTESIAN_POINT ( 'NONE',  ( 4.886124051547468206, -1.072500323723464932, 1.992072436074944219 ) ) ;
#117740=CARTESIAN_POINT ( 'NONE',  ( 4.640750240102114788, 1.735609681454729492, 0.5192115853321179753 ) ) ;
#117741=CARTESIAN_POINT ( 'NONE',  ( 4.821452977306352139, -1.359283356373307328, -1.350213215339219897 ) ) ;
#117745=CARTESIAN_POINT ( 'NONE',  ( 3.608241331778249350, -0.7978255515562487910, -1.802987302761626998 ) ) ;
#117746=CARTESIAN_POINT ( 'NONE',  ( 5.137510444216992767, -1.323429205136433140, -1.322332877454430955 ) ) ;
#117747=CARTESIAN_POINT ( 'NONE',  ( 4.404655029226283602, 0.4953248787317258706, 1.793866421858918869 ) ) ;
#117750=CARTESIAN_POINT ( 'NONE',  ( 0.4621254960020632074, -1.116205757145168231, 1.679226196708947239 ) ) ;
#117752=CARTESIAN_POINT ( 'NONE',  ( 1.295691649255722888, 1.595764685746006384, 1.374534258749359861 ) ) ;
#117755=CARTESIAN_POINT ( 'NONE',  ( 0.07479286986305545837, 0.7422478802248284602, -1.939684878352589070 ) ) ;
#117756=CARTESIAN_POINT ( 'NONE',  ( 3.445663904809421307, -1.957918079443463855, 0.8150281543025169606 ) ) ;
#117758=CARTESIAN_POINT ( 'NONE',  ( 2.302995500392619022, -0.3493979467522835836, -1.989178256620740548 ) ) ;
#117760=CARTESIAN_POINT ( 'NONE',  ( 6.720655732516641834, 0.008434553976904584152, 1.726293928996263771 ) ) ;
#117763=CARTESIAN_POINT ( 'NONE',  ( 2.003414267471514965, 1.795956895356983551, 1.202623776965026536 ) ) ;
#117764=CARTESIAN_POINT ( 'NONE',  ( 6.610000000000009202, 1.996100381701769289, 2.581056663040970811 ) ) ;
#117771=CARTESIAN_POINT ( 'NONE',  ( 1.224469250947546328, 2.113408192816915943, 0.5798510048089372537 ) ) ;
#117773=CARTESIAN_POINT ( 'NONE',  ( 1.235668275047563380, -2.044475609799735416, 0.9693208282701860634 ) ) ;
#117780=CARTESIAN_POINT ( 'NONE',  ( 4.512129967005336084, -0.7409026826630369378, -1.557792038885176700 ) ) ;
#117782=CARTESIAN_POINT ( 'NONE',  ( 2.618099050500310998, 1.159573672392331112, -1.336980558935680241 ) ) ;
#117785=CARTESIAN_POINT ( 'NONE',  ( 5.790102700048295858, -0.9971039342967463748, 1.968745932239771568 ) ) ;
#117787=CARTESIAN_POINT ( 'NONE',  ( 4.289322773248661846, -0.004189350761124934451, -2.019972750201783906 ) ) ;
#117789=CARTESIAN_POINT ( 'NONE',  ( 5.237907724141787291, 2.013986247903374327, -0.1017665992488273330 ) ) ;
#117791=CARTESIAN_POINT ( 'NONE',  ( 2.166681600665042229, -1.709288833360942617, -0.7604731621856930524 ) ) ;
#117793=CARTESIAN_POINT ( 'NONE',  ( 1.687617486097678476, 1.829050272730630144, -0.5582976189952293389 ) ) ;
#117798=CARTESIAN_POINT ( 'NONE',  ( -0.05268457437105151381, -1.747710896673961400, 0.7768168958157273263 ) ) ;
#117800=CARTESIAN_POINT ( 'NONE',  ( 2.224987305166142626, -1.792472147789250236, -0.7979012372742313453 ) ) ;
#117803=CARTESIAN_POINT ( 'NONE',  ( 5.256147377898004791, 0.8573370980917978113, -1.939729252509444279 ) ) ;
#117805=CARTESIAN_POINT ( 'NONE',  ( 6.620655732516647518, 0.007553340620044743381, 1.826407896915738238 ) ) ;
#117807=CARTESIAN_POINT ( 'NONE',  ( 6.696557531595894730, -0.5234078932761144776, -1.900562160593147754 ) ) ;
#117809=CARTESIAN_POINT ( 'NONE',  ( 1.617441171277278711, 1.676116182522195519, 1.114898189108826543 ) ) ;
#117812=CARTESIAN_POINT ( 'NONE',  ( 0.9665973488726641305, -2.066607521123296376, -0.4595904307344770290 ) ) ;
#117814=CARTESIAN_POINT ( 'NONE',  ( 3.121598655985452275, 0.3063859900464052100, -2.047459029603612368 ) ) ;
#117818=CARTESIAN_POINT ( 'NONE',  ( 5.085920031106448747, -2.074780370831377230, -0.2563659892118006489 ) ) ;
#117820=CARTESIAN_POINT ( 'NONE',  ( 3.012524388372894713, 1.323457619556423381, -1.257707024427484388 ) ) ;
#117821=CARTESIAN_POINT ( 'NONE',  ( 3.193826918316445163, 1.151326796633693084, 1.398496967315324246 ) ) ;
#117823=CARTESIAN_POINT ( 'NONE',  ( 6.551417122825020201, -1.769646310455679217, -1.318412661681533260 ) ) ;
#117824=CARTESIAN_POINT ( 'NONE',  ( 6.890000000000000568, 2.439643239904603966, 2.382311923195524095 ) ) ;
#117826=CARTESIAN_POINT ( 'NONE',  ( 5.157340341976529352, -1.861842412690998039, -1.184373046124863160 ) ) ;
#117828=CARTESIAN_POINT ( 'NONE',  ( 4.231050068913538631, 1.749697241329374098, 0.7720063087622434095 ) ) ;
#117838=CARTESIAN_POINT ( 'NONE',  ( 3.743291833738107144, -1.414529149469236691, -1.224010458943748603 ) ) ;
#117840=CARTESIAN_POINT ( 'NONE',  ( -0.2409995289980003397, 2.873648158547074338, -2.488896373646624749 ) ) ;
#117842=CARTESIAN_POINT ( 'NONE',  ( 0.1934256698341470238, 1.783621342183003389, -0.6902995980747894667 ) ) ;
#117844=CARTESIAN_POINT ( 'NONE',  ( 0.5671661303022774714, 1.710823773062917219, 0.9755123711343968163 ) ) ;
#117845=CARTESIAN_POINT ( 'NONE',  ( 2.724232643812212196, 2.001515029240468646, 0.2440086781289458329 ) ) ;
#117848=CARTESIAN_POINT ( 'NONE',  ( 2.431793384409334902, 1.031818167245980744, -1.933333044699904857 ) ) ;
#117849=CARTESIAN_POINT ( 'NONE',  ( 6.217409598193539999, -0.2183660865492654257, 1.812524795094340835 ) ) ;
#117857=CARTESIAN_POINT ( 'NONE',  ( 3.895923546780861724, -0.5813109859279729230, -1.747131793041277970 ) ) ;
#117858=CARTESIAN_POINT ( 'NONE',  ( 0.3639315877056762405, 0.6293089562653730873, -1.912281478549708202 ) ) ;
#117859=CARTESIAN_POINT ( 'NONE',  ( 3.234050759648151363, -2.122446487128562875, -0.8823414489649589187 ) ) ;
#117861=CARTESIAN_POINT ( 'NONE',  ( 0.5493571781046421298, 1.373546829346812714, 1.255761559867879962 ) ) ;
#117865=CARTESIAN_POINT ( 'NONE',  ( 5.009976098083095408, -0.6827417919906975108, 1.786564173047608062 ) ) ;
#117869=CARTESIAN_POINT ( 'NONE',  ( 4.107036007299074143, -0.3554739980045698022, 2.060130632118581051 ) ) ;
#117870=CARTESIAN_POINT ( 'NONE',  ( 1.990876257202532695, 1.628914321797021669, -0.9196232060951770038 ) ) ;
#117873=CARTESIAN_POINT ( 'NONE',  ( 3.526658842500699720, -1.606625690567566656, 0.6697392890405767796 ) ) ;
#117877=CARTESIAN_POINT ( 'NONE',  ( 4.476996172482918368, -0.003761094005936410634, -1.725068444937064349 ) ) ;
#117879=CARTESIAN_POINT ( 'NONE',  ( 6.076841795016812320, -2.094286673724785164, -0.6961510500591641115 ) ) ;
#117881=CARTESIAN_POINT ( 'NONE',  ( 3.731445244768144764, 0.05858319805804703545, -2.170454240781857003 ) ) ;
#117882=CARTESIAN_POINT ( 'NONE',  ( 1.875362892791394787, 1.747422460009705913, -0.5287960245906262458 ) ) ;
#117884=CARTESIAN_POINT ( 'NONE',  ( 6.104719058799578768, 1.976458628850938704, 0.7599229572291065216 ) ) ;
#117886=CARTESIAN_POINT ( 'NONE',  ( 6.058190142838977721, -1.623990863767441617, 1.618158029567408729 ) ) ;
#117890=CARTESIAN_POINT ( 'NONE',  ( 1.559403367407938390, -1.789607135292633266, 1.137164086494051096 ) ) ;
#117896=CARTESIAN_POINT ( 'NONE',  ( 0.8037664367953377687, 1.956346004370253633, -1.052120880887427390 ) ) ;
#117898=CARTESIAN_POINT ( 'NONE',  ( 0.08910568399025410591, -0.6041685166103001325, 2.217849651370594088 ) ) ;
#117900=CARTESIAN_POINT ( 'NONE',  ( 4.926661567281545473, -1.351126562560464484, 1.558462338037209349 ) ) ;
#117906=CARTESIAN_POINT ( 'NONE',  ( 1.043050037176814326, -1.649054093272810606, -1.284947313888247900 ) ) ;
#117907=CARTESIAN_POINT ( 'NONE',  ( 4.817029820108094995, 1.034167108704350024, -1.730865207599366240 ) ) ;
#117908=CARTESIAN_POINT ( 'NONE',  ( 3.878315922200573862, -0.1843894689829879696, -1.832007427040844183 ) ) ;
#117909=EDGE_CURVE ( 'NONE', #141519, #102469, #119206, .T. ) ;
#117912=CARTESIAN_POINT ( 'NONE',  ( 0.6919144707170435948, -1.710882258413017221, -0.2179282654613586834 ) ) ;
#117913=CARTESIAN_POINT ( 'NONE',  ( -0.1355283706049141557, -1.957205112593700003, -0.4852584411360050254 ) ) ;
#117915=CARTESIAN_POINT ( 'NONE',  ( 1.159873712335700802, 0.4409813497070895760, -2.218855480106549649 ) ) ;
#117916=CARTESIAN_POINT ( 'NONE',  ( 2.895255201988570892, 1.806112693971681615, -1.083030686944158161 ) ) ;
#117920=CARTESIAN_POINT ( 'NONE',  ( 0.000000000000000000, 0.4651705836652164638, -2.021763587583139010 ) ) ;
#117925=CARTESIAN_POINT ( 'NONE',  ( 5.642908736356011978, 2.140874091242400912, 0.5926086046802480078 ) ) ;
#117926=CARTESIAN_POINT ( 'NONE',  ( 3.170069416559752273, -1.305109287949431929, 1.760291797049506446 ) ) ;
#117929=CARTESIAN_POINT ( 'NONE',  ( 6.004347769543215030, 1.959566550440184907, 0.09775035808561728656 ) ) ;
#117931=CARTESIAN_POINT ( 'NONE',  ( 6.610000000000009202, 6.036727194997777879, 2.594899704271665275 ) ) ;
#117933=CARTESIAN_POINT ( 'NONE',  ( 4.658503719480325600, 2.115088938745744329, 0.1532479335744421078 ) ) ;
#117937=CARTESIAN_POINT ( 'NONE',  ( 6.104392421991035711, -0.7735064434604683736, -2.018760209060527888 ) ) ;
#117939=CARTESIAN_POINT ( 'NONE',  ( 5.653808312887881549, 0.7519890275384639722, 1.680886247995525773 ) ) ;
#117942=CARTESIAN_POINT ( 'NONE',  ( 1.311604768886602157, 1.169564267535606605, -1.289085965974474668 ) ) ;
#117946=CARTESIAN_POINT ( 'NONE',  ( 5.577088068215094729, -0.04877400797019536272, -2.161318155665878038 ) ) ;
#117949=CARTESIAN_POINT ( 'NONE',  ( 4.170900312159072421, -2.016029151617684256, -0.7805680927704603533 ) ) ;
#117951=CARTESIAN_POINT ( 'NONE',  ( 6.468046296993485988, 1.011472520757991767, 1.691939633080985272 ) ) ;
#117952=CARTESIAN_POINT ( 'NONE',  ( 4.551880008920849541, 1.548817843433186736, -0.7794160303473545159 ) ) ;
#117953=CARTESIAN_POINT ( 'NONE',  ( 1.751786407749492014, 2.185395279939935431, -0.1653414253460702699 ) ) ;
#117954=CARTESIAN_POINT ( 'NONE',  ( 2.696638560983040112, -2.301352489519994382, -0.1704845361689636130 ) ) ;
#117955=CARTESIAN_POINT ( 'NONE',  ( 4.973930670403752252, 1.183205397963146499, 1.687068388967316368 ) ) ;
#117956=CARTESIAN_POINT ( 'NONE',  ( 0.1638716437233995460, -1.269140265717118465, 1.469938112931449270 ) ) ;
#117962=CARTESIAN_POINT ( 'NONE',  ( 1.723279953462612202, 1.994870059565261755, 0.2930690452552578429 ) ) ;
#117964=CARTESIAN_POINT ( 'NONE',  ( 2.925073249431627165, 2.077443920948469192, 0.7446974470129495982 ) ) ;
#117966=CARTESIAN_POINT ( 'NONE',  ( 1.375590602687895458, -1.817075280682054927, 0.4009801126106312674 ) ) ;
#117968=CARTESIAN_POINT ( 'NONE',  ( 0.1399997263885794929, 4.089933038008564559, -2.554595152914000078 ) ) ;
#117972=CARTESIAN_POINT ( 'NONE',  ( 6.825078400183544503, 3.684911640780349718, 2.658296617506946458 ) ) ;
#117975=CARTESIAN_POINT ( 'NONE',  ( 3.889569955515647326, 1.491445920024776051, 1.422513881352378107 ) ) ;
#117978=UNCERTAINTY_MEASURE_WITH_UNIT (LENGTH_MEASURE( 1.000000000000000082E-05 ), #194247, 'distance_accuracy_value', 'NONE');
#117980=CARTESIAN_POINT ( 'NONE',  ( 1.822921661270057836, 1.494980448624585234, -1.358156064218164927 ) ) ;
#117983=CARTESIAN_POINT ( 'NONE',  ( 2.395450018592326646, 1.592181132671898869, 1.308497088967359723 ) ) ;
#117987=CARTESIAN_POINT ( 'NONE',  ( -0.1408020194049964258, 1.331054986036240173, -2.350941690117592575 ) ) ;
#117988=CARTESIAN_POINT ( 'NONE',  ( 5.145248760827346501, -1.894204247122273088, 1.132176536499051700 ) ) ;
#117990=CARTESIAN_POINT ( 'NONE',  ( 1.106953007505812492, 1.637591863572019690, -1.411084338363017832 ) ) ;
#117992=CARTESIAN_POINT ( 'NONE',  ( 1.639861632979456418, 2.010800986640928656, -0.1531718788195315928 ) ) ;
#117994=CARTESIAN_POINT ( 'NONE',  ( 0.4791068267422092797, 1.747065859276742072, -0.6691465683838908607 ) ) ;
#117998=CARTESIAN_POINT ( 'NONE',  ( 2.412791964582483129, 1.669947582624079274, 0.8431454209596804805 ) ) ;
#117999=CARTESIAN_POINT ( 'NONE',  ( 3.889861467948489082, -2.010801299972611478, 0.1531677096566556595 ) ) ;
#118004=CARTESIAN_POINT ( 'NONE',  ( 5.531892221078217098, -1.335191642697653336, -1.628727054747380887 ) ) ;
#118007=CARTESIAN_POINT ( 'NONE',  ( 6.639320575229286092, 2.965970653406803770, 2.456291990408800086 ) ) ;
#118008=CARTESIAN_POINT ( 'NONE',  ( 5.150651408520660723, 1.990593866887302221, 0.3411176234145337216 ) ) ;
#118010=CARTESIAN_POINT ( 'NONE',  ( 0.4442778734073973279, -0.9756673871180139290, 1.817250197203540640 ) ) ;
#118018=CARTESIAN_POINT ( 'NONE',  ( 3.508415132820621007, 2.171350060761201295, 0.003086831990101178078 ) ) ;
#118021=CARTESIAN_POINT ( 'NONE',  ( 3.280630368989821743, 1.663260157205956880, -0.7901080472864712156 ) ) ;
#118023=CARTESIAN_POINT ( 'NONE',  ( 4.036819321710017228, -1.906298169312226953, 1.081085072550565407 ) ) ;
#118025=CARTESIAN_POINT ( 'NONE',  ( 4.856464543430921488, 0.8614301073998543723, 2.092300974686135184 ) ) ;
#118032=CARTESIAN_POINT ( 'NONE',  ( 6.151566388294868126, 0.5118450565497618676, -1.694058711534670358 ) ) ;
#118033=CARTESIAN_POINT ( 'NONE',  ( 4.336591701909254581, 1.236597081578957757, -1.588450131361287987 ) ) ;
#118035=CARTESIAN_POINT ( 'NONE',  ( 2.766744854014174138, -1.453255750356880371, 1.524405782528108766 ) ) ;
#118036=CARTESIAN_POINT ( 'NONE',  ( 0.8080361750046762825, 1.140156559909396128, -1.539198610912548171 ) ) ;
#118039=CARTESIAN_POINT ( 'NONE',  ( 2.066797411385603578, 1.461431172244957333, -1.320572070109968799 ) ) ;
#118040=CARTESIAN_POINT ( 'NONE',  ( 4.922131295886445379, -2.009687048479208205, 0.2019785858936548328 ) ) ;
#118041=CARTESIAN_POINT ( 'NONE',  ( 1.024039198018782626, 1.117340804906666873, -1.500143343703803422 ) ) ;
#118042=CARTESIAN_POINT ( 'NONE',  ( 1.328483007144948935, -1.247240240105648601, 1.514344512384787622 ) ) ;
#118043=CARTESIAN_POINT ( 'NONE',  ( 0.4043728756845180183, -1.898191424145349471, -0.2318213773434482650 ) ) ;
#118048=CARTESIAN_POINT ( 'NONE',  ( 5.875831987524620992, 1.115552982110395330, 1.501486808359139946 ) ) ;
#118051=CARTESIAN_POINT ( 'NONE',  ( 5.823117640241993520, -1.869163851432435575, -0.8903994044791310181 ) ) ;
#118054=CARTESIAN_POINT ( 'NONE',  ( 0.07661050522433658638, 0.008287133257128469904, -1.710863442170394988 ) ) ;
#118061=CARTESIAN_POINT ( 'NONE',  ( 5.160583804383015227, -0.6592509027269661814, -1.847929681152965520 ) ) ;
#118063=CARTESIAN_POINT ( 'NONE',  ( 2.653672528425448540, -0.3418824089525332455, -1.986742401007553172 ) ) ;
#118064=CARTESIAN_POINT ( 'NONE',  ( 2.817496537900533671, -1.290266535947793392, -1.416188432289398058 ) ) ;
#118066=CARTESIAN_POINT ( 'NONE',  ( 0.6971427418834205136, 1.794861059153027627, 1.257291590721874686 ) ) ;
#118068=CARTESIAN_POINT ( 'NONE',  ( 3.145614842782416432, 0.6765965015090926737, -1.744060075730607950 ) ) ;
#118072=CARTESIAN_POINT ( 'NONE',  ( 3.937202496034042376, -1.761399977300786901, -1.174509457245224597 ) ) ;
#118074=CARTESIAN_POINT ( 'NONE',  ( 5.529760519541640384, 1.996289034380031913, -0.5486624943154896350 ) ) ;
#118075=CARTESIAN_POINT ( 'NONE',  ( 1.751626234865871767, 2.084932195785852649, -0.1569159079413025293 ) ) ;
#118077=CARTESIAN_POINT ( 'NONE',  ( 0.8324923845523107824, 0.1201152365052655241, 1.720655618271366150 ) ) ;
#118087=CARTESIAN_POINT ( 'NONE',  ( 0.2229362713279548491, 1.575107908988721883, 0.8944890650159162959 ) ) ;
#118099=CARTESIAN_POINT ( 'NONE',  ( 5.835564593388589572, 0.5826401998472263699, -1.930423629703325927 ) ) ;
#118105=CARTESIAN_POINT ( 'NONE',  ( 3.643367292660666390, 1.782436080146361013, -0.8378801856493125477 ) ) ;
#118106=CARTESIAN_POINT ( 'NONE',  ( 0.9793288802587530872, -1.918618388578940737, -0.9032494106611320683 ) ) ;
#118109=CARTESIAN_POINT ( 'NONE',  ( 6.727182134110194056, 3.682851444631680682, 2.702965647100654234 ) ) ;
#118110=CARTESIAN_POINT ( 'NONE',  ( 6.439412520197737244, 0.8424478218750917069, -2.023249321508275855 ) ) ;
#118112=CARTESIAN_POINT ( 'NONE',  ( 4.366181854897908998, 0.9076448143166337967, 1.699152538019559788 ) ) ;
#118114=CARTESIAN_POINT ( 'NONE',  ( -0.02988540731099689068, 4.098597030192621560, -2.281328281275496916 ) ) ;
#118115=CARTESIAN_POINT ( 'NONE',  ( 0.8036966383840878914, 1.806304194667744500, 1.267646993260997945 ) ) ;
#118117=ORIENTED_EDGE ( 'NONE', *, *, #66399, .T. ) ;
#118119=CARTESIAN_POINT ( 'NONE',  ( 6.754754220498722539, -0.5220956727660872598, -1.898933868174660589 ) ) ;
#118120=CARTESIAN_POINT ( 'NONE',  ( 0.5912263705248020917, -0.6977439394254668636, 1.812568619595144925 ) ) ;
#118121=CARTESIAN_POINT ( 'NONE',  ( 6.292345239091892140, -2.167472901860421519, 0.7650227848022586041 ) ) ;
#118123=CARTESIAN_POINT ( 'NONE',  ( 4.346440162718026912, -1.840208154270198015, -0.2762933559420696072 ) ) ;
#118129=CARTESIAN_POINT ( 'NONE',  ( 6.603094310190187777, -0.4545541770063685760, 2.048106021177148683 ) ) ;
#118134=CARTESIAN_POINT ( 'NONE',  ( 0.7151340513122245168, -0.2707656271505008982, 1.805370379145049275 ) ) ;
#118136=CARTESIAN_POINT ( 'NONE',  ( 3.111645937125429029, 0.04567828748044086562, 1.733733899787115229 ) ) ;
#118138=CARTESIAN_POINT ( 'NONE',  ( 6.509000000000010999, 0.004788705324892603143, 2.000274819378269786 ) ) ;
#118140=CARTESIAN_POINT ( 'NONE',  ( 6.481070005604858686, -0.09514881109910081070, -1.823337098959529001 ) ) ;
#118141=CARTESIAN_POINT ( 'NONE',  ( 2.869914117416060062, -1.941089286637355693, 0.2830422620509198128 ) ) ;
#118145=CARTESIAN_POINT ( 'NONE',  ( 5.303433364654348559, 1.869980213031800398, -0.9998494819224086338 ) ) ;
#118149=CARTESIAN_POINT ( 'NONE',  ( 2.852461952307944415, -2.064405766265942521, -0.1567919417525542591 ) ) ;
#118152=CARTESIAN_POINT ( 'NONE',  ( 5.004621511133813705, -2.204373672735039147, -0.2730638322096557435 ) ) ;
#118154=CARTESIAN_POINT ( 'NONE',  ( 3.077065830326791929, -0.9295426453954873658, 2.102514275539566935 ) ) ;
#118161=CARTESIAN_POINT ( 'NONE',  ( 3.849791259674230748, -1.322437695595569673, -1.381667681676468140 ) ) ;
#118163=CARTESIAN_POINT ( 'NONE',  ( 4.102375631063598149, -0.5418327121037533889, -1.637530703111476305 ) ) ;
#118164=CARTESIAN_POINT ( 'NONE',  ( 3.872279980006509970, -1.995268062538615883, -0.2910826752766728642 ) ) ;
#118165=CARTESIAN_POINT ( 'NONE',  ( 4.219567396149206395, 2.254377101126247229, 0.4485144814023647730 ) ) ;
#118167=CARTESIAN_POINT ( 'NONE',  ( 6.358053323650514344, 2.100580423050825818, -0.1529390103112079069 ) ) ;
#118170=CARTESIAN_POINT ( 'NONE',  ( 5.202326708214688900, -0.5966268589385533838, -1.666288158821194187 ) ) ;
#118172=CARTESIAN_POINT ( 'NONE',  ( 0.4458144982435990888, 0.7132466706018144587, -2.178543642160748917 ) ) ;
#118173=CARTESIAN_POINT ( 'NONE',  ( 6.527308116070499544, -1.206667617865687214, -1.390688675169844624 ) ) ;
#118179=CARTESIAN_POINT ( 'NONE',  ( 0.5378411956755309031, 2.025704276806821191, -0.7818309977141599809 ) ) ;
#118180=CARTESIAN_POINT ( 'NONE',  ( 1.516814941429758701, 0.2024661778830244008, 2.006371303556075958 ) ) ;
#118182=CARTESIAN_POINT ( 'NONE',  ( 4.969325399568108814, 0.1871947810346066554, -1.917384544105669386 ) ) ;
#118184=CARTESIAN_POINT ( 'NONE',  ( 2.004415182159818176, -0.9449143528836713157, 2.010537586115124231 ) ) ;
#118192=CARTESIAN_POINT ( 'NONE',  ( 3.931004251652202353, -1.203735069864294571, -1.257276804044287655 ) ) ;
#118193=CARTESIAN_POINT ( 'NONE',  ( 2.119516022818414669, 0.3384452847540948550, -1.932298432780136244 ) ) ;
#118198=CARTESIAN_POINT ( 'NONE',  ( 1.451709319293143396, 1.560653109857246701, 1.348772525646862341 ) ) ;
#118201=CARTESIAN_POINT ( 'NONE',  ( 1.446537619816448572, 2.259995149683653448, 0.1094724083178944679 ) ) ;
#118204=EDGE_CURVE ( 'NONE', #97371, #57833, #99330, .T. ) ;
#118205=CARTESIAN_POINT ( 'NONE',  ( 2.477632765499269141, 1.147360842229189437, 1.477270975257204411 ) ) ;
#118206=CARTESIAN_POINT ( 'NONE',  ( 1.019655691060247227, -1.568448733338474455, 0.7400992899176340734 ) ) ;
#118207=CARTESIAN_POINT ( 'NONE',  ( 5.724229345562060089, 2.111793275502030554, 0.5857118945327836057 ) ) ;
#118208=CARTESIAN_POINT ( 'NONE',  ( 5.175001447075725736, -2.170742607874641461, -0.7831926130325519431 ) ) ;
#118209=CARTESIAN_POINT ( 'NONE',  ( 1.358354339613274675, 0.8343398477911911915, 1.884629720726511692 ) ) ;
#118210=CARTESIAN_POINT ( 'NONE',  ( 3.556523421261322149, -1.712991659986836002, -0.9147756334835445147 ) ) ;
#118212=CARTESIAN_POINT ( 'NONE',  ( 6.186763334926775215, -0.2743023915687745617, -1.850177433978140051 ) ) ;
#118214=CARTESIAN_POINT ( 'NONE',  ( 6.679064532090532857, -0.9478974852125362505, -1.779352858464311016 ) ) ;
#118217=CARTESIAN_POINT ( 'NONE',  ( 4.869767617671093340, -0.2496050341583149201, -2.000857388266870984 ) ) ;
#118221=CARTESIAN_POINT ( 'NONE',  ( 2.139018802738294589, -1.631172329757241801, 0.8201644002571031322 ) ) ;
#118226=ORIENTED_EDGE ( 'NONE', *, *, #205304, .F. ) ;
#118232=CARTESIAN_POINT ( 'NONE',  ( 5.637369771878480762, -0.04735730112789998669, 2.019284605405778255 ) ) ;
#118233=CARTESIAN_POINT ( 'NONE',  ( 0.1004478525090373164, -0.9956121213324088393, 1.872212410442177344 ) ) ;
#118236=CARTESIAN_POINT ( 'NONE',  ( 4.891509840769978190, 1.525608517091806782, 1.385742337522611223 ) ) ;
#118237=CARTESIAN_POINT ( 'NONE',  ( 5.379529795981254914, -0.4926393568372189891, -1.955173248319847845 ) ) ;
#118243=CIRCLE ( 'NONE', #201169, 0.04999999999999969746 ) ;
#118247=CARTESIAN_POINT ( 'NONE',  ( 4.569685373303983944, 1.560260980002409870, -1.276848140101802365 ) ) ;
#118248=CARTESIAN_POINT ( 'NONE',  ( 3.046634964419430158, -1.505538468004435027, -1.059505732788845966 ) ) ;
#118251=CARTESIAN_POINT ( 'NONE',  ( 2.684532350912737009, -1.185368471958246905, 1.979860261248457931 ) ) ;
#118253=CARTESIAN_POINT ( 'NONE',  ( 4.886082254767631916, -1.023713625618065004, 1.903838226609423590 ) ) ;
#118255=CARTESIAN_POINT ( 'NONE',  ( 0.1166052997346351955, -0.09441621361710265947, 1.939868080593883048 ) ) ;
#118258=CARTESIAN_POINT ( 'NONE',  ( 4.012460596634464416, 1.323225596166040186, -1.322536486416127977 ) ) ;
#118262=CARTESIAN_POINT ( 'NONE',  ( 1.506762622594171930, -0.7967928049063888185, -2.058199171410409978 ) ) ;
#118267=CARTESIAN_POINT ( 'NONE',  ( 0.6847650648834556764, -0.2371060910116972453, -1.956967405937762639 ) ) ;
#118268=CARTESIAN_POINT ( 'NONE',  ( 6.287736656369789401, 1.586309881779718323, 1.676255113901073512 ) ) ;
#118269=CARTESIAN_POINT ( 'NONE',  ( 1.697631272820496307, -1.418720726069604865, -1.355276769646639901 ) ) ;
#118270=CARTESIAN_POINT ( 'NONE',  ( 4.082923458916259740, 1.956979318386397715, 0.6515942777399350572 ) ) ;
#118278=CARTESIAN_POINT ( 'NONE',  ( 6.725048307591657171, -1.982231927674932948, -0.8863045971672071088 ) ) ;
#118280=CARTESIAN_POINT ( 'NONE',  ( 6.075717905342373548, -0.9791751913862613010, 1.559117742379905858 ) ) ;
#118283=CARTESIAN_POINT ( 'NONE',  ( 1.071320448993583918, 1.804315561281001123, -0.4931735697189034151 ) ) ;
#118288=CARTESIAN_POINT ( 'NONE',  ( 1.312987857083922627, 1.562780923097413677, -1.101767902142808175 ) ) ;
#118289=CARTESIAN_POINT ( 'NONE',  ( 3.010364070732887143, 1.283045204736869671, -1.219329851163194922 ) ) ;
#118290=CARTESIAN_POINT ( 'NONE',  ( 0.6449871831117168774, 0.1410837285014763798, 1.907147727228817757 ) ) ;
#118292=CARTESIAN_POINT ( 'NONE',  ( 4.692942998425689183, 1.668811738553135804, 0.9403632788237480389 ) ) ;
#118294=CARTESIAN_POINT ( 'NONE',  ( 4.861744415569490663, -0.5273948137594737240, 1.897533870164061831 ) ) ;
#118295=CARTESIAN_POINT ( 'NONE',  ( 1.283610819548046011, 0.1505422781087061845, -2.115291873224629082 ) ) ;
#118297=CARTESIAN_POINT ( 'NONE',  ( 4.416781281874038179, 1.710313510141375115, 0.7581657270378170388 ) ) ;
#118298=CARTESIAN_POINT ( 'NONE',  ( 0.06470675514189982991, -1.629034059718449834, -0.8243793580787887043 ) ) ;
#118300=CARTESIAN_POINT ( 'NONE',  ( 3.774219598512587037, 1.225428716765289749, 1.835190637982798023 ) ) ;
#118303=CARTESIAN_POINT ( 'NONE',  ( 0.4321753131953905980, 1.186194839137414414, 1.687308244272892166 ) ) ;
#118311=CARTESIAN_POINT ( 'NONE',  ( 2.980987059868035693, 1.948563265827065960, 0.6999735360200682877 ) ) ;
#118313=CARTESIAN_POINT ( 'NONE',  ( 1.616726252867954683, 1.452999108549270169, -1.600537328674697779 ) ) ;
#118315=CARTESIAN_POINT ( 'NONE',  ( 0.4518267731568551548, -1.429874679360541023, -1.426642250087527541 ) ) ;
#118318=CARTESIAN_POINT ( 'NONE',  ( 0.1749903794560566661, 7.629137130509112907, -2.555305779167945435 ) ) ;
#118320=CARTESIAN_POINT ( 'NONE',  ( 6.661482485103542572, -0.5350097378542042481, -1.943772860543022230 ) ) ;
#118321=CARTESIAN_POINT ( 'NONE',  ( 5.630082600720735186, 1.913861949906026538, 0.08686293782892740012 ) ) ;
#118322=CARTESIAN_POINT ( 'NONE',  ( 6.539320575229294441, -0.001643797937642132567, 2.203502507913539521 ) ) ;
#118323=CARTESIAN_POINT ( 'NONE',  ( 3.632539538618652752, 0.3231117836275977373, 2.167502126216628522 ) ) ;
#118325=CARTESIAN_POINT ( 'NONE',  ( 3.181800181368432678, 1.864768544494728175, -0.4233684943922080834 ) ) ;
#118330=CARTESIAN_POINT ( 'NONE',  ( 1.054314798682391530, -1.277026470193865171, 1.560515422851154854 ) ) ;
#118332=CARTESIAN_POINT ( 'NONE',  ( -0.04093971525966337566, -2.051586291785143512, -1.022954789973041123 ) ) ;
#118334=CARTESIAN_POINT ( 'NONE',  ( 3.873808679987042147, 0.9582704680195216485, 1.433834079761304281 ) ) ;
#118336=CARTESIAN_POINT ( 'NONE',  ( -0.1399997263889612154, 1.357298622859518078, -2.254419820505838334 ) ) ;
#118341=CARTESIAN_POINT ( 'NONE',  ( 1.609737659951641309, 0.5726723138891121057, -1.876404140693301414 ) ) ;
#118344=CARTESIAN_POINT ( 'NONE',  ( 0.07536363704235825300, -0.001874865094115065866, -2.144269471569634433 ) ) ;
#118347=CARTESIAN_POINT ( 'NONE',  ( 4.143061475816012695, 0.09292765117045087564, 1.809223169447377710 ) ) ;
#118351=CARTESIAN_POINT ( 'NONE',  ( 5.479120714502029976, -1.640381486070506156, -0.7687909062009666838 ) ) ;
#118356=CARTESIAN_POINT ( 'NONE',  ( 5.705462897529653965, -1.467230705000615032, -1.144726319735862585 ) ) ;
#118358=CARTESIAN_POINT ( 'NONE',  ( 3.251485182540703622, 1.868192404686802810, -0.4227579483004426653 ) ) ;
#118364=CARTESIAN_POINT ( 'NONE',  ( 1.077287230265553175, -0.05381693868444263618, -2.161191418701657430 ) ) ;
#118368=CARTESIAN_POINT ( 'NONE',  ( 0.6920833903016985200, -1.811158644599793810, -0.2285449354127722099 ) ) ;
#118370=CARTESIAN_POINT ( 'NONE',  ( 3.223480179809079971, -1.759765543241718966, 0.4855387900214308550 ) ) ;
#118372=CARTESIAN_POINT ( 'NONE',  ( 2.144650067465687648, 1.855875215511919363, 0.4610605321611755958 ) ) ;
#118373=CARTESIAN_POINT ( 'NONE',  ( 3.262113425008953183, -1.967426182293503079, 0.09390151542597660606 ) ) ;
#118374=CARTESIAN_POINT ( 'NONE',  ( 3.456523497251274168, -1.714022962016878759, -0.9130526778427237033 ) ) ;
#118377=CARTESIAN_POINT ( 'NONE',  ( 4.148766697842418694, 2.080301416381886703, 0.4105806053946169376 ) ) ;
#118386=CARTESIAN_POINT ( 'NONE',  ( 3.879382553896340013, 1.718498013671100777, -0.6167319420108534622 ) ) ;
#118392=CARTESIAN_POINT ( 'NONE',  ( 4.803500792215161574, -0.4985019455652460740, 1.802925825644098534 ) ) ;
#118394=AXIS2_PLACEMENT_3D ( 'NONE', #71649, #203783, #188622 ) ;
#118395=CARTESIAN_POINT ( 'NONE',  ( 3.457566480858861091, 0.4672022665876771619, -1.868877010067309330 ) ) ;
#118403=CARTESIAN_POINT ( 'NONE',  ( 1.019337291899083064, -1.912195925978699140, 0.9092529662874779817 ) ) ;
#118407=CARTESIAN_POINT ( 'NONE',  ( 6.702015291077846548, 0.7979701500827086624, -1.910492173269620508 ) ) ;
#118408=CARTESIAN_POINT ( 'NONE',  ( 1.575478407343299692, -0.9843019613302635973, 1.555867251595323353 ) ) ;
#118411=CARTESIAN_POINT ( 'NONE',  ( 0.1464030204712711281, -0.1495716826577230818, -2.263613701224455710 ) ) ;
#118415=CARTESIAN_POINT ( 'NONE',  ( 1.060933235008169051, -2.074266264760935563, -0.9759354127518887756 ) ) ;
#118416=EDGE_CURVE ( 'NONE', #167392, #103946, #73617, .T. ) ;
#118417=CARTESIAN_POINT ( 'NONE',  ( 5.841732304440537149, 1.939831336911639781, 0.09320031894976579800 ) ) ;
#118421=CARTESIAN_POINT ( 'NONE',  ( 0.6506401683969212923, 1.984111478139438667, 0.3401018483101604928 ) ) ;
#118426=CARTESIAN_POINT ( 'NONE',  ( 4.382818795122591204, 1.867623683829922054, -0.9396962251831328938 ) ) ;
#118427=CARTESIAN_POINT ( 'NONE',  ( 2.746659024021454787, -1.472625519509669134, 0.9813492100937453166 ) ) ;
#118430=CARTESIAN_POINT ( 'NONE',  ( 4.892671604017262865, 1.907728271999886704, -1.270570218630202808 ) ) ;
#118431=CARTESIAN_POINT ( 'NONE',  ( 3.855166295008194410, 1.726882014201753801, -0.2153026951989250037 ) ) ;
#118435=CARTESIAN_POINT ( 'NONE',  ( 3.180671111220879865, -0.8518272437034493105, -1.510038686645834183 ) ) ;
#118436=CARTESIAN_POINT ( 'NONE',  ( 3.824824921856139870, -1.460638251479762229, 1.606552252625459420 ) ) ;
#118438=CARTESIAN_POINT ( 'NONE',  ( 4.241422899474024177, 0.4370803545316758743, -1.968444674787086512 ) ) ;
#118439=CARTESIAN_POINT ( 'NONE',  ( 1.343750000000001110, 1.895863743164117654, 0.7852924748299160429 ) ) ;
#118441=CARTESIAN_POINT ( 'NONE',  ( 1.940333228260374021, 1.905070304733847752, 0.2851023952017122665 ) ) ;
#118443=CARTESIAN_POINT ( 'NONE',  ( 6.029551324705815674, -0.2728526602329122142, 2.204496564233568989 ) ) ;
#118445=CARTESIAN_POINT ( 'NONE',  ( -0.2106854629475244378, 7.629137130509075604, -2.597154134060948749 ) ) ;
#118450=CARTESIAN_POINT ( 'NONE',  ( 1.137687779795238052, -0.04954009815814026940, 2.220905934856795216 ) ) ;
#118451=CARTESIAN_POINT ( 'NONE',  ( 5.898874287966751950, 0.3812104124719677412, 1.924297140916144455 ) ) ;
#118454=CARTESIAN_POINT ( 'NONE',  ( 6.468092748254181679, 1.154776641680499205, 1.945382213218769252 ) ) ;
#118458=CARTESIAN_POINT ( 'NONE',  ( 4.510253362402360189, 2.062282729996979924, -0.04753222776765659435 ) ) ;
#118462=CARTESIAN_POINT ( 'NONE',  ( 5.817618194842751222, -1.825074353437942554, 0.4092329068215995180 ) ) ;
#118463=CARTESIAN_POINT ( 'NONE',  ( 5.010307813345768579, -1.644221866518974728, 0.5513857468827707553 ) ) ;
#118464=CARTESIAN_POINT ( 'NONE',  ( 3.315673178333057969, 1.101538733106369072, -1.347505558334564535 ) ) ;
#118466=CARTESIAN_POINT ( 'NONE',  ( 1.611265326866499148, -0.2753845699034764838, 2.275703152891339176 ) ) ;
#118468=CARTESIAN_POINT ( 'NONE',  ( 6.181206942494069878, 1.442326931096184151, 1.513799708994074900 ) ) ;
#118469=CARTESIAN_POINT ( 'NONE',  ( 0.5679803739370090643, -1.732728882149033645, -0.6228371021387222317 ) ) ;
#118472=CARTESIAN_POINT ( 'NONE',  ( 2.145157927413956944, 0.8647252629472859109, 1.821741647932619390 ) ) ;
#118473=CARTESIAN_POINT ( 'NONE',  ( 0.006183538434290089709, -0.9405624870862171472, -1.977291442860461768 ) ) ;
#118477=CARTESIAN_POINT ( 'NONE',  ( 2.860144583491229131, 0.7611018733697445526, -1.979373954265637892 ) ) ;
#118479=CARTESIAN_POINT ( 'NONE',  ( 5.320859459983126705, 1.688362619374352613, 0.6951667914897319278 ) ) ;
#118486=CARTESIAN_POINT ( 'NONE',  ( 2.004171506046021012, -0.8596719693435939114, 1.827822491074476918 ) ) ;
#118487=CARTESIAN_POINT ( 'NONE',  ( 0.2531349071235571846, -1.691105571228457505, 1.254881668439677966 ) ) ;
#118490=CARTESIAN_POINT ( 'NONE',  ( 4.012436097835626825, 0.6663421089948203813, 1.737758261286206807 ) ) ;
#118500=CARTESIAN_POINT ( 'NONE',  ( 2.196291916443537939, -1.129096229514385819, -1.315908775350557169 ) ) ;
#118501=CARTESIAN_POINT ( 'NONE',  ( 1.622608716997505418, -1.639457832600412113, 0.5842430463761526527 ) ) ;
#118502=CARTESIAN_POINT ( 'NONE',  ( 5.848310222665911162, 2.304730150483401463, 0.1192407711079427196 ) ) ;
#118505=CARTESIAN_POINT ( 'NONE',  ( 1.546242023939500276, 2.058303352229321703, 0.1039559743286587457 ) ) ;
#118506=CARTESIAN_POINT ( 'NONE',  ( 6.819654193105592732, -1.783474119298094296, 1.449237643660877151 ) ) ;
#118509=CARTESIAN_POINT ( 'NONE',  ( 0.5671783758751040017, 0.1957704533250003986, -1.961731083161978306 ) ) ;
#118510=CARTESIAN_POINT ( 'NONE',  ( 3.691585721427274258, 1.799035686688513325, -0.6489376663148455071 ) ) ;
#118512=CARTESIAN_POINT ( 'NONE',  ( 6.709632191794143274, -0.4886956906769434061, 2.160084693451309601 ) ) ;
#118517=CARTESIAN_POINT ( 'NONE',  ( 6.340501840829311675, 1.221348521443364366, -1.733245716811770309 ) ) ;
#118519=CARTESIAN_POINT ( 'NONE',  ( 3.610674682972123684, -0.9327887667434494601, -2.110822472020437601 ) ) ;
#118520=CARTESIAN_POINT ( 'NONE',  ( 4.351973852746993110, -0.7528527933186466292, 1.811862133468461922 ) ) ;
#118521=CARTESIAN_POINT ( 'NONE',  ( 1.129655866247070595, 1.892139549451707037, -0.5178372573612434193 ) ) ;
#118524=CARTESIAN_POINT ( 'NONE',  ( 6.403528931544730796, -1.954801056786956259, 0.4946215565981848528 ) ) ;
#118527=CARTESIAN_POINT ( 'NONE',  ( 0.2339851986729903077, 0.3116528534230639247, 1.814411239467295101 ) ) ;
#118528=CARTESIAN_POINT ( 'NONE',  ( 2.624086282063769815, 2.129961278301984784, -0.4196836606994054364 ) ) ;
#118530=CARTESIAN_POINT ( 'NONE',  ( 1.107859837811319581, 1.609452232531217275, 1.380942675281403353 ) ) ;
#118535=CARTESIAN_POINT ( 'NONE',  ( 2.073578556082512403, 1.972924284924733929, -0.5953725496260859895 ) ) ;
#118541=ORIENTED_EDGE ( 'NONE', *, *, #90321, .T. ) ;
#118542=CARTESIAN_POINT ( 'NONE',  ( 4.617770051018644573, -0.5065499601877522240, 1.843912185298258066 ) ) ;
#118544=CARTESIAN_POINT ( 'NONE',  ( -0.02968770228139894218, 7.629137130509075604, -2.426318643530885222 ) ) ;
#118545=CARTESIAN_POINT ( 'NONE',  ( 1.019259390987249603, 2.090591978351970859, 0.8652678750288608223 ) ) ;
#118547=CARTESIAN_POINT ( 'NONE',  ( 1.863241329703895888, -1.456548260382009685, -1.076974786960547048 ) ) ;
#118548=CARTESIAN_POINT ( 'NONE',  ( 0.3388992355649001476, -1.619940322034026270, -1.022281207937189684 ) ) ;
#118549=CARTESIAN_POINT ( 'NONE',  ( 1.469279758060073160, 1.824989553406907383, 0.9776941847434923449 ) ) ;
#118551=CARTESIAN_POINT ( 'NONE',  ( 0.1628737759792201201, -1.759808232078699630, -0.8888803535714930870 ) ) ;
#118552=CARTESIAN_POINT ( 'NONE',  ( 5.566998737003931552, -1.742544991934717125, -0.8218319283359241112 ) ) ;
#118554=CARTESIAN_POINT ( 'NONE',  ( 0.4523713176287887383, 0.7179250195528188438, -2.193251166140824715 ) ) ;
#118557=CARTESIAN_POINT ( 'NONE',  ( 3.930177659428602865, 1.143423634368987196, 1.716560605327678513 ) ) ;
#118562=CARTESIAN_POINT ( 'NONE',  ( 5.667048493276758414, -1.902512422570214357, -0.9033719842039839021 ) ) ;
#118564=CARTESIAN_POINT ( 'NONE',  ( 6.057099581687969803, 1.694805161836069107, -1.188877858866774107 ) ) ;
#118566=CARTESIAN_POINT ( 'NONE',  ( 4.745497693432328745, -1.667575968047749546, -1.375352955852253922 ) ) ;
#118567=CARTESIAN_POINT ( 'NONE',  ( 4.231121231147261241, 1.847467856137770204, 0.8164654241873505747 ) ) ;
#118573=CARTESIAN_POINT ( 'NONE',  ( 4.048064755690682581, 0.9548552675892291175, 1.776167154503265566 ) ) ;
#118579=CARTESIAN_POINT ( 'NONE',  ( 4.095327490859664188, -0.3419149367107060522, 1.987051255384481463 ) ) ;
#118581=CARTESIAN_POINT ( 'NONE',  ( 0.6094340267816320544, -1.717071606940338446, 0.1640370458491739458 ) ) ;
#118587=CARTESIAN_POINT ( 'NONE',  ( 4.991395955090764502, 1.385047395102714685, 1.257364466828891914 ) ) ;
#118588=CARTESIAN_POINT ( 'NONE',  ( 6.258070432960613161, 0.7665029349510013024, -1.861766797742714585 ) ) ;
#118592=CARTESIAN_POINT ( 'NONE',  ( 1.159780049612362030, 1.203373692603469935, 1.617804775344060308 ) ) ;
#118593=CARTESIAN_POINT ( 'NONE',  ( 1.335881098409009704, -1.007921504507871102, -1.505067075931452392 ) ) ;
#118594=EDGE_CURVE ( 'NONE', #176125, #41277, #157206, .T. ) ;
#118596=CARTESIAN_POINT ( 'NONE',  ( 5.946190753372003535, 2.158995856162956084, 0.1107517376499680406 ) ) ;
#118600=CARTESIAN_POINT ( 'NONE',  ( -0.1532965272393977951, -1.712378426511364404, -0.8589627718659180733 ) ) ;
#118603=PLANE ( 'NONE',  #187222 ) ;
#118608=CARTESIAN_POINT ( 'NONE',  ( 3.713887418366210724, -2.130098009959373151, 0.3673708613747132534 ) ) ;
#118612=CARTESIAN_POINT ( 'NONE',  ( 1.037531286769650452, -0.04638328994046451298, 2.120250110247793085 ) ) ;
#118615=CARTESIAN_POINT ( 'NONE',  ( 1.739464312186237871, -1.425129977898047740, -1.362296117697106013 ) ) ;
#118616=CARTESIAN_POINT ( 'NONE',  ( 4.623256175466385010, 1.666654777633369555, 0.9376445158523971646 ) ) ;
#118619=CARTESIAN_POINT ( 'NONE',  ( 5.986760398725940568, 1.897641426698594813, 0.5270043353632068994 ) ) ;
#118620=CARTESIAN_POINT ( 'NONE',  ( 0.1462902992968219407, -1.560392365369901668, 1.155808223090015963 ) ) ;
#118627=CARTESIAN_POINT ( 'NONE',  ( 5.180287844241702189, 0.9460499258955605839, 1.661804969971327761 ) ) ;
#118630=CARTESIAN_POINT ( 'NONE',  ( 3.352369063006555905, 2.207063162671081713, 4.936380160885933677E-05 ) ) ;
#118632=CARTESIAN_POINT ( 'NONE',  ( 2.327434156339613924, -0.0004056629378437063877, 2.206952907597827362 ) ) ;
#118634=CARTESIAN_POINT ( 'NONE',  ( 0.5746843702075511429, -1.384840223850939855, 1.318951758179337741 ) ) ;
#118638=CARTESIAN_POINT ( 'NONE',  ( 3.578635096964689843, 1.315621898185691974, -1.598582974826658010 ) ) ;
#118642=CARTESIAN_POINT ( 'NONE',  ( 0.4269344243218140544, 2.069031678568326704, 0.6260965431626740463 ) ) ;
#118643=CARTESIAN_POINT ( 'NONE',  ( 2.718528139169604341, 2.064530135181973591, 0.7356957861901700646 ) ) ;
#118644=DIRECTION ( 'NONE',  ( 2.949029909160572061E-17, 1.000000000000000000, -8.673600428462391266E-15 ) ) ;
#118649=CARTESIAN_POINT ( 'NONE',  ( 6.258463337875916466, 1.656396116010181219, -0.5134576769376431038 ) ) ;
#118651=CARTESIAN_POINT ( 'NONE',  ( 3.344645782512998267, -2.038826501179476391, -0.3585456059004287765 ) ) ;
#118652=CARTESIAN_POINT ( 'NONE',  ( 4.903976463145187203, -1.133744943205544642, -1.787932202283550875 ) ) ;
#118656=CARTESIAN_POINT ( 'NONE',  ( 2.377736956781382638, -1.911501772163497481, 0.4737601246572603064 ) ) ;
#118657=CARTESIAN_POINT ( 'NONE',  ( 0.9844543725016400293, -1.211084316286781037, 1.480072698922259455 ) ) ;
#118659=CARTESIAN_POINT ( 'NONE',  ( 4.716876218882520178, -0.1156266834452194386, 2.289457304130739779 ) ) ;
#118660=CARTESIAN_POINT ( 'NONE',  ( 2.543341688579534132, -1.352695106659363544, -1.226303905950577144 ) ) ;
#118665=CARTESIAN_POINT ( 'NONE',  ( 4.043230579294037952, 0.1031557717955585846, 2.010702285795034072 ) ) ;
#118666=CARTESIAN_POINT ( 'NONE',  ( 4.364078322825436729, -1.956782558839207375, 0.1401112987177987601 ) ) ;
#118670=CARTESIAN_POINT ( 'NONE',  ( 0.1168898295945815374, -0.09829507837614966104, 2.088553102151818219 ) ) ;
#118671=CARTESIAN_POINT ( 'NONE',  ( 5.365971031753679732, 0.8746336007162245352, 1.538519630229380875 ) ) ;
#118672=FACE_OUTER_BOUND ( 'NONE', #198481, .T. ) ;
#118673=CARTESIAN_POINT ( 'NONE',  ( 2.326364362698669641, 2.126017103801054464, 0.5310240739047759062 ) ) ;
#118674=CARTESIAN_POINT ( 'NONE',  ( 6.228409164912255491, 0.1778687648950585953, 1.731214608917114317 ) ) ;
#118677=CARTESIAN_POINT ( 'NONE',  ( 0.1699431646460221601, -1.131269863993559222, 1.302202208916112269 ) ) ;
#118678=CARTESIAN_POINT ( 'NONE',  ( 0.2049558871960316941, 1.909868400323280424, 1.074723926240577221 ) ) ;
#118679=CARTESIAN_POINT ( 'NONE',  ( 2.438337523484556790, 1.039148161723329578, -1.946916322307743474 ) ) ;
#118681=CARTESIAN_POINT ( 'NONE',  ( 6.865710891575433905, -0.4862813381408522817, 2.124062634707358566 ) ) ;
#118683=CARTESIAN_POINT ( 'NONE',  ( 0.7259617406208430657, 0.8522569803141609723, -1.938411259892757421 ) ) ;
#118686=CARTESIAN_POINT ( 'NONE',  ( 5.948256396973989446, 1.924214498663083139, 0.09423418586224258098 ) ) ;
#118688=CARTESIAN_POINT ( 'NONE',  ( 1.927642574099263983, -1.500803908722462499, -1.732858182149794812 ) ) ;
#118692=CARTESIAN_POINT ( 'NONE',  ( 3.580930751873512285, -1.490882799914891033, 1.646821992171596971 ) ) ;
#118698=CARTESIAN_POINT ( 'NONE',  ( 1.705704151892040832, 1.882474636155605507, 0.7231385473688843879 ) ) ;
#118700=CARTESIAN_POINT ( 'NONE',  ( 1.534110023759263308, 1.225272132802219360, 1.659075958507538973 ) ) ;
#118703=CARTESIAN_POINT ( 'NONE',  ( 4.505938053128990539, -0.9357023767473917619, -1.981784127816770935 ) ) ;
#118704=CARTESIAN_POINT ( 'NONE',  ( 0.7564826839323666174, 1.942540863013635821, -0.5404934282097761944 ) ) ;
#118705=CARTESIAN_POINT ( 'NONE',  ( 1.083273795380396143, -0.8277460070302902206, 1.644747122058511035 ) ) ;
#118706=CARTESIAN_POINT ( 'NONE',  ( 5.232074500395570205, 2.258064205686944437, 0.3942454582816708464 ) ) ;
#118707=CARTESIAN_POINT ( 'NONE',  ( 2.958754162918544761, 0.2696264243384552950, -1.821159755858774654 ) ) ;
#118709=CARTESIAN_POINT ( 'NONE',  ( 4.207882836062684540, -1.820678405428953095, 0.1343838851760314757 ) ) ;
#118710=CARTESIAN_POINT ( 'NONE',  ( 4.764296165657141202, 1.880435471729305030, -0.7283773170061805802 ) ) ;
#118712=CARTESIAN_POINT ( 'NONE',  ( 4.188523121243816760, -2.237390873258153778, -0.3355513299154490592 ) ) ;
#118714=CARTESIAN_POINT ( 'NONE',  ( 6.633818197422741925, -1.372689285068533271, -1.597217228543364564 ) ) ;
#118716=CARTESIAN_POINT ( 'NONE',  ( 3.227070907399377298, -1.911900318415656441, -0.7948586591664741352 ) ) ;
#118721=CARTESIAN_POINT ( 'NONE',  ( 2.139170349095420143, -1.720849962885454110, 0.8662218532024426043 ) ) ;
#118722=UNCERTAINTY_MEASURE_WITH_UNIT (LENGTH_MEASURE( 1.000000000000000082E-05 ), #2030, 'distance_accuracy_value', 'NONE');
#118724=CARTESIAN_POINT ( 'NONE',  ( 6.965690641875434075, -0.4316760948062084990, 1.928339623932231239 ) ) ;
#118729=CARTESIAN_POINT ( 'NONE',  ( 2.127449211838834398, 1.986592753075850037, 0.9941332784057993477 ) ) ;
#118731=CARTESIAN_POINT ( 'NONE',  ( 3.540152450731326450, 0.9484212380423739930, -1.880392733946538719 ) ) ;
#118734=CARTESIAN_POINT ( 'NONE',  ( 0.6954782174160825114, -1.312119466559122927, -1.320074052667360665 ) ) ;
#118739=CARTESIAN_POINT ( 'NONE',  ( 1.406653384705614629, -2.110883996484512970, -0.2024971186788473154 ) ) ;
#118742=CARTESIAN_POINT ( 'NONE',  ( 4.527759979645433752, 1.903474890065796732, -0.4746247275292309609 ) ) ;
#118743=CARTESIAN_POINT ( 'NONE',  ( 3.063507763784904192, 0.3185916186679502715, -2.137983152197140413 ) ) ;
#118744=CARTESIAN_POINT ( 'NONE',  ( 1.382094229771430705, -0.2707140722739818650, -1.821126350552772832 ) ) ;
#118746=DIRECTION ( 'NONE',  ( -3.451266460341926649E-31, -5.200010849845536803E-32, 1.000000000000000000 ) ) ;
#118747=CARTESIAN_POINT ( 'NONE',  ( 4.997892061590047952, -0.5910035050068825901, -1.637047790839076589 ) ) ;
#118751=CARTESIAN_POINT ( 'NONE',  ( 2.202237438260604030, -2.161223104231101644, 0.05255616829508147347 ) ) ;
#118752=CARTESIAN_POINT ( 'NONE',  ( 3.690779688840303496, -1.198677090843719872, -1.620934038430859703 ) ) ;
#118754=CARTESIAN_POINT ( 'NONE',  ( 1.217891636700708435, -2.108894920778502602, 0.4742063263511315796 ) ) ;
#118755=CARTESIAN_POINT ( 'NONE',  ( 2.922686454756417085, 1.855838157306726632, 0.6655703372969791198 ) ) ;
#118756=CARTESIAN_POINT ( 'NONE',  ( 6.509000000000010111, 3.701365531483376881, 2.414445852726577080 ) ) ;
#118757=CARTESIAN_POINT ( 'NONE',  ( 3.895986966309549882, -0.6120611862858457153, -1.843141947886927978 ) ) ;
#118762=CARTESIAN_POINT ( 'NONE',  ( -0.1106856583840878927, 5.722746153615347886, -2.590994828783958592 ) ) ;
#118768=CARTESIAN_POINT ( 'NONE',  ( 0.2181801407958559869, -2.163675782650812618, 0.4331315337846516900 ) ) ;
#118771=CARTESIAN_POINT ( 'NONE',  ( 4.522284091987982535, 0.9210895807079204634, 1.732038000912524689 ) ) ;
#118773=CARTESIAN_POINT ( 'NONE',  ( 2.250625165576759290, 1.976955744075848065, -0.3961026872240576702 ) ) ;
#118775=CARTESIAN_POINT ( 'NONE',  ( 3.169268314845040901, 1.912196763353574358, -0.9095376832224701946 ) ) ;
#118778=CARTESIAN_POINT ( 'NONE',  ( 2.835703941817575124, 1.827261480098177460, 0.2250241719141122809 ) ) ;
#118782=CARTESIAN_POINT ( 'NONE',  ( 4.043311264919998038, 0.1072909356813686182, 2.118029240109862155 ) ) ;
#118786=CARTESIAN_POINT ( 'NONE',  ( 5.870404149471736943, -1.310866377807779593, 1.590078559457400287 ) ) ;
#118787=CARTESIAN_POINT ( 'NONE',  ( 0.8536796107712171233, -0.6749765833247187707, 1.734523287792593571 ) ) ;
#118788=CARTESIAN_POINT ( 'NONE',  ( 2.190726087351921425, 1.424366561657765207, 1.166803476217087576 ) ) ;
#118793=CARTESIAN_POINT ( 'NONE',  ( 1.981372325807278623, -0.1102420082176903682, -2.204251428397439483 ) ) ;
#118794=CARTESIAN_POINT ( 'NONE',  ( 4.780719109985231974, -2.192918799143634079, -0.5559354454096259168 ) ) ;
#118796=CARTESIAN_POINT ( 'NONE',  ( 5.168131652730963310, 1.809155975298855523, -0.09671077906142805380 ) ) ;
#118797=CARTESIAN_POINT ( 'NONE',  ( 4.311684426593565433, -1.183387839401760511, -1.506387502079686191 ) ) ;
#118798=ADVANCED_FACE ( 'NONE', ( #114937 ), #1072, .F. ) ;
#118800=CARTESIAN_POINT ( 'NONE',  ( 3.854335392261270421, 0.7083531993744094368, 1.839989435513892380 ) ) ;
#118801=CARTESIAN_POINT ( 'NONE',  ( 4.961713530105988923, 1.850188064717460223, -0.2750520410098392654 ) ) ;
#118803=CARTESIAN_POINT ( 'NONE',  ( 4.791365544089026152, -1.701862485369805000, 0.7535167838805619800 ) ) ;
#118805=CARTESIAN_POINT ( 'NONE',  ( 0.5851731681005939434, 1.651346252830317551, 1.157095189655330314 ) ) ;
#118806=( BOUNDED_CURVE ( )  B_SPLINE_CURVE ( 3, ( #30570, #98762, #180012, #80371 ),
 .UNSPECIFIED., .F., .T. ) 
 B_SPLINE_CURVE_WITH_KNOTS ( ( 4, 4 ),
 ( 0.000000000000000000, 0.5000000000000018874 ),
 .UNSPECIFIED. ) 
 CURVE ( )  GEOMETRIC_REPRESENTATION_ITEM ( )  RATIONAL_B_SPLINE_CURVE ( ( 1.000000000000000000, 0.3333333333333308723, 0.3333333333333333703, 1.000000000000002442 ) ) 
 REPRESENTATION_ITEM ( '' )  );
#118808=CARTESIAN_POINT ( 'NONE',  ( 1.858176280533967661, 2.100347624109857758, -0.1560452747076390423 ) ) ;
#118813=CARTESIAN_POINT ( 'NONE',  ( 2.338154391725711267, -1.166417678377267064, -1.648725491961404055 ) ) ;
#118817=CARTESIAN_POINT ( 'NONE',  ( 2.618638089201937635, 1.414096770131420877, -1.634928933042498755 ) ) ;
#118818=CARTESIAN_POINT ( 'NONE',  ( 6.610000000000026965, 7.052677709320480659, 2.598153670447616470 ) ) ;
#118823=CARTESIAN_POINT ( 'NONE',  ( 6.421112215724263272, -1.799107166270615732, 0.9110519380226205222 ) ) ;
#118826=CARTESIAN_POINT ( 'NONE',  ( 1.347511689332027807, 0.6317163119916607839, -2.098556723903362009 ) ) ;
#118828=CARTESIAN_POINT ( 'NONE',  ( 1.270828881381684150, -1.433710284283566949, 1.750253757905173124 ) ) ;
#118835=CARTESIAN_POINT ( 'NONE',  ( 3.562884411436726850, -1.522066076379503974, -0.8114761229951471533 ) ) ;
#118838=CARTESIAN_POINT ( 'NONE',  ( 2.196244507144041513, -0.4668761045134894871, -1.706985182271273382 ) ) ;
#118840=CARTESIAN_POINT ( 'NONE',  ( 2.789700014133191797, 1.910882804325767070, -0.6334545493084097201 ) ) ;
#118842=CARTESIAN_POINT ( 'NONE',  ( 5.473716482686670659, 2.128106746890707335, -0.5837492795209007213 ) ) ;
#118845=CARTESIAN_POINT ( 'NONE',  ( 4.500263427444707531, -0.9482861330638262531, 1.783302102689677371 ) ) ;
#118847=CARTESIAN_POINT ( 'NONE',  ( 3.515250061227533696, -1.862011288300661871, 0.7743320027404425598 ) ) ;
#118848=CARTESIAN_POINT ( 'NONE',  ( 4.289189881116685754, -0.006549295265783834294, -1.811767228872669389 ) ) ;
#118850=CARTESIAN_POINT ( 'NONE',  ( 3.045614982896325262, 0.6747646648952825288, -1.744891315567910439 ) ) ;
#118852=CARTESIAN_POINT ( 'NONE',  ( 2.179812656587180264, 1.874749209517186710, -0.3766967574026017229 ) ) ;
#118857=CARTESIAN_POINT ( 'NONE',  ( 0.1934256698341470238, 1.783621342183003389, -0.6902995980747894667 ) ) ;
#118859=CARTESIAN_POINT ( 'NONE',  ( 1.451531895509536874, 1.483362660712842063, 1.284035263222626844 ) ) ;
#118863=CARTESIAN_POINT ( 'NONE',  ( 5.431924468521282634, -2.068440459917933794, 0.4666711972392265650 ) ) ;
#118866=CARTESIAN_POINT ( 'NONE',  ( 5.729747329291909885, -1.248464225167019714, -1.525673545143470200 ) ) ;
#118868=CARTESIAN_POINT ( 'NONE',  ( 0.9670423206251937964, -1.584547017232017518, 1.241716394148101088 ) ) ;
#118870=CARTESIAN_POINT ( 'NONE',  ( 1.089646232962078853, -0.5102306600231114597, 2.054730298310704750 ) ) ;
#118872=CARTESIAN_POINT ( 'NONE',  ( 2.594261239525695206, 0.9781076984213372683, -1.824767828009652426 ) ) ;
#118876=CARTESIAN_POINT ( 'NONE',  ( 4.417973705048302335, 1.286473518301757712, -1.647865739169761978 ) ) ;
#118878=CARTESIAN_POINT ( 'NONE',  ( 3.293790705515726280, -0.7410340593078695859, 1.668602820345471027 ) ) ;
#118879=CARTESIAN_POINT ( 'NONE',  ( 1.892921280605066370, -0.08938092231483388272, -1.809401395368259280 ) ) ;
#118881=CARTESIAN_POINT ( 'NONE',  ( 6.445939570963195031, 0.8488519614954294079, -2.037301952897092594 ) ) ;
#118884=CARTESIAN_POINT ( 'NONE',  ( 5.333140672905051893, 0.1575165696711364749, 2.201206011701982934 ) ) ;
#118888=CARTESIAN_POINT ( 'NONE',  ( 4.494721087910216184, -1.855708629272670773, -0.4612273479895279138 ) ) ;
#118892=CARTESIAN_POINT ( 'NONE',  ( 6.707487347292075519, -1.660346423639452951, -1.236579608897829363 ) ) ;
#118899=CARTESIAN_POINT ( 'NONE',  ( 3.303821147848403861, -1.868562489643767144, 0.08839296284299941187 ) ) ;
#118901=CARTESIAN_POINT ( 'NONE',  ( -0.2409995289980245703, 0.2355275985303668385, -2.034371242098035548 ) ) ;
#118906=CARTESIAN_POINT ( 'NONE',  ( 6.526242037438201749, 1.059062773735760521, 1.778703558766213000 ) ) ;
#118907=CARTESIAN_POINT ( 'NONE',  ( 0.8257962581623284892, 0.8146080751335778025, -1.844719337431327544 ) ) ;
#118913=CARTESIAN_POINT ( 'NONE',  ( 0.9025786099917804117, 1.657183926254527595, -1.434042119274607563 ) ) ;
#118914=CARTESIAN_POINT ( 'NONE',  ( 6.252569598636129378, 0.5776572744066663656, 1.731972519516040032 ) ) ;
#118923=CARTESIAN_POINT ( 'NONE',  ( 4.300242120186610784, 1.420457692841030850, -1.171515996850613694 ) ) ;
#118924=CARTESIAN_POINT ( 'NONE',  ( 0.8209481077818219230, 1.523044454047136176, -1.316462280350006342 ) ) ;
#118925=CARTESIAN_POINT ( 'NONE',  ( 2.337686028923485537, -1.414513361329417851, 1.811461888080208027 ) ) ;
#118927=CARTESIAN_POINT ( 'NONE',  ( 0.4439182389155779673, -0.8842316343482552465, 1.637490449460777153 ) ) ;
#118931=CARTESIAN_POINT ( 'NONE',  ( 4.711142613322857109, 1.586760866459841379, -1.067142987418716604 ) ) ;
#118935=CARTESIAN_POINT ( 'NONE',  ( 4.089459622424143070, -0.7983975988373869237, 1.932503512935821011 ) ) ;
#118936=CARTESIAN_POINT ( 'NONE',  ( 1.867826558377215118, 0.9591755677602131769, 1.605880698980370225 ) ) ;
#118939=CARTESIAN_POINT ( 'NONE',  ( 3.175097308692858444, 1.106666961078702771, 1.343256515094106041 ) ) ;
#118943=CARTESIAN_POINT ( 'NONE',  ( 3.703458238649427692, -0.4988927697323896071, 1.651148375757867326 ) ) ;
#118945=CARTESIAN_POINT ( 'NONE',  ( 3.896163805485418852, -0.6886730243073329039, -2.080591098665984795 ) ) ;
#118946=CARTESIAN_POINT ( 'NONE',  ( 6.727182134110200273, -0.004969159814478123736, 2.189081792362323586 ) ) ;
#118948=CARTESIAN_POINT ( 'NONE',  ( 3.415042003188377251, -1.647272610417279015, 1.414370313860166872 ) ) ;
#118949=CARTESIAN_POINT ( 'NONE',  ( 2.086296903703276140, -1.790263230197926436, -0.3570169370194844483 ) ) ;
#118951=CARTESIAN_POINT ( 'NONE',  ( 4.294233728257051297, -0.9087460953031538669, -1.912572187454407047 ) ) ;
#118952=ORIENTED_EDGE ( 'NONE', *, *, #37494, .F. ) ;
#118953=CARTESIAN_POINT ( 'NONE',  ( 4.335649905164426166, 0.9806507323757740480, -2.072138663387664614 ) ) ;
#118955=CARTESIAN_POINT ( 'NONE',  ( 6.720655732516657821, 4.700665033810172311, 2.388972926809574737 ) ) ;
#118957=CARTESIAN_POINT ( 'NONE',  ( 0.9617728337494994006, -1.673954878106189703, -1.301583125534570673 ) ) ;
#118964=CARTESIAN_POINT ( 'NONE',  ( 6.381482430641396419, -0.5404875331735843336, -1.942542459342583294 ) ) ;
#118966=CARTESIAN_POINT ( 'NONE',  ( 4.504768599022889397, 0.5450402360923761735, 1.989220403428487938 ) ) ;
#118968=CARTESIAN_POINT ( 'NONE',  ( -0.2409995289980246813, 5.721856934700204178, -2.594540323675114113 ) ) ;
#118971=CARTESIAN_POINT ( 'NONE',  ( 0.1331565106231363538, 7.629137130509071163, -2.545925718843544239 ) ) ;
#118972=CARTESIAN_POINT ( 'NONE',  ( 0.5332922803617061724, -1.479851573012560761, -1.477019686621689143 ) ) ;
#118973=CARTESIAN_POINT ( 'NONE',  ( 4.711564657724523819, 1.930417226389494090, 0.5826574956761670920 ) ) ;
#118974=CARTESIAN_POINT ( 'NONE',  ( 4.722110844128335039, 1.763445737372179689, 0.5296355584529164329 ) ) ;
#118976=CARTESIAN_POINT ( 'NONE',  ( 1.131409910074301806, -1.089654060068695252, -1.336973495911207843 ) ) ;
#118977=CARTESIAN_POINT ( 'NONE',  ( 0.3390778084843976137, -1.706115258973059490, -1.074657883261991076 ) ) ;
#118978=CARTESIAN_POINT ( 'NONE',  ( 1.161203735943004300, 1.374334461307982425, 1.842484299438088557 ) ) ;
#118980=CARTESIAN_POINT ( 'NONE',  ( 0.8435138722653515719, -1.939887490614403687, 1.163926157780611925 ) ) ;
#118981=CARTESIAN_POINT ( 'NONE',  ( 3.492891347888595455, -0.4109570828031941514, -2.065403110348571492 ) ) ;
#118986=CARTESIAN_POINT ( 'NONE',  ( 6.062500000000003553, -1.451031289061355478, -1.451031289060867868 ) ) ;
#118991=CARTESIAN_POINT ( 'NONE',  ( 4.728890529236228879, 1.530954898644999451, -1.609847601234422276 ) ) ;
#118992=CARTESIAN_POINT ( 'NONE',  ( 2.677880624963273171, -1.125664371729949265, 1.880105217535378959 ) ) ;
#118995=CARTESIAN_POINT ( 'NONE',  ( 5.881297811770386907, -0.04968318840743202180, 1.961410508136133712 ) ) ;
#119001=CARTESIAN_POINT ( 'NONE',  ( 4.676102344489991403, 2.097148071331572439, -0.3138259731317455392 ) ) ;
#119005=CARTESIAN_POINT ( 'NONE',  ( 6.508665849870632236, 1.605377118863276387, -1.447859449074364591 ) ) ;
#119007=CARTESIAN_POINT ( 'NONE',  ( 5.601068772352080671, -0.4412860211496574814, 1.787476196608045464 ) ) ;
#119010=CARTESIAN_POINT ( 'NONE',  ( 1.241335265265028687, 1.738410175110545852, 0.08621907427421551806 ) ) ;
#119014=CARTESIAN_POINT ( 'NONE',  ( 5.787991602622606813, -0.9759734195362681497, 1.928925553883020338 ) ) ;
#119017=CARTESIAN_POINT ( 'NONE',  ( 4.715790015261832835, -2.120648752638915724, 0.4184459369844309440 ) ) ;
#119019=CARTESIAN_POINT ( 'NONE',  ( 4.692626201678701925, -0.4289087433139714411, -1.923991814828669433 ) ) ;
#119020=CARTESIAN_POINT ( 'NONE',  ( 3.813592814792550190, -1.418126570600848124, 0.9972168832048341480 ) ) ;
#119021=CARTESIAN_POINT ( 'NONE',  ( 0.7322823680011962821, 2.160084099745246178, 0.3691886501416344335 ) ) ;
#119022=CARTESIAN_POINT ( 'NONE',  ( 2.028779783278670035, 1.327905328797769569, -1.887045328260747112 ) ) ;
#119023=CARTESIAN_POINT ( 'NONE',  ( 5.114554592455347048, 1.424167462454002608, -1.489711086068323587 ) ) ;
#119024=CARTESIAN_POINT ( 'NONE',  ( 6.286669113786358842, 1.687405947569386999, -0.9612952809280647104 ) ) ;
#119027=CARTESIAN_POINT ( 'NONE',  ( 0.8795299900376440938, -0.4926441280813895762, -1.955172062459666904 ) ) ;
#119029=CARTESIAN_POINT ( 'NONE',  ( 3.153566124713353513, -1.803153744294363481, -1.271922660818012973 ) ) ;
#119031=CARTESIAN_POINT ( 'NONE',  ( 1.164654898877310885, 1.413799132238046985, -1.210232755764220069 ) ) ;
#119036=CARTESIAN_POINT ( 'NONE',  ( 6.925078400183513949, 3.679108800414055302, 2.758152782261179325 ) ) ;
#119037=CARTESIAN_POINT ( 'NONE',  ( 6.017501326166345699, -1.026660802952833240, -1.528114487065170390 ) ) ;
#119039=CARTESIAN_POINT ( 'NONE',  ( 2.940362659251498645, 2.045167860313545916, 0.2535661900368457733 ) ) ;
#119042=CARTESIAN_POINT ( 'NONE',  ( 2.033858944562048965, -1.958440182618191416, 0.4929867953931149627 ) ) ;
#119045=CARTESIAN_POINT ( 'NONE',  ( 2.079048039887823052, -0.09986672515850322784, -2.058587512739398662 ) ) ;
#119049=CARTESIAN_POINT ( 'NONE',  ( -0.2409995289980246258, 1.355929887833319469, -2.254219809973062816 ) ) ;
#119050=CARTESIAN_POINT ( 'NONE',  ( 5.074942902252104204, -2.077123540546990110, -0.7459609299403434646 ) ) ;
#119051=CARTESIAN_POINT ( 'NONE',  ( 1.739762150092131643, -1.564342989677082629, -1.491970722459233345 ) ) ;
#119053=CARTESIAN_POINT ( 'NONE',  ( 0.4972802279516430612, -0.2910764605805628014, 1.995268990643041640 ) ) ;
#119055=CARTESIAN_POINT ( 'NONE',  ( 2.021309514094786763, 2.292189817666248075, -0.1691314976695507954 ) ) ;
#119061=CARTESIAN_POINT ( 'NONE',  ( 2.254581950620972997, -1.447608085528677480, 1.184820545849271767 ) ) ;
#119062=CARTESIAN_POINT ( 'NONE',  ( 3.661342437515973547, 1.897110692972364454, -0.6839366698164971448 ) ) ;
#119066=CARTESIAN_POINT ( 'NONE',  ( 5.391282926306558032, 1.858022621660906371, -0.9916069233004040084 ) ) ;
#119072=CARTESIAN_POINT ( 'NONE',  ( 4.904559663377827228, -2.005024252762297898, -0.2429568683046164634 ) ) ;
#119074=CARTESIAN_POINT ( 'NONE',  ( 0.6376417299419987472, 1.925892387546113582, -0.7388170802648945656 ) ) ;
#119083=CARTESIAN_POINT ( 'NONE',  ( 3.244746832269917558, -2.138594630188391132, -0.3739374351436116073 ) ) ;
#119086=CARTESIAN_POINT ( 'NONE',  ( 1.505144418776669601, -1.827259764946763454, 0.2261131901925839127 ) ) ;
#119088=CARTESIAN_POINT ( 'NONE',  ( 4.388337494309430653, -0.4807229498768311182, -2.138019847805587403 ) ) ;
#119090=CARTESIAN_POINT ( 'NONE',  ( 4.698257824713211406, -2.261882422057570619, -0.06011341499151043322 ) ) ;
#119097=CARTESIAN_POINT ( 'NONE',  ( 5.342920941031360726, -1.517576202870707380, 0.9101455627106845858 ) ) ;
#119099=CARTESIAN_POINT ( 'NONE',  ( 1.747240475267642257, -1.779442529384717808, 1.126025380906693352 ) ) ;
#119102=CARTESIAN_POINT ( 'NONE',  ( 2.049204468142644231, 1.715183525312633517, -0.9679544390571446222 ) ) ;
#119103=CARTESIAN_POINT ( 'NONE',  ( 0.1802491246630563426, -1.813337052076903877, -0.4591185353455888296 ) ) ;
#119104=CARTESIAN_POINT ( 'NONE',  ( 0.6956633456795427994, -1.384754418207832405, -1.389998539416361423 ) ) ;
#119105=CARTESIAN_POINT ( 'NONE',  ( 5.695527492674265169, 1.670499194714653468, -0.7014341174245084520 ) ) ;
#119109=CARTESIAN_POINT ( 'NONE',  ( 6.315307248462690204, -0.2269180964024133385, 1.856785020699961875 ) ) ;
#119112=CARTESIAN_POINT ( 'NONE',  ( 5.313363446356571984, -1.745981802610725442, -1.112170280247841703 ) ) ;
#119122=CARTESIAN_POINT ( 'NONE',  ( 4.949637131784443866, 1.452432516441283905, 1.319008059494260143 ) ) ;
#119124=CARTESIAN_POINT ( 'NONE',  ( 3.638045922354939954, 0.05228986736816390590, -2.015604357568132166 ) ) ;
#119126=CARTESIAN_POINT ( 'NONE',  ( 2.395587962911712498, -1.894220731477358921, 0.2854614921951497686 ) ) ;
#119128=CARTESIAN_POINT ( 'NONE',  ( 0.8729168595149154886, -0.05911722906676297740, -2.190938979806676734 ) ) ;
#119129=CARTESIAN_POINT ( 'NONE',  ( 0.2335667940003021970, 4.085521407782252368, -2.708192491817535075 ) ) ;
#119130=CARTESIAN_POINT ( 'NONE',  ( 1.598681293450100904, 1.532267803987485077, -1.072633048482305229 ) ) ;
#119132=CARTESIAN_POINT ( 'NONE',  ( 4.289318580081720178, -0.004264002974461738975, -2.013376228308662252 ) ) ;
#119135=CARTESIAN_POINT ( 'NONE',  ( 4.868830934094980911, -0.2605620880507720227, -2.101091820269097354 ) ) ;
#119136=CARTESIAN_POINT ( 'NONE',  ( 6.461392557816405535, 1.719054114842766268, 1.153505076091146053 ) ) ;
#119137=CARTESIAN_POINT ( 'NONE',  ( 1.698888801382715252, 1.740066399362389271, 1.158727311120285819 ) ) ;
#119138=CARTESIAN_POINT ( 'NONE',  ( 6.620655732516620873, 2.403464043289889496, 2.653833411862613012 ) ) ;
#119139=CARTESIAN_POINT ( 'NONE',  ( 0.1996746939399509924, -1.724222465425511386, -0.05034706749046553159 ) ) ;
#119148=CARTESIAN_POINT ( 'NONE',  ( 0.8909134567714148689, -0.04341352697850982267, -1.811128585712480366 ) ) ;
#119154=CARTESIAN_POINT ( 'NONE',  ( 5.993767587909683670, -2.000856116866961187, 0.2496242821527286382 ) ) ;
#119155=CARTESIAN_POINT ( 'NONE',  ( 0.5926325054007793858, -1.174586488569592690, 1.765252418913294319 ) ) ;
#119157=CARTESIAN_POINT ( 'NONE',  ( -0.1394461523061351904, -0.009327122704730000241, -2.280146446826665230 ) ) ;
#119161=CARTESIAN_POINT ( 'NONE',  ( 3.871889627987592064, -1.941038753702705177, 0.3322218420921344562 ) ) ;
#119162=CARTESIAN_POINT ( 'NONE',  ( 4.253529916566947122, 1.955168710539030075, -0.4926619687581067497 ) ) ;
#119167=CARTESIAN_POINT ( 'NONE',  ( 5.015667846030231303, -1.170523448010954315, -1.852474865436819274 ) ) ;
#119169=CARTESIAN_POINT ( 'NONE',  ( 3.610301043878104021, -0.7796817500047310556, -1.761725471645478436 ) ) ;
#119171=CARTESIAN_POINT ( 'NONE',  ( -0.02968770228140016343, 0.2527710104786498047, -1.861515397111657144 ) ) ;
#119172=CARTESIAN_POINT ( 'NONE',  ( 0.1333542156527660338, 0.2446709926765543996, -2.080993637364982884 ) ) ;
#119176=CARTESIAN_POINT ( 'NONE',  ( 4.785976182654667177, -1.208483435658064487, -1.555025035033012148 ) ) ;
#119177=CARTESIAN_POINT ( 'NONE',  ( 0.2572359396431650458, 1.920763697077633614, -0.2861409625158922165 ) ) ;
#119178=CARTESIAN_POINT ( 'NONE',  ( 3.774091158939500978, 1.997611739970482692, -0.2487840229714877727 ) ) ;
#119179=CARTESIAN_POINT ( 'NONE',  ( 5.589350027729360626, 1.375356176494828553, -1.841343765151080003 ) ) ;
#119181=CARTESIAN_POINT ( 'NONE',  ( 4.574962676454192412, 1.700228875758927671, 0.7569903647998057483 ) ) ;
#119187=CARTESIAN_POINT ( 'NONE',  ( 6.720655732516650716, 2.467238681591706673, 2.210725262702870175 ) ) ;
#119188=CARTESIAN_POINT ( 'NONE',  ( 0.6795420635867071013, 1.475991390215245058, 1.620154534501851096 ) ) ;
#119193=CARTESIAN_POINT ( 'NONE',  ( 0.3986991128735201673, 1.519733473351183362, -1.011397189243423700 ) ) ;
#119195=CARTESIAN_POINT ( 'NONE',  ( 2.443678673881148011, -1.509841515647825094, -0.8527992262679043867 ) ) ;
#119199=CARTESIAN_POINT ( 'NONE',  ( 6.024025069106937913, -1.018266858664597763, -1.515143308444939274 ) ) ;
#119200=CARTESIAN_POINT ( 'NONE',  ( 3.783995958019512607, -1.164969938643352299, -1.578273546942794647 ) ) ;
#119204=CARTESIAN_POINT ( 'NONE',  ( 4.530007735025624704, -2.079396993832134388, 0.4145621898983055109 ) ) ;
#119206=CIRCLE ( 'NONE', #153784, 0.05000000000000056483 ) ;
#119209=CARTESIAN_POINT ( 'NONE',  ( 2.536061329345109971, 1.270221119870031057, 1.634730569901183150 ) ) ;
#119213=CARTESIAN_POINT ( 'NONE',  ( 4.266425542637849233, 2.220793247050854902, -0.05466516159106404871 ) ) ;
#119215=CARTESIAN_POINT ( 'NONE',  ( 3.252836000005991046, 2.242300829042419785, -0.5054477054214584486 ) ) ;
#119222=CARTESIAN_POINT ( 'NONE',  ( 2.847809051801777791, -1.287500320553297994, -1.414207669007704116 ) ) ;
#119224=CARTESIAN_POINT ( 'NONE',  ( 4.260587326446613865, -1.277293937326873019, 1.159233799866489889 ) ) ;
#119225=CARTESIAN_POINT ( 'NONE',  ( 3.485564796978508184, -0.5807542032013839339, 1.931124776463407189 ) ) ;
#119226=CARTESIAN_POINT ( 'NONE',  ( 3.938341551375645011, -1.911473949098478897, -1.276577049080502624 ) ) ;
#119229=CARTESIAN_POINT ( 'NONE',  ( 6.024072228909682636, -1.168613738950954550, -1.751890494488865357 ) ) ;
#119232=CARTESIAN_POINT ( 'NONE',  ( 4.569463179464338332, 1.716784003608927467, -0.4291735618162701438 ) ) ;
#119234=CARTESIAN_POINT ( 'NONE',  ( 0.8675860333910101474, 2.207824459889203172, -0.6162223019612712571 ) ) ;
#119235=CARTESIAN_POINT ( 'NONE',  ( 0.3744471653823171486, 1.625640304646416734, -0.6218004557168725910 ) ) ;
#119237=CARTESIAN_POINT ( 'NONE',  ( 6.351546390744761794, 2.185874319550953793, -0.1572705277706408222 ) ) ;
#119241=CARTESIAN_POINT ( 'NONE',  ( 6.742638474511262636, -2.029596885996234334, -0.4079607620106340260 ) ) ;
#119242=CARTESIAN_POINT ( 'NONE',  ( 0.8664231474371618669, -1.968446048378743152, -0.4370742218882398000 ) ) ;
#119244=CARTESIAN_POINT ( 'NONE',  ( 5.971306315489836258, 0.1393824199819072851, -1.921517340817725961 ) ) ;
#119246=CARTESIAN_POINT ( 'NONE',  ( 1.125557598851456786, 1.962289056045916524, 1.041162070263027761 ) ) ;
#119255=CARTESIAN_POINT ( 'NONE',  ( 4.089206054525551970, -0.6613740077951230090, 1.610090703890323605 ) ) ;
#119256=CARTESIAN_POINT ( 'NONE',  ( 2.365611650783586040, -0.4327418640146082907, 1.913375882425945917 ) ) ;
#119260=CARTESIAN_POINT ( 'NONE',  ( 6.232861002365865488, -1.862453515449840724, -0.6167318247369477646 ) ) ;
#119264=CARTESIAN_POINT ( 'NONE',  ( 5.436732529336289588, -1.586671906620169104, 1.244382051841623538 ) ) ;
#119265=CARTESIAN_POINT ( 'NONE',  ( 1.218052960884225433, -2.206959832567402469, 0.4976822367108637013 ) ) ;
#119269=CARTESIAN_POINT ( 'NONE',  ( 1.827212670807505379, -1.763035892288829620, 0.6254473451912796467 ) ) ;
#119270=CARTESIAN_POINT ( 'NONE',  ( 0.1407077508718111714, 0.6607813331330723017, 1.603534759577706303 ) ) ;
#119271=CARTESIAN_POINT ( 'NONE',  ( 4.652002595327206613, 0.8389548150543740812, 2.024815518666116088 ) ) ;
#119272=CARTESIAN_POINT ( 'NONE',  ( 5.965930945686983122, 2.274828880937030728, -0.3866611637039600313 ) ) ;
#119273=CARTESIAN_POINT ( 'NONE',  ( 0.8310182365124726411, 0.1507505247145359273, 2.055422933874837099 ) ) ;
#119274=CARTESIAN_POINT ( 'NONE',  ( 3.363160477839432172, 1.894460165981373789, -0.4261612883773926441 ) ) ;
#119277=CARTESIAN_POINT ( 'NONE',  ( 5.360568611784803927, -1.355617963529401893, 1.289147430649554948 ) ) ;
#119279=CARTESIAN_POINT ( 'NONE',  ( 6.503279807981923177, 1.993766592317405051, 0.2985777636397292101 ) ) ;
#119281=CARTESIAN_POINT ( 'NONE',  ( 4.412732527109735514, -1.242725882911545510, -1.587838301257207041 ) ) ;
#119285=CARTESIAN_POINT ( 'NONE',  ( 1.629252094361890890, -1.719607636260962025, 0.6136192449261099746 ) ) ;
#119294=CARTESIAN_POINT ( 'NONE',  ( 6.164714676696682716, 0.6357101859572679148, 1.917071687811313652 ) ) ;
#119295=CARTESIAN_POINT ( 'NONE',  ( 0.2059360158346480729, 1.574223368660916611, 1.420867075595611650 ) ) ;
#119299=CARTESIAN_POINT ( 'NONE',  ( 4.996976137430897857, 1.714615628211055398, -1.143075302399678472 ) ) ;
#119300=CARTESIAN_POINT ( 'NONE',  ( 5.045546153961558922, -1.458558117013383892, 1.392544180963309230 ) ) ;
#119308=CARTESIAN_POINT ( 'NONE',  ( 5.167342215279058237, -0.6766115767681828430, -1.899327316215810857 ) ) ;
#119309=CARTESIAN_POINT ( 'NONE',  ( 3.661895226921571656, -1.235415792305821325, 1.365283978338522441 ) ) ;
#119311=CARTESIAN_POINT ( 'NONE',  ( 2.368180137760375281, 2.262835426277497675, -0.4520343961368147312 ) ) ;
#119313=CARTESIAN_POINT ( 'NONE',  ( 5.079442160427912967, 2.018932005888602887, -0.7727740077691500620 ) ) ;
#119315=CARTESIAN_POINT ( 'NONE',  ( -0.1119450412391852639, -0.4286113830911059130, -1.901434273657340412 ) ) ;
#119316=CARTESIAN_POINT ( 'NONE',  ( 2.659388954101277847, 1.913261587491304150, -0.6371546050257800298 ) ) ;
#119322=CARTESIAN_POINT ( 'NONE',  ( 3.520239479114236403, 1.187513476551487424, -1.445374034619356207 ) ) ;
#119324=CARTESIAN_POINT ( 'NONE',  ( 0.2980362317399931626, -1.970818609879662953, -0.05296617050038961161 ) ) ;
#119327=CARTESIAN_POINT ( 'NONE',  ( 1.243116305521356990, 0.4334984505205765060, 2.163720904216937857 ) ) ;
#119333=CARTESIAN_POINT ( 'NONE',  ( 0.1808907491311480820, -0.1332662104699660066, -1.940345832946618554 ) ) ;
#119334=CARTESIAN_POINT ( 'NONE',  ( 0.2886476729930695373, -1.083662648423104891, 2.037333779670726930 ) ) ;
#119335=CARTESIAN_POINT ( 'NONE',  ( 0.2386218892466463737, -1.902018210125755004, -0.4804332253167050149 ) ) ;
#119336=CARTESIAN_POINT ( 'NONE',  ( 3.766515156912704665, -0.8315086482118605460, -1.887695802070661344 ) ) ;
#119345=CARTESIAN_POINT ( 'NONE',  ( 6.883263157960365142, -0.007059606330772279746, 2.153658854459541416 ) ) ;
#119347=CARTESIAN_POINT ( 'NONE',  ( 5.653808312887880660, 0.7519890275384639722, 1.680886247995525773 ) ) ;
#119350=DIRECTION ( 'NONE',  ( 1.040834085586084257E-15, 1.000000000000000000, -4.622230424712076367E-32 ) ) ;
#119355=CARTESIAN_POINT ( 'NONE',  ( 1.594246750649646494, -1.022002606473694675, 1.616071880676916317 ) ) ;
#119356=CARTESIAN_POINT ( 'NONE',  ( 2.113771285056417426, -0.8311870117129838142, -1.562508279020339064 ) ) ;
#119357=CARTESIAN_POINT ( 'NONE',  ( 5.865890606937535168, 0.5820329372835297832, -1.927131433562751406 ) ) ;
#119359=CARTESIAN_POINT ( 'NONE',  ( 4.024928501738918030, -1.664925135935046763, 0.9472863605698205181 ) ) ;
#119361=CARTESIAN_POINT ( 'NONE',  ( 5.055114266443681004, 1.638575763527612583, -1.092465951337840524 ) ) ;
#119362=CARTESIAN_POINT ( 'NONE',  ( 6.398695825915057256, -1.981597308308700844, -0.3899587018172407382 ) ) ;
#119364=CARTESIAN_POINT ( 'NONE',  ( 4.012460596634464416, 1.323225596166040186, -1.322536486416127977 ) ) ;
#119365=CARTESIAN_POINT ( 'NONE',  ( 5.936138232048088881, 0.8439337091313244832, -1.504256470664022238 ) ) ;
#119367=CARTESIAN_POINT ( 'NONE',  ( 3.282038605231399231, 1.400092287458438722, 1.705885466304429166 ) ) ;
#119370=CARTESIAN_POINT ( 'NONE',  ( 0.7485702846574161518, -2.046882729015482738, -0.2544144183350918742 ) ) ;
#119375=CARTESIAN_POINT ( 'NONE',  ( 0.1747926744264677867, 6.948552888299643904, -2.450368216405907962 ) ) ;
#119378=CARTESIAN_POINT ( 'NONE',  ( 2.910663983731573090, 0.6951178490613962868, 1.950330170896700022 ) ) ;
#119383=CARTESIAN_POINT ( 'NONE',  ( 0.6803390939152150763, 0.9973279206440927025, 1.756184504224398202 ) ) ;
#119385=CARTESIAN_POINT ( 'NONE',  ( 0.07499057489264347731, 1.360887136235461758, -2.209073988085366480 ) ) ;
#119387=CARTESIAN_POINT ( 'NONE',  ( 6.696638777208028692, -1.314797947003863543, -1.528504179509587280 ) ) ;
#119388=CARTESIAN_POINT ( 'NONE',  ( 5.559766488213514712, 1.146785110015311915, 1.534377285673252267 ) ) ;
#119389=CARTESIAN_POINT ( 'NONE',  ( 6.539320575229251808, 2.414832891527439962, 2.584256253838035366 ) ) ;
#119390=CARTESIAN_POINT ( 'NONE',  ( 3.755584314896889264, 2.174856280799509545, -0.2696606696684644700 ) ) ;
#119391=CIRCLE ( 'NONE', #28877, 0.04999999999999930889 ) ;
#119393=CARTESIAN_POINT ( 'NONE',  ( 3.076317393561965208, 0.8638369986560844316, 1.706277067364106115 ) ) ;
#119397=CARTESIAN_POINT ( 'NONE',  ( 0.7554827284574801016, 1.942536278707338360, -0.5405140857882018146 ) ) ;
#119399=CARTESIAN_POINT ( 'NONE',  ( 6.181208317857348256, 1.509947553572440704, 1.588605474358975478 ) ) ;
#119401=CARTESIAN_POINT ( 'NONE',  ( 3.487030103973333794, 1.559624344477263502, -0.7367539641185815169 ) ) ;
#119407=CARTESIAN_POINT ( 'NONE',  ( 1.328483007144948935, -1.247240240105648601, 1.514344512384787622 ) ) ;
#119410=CARTESIAN_POINT ( 'NONE',  ( 0.07516593201277278757, 5.721767059778611220, -2.638283098249011971 ) ) ;
#119414=CARTESIAN_POINT ( 'NONE',  ( 3.404753564208697014, -0.3562933990706117493, -1.775892323017129737 ) ) ;
#119419=CARTESIAN_POINT ( 'NONE',  ( 4.758376837038695406, 1.806999933331495445, 0.1280191873242030876 ) ) ;
#119423=CARTESIAN_POINT ( 'NONE',  ( 5.476954007041204164, 1.719599228052148154, 0.7121796456092708283 ) ) ;
#119425=CARTESIAN_POINT ( 'NONE',  ( 2.636237813805066388, 0.6479696587880221514, 1.802806680411846774 ) ) ;
#119435=CARTESIAN_POINT ( 'NONE',  ( 1.921934154048171584, 1.202774473455773041, -1.709796194579858319 ) ) ;
#119437=CARTESIAN_POINT ( 'NONE',  ( 0.3580656308817787292, 0.6935259069400134813, 1.688922952486398454 ) ) ;
#119439=CARTESIAN_POINT ( 'NONE',  ( 2.239018641000252607, -1.631965468365924377, 0.8183158014263000046 ) ) ;
#119441=CARTESIAN_POINT ( 'NONE',  ( 1.968876373762207255, -1.476028252698018628, 1.215921256797661609 ) ) ;
#119442=CARTESIAN_POINT ( 'NONE',  ( 2.189847533163618465, -1.284324338361255258, -1.493307823759764341 ) ) ;
#119443=CARTESIAN_POINT ( 'NONE',  ( 3.228005407155889461, 1.895358990768666096, 0.4226955006484037214 ) ) ;
#119446=CARTESIAN_POINT ( 'NONE',  ( 4.060867369437678676, 0.5686956411946364476, 2.042824496258560441 ) ) ;
#119455=CARTESIAN_POINT ( 'NONE',  ( 3.844227010333609584, 1.817057058749595777, 0.1772887374331885701 ) ) ;
#119456=CARTESIAN_POINT ( 'NONE',  ( 0.1509401653462701109, -0.4529219869476922011, -2.027634260368789576 ) ) ;
#119460=CARTESIAN_POINT ( 'NONE',  ( 4.522238337509359773, 1.150754656758418593, -1.474723989322044959 ) ) ;
#119462=CARTESIAN_POINT ( 'NONE',  ( 2.279798536657418495, 1.185040197188882871, 1.518827336823719953 ) ) ;
#119471=CARTESIAN_POINT ( 'NONE',  ( 1.001738948178192645, -2.064706785862341132, 0.4679990497924620407 ) ) ;
#119474=CARTESIAN_POINT ( 'NONE',  ( 6.455931442665615805, -0.7031469350025701948, 1.947301169641938223 ) ) ;
#119475=CARTESIAN_POINT ( 'NONE',  ( 0.8020088176248600931, 1.394402496181508466, -1.202495849378336423 ) ) ;
#119477=CARTESIAN_POINT ( 'NONE',  ( 0.3163000706473735879, -1.844146670390820475, 1.371622413452098233 ) ) ;
#119481=CARTESIAN_POINT ( 'NONE',  ( 1.236728449817244835, 0.4514257060114800213, 2.247219992417306411 ) ) ;
#119484=CARTESIAN_POINT ( 'NONE',  ( 5.542900022196344700, -1.532237948119744342, -1.192973588722973100 ) ) ;
#119487=CARTESIAN_POINT ( 'NONE',  ( 0.2814942100668381131, 0.1933317163467423994, -2.003872996790170724 ) ) ;
#119488=CARTESIAN_POINT ( 'NONE',  ( 6.368375356916068597, -1.978549699825098429, -0.3886382054163611821 ) ) ;
#119491=CARTESIAN_POINT ( 'NONE',  ( 2.361375956566538648, 2.050102581710811389, -0.4087646360023765024 ) ) ;
#119492=CARTESIAN_POINT ( 'NONE',  ( 0.9008075156715513732, 1.443549170786810443, 1.023676300919857507 ) ) ;
#119496=CARTESIAN_POINT ( 'NONE',  ( 4.664210274407590617, -1.499448637150493813, 1.733910808658318814 ) ) ;
#119497=CARTESIAN_POINT ( 'NONE',  ( 3.521201755802486844, -1.038059167858174092, -1.396672450663126508 ) ) ;
#119500=CARTESIAN_POINT ( 'NONE',  ( 3.409274926616968404, 0.4192967605245543905, 1.682228440661166502 ) ) ;
#119502=CARTESIAN_POINT ( 'NONE',  ( 3.895131827238162536, 0.3151296210822142063, 2.148063795774640461 ) ) ;
#119504=CARTESIAN_POINT ( 'NONE',  ( 4.733611406029458735, 0.6279933214467496860, -1.916352419866963697 ) ) ;
#119505=CARTESIAN_POINT ( 'NONE',  ( 3.093750000000001776, -1.895863743164152071, -0.7852924748298234503 ) ) ;
#119507=CARTESIAN_POINT ( 'NONE',  ( 2.625899107431714175, -1.107553820047700199, -1.575994028688005644 ) ) ;
#119509=CARTESIAN_POINT ( 'NONE',  ( 4.799211390369230834, -0.2731021391014861188, -2.204526388291703221 ) ) ;
#119511=CARTESIAN_POINT ( 'NONE',  ( -0.2108831679770924727, 4.091978752061476321, -2.452067053820900622 ) ) ;
#119516=CARTESIAN_POINT ( 'NONE',  ( 0.7686061912218185022, 2.218469807834182017, -0.1147041126551024554 ) ) ;
#119517=CARTESIAN_POINT ( 'NONE',  ( 5.529730448059603454, 1.891198321494348633, -0.5216162335564683561 ) ) ;
#119519=CARTESIAN_POINT ( 'NONE',  ( 6.714178486276241919, -1.057601618853749148, -1.999996817866441123 ) ) ;
#119523=CARTESIAN_POINT ( 'NONE',  ( 3.789554774376595159, -1.906935327315992579, 0.7867413014382127479 ) ) ;
#119528=CARTESIAN_POINT ( 'NONE',  ( 5.325416506339426981, -1.776575524504429016, 0.5857008802128694791 ) ) ;
#119529=CARTESIAN_POINT ( 'NONE',  ( 5.291581958225426874, 1.307657812419236176, -1.139094164941084841 ) ) ;
#119530=CARTESIAN_POINT ( 'NONE',  ( 3.087183437724149826, -0.7025620359558025774, 1.592517242405028233 ) ) ;
#119531=CARTESIAN_POINT ( 'NONE',  ( 1.910137617552462030, -1.084854587848137708, -2.019442561568355110 ) ) ;
#119534=CARTESIAN_POINT ( 'NONE',  ( 5.249593148720715696, 2.088313038247250120, -0.1037309089504182269 ) ) ;
#119535=CARTESIAN_POINT ( 'NONE',  ( 6.650339433524894872, -1.499410535642144549, 1.233700977392115705 ) ) ;
#119538=CARTESIAN_POINT ( 'NONE',  ( 1.389296306420295224, -0.7283806465635984662, -1.880434191983325398 ) ) ;
#119539=CARTESIAN_POINT ( 'NONE',  ( 0.4807640440005827576, -0.2721776580492247799, -2.174417363000572756 ) ) ;
#119543=CARTESIAN_POINT ( 'NONE',  ( 2.684367718930933844, 1.136400967617630986, 1.790090880730066392 ) ) ;
#119545=CARTESIAN_POINT ( 'NONE',  ( 5.004447790439923160, -0.6182884515001166870, -1.717943145347331502 ) ) ;
#119551=CARTESIAN_POINT ( 'NONE',  ( 2.355728564803623915, -1.499445635549499389, -1.353443481924651470 ) ) ;
#119552=CARTESIAN_POINT ( 'NONE',  ( 0.4816451290811329389, 1.964891932219949844, -0.7582931990086133611 ) ) ;
#119554=CARTESIAN_POINT ( 'NONE',  ( 3.836619860451701669, -1.792334419201064399, -0.5002748670543122333 ) ) ;
#119559=CARTESIAN_POINT ( 'NONE',  ( 5.566980414702134894, -1.652319403193935887, -0.7768266693391965294 ) ) ;
#119564=CARTESIAN_POINT ( 'NONE',  ( 1.686441086386183619, -0.9581320880991549549, -1.444804011637023322 ) ) ;
#119565=CARTESIAN_POINT ( 'NONE',  ( 6.386648935047418263, 1.599332519906123462, -0.9119682274050244786 ) ) ;
#119566=CARTESIAN_POINT ( 'NONE',  ( 5.162836451262333703, -1.674513216643868985, 1.588141549981958001 ) ) ;
#119569=CARTESIAN_POINT ( 'NONE',  ( 1.757177114327221901, -1.766000478700447074, -1.061884917490847791 ) ) ;
#119572=CARTESIAN_POINT ( 'NONE',  ( 6.643951024375948755, -0.1027215121673381443, -2.296211363497886460 ) ) ;
#119575=CARTESIAN_POINT ( 'NONE',  ( 6.561405567229332547, 0.3174558530528898692, -1.843364171016811603 ) ) ;
#119578=CARTESIAN_POINT ( 'NONE',  ( 3.937688585161042809, -1.828529804631402023, 0.5600222464785462595 ) ) ;
#119580=CARTESIAN_POINT ( 'NONE',  ( 4.723365791888975096, -0.1103408873950258995, 2.204240794804641190 ) ) ;
#119586=CARTESIAN_POINT ( 'NONE',  ( 5.830757645730302308, 1.424217953154560012, -1.571192434731554677 ) ) ;
#119587=VERTEX_POINT ( 'NONE', #110421 ) ;
#119588=CARTESIAN_POINT ( 'NONE',  ( 3.927071981709300719, 2.190135382617847792, 0.7269923479944776501 ) ) ;
#119589=CARTESIAN_POINT ( 'NONE',  ( 3.912515228517557286, 0.7039278570535618673, 1.831416474553926310 ) ) ;
#119591=CARTESIAN_POINT ( 'NONE',  ( 1.076917802502619592, 1.810449747239597951, 0.7559744942375111743 ) ) ;
#119594=ORIENTED_EDGE ( 'NONE', *, *, #106096, .F. ) ;
#119595=CARTESIAN_POINT ( 'NONE',  ( 5.999232488047272049, -0.2420365156972601739, 2.001857322483958423 ) ) ;
#119597=CARTESIAN_POINT ( 'NONE',  ( -0.01213283819992416745, -0.3988646234997471618, -1.803908381610368261 ) ) ;
#119598=CARTESIAN_POINT ( 'NONE',  ( 3.151421466623941292, 1.864366918651944927, -1.112252681494025897 ) ) ;
#119600=CARTESIAN_POINT ( 'NONE',  ( 0.4750491441844888474, -1.531729482103380224, 1.466773057065169361 ) ) ;
#119605=CARTESIAN_POINT ( 'NONE',  ( 1.616555492630408875, 1.386288697630438715, -1.524948804171057493 ) ) ;
#119611=CARTESIAN_POINT ( 'NONE',  ( 4.740819843082155316, 1.831016553098392619, 0.5515768964349797576 ) ) ;
#119615=CARTESIAN_POINT ( 'NONE',  ( 0.7733460811225587594, 0.3524055278083237930, -1.776778109436588204 ) ) ;
#119618=CARTESIAN_POINT ( 'NONE',  ( 0.4971116367980681350, -0.2779505141972256066, 1.895288638825567862 ) ) ;
#119619=CARTESIAN_POINT ( 'NONE',  ( 2.488806849732328796, 2.007603858877416769, 0.5053560088097220904 ) ) ;
#119621=CARTESIAN_POINT ( 'NONE',  ( 0.4617158845385913590, 1.950347379310466422, -0.2869839225536646166 ) ) ;
#119622=CARTESIAN_POINT ( 'NONE',  ( 2.613660848560446226, -1.805822647967849193, 0.2677728182119283318 ) ) ;
#119623=CARTESIAN_POINT ( 'NONE',  ( 0.1007806894988797913, -2.307328790448114120, -0.04970016441883937791 ) ) ;
#119626=CARTESIAN_POINT ( 'NONE',  ( 4.492669715648281326, 2.022274968565600517, 0.4054665169595774721 ) ) ;
#119631=CARTESIAN_POINT ( 'NONE',  ( 5.825249245718299385, -0.05505390245461554838, 2.105416907300653673 ) ) ;
#119634=CARTESIAN_POINT ( 'NONE',  ( 0.2390591215055883068, -2.106223889411312999, -0.5266447289704286883 ) ) ;
#119636=CARTESIAN_POINT ( 'NONE',  ( 3.708425082824120533, -0.8722964037291662809, -1.977944213000272455 ) ) ;
#119637=CARTESIAN_POINT ( 'NONE',  ( 3.932289538495234549, -1.040048408385336964, -1.731156807262229425 ) ) ;
#119638=CARTESIAN_POINT ( 'NONE',  ( 6.620655732516647518, 3.684600858287550906, 2.687722323901103660 ) ) ;
#119643=CARTESIAN_POINT ( 'NONE',  ( 2.887907956677421506, -2.014008092954455265, 0.1037802451031161477 ) ) ;
#119650=CARTESIAN_POINT ( 'NONE',  ( 4.974232547167513729, -2.001514726140873890, -0.2440111082952014510 ) ) ;
#119652=CARTESIAN_POINT ( 'NONE',  ( 0.1524156081505250449, -1.388816673012055025, 1.022707173280016368 ) ) ;
#119657=CARTESIAN_POINT ( 'NONE',  ( 5.905500869136258046, -0.4549164269060863020, 1.814235589242949587 ) ) ;
#119658=CARTESIAN_POINT ( 'NONE',  ( 6.187749739576326569, 1.925281575520617849, -0.5883678985393098193 ) ) ;
#119663=CARTESIAN_POINT ( 'NONE',  ( 1.212517793387542842, 1.944078472882956987, 0.5350667013180390175 ) ) ;
#119669=CARTESIAN_POINT ( 'NONE',  ( 6.292599812010432281, 1.415705964336026357, -1.290654269910092911 ) ) ;
#119678=CARTESIAN_POINT ( 'NONE',  ( 3.819328725847204620, -0.1613130240520690706, 2.155748724213396361 ) ) ;
#119681=CARTESIAN_POINT ( 'NONE',  ( 1.213308285724056690, 1.730450836393576886, -1.225479750871574680 ) ) ;
#119682=CARTESIAN_POINT ( 'NONE',  ( 5.649374308873757577, -1.440485763676568443, -1.121356984487072328 ) ) ;
#119684=CARTESIAN_POINT ( 'NONE',  ( 2.214082964306641532, -0.9260232682030484774, -1.740301080291997149 ) ) ;
#119685=CARTESIAN_POINT ( 'NONE',  ( 4.148624843374196125, 1.876505540506741010, 0.3678670841067502861 ) ) ;
#119689=CARTESIAN_POINT ( 'NONE',  ( 6.127403468923573904, 0.1463605449630276667, -1.964188589371117954 ) ) ;
#119690=CARTESIAN_POINT ( 'NONE',  ( 0.3748122768056568743, 1.812325467826606085, -0.6980362920307162655 ) ) ;
#119698=CARTESIAN_POINT ( 'NONE',  ( 5.373660369522260005, 0.3689257714810100786, -1.876182517032434216 ) ) ;
#119700=CARTESIAN_POINT ( 'NONE',  ( 0.3587983166186413109, 0.8468606107991830667, 2.038007455039527294 ) ) ;
#119702=CARTESIAN_POINT ( 'NONE',  ( 6.375645430456404306, 0.3419251235410331602, -1.983688181122665650 ) ) ;
#119706=CARTESIAN_POINT ( 'NONE',  ( 2.752462066230080495, -2.064650614848703825, -0.1547973748374023295 ) ) ;
#119711=CARTESIAN_POINT ( 'NONE',  ( 0.8487565004985967443, 0.6285140637429244004, 2.068326486519965979 ) ) ;
#119716=CARTESIAN_POINT ( 'NONE',  ( 6.825078400183550720, 7.629137130509051623, 2.555651831298339616 ) ) ;
#119718=CARTESIAN_POINT ( 'NONE',  ( 5.520041967268690897, -1.564255855279505836, 0.7489400339724672229 ) ) ;
#119722=CARTESIAN_POINT ( 'NONE',  ( 4.065334711822697678, 1.773058433220272789, 1.068561072119569522 ) ) ;
#119723=CARTESIAN_POINT ( 'NONE',  ( 4.939118062403117904, -1.789252976562827779, -1.131630611658622332 ) ) ;
#119726=CARTESIAN_POINT ( 'NONE',  ( 2.641402650619076198, 1.802640082279869382, -0.7936183362749064107 ) ) ;
#119727=CARTESIAN_POINT ( 'NONE',  ( 1.107505169401588274, 1.450017293480215352, 1.247013401884336403 ) ) ;
#119728=CARTESIAN_POINT ( 'NONE',  ( 4.629038687585553369, -2.096899809942855075, 0.9264041093646653291 ) ) ;
#119729=CARTESIAN_POINT ( 'NONE',  ( 3.017977635683791071, -0.9002817137206723386, -1.588204215665294461 ) ) ;
#119734=CARTESIAN_POINT ( 'NONE',  ( 4.377201702235844927, -1.800125857882298508, -0.9014936589236545172 ) ) ;
#119735=CARTESIAN_POINT ( 'NONE',  ( 3.168751141962049545, 1.424179589570490512, -1.349414796185027576 ) ) ;
#119738=CARTESIAN_POINT ( 'NONE',  ( 0.1753634416057497647, 2.004068818557998011, -2.558292918872175914 ) ) ;
#119739=CARTESIAN_POINT ( 'NONE',  ( 6.052696072153842977, -1.792546385985850810, -1.075631278504029620 ) ) ;
#119740=CARTESIAN_POINT ( 'NONE',  ( 4.188192146485575584, -1.750654529572701179, -0.2590412592250490587 ) ) ;
#119742=CARTESIAN_POINT ( 'NONE',  ( 0.7268461993804631316, 0.1648446022758827123, 2.185306563462440899 ) ) ;
#119743=CARTESIAN_POINT ( 'NONE',  ( 6.509682854689390119, -0.8273637111445523162, -1.531083434488962780 ) ) ;
#119745=CARTESIAN_POINT ( 'NONE',  ( 0.1333692844072801587, 4.087911462428309051, -2.608372271572469092 ) ) ;
#119746=CARTESIAN_POINT ( 'NONE',  ( 0.01170749999939314084, -0.7329999334961794233, -1.560365621481168086 ) ) ;
#119747=CARTESIAN_POINT ( 'NONE',  ( 0.4042330683431404892, 0.3962127685512468744, 2.263842283499896801 ) ) ;
#119748=CARTESIAN_POINT ( 'NONE',  ( 0.9432342461353732110, -1.730868645791438842, -1.344178957308760802 ) ) ;
#119749=CARTESIAN_POINT ( 'NONE',  ( 3.475398437264758833, 0.05438942809191970457, -2.206374867412825402 ) ) ;
#119750=CARTESIAN_POINT ( 'NONE',  ( 6.566846207931698487, 1.613421326539933531, -1.453093050198107861 ) ) ;
#119752=CARTESIAN_POINT ( 'NONE',  ( 1.288444443960437225, -0.7676182150243222591, -1.973457848717992569 ) ) ;
#119753=CARTESIAN_POINT ( 'NONE',  ( 3.656250000000002665, -1.895863743164003523, 0.7852924748301777225 ) ) ;
#119754=CARTESIAN_POINT ( 'NONE',  ( 6.727182134110194944, 2.413774403037728167, 2.569658639860139093 ) ) ;
#119755=CARTESIAN_POINT ( 'NONE',  ( 5.157218254430565807, -1.627291586725558181, -1.030705938667796140 ) ) ;
#119757=CARTESIAN_POINT ( 'NONE',  ( 1.523386150502318737, -2.156637510313658801, 0.7774349738483375960 ) ) ;
#119761=CARTESIAN_POINT ( 'NONE',  ( 3.229344874888330441, 2.008827177783510720, 0.9482931344305007837 ) ) ;
#119767=CARTESIAN_POINT ( 'NONE',  ( 2.320935597664942396, 0.9480396085976348086, -1.779626998253575509 ) ) ;
#119769=CARTESIAN_POINT ( 'NONE',  ( 1.375913251025398409, -2.013209319166248346, 0.4479213407221314669 ) ) ;
#119772=CARTESIAN_POINT ( 'NONE',  ( 6.339394973347380002, 0.6569538336487945607, -1.611921592020611582 ) ) ;
#119775=CARTESIAN_POINT ( 'NONE',  ( 2.917004591651660927, -0.1773711190117404635, 1.760840049638369154 ) ) ;
#119776=CARTESIAN_POINT ( 'NONE',  ( 1.301407962653992501, 1.352153127569672098, -1.496052916918483522 ) ) ;
#119777=CARTESIAN_POINT ( 'NONE',  ( 0.1164230846485321547, -0.09151219166612066525, 1.839079034809627755 ) ) ;
#119778=CARTESIAN_POINT ( 'NONE',  ( 5.003627799853592073, -2.281530862488420297, 0.2229171871234881530 ) ) ;
#119779=CARTESIAN_POINT ( 'NONE',  ( 3.064218985076866630, -1.701416833343888824, -0.7040189834505713451 ) ) ;
#119781=CARTESIAN_POINT ( 'NONE',  ( 3.627796970749700201, -1.086779551322129445, -1.466705181690882709 ) ) ;
#119782=CARTESIAN_POINT ( 'NONE',  ( 5.080704010962952211, -0.7231418808758652839, 1.882473355234378865 ) ) ;
#119784=CARTESIAN_POINT ( 'NONE',  ( 3.415140116862291908, 2.044469143995849780, 0.9693780919050251077 ) ) ;
#119786=CARTESIAN_POINT ( 'NONE',  ( -0.005051300619423290325, -0.4623140147347043483, -2.061856797492032545 ) ) ;
#119788=CARTESIAN_POINT ( 'NONE',  ( 3.209495720308676248, -1.691010085789945716, -1.194244797349801157 ) ) ;
#119791=CARTESIAN_POINT ( 'NONE',  ( 5.883467998083113493, 0.1561420574479575052, -2.114776682634044391 ) ) ;
#119795=CARTESIAN_POINT ( 'NONE',  ( 1.945805723040757051, 0.7375614711745586138, -1.779911670397672951 ) ) ;
#119797=CARTESIAN_POINT ( 'NONE',  ( 6.438338856661699694, -1.056498591242978957, 1.661895973567611540 ) ) ;
#119802=CARTESIAN_POINT ( 'NONE',  ( 0.4400545237335662940, -2.106857831338632359, 0.7043091553551988904 ) ) ;
#119803=CARTESIAN_POINT ( 'NONE',  ( 3.891714145839750838, 1.523869777361567479, 1.453819373739003051 ) ) ;
#119806=CARTESIAN_POINT ( 'NONE',  ( 0.8009387066525032184, -1.599029608822761128, 0.9519043452789009985 ) ) ;
#119811=CARTESIAN_POINT ( 'NONE',  ( 1.248456593208754795, 1.040400552670465162, -1.847740296886036582 ) ) ;
#119814=CARTESIAN_POINT ( 'NONE',  ( 4.035565188342554954, 1.848088059160474694, -0.6588067414724924076 ) ) ;
#119815=CARTESIAN_POINT ( 'NONE',  ( 1.920999885407469243, 2.016935458891587096, 0.7782144962657986387 ) ) ;
#119816=CARTESIAN_POINT ( 'NONE',  ( 1.276629239279066574, 1.701104413791530767, -0.7050613402737049284 ) ) ;
#119820=CARTESIAN_POINT ( 'NONE',  ( 3.626658729539467441, -1.607292185769314097, 0.6678421186538037180 ) ) ;
#119824=CARTESIAN_POINT ( 'NONE',  ( 0.8487565004985967443, 0.6285140637429244004, 2.068326486519965979 ) ) ;
#119826=CARTESIAN_POINT ( 'NONE',  ( 3.708361104356564297, -1.524809962200252444, -1.319026932540816599 ) ) ;
#119828=CARTESIAN_POINT ( 'NONE',  ( 0.3741789627117291239, 1.245922373857488274, 1.766349570875298758 ) ) ;
#119829=CARTESIAN_POINT ( 'NONE',  ( 3.379716691394366368, 1.249474069150168454, 1.524969178572218809 ) ) ;
#119832=CARTESIAN_POINT ( 'NONE',  ( 2.102980028956519476, -0.4233231936755370572, 1.895218400837359818 ) ) ;
#119833=CARTESIAN_POINT ( 'NONE',  ( 6.486579876843341808, -1.171037552013409089, 1.512559164390047783 ) ) ;
#119843=CARTESIAN_POINT ( 'NONE',  ( 0.5697015142280477118, 0.2141057807664332180, -2.196374807094509496 ) ) ;
#119845=CARTESIAN_POINT ( 'NONE',  ( 4.047668389856577065, 1.417901948909123799, 1.355967163993692992 ) ) ;
#119847=CARTESIAN_POINT ( 'NONE',  ( 1.916638904718031000, -1.319229391439219246, -1.525043083973671498 ) ) ;
#119849=CARTESIAN_POINT ( 'NONE',  ( 2.044302899665669138, 0.9103292306275132528, 1.911821358334654608 ) ) ;
#119853=CARTESIAN_POINT ( 'NONE',  ( 3.521284115754549582, -1.097709940230184200, -1.477957507169822104 ) ) ;
#119857=CARTESIAN_POINT ( 'NONE',  ( 3.515986968957810266, -0.6120941298391362473, 2.030368431519948391 ) ) ;
#119860=CARTESIAN_POINT ( 'NONE',  ( 4.973930670403752252, 1.183205397963146499, 1.687068388967316368 ) ) ;
#119862=CARTESIAN_POINT ( 'NONE',  ( 2.120424178990498731, 0.001545453418709194504, 1.841430844159386293 ) ) ;
#119868=CARTESIAN_POINT ( 'NONE',  ( 2.209865124170300898, -0.4819264253047173541, 2.153463223375853719 ) ) ;
#119869=CARTESIAN_POINT ( 'NONE',  ( 3.954570948191834745, 0.8096313216635497856, 2.112761250790657908 ) ) ;
#119871=CARTESIAN_POINT ( 'NONE',  ( 4.517698195727691157, -0.4766141805869225645, 1.747713001785702325 ) ) ;
#119872=CARTESIAN_POINT ( 'NONE',  ( 4.135878506090823414, 1.915180532728939289, -0.05283342432932899152 ) ) ;
#119875=CARTESIAN_POINT ( 'NONE',  ( 3.573081558413326864, 0.04979752193529430465, -1.971001165494235652 ) ) ;
#119876=CARTESIAN_POINT ( 'NONE',  ( 0.5516240470409677910, 0.6072917441693607143, -1.828224634575502883 ) ) ;
#119877=CARTESIAN_POINT ( 'NONE',  ( 4.557402362779487959, 0.4096945884842878582, -1.825068887194372991 ) ) ;
#119878=CARTESIAN_POINT ( 'NONE',  ( 3.633692980683305152, -2.132556294031516142, 0.8823059210255141949 ) ) ;
#119879=CARTESIAN_POINT ( 'NONE',  ( 4.756226040108163744, -1.860656195911802646, -0.04637829637440040592 ) ) ;
#119883=CARTESIAN_POINT ( 'NONE',  ( 1.699976503534783356, -0.7083771898081425711, 1.983499743616623956 ) ) ;
#119888=CARTESIAN_POINT ( 'NONE',  ( 3.305043459179863419, -0.4174351347619070229, -2.078937965663613774 ) ) ;
#119890=CARTESIAN_POINT ( 'NONE',  ( 0.7209703750307445702, 1.526537956607315172, -1.322641891180293516 ) ) ;
#119897=CARTESIAN_POINT ( 'NONE',  ( 1.862795570070171713, -1.530026953448139659, 1.527182012981804560 ) ) ;
#119900=CARTESIAN_POINT ( 'NONE',  ( 6.825078400183570260, 4.696493799637426747, 2.518305144748238966 ) ) ;
#119903=CARTESIAN_POINT ( 'NONE',  ( 5.753138727196851043, 0.1435251449807967150, -2.011451301405759118 ) ) ;
#119905=CARTESIAN_POINT ( 'NONE',  ( 0.2225716830646235489, 2.098996182288978218, 0.6302611576235671587 ) ) ;
#119907=CARTESIAN_POINT ( 'NONE',  ( 1.552057811931725428, 0.6552935188219483065, -2.165526471026494537 ) ) ;
#119914=CARTESIAN_POINT ( 'NONE',  ( 4.266008093515370803, 0.8158808812368329999, 1.519711535667643609 ) ) ;
#119916=CARTESIAN_POINT ( 'NONE',  ( 1.914973420724352726, -0.2224279105748054597, 1.755648307094020311 ) ) ;
#119917=CARTESIAN_POINT ( 'NONE',  ( 2.877592485514004039, 0.2932790309252801819, -1.991490711024199944 ) ) ;
#119918=CARTESIAN_POINT ( 'NONE',  ( 4.805825877545530922, -0.5924843665619135002, 2.125676689404366826 ) ) ;
#119920=CARTESIAN_POINT ( 'NONE',  ( 3.867448311701796371, -1.681569574351711838, -1.118542113429069396 ) ) ;
#119922=CARTESIAN_POINT ( 'NONE',  ( 5.883467998083113493, 0.1561420574479575329, -2.114776682634044391 ) ) ;
#119923=CARTESIAN_POINT ( 'NONE',  ( 3.691029940746898053, 1.730877988113326493, 1.034147909374658170 ) ) ;
#119924=CARTESIAN_POINT ( 'NONE',  ( 4.148556159002002808, 1.777816924242316299, 0.3471830323657533746 ) ) ;
#119927=CARTESIAN_POINT ( 'NONE',  ( 1.059204734455133412, 0.3686402435371800568, -1.833797362824276078 ) ) ;
#119929=CARTESIAN_POINT ( 'NONE',  ( 5.971335983229998590, -1.557292021941504734, -0.9250951156042800383 ) ) ;
#119934=CARTESIAN_POINT ( 'NONE',  ( 0.2637284958507991606, 0.5978344860198721022, -1.816641584731902626 ) ) ;
#119937=CARTESIAN_POINT ( 'NONE',  ( 1.943732651021431224, 1.350599318427040840, 1.423195245143428433 ) ) ;
#119938=PLANE ( 'NONE',  #78773 ) ;
#119940=CARTESIAN_POINT ( 'NONE',  ( 4.078469121099765005, 1.002472831208834680, 1.868716877859360137 ) ) ;
#119942=CARTESIAN_POINT ( 'NONE',  ( 5.430923302262330665, 0.1424395525144121211, 1.966244542718327715 ) ) ;
#119944=CARTESIAN_POINT ( 'NONE',  ( 1.265886429849511163, 0.5802531365422005649, -1.927800331509860632 ) ) ;
#119947=CARTESIAN_POINT ( 'NONE',  ( 0.8962975493561256002, -0.9559892387472949116, -1.889204697816506240 ) ) ;
#119949=CARTESIAN_POINT ( 'NONE',  ( 2.295452831283749440, -1.850383948470477602, 0.9288054807428181014 ) ) ;
#119953=CARTESIAN_POINT ( 'NONE',  ( 4.382818795122591204, 1.867623683829922054, -0.9396962251831328938 ) ) ;
#119955=CARTESIAN_POINT ( 'NONE',  ( 3.276193339942961913, -1.088440757138483539, 1.465454812695582643 ) ) ;
#119956=CARTESIAN_POINT ( 'NONE',  ( 1.840194262915356260, 1.042575051921472040, -1.481162322861505620 ) ) ;
#119958=CARTESIAN_POINT ( 'NONE',  ( 6.375609195709820654, 2.113139023092651225, -0.6363509056886568205 ) ) ;
#119961=CARTESIAN_POINT ( 'NONE',  ( 5.877994779194309238, 1.310017027744770246, 1.775731318763192013 ) ) ;
#119965=CARTESIAN_POINT ( 'NONE',  ( 3.563058999304801411, -1.561743426874351970, 1.103242700682869781 ) ) ;
#119968=CARTESIAN_POINT ( 'NONE',  ( 6.285608408418759119, -1.950803066209889636, 0.6937918898708081983 ) ) ;
#119970=CARTESIAN_POINT ( 'NONE',  ( 6.497619750234602698, -2.191128968173004843, 0.05151875470104508997 ) ) ;
#119975=CARTESIAN_POINT ( 'NONE',  ( 3.567518508692040236, 1.825626599287116791, -0.4067673385957787380 ) ) ;
#119976=CARTESIAN_POINT ( 'NONE',  ( -0.02319159430947542733, 0.7471999394491578572, -1.895068635927643630 ) ) ;
#119983=CARTESIAN_POINT ( 'NONE',  ( 6.561392567526037389, 1.717850402480676664, 1.155108059606273052 ) ) ;
#119984=CARTESIAN_POINT ( 'NONE',  ( 1.476185646619165626, -2.006963189339417308, -0.1948195631672477446 ) ) ;
#119988=CARTESIAN_POINT ( 'NONE',  ( 1.148660753082946240, -1.725648174752218100, 1.350667304935410318 ) ) ;
#119989=CARTESIAN_POINT ( 'NONE',  ( 6.358013415952256331, 1.820405254634300363, -0.1396899356524081148 ) ) ;
#119996=CARTESIAN_POINT ( 'NONE',  ( 4.335397732480402055, 0.7831895168094182846, -1.666506522714307437 ) ) ;
#119997=CARTESIAN_POINT ( 'NONE',  ( 0.5221354380547962304, -2.003184638039813503, 0.1996226354380666868 ) ) ;
#119998=CARTESIAN_POINT ( 'NONE',  ( 2.073957380999270850, 1.703569143382680506, -1.543048383257297207 ) ) ;
#120000=CARTESIAN_POINT ( 'NONE',  ( 6.157081138237819218, 1.605775322519078729, -1.126676614267435150 ) ) ;
#120004=CARTESIAN_POINT ( 'NONE',  ( 4.886922752366290368, -1.802716094696995786, -0.6387714794457154399 ) ) ;
#120008=CARTESIAN_POINT ( 'NONE',  ( 2.788710525494293879, 1.791885054564039903, -1.076980376859866029 ) ) ;
#120009=CARTESIAN_POINT ( 'NONE',  ( 2.571000202304725590, 0.09389976206976291540, -1.868427151830873267 ) ) ;
#120012=CARTESIAN_POINT ( 'NONE',  ( 3.210250486799534286, 1.574880741971116827, 0.7411356085459307463 ) ) ;
#120016=CARTESIAN_POINT ( 'NONE',  ( 4.389066697632080682, 1.539216480442310075, -0.7786167122535156970 ) ) ;
#120017=CARTESIAN_POINT ( 'NONE',  ( 4.071962858106247474, -1.261020321617589479, 1.792237525612811355 ) ) ;
#120018=CARTESIAN_POINT ( 'NONE',  ( 6.164705905600972535, -1.563586322211576674, 1.557672334054376773 ) ) ;
#120021=CARTESIAN_POINT ( 'NONE',  ( 3.081114545232612301, 2.042771114613873173, 0.7355539269583191153 ) ) ;
#120022=CARTESIAN_POINT ( 'NONE',  ( 1.752308680507021155, 0.5713779359179693706, 1.734036872924920702 ) ) ;
#120024=CARTESIAN_POINT ( 'NONE',  ( 4.223895228407223534, 0.9020499113536835090, -1.915681561053275139 ) ) ;
#120026=CARTESIAN_POINT ( 'NONE',  ( 5.109026413134919231, -0.3384823820529453964, 2.267118282965301379 ) ) ;
#120028=CARTESIAN_POINT ( 'NONE',  ( 6.620655732516656400, 2.994310854299454316, 2.180639477081049993 ) ) ;
#120031=CARTESIAN_POINT ( 'NONE',  ( 0.6277789859737945566, -0.3070864893036719945, 2.098006834332386994 ) ) ;
#120039=CARTESIAN_POINT ( 'NONE',  ( 5.168592345394213972, 1.356298078840772803, 1.492257005506092193 ) ) ;
#120041=CARTESIAN_POINT ( 'NONE',  ( 4.205966187000295342, 0.6995128471476423915, -1.940432845919232374 ) ) ;
#120043=CARTESIAN_POINT ( 'NONE',  ( -0.1411974294642332484, 2.879603353482541817, -2.388950311486548461 ) ) ;
#120047=CARTESIAN_POINT ( 'NONE',  ( 0.3750906047784249853, 1.949931092985623726, -0.7544815049443721611 ) ) ;
#120048=CARTESIAN_POINT ( 'NONE',  ( 4.360000113718985659, -0.002809843368253156070, -2.016597020062675050 ) ) ;
#120049=CARTESIAN_POINT ( 'NONE',  ( 3.456447201099471123, -1.625387274077850996, -0.8650149607793489182 ) ) ;
#120053=CARTESIAN_POINT ( 'NONE',  ( 0.6391468373067762387, -1.214715217071378195, -1.224744053251116904 ) ) ;
#120055=CARTESIAN_POINT ( 'NONE',  ( 0.6690544563107813092, 1.549219078230345215, 1.698357357312555660 ) ) ;
#120057=CARTESIAN_POINT ( 'NONE',  ( 6.438354578037611908, 2.236760482230481184, 0.3397759937929164531 ) ) ;
#120058=CARTESIAN_POINT ( 'NONE',  ( 3.387430394310109616, 1.903944824823229798, -0.9005924351132842398 ) ) ;
#120062=CARTESIAN_POINT ( 'NONE',  ( 6.125000000000003553, -2.052068128417929849, 3.487440458529189440E-13 ) ) ;
#120067=CARTESIAN_POINT ( 'NONE',  ( 2.478903650112133317, -1.459102030866548994, 1.539066919819010781 ) ) ;
#120068=CARTESIAN_POINT ( 'NONE',  ( 3.568779976319371272, 0.8023129380761647722, 2.071619486725768677 ) ) ;
#120069=CARTESIAN_POINT ( 'NONE',  ( 2.519692321801832335, -1.262790281060278907, -1.790845962237663791 ) ) ;
#120072=CARTESIAN_POINT ( 'NONE',  ( 5.846142468697441252, -0.8834969228576605715, 1.751761657833034613 ) ) ;
#120077=CARTESIAN_POINT ( 'NONE',  ( 5.133110336712339183, 1.960249873928998410, 0.8093987030339530042 ) ) ;
#120081=CARTESIAN_POINT ( 'NONE',  ( 6.473507614529132148, 2.070149491355821159, -0.6224772505839873959 ) ) ;
#120083=CARTESIAN_POINT ( 'NONE',  ( 5.179192671508887180, 1.240781939916297372, 1.360553736468192554 ) ) ;
#120087=CARTESIAN_POINT ( 'NONE',  ( 1.258879523317941285, 1.714807473692409268, -0.2965960235774521836 ) ) ;
#120091=CARTESIAN_POINT ( 'NONE',  ( 4.926735330553584369, 2.067573386176469796, 0.6309256262674377558 ) ) ;
#120094=CARTESIAN_POINT ( 'NONE',  ( 5.155217493315787713, -1.824165352752779246, -1.159627250419709155 ) ) ;
#120095=CARTESIAN_POINT ( 'NONE',  ( 4.780523264075623224, -1.911459794658072697, -0.4817293046612564633 ) ) ;
#120096=CARTESIAN_POINT ( 'NONE',  ( 4.217908468276907463, -1.441162302510163640, -0.9635822893686758484 ) ) ;
#120097=CARTESIAN_POINT ( 'NONE',  ( 0.7498831369015904746, 2.188782640433343474, -0.1130235578899463078 ) ) ;
#120098=CARTESIAN_POINT ( 'NONE',  ( 1.835461723582560767, 0.2275736305563350881, 2.296322244814374081 ) ) ;
#120099=CARTESIAN_POINT ( 'NONE',  ( 3.725900457647839392, -1.224662966953151688, -1.657274842633131851 ) ) ;
#120100=CARTESIAN_POINT ( 'NONE',  ( 6.233930015136599501, 1.921560620327814606, 0.2806146417165931717 ) ) ;
#120107=CARTESIAN_POINT ( 'NONE',  ( 3.171135245091468491, -2.038329301889611589, -0.8460836234857532778 ) ) ;
#120110=CARTESIAN_POINT ( 'NONE',  ( 6.977413161700751765, -0.1449424838519241254, 1.929857014940839832 ) ) ;
#120114=CARTESIAN_POINT ( 'NONE',  ( 6.825078400183510752, 2.433016701115862102, 2.426111979085682879 ) ) ;
#120117=CARTESIAN_POINT ( 'NONE',  ( 2.905207415116388248, 1.740275362031361794, 1.103647167516639938 ) ) ;
#120119=UNCERTAINTY_MEASURE_WITH_UNIT (LENGTH_MEASURE( 1.000000000000000082E-05 ), #30165, 'distance_accuracy_value', 'NONE');
#120125=CARTESIAN_POINT ( 'NONE',  ( 2.043891306636512528, 0.7897949731258145922, -1.903750762553678921 ) ) ;
#120131=CARTESIAN_POINT ( 'NONE',  ( 5.865903189996044098, 2.174886565178067777, -0.3735607071253948530 ) ) ;
#120132=CARTESIAN_POINT ( 'NONE',  ( 0.6675187767142229944, 0.2125181155594977611, -2.151144519195991922 ) ) ;
#120134=CARTESIAN_POINT ( 'NONE',  ( 0.6906390985809904848, 1.523792322931913468, -1.320830384837400118 ) ) ;
#120135=CARTESIAN_POINT ( 'NONE',  ( 1.617049182541079544, 0.6662764605713987764, -2.199669867806148371 ) ) ;
#120138=DIRECTION ( 'NONE',  ( 1.016547956922408957E-15, 1.000000000000000000, -4.622230424712075819E-32 ) ) ;
#120139=CARTESIAN_POINT ( 'NONE',  ( 1.533845512228737551, 0.9248708299973290581, -1.625957014461040906 ) ) ;
#120140=CARTESIAN_POINT ( 'NONE',  ( 3.626185617424378282, 2.007256095728218614, 0.1928357053486499662 ) ) ;
#120142=CARTESIAN_POINT ( 'NONE',  ( 6.639320575229255894, 6.035237531390704291, 2.698156163645454964 ) ) ;
#120144=CARTESIAN_POINT ( 'NONE',  ( 4.582709122986449835, -2.042650070554121733, -0.5124292222106421324 ) ) ;
#120150=CARTESIAN_POINT ( 'NONE',  ( 4.570572472720978219, 0.7768735290680817140, 1.864611197846306911 ) ) ;
#120153=CARTESIAN_POINT ( 'NONE',  ( 0.3036763228623740041, -1.592034637876770908, -1.310935287704196206 ) ) ;
#120155=CARTESIAN_POINT ( 'NONE',  ( 6.081358973892867503, 1.999796440023202448, -0.8210498935554910727 ) ) ;
#120159=CARTESIAN_POINT ( 'NONE',  ( -0.1106856583841061281, -0.002128758811529350356, -1.996853503091333693 ) ) ;
#120161=CARTESIAN_POINT ( 'NONE',  ( 2.682273331476907607, -1.248350377418592672, -1.776241996044833238 ) ) ;
#120163=CARTESIAN_POINT ( 'NONE',  ( 2.243484787601189634, 1.840893492186860492, 0.04347913094143729396 ) ) ;
#120165=CARTESIAN_POINT ( 'NONE',  ( 3.667680160636753506, 1.218766932906123479, 1.821211977396507198 ) ) ;
#120167=CARTESIAN_POINT ( 'NONE',  ( 5.120128864776952504, -1.205885850527373293, -1.914207236704228654 ) ) ;
#120174=CARTESIAN_POINT ( 'NONE',  ( 4.903428802837151324, -0.4723676116331463892, 1.705421244663980263 ) ) ;
#120176=( BOUNDED_SURFACE ( )  B_SPLINE_SURFACE ( 3, 3, ( 
 ( #100584, #183961, #52898, #86471, #152536, #17178, #4121, #66985, #34511, #70190 ),
 ( #136302, #169849, #53974, #186090, #37721, #103799, #49701, #134186, #182895, #166658 ),
 ( #18248, #35572, #101652, #88621, #73408, #39865, #139511, #58240, #90761, #124396 ),
 ( #72332, #156822, #141668, #138438, #105974, #154676, #87544, #71260, #155746, #6261 ),
 ( #137374, #109199, #171996, #104872, #107047, #204456, #56110, #23588, #153613, #74495 ),
 ( #122268, #55043, #205538, #188225, #89696, #190354, #7331, #38790, #25725, #57175 ),
 ( #203390, #121192, #123337, #207679, #157893, #5184, #140600, #189301, #40941, #22511 ) ),
 .UNSPECIFIED., .T., .F., .T. ) 
 B_SPLINE_SURFACE_WITH_KNOTS ( ( 4, 3, 4 ),
 ( 4, 1, 1, 1, 1, 1, 1, 4 ),
 ( 0.000000000000000000, 0.5000000000000000000, 1.000000000000000000 ),
 ( 0.000000000000000000, 0.09123828766142533242, 0.1830323254715014447, 0.2554767746403809325, 0.3605042187413262100, 0.5206858269973231312, 0.7335850107976985557, 1.000000000000000000 ),
 .UNSPECIFIED. ) 
 GEOMETRIC_REPRESENTATION_ITEM ( )  RATIONAL_B_SPLINE_SURFACE ( (
 ( 1.000000000000000000, 1.000000000000000000, 1.000000000000000000, 0.9999999999999997780, 1.000000000000000000, 1.000000000000000000, 1.000000000000000222, 1.000000000000000000, 1.000000000000000000, 1.000000000000000000),
 ( 0.3333333333333333703, 0.3333333333333333703, 0.3333333333333334259, 0.3333333333333332593, 0.3333333333333333703, 0.3333333333333333703, 0.3333333333333334814, 0.3333333333333333703, 0.3333333333333333703, 0.3333333333333333703),
 ( 0.3333333333333333703, 0.3333333333333333703, 0.3333333333333334259, 0.3333333333333332593, 0.3333333333333333703, 0.3333333333333333703, 0.3333333333333334814, 0.3333333333333333703, 0.3333333333333333703, 0.3333333333333333703),
 ( 1.000000000000000000, 1.000000000000000000, 1.000000000000000000, 0.9999999999999997780, 1.000000000000000000, 1.000000000000000000, 1.000000000000000222, 1.000000000000000000, 1.000000000000000000, 1.000000000000000000),
 ( 0.3333333333333333703, 0.3333333333333333703, 0.3333333333333334259, 0.3333333333333332593, 0.3333333333333333703, 0.3333333333333333703, 0.3333333333333334814, 0.3333333333333333703, 0.3333333333333333703, 0.3333333333333333703),
 ( 0.3333333333333333703, 0.3333333333333333703, 0.3333333333333334259, 0.3333333333333332593, 0.3333333333333333703, 0.3333333333333333703, 0.3333333333333334814, 0.3333333333333333703, 0.3333333333333333703, 0.3333333333333333703),
 ( 1.000000000000000000, 1.000000000000000000, 1.000000000000000000, 0.9999999999999997780, 1.000000000000000000, 1.000000000000000000, 1.000000000000000222, 1.000000000000000000, 1.000000000000000000, 1.000000000000000000) ) ) 
 REPRESENTATION_ITEM ( '' )  SURFACE ( )  );
#120178=CARTESIAN_POINT ( 'NONE',  ( 1.870285774507766119, 1.081916120455215902, 1.806640566525853808 ) ) ;
#120181=CARTESIAN_POINT ( 'NONE',  ( 2.365619736264668038, -0.4344343780767513374, 1.920862584678226348 ) ) ;
#120184=CARTESIAN_POINT ( 'NONE',  ( 5.959207022242491547, -1.525490245149653701, 0.9768169865009832531 ) ) ;
#120189=CARTESIAN_POINT ( 'NONE',  ( 4.979306205331720747, 1.745251617482036943, -0.6738592683939447214 ) ) ;
#120190=CARTESIAN_POINT ( 'NONE',  ( 5.770397209236588942, -0.9257025293247715947, -1.851810055641222252 ) ) ;
#120201=CARTESIAN_POINT ( 'NONE',  ( 5.072687121480487171, 1.354251660176824856, -1.419695456575476689 ) ) ;
#120203=CARTESIAN_POINT ( 'NONE',  ( 3.110703712691643918, 0.7282687159771012997, -1.880146464672841411 ) ) ;
#120204=CARTESIAN_POINT ( 'NONE',  ( 3.081152777801674958, 1.513245778044673306, 1.174690267158661872 ) ) ;
#120206=CARTESIAN_POINT ( 'NONE',  ( 0.2401087780563165297, 2.186128513634697512, 0.1550312349237955856 ) ) ;
#120208=CARTESIAN_POINT ( 'NONE',  ( 2.653401028632852654, 0.5028369177751991215, -1.801603059227441239 ) ) ;
#120210=CARTESIAN_POINT ( 'NONE',  ( 4.342045473679829293, -1.241779438462310203, -1.584497923379190931 ) ) ;
#120214=CARTESIAN_POINT ( 'NONE',  ( 4.640305734921336800, 0.8116497034467985427, 1.955664341570842790 ) ) ;
#120216=CARTESIAN_POINT ( 'NONE',  ( 6.057099581687969803, 1.694805161836069107, -1.188877858866774107 ) ) ;
#120217=CARTESIAN_POINT ( 'NONE',  ( 1.224293845215556953, 2.015865829440838031, 0.5543246906533367824 ) ) ;
#120219=CARTESIAN_POINT ( 'NONE',  ( 6.668987789458199700, -1.670617902683011025, -0.7365018021969899076 ) ) ;
#120229=CARTESIAN_POINT ( 'NONE',  ( 0.7327119416217167114, 1.673282569690562882, 0.6944263290599298477 ) ) ;
#120236=CARTESIAN_POINT ( 'NONE',  ( 5.853138716089107518, 0.1455171034051294665, -2.011206573937059261 ) ) ;
#120237=CARTESIAN_POINT ( 'NONE',  ( 0.1531979293848736434, 0.3668625560977051281, 2.088361607889513305 ) ) ;
#120242=CARTESIAN_POINT ( 'NONE',  ( 3.414863416077691838, -1.494280747806640885, 1.283048038104795507 ) ) ;
#120243=CARTESIAN_POINT ( 'NONE',  ( 4.605092316430917876, -0.09611821078869468848, 2.014234682242924457 ) ) ;
#120246=CARTESIAN_POINT ( 'NONE',  ( 6.727182134110200273, -0.004969159814478123736, 2.189081792362323586 ) ) ;
#120247=CARTESIAN_POINT ( 'NONE',  ( 4.945371362016417471, 0.6893947036107104243, -2.080263006054481334 ) ) ;
#120249=CARTESIAN_POINT ( 'NONE',  ( 3.381779240904962069, 1.220913077095790111, 1.490098802054098837 ) ) ;
#120251=CARTESIAN_POINT ( 'NONE',  ( -0.02948999725180690215, 0.001137248348246927814, -1.926291057026579656 ) ) ;
#120252=CARTESIAN_POINT ( 'NONE',  ( -0.004863692847738298151, -0.4900785244342681923, -2.159743284330918112 ) ) ;
#120257=CARTESIAN_POINT ( 'NONE',  ( 4.662928361469391270, 1.524974937183399160, -1.246301010749743199 ) ) ;
#120259=CARTESIAN_POINT ( 'NONE',  ( 0.7142757748631656245, 1.794906310038762109, 0.7420174003010558961 ) ) ;
#120260=CARTESIAN_POINT ( 'NONE',  ( 3.967443207080887380, -1.674941000623398457, -1.116458483097344301 ) ) ;
#120262=CARTESIAN_POINT ( 'NONE',  ( 5.554211264220430877, 2.030576384096828502, -1.076727444025220803 ) ) ;
#120264=CARTESIAN_POINT ( 'NONE',  ( 3.801460577334394575, -1.406423387113703960, -1.218697170607488944 ) ) ;
#120269=CARTESIAN_POINT ( 'NONE',  ( 0.1170720436180875679, -0.1011795954627830590, 2.189343785608413917 ) ) ;
#120271=EDGE_CURVE ( 'NONE', #39684, #12895, #3595, .T. ) ;
#120272=CARTESIAN_POINT ( 'NONE',  ( 6.825078400183575589, 7.629137130509070275, 2.455651831298297338 ) ) ;
#120274=CARTESIAN_POINT ( 'NONE',  ( 1.031563979315492485, -1.156294252604734396, -1.412831148817683680 ) ) ;
#120276=CARTESIAN_POINT ( 'NONE',  ( 2.672175078814063909, 1.228020439816409848, 1.224710958539473094 ) ) ;
#120278=CARTESIAN_POINT ( 'NONE',  ( 6.509000000000053632, 6.037921079186737927, 2.494901127718162304 ) ) ;
#120281=CARTESIAN_POINT ( 'NONE',  ( 5.988856447087389512, -0.2726756491404982441, -1.805090154579996442 ) ) ;
#120282=CARTESIAN_POINT ( 'NONE',  ( 3.485159065011545376, 0.04355839926390054490, 1.961427607708135179 ) ) ;
#120287=CARTESIAN_POINT ( 'NONE',  ( 3.985108911058360182, -1.979049277059058864, -0.7619450576143712572 ) ) ;
#120288=CARTESIAN_POINT ( 'NONE',  ( 6.827182134110199918, 7.629137130509069387, 2.789055895399249252 ) ) ;
#120292=CARTESIAN_POINT ( 'NONE',  ( 2.237250781069185734, -0.09733102107959036575, -2.068066387140480522 ) ) ;
#120295=CARTESIAN_POINT ( 'NONE',  ( 4.688250436721117964, 1.278455086129190121, 1.816331037743470933 ) ) ;
#120297=CARTESIAN_POINT ( 'NONE',  ( 1.829147786997789016, 0.8750025983248543859, -2.125820487401499204 ) ) ;
#120301=CARTESIAN_POINT ( 'NONE',  ( 6.509000000000010999, 0.004788705324892603143, 2.000274819378269786 ) ) ;
#120303=CARTESIAN_POINT ( 'NONE',  ( 3.287273477832891366, 0.04233216220104508987, -1.912079899511004433 ) ) ;
#120305=CARTESIAN_POINT ( 'NONE',  ( 4.155083606764530479, -1.434382041474260516, -0.9574503856549732017 ) ) ;
#120306=CARTESIAN_POINT ( 'NONE',  ( 1.762908039156896978, -0.1037823317905466058, -2.014007988105172231 ) ) ;
#120307=CARTESIAN_POINT ( 'NONE',  ( 3.674713919220749414, 1.665813291469726787, 1.584223201981638685 ) ) ;
#120309=CARTESIAN_POINT ( 'NONE',  ( 6.445935634123193481, 0.8078061350838610100, -1.945192272397469280 ) ) ;
#120312=CARTESIAN_POINT ( 'NONE',  ( 5.008955365368598756, 1.539791945809299012, 0.8722439129504773181 ) ) ;
#120314=CARTESIAN_POINT ( 'NONE',  ( 0.3227791477718846558, 2.195406398872503217, 0.6593016323864949735 ) ) ;
#120315=CARTESIAN_POINT ( 'NONE',  ( 6.509700743154069436, -0.8726169035938921015, -1.621212818125779220 ) ) ;
#120317=CARTESIAN_POINT ( 'NONE',  ( 5.824229312739954700, 2.111140916326431416, 0.5876101183235474812 ) ) ;
#120321=CARTESIAN_POINT ( 'NONE',  ( 0.5026746641029911089, 2.165404592850531440, 0.1593437185135812284 ) ) ;
#120322=CARTESIAN_POINT ( 'NONE',  ( 1.411342602523330214, -1.897109289313268166, 0.6839406069230756779 ) ) ;
#120324=CARTESIAN_POINT ( 'NONE',  ( 4.195867187722844172, -0.7361232629885716694, 1.780507395703424978 ) ) ;
#120326=CARTESIAN_POINT ( 'NONE',  ( 0.7389115964958146154, 1.317144317036992973, -1.788695212975628168 ) ) ;
#120335=CARTESIAN_POINT ( 'NONE',  ( 3.790341827058436142, 1.467891733132551613, -0.9347920342070329403 ) ) ;
#120337=CARTESIAN_POINT ( 'NONE',  ( 2.805073129645048624, -1.632656238785214597, 1.087510969322850629 ) ) ;
#120342=CARTESIAN_POINT ( 'NONE',  ( 0.3618804954101816906, -0.5516051106895186740, 1.987472385349927428 ) ) ;
#120345=CARTESIAN_POINT ( 'NONE',  ( 5.155482549980198392, 1.942097955248718533, -0.5424665614216088727 ) ) ;
#120346=CARTESIAN_POINT ( 'NONE',  ( 0.7610528644104715967, -1.636749228899089470, 1.562301092707372607 ) ) ;
#120350=CARTESIAN_POINT ( 'NONE',  ( 1.704156511045151978, -0.6684128243485131238, -1.747238085743174185 ) ) ;
#120351=CARTESIAN_POINT ( 'NONE',  ( -0.08779760418278770295, -1.063538860511966444, -1.369745729481768759 ) ) ;
#120353=CARTESIAN_POINT ( 'NONE',  ( 4.335597073515660149, 0.9364531651635084053, -1.981528385891350386 ) ) ;
#120354=CARTESIAN_POINT ( 'NONE',  ( 5.561655955723623812, 0.4570820274143985729, -2.261718950934066275 ) ) ;
#120355=CARTESIAN_POINT ( 'NONE',  ( 0.4618819262211275034, 2.038552468250200533, -0.3016747405163843765 ) ) ;
#120356=CARTESIAN_POINT ( 'NONE',  ( 3.328005318368632892, 1.894807597966931878, 0.4246257584521081485 ) ) ;
#120362=CARTESIAN_POINT ( 'NONE',  ( 4.201796189063250253, 1.844709454618495670, 0.8146275914719460776 ) ) ;
#120366=CARTESIAN_POINT ( 'NONE',  ( 0.8908993799596062191, 1.611356928563783208, -0.8583080905386344384 ) ) ;
#120372=CARTESIAN_POINT ( 'NONE',  ( 0.2159880523044250267, -2.119658899406823505, 0.4233941889316418239 ) ) ;
#120376=CARTESIAN_POINT ( 'NONE',  ( 5.496742197731416368, -1.970900515782060936, -0.4404336293717215356 ) ) ;
#120377=CARTESIAN_POINT ( 'NONE',  ( 5.496814983966967993, -2.166796134289544984, -0.4884321829702345519 ) ) ;
#120381=CARTESIAN_POINT ( 'NONE',  ( 5.243067039532245843, -1.768777590322716309, 1.057421601032474623 ) ) ;
#120382=CARTESIAN_POINT ( 'NONE',  ( 4.377577386359387646, -0.4445010797573499817, -1.966645064109616481 ) ) ;
#120390=CARTESIAN_POINT ( 'NONE',  ( 4.042342166264912606, 1.899327733865597168, -0.6766104081444989093 ) ) ;
#120391=CARTESIAN_POINT ( 'NONE',  ( 3.820104440490858622, 1.748809976318686177, 0.5759312369505511509 ) ) ;
#120393=CARTESIAN_POINT ( 'NONE',  ( 2.438448314377542392, 1.086391669559241047, -2.035977865114136254 ) ) ;
#120395=CARTESIAN_POINT ( 'NONE',  ( 4.710339443014814442, -0.9195336665917231977, -1.956380038831563972 ) ) ;
#120397=CARTESIAN_POINT ( 'NONE',  ( 0.5736477084636192325, -1.077812090576779402, 1.615333711560530849 ) ) ;
#120401=CARTESIAN_POINT ( 'NONE',  ( 2.535844406030359544, 0.8837261853790435717, -1.648756255988912400 ) ) ;
#120402=CARTESIAN_POINT ( 'NONE',  ( 0.4210825541404016326, -0.1013260788591107547, 1.968891031686560211 ) ) ;
#120405=CARTESIAN_POINT ( 'NONE',  ( 2.016531038934398445, -1.041976349804032420, -1.945408382319254503 ) ) ;
#120412=CARTESIAN_POINT ( 'NONE',  ( 6.174684870424203886, -1.871919000353940099, -0.6187097519457245287 ) ) ;
#120413=CARTESIAN_POINT ( 'NONE',  ( 0.4468379896771547122, 2.301730118641607703, 0.1654463548556948105 ) ) ;
#120414=CARTESIAN_POINT ( 'NONE',  ( 0.6780837441340243910, -1.046368970337024473, -1.659334490400856454 ) ) ;
#120416=CARTESIAN_POINT ( 'NONE',  ( 3.713784835328519218, 0.5057260441109856508, -1.999473844451674642 ) ) ;
#120424=CARTESIAN_POINT ( 'NONE',  ( 6.250449712397290192, -2.160098187209258835, -0.2192636458223720386 ) ) ;
#120426=CARTESIAN_POINT ( 'NONE',  ( 5.407694413872749628, -0.8332299576223768378, -1.642021276980778932 ) ) ;
#120429=CARTESIAN_POINT ( 'NONE',  ( 0.2978465640060874997, -1.869987984933557890, -0.05268733258671080832 ) ) ;
#120435=CARTESIAN_POINT ( 'NONE',  ( 2.395042364772178356, 1.366200922416866526, 1.125074557178520118 ) ) ;
#120437=CARTESIAN_POINT ( 'NONE',  ( 6.076820132975093713, -1.421968828841757126, 1.425219213311772926 ) ) ;
#120439=CARTESIAN_POINT ( 'NONE',  ( 4.288635103545942684, 1.478190772419993415, -1.218367487985058339 ) ) ;
#120441=CARTESIAN_POINT ( 'NONE',  ( 5.318794011649015552, -1.427836685786993742, 1.356881127696080158 ) ) ;
#120442=CARTESIAN_POINT ( 'NONE',  ( 0.07077104593807002908, 0.8175350930016941353, 1.956879683024402183 ) ) ;
#120444=CARTESIAN_POINT ( 'NONE',  ( 2.957714569337116295, 1.861795396119047208, -0.1817069356538636715 ) ) ;
#120445=CARTESIAN_POINT ( 'NONE',  ( 6.604117967919251875, -1.724316898024110811, 0.05080964468639861259 ) ) ;
#120447=CARTESIAN_POINT ( 'NONE',  ( 3.633602750639616019, -2.039237483250630589, 0.8441791899983088765 ) ) ;
#120450=CARTESIAN_POINT ( 'NONE',  ( 0.2563952634283462872, -2.062181505987520147, -0.05231737696831904177 ) ) ;
#120459=VERTEX_POINT ( 'NONE', #167119 ) ;
#120460=CARTESIAN_POINT ( 'NONE',  ( 2.717306809760032138, -1.800131872397674471, -1.022606600864908399 ) ) ;
#120464=CARTESIAN_POINT ( 'NONE',  ( 1.014326189163064607, -2.019862491587170350, 0.002270882547714125031 ) ) ;
#120468=CARTESIAN_POINT ( 'NONE',  ( 0.1747926744264451659, 0.2546335194838904581, -1.890750172325323275 ) ) ;
#120470=CARTESIAN_POINT ( 'NONE',  ( 6.081407632663145435, 1.356090666932512789, -1.492028312255622824 ) ) ;
#120471=CARTESIAN_POINT ( 'NONE',  ( 5.682812683241409424, 1.562005318756795713, -1.108807820749290851 ) ) ;
#120473=CARTESIAN_POINT ( 'NONE',  ( 3.474349307649237328, -2.112600797985896950, -0.5827812199917583591 ) ) ;
#120475=CARTESIAN_POINT ( 'NONE',  ( 2.882959773793275726, -1.768624019741386277, -0.7279546805132871556 ) ) ;
#120479=CARTESIAN_POINT ( 'NONE',  ( 1.247672978039487734, 1.986097573956084439, -0.3474914183895366215 ) ) ;
#120482=CARTESIAN_POINT ( 'NONE',  ( 6.339412547452306868, 0.8406370108028878851, -2.024118718474729128 ) ) ;
#120484=CARTESIAN_POINT ( 'NONE',  ( 2.906937612971383089, 1.455985047528246090, 0.9243032718214757582 ) ) ;
#120486=CARTESIAN_POINT ( 'NONE',  ( 0.1405533004714383249, 7.629137130509051623, -2.879722665736083709 ) ) ;
#120490=CARTESIAN_POINT ( 'NONE',  ( 1.187862215860764126, -1.241893603568875903, -1.518774446641702580 ) ) ;
#120498=ORIENTED_EDGE ( 'NONE', *, *, #14173, .T. ) ;
#120499=CARTESIAN_POINT ( 'NONE',  ( 4.389189793862141364, -0.004542125399705549196, -1.811656973097997447 ) ) ;
#120503=CARTESIAN_POINT ( 'NONE',  ( 4.529823624924778969, -1.775545877285337193, 0.3580350944670795399 ) ) ;
#120506=CARTESIAN_POINT ( 'NONE',  ( 5.617585446245374037, 0.3627780356338809464, -1.825160902907280613 ) ) ;
#120508=CARTESIAN_POINT ( 'NONE',  ( 2.442874106818424096, -1.667949397242382448, -0.9418811778915718858 ) ) ;
#120515=CARTESIAN_POINT ( 'NONE',  ( 1.306708042577527262, 1.844576602789575137, 0.9840055123579400931 ) ) ;
#120517=CARTESIAN_POINT ( 'NONE',  ( 6.088885551643496541, -0.2832829338282101261, -1.905325039026314560 ) ) ;
#120519=CARTESIAN_POINT ( 'NONE',  ( 2.731258071184277103, -1.704167518380688140, 0.6551187846031494288 ) ) ;
#120521=CARTESIAN_POINT ( 'NONE',  ( 2.109489925670060551, 1.480643174185194200, 1.210387159491378650 ) ) ;
#120522=CARTESIAN_POINT ( 'NONE',  ( 2.101947443238092017, 0.7566099462053441638, -1.818632640566263614 ) ) ;
#120523=CARTESIAN_POINT ( 'NONE',  ( 3.351055748958339908, 0.4689680007726776401, -1.884483806560928398 ) ) ;
#120528=CARTESIAN_POINT ( 'NONE',  ( 3.832379111121624327, -1.093062754469842579, -1.817066923117337751 ) ) ;
#120538=CARTESIAN_POINT ( 'NONE',  ( 3.756323439517950558, 0.6585720284536450420, 1.702948436616057881 ) ) ;
#120542=DIRECTION ( 'NONE',  ( -1.000000000000000000, 0.000000000000000000, 0.000000000000000000 ) ) ;
#120543=CARTESIAN_POINT ( 'NONE',  ( 4.715616592392388284, -1.834479983729628616, 0.3652084810651031743 ) ) ;
#120545=CARTESIAN_POINT ( 'NONE',  ( 1.822755070894378271, 1.797457900398396813, 0.6936678961073846628 ) ) ;
#120546=CARTESIAN_POINT ( 'NONE',  ( 6.561383603009730336, 1.629167342741120406, 1.092533971175007723 ) ) ;
#120552=CARTESIAN_POINT ( 'NONE',  ( 1.195080948601736859, 1.869106744463861158, 0.9945057017613133654 ) ) ;
#120555=CARTESIAN_POINT ( 'NONE',  ( 4.856339096887199780, -2.069677458173447171, -0.05615216265978521804 ) ) ;
#120556=CARTESIAN_POINT ( 'NONE',  ( 0.7316835000789992938, 1.813914744281470925, 0.3150931809976220133 ) ) ;
#120559=CARTESIAN_POINT ( 'NONE',  ( 5.678471694547736703, 1.738760799997655537, 1.503693327295371862 ) ) ;
#120564=CARTESIAN_POINT ( 'NONE',  ( 1.447684683128658278, 0.6615928844308440748, -2.194714443420691552 ) ) ;
#120567=CARTESIAN_POINT ( 'NONE',  ( 5.912047867262844925, 1.302452500554865722, -1.440575834569270519 ) ) ;
#120572=CARTESIAN_POINT ( 'NONE',  ( 6.222915752822945734, 1.412394824171304908, -1.289504995239741714 ) ) ;
#120577=CARTESIAN_POINT ( 'NONE',  ( 2.537156728381038118, -1.549654062961543177, -1.403521045075975415 ) ) ;
#120578=CARTESIAN_POINT ( 'NONE',  ( 1.076598688339102772, -0.03801472141184288056, -1.769612961288852926 ) ) ;
#120579=CARTESIAN_POINT ( 'NONE',  ( 6.486953984781112403, -2.015912550161761629, 0.05229459904129707404 ) ) ;
#120581=CARTESIAN_POINT ( 'NONE',  ( 3.785359544849807190, 1.659571404495253866, 1.581462771572618609 ) ) ;
#120582=CARTESIAN_POINT ( 'NONE',  ( 2.958654558096874609, 0.2547609298257165200, -1.721438497358678932 ) ) ;
#120585=CARTESIAN_POINT ( 'NONE',  ( 3.356526315702735186, -0.7047320765170405066, 1.584360681437890550 ) ) ;
#120586=CARTESIAN_POINT ( 'NONE',  ( 3.367796644333774569, -0.4264072692300807099, 2.128736309618290079 ) ) ;
#120588=CARTESIAN_POINT ( 'NONE',  ( 4.294157853547872605, -0.8666056138363428252, -1.820986994602634024 ) ) ;
#120589=CARTESIAN_POINT ( 'NONE',  ( 2.000000000000001332, -1.212302805901314492E-13, -2.052068128417949389 ) ) ;
#120592=CARTESIAN_POINT ( 'NONE',  ( 1.430555067506549483, 1.855864167146383581, 0.5162276523679990570 ) ) ;
#120594=CARTESIAN_POINT ( 'NONE',  ( 4.447658085050952614, -2.030299463072975819, 0.9018405843745944672 ) ) ;
#120596=CARTESIAN_POINT ( 'NONE',  ( -0.2106854629475400364, 0.7093903261615883693, -2.078205123749873984 ) ) ;
#120601=CARTESIAN_POINT ( 'NONE',  ( 0.4697634657386277612, -1.879787550458272394, -1.183196895768683365 ) ) ;
#120602=CARTESIAN_POINT ( 'NONE',  ( 5.389097038490845648, 0.1425914310585977562, 1.956722230749982971 ) ) ;
#120605=CARTESIAN_POINT ( 'NONE',  ( 0.5093243970649004027, 1.880507610096779025, 1.065828983023514809 ) ) ;
#120608=CARTESIAN_POINT ( 'NONE',  ( 3.297386996040070795, -1.820318649397782318, 0.9700563119749375796 ) ) ;
#120612=CARTESIAN_POINT ( 'NONE',  ( 4.956247902659736582, 0.7144662795386286236, 1.728917671469521800 ) ) ;
#120613=CARTESIAN_POINT ( 'NONE',  ( 3.920349067101033036, -1.199671410015031192, -1.252466492151423694 ) ) ;
#120614=CARTESIAN_POINT ( 'NONE',  ( 3.913389451132457619, -0.8987009378256786141, -1.490314472085547237 ) ) ;
#120615=CARTESIAN_POINT ( 'NONE',  ( 1.066458480799619135, -1.449176446249898831, 1.776219484066744903 ) ) ;
#120617=CARTESIAN_POINT ( 'NONE',  ( 4.634370609685579900, 0.3589238887658425248, 2.059545865661859931 ) ) ;
#120618=CARTESIAN_POINT ( 'NONE',  ( 0.2515690823673248921, 0.7017594223384625574, 1.702352774230586618 ) ) ;
#120621=CARTESIAN_POINT ( 'NONE',  ( 2.180314765559120183, 1.560501322096979449, 1.277041908422072991 ) ) ;
#120627=CARTESIAN_POINT ( 'NONE',  ( 2.227333921462580246, 1.895369558270381338, 0.9509248740046101211 ) ) ;
#120629=CARTESIAN_POINT ( 'NONE',  ( 5.303274670167754223, 1.494737065598227943, 1.048009559513597866 ) ) ;
#120635=CARTESIAN_POINT ( 'NONE',  ( 2.056904690034748739, 0.4466968674397324701, 1.969590803855451933 ) ) ;
#120636=CARTESIAN_POINT ( 'NONE',  ( 5.122202071631626552, -1.176711583861598243, -1.866687997650509079 ) ) ;
#120638=CARTESIAN_POINT ( 'NONE',  ( 3.748742453178009360, -0.3589989779783793744, -1.825800159725386118 ) ) ;
#120643=CARTESIAN_POINT ( 'NONE',  ( 5.443921307256319508, 0.7362202147598860824, -1.670853202368662860 ) ) ;
#120647=CARTESIAN_POINT ( 'NONE',  ( 0.6668559383766320403, -0.5766704339003425606, -1.635293367498649397 ) ) ;
#120648=CARTESIAN_POINT ( 'NONE',  ( 0.3744471653823171486, 1.625640304646416734, -0.6218004557168725910 ) ) ;
#120649=CARTESIAN_POINT ( 'NONE',  ( 6.059233210108489587, -1.975957287588899769, -1.191867793525339669 ) ) ;
#120651=CARTESIAN_POINT ( 'NONE',  ( 1.722021792205346902, -1.142311743720581196, -1.714993188781144928 ) ) ;
#120654=CARTESIAN_POINT ( 'NONE',  ( 0.1751529202326657098, -0.8592662624449104447, -1.822031250676876768 ) ) ;
#120657=CARTESIAN_POINT ( 'NONE',  ( 5.576977133510579776, -0.04717937999037385977, -1.870219006134994588 ) ) ;
#120658=CARTESIAN_POINT ( 'NONE',  ( 4.043146078444789460, 0.09904687726844901841, 1.909973672635330910 ) ) ;
#120660=CARTESIAN_POINT ( 'NONE',  ( 4.530015419921377351, -1.356323209173672106, -1.740806116466916409 ) ) ;
#120666=CARTESIAN_POINT ( 'NONE',  ( 5.795592431653455279, 1.959276243578732091, -0.8114611383256833399 ) ) ;
#120668=CARTESIAN_POINT ( 'NONE',  ( 3.593080373992099119, -0.4475695053229776788, -2.263611109821815681 ) ) ;
#120669=CARTESIAN_POINT ( 'NONE',  ( 3.596105239937871456, 0.8843387906064968940, -1.751336483779348585 ) ) ;
#120671=CARTESIAN_POINT ( 'NONE',  ( 1.164813196467245904, 1.489159823276710926, -1.277213275948145599 ) ) ;
#120675=CARTESIAN_POINT ( 'NONE',  ( 5.964077395145578109, -1.074666730956087335, 1.706109649615504154 ) ) ;
#120678=CARTESIAN_POINT ( 'NONE',  ( 3.221698175004498399, 0.3232067185854271552, -2.146787281877101439 ) ) ;
#120680=CARTESIAN_POINT ( 'NONE',  ( 0.7035762090183244055, 1.867434778015097940, -1.004864118554361863 ) ) ;
#120686=CARTESIAN_POINT ( 'NONE',  ( 1.352885421680804834, -1.626251134426279332, 1.265669239494594311 ) ) ;
#120692=CARTESIAN_POINT ( 'NONE',  ( 4.389254143344611947, -0.003399479254035177832, -1.912461472815998542 ) ) ;
#120694=CARTESIAN_POINT ( 'NONE',  ( 4.996827606291168955, 1.470251540571869020, -0.9849021259363596181 ) ) ;
#120697=CARTESIAN_POINT ( 'NONE',  ( 0.1580966392830873424, 1.806712829659435027, 0.1331060069221217668 ) ) ;
#120699=CARTESIAN_POINT ( 'NONE',  ( 1.129944905810562839, 1.913687095308055808, 0.09034645858918381733 ) ) ;
#120700=CARTESIAN_POINT ( 'NONE',  ( 2.225130849662222410, -1.891980959128433781, -0.8411517639917851508 ) ) ;
#120702=CARTESIAN_POINT ( 'NONE',  ( 0.8835904138565253696, 1.322268204680861814, 1.462458760404183433 ) ) ;
#120703=CARTESIAN_POINT ( 'NONE',  ( 2.578497204056416692, -1.747032809129964503, -0.5301130021647950663 ) ) ;
#120704=CARTESIAN_POINT ( 'NONE',  ( 0.08326089795122111614, -2.240168680488762387, -0.5538300120674977123 ) ) ;
#120707=CARTESIAN_POINT ( 'NONE',  ( 4.018078825213769356, 2.047437054436978876, -0.2496575186523365686 ) ) ;
#120714=CARTESIAN_POINT ( 'NONE',  ( 5.192451847192011805, -2.089709803398311028, -0.2606072588380181076 ) ) ;
#120716=CARTESIAN_POINT ( 'NONE',  ( 6.180147188013234150, -1.146869210499700920, -1.723488058659912392 ) ) ;
#120718=CARTESIAN_POINT ( 'NONE',  ( 3.743588348364734752, -1.634107004491680115, -1.415051943026650161 ) ) ;
#120719=CARTESIAN_POINT ( 'NONE',  ( 4.828773858256512064, 1.391243881446821762, -1.464325142460545459 ) ) ;
#120720=CARTESIAN_POINT ( 'NONE',  ( 6.620655732516648406, 3.679503859435423241, 2.787618683092321969 ) ) ;
#120725=CARTESIAN_POINT ( 'NONE',  ( 2.290250256651988892, -0.7762311197250795214, -1.861343989391924358 ) ) ;
#120730=CARTESIAN_POINT ( 'NONE',  ( 5.537344615273096515, -0.04053095765194079242, 1.912125305397804009 ) ) ;
#120733=CARTESIAN_POINT ( 'NONE',  ( 4.130482583401101415, 0.5405105419177670401, 1.942537254285629400 ) ) ;
#120736=CARTESIAN_POINT ( 'NONE',  ( 6.528329376709017140, 0.9880424216301281204, -1.413504571246849695 ) ) ;
#120741=CARTESIAN_POINT ( 'NONE',  ( 5.518772846390051612, 1.727975122137341613, 0.7167417953098526029 ) ) ;
#120742=CARTESIAN_POINT ( 'NONE',  ( 0.01235793338260140865, -2.012684344489227062, -0.04732037452980299846 ) ) ;
#120744=CARTESIAN_POINT ( 'NONE',  ( 1.885682352965558861, -1.950755244972163904, 0.6936349442826782452 ) ) ;
#120748=CARTESIAN_POINT ( 'NONE',  ( 0.6851730022342136239, 1.650096953764205399, 1.158669022729153175 ) ) ;
#120754=CARTESIAN_POINT ( 'NONE',  ( 5.730082575778132181, 1.913663781862886104, 0.08886097549761286241 ) ) ;
#120762=CARTESIAN_POINT ( 'NONE',  ( 2.501032641837992454, 1.736685530831501456, -1.287010829427559289 ) ) ;
#120765=CARTESIAN_POINT ( 'NONE',  ( 1.230900525853476868, 1.420129835883350955, -1.575055732827963295 ) ) ;
#120766=CARTESIAN_POINT ( 'NONE',  ( 5.403274641334286699, 1.493489847867332854, 1.049580640413529276 ) ) ;
#120767=CARTESIAN_POINT ( 'NONE',  ( 2.460178626894731213, 0.8396039701564265156, 1.783738064433965986 ) ) ;
#120768=CARTESIAN_POINT ( 'NONE',  ( 5.009976098083095408, -0.6827417919906975108, 1.786564173047608062 ) ) ;
#120770=CARTESIAN_POINT ( 'NONE',  ( 4.615651692036619735, 0.4336440386765746946, -1.921039654613013292 ) ) ;
#120771=CARTESIAN_POINT ( 'NONE',  ( 0.9724825242501096145, -0.04715749842807348546, -1.941539141333733953 ) ) ;
#120777=CARTESIAN_POINT ( 'NONE',  ( 5.162724115531083235, 0.5589384127702141658, 1.828758346017298919 ) ) ;
#120779=CARTESIAN_POINT ( 'NONE',  ( 1.149787729276055437, -1.740433383357189223, -1.356609624190791008 ) ) ;
#120782=CARTESIAN_POINT ( 'NONE',  ( 6.410797320372758179, -0.5389820150160546941, -1.939520479220447902 ) ) ;
#120784=( BOUNDED_CURVE ( )  B_SPLINE_CURVE ( 3, ( #167478, #19074, #85155, #2807 ),
 .UNSPECIFIED., .F., .T. ) 
 B_SPLINE_CURVE_WITH_KNOTS ( ( 4, 4 ),
 ( 0.000000000000000000, 0.4999999999999993894 ),
 .UNSPECIFIED. ) 
 CURVE ( )  GEOMETRIC_REPRESENTATION_ITEM ( )  RATIONAL_B_SPLINE_CURVE ( ( 1.000000000000000000, 0.3333333333333342030, 0.3333333333333333703, 0.9999999999999992228 ) ) 
 REPRESENTATION_ITEM ( '' )  );
#120787=CARTESIAN_POINT ( 'NONE',  ( 3.068866956829822801, 1.501395149897828851, -1.425812640530661479 ) ) ;
#120791=CARTESIAN_POINT ( 'NONE',  ( 0.8663662989462637132, 1.066309655776727539, 1.880320099339624296 ) ) ;
#120797=CARTESIAN_POINT ( 'NONE',  ( 6.925078400183556582, 1.261064080992575498, 2.068696352333323052 ) ) ;
#120799=CIRCLE ( 'NONE', #183023, 0.04999999999999969746 ) ;
#120800=CARTESIAN_POINT ( 'NONE',  ( 4.535645802837630747, -1.388783131305007634, 1.038275480396163353 ) ) ;
#120802=CARTESIAN_POINT ( 'NONE',  ( 3.080986915251407776, 1.947773190787219555, 0.7018234266842755531 ) ) ;
#120803=CARTESIAN_POINT ( 'NONE',  ( 4.534827772108455335, -1.699605468249162588, 1.262326912638973786 ) ) ;
#120806=CARTESIAN_POINT ( 'NONE',  ( 2.324999910687207461, -1.798643183423669134, -0.8027048682860711271 ) ) ;
#120807=CARTESIAN_POINT ( 'NONE',  ( 1.089939655121434203, 1.141396045679959004, 1.534244836814010693 ) ) ;
#120808=CARTESIAN_POINT ( 'NONE',  ( 4.646573614920027850, -1.842837963294202464, 1.363044294324888162 ) ) ;
#120809=CARTESIAN_POINT ( 'NONE',  ( 2.068725586703868746, -1.668841220716179130, -0.7407507213199536755 ) ) ;
#120813=CARTESIAN_POINT ( 'NONE',  ( 2.707291822170342144, 1.724471752635655664, -1.038662168513148965 ) ) ;
#120814=CARTESIAN_POINT ( 'NONE',  ( 3.766413727395605093, -0.7909564911158167844, -1.795405819223389488 ) ) ;
#120817=CARTESIAN_POINT ( 'NONE',  ( 0.1755611466353655115, 0.2306421705509461850, -2.278008211689793061 ) ) ;
#120818=CARTESIAN_POINT ( 'NONE',  ( 6.070280604649140876, -1.984772539198733865, -0.6570628365835521345 ) ) ;
#120819=CARTESIAN_POINT ( 'NONE',  ( 4.399107752292472640, 1.421951945714538867, 1.053510053677222613 ) ) ;
#120821=CARTESIAN_POINT ( 'NONE',  ( 1.201424296212102893, -0.5295503721958020327, 2.126384922054704862 ) ) ;
#120822=CARTESIAN_POINT ( 'NONE',  ( 0.2041417395101949583, 1.512754574849054956, 0.8604388899705726068 ) ) ;
#120825=CARTESIAN_POINT ( 'NONE',  ( 0.2331713839410939626, 4.091360563681152307, -2.508188233588979799 ) ) ;
#120826=CARTESIAN_POINT ( 'NONE',  ( 0.9842439076201170423, 2.124318566921878482, 0.8778218499742740377 ) ) ;
#120827=CARTESIAN_POINT ( 'NONE',  ( -0.02351032182101517320, -2.127384168920816165, -0.5261613093957145937 ) ) ;
#120828=CARTESIAN_POINT ( 'NONE',  ( 6.327464733921618567, -1.223274778582748246, 1.229020038707399065 ) ) ;
#120829=CARTESIAN_POINT ( 'NONE',  ( 1.700138637298425737, -0.7412910010123253679, 2.078789392164873906 ) ) ;
#120831=CARTESIAN_POINT ( 'NONE',  ( 0.7960475122521799562, -1.534068779871503363, -1.536527999751842621 ) ) ;
#120833=CARTESIAN_POINT ( 'NONE',  ( 1.604857428818485587, 1.977717902320776266, 0.7566523057890365278 ) ) ;
#120834=CARTESIAN_POINT ( 'NONE',  ( 4.250000000000002665, 2.550977938801684432E-13, 2.052068128417944948 ) ) ;
#120835=CARTESIAN_POINT ( 'NONE',  ( 6.727182134110167411, 4.690976314540481695, 2.651619508270358416 ) ) ;
#120836=CARTESIAN_POINT ( 'NONE',  ( 4.454074118230034962, 1.925978650549282856, -0.04673309505795821689 ) ) ;
#120839=CARTESIAN_POINT ( 'NONE',  ( 1.189493828671518427, 1.739998485882883861, 1.492566873345043010 ) ) ;
#120842=B_SPLINE_CURVE_WITH_KNOTS ( 'NONE', 3,
 ( #94926, #27767, #93863, #144764, #50155, #67431, #166036, #181209, #177225, #132512 ),
 .UNSPECIFIED., .F., .F.,
 ( 4, 1, 1, 1, 1, 1, 1, 4 ),
 ( 0.000000000000000000, 0.09373397616858752945, 0.1863105892815605236, 0.2574079725677296260, 0.3612190813870841954, 0.5208938042821120717, 0.7336009914826546741, 1.000000000000000000 ),
 .UNSPECIFIED. ) ;
#120844=CARTESIAN_POINT ( 'NONE',  ( 4.196076301648347773, 1.450992468586336459, 1.681961854464069983 ) ) ;
#120851=CARTESIAN_POINT ( 'NONE',  ( 1.371720446232262081, -0.2986288616722633793, -1.994071132515719658 ) ) ;
#120853=CARTESIAN_POINT ( 'NONE',  ( 0.4618802912403723870, -0.5535076142849646441, 1.986819116141485653 ) ) ;
#120856=CARTESIAN_POINT ( 'NONE',  ( -0.02423404108400224743, -1.785672699080865788, -0.4486397487279417118 ) ) ;
#120859=CARTESIAN_POINT ( 'NONE',  ( 1.493014682725684938, 1.335586794047480153, 1.161194053514543745 ) ) ;
#120860=CARTESIAN_POINT ( 'NONE',  ( -0.1341500063891595818, -0.1486117279969369209, -1.983907055413631992 ) ) ;
#120861=CARTESIAN_POINT ( 'NONE',  ( 6.427322163675834865, -1.144589508088897478, -1.311236935029986173 ) ) ;
#120862=CARTESIAN_POINT ( 'NONE',  ( 4.247812404936269992, 2.291854478692372687, -0.05604449276840757499 ) ) ;
#120863=CARTESIAN_POINT ( 'NONE',  ( 3.749809578975582536, 0.6641696684822319119, 1.717346325712478583 ) ) ;
#120865=CARTESIAN_POINT ( 'NONE',  ( 3.856323340278215106, 0.6566615474184741563, 1.703573633380930152 ) ) ;
#120866=CARTESIAN_POINT ( 'NONE',  ( 4.606092368833686557, -0.09613688574180989654, 2.014232646917232916 ) ) ;
#120868=CARTESIAN_POINT ( 'NONE',  ( 2.905426592119991991, 1.910755973352752379, 1.211346930818749890 ) ) ;
#120870=CARTESIAN_POINT ( 'NONE',  ( 6.458053290436937210, 2.100604981398071835, -0.1509308302805877633 ) ) ;
#120872=CARTESIAN_POINT ( 'NONE',  ( 4.158688916442685013, -0.6465363538536235133, -1.966910096795893681 ) ) ;
#120875=CARTESIAN_POINT ( 'NONE',  ( 6.094406630213896392, -1.134638919006492275, 1.791192486788994120 ) ) ;
#120878=CARTESIAN_POINT ( 'NONE',  ( 2.121591023604427306, -1.868723361717766096, 0.4677975013653943859 ) ) ;
#120881=CARTESIAN_POINT ( 'NONE',  ( 6.508657463561863921, 0.6146053541861602465, 1.871187945041019152 ) ) ;
#120886=CARTESIAN_POINT ( 'NONE',  ( 0.3346308043965214307, -1.195296165414746037, -1.872270659723746622 ) ) ;
#120887=CARTESIAN_POINT ( 'NONE',  ( 2.854625263381281641, 0.7083305855763160075, 1.983406512126543841 ) ) ;
#120890=CARTESIAN_POINT ( 'NONE',  ( 0.2208628207966298607, -1.659654761427356240, -0.8422171645118268213 ) ) ;
#120895=CARTESIAN_POINT ( 'NONE',  ( 1.652743449602233072, 2.098267697663995790, 0.3060111223712052020 ) ) ;
#120898=CARTESIAN_POINT ( 'NONE',  ( 3.156644782993088150, -0.5669402238272451822, -1.878178299617596192 ) ) ;
#120899=CARTESIAN_POINT ( 'NONE',  ( 2.553791647773369089, 0.5774160426356907960, -2.083079400968433248 ) ) ;
#120900=CARTESIAN_POINT ( 'NONE',  ( 1.804012939494209267, 1.363607186100148638, -1.237405090928713092 ) ) ;
#120903=CARTESIAN_POINT ( 'NONE',  ( 3.450842174108187610, 0.4214097805228322891, -1.688396943527884053 ) ) ;
#120907=CARTESIAN_POINT ( 'NONE',  ( 1.270647086845246188, -1.370953960119488668, 1.671340013135722558 ) ) ;
#120908=CARTESIAN_POINT ( 'NONE',  ( 3.374374892241317703, -0.3960410224921434574, 1.976653181598592601 ) ) ;
#120911=CARTESIAN_POINT ( 'NONE',  ( 3.731288366010646396, -1.822051990069279315, 0.7533225318517923208 ) ) ;
#120912=CARTESIAN_POINT ( 'NONE',  ( 6.609000000000064823, 1.245995683336246884, 2.213443714173808807 ) ) ;
#120913=CARTESIAN_POINT ( 'NONE',  ( 2.243606950041766357, 1.941679294436208680, 0.04551257769231514122 ) ) ;
#120918=CARTESIAN_POINT ( 'NONE',  ( -0.1106856583841424602, 0.7110496148716296538, -2.078439740052108853 ) ) ;
#120923=CARTESIAN_POINT ( 'NONE',  ( 6.668959562645871308, -2.105872948262592192, -0.9439719561973120010 ) ) ;
#120925=CARTESIAN_POINT ( 'NONE',  ( 4.416819765676714304, -1.456490764316048292, 1.314424223973277961 ) ) ;
#120927=CARTESIAN_POINT ( 'NONE',  ( 1.811172873341511336, 1.158687402475454098, -1.650082692374904125 ) ) ;
#120929=CARTESIAN_POINT ( 'NONE',  ( 2.413409855213846544, -1.973772631060242144, 0.7668006401621522139 ) ) ;
#120933=CARTESIAN_POINT ( 'NONE',  ( 3.064218985076866630, -1.701416833343888824, -0.7040189834505713451 ) ) ;
#120937=CARTESIAN_POINT ( 'NONE',  ( 3.867525618572264623, -1.764951123045129577, -1.175235903013646332 ) ) ;
#120940=CARTESIAN_POINT ( 'NONE',  ( 0.4625323210639306071, 0.1833022542275381250, -1.831979997761295165 ) ) ;
#120943=CARTESIAN_POINT ( 'NONE',  ( 4.798151449762615428, -2.060242214822493256, -0.05457638173838111340 ) ) ;
#120946=CARTESIAN_POINT ( 'NONE',  ( 1.153568636672014369, 0.7464410156945017194, 1.683350060182234209 ) ) ;
#120952=CARTESIAN_POINT ( 'NONE',  ( 1.752831059180045115, 0.6944836804415283060, 2.094827981560241970 ) ) ;
#120953=CARTESIAN_POINT ( 'NONE',  ( 4.024925711125073136, 2.146699088035211922, 0.7144036547655304714 ) ) ;
#120955=CARTESIAN_POINT ( 'NONE',  ( 3.814574336081223649, -0.5739048956562255999, -1.718320587032542202 ) ) ;
#120956=CARTESIAN_POINT ( 'NONE',  ( 3.872214865662172656, -1.895674933386840344, -0.2753630107846723463 ) ) ;
#120957=CARTESIAN_POINT ( 'NONE',  ( 5.389151899530504330, 0.1487064154041470299, 2.065066873896327593 ) ) ;
#120959=CARTESIAN_POINT ( 'NONE',  ( 3.713711766734467012, -1.942503170530969436, 0.3358077238896309824 ) ) ;
#120960=CARTESIAN_POINT ( 'NONE',  ( 1.289925581193847925, -0.8688078642279849495, 1.719429354455022096 ) ) ;
#120961=CARTESIAN_POINT ( 'NONE',  ( 4.364026845288040413, 0.8817440624687390427, 1.649792572839225091 ) ) ;
#120963=CARTESIAN_POINT ( 'NONE',  ( 3.053680222918000453, -1.886840229487633414, -1.328398743635789803 ) ) ;
#120964=CARTESIAN_POINT ( 'NONE',  ( 5.019887821480574885, 1.840843491799005527, -0.2725137592536843734 ) ) ;
#120968=CARTESIAN_POINT ( 'NONE',  ( 2.051528240825768012, -1.692106715078506296, -1.253703384363166196 ) ) ;
#120973=CARTESIAN_POINT ( 'NONE',  ( 2.777707764728345907, 0.3069055913166895966, -2.098134212408508059 ) ) ;
#120976=CARTESIAN_POINT ( 'NONE',  ( 0.4572932007271997001, -1.730182198833930318, 1.041906760498239271 ) ) ;
#120981=CARTESIAN_POINT ( 'NONE',  ( 1.634274655659254005, 1.066924998833935989, -1.879885089102695250 ) ) ;
#120988=CARTESIAN_POINT ( 'NONE',  ( 5.436732529336289588, -1.586671906620169104, 1.244382051841623538 ) ) ;
#120990=CARTESIAN_POINT ( 'NONE',  ( 6.374567656919228220, -0.1030857042376011334, -2.088345373630628554 ) ) ;
#120992=CARTESIAN_POINT ( 'NONE',  ( 6.737200384369169903, -1.933438233944267060, 0.9670071574134844195 ) ) ;
#120999=CARTESIAN_POINT ( 'NONE',  ( 2.947548438991169473, 0.6205982292267105960, -1.609554129922322163 ) ) ;
#121001=CARTESIAN_POINT ( 'NONE',  ( 1.721574597234516890, -0.9778441516922768972, -1.474834890465251291 ) ) ;
#121002=CARTESIAN_POINT ( 'NONE',  ( 3.053387886640859694, -1.774279702891886190, 0.9510675200815300601 ) ) ;
#121003=CARTESIAN_POINT ( 'NONE',  ( 5.877994779194309238, 1.310017027744770246, 1.775731318763192013 ) ) ;
#121005=CARTESIAN_POINT ( 'NONE',  ( 4.693620712453854260, 1.883065523094022753, -0.7309246526977104530 ) ) ;
#121007=CARTESIAN_POINT ( 'NONE',  ( 4.459710115430675081, -1.639780234044617035, -1.344486126324248465 ) ) ;
#121008=CARTESIAN_POINT ( 'NONE',  ( 3.849232595480827079, 0.2440098934328518987, -2.001514877671112025 ) ) ;
#121009=CARTESIAN_POINT ( 'NONE',  ( 4.043061577595566725, 0.09493798274137112136, 1.809245059475625750 ) ) ;
#121015=CARTESIAN_POINT ( 'NONE',  ( 1.358040219746913024, 0.7549631825471068147, 1.711723683848711985 ) ) ;
#121017=CARTESIAN_POINT ( 'NONE',  ( 6.551413666264667590, -1.614568043246225271, 0.8214943993307096681 ) ) ;
#121022=CARTESIAN_POINT ( 'NONE',  ( 0.5625819312903358460, 0.5574351770905332515, 1.829310545699929458 ) ) ;
#121025=CARTESIAN_POINT ( 'NONE',  ( 1.293326634533353170, -1.775083115552608559, 0.8357255594537355003 ) ) ;
#121028=CARTESIAN_POINT ( 'NONE',  ( 4.359710196644346780, -1.641147893522959089, -1.343014508298406628 ) ) ;
#121029=CARTESIAN_POINT ( 'NONE',  ( -0.02988540731103071432, 0.005807295984020746475, -1.726291166677936362 ) ) ;
#121031=CARTESIAN_POINT ( 'NONE',  ( 6.028588005634209601, 1.899229357904350879, 0.5280594692760686160 ) ) ;
#121033=CARTESIAN_POINT ( 'NONE',  ( 0.7209482731112315523, 1.521806550355369492, -1.318046908132961104 ) ) ;
#121035=CARTESIAN_POINT ( 'NONE',  ( -0.08807185805374209697, -1.306980724784766013, -1.666505321573110265 ) ) ;
#121037=CARTESIAN_POINT ( 'NONE',  ( 1.697802635435996743, -1.498143435978617877, -1.429203828351800487 ) ) ;
#121041=CARTESIAN_POINT ( 'NONE',  ( 5.121074860632232273, -1.985326386471301552, 0.6553513102709652705 ) ) ;
#121043=CARTESIAN_POINT ( 'NONE',  ( 2.590611583786633254, -0.3098195481324728107, -1.798931244660670448 ) ) ;
#121044=CARTESIAN_POINT ( 'NONE',  ( 2.068756839025966521, -1.399621434743709703, 1.149952615172030512 ) ) ;
#121046=CARTESIAN_POINT ( 'NONE',  ( 6.340462157465731607, 2.182225300935904055, 0.3281612982340698093 ) ) ;
#121047=CARTESIAN_POINT ( 'NONE',  ( 4.296070028909639404, -0.8476096858263427736, 2.037697185916572007 ) ) ;
#121050=CARTESIAN_POINT ( 'NONE',  ( 2.596233987490266681, -0.9813665562012074961, 1.641104690102652919 ) ) ;
#121053=CARTESIAN_POINT ( 'NONE',  ( 6.725056259267968350, -1.891221747171191403, -0.8428681758992571105 ) ) ;
#121055=CARTESIAN_POINT ( 'NONE',  ( 6.374583145400191775, -0.1054333438532777389, -2.189162923280890904 ) ) ;
#121057=CARTESIAN_POINT ( 'NONE',  ( 0.1753634416057732182, 7.629137130509072051, -2.744001747789548418 ) ) ;
#121061=CARTESIAN_POINT ( 'NONE',  ( 3.356579238971897805, -1.418645411611328067, 1.219307012350186126 ) ) ;
#121066=CARTESIAN_POINT ( 'NONE',  ( 6.666853767972947153, 1.538155548931797956, -1.385880503156889487 ) ) ;
#121067=CARTESIAN_POINT ( 'NONE',  ( 1.493767781312784981, -2.000855510370867840, 0.2496291452861176263 ) ) ;
#121071=CARTESIAN_POINT ( 'NONE',  ( 1.412352946837617473, 1.469754387505791460, -1.625674263109680329 ) ) ;
#121072=CARTESIAN_POINT ( 'NONE',  ( 5.742758765878789085, 0.3605303665093101406, 1.789564367143759327 ) ) ;
#121081=CARTESIAN_POINT ( 'NONE',  ( 3.456447201099471123, -1.625387274077850996, -0.8650149607793489182 ) ) ;
#121082=CARTESIAN_POINT ( 'NONE',  ( 6.135026823787811168, 1.880036687389478489, 0.7205229627402914838 ) ) ;
#121083=CARTESIAN_POINT ( 'NONE',  ( 1.546695614565428922, 2.123301925303363369, -0.8802762395820094010 ) ) ;
#121085=CARTESIAN_POINT ( 'NONE',  ( 6.561383603009730336, 1.629167342741120406, 1.092533971175007723 ) ) ;
#121088=CARTESIAN_POINT ( 'NONE',  ( 3.445477555875466891, -1.765175379189663607, 0.7362804355328657069 ) ) ;
#121092=CARTESIAN_POINT ( 'NONE',  ( 2.982061477060811150, -2.060241282245252048, -0.3548380112704754286 ) ) ;
#121093=CARTESIAN_POINT ( 'NONE',  ( 1.428351348257720588, 1.801920623737063520, 0.5021531274154652502 ) ) ;
#121094=CARTESIAN_POINT ( 'NONE',  ( 2.231795861093866851, -1.842164517099669441, -0.8196493499348647127 ) ) ;
#121097=CARTESIAN_POINT ( 'NONE',  ( 3.333312927339195930, 0.7792813341828198626, -1.556285420506423600 ) ) ;
#121101=CARTESIAN_POINT ( 'NONE',  ( 3.422183312176851455, 1.093272757541150719, -1.334144266598129791 ) ) ;
#121102=CARTESIAN_POINT ( 'NONE',  ( 3.351304529449970371, 0.5305821810032870234, -2.126252377916526992 ) ) ;
#121103=CARTESIAN_POINT ( 'NONE',  ( 5.813141826352885566, 1.944573597739504889, 1.043518232037063287 ) ) ;
#121106=CARTESIAN_POINT ( 'NONE',  ( 3.520551232162504540, 0.9717998864677798165, 1.941468132180910189 ) ) ;
#121107=CARTESIAN_POINT ( 'NONE',  ( 1.681982107312831154, -0.9779208310041755947, 1.541497997293653555 ) ) ;
#121109=CARTESIAN_POINT ( 'NONE',  ( 4.346934998023818331, -1.892857631927163498, -0.9488708475321022684 ) ) ;
#121113=CARTESIAN_POINT ( 'NONE',  ( 4.880587636231574322, -0.2790779774165750293, -2.275280792031343147 ) ) ;
#121115=CARTESIAN_POINT ( 'NONE',  ( 6.720655732516650716, 2.984497329163855461, 2.280179935440066252 ) ) ;
#121117=CARTESIAN_POINT ( 'NONE',  ( 0.5750489506927083383, -1.533040007955801531, 1.465245631482835043 ) ) ;
#121124=CARTESIAN_POINT ( 'NONE',  ( 5.766250055133458119, 1.862018000461727052, -0.7743128548072516493 ) ) ;
#121126=CARTESIAN_POINT ( 'NONE',  ( 3.379784452013841367, -1.989113752706978433, 0.5454275443767720999 ) ) ;
#121128=CARTESIAN_POINT ( 'NONE',  ( -0.2411972340276230808, 0.2378665717568603510, -1.934216014300967235 ) ) ;
#121133=CARTESIAN_POINT ( 'NONE',  ( 6.386699327874667986, 1.908680410311427655, -1.076638258889956345 ) ) ;
#121134=CARTESIAN_POINT ( 'NONE',  ( 5.221327349844218091, 1.987046161919112430, 0.3419379449052239450 ) ) ;
#121135=CARTESIAN_POINT ( 'NONE',  ( 3.069684041021227827, -1.094477399149307306, 1.480508570315848482 ) ) ;
#121138=CARTESIAN_POINT ( 'NONE',  ( 0.5688600258280833710, 0.1761389027815796759, -1.715759018540372827 ) ) ;
#121139=CARTESIAN_POINT ( 'NONE',  ( 1.108484992968819416, -0.04990477548066223068, 2.298298319747505758 ) ) ;
#121141=CARTESIAN_POINT ( 'NONE',  ( 6.614178507701674370, -1.059427008983104601, -1.999161347636166930 ) ) ;
#121142=CARTESIAN_POINT ( 'NONE',  ( 3.246800538002168945, 0.5120957664956159450, 2.042728137747833461 ) ) ;
#121151=CARTESIAN_POINT ( 'NONE',  ( 4.465202103771027886, -1.783222260262930181, 1.324459880397445666 ) ) ;
#121152=CARTESIAN_POINT ( 'NONE',  ( 2.607599380506659514, -2.167453834138896696, 0.3226137089109848421 ) ) ;
#121155=CARTESIAN_POINT ( 'NONE',  ( 5.195737816846159873, -1.386088135442983260, -1.388664821390848347 ) ) ;
#121157=CARTESIAN_POINT ( 'NONE',  ( 6.610000000000028741, 4.695285100415147461, 2.562642482393460597 ) ) ;
#121159=CARTESIAN_POINT ( 'NONE',  ( 4.623349522974431025, 1.846400237221163865, 1.042759738753673338 ) ) ;
#121162=CARTESIAN_POINT ( 'NONE',  ( 5.084929678302336775, -0.2608814864752464491, -2.145832476913120068 ) ) ;
#121164=CARTESIAN_POINT ( 'NONE',  ( 4.950658015114751009, -1.558304906039936988, -0.9804572199803849308 ) ) ;
#121167=CARTESIAN_POINT ( 'NONE',  ( 0.08108764725259924588, -0.8233000410203991093, 1.533359828670758374 ) ) ;
#121172=CARTESIAN_POINT ( 'NONE',  ( 4.118171802502921253, -1.108985364570359566, -1.855417305202881506 ) ) ;
#121175=CARTESIAN_POINT ( 'NONE',  ( 4.047864428982482110, 0.7307185629543844207, -2.034579650689218866 ) ) ;
#121176=CARTESIAN_POINT ( 'NONE',  ( 4.464113681242611875, 0.9267091202830781693, 1.739933209567791073 ) ) ;
#121177=CARTESIAN_POINT ( 'NONE',  ( 3.760871765136180933, -1.731833850012770126, -0.08630056690941270703 ) ) ;
#121178=CARTESIAN_POINT ( 'NONE',  ( 1.242012060539962492, 2.189267750446591609, 0.1026977899005257211 ) ) ;
#121179=CARTESIAN_POINT ( 'NONE',  ( 2.169360633853111509, -2.109970246048063380, -0.9347365353246681607 ) ) ;
#121180=CARTESIAN_POINT ( 'NONE',  ( 3.743479925124373331, -1.557965094614376378, -1.348979221448711519 ) ) ;
#121181=CARTESIAN_POINT ( 'NONE',  ( 6.005412763054238212, -1.926851508234005195, 0.2422190414417753623 ) ) ;
#121188=CARTESIAN_POINT ( 'NONE',  ( 3.100804818134130780, -0.6391501652806098610, -2.112195066926085829 ) ) ;
#121191=CARTESIAN_POINT ( 'NONE',  ( 0.7603355536747276044, -0.6198598984368717257, -1.754846704163029125 ) ) ;
#121192=CARTESIAN_POINT ( 'NONE',  ( -0.1290005225502398323, 0.2247172878383028038, -2.207197350255707402 ) ) ;
#121196=CARTESIAN_POINT ( 'NONE',  ( 6.925078400183593885, 7.051837472187183486, 2.742497896504832333 ) ) ;
#121199=CARTESIAN_POINT ( 'NONE',  ( 2.166935907724653720, -1.883791910722651952, -0.8362540481525667646 ) ) ;
#121206=CARTESIAN_POINT ( 'NONE',  ( 1.920846698078120474, 1.922532266116746325, 0.7428477115608185244 ) ) ;
#121211=CARTESIAN_POINT ( 'NONE',  ( 5.584669497696876483, -2.152379054646291756, -0.4867646435422824935 ) ) ;
#121212=CARTESIAN_POINT ( 'NONE',  ( 0.7026770610618977564, -0.7276074859871293210, -2.035605373553108777 ) ) ;
#121214=CARTESIAN_POINT ( 'NONE',  ( 0.05278957052760185897, 0.3289079202175131389, 1.883742972368242174 ) ) ;
#121215=CARTESIAN_POINT ( 'NONE',  ( 1.165250339122084533, 1.861343190080061882, -0.7762330495894869120 ) ) ;
#121217=CARTESIAN_POINT ( 'NONE',  ( 1.476342052747819045, 2.027250371889641301, 1.083024425860839690 ) ) ;
#121219=CARTESIAN_POINT ( 'NONE',  ( 6.358066468859800757, 0.7272683628555456359, -1.768788954293845528 ) ) ;
#121221=CARTESIAN_POINT ( 'NONE',  ( 1.815107966846595255, -0.2319292346777863389, 1.856160199827073587 ) ) ;
#121222=CARTESIAN_POINT ( 'NONE',  ( 3.520720487665735643, 0.3006478860226591276, 1.993893439002386581 ) ) ;
#121226=CARTESIAN_POINT ( 'NONE',  ( 5.285806214103678791, 1.413684203821091945, 1.561263235811745309 ) ) ;
#121231=CARTESIAN_POINT ( 'NONE',  ( 4.342060261306793123, -1.245981751006501437, -1.589553384294100091 ) ) ;
#121233=CARTESIAN_POINT ( 'NONE',  ( 6.478975546884585768, 1.923237475310497047, 0.7459448616168369295 ) ) ;
#121235=CARTESIAN_POINT ( 'NONE',  ( 5.079442160427912967, 2.018932005888602887, -0.7727740077691500620 ) ) ;
#121241=CARTESIAN_POINT ( 'NONE',  ( 3.385384905382606391, 0.05040654291960967176, 2.170743301239473233 ) ) ;
#121244=CARTESIAN_POINT ( 'NONE',  ( 1.610644152589552958, -0.2245515952020246675, 1.827417025815617935 ) ) ;
#121246=CARTESIAN_POINT ( 'NONE',  ( 3.562233144267571650, -1.470601008620987749, 1.625073949779440419 ) ) ;
#121247=CARTESIAN_POINT ( 'NONE',  ( 6.983263157960365675, 7.629137130509070275, 2.653810918356712900 ) ) ;
#121248=CARTESIAN_POINT ( 'NONE',  ( 3.344836307015612409, 0.5477570922035517320, 2.195101814764536030 ) ) ;
#121254=CARTESIAN_POINT ( 'NONE',  ( 5.817594836490700416, -1.726241941513080747, 0.3891773745644273030 ) ) ;
#121255=CARTESIAN_POINT ( 'NONE',  ( 2.292140615954643579, -0.9012634372634602542, 1.903512165690796065 ) ) ;
#121258=CARTESIAN_POINT ( 'NONE',  ( 0.6077773097897182231, 0.6213696771984353884, -1.869019927991413921 ) ) ;
#121261=CARTESIAN_POINT ( 'NONE',  ( 5.853729002925880387, -1.318332981873654441, -1.242799640730863464 ) ) ;
#121266=CARTESIAN_POINT ( 'NONE',  ( 4.364026845288040413, 0.8817440624687390427, 1.649792572839225091 ) ) ;
#121267=CARTESIAN_POINT ( 'NONE',  ( 5.946161111532238586, -0.9360204806616537754, 1.846680006623670156 ) ) ;
#121276=CARTESIAN_POINT ( 'NONE',  ( 5.318788500806308051, -1.422220495204097546, 1.351624447685224162 ) ) ;
#121278=CARTESIAN_POINT ( 'NONE',  ( 1.809922493048341074, -1.704678386728165185, 1.076150803433255865 ) ) ;
#121280=CARTESIAN_POINT ( 'NONE',  ( 0.3456114054924685486, 0.6817542107791437767, -2.082909237240769151 ) ) ;
#121282=CARTESIAN_POINT ( 'NONE',  ( 2.354581831802166736, -1.448805955455864769, 1.183207591018392568 ) ) ;
#121284=CARTESIAN_POINT ( 'NONE',  ( 3.885024706246028803, -1.880017414580990032, -0.7205730073996403640 ) ) ;
#121288=CARTESIAN_POINT ( 'NONE',  ( 4.499685226448436381, -2.076086866053193258, 0.4145649545581850393 ) ) ;
#121290=CARTESIAN_POINT ( 'NONE',  ( 6.373496627357888578, -0.2573980274669443458, 2.054251119134167691 ) ) ;
#121291=CARTESIAN_POINT ( 'NONE',  ( 1.030938747749777118, -1.888616091942503461, 0.8971857714693499686 ) ) ;
#121292=CARTESIAN_POINT ( 'NONE',  ( 6.720655732516647163, -0.001531948155462491612, 2.073773125298985054 ) ) ;
#121293=CARTESIAN_POINT ( 'NONE',  ( 6.317409609008933558, -0.2203418483949574069, 1.812181760327068680 ) ) ;
#121302=CARTESIAN_POINT ( 'NONE',  ( 6.111958284735683478, -0.6397702040911549259, 1.802229686255519603 ) ) ;
#121311=CARTESIAN_POINT ( 'NONE',  ( 5.571888728144736902, -0.9040954357531080232, 1.802425742427179012 ) ) ;
#121312=CARTESIAN_POINT ( 'NONE',  ( 0.2586463447097427926, 2.115114616003030079, 0.1516365082330217162 ) ) ;
#121314=CARTESIAN_POINT ( 'NONE',  ( -0.1394461523061377994, 7.629137130509062281, -2.880276239818948536 ) ) ;
#121317=CARTESIAN_POINT ( 'NONE',  ( 3.291813281336749331, -1.319317765291039946, -1.462433841519056532 ) ) ;
#121318=CARTESIAN_POINT ( 'NONE',  ( 4.235953958900400274, 2.015913684659226490, -0.05231418598541925924 ) ) ;
#121321=CARTESIAN_POINT ( 'NONE',  ( 5.121103774788174690, -2.081602751171758747, 0.6852947426586111224 ) ) ;
#121323=CARTESIAN_POINT ( 'NONE',  ( 3.364200941815390866, 0.8650686769993837233, 1.721291803412771992 ) ) ;
#121325=CARTESIAN_POINT ( 'NONE',  ( -0.02948999725182251466, 0.2504340119564217870, -1.961592983597350459 ) ) ;
#121326=CARTESIAN_POINT ( 'NONE',  ( 0.3115100037339203487, 1.922317768103290803, 1.083863418116323807 ) ) ;
#121332=CARTESIAN_POINT ( 'NONE',  ( 5.366046204681790499, -1.960318410495393238, 0.1889891646899461708 ) ) ;
#121334=CARTESIAN_POINT ( 'NONE',  ( 0.02871324022350740107, -1.775192216153992808, 0.7880070256306227483 ) ) ;
#121335=CARTESIAN_POINT ( 'NONE',  ( 4.301435403400270197, 1.797132274555211184, -0.9072848608384380675 ) ) ;
#121336=CARTESIAN_POINT ( 'NONE',  ( 5.519047587058080850, 2.296088720628499669, -0.1051655125834053545 ) ) ;
#121338=CARTESIAN_POINT ( 'NONE',  ( 3.643253357272932647, 1.684219189441754416, -0.7917782423425399063 ) ) ;
#121344=CARTESIAN_POINT ( 'NONE',  ( 5.671452434703694756, 1.246268910035509991, 1.678523727997438986 ) ) ;
#121348=CARTESIAN_POINT ( 'NONE',  ( 0.8557438351849018243, 1.823752217391808372, -0.08689656109241167270 ) ) ;
#121350=STYLED_ITEM ( 'NONE', ( #184964 ), #47143 ) ;
#121351=CARTESIAN_POINT ( 'NONE',  ( 2.601899516932767220, -0.1674142849007881351, 1.726012112926772701 ) ) ;
#121356=CARTESIAN_POINT ( 'NONE',  ( 6.684450694706582929, 1.257157530024972658, -1.769884466434832548 ) ) ;
#121357=CARTESIAN_POINT ( 'NONE',  ( 5.039593146249602640, -1.293522693445446015, -1.288650932716684849 ) ) ;
#121358=CARTESIAN_POINT ( 'NONE',  ( 3.063279882407277999, 1.654721480355027863, 1.053479689057647217 ) ) ;
#121362=CARTESIAN_POINT ( 'NONE',  ( 4.020270485675044192, -2.114722421624544157, 0.1573160286183969692 ) ) ;
#121365=CARTESIAN_POINT ( 'NONE',  ( 1.235311698660218838, -0.04697018572753957483, -2.069874154031334790 ) ) ;
#121368=CARTESIAN_POINT ( 'NONE',  ( 4.442156590966897411, -1.366343709131916828, -1.751266766990001944 ) ) ;
#121370=CARTESIAN_POINT ( 'NONE',  ( 2.092814488687055441, -0.4990534829178472354, 2.243750245495256035 ) ) ;
#121372=CARTESIAN_POINT ( 'NONE',  ( 6.332891742935283119, -1.956728314951971637, -0.6523575503349694493 ) ) ;
#121380=CARTESIAN_POINT ( 'NONE',  ( 2.566550162062298579, 0.6480892470011965223, 1.799338185917313870 ) ) ;
#121382=CARTESIAN_POINT ( 'NONE',  ( 4.401177694619070380, 1.385992036768167068, 1.026327495003590551 ) ) ;
#121383=CARTESIAN_POINT ( 'NONE',  ( 2.571500236035813902, 1.429449181443824823, 1.422607194786096541 ) ) ;
#121384=CARTESIAN_POINT ( 'NONE',  ( 4.149308075173010479, 1.083998706471595463, 2.027078093135482817 ) ) ;
#121385=CARTESIAN_POINT ( 'NONE',  ( 3.726065177040696952, -1.343991584994163269, -1.819822530443465425 ) ) ;
#121386=CARTESIAN_POINT ( 'NONE',  ( -0.004863692847738298151, -0.4900785244342681368, -2.159743284330918112 ) ) ;
#121389=CARTESIAN_POINT ( 'NONE',  ( 4.850734264762338377, -1.421546097138610243, 1.053919008203674013 ) ) ;
#121391=CARTESIAN_POINT ( 'NONE',  ( 1.043418098205237676, -1.810020423698131653, -1.406424589915030943 ) ) ;
#121392=CARTESIAN_POINT ( 'NONE',  ( 5.367088761235753402, 1.773375748883701419, -0.4946613714205680967 ) ) ;
#121394=CARTESIAN_POINT ( 'NONE',  ( 6.228506716250251429, 0.2110190803071687327, 2.181275323772186248 ) ) ;
#121399=CARTESIAN_POINT ( 'NONE',  ( 5.318829906782316819, -1.502041817331278173, 1.425132596443792643 ) ) ;
#121400=CARTESIAN_POINT ( 'NONE',  ( 1.604704241733472037, 1.883313803065278513, 0.7212895827233902768 ) ) ;
#121402=CARTESIAN_POINT ( 'NONE',  ( 3.826716429392281071, 1.829700617163315002, 0.6032043533580729866 ) ) ;
#121404=CARTESIAN_POINT ( 'NONE',  ( 1.213460986420217047, 1.812193587075833667, -1.284517086575332367 ) ) ;
#121413=CARTESIAN_POINT ( 'NONE',  ( 2.857805160684105950, -0.6180756922911297968, 1.862011555624979886 ) ) ;
#121417=CARTESIAN_POINT ( 'NONE',  ( 6.162552467866693640, -0.7048080804108979303, -1.831077584432870609 ) ) ;
#121421=CARTESIAN_POINT ( 'NONE',  ( 5.296111364736042937, -0.9110065213352031011, -1.799124599017036585 ) ) ;
#121422=CARTESIAN_POINT ( 'NONE',  ( 0.4446536212460248105, 2.256715800172736763, 0.1630166291790128841 ) ) ;
#121426=CARTESIAN_POINT ( 'NONE',  ( 1.159204581426832803, 0.3705859133612994794, -1.833297903905316772 ) ) ;
#121427=CARTESIAN_POINT ( 'NONE',  ( 6.854911444608583260, -0.7389736882487309977, 1.567799899397160912 ) ) ;
#121429=CARTESIAN_POINT ( 'NONE',  ( 3.702820756938397295, 1.880440254450808757, 1.125299312022425280 ) ) ;
#121430=CARTESIAN_POINT ( 'NONE',  ( 5.719831105939597649, -2.253009325453013023, 0.4983019283236743702 ) ) ;
#121432=CARTESIAN_POINT ( 'NONE',  ( 6.714142707505978080, -0.9671387161254895171, -1.819716304366093551 ) ) ;
#121433=CARTESIAN_POINT ( 'NONE',  ( 2.536971540620248433, -1.439279119694805820, -1.303886525222669901 ) ) ;
#121439=CARTESIAN_POINT ( 'NONE',  ( 3.006482587178582300, -1.942541511447487990, 0.5404910644229294903 ) ) ;
#121443=CARTESIAN_POINT ( 'NONE',  ( 0.7326872660318053398, 0.1314506862302306234, 1.821024990000128518 ) ) ;
#121449=CARTESIAN_POINT ( 'NONE',  ( 6.526252491562488878, 1.188822440972692185, -1.683233108126303446 ) ) ;
#121453=CARTESIAN_POINT ( 'NONE',  ( 5.444012513273879250, -1.283034597847107161, -1.559753263307301463 ) ) ;
#121454=CARTESIAN_POINT ( 'NONE',  ( 5.233148740271514221, 2.051824077619863296, 0.8514482647801949744 ) ) ;
#121458=MECHANICAL_DESIGN_GEOMETRIC_PRESENTATION_REPRESENTATION('',(#38341),#100642);
#121459=CARTESIAN_POINT ( 'NONE',  ( 5.067286680778130936, 0.2040240636430467047, -2.050771057314598966 ) ) ;
#121460=CARTESIAN_POINT ( 'NONE',  ( 3.674454069786535548, 1.462445212485608437, 1.388486266691544957 ) ) ;
#121464=( BOUNDED_CURVE ( )  B_SPLINE_CURVE ( 3, ( #137992, #188858, #6882, #40494 ),
 .UNSPECIFIED., .F., .T. ) 
 B_SPLINE_CURVE_WITH_KNOTS ( ( 4, 4 ),
 ( 0.000000000000000000, 0.4999999999999963918 ),
 .UNSPECIFIED. ) 
 CURVE ( )  GEOMETRIC_REPRESENTATION_ITEM ( )  RATIONAL_B_SPLINE_CURVE ( ( 1.000000000000000000, 0.3333333333333381998, 0.3333333333333333703, 0.9999999999999952260 ) ) 
 REPRESENTATION_ITEM ( '' )  );
#121468=CARTESIAN_POINT ( 'NONE',  ( 4.077499844852236599, 1.427718728413525318, -1.423743541103118737 ) ) ;
#121469=CARTESIAN_POINT ( 'NONE',  ( 3.468544592087896561, 0.04396668885017079864, -1.840778273432375212 ) ) ;
#121471=CARTESIAN_POINT ( 'NONE',  ( 1.911159365042811809, 1.708073263224022975, -1.551933148444275989 ) ) ;
#121473=CARTESIAN_POINT ( 'NONE',  ( 4.095124908492456584, 1.828510582809875107, -1.152538879107746439 ) ) ;
#121477=CARTESIAN_POINT ( 'NONE',  ( 3.128558558221442354, 0.3401759809690939051, -2.272988164180503201 ) ) ;
#121479=CARTESIAN_POINT ( 'NONE',  ( 2.272138710904994863, -1.152746988206950096, 1.473173409640892162 ) ) ;
#121480=CARTESIAN_POINT ( 'NONE',  ( 6.438353018038387887, 1.949953777973761015, 0.2897296601065552091 ) ) ;
#121483=CARTESIAN_POINT ( 'NONE',  ( 1.664966938652842954, -1.558911317520403239, 1.562347339584921002 ) ) ;
#121489=CARTESIAN_POINT ( 'NONE',  ( 5.911001178172424986, 1.738356976118849984, 0.9299647631116741975 ) ) ;
#121490=CARTESIAN_POINT ( 'NONE',  ( 5.901056178406707708, 1.890114102979102650, -1.323741089068092958 ) ) ;
#121491=CARTESIAN_POINT ( 'NONE',  ( 6.777813018113469923, -1.804774468322063452, 0.4538611949938906043 ) ) ;
#121492=CARTESIAN_POINT ( 'NONE',  ( 4.715719689075464238, 0.4568931354213046636, -2.011171341922016076 ) ) ;
#121499=CARTESIAN_POINT ( 'NONE',  ( 6.584450689261575285, 1.255587272919860942, -1.771131291935989616 ) ) ;
#121501=CARTESIAN_POINT ( 'NONE',  ( 4.933073973922719624, -1.305863698873997780, -1.298312775753200699 ) ) ;
#121504=CARTESIAN_POINT ( 'NONE',  ( 0.7724589312842686795, -1.759198622581410021, -0.6360808729843556719 ) ) ;
#121509=CARTESIAN_POINT ( 'NONE',  ( 0.3110002902955294468, 1.589785527739733695, -1.062417771062994287 ) ) ;
#121510=CARTESIAN_POINT ( 'NONE',  ( 1.727073733189425031, -1.667858853059518420, 0.5925122568580538651 ) ) ;
#121512=CARTESIAN_POINT ( 'NONE',  ( 6.305343602688459725, 1.750316497599126331, -0.9943532346578187742 ) ) ;
#121514=CARTESIAN_POINT ( 'NONE',  ( 4.921452907191903314, -1.357786409588169096, -1.351554235494869749 ) ) ;
#121517=CARTESIAN_POINT ( 'NONE',  ( 5.424252406547988237, 0.9690106866696795995, 1.714583495817107783 ) ) ;
#121518=CARTESIAN_POINT ( 'NONE',  ( -0.1577409392781377873, -1.310076727147227560, -1.668215054097483385 ) ) ;
#121521=CARTESIAN_POINT ( 'NONE',  ( 3.362029495745801899, 0.8400119854848131506, 1.671504782411597612 ) ) ;
#121522=CARTESIAN_POINT ( 'NONE',  ( 6.533849689656099358, -1.133137674240388248, -1.300586445545851344 ) ) ;
#121524=CARTESIAN_POINT ( 'NONE',  ( 2.332911791115964473, 2.140974936812658935, 0.5348262304398290201 ) ) ;
#121527=CARTESIAN_POINT ( 'NONE',  ( 0.5376419320063254847, 1.925266156408891316, -0.7407299734314594097 ) ) ;
#121534=ORIENTED_EDGE ( 'NONE', *, *, #72903, .F. ) ;
#121535=CARTESIAN_POINT ( 'NONE',  ( 3.227070907399377298, -1.911900318415656441, -0.7948586591664741352 ) ) ;
#121539=CARTESIAN_POINT ( 'NONE',  ( 0.4166731193052671256, -0.6827031231213858131, -1.900913249881502232 ) ) ;
#121542=CARTESIAN_POINT ( 'NONE',  ( 0.07459516483345349225, 1.413926688351078154, -2.016100038618890089 ) ) ;
#121544=CARTESIAN_POINT ( 'NONE',  ( 5.923203835008548523, 0.8145033986626595279, 1.844426808122232142 ) ) ;
#121545=CARTESIAN_POINT ( 'NONE',  ( 5.489432593909100433, -0.4588279098093718256, 1.859853701273159743 ) ) ;
#121546=CARTESIAN_POINT ( 'NONE',  ( 6.639320575229251453, 2.441375407831634536, 2.385816205380648203 ) ) ;
#121547=CARTESIAN_POINT ( 'NONE',  ( 3.527062600443749307, -2.024233912922444478, 0.8403589366152917073 ) ) ;
#121549=CARTESIAN_POINT ( 'NONE',  ( 2.338023529656753752, -1.104205016203146705, -1.561194055274425452 ) ) ;
#121552=CARTESIAN_POINT ( 'NONE',  ( 0.7730648107450198703, 1.777001872080404166, -0.9530316558409923644 ) ) ;
#121554=CARTESIAN_POINT ( 'NONE',  ( 6.110890996357365879, -0.2699588104537915534, 2.174781792473476472 ) ) ;
#121556=CARTESIAN_POINT ( 'NONE',  ( 3.522183196695947593, 1.094745356718468399, -1.332776395737497399 ) ) ;
#121558=CARTESIAN_POINT ( 'NONE',  ( 0.1399997263886003374, 0.002789056014650820314, -1.999853399661279063 ) ) ;
#121569=CARTESIAN_POINT ( 'NONE',  ( 4.090334381980924583, -1.039670344891037601, 1.483205724144847748 ) ) ;
#121573=CARTESIAN_POINT ( 'NONE',  ( 4.688045340743730804, 1.047092163662701525, 1.477968688824328858 ) ) ;
#121577=CARTESIAN_POINT ( 'NONE',  ( 5.283604245000163679, -1.767202373759840572, 0.5838029059755837080 ) ) ;
#121579=CARTESIAN_POINT ( 'NONE',  ( 2.882342042720618558, -0.5589011775578194285, -1.832234547041192929 ) ) ;
#121587=CARTESIAN_POINT ( 'NONE',  ( 1.763735852432495754, 1.075751846022491964, 1.792481376920366687 ) ) ;
#121589=CARTESIAN_POINT ( 'NONE',  ( 6.739296538182359519, -1.720230304288400625, 0.8672215684524892110 ) ) ;
#121591=CARTESIAN_POINT ( 'NONE',  ( 2.643341535394112540, -1.351257319430071435, -1.227710988083303256 ) ) ;
#121594=CARTESIAN_POINT ( 'NONE',  ( 1.486696478045932635, 1.897211281248304848, 0.5285659569534242319 ) ) ;
#121595=CARTESIAN_POINT ( 'NONE',  ( 3.825673241664818036, 1.036335792742661299, -1.642260645495984495 ) ) ;
#121599=CARTESIAN_POINT ( 'NONE',  ( 6.578945215809504532, 1.736110340762307969, 0.6705269824554618285 ) ) ;
#121601=CARTESIAN_POINT ( 'NONE',  ( 3.779626292077961747, 0.2561244552635975058, -2.104982076983111572 ) ) ;
#121610=CARTESIAN_POINT ( 'NONE',  ( 3.369579884941567016, 1.780956498284639533, -0.4009276245297774266 ) ) ;
#121611=CARTESIAN_POINT ( 'NONE',  ( 5.911342272548038679, -1.897112096406332382, 0.6839327336411115121 ) ) ;
#121617=CARTESIAN_POINT ( 'NONE',  ( 4.399188623838041323, 1.502396186649012311, 1.114296746780506497 ) ) ;
#121619=CARTESIAN_POINT ( 'NONE',  ( 1.805176890173798565, 1.601487618425012638, 1.070529213009919101 ) ) ;
#121626=CARTESIAN_POINT ( 'NONE',  ( 1.300578652796330115, 1.418844934001600944, -1.571659118156268908 ) ) ;
#121629=CARTESIAN_POINT ( 'NONE',  ( 4.838769763947080804, -2.006773940031422399, -0.5081810985937407210 ) ) ;
#121630=CARTESIAN_POINT ( 'NONE',  ( 0.6789530235665336422, 1.236279375446739603, 1.364625092910062953 ) ) ;
#121632=CARTESIAN_POINT ( 'NONE',  ( 5.660817213934862480, 1.366460917787317930, 1.848312285176759717 ) ) ;
#121636=CARTESIAN_POINT ( 'NONE',  ( 1.570720025219290328, -2.177795595024238473, -0.7155201368211090429 ) ) ;
#121640=CARTESIAN_POINT ( 'NONE',  ( 4.822180446859828606, 1.858854579410177843, 0.5619951038204271665 ) ) ;
#121645=CARTESIAN_POINT ( 'NONE',  ( 5.853752780977106163, -1.389761788226477002, -1.313969904969368496 ) ) ;
#121646=CARTESIAN_POINT ( 'NONE',  ( 5.489470343000498076, -0.4852711138302409077, 1.957169415941109269 ) ) ;
#121650=CARTESIAN_POINT ( 'NONE',  ( 2.959016038526005143, 0.3060221511422682727, -2.067984839732572855 ) ) ;
#121651=CARTESIAN_POINT ( 'NONE',  ( 1.762210296550786204, -1.254468555733399660, 1.248734745320427830 ) ) ;
#121654=CARTESIAN_POINT ( 'NONE',  ( 4.716876218882520178, -0.1156266834452194386, 2.289457304130739779 ) ) ;
#121655=CARTESIAN_POINT ( 'NONE',  ( 2.167524683544871600, -1.071679988950867024, 1.371128027196461208 ) ) ;
#121658=CARTESIAN_POINT ( 'NONE',  ( 2.723678392350858957, -1.506833864184083493, -0.8575499777047421723 ) ) ;
#121660=CARTESIAN_POINT ( 'NONE',  ( 2.067058339702015246, 1.609816819982702985, -1.457078277656477905 ) ) ;
#121662=CARTESIAN_POINT ( 'NONE',  ( 4.048064755690682581, 0.9548552675892291175, 1.776167154503265566 ) ) ;
#121663=CARTESIAN_POINT ( 'NONE',  ( 2.343750000000001332, 1.895863743164134307, 0.7852924748298687474 ) ) ;
#121666=CARTESIAN_POINT ( 'NONE',  ( 1.166875649673270399, -1.740261045891202230, -0.8264182621567657261 ) ) ;
#121668=CARTESIAN_POINT ( 'NONE',  ( 4.113701061080524468, 1.785520537663972451, 1.321432767922005924 ) ) ;
#121670=CARTESIAN_POINT ( 'NONE',  ( -0.2106854629475270468, 2.024676876401194203, -2.413177685601196831 ) ) ;
#121676=CARTESIAN_POINT ( 'NONE',  ( 0.3818600843802121836, 0.2116341679995105141, -2.211193375792892546 ) ) ;
#121677=CARTESIAN_POINT ( 'NONE',  ( 6.039501783790233169, 1.813256598412491982, -0.7494862575098263369 ) ) ;
#121680=CARTESIAN_POINT ( 'NONE',  ( 0.5620833348847533717, 2.138143771118843350, -0.3165822943479515983 ) ) ;
#121682=CARTESIAN_POINT ( 'NONE',  ( 3.068856176772206457, 1.495872946324308783, -1.420456422295824916 ) ) ;
#121686=CARTESIAN_POINT ( 'NONE',  ( 4.815616550699190590, -1.834762568278673900, 0.3632225495420540184 ) ) ;
#121687=CARTESIAN_POINT ( 'NONE',  ( 4.166485388134741008, 1.137239580169274067, 1.309253364134143505 ) ) ;
#121688=CARTESIAN_POINT ( 'NONE',  ( 2.964111632446063016, -1.609175542312387908, -0.6635834015607346981 ) ) ;
#121689=CARTESIAN_POINT ( 'NONE',  ( 0.3633196395196974793, 0.2168307188613327052, -2.282096724506751162 ) ) ;
#121691=CARTESIAN_POINT ( 'NONE',  ( 4.792568760853118448, 1.737405308921141645, -1.162709912544395152 ) ) ;
#121692=CARTESIAN_POINT ( 'NONE',  ( 6.421825219014824171, 1.115965409679237963, -1.589096094497045142 ) ) ;
#121696=CARTESIAN_POINT ( 'NONE',  ( 0.4752326960846975923, -2.001511663014220677, -0.2440270837566413387 ) ) ;
#121697=CARTESIAN_POINT ( 'NONE',  ( 0.7211286721200690364, 1.601891702520108485, -1.389630591760198541 ) ) ;
#121699=CARTESIAN_POINT ( 'NONE',  ( 6.346327303948391396, 0.3419391630616851474, -1.987045965717588958 ) ) ;
#121702=CARTESIAN_POINT ( 'NONE',  ( 2.491022521637117570, -2.029929026191950925, -0.6131127883793399125 ) ) ;
#121704=CARTESIAN_POINT ( 'NONE',  ( 4.213378774425760476, -0.3099129147984269195, 1.799030153321119263 ) ) ;
#121712=CARTESIAN_POINT ( 'NONE',  ( 2.021745798758204149, -0.4384165714973499162, 1.971471537551409803 ) ) ;
#121713=CARTESIAN_POINT ( 'NONE',  ( 5.842855468016632692, 0.4250294216477692455, 2.165293060021292515 ) ) ;
#121715=CARTESIAN_POINT ( 'NONE',  ( 3.080726782406420838, 1.750568488035513681, 0.6316850995219197573 ) ) ;
#121720=CARTESIAN_POINT ( 'NONE',  ( 5.479063914364931343, -0.04889757770590653918, -1.825204647902956889 ) ) ;
#121724=CARTESIAN_POINT ( 'NONE',  ( 6.884150277402729223, -0.1485532345978715640, 1.983297619905934006 ) ) ;
#121725=CARTESIAN_POINT ( 'NONE',  ( 0.02286245922865359423, -1.065969982613410583, -1.375977130364250955 ) ) ;
#121726=CARTESIAN_POINT ( 'NONE',  ( 5.707753894846095299, -0.5660891107236701858, 2.237086922978877457 ) ) ;
#121728=CARTESIAN_POINT ( 'NONE',  ( 0.6146155864290882009, 1.423047967033652883, -1.490775708471054006 ) ) ;
#121730=CARTESIAN_POINT ( 'NONE',  ( 5.202631756544580988, -1.620200680833181694, -1.630429044757361723 ) ) ;
#121734=CARTESIAN_POINT ( 'NONE',  ( 5.910993886665249164, 1.650546521282238110, 0.8803886038859505270 ) ) ;
#121735=CARTESIAN_POINT ( 'NONE',  ( 3.726736447152957599, 1.348887845406310682, -1.355897031963343213 ) ) ;
#121737=CARTESIAN_POINT ( 'NONE',  ( 5.074942902252104204, -2.077123540546990110, -0.7459609299403434646 ) ) ;
#121742=CARTESIAN_POINT ( 'NONE',  ( 5.918629486560170960, -0.7630358368452618834, -1.978611909900826582 ) ) ;
#121743=CARTESIAN_POINT ( 'NONE',  ( 2.345130104517737291, 0.5056967325399002178, 2.251352274652190122 ) ) ;
#121744=CARTESIAN_POINT ( 'NONE',  ( 3.754310534785664899, -1.959519245081872585, -0.09869234604030494018 ) ) ;
#121745=CARTESIAN_POINT ( 'NONE',  ( 0.2507196182260813533, -0.4238382354822354259, -1.922440920834954436 ) ) ;
#121749=CARTESIAN_POINT ( 'NONE',  ( 5.630092293170263495, 2.014432788975322630, 0.09412139267171715229 ) ) ;
#121751=CARTESIAN_POINT ( 'NONE',  ( 0.2515690823673248921, 0.7017594223384625574, 1.702352774230586618 ) ) ;
#121753=CARTESIAN_POINT ( 'NONE',  ( 3.397511025282150321, -1.916906860828609727, 1.019255427985159779 ) ) ;
#121755=CARTESIAN_POINT ( 'NONE',  ( 0.4926326669930108371, -1.172979896111199904, 1.766458537607276114 ) ) ;
#121760=CARTESIAN_POINT ( 'NONE',  ( 0.9310180319365793933, 0.1487380178207615700, 2.055447871051790720 ) ) ;
#121766=CARTESIAN_POINT ( 'NONE',  ( 3.457576163436149486, -1.449788379102138869, -1.247086912153513749 ) ) ;
#121767=CARTESIAN_POINT ( 'NONE',  ( 5.594547536969180612, -0.4332151766474266474, -1.715878325482506517 ) ) ;
#121770=CARTESIAN_POINT ( 'NONE',  ( 0.3514446173804542939, -1.281351489097491303, -1.280874292944272685 ) ) ;
#121772=CARTESIAN_POINT ( 'NONE',  ( 0.4267777427376097665, -1.641576225293687630, 0.9873106011929821957 ) ) ;
#121773=CARTESIAN_POINT ( 'NONE',  ( 2.277862540309500083, -2.008769142935047380, 0.5008063122204224893 ) ) ;
#121775=CIRCLE ( 'NONE', #187384, 0.1399999999999995970 ) ;
#121777=CARTESIAN_POINT ( 'NONE',  ( 6.385618529757402406, 1.291587659170100766, 1.353439767483602285 ) ) ;
#121778=CARTESIAN_POINT ( 'NONE',  ( 2.525780997283606499, -1.050937884436175418, -1.492673824175783093 ) ) ;
#121779=CARTESIAN_POINT ( 'NONE',  ( 6.639307388351803674, -1.973492857608965423, 0.9879489342229507143 ) ) ;
#121782=CARTESIAN_POINT ( 'NONE',  ( 4.369619704168957952, -0.3557292467365941180, 2.031631830423554774 ) ) ;
#121787=CARTESIAN_POINT ( 'NONE',  ( 6.877413708759195998, -0.1538780216673047430, 2.036608477593480959 ) ) ;
#121789=CARTESIAN_POINT ( 'NONE',  ( 4.007220386668823409, 1.851715269821294418, 1.114988852100415428 ) ) ;
#121790=CARTESIAN_POINT ( 'NONE',  ( 3.967448252881644155, -1.680364903119958120, -1.120146540189705497 ) ) ;
#121791=CARTESIAN_POINT ( 'NONE',  ( 6.620655732516642189, 2.417337544263608251, 2.554705107920357321 ) ) ;
#121792=B_SPLINE_CURVE_WITH_KNOTS ( 'NONE', 3,
 ( #159607, #17588, #133541, #131425, #201671, #16526, #184369, #197425, #99940, #37058 ),
 .UNSPECIFIED., .F., .F.,
 ( 4, 1, 1, 1, 1, 1, 1, 4 ),
 ( 0.000000000000000000, 0.09599525230796020214, 0.1893027314675523320, 0.2592390727089966540, 0.3619855251144610819, 0.5211967264240887632, 0.7336899926499302893, 1.000000000000000000 ),
 .UNSPECIFIED. ) ;
#121796=CARTESIAN_POINT ( 'NONE',  ( 2.132046339962359038, 2.016188815772378629, 0.04465230659478347519 ) ) ;
#121801=CARTESIAN_POINT ( 'NONE',  ( 5.273660385517703553, 0.3669835118517565942, -1.876681294024809210 ) ) ;
#121805=CARTESIAN_POINT ( 'NONE',  ( 4.218375177057286152, 1.978055892313890229, 0.3905773888849966013 ) ) ;
#121808=CARTESIAN_POINT ( 'NONE',  ( 6.422847680425099348, 1.611446996373969265, 0.6153535913232581755 ) ) ;
#121812=CARTESIAN_POINT ( 'NONE',  ( 6.028550586359523678, 1.802609027081774951, 0.4991829554215552744 ) ) ;
#121814=CARTESIAN_POINT ( 'NONE',  ( 2.149362472714404504, 1.803301116200561882, -1.016697834320609672 ) ) ;
#121819=CARTESIAN_POINT ( 'NONE',  ( 0.5445462702219765472, -1.458543044971000402, 1.392561646250379814 ) ) ;
#121825=CARTESIAN_POINT ( 'NONE',  ( 5.817977454128726578, 0.9396041113334742123, -1.669243033268079879 ) ) ;
#121826=CARTESIAN_POINT ( 'NONE',  ( 0.1749903794560746517, 0.004523422195302349846, -1.955468523092759314 ) ) ;
#121832=CARTESIAN_POINT ( 'NONE',  ( 3.045950098598048328, 0.7793912989166664751, -2.016482303682599841 ) ) ;
#121835=CARTESIAN_POINT ( 'NONE',  ( 1.107859837811319581, 1.609452232531217275, 1.380942675281403353 ) ) ;
#121836=CARTESIAN_POINT ( 'NONE',  ( 5.983392046985361645, 1.685759371660649375, -0.7011634845648376801 ) ) ;
#121838=CARTESIAN_POINT ( 'NONE',  ( 1.932829124449897851, 0.1894527445373411501, 1.962211987329742113 ) ) ;
#121839=CARTESIAN_POINT ( 'NONE',  ( 4.095896644567202038, 1.253117935160457552, 1.444681106026260320 ) ) ;
#121842=CARTESIAN_POINT ( 'NONE',  ( 4.650814871655007288, -0.4294639348428323511, -1.921992245654633447 ) ) ;
#121843=CARTESIAN_POINT ( 'NONE',  ( 6.585517519612275272, -0.8250364709028266130, 1.756089425624817180 ) ) ;
#121849=CARTESIAN_POINT ( 'NONE',  ( 5.338497774373327509, 1.135723818413657549, -1.538349510941657838 ) ) ;
#121851=CARTESIAN_POINT ( 'NONE',  ( 1.360703683432495259, 0.8952624662355922469, 2.017188127302282030 ) ) ;
#121854=CARTESIAN_POINT ( 'NONE',  ( 5.777995030156034773, 1.982912992605226465, -0.3464542934713372158 ) ) ;
#121855=CARTESIAN_POINT ( 'NONE',  ( -0.02319159430947541692, 2.051704324979522820, -2.228571760951563618 ) ) ;
#121858=CARTESIAN_POINT ( 'NONE',  ( 3.613788337741298040, 0.5058112091442801272, -2.007490274132675445 ) ) ;
#121862=CARTESIAN_POINT ( 'NONE',  ( 0.9366540776252421097, 2.129889809250965271, 0.3686189752144660714 ) ) ;
#121867=CARTESIAN_POINT ( 'NONE',  ( 6.925078400183555694, 1.300159714275823664, 1.872400972051186496 ) ) ;
#121869=CARTESIAN_POINT ( 'NONE',  ( 4.957493672250036454, -1.635265592371325960, -0.5776676170772595542 ) ) ;
#121872=CARTESIAN_POINT ( 'NONE',  ( 2.043885321627556095, 1.424625833772466210, 1.502381739045772546 ) ) ;
#121873=CARTESIAN_POINT ( 'NONE',  ( 4.921547094770428288, -1.498112151610554665, -1.496348102564814209 ) ) ;
#121876=CARTESIAN_POINT ( 'NONE',  ( 2.061320199224637051, 1.634538341387161475, 1.098309876814192565 ) ) ;
#121879=CARTESIAN_POINT ( 'NONE',  ( 5.033284615878021562, -1.618354306187347769, -1.623638663579999752 ) ) ;
#121880=CARTESIAN_POINT ( 'NONE',  ( 1.471042373949003501, 0.1361147407585860392, -1.820667060309004937 ) ) ;
#121885=CARTESIAN_POINT ( 'NONE',  ( 2.320566727126192053, -0.7743817983801875027, -1.858503283895854841 ) ) ;
#121886=CARTESIAN_POINT ( 'NONE',  ( 3.010546455304231372, 0.6564385890225448161, 1.848828695667027677 ) ) ;
#121891=CARTESIAN_POINT ( 'NONE',  ( 5.982390446235332782, -0.3055207467456683701, -2.068066053634140200 ) ) ;
#121892=CARTESIAN_POINT ( 'NONE',  ( 4.645211000723334926, -1.368906681764755939, -1.121767690593698186 ) ) ;
#121894=CARTESIAN_POINT ( 'NONE',  ( 1.236564921189796662, 0.4304113295856801247, 2.148598399174222351 ) ) ;
#121895=CARTESIAN_POINT ( 'NONE',  ( -0.04197470322641042723, -1.553021824201283208, -0.7857045047398486526 ) ) ;
#121898=CARTESIAN_POINT ( 'NONE',  ( 0.1333692844072802142, 0.2389375359408679178, -2.087895146362698906 ) ) ;
#121899=CARTESIAN_POINT ( 'NONE',  ( 5.678471694547736703, 1.738760799997655537, 1.503693327295371862 ) ) ;
#121900=CARTESIAN_POINT ( 'NONE',  ( -0.09381621004311831158, -0.9424329983100244723, -1.976553698157037076 ) ) ;
#121901=CARTESIAN_POINT ( 'NONE',  ( 5.993412714446900047, 1.671717086469927560, 0.4595231857335341785 ) ) ;
#121902=CARTESIAN_POINT ( 'NONE',  ( 2.368051099418837069, 2.164043333312406503, -0.4318774905316472013 ) ) ;
#121903=CARTESIAN_POINT ( 'NONE',  ( 0.2511275705787468504, -0.4786951167374750571, -2.125832126681607370 ) ) ;
#121905=CARTESIAN_POINT ( 'NONE',  ( 1.446650934045516701, -1.493148645901293925, 1.501467539593546840 ) ) ;
#121906=CARTESIAN_POINT ( 'NONE',  ( 3.531250000000002220, -0.7852924748301699509, -1.895863743164005744 ) ) ;
#121907=CARTESIAN_POINT ( 'NONE',  ( 6.727182134110195832, 3.687949058358138466, 2.603069318070629912 ) ) ;
#121908=CARTESIAN_POINT ( 'NONE',  ( 4.313445203237777470, -0.3300861979738233254, 1.897755268844825816 ) ) ;
#121909=CARTESIAN_POINT ( 'NONE',  ( 0.9619568641448449364, -1.754440713604523916, -1.362318395052774633 ) ) ;
#121911=CARTESIAN_POINT ( 'NONE',  ( 1.611265326866499148, -0.2753845699034764838, 2.275703152891339176 ) ) ;
#121915=CARTESIAN_POINT ( 'NONE',  ( 3.756649600333416217, 2.210663847611141986, 0.2169408864148083815 ) ) ;
#121923=CARTESIAN_POINT ( 'NONE',  ( 1.617814789376757156, 0.2004366740697149929, 2.006445999502483257 ) ) ;
#121925=CARTESIAN_POINT ( 'NONE',  ( 6.232891784722141892, -1.957473889884550289, -0.6504925196839649315 ) ) ;
#121927=CARTESIAN_POINT ( 'NONE',  ( -0.1296875068448159751, 0.001480089298542403009, -1.826395826379861864 ) ) ;
#121930=CARTESIAN_POINT ( 'NONE',  ( 1.246904684444858136, -1.390570190391905658, -1.094529049636628226 ) ) ;
#121931=CARTESIAN_POINT ( 'NONE',  ( 0.3873425458618062200, -0.6819987885887256462, -1.897696807414723796 ) ) ;
#121932=CARTESIAN_POINT ( 'NONE',  ( -0.07694640568740516995, -1.131669979810394633, -1.452919414246391261 ) ) ;
#121933=CARTESIAN_POINT ( 'NONE',  ( 3.650172380179962150, 0.8259502761284505112, 2.138564905064809896 ) ) ;
#121934=CARTESIAN_POINT ( 'NONE',  ( 3.152128525617302834, -1.393660036906883226, 1.203213496783587910 ) ) ;
#121937=CARTESIAN_POINT ( 'NONE',  ( 3.047666980291532823, 0.6586017179070653427, -1.702814618940437619 ) ) ;
#121938=CARTESIAN_POINT ( 'NONE',  ( 3.920546200773936896, -1.392545040883992336, -1.458557299768625581 ) ) ;
#121940=CARTESIAN_POINT ( 'NONE',  ( 3.327297708271567345, 0.05365531978675056046, 2.262033696468904065 ) ) ;
#121942=CARTESIAN_POINT ( 'NONE',  ( 5.526436043951506782, 1.257118228488460110, -1.689427636868174210 ) ) ;
#121944=CARTESIAN_POINT ( 'NONE',  ( 3.420434311836465291, 0.9283866757503267397, 1.850595421526677775 ) ) ;
#121947=CARTESIAN_POINT ( 'NONE',  ( 5.268275487455277073, 2.118052368503114291, -0.1043780312826799589 ) ) ;
#121949=CARTESIAN_POINT ( 'NONE',  ( 1.137189532436083672, -1.741952243817600721, 0.8230948124841385161 ) ) ;
#121956=CARTESIAN_POINT ( 'NONE',  ( 0.7212869692094016072, 1.677245448433011710, -1.456619292340176841 ) ) ;
#121957=CARTESIAN_POINT ( 'NONE',  ( 2.221831145078187575, -2.042928948074810069, 0.5108812299794410761 ) ) ;
#121960=CARTESIAN_POINT ( 'NONE',  ( 0.1388275050690327694, -0.1366109201720016320, -1.830645452005694951 ) ) ;
#121966=CARTESIAN_POINT ( 'NONE',  ( 1.758217466200185042, 0.8068918862002281145, -1.961288232260410380 ) ) ;
#121969=CARTESIAN_POINT ( 'NONE',  ( 3.771884902471400292, -1.933230903833718539, 0.3329965046865584477 ) ) ;
#121970=CARTESIAN_POINT ( 'NONE',  ( 1.780366757100563913, -1.156431984057613827, 1.826190802295484472 ) ) ;
#121972=CARTESIAN_POINT ( 'NONE',  ( 1.768857366986800406, 1.761637791510446860, -0.5354853023365884201 ) ) ;
#121976=CARTESIAN_POINT ( 'NONE',  ( 3.679424820307465538, -0.8558964687110992564, 1.515225693578539978 ) ) ;
#121979=CARTESIAN_POINT ( 'NONE',  ( 0.7608789386071808103, -1.564954856162886765, 1.491513986042219297 ) ) ;
#121980=CARTESIAN_POINT ( 'NONE',  ( 3.919295934624257960, 0.7230291454519314209, 1.882185965797255278 ) ) ;
#121981=CARTESIAN_POINT ( 'NONE',  ( 6.825078400183518745, 0.5555073798480349989, 2.295529415773037929 ) ) ;
#121982=CARTESIAN_POINT ( 'NONE',  ( 0.1105426557568081891, -0.9253945370547181914, -1.951590883024490353 ) ) ;
#121984=CARTESIAN_POINT ( 'NONE',  ( 2.799638878761875116, -0.6198165829789729075, 1.871555056500016745 ) ) ;
#121985=CARTESIAN_POINT ( 'NONE',  ( 6.609000000000042618, 6.036791015687303918, 2.594900324319386886 ) ) ;
#121986=CARTESIAN_POINT ( 'NONE',  ( 2.454547613406708351, -1.690768538996465509, -0.9553028803331271579 ) ) ;
#121991=CARTESIAN_POINT ( 'NONE',  ( -0.1106856583840877539, 4.089587022985669229, -2.551888050631024640 ) ) ;
#121996=CARTESIAN_POINT ( 'NONE',  ( 6.352564483950959406, 0.7153834962906236994, 2.193980215933882150 ) ) ;
#121997=CARTESIAN_POINT ( 'NONE',  ( 6.760214184729610665, -1.961454122871961747, 0.04698431645466792650 ) ) ;
#121998=CARTESIAN_POINT ( 'NONE',  ( 4.223457129239616137, 0.2443821477370981265, -1.946437379933690481 ) ) ;
#122000=CARTESIAN_POINT ( 'NONE',  ( 0.9674229098759130618, -1.967888300253183953, -0.4390273639364171698 ) ) ;
#122002=CARTESIAN_POINT ( 'NONE',  ( 2.501287867402203879, -0.2026288386562236921, 2.107594835487134777 ) ) ;
#122006=CARTESIAN_POINT ( 'NONE',  ( 3.609164914601064922, -1.813629950718143702, 0.3161406477080672128 ) ) ;
#122009=CARTESIAN_POINT ( 'NONE',  ( 4.166350089634453191, 2.120059694336435374, -0.05518752902338577848 ) ) ;
#122010=CARTESIAN_POINT ( 'NONE',  ( 0.1636598862229492191, -1.205073137261414962, 1.392071761982638378 ) ) ;
#122014=CARTESIAN_POINT ( 'NONE',  ( 4.077457721052785367, 1.941698500476006117, -0.6908173846359686454 ) ) ;
#122016=CARTESIAN_POINT ( 'NONE',  ( 1.505144418776669601, -1.827259764946763454, 0.2261131901925839127 ) ) ;
#122021=CARTESIAN_POINT ( 'NONE',  ( 0.6630615684519860498, -1.595754342771567025, 1.524677653706180802 ) ) ;
#122023=CARTESIAN_POINT ( 'NONE',  ( 3.901889172025752472, -0.6612649319669267056, 2.163591406342895596 ) ) ;
#122025=CARTESIAN_POINT ( 'NONE',  ( 3.498146571883210321, -0.8881612436112231723, 1.578813691393302410 ) ) ;
#122026=CARTESIAN_POINT ( 'NONE',  ( 3.784325452683900526, -0.6063896298742013080, -1.817255877250848473 ) ) ;
#122027=CARTESIAN_POINT ( 'NONE',  ( 5.898901817742318698, 0.4001337562283372451, 2.031160294743330486 ) ) ;
#122030=CARTESIAN_POINT ( 'NONE',  ( 2.395336953769642729, 1.522948423943527363, 1.251906274522778251 ) ) ;
#122031=CARTESIAN_POINT ( 'NONE',  ( 1.237189336409921570, -1.742702465754492058, 0.8212270227533255973 ) ) ;
#122032=CARTESIAN_POINT ( 'NONE',  ( 4.117926171558832671, -0.9613396577640184182, -1.604580606731422554 ) ) ;
#122033=CARTESIAN_POINT ( 'NONE',  ( 3.317284684000018746, 2.086097511483188338, 0.9870085806921449212 ) ) ;
#122034=CARTESIAN_POINT ( 'NONE',  ( 3.174093412877276865, -0.9148440431442562693, -1.620569831483926082 ) ) ;
#122039=CARTESIAN_POINT ( 'NONE',  ( 1.014449334229026611, -0.9484566428747326361, -1.880489036503508959 ) ) ;
#122045=CARTESIAN_POINT ( 'NONE',  ( 1.090109951703751801, 1.206612241219229942, 1.619577932830415623 ) ) ;
#122050=CARTESIAN_POINT ( 'NONE',  ( 1.581558009922879204, 1.997867266642009643, -0.8257073301623578665 ) ) ;
#122053=CARTESIAN_POINT ( 'NONE',  ( 6.825078400183548055, 3.702925343214446663, 2.370119418288775925 ) ) ;
#122056=CARTESIAN_POINT ( 'NONE',  ( 5.366422816783521732, -1.968444216653497003, -0.4370823996120917765 ) ) ;
#122058=CARTESIAN_POINT ( 'NONE',  ( 0.06437606466144081552, -1.426665095847098330, 1.663708609037084951 ) ) ;
#122060=CARTESIAN_POINT ( 'NONE',  ( 6.702040708066513197, -2.161345696851162845, 0.04751196314212167288 ) ) ;
#122064=CARTESIAN_POINT ( 'NONE',  ( 1.458442676765151269, -1.819496111524568027, -0.5994125798251969117 ) ) ;
#122069=CARTESIAN_POINT ( 'NONE',  ( 2.789346554370454534, 1.219787599184172233, 1.219827592095571456 ) ) ;
#122071=CARTESIAN_POINT ( 'NONE',  ( 1.985279565377489508, 1.216254750358658487, 1.285827030011628347 ) ) ;
#122073=CARTESIAN_POINT ( 'NONE',  ( 2.490887342608373078, -1.927107516443892221, -0.5821121120333644372 ) ) ;
#122075=CARTESIAN_POINT ( 'NONE',  ( 5.280388062626482970, -1.229865305990836877, 1.832093573602276759 ) ) ;
#122078=CARTESIAN_POINT ( 'NONE',  ( 4.617906949270495609, -0.5647423089508787353, 2.043846993246847710 ) ) ;
#122079=CARTESIAN_POINT ( 'NONE',  ( 4.271111354109316416, 1.799915745204151429, -0.9091612155255476280 ) ) ;
#122080=CARTESIAN_POINT ( 'NONE',  ( 4.588045372560112689, 1.048790434826195384, 1.476901585074356316 ) ) ;
#122084=CARTESIAN_POINT ( 'NONE',  ( 1.639302681421180852, -1.352760811461351187, -1.292285834730774852 ) ) ;
#122085=CARTESIAN_POINT ( 'NONE',  ( 6.674438497507635404, -1.118711561685633349, 1.443368817030561635 ) ) ;
#122086=CARTESIAN_POINT ( 'NONE',  ( 6.076794983551159213, -1.275939312151072258, 1.286130553019491307 ) ) ;
#122095=CARTESIAN_POINT ( 'NONE',  ( 4.183913158364858553, 2.056144659531285779, -0.5182805708664263156 ) ) ;
#122096=CARTESIAN_POINT ( 'NONE',  ( -0.1296875068447916890, 6.948706544289747988, -2.421546651465163347 ) ) ;
#122098=CARTESIAN_POINT ( 'NONE',  ( 6.098895391831223201, 1.613120528903468243, -1.132937624142603905 ) ) ;
#122100=CARTESIAN_POINT ( 'NONE',  ( 0.4396980093101590659, -1.910362728465137439, 0.6353400594101745735 ) ) ;
#122102=CARTESIAN_POINT ( 'NONE',  ( 0.1931602983361295767, 1.844477155017531844, 1.039358475685886907 ) ) ;
#122104=CARTESIAN_POINT ( 'NONE',  ( 2.049362625460974030, 1.802418521853879962, -1.018503948505583789 ) ) ;
#122108=CARTESIAN_POINT ( 'NONE',  ( 4.769523239323490316, 1.203412094891454842, 1.709343392706575315 ) ) ;
#122111=CARTESIAN_POINT ( 'NONE',  ( 3.188313505853744179, -1.798300186086329688, -0.3134973320952222364 ) ) ;
#122112=CARTESIAN_POINT ( 'NONE',  ( 1.769862606763368706, 1.806619053477545700, -0.1335387089566111574 ) ) ;
#122116=CARTESIAN_POINT ( 'NONE',  ( 4.700333112842928429, -2.206180118464650786, -0.05804534286662357823 ) ) ;
#122119=CARTESIAN_POINT ( 'NONE',  ( 2.332540574144434053, 1.247770424613745543, -1.449200414897835687 ) ) ;
#122122=CARTESIAN_POINT ( 'NONE',  ( 6.637176860265922684, -0.09746846054551477900, -2.068182370504913159 ) ) ;
#122124=CARTESIAN_POINT ( 'NONE',  ( 5.390230798962840630, -0.5317533105795355652, -2.125930911514521959 ) ) ;
#122135=CARTESIAN_POINT ( 'NONE',  ( 5.752806990244247132, -0.4974732019265226679, -2.009498513695342936 ) ) ;
#122136=CARTESIAN_POINT ( 'NONE',  ( 1.704704067347760699, 1.882482151684254923, 0.7231221989368596947 ) ) ;
#122139=CARTESIAN_POINT ( 'NONE',  ( 1.570551226722196381, -2.081687204081467346, -0.6850663153453034893 ) ) ;
#122140=CARTESIAN_POINT ( 'NONE',  ( 5.408770660633122063, 1.379882519126625295, -1.195542987486551301 ) ) ;
#122148=CARTESIAN_POINT ( 'NONE',  ( 2.823586671956069605, 1.020774559177588081, -1.532180179759069283 ) ) ;
#122149=CARTESIAN_POINT ( 'NONE',  ( 6.310797300923185915, -0.5409384057308598281, -1.939081195975641769 ) ) ;
#122150=CARTESIAN_POINT ( 'NONE',  ( 2.038793776981039141, 2.199649879376049721, -0.6664975855598854748 ) ) ;
#122152=CARTESIAN_POINT ( 'NONE',  ( 6.403176761927252159, -1.659045864033869666, 1.046607237317781269 ) ) ;
#122154=CARTESIAN_POINT ( 'NONE',  ( 0.1833691866889655686, 7.629137130509075604, -2.653448492709729933 ) ) ;
#122155=CARTESIAN_POINT ( 'NONE',  ( 3.920094060441734030, -1.906919942518231936, 0.1457910263855527466 ) ) ;
#122157=CARTESIAN_POINT ( 'NONE',  ( 0.2739938332866619364, -2.030697503880642518, 0.4024348779970430834 ) ) ;
#122160=CARTESIAN_POINT ( 'NONE',  ( 2.718400508848108466, 1.969533948853121386, 0.7019594197221010745 ) ) ;
#122161=CARTESIAN_POINT ( 'NONE',  ( 1.199835987674138460, -1.870836310881810682, -0.003643258294119822160 ) ) ;
#122162=CARTESIAN_POINT ( 'NONE',  ( 1.880232294074701604, -0.2495702131940503166, 2.000550610736757218 ) ) ;
#122166=CARTESIAN_POINT ( 'NONE',  ( 2.647703282711162398, 0.5884205719196273776, 1.638072370343154116 ) ) ;
#122171=CARTESIAN_POINT ( 'NONE',  ( 2.754212737529265986, 0.5811417601193774596, 1.624163882408189652 ) ) ;
#122172=CARTESIAN_POINT ( 'NONE',  ( 3.193114300108112147, 1.729001323093733111, 1.346577201094656395 ) ) ;
#122173=CARTESIAN_POINT ( 'NONE',  ( 5.285833163787800437, 1.479997892162682849, 1.637210856327932618 ) ) ;
#122176=CARTESIAN_POINT ( 'NONE',  ( 3.309609623814670165, -1.772202297075220256, -1.253863066769088874 ) ) ;
#122177=CARTESIAN_POINT ( 'NONE',  ( 2.314841291766779108, 1.630546960418734148, 0.8213866120303781049 ) ) ;
#122179=CARTESIAN_POINT ( 'NONE',  ( 4.136029606254186142, 2.116781002543933088, -0.05581379417103624063 ) ) ;
#122180=CARTESIAN_POINT ( 'NONE',  ( 6.539320575229245591, 2.459069921018588900, 2.280790101157427419 ) ) ;
#122182=CARTESIAN_POINT ( 'NONE',  ( 4.950848118218736715, -1.935628577297190400, -1.227853487085520001 ) ) ;
#122186=CARTESIAN_POINT ( 'NONE',  ( -0.1104750535120025967, -0.004616138082884357029, -2.103378236956429337 ) ) ;
#122193=CARTESIAN_POINT ( 'NONE',  ( 6.883263157960391787, 1.253787318140922480, 2.167784446185747171 ) ) ;
#122195=CARTESIAN_POINT ( 'NONE',  ( 5.274064633610318076, 1.777012466945230962, -0.9530095070046653571 ) ) ;
#122197=CARTESIAN_POINT ( 'NONE',  ( 3.608308625203029862, 2.062741128266020851, 0.004805803398660184710 ) ) ;
#122199=CARTESIAN_POINT ( 'NONE',  ( 6.883263157960371359, 7.052674735402435502, 2.544342468817725855 ) ) ;
#122203=CARTESIAN_POINT ( 'NONE',  ( 6.509741685903361663, -1.029359178063901092, -1.934661654277470166 ) ) ;
#122204=CARTESIAN_POINT ( 'NONE',  ( 3.621720349255663773, 0.2986264320336135536, 1.994071497604548382 ) ) ;
#122205=CARTESIAN_POINT ( 'NONE',  ( 3.597050949361340511, -0.5310884314010614338, 1.763007376093472800 ) ) ;
#122207=CARTESIAN_POINT ( 'NONE',  ( 0.2699429432127123385, -1.132711312255540115, 1.300796998575669772 ) ) ;
#122210=CARTESIAN_POINT ( 'NONE',  ( 1.389710824352110574, -0.8328434156393785814, -2.142668459815112669 ) ) ;
#122212=CARTESIAN_POINT ( 'NONE',  ( 6.737213295527981316, -2.024711933681651477, 1.009942563148768846 ) ) ;
#122213=CARTESIAN_POINT ( 'NONE',  ( 2.244876548131835126, 0.4624279887704956238, 2.054504457251419502 ) ) ;
#122223=CARTESIAN_POINT ( 'NONE',  ( 3.621504738650199950, 1.906737781736141280, 1.139490138724685853 ) ) ;
#122224=CARTESIAN_POINT ( 'NONE',  ( 2.343918204863020271, 2.190988169473460090, 0.05230688499441307066 ) ) ;
#122226=CARTESIAN_POINT ( 'NONE',  ( 6.883263157960398892, 2.970623603138923929, 2.399364662246627589 ) ) ;
#122228=CARTESIAN_POINT ( 'NONE',  ( 5.986763597034562068, 1.890319730748804439, 0.5246630281777532323 ) ) ;
#122231=CARTESIAN_POINT ( 'NONE',  ( 6.610000000000026965, 7.052677709320480659, 2.598153670447616470 ) ) ;
#122234=CARTESIAN_POINT ( 'NONE',  ( 4.992489932941452935, -1.175987964647656536, 1.764448611491518548 ) ) ;
#122237=CARTESIAN_POINT ( 'NONE',  ( 5.946190753372003535, 2.158995856162956084, 0.1107517376499680406 ) ) ;
#122239=CARTESIAN_POINT ( 'NONE',  ( 5.038538826285253514, -1.576363729006284187, 0.9512496309353534185 ) ) ;
#122243=CARTESIAN_POINT ( 'NONE',  ( 0.3447215323711784740, 0.5487897507440896439, -1.651745661738156734 ) ) ;
#122244=CARTESIAN_POINT ( 'NONE',  ( 6.827182134110222123, 7.629137130509070275, 2.410944104600701188 ) ) ;
#122246=CARTESIAN_POINT ( 'NONE',  ( 4.065412822539622439, 0.2671453805177248508, -2.145074402785766665 ) ) ;
#122249=CARTESIAN_POINT ( 'NONE',  ( 3.432649856329002880, 2.108609624295390006, 0.4754391814798044069 ) ) ;
#122250=CARTESIAN_POINT ( 'NONE',  ( 4.393795938483449071, -0.7573388051436024115, 1.820269059793070410 ) ) ;
#122251=CARTESIAN_POINT ( 'NONE',  ( 3.954193900006929052, 1.254965027507263464, 1.196595854207074261 ) ) ;
#122252=CARTESIAN_POINT ( 'NONE',  ( 1.224469250947546328, 2.113408192816915943, 0.5798510048089372537 ) ) ;
#122253=CARTESIAN_POINT ( 'NONE',  ( 0.6754003219355340093, -2.174137316696134636, -0.7736760779102586083 ) ) ;
#122254=CARTESIAN_POINT ( 'NONE',  ( 4.059881558241601240, 2.045671965140416937, -0.2483333800566180083 ) ) ;
#122255=CARTESIAN_POINT ( 'NONE',  ( 5.952673665805181535, -1.667821083538678861, -0.9947414763863350329 ) ) ;
#122261=ORIENTED_EDGE ( 'NONE', *, *, #24409, .T. ) ;
#122263=CARTESIAN_POINT ( 'NONE',  ( 3.733602637680955461, -2.039903990487580643, 0.8422819887162477093 ) ) ;
#122266=CARTESIAN_POINT ( 'NONE',  ( 0.2857036466711966316, -1.138303949996006148, -1.472634861895638636 ) ) ;
#122268=CARTESIAN_POINT ( 'NONE',  ( -0.1291982275798781443, -0.004298614154785855221, -2.073875112923003083 ) ) ;
#122272=CARTESIAN_POINT ( 'NONE',  ( 6.714805130922314014, -0.1276373473727103192, 1.811824464382847832 ) ) ;
#122274=CARTESIAN_POINT ( 'NONE',  ( 1.903268112024224523, 1.712809940758196259, 1.145777703309367457 ) ) ;
#122280=CARTESIAN_POINT ( 'NONE',  ( 0.4970371946629085769, 1.713755840317375601, -1.144362063176207922 ) ) ;
#122282=CARTESIAN_POINT ( 'NONE',  ( 5.161589042655139181, 0.9124512986629171873, 1.599201395118980740 ) ) ;
#122287=CARTESIAN_POINT ( 'NONE',  ( 4.406973378220558679, 1.706932345810768359, -1.398813476408675260 ) ) ;
#122288=CARTESIAN_POINT ( 'NONE',  ( 0.5269342146079664113, 2.068330297753611546, 0.6279826202375409228 ) ) ;
#122290=CARTESIAN_POINT ( 'NONE',  ( 6.469024005207689498, -1.393930998056407189, 1.156871781951673395 ) ) ;
#122291=CARTESIAN_POINT ( 'NONE',  ( 1.147673126774436225, 1.985868168208399842, -0.3494872464938902357 ) ) ;
#122293=CARTESIAN_POINT ( 'NONE',  ( 1.687308557152231270, -1.277188091954140514, -1.910694296540839332 ) ) ;
#122298=CARTESIAN_POINT ( 'NONE',  ( 1.375632740723360836, 1.111493989511678881, 1.504490780774490499 ) ) ;
#122299=CARTESIAN_POINT ( 'NONE',  ( 2.342982756445275427, -1.756855002775299379, -0.9896843009072553432 ) ) ;
#122303=CARTESIAN_POINT ( 'NONE',  ( 5.250649905694958264, 0.6104557620976447385, 2.015647016877469166 ) ) ;
#122308=CARTESIAN_POINT ( 'NONE',  ( 4.008073073761713623, -0.7691326184188684856, 1.867817587601346307 ) ) ;
#122311=CARTESIAN_POINT ( 'NONE',  ( 6.619587925713169341, 0.3565228922877783924, -2.031493691534612012 ) ) ;
#122313=CARTESIAN_POINT ( 'NONE',  ( 4.024825912876791811, 2.051136489140188424, 0.6822911077620784637 ) ) ;
#122319=CARTESIAN_POINT ( 'NONE',  ( 2.330757530436095237, -1.336968151498512336, 1.710609410560095522 ) ) ;
#122322=CARTESIAN_POINT ( 'NONE',  ( 1.382094229771430705, -0.2707140722739818650, -1.821126350552772610 ) ) ;
#122324=CARTESIAN_POINT ( 'NONE',  ( 3.175498511859841333, 1.392037702009111033, 1.692654053968026151 ) ) ;
#122325=CARTESIAN_POINT ( 'NONE',  ( 6.983263157960365675, 7.629137130509066722, 2.553810918356711479 ) ) ;
#122326=CARTESIAN_POINT ( 'NONE',  ( 3.590934319571597033, -0.4389823211032486960, -2.219365549907009960 ) ) ;
#122332=CARTESIAN_POINT ( 'NONE',  ( 5.536323748068817885, 1.743679661707888018, 0.3015777700523143978 ) ) ;
#122333=CARTESIAN_POINT ( 'NONE',  ( 3.492840887459470522, -1.940756296261561209, -0.5346130827820451126 ) ) ;
#122335=CARTESIAN_POINT ( 'NONE',  ( 2.081218647941612154, -0.1023907900198107734, -2.103586654547675128 ) ) ;
#122338=CARTESIAN_POINT ( 'NONE',  ( 1.047236342219150407, 1.738656489303032737, -0.9252727719080054980 ) ) ;
#122341=CARTESIAN_POINT ( 'NONE',  ( 6.117428737855862941, 1.511353622793030427, 0.9985130155200862001 ) ) ;
#122345=CARTESIAN_POINT ( 'NONE',  ( 5.207814216083940018, -1.861544245658670604, 0.1842191830812093256 ) ) ;
#122347=CARTESIAN_POINT ( 'NONE',  ( 5.717656431054087385, 0.4094431674900833040, -2.029196096928844284 ) ) ;
#122354=EDGE_CURVE ( 'NONE', #136413, #11785, #106169, .T. ) ;
#122358=CARTESIAN_POINT ( 'NONE',  ( 4.914483161888778540, 0.7490505147796695518, 1.813437088826752142 ) ) ;
#122360=CARTESIAN_POINT ( 'NONE',  ( 2.214220036344019871, -1.617569417291262690, -1.203170845901546215 ) ) ;
#122363=CARTESIAN_POINT ( 'NONE',  ( 0.9783777488623355278, -2.139296967303818686, -0.4750931833387496694 ) ) ;
#122365=CARTESIAN_POINT ( 'NONE',  ( 1.774454573425466863, -1.774572579973210384, -0.5916213571805841731 ) ) ;
#122367=CARTESIAN_POINT ( 'NONE',  ( 4.201435496602879738, 1.796340046740346086, -0.9091319694144882613 ) ) ;
#122370=CARTESIAN_POINT ( 'NONE',  ( 3.779011003814860548, 1.787463462570267447, -1.134484337778138174 ) ) ;
#122372=CARTESIAN_POINT ( 'NONE',  ( 4.773920332862017446, -2.031068740936771366, 0.4005940302675218834 ) ) ;
#122374=CARTESIAN_POINT ( 'NONE',  ( 1.681308932615958041, 1.444198878393717411, 1.512019500502481018 ) ) ;
#122375=CARTESIAN_POINT ( 'NONE',  ( 6.720655732516647163, -0.004400176169771369272, 2.173773060281408931 ) ) ;
#122376=CARTESIAN_POINT ( 'NONE',  ( 6.159193757800505153, -1.567253032978152660, -0.9359774744091067245 ) ) ;
#122384=CARTESIAN_POINT ( 'NONE',  ( 5.865855438783555087, 0.5507134639845879809, -1.831277125143706552 ) ) ;
#122391=CARTESIAN_POINT ( 'NONE',  ( 6.433220217788329087, -1.621194592471734364, -1.198847091081943539 ) ) ;
#122394=CARTESIAN_POINT ( 'NONE',  ( 0.1394461523057474728, 0.7845381482947767493, -1.808261586923729736 ) ) ;
#122397=CARTESIAN_POINT ( 'NONE',  ( 4.030098220014290078, 1.090402053431119622, 1.639822181875214557 ) ) ;
#122398=CARTESIAN_POINT ( 'NONE',  ( 4.517203946846011675, -1.842441744247227842, 0.8197884948388589610 ) ) ;
#122401=CARTESIAN_POINT ( 'NONE',  ( 4.418054252288761141, 1.349281245414082342, -1.726737887558588591 ) ) ;
#122403=CARTESIAN_POINT ( 'NONE',  ( 2.731371607455813422, -1.798138232897347644, 0.6916047562727283271 ) ) ;
#122405=CARTESIAN_POINT ( 'NONE',  ( -0.1298852118743892559, 2.894271690123681573, -2.215574276383952768 ) ) ;
#122406=FACE_OUTER_BOUND ( 'NONE', #137608, .T. ) ;
#122412=CARTESIAN_POINT ( 'NONE',  ( 5.724118993814841794, 1.776208094789998304, 0.4848738846057951135 ) ) ;
#122413=CARTESIAN_POINT ( 'NONE',  ( 3.141273780804701765, 0.05169848057553745602, 2.012594475454997145 ) ) ;
#122414=CARTESIAN_POINT ( 'NONE',  ( 5.642068729656325665, -0.04839715497878017969, -2.298027403377851385 ) ) ;
#122416=CARTESIAN_POINT ( 'NONE',  ( 3.080726782406420838, 1.750568488035513681, 0.6316850995219197573 ) ) ;
#122424=CARTESIAN_POINT ( 'NONE',  ( 6.269093502906415871, 2.000459608610676288, -0.6076830679577133187 ) ) ;
#122429=CARTESIAN_POINT ( 'NONE',  ( 0.8030139110496161692, 1.490934425176414502, 1.053415343471690857 ) ) ;
#122432=CARTESIAN_POINT ( 'NONE',  ( 2.127222352579770881, 0.3811697317757706815, 1.691523546451817683 ) ) ;
#122435=CARTESIAN_POINT ( 'NONE',  ( 6.727182134110200273, 7.629137130509069387, 2.789055895399249696 ) ) ;
#122436=CARTESIAN_POINT ( 'NONE',  ( 6.895391736652770831, -1.943277935985653349, 0.9682779983983346161 ) ) ;
#122437=CARTESIAN_POINT ( 'NONE',  ( 5.953692858212231265, 0.5253669772854427933, -1.748464709795935157 ) ) ;
#122438=CARTESIAN_POINT ( 'NONE',  ( 3.116010788575247936, 1.952738871351952232, -0.1875660449981580158 ) ) ;
#122442=CARTESIAN_POINT ( 'NONE',  ( 3.369896858953733698, 0.5134250039646214292, -2.057278921464212207 ) ) ;
#122446=CARTESIAN_POINT ( 'NONE',  ( 1.885682352965558639, -1.950755244972163904, 0.6936349442826782452 ) ) ;
#122449=CARTESIAN_POINT ( 'NONE',  ( 4.828890449103202975, 1.532327986240004103, -1.608379539844583705 ) ) ;
#122451=CARTESIAN_POINT ( 'NONE',  ( 1.723655420059172050, 2.274453554295458702, 0.3322429970207661509 ) ) ;
#122453=CARTESIAN_POINT ( 'NONE',  ( 0.3913574919355842785, -1.795980968407092426, 0.7896611536716554580 ) ) ;
#122457=CARTESIAN_POINT ( 'NONE',  ( 6.216338285296751920, 1.720575329815833943, 0.6561210673821931127 ) ) ;
#122461=CARTESIAN_POINT ( 'NONE',  ( 2.953266587970606150, -1.684550232849800544, 0.9053361341156559439 ) ) ;
#122462=CARTESIAN_POINT ( 'NONE',  ( -0.2102771530458225069, 7.629137130509110243, -2.803678522703976661 ) ) ;
#122463=CARTESIAN_POINT ( 'NONE',  ( 3.610098185430905104, -0.6985691267104906510, -1.577150584296799440 ) ) ;
#122464=CARTESIAN_POINT ( 'NONE',  ( 2.747280062631300535, 0.2910806042949847239, -1.995268371848608835 ) ) ;
#122465=CARTESIAN_POINT ( 'NONE',  ( 3.481312804724666421, -2.296076454524886845, -0.1115701876132721843 ) ) ;
#122466=CARTESIAN_POINT ( 'NONE',  ( 3.409705294423628352, -0.4451680670645007387, 2.218022689048837481 ) ) ;
#122467=CARTESIAN_POINT ( 'NONE',  ( 6.656868561830338038, -1.629224735911166233, 1.334343933791133141 ) ) ;
#122469=CARTESIAN_POINT ( 'NONE',  ( 4.534285406439878763, 1.735348426437629765, 0.3461848140887160974 ) ) ;
#122471=CARTESIAN_POINT ( 'NONE',  ( 1.377341666110833529, 2.116387791839238641, -0.8810097948994728423 ) ) ;
#122472=CARTESIAN_POINT ( 'NONE',  ( 6.105383947169263692, -1.826632712061267094, 0.2301338403083788009 ) ) ;
#122474=CARTESIAN_POINT ( 'NONE',  ( 5.384801694919699067, 1.933943663793664225, -1.030698541907522081 ) ) ;
#122477=CARTESIAN_POINT ( 'NONE',  ( 5.846161131210033446, -0.9342735719010831774, 1.847668428805064655 ) ) ;
#122478=CARTESIAN_POINT ( 'NONE',  ( 0.3742329010679063539, -2.001858617179689492, -0.2420261300371470137 ) ) ;
#122480=CARTESIAN_POINT ( 'NONE',  ( 4.318917837333097864, 1.761897194459721927, 0.7795765077616281236 ) ) ;
#122483=CARTESIAN_POINT ( 'NONE',  ( 1.688022500292500228, 2.124017718264622268, -0.6504838024826449239 ) ) ;
#122493=CARTESIAN_POINT ( 'NONE',  ( 1.433958818539453395, 1.165882187713672247, 1.577721859592796205 ) ) ;
#122498=CARTESIAN_POINT ( 'NONE',  ( 6.320756440275016708, -1.388331291134708767, 1.386421665916007795 ) ) ;
#122501=CARTESIAN_POINT ( 'NONE',  ( 6.789893189004300389, -0.9291300992274166282, 1.949920244826188309 ) ) ;
#122505=CARTESIAN_POINT ( 'NONE',  ( 0.9834252619641962179, 1.251819791611600285, 1.390119989509101650 ) ) ;
#122506=CARTESIAN_POINT ( 'NONE',  ( 6.784571902810725419, -1.680486618648807218, 0.4264331113166124343 ) ) ;
#122509=CARTESIAN_POINT ( 'NONE',  ( 4.177398808104064720, 1.432170664236757540, 1.658919600136643524 ) ) ;
#122510=CARTESIAN_POINT ( 'NONE',  ( 4.067613405475267285, 0.2862205578705340203, -2.289715105617713409 ) ) ;
#122511=CARTESIAN_POINT ( 'NONE',  ( 0.1982117360312448395, -2.060432452642831702, -0.05102901230808094130 ) ) ;
#122512=CARTESIAN_POINT ( 'NONE',  ( 2.572129589083424150, -1.858482343604623610, -0.5632287606567585314 ) ) ;
#122515=CARTESIAN_POINT ( 'NONE',  ( 5.062787373817618786, 0.6179034821891697948, 2.028544477791139222 ) ) ;
#122517=CARTESIAN_POINT ( 'NONE',  ( 3.674454069786535548, 1.462445212485608437, 1.388486266691544957 ) ) ;
#122521=CARTESIAN_POINT ( 'NONE',  ( 0.8205984872286451459, 1.685833220154912881, 0.7012733028506010768 ) ) ;
#122526=CARTESIAN_POINT ( 'NONE',  ( 5.120021580010623907, -1.100570584753908454, -1.742215132906791641 ) ) ;
#122532=CARTESIAN_POINT ( 'NONE',  ( 5.162762804107727810, 0.5884847259931770269, 1.932018068032066438 ) ) ;
#122533=CARTESIAN_POINT ( 'NONE',  ( 5.426523936546859161, -0.9972995744461101708, -1.984925452567573023 ) ) ;
#122537=CARTESIAN_POINT ( 'NONE',  ( 4.399328490915206835, 1.653984737846543540, 1.229246434344443806 ) ) ;
#122538=CARTESIAN_POINT ( 'NONE',  ( 3.551407868487792552, -1.352154898762620849, 1.496051317864898866 ) ) ;
#122545=CARTESIAN_POINT ( 'NONE',  ( 4.253279712585047001, -1.993766238088546361, -0.2985801555873274227 ) ) ;
#122546=CARTESIAN_POINT ( 'NONE',  ( 3.363068133243895197, 1.796009578954290253, -0.4044003374430102382 ) ) ;
#122548=CARTESIAN_POINT ( 'NONE',  ( 1.717812883538033297, -0.2792282863031622653, 2.290681961221084695 ) ) ;
#122551=CARTESIAN_POINT ( 'NONE',  ( 4.253314833958360630, -1.794556715717060769, -1.204719293387515267 ) ) ;
#122554=CARTESIAN_POINT ( 'NONE',  ( 3.726148964702048705, -2.024938297411133625, -1.087335920097615594 ) ) ;
#122556=CARTESIAN_POINT ( 'NONE',  ( 2.043623373375623942, 0.7184291972081280342, -1.727395513401897453 ) ) ;
#122557=CARTESIAN_POINT ( 'NONE',  ( 6.825078400183526739, -0.0002198122173602961866, 1.955566246027613531 ) ) ;
#122561=CARTESIAN_POINT ( 'NONE',  ( 2.051678093609669240, -1.773579625386853875, -1.313098587465796774 ) ) ;
#122566=CARTESIAN_POINT ( 'NONE',  ( 6.491095702449441340, 1.715375089605765124, -0.9715357305846801239 ) ) ;
#122567=CARTESIAN_POINT ( 'NONE',  ( 5.426528828858072195, 1.378586375901286187, -1.850541897242431677 ) ) ;
#122568=CARTESIAN_POINT ( 'NONE',  ( 6.830517471914854255, -1.143533572366756124, 1.468690548319721900 ) ) ;
#122570=CARTESIAN_POINT ( 'NONE',  ( 2.641531011850445143, 1.887532825382558066, -0.8318756707885038848 ) ) ;
#122577=CARTESIAN_POINT ( 'NONE',  ( 5.266168369200141086, -2.161202989243858674, 0.2077703183603739345 ) ) ;
#122578=APPLICATION_CONTEXT ( 'automotive_design' ) ;
#122580=CARTESIAN_POINT ( 'NONE',  ( 5.056134578334451568, -1.329838508726857382, 1.273713382018211382 ) ) ;
#122583=CARTESIAN_POINT ( 'NONE',  ( 0.4033012769992084245, -0.5052730135347225371, 1.800932346938296069 ) ) ;
#122584=CARTESIAN_POINT ( 'NONE',  ( 0.7732102150014728004, -2.130643883221981838, -0.7610950190743612787 ) ) ;
#122589=CARTESIAN_POINT ( 'NONE',  ( 1.762210296550786204, -1.254468555733399660, 1.248734745320427830 ) ) ;
#122590=CARTESIAN_POINT ( 'NONE',  ( 6.533844907621704223, -1.952130696095262463, 0.4912315161729706725 ) ) ;
#122592=CARTESIAN_POINT ( 'NONE',  ( 3.567908551050925858, -0.9411222629213971125, 1.668380548182837542 ) ) ;
#122594=CARTESIAN_POINT ( 'NONE',  ( 3.982825254072485777, 1.869399454171687180, 0.6202158817144760583 ) ) ;
#122595=CARTESIAN_POINT ( 'NONE',  ( 0.3168469074051638024, -0.7203255543706194031, -1.994627023381766673 ) ) ;
#122597=CARTESIAN_POINT ( 'NONE',  ( 3.326877442632663939, 0.04465521416292458912, 1.870282673472216439 ) ) ;
#122598=CARTESIAN_POINT ( 'NONE',  ( 6.234932630344998117, 0.1766075427261544484, 1.715814389380666327 ) ) ;
#122600=CARTESIAN_POINT ( 'NONE',  ( 2.192262590105994668, -0.9421081357594159877, 1.995820444975453745 ) ) ;
#122603=CARTESIAN_POINT ( 'NONE',  ( 6.373494408814909917, -0.2414686440028299685, 1.946897059556201848 ) ) ;
#122607=CARTESIAN_POINT ( 'NONE',  ( 0.1747926744264677867, 0.7439089246787933263, -1.939883394317852616 ) ) ;
#122611=CARTESIAN_POINT ( 'NONE',  ( 2.963400493335893948, 1.747644659881589568, 1.109742091278065113 ) ) ;
#122615=CARTESIAN_POINT ( 'NONE',  ( 0.4694063198951373694, -1.707435420315214003, -1.078448885650341582 ) ) ;
#122620=CARTESIAN_POINT ( 'NONE',  ( 0.07459516483343266169, 4.098104556601829707, -2.310507343083552989 ) ) ;
#122622=CARTESIAN_POINT ( 'NONE',  ( 5.518907608433407219, 2.013924273726455549, -0.09612181791086168992 ) ) ;
#122623=CARTESIAN_POINT ( 'NONE',  ( 5.770691199759951040, -0.2880491948782157308, -1.893834403066462446 ) ) ;
#122625=CARTESIAN_POINT ( 'NONE',  ( 3.685266855566126321, 1.588411730319793769, 1.510178839762461811 ) ) ;
#122627=CARTESIAN_POINT ( 'NONE',  ( 2.795058504854182946, -0.1448928079688660830, -1.906987441340234568 ) ) ;
#122631=CARTESIAN_POINT ( 'NONE',  ( -0.1234324464992678227, -0.4448297287729073846, -1.973926538189611835 ) ) ;
#122633=CARTESIAN_POINT ( 'NONE',  ( 5.689076433642084041, 1.658752129386225516, 1.432425853890168188 ) ) ;
#122635=CARTESIAN_POINT ( 'NONE',  ( 3.170621359714973941, -1.593115903276512757, -0.6614109595024783017 ) ) ;
#122637=CARTESIAN_POINT ( 'NONE',  ( 6.011998765391792787, -0.7129019540204998284, 1.997330473063135381 ) ) ;
#122641=CARTESIAN_POINT ( 'NONE',  ( 0.6253529088778920775, 0.1960189665039281104, -1.952063659030291998 ) ) ;
#122647=CARTESIAN_POINT ( 'NONE',  ( 3.158660791640830467, 0.4427227019567353539, 1.756387338163778233 ) ) ;
#122651=CARTESIAN_POINT ( 'NONE',  ( 3.773895570499671503, 1.797357569013877887, -0.2251608728849313346 ) ) ;
#122655=CARTESIAN_POINT ( 'NONE',  ( 5.213276571848306951, -1.572085989900060765, -0.9957144527335654027 ) ) ;
#122657=CARTESIAN_POINT ( 'NONE',  ( 2.812013442917372430, 1.061847183940438422, -1.594151112820214822 ) ) ;
#122658=CARTESIAN_POINT ( 'NONE',  ( 0.8502975112493587062, 0.5252643332615304361, 1.748389446526978031 ) ) ;
#122670=CARTESIAN_POINT ( 'NONE',  ( 1.640690513341718670, -1.765443103004183056, 1.119499978516135252 ) ) ;
#122671=CARTESIAN_POINT ( 'NONE',  ( 6.458035534591947346, 1.921153000004784284, -0.1426463852419664891 ) ) ;
#122673=CARTESIAN_POINT ( 'NONE',  ( 2.432394421669949569, 1.770131964307398498, 0.4459858026567494194 ) ) ;
#122674=CARTESIAN_POINT ( 'NONE',  ( 3.826972293661185187, 2.095320012007126476, 0.6930106488920934060 ) ) ;
#122676=CARTESIAN_POINT ( 'NONE',  ( 0.7031954830387620037, 1.685401770928725007, -0.9037484838233383888 ) ) ;
#122677=CARTESIAN_POINT ( 'NONE',  ( 1.310928286630644646, -1.554615626247756177, 1.209165358520351674 ) ) ;
#122678=CARTESIAN_POINT ( 'NONE',  ( 3.526839302598220982, -1.793260235690095072, 0.7459913709994684394 ) ) ;
#122682=CARTESIAN_POINT ( 'NONE',  ( 6.561375291409637711, 1.546756896810308035, 1.034385502077879382 ) ) ;
#122687=CARTESIAN_POINT ( 'NONE',  ( 2.736070936638954176, 2.175344985778558726, 0.2654339622269741295 ) ) ;
#122693=CARTESIAN_POINT ( 'NONE',  ( 4.002439121739418404, -0.5745171773131328985, -1.733004836422600725 ) ) ;
#122697=CARTESIAN_POINT ( 'NONE',  ( -0.02968770228139894218, 7.629137130509075604, -2.426318643530885222 ) ) ;
#122698=CARTESIAN_POINT ( 'NONE',  ( 4.030043484472041193, 1.001115284758803625, -1.580040089582811280 ) ) ;
#122700=CARTESIAN_POINT ( 'NONE',  ( 2.490742943097464135, -0.3295026218355610603, -1.897965567226393979 ) ) ;
#122701=CARTESIAN_POINT ( 'NONE',  ( 6.631700630569578259, 1.878258136613653040, -0.5663492180864730940 ) ) ;
#122706=CARTESIAN_POINT ( 'NONE',  ( -0.07047696482224277692, -1.639844204322737697, -1.338861086256079913 ) ) ;
#122710=CARTESIAN_POINT ( 'NONE',  ( 4.610256228194366201, 2.069909489248497714, -0.04556564433023241323 ) ) ;
#122711=CARTESIAN_POINT ( 'NONE',  ( -0.04178991631376138827, -1.644041690304678616, -0.8291446804715857377 ) ) ;
#122714=CARTESIAN_POINT ( 'NONE',  ( 5.608098314261791728, -0.05969564267381716194, 2.298051806275173359 ) ) ;
#122718=CARTESIAN_POINT ( 'NONE',  ( 0.1645876019286318381, -1.492192613954560265, 1.740154187221523818 ) ) ;
#122720=CARTESIAN_POINT ( 'NONE',  ( 5.384693163835662766, 1.711646917711911353, -0.9173020705802971131 ) ) ;
#122721=ORIENTED_EDGE ( 'NONE', *, *, #16450, .F. ) ;
#122725=CARTESIAN_POINT ( 'NONE',  ( 6.117437049485344502, 1.593764408019750389, 1.056661447057717362 ) ) ;
#122726=CARTESIAN_POINT ( 'NONE',  ( 5.542203953035277131, 0.8216685229280199509, 1.841735684200429990 ) ) ;
#122730=CARTESIAN_POINT ( 'NONE',  ( 2.378955762007132435, 1.911079870108543410, -0.8480884496332024014 ) ) ;
#122731=CARTESIAN_POINT ( 'NONE',  ( 1.621574733132331358, -0.9795727578338263575, -1.473812506242745179 ) ) ;
#122732=CARTESIAN_POINT ( 'NONE',  ( 6.381482430641396419, -0.5404875331735843336, -1.942542459342583294 ) ) ;
#122734=CARTESIAN_POINT ( 'NONE',  ( 4.031398662939575495, -1.579512745870830237, -1.661420017294244156 ) ) ;
#122735=CARTESIAN_POINT ( 'NONE',  ( 2.571852248423611709, -1.665254919270848344, -0.5056227470447529626 ) ) ;
#122738=CARTESIAN_POINT ( 'NONE',  ( 1.668881318695322413, -0.6185640615885504845, -1.619952590838618312 ) ) ;
#122740=CARTESIAN_POINT ( 'NONE',  ( 1.170091191536073660, -0.8321358839059491697, -1.664716676500255010 ) ) ;
#122741=CARTESIAN_POINT ( 'NONE',  ( 2.787735123443566110, -2.026669663610313865, 0.7793237752812106622 ) ) ;
#122743=CARTESIAN_POINT ( 'NONE',  ( 3.696500153570709379, 1.422608671726926177, -1.429447704489300364 ) ) ;
#122744=CARTESIAN_POINT ( 'NONE',  ( 2.750000000000001332, 1.574424887750340441E-13, 2.052068128417947612 ) ) ;
#122747=CARTESIAN_POINT ( 'NONE',  ( 1.219610691686360049, -1.880083933147856934, 0.4191893400790832613 ) ) ;
#122749=CARTESIAN_POINT ( 'NONE',  ( 4.060924178622978609, 0.5945426864985210447, 2.140278595106285042 ) ) ;
#122756=CARTESIAN_POINT ( 'NONE',  ( 0.6279475770487872310, -0.3202071342675495425, 2.197987568497254074 ) ) ;
#122757=CARTESIAN_POINT ( 'NONE',  ( 4.861744986159981075, -0.5251177144562025889, 1.890194517805739771 ) ) ;
#122761=CARTESIAN_POINT ( 'NONE',  ( 5.483742561420515749, 1.513553928502100465, 1.681752807289581986 ) ) ;
#122764=CARTESIAN_POINT ( 'NONE',  ( 2.945816691342293847, 1.456820166381930015, 1.460492231956188824 ) ) ;
#122768=CARTESIAN_POINT ( 'NONE',  ( 4.587079231881330266, 1.671727914585485530, -0.8392916717318499309 ) ) ;
#122769=CARTESIAN_POINT ( 'NONE',  ( 3.287501071874948000, 1.364548152031169082, -1.070007228145404943 ) ) ;
#122770=CARTESIAN_POINT ( 'NONE',  ( 3.368457041919175055, 0.03905506635776007096, -1.740168019110074793 ) ) ;
#122771=CARTESIAN_POINT ( 'NONE',  ( 0.6094042559229868594, -0.3290114652876909296, 2.268531362689259812 ) ) ;
#122772=CARTESIAN_POINT ( 'NONE',  ( 1.290363523627102049, -0.9912053058820711193, 1.971723787660728977 ) ) ;
#122773=CARTESIAN_POINT ( 'NONE',  ( 4.564062515778636531, -1.364536961465147913, 1.584173057036510013 ) ) ;
#122774=CARTESIAN_POINT ( 'NONE',  ( 5.841732304440537149, 1.939831336911639781, 0.09320031894976579800 ) ) ;
#122777=CARTESIAN_POINT ( 'NONE',  ( 0.4400775573648734174, -1.704940109561555950, -1.076314675215600314 ) ) ;
#122778=CARTESIAN_POINT ( 'NONE',  ( 1.090261293813089560, 1.267680250814690934, 1.699812782343253170 ) ) ;
#122783=CARTESIAN_POINT ( 'NONE',  ( 4.019992336727182369, -0.9402185374879183932, -1.564826772493657536 ) ) ;
#122790=CARTESIAN_POINT ( 'NONE',  ( 2.197526642425628118, 1.844980167888200961, -0.8223984085018556378 ) ) ;
#122791=CARTESIAN_POINT ( 'NONE',  ( 6.176841753231244958, -2.093540797633717254, -0.6980159708611932690 ) ) ;
#122794=CARTESIAN_POINT ( 'NONE',  ( 2.781907013001069906, -1.067198605185412763, -1.524341717138616215 ) ) ;
#122800=CARTESIAN_POINT ( 'NONE',  ( 5.461492464141177727, 0.3521552718798379722, -1.791230276788812414 ) ) ;
#122804=CARTESIAN_POINT ( 'NONE',  ( 0.2273701076888709205, -1.544753302685021534, -0.7874640570253422789 ) ) ;
#122805=CARTESIAN_POINT ( 'NONE',  ( 0.2689661900789627746, 0.9977586965290600185, 1.425695987021274647 ) ) ;
#122806=CARTESIAN_POINT ( 'NONE',  ( 5.268348002110199602, 1.133478272989609348, 2.010090980756351176 ) ) ;
#122808=CARTESIAN_POINT ( 'NONE',  ( 0.7025034608351670151, -0.6919086601019829308, -1.941309234904058600 ) ) ;
#122810=CARTESIAN_POINT ( 'NONE',  ( 6.011119390975155241, 2.295276066174879670, 0.1220560631845988148 ) ) ;
#122814=CARTESIAN_POINT ( 'NONE',  ( 5.700035372616791385, -1.870836310086241294, 0.001406584917262864625 ) ) ;
#122816=CARTESIAN_POINT ( 'NONE',  ( 3.357576282340120066, -1.451192137084562628, -1.245647637661301044 ) ) ;
#122818=CARTESIAN_POINT ( 'NONE',  ( 5.057340365224886725, -1.863002784048470639, -1.182737378625432489 ) ) ;
#122819=CARTESIAN_POINT ( 'NONE',  ( 4.891875743818586919, -2.106850654347144580, 0.2108507618673941542 ) ) ;
#122821=CARTESIAN_POINT ( 'NONE',  ( 6.983263157960335477, 4.692686028926381425, 2.608776679625654182 ) ) ;
#122824=CARTESIAN_POINT ( 'NONE',  ( 5.654972079148370412, 0.4136758123431219514, 2.079573305287989449 ) ) ;
#122825=CARTESIAN_POINT ( 'NONE',  ( 2.380262917520099553, 1.419673959206497527, 1.819133949716137844 ) ) ;
#122826=CARTESIAN_POINT ( 'NONE',  ( 3.385159196556942085, 0.04556868695702701727, 1.961494628812537444 ) ) ;
#122829=CARTESIAN_POINT ( 'NONE',  ( 6.508646177561060675, 0.6413444998595011493, 1.960425241914983907 ) ) ;
#122833=CARTESIAN_POINT ( 'NONE',  ( 6.034388706570055660, 0.6371486477873434806, 1.913263546360920220 ) ) ;
#122837=CARTESIAN_POINT ( 'NONE',  ( 1.780376006863694904, -1.203675225865230569, -1.806662255390781180 ) ) ;
#122839=CARTESIAN_POINT ( 'NONE',  ( 0.3168469074051638024, -0.7203255543706194031, -1.994627023381766673 ) ) ;
#122844=CARTESIAN_POINT ( 'NONE',  ( 1.018906392562862528, 1.903027849223213330, 0.7912521351585340978 ) ) ;
#122846=CARTESIAN_POINT ( 'NONE',  ( 6.727182134110193168, 4.701113012587437190, 2.373661997258198486 ) ) ;
#122851=CARTESIAN_POINT ( 'NONE',  ( 3.545477442914763078, -1.765841875850767906, 0.7343832577718925059 ) ) ;
#122852=CARTESIAN_POINT ( 'NONE',  ( 5.067173336470212064, 0.1711322554274422036, -1.761558580727173862 ) ) ;
#122856=CARTESIAN_POINT ( 'NONE',  ( 0.5799530485631685384, 0.8934014309100688500, 1.575905833579164694 ) ) ;
#122858=CARTESIAN_POINT ( 'NONE',  ( 6.169544653506280341, 1.324940883694783578, 1.383738526680919012 ) ) ;
#122859=CARTESIAN_POINT ( 'NONE',  ( 0.5024991115675537801, 2.064720838319131779, 0.1538615064654233477 ) ) ;
#122861=CARTESIAN_POINT ( 'NONE',  ( 5.805500895539822181, -0.4530025297027094888, 1.814837910242727226 ) ) ;
#122862=CARTESIAN_POINT ( 'NONE',  ( 2.455445036260803349, 0.4872311372507812655, -1.759406031448563557 ) ) ;
#122863=CARTESIAN_POINT ( 'NONE',  ( 6.270183524512255246, 1.130759168108757873, 1.895055401287759178 ) ) ;
#122866=CARTESIAN_POINT ( 'NONE',  ( 3.578633024105078331, 1.310608547571969540, -1.592757226543355165 ) ) ;
#122870=CARTESIAN_POINT ( 'NONE',  ( 0.4741787938652639034, 1.244221353789766837, 1.767418780601250017 ) ) ;
#122871=CARTESIAN_POINT ( 'NONE',  ( 6.426242046702522082, 1.060841730010402495, 1.777776562702712226 ) ) ;
#122873=CARTESIAN_POINT ( 'NONE',  ( 3.532649767544591590, 2.108058052951222283, 0.4773693597190583060 ) ) ;
#122874=CARTESIAN_POINT ( 'NONE',  ( 3.791669620513484773, 1.900943035724310448, -0.6826196560621737852 ) ) ;
#122875=CARTESIAN_POINT ( 'NONE',  ( 2.576550507925364109, 1.283677811227203147, -1.483670167215108693 ) ) ;
#122877=CARTESIAN_POINT ( 'NONE',  ( 6.720655732516663150, 7.051555433583626353, 2.871889998671435240 ) ) ;
#122884=CARTESIAN_POINT ( 'NONE',  ( 2.466030083290056130, -1.032479112849067793, 1.731996155473938259 ) ) ;
#122887=CARTESIAN_POINT ( 'NONE',  ( 6.240485052285455581, 1.095381943021833449, -1.567431287326017886 ) ) ;
#122891=CARTESIAN_POINT ( 'NONE',  ( 3.901970389206737444, -1.039011544341267745, -1.727992587138134306 ) ) ;
#122894=CARTESIAN_POINT ( 'NONE',  ( 6.774431772926147843, -1.055741295204252195, 1.364281925921766447 ) ) ;
#122898=CARTESIAN_POINT ( 'NONE',  ( 4.710133486059870478, -0.7981590245086762625, -1.691823354513532163 ) ) ;
#122900=CARTESIAN_POINT ( 'NONE',  ( 1.815371668717490339, -1.773540675419151169, -1.067758146248848128 ) ) ;
#122904=CARTESIAN_POINT ( 'NONE',  ( 0.4390776481996219727, -1.704952938511293814, -1.076296438737800454 ) ) ;
#122905=CARTESIAN_POINT ( 'NONE',  ( -0.2051949539778260834, -0.1395167590549877823, -1.781371329038708096 ) ) ;
#122911=CARTESIAN_POINT ( 'NONE',  ( 5.888286034446420736, -0.6943482264498787027, -1.785519067699488982 ) ) ;
#122918=CARTESIAN_POINT ( 'NONE',  ( 3.256853613824191029, -1.637998819981079990, 1.410756932016984155 ) ) ;
#122921=CARTESIAN_POINT ( 'NONE',  ( 1.266058358664986949, 0.6103625328083387425, -2.030891291126469600 ) ) ;
#122922=CARTESIAN_POINT ( 'NONE',  ( 6.334959139596201716, 0.1821375521317940283, 1.816452708017932238 ) ) ;
#122923=CARTESIAN_POINT ( 'NONE',  ( 0.9835902346791641770, 1.320712255264442803, 1.463733941802777716 ) ) ;
#122924=CARTESIAN_POINT ( 'NONE',  ( 3.252119977711815491, 0.8557668478980616777, -1.710280963351323846 ) ) ;
#122927=CARTESIAN_POINT ( 'NONE',  ( 5.301205566836260985, -1.690247886301226909, 1.010757534590230433 ) ) ;
#122929=CARTESIAN_POINT ( 'NONE',  ( 0.6384921070224542916, -1.665899481912515245, 0.9977595643581302909 ) ) ;
#122933=CARTESIAN_POINT ( 'NONE',  ( 5.959260761812961604, -1.790568634313693730, 1.135864312162476297 ) ) ;
#122935=CARTESIAN_POINT ( 'NONE',  ( 5.233030847706650057, 1.768443763404730307, 0.7281017474275592871 ) ) ;
#122937=CARTESIAN_POINT ( 'NONE',  ( 0.5345543961663907773, 1.132513062451316221, -1.893880525681296723 ) ) ;
#122939=CARTESIAN_POINT ( 'NONE',  ( 6.551439491213440824, -1.797098368391306655, 0.9074013689854224518 ) ) ;
#122943=CARTESIAN_POINT ( 'NONE',  ( 2.102089431743926706, 0.7944251937819692966, -1.912079865474418439 ) ) ;
#122946=CARTESIAN_POINT ( 'NONE',  ( 0.1632417891470130944, -1.931755829615459996, -0.9703963252955111196 ) ) ;
#122953=CARTESIAN_POINT ( 'NONE',  ( 6.925078400183573457, 0.5887076473912872254, 1.908330883025354030 ) ) ;
#122956=CARTESIAN_POINT ( 'NONE',  ( 4.412597608232919022, -1.071937594435016683, -1.363045487976799475 ) ) ;
#122958=CARTESIAN_POINT ( 'NONE',  ( 1.956005403265232978, -0.7013823251572397499, 1.947930506816720087 ) ) ;
#122959=CARTESIAN_POINT ( 'NONE',  ( 3.989952538763715140, -2.111419002029162328, 0.1578513319024783257 ) ) ;
#122963=CARTESIAN_POINT ( 'NONE',  ( 1.832793114640043131, -1.868399652882225981, -0.6228533014895777375 ) ) ;
#122965=CARTESIAN_POINT ( 'NONE',  ( 0.08795244648929222142, 1.102731429460445334, 1.562230693318837238 ) ) ;
#122966=CARTESIAN_POINT ( 'NONE',  ( 4.066585926679040064, -2.138228679320841152, -0.8265488639036464580 ) ) ;
#122967=CARTESIAN_POINT ( 'NONE',  ( 1.998415063578623085, -0.4859047700337820741, -1.759764234465097221 ) ) ;
#122972=CARTESIAN_POINT ( 'NONE',  ( 2.654543897082308312, 1.998474955683330334, 0.2423782132614532570 ) ) ;
#122973=CARTESIAN_POINT ( 'NONE',  ( 3.256644689873238629, -0.5649923015349536115, -1.878667693404307171 ) ) ;
#122976=CARTESIAN_POINT ( 'NONE',  ( 0.07536363704233049743, 2.002983476668462881, -2.558365315478607904 ) ) ;
#122977=CARTESIAN_POINT ( 'NONE',  ( 6.210894578592706772, -0.2570060295814159401, 2.074700711848826096 ) ) ;
#122978=CARTESIAN_POINT ( 'NONE',  ( 4.750734298983296355, -1.420434005603900429, 1.055588576545069657 ) ) ;
#122980=CARTESIAN_POINT ( 'NONE',  ( 0.6740948890744530297, -1.214310170130480593, 1.824057261183717582 ) ) ;
#122981=CARTESIAN_POINT ( 'NONE',  ( 6.140530580581591735, -1.466303750465405065, 0.9370796520578956734 ) ) ;
#122985=CARTESIAN_POINT ( 'NONE',  ( 6.416599408848439268, -1.497502150434773194, -1.744030381972218047 ) ) ;
#122987=CARTESIAN_POINT ( 'NONE',  ( 5.835191860132536767, -1.097891704307648597, 1.341895879554096727 ) ) ;
#122988=CARTESIAN_POINT ( 'NONE',  ( 1.471597369358583318, 0.1596246592955492538, -2.201166978212334424 ) ) ;
#122989=CARTESIAN_POINT ( 'NONE',  ( 6.250449712397290192, -2.160098187209258835, -0.2192636458223720386 ) ) ;
#122991=CARTESIAN_POINT ( 'NONE',  ( 1.516979485257620608, 0.2134662686405098542, 2.106589464619255558 ) ) ;
#122992=CARTESIAN_POINT ( 'NONE',  ( 2.593750000000001776, -1.895863743164140525, -0.7852924748298559798 ) ) ;
#122994=CARTESIAN_POINT ( 'NONE',  ( 6.727182134110178069, 2.947419669445831669, 2.641212418657997496 ) ) ;
#122995=CARTESIAN_POINT ( 'NONE',  ( 4.207974007929848881, -1.921269893987355593, 0.1410920886178046452 ) ) ;
#122996=CARTESIAN_POINT ( 'NONE',  ( 0.7509959265504009274, 2.189410886431830239, 0.3742058002541984729 ) ) ;
#123002=CARTESIAN_POINT ( 'NONE',  ( 3.387547421374631273, 0.05309406834838430178, -2.220816570709438498 ) ) ;
#123011=CARTESIAN_POINT ( 'NONE',  ( 1.793592486599729252, 1.492254607734722072, -1.356300734917381678 ) ) ;
#123013=CARTESIAN_POINT ( 'NONE',  ( 0.4267248635717044158, -1.349908593859616257, 1.559510075185864153 ) ) ;
#123016=CARTESIAN_POINT ( 'NONE',  ( 6.567905868640212752, -1.062476624526029312, 1.378933096211315101 ) ) ;
#123019=CARTESIAN_POINT ( 'NONE',  ( 1.510649146982666613, 1.557664219135522110, 0.8400682108315477015 ) ) ;
#123020=CARTESIAN_POINT ( 'NONE',  ( 0.05336153386781630759, -1.314994204386025434, 1.528742563917218078 ) ) ;
#123021=CARTESIAN_POINT ( 'NONE',  ( 0.2746299231596514012, 1.718356743839201561, -0.6618312839273902126 ) ) ;
#123022=CARTESIAN_POINT ( 'NONE',  ( 3.984120879971131401, -2.267471576223866414, -0.3361144993852988594 ) ) ;
#123023=CARTESIAN_POINT ( 'NONE',  ( 2.273173984786102775, 1.132353773513800510, 1.451651336590239927 ) ) ;
#123027=CARTESIAN_POINT ( 'NONE',  ( 3.399243825379614226, 1.438455020490635450, 1.123966471122700650 ) ) ;
#123028=CARTESIAN_POINT ( 'NONE',  ( 3.867814693791224112, -0.2004342644464084944, -2.006446243107910199 ) ) ;
#123030=CARTESIAN_POINT ( 'NONE',  ( 3.661208364039827856, -1.994111792441630726, -1.068896079077549910 ) ) ;
#123032=CARTESIAN_POINT ( 'NONE',  ( 5.034254431704021648, 1.084988065057530982, -1.804815602348212256 ) ) ;
#123034=CARTESIAN_POINT ( 'NONE',  ( 2.207561477879273593, -1.661462528888792090, -1.235070534849058266 ) ) ;
#123037=CARTESIAN_POINT ( 'NONE',  ( 6.217454246653871586, 1.762742247767977055, 1.178343227268910276 ) ) ;
#123040=CARTESIAN_POINT ( 'NONE',  ( 1.084454569787800304, -1.879374161238209773, -0.4228483607967240543 ) ) ;
#123048=CARTESIAN_POINT ( 'NONE',  ( 1.125557598851456786, 1.962289056045916524, 1.041162070263027761 ) ) ;
#123049=CARTESIAN_POINT ( 'NONE',  ( 1.835132634908468452, 0.2055991040930336133, 2.095883127255711464 ) ) ;
#123052=CARTESIAN_POINT ( 'NONE',  ( 6.104338052012460381, 1.858797879379699536, 0.09248701691148655812 ) ) ;
#123056=CARTESIAN_POINT ( 'NONE',  ( 0.01804983835817890528, -0.5593552815991027494, 2.045460531183339814 ) ) ;
#123059=CARTESIAN_POINT ( 'NONE',  ( 3.191801227909254912, -1.315628469008291557, -1.455533501494077342 ) ) ;
#123060=CARTESIAN_POINT ( 'NONE',  ( 2.536181837661064087, 1.019768383293401248, -1.906060392209196763 ) ) ;
#123061=CARTESIAN_POINT ( 'NONE',  ( 0.9953642579336658969, -1.841430844361633845, 2.783310008858119066E-05 ) ) ;
#123065=CARTESIAN_POINT ( 'NONE',  ( 3.978220273661048356, -0.1731065449946489199, -1.731690827559639878 ) ) ;
#123068=CARTESIAN_POINT ( 'NONE',  ( 0.9015118058452382677, 1.767791302423503685, 1.243857928393626633 ) ) ;
#123070=CARTESIAN_POINT ( 'NONE',  ( 2.091172504846372959, 1.163092143266548639, -1.646586049616038494 ) ) ;
#123072=CARTESIAN_POINT ( 'NONE',  ( 0.3566080023540801336, 0.8287714912002723811, 1.996717379258300840 ) ) ;
#123073=CARTESIAN_POINT ( 'NONE',  ( 2.219545571343143120, -1.912749475042923475, 0.4771270530836198565 ) ) ;
#123080=CARTESIAN_POINT ( 'NONE',  ( 2.121745675717867652, -0.4403476065239861903, 1.970919799026500607 ) ) ;
#123082=CARTESIAN_POINT ( 'NONE',  ( 5.790114358714919973, -1.044397830967594976, 2.057800239056095659 ) ) ;
#123085=CARTESIAN_POINT ( 'NONE',  ( 3.309375504473045293, -1.601080850277468715, -1.133301831143386007 ) ) ;
#123087=CARTESIAN_POINT ( 'NONE',  ( 0.1764080092822375156, 1.496053712750060383, 1.352152247781977179 ) ) ;
#123089=CARTESIAN_POINT ( 'NONE',  ( 2.888026961012623239, -2.114693475102703779, 0.1087559668010943809 ) ) ;
#123092=CARTESIAN_POINT ( 'NONE',  ( 1.833694255977034615, 1.820935426717207317, 0.2711280389895084353 ) ) ;
#123096=CARTESIAN_POINT ( 'NONE',  ( 4.570628194609677841, 0.8141925398062774821, 1.958264201954627026 ) ) ;
#123097=CARTESIAN_POINT ( 'NONE',  ( 0.4976878544296211015, -0.6176706345307936274, -1.734562967469073236 ) ) ;
#123101=CARTESIAN_POINT ( 'NONE',  ( 4.868464682339723737, -1.349271924330990080, 1.557713215823807174 ) ) ;
#123103=CARTESIAN_POINT ( 'NONE',  ( 0.9953642579336658969, -1.841430844361633845, 2.783310008858119066E-05 ) ) ;
#123108=CARTESIAN_POINT ( 'NONE',  ( 1.190363680384380229, -0.9894552095768920363, 1.972713631218452557 ) ) ;
#123109=CARTESIAN_POINT ( 'NONE',  ( 4.306154650063803935, -2.256721687276264099, 0.1609511959119753199 ) ) ;
#123111=CARTESIAN_POINT ( 'NONE',  ( 3.252039308394638173, 0.8100161731663655384, -1.620448113725055483 ) ) ;
#123112=CARTESIAN_POINT ( 'NONE',  ( 3.678834806144789749, 1.615436204272060472, -1.029439157428935658 ) ) ;
#123113=CARTESIAN_POINT ( 'NONE',  ( 5.793440749948310042, -1.873300974885267589, 0.8818263447485861217 ) ) ;
#123115=CARTESIAN_POINT ( 'NONE',  ( 3.080892710809614243, -0.1436740641204778401, -1.966277672030048107 ) ) ;
#123116=CARTESIAN_POINT ( 'NONE',  ( 0.6395170938602061650, -1.359983930408629194, -1.364592209491755082 ) ) ;
#123117=CARTESIAN_POINT ( 'NONE',  ( 3.942156681999692491, 1.861596489644477437, 0.1839347620080991341 ) ) ;
#123118=CARTESIAN_POINT ( 'NONE',  ( 2.684532350912737009, -1.185368471958246905, 1.979860261248457931 ) ) ;
#123119=CARTESIAN_POINT ( 'NONE',  ( 3.543253484755361615, 1.683469864222198797, -0.7936445362404942472 ) ) ;
#123125=CARTESIAN_POINT ( 'NONE',  ( 0.7507728315698600774, 0.6134373412659529512, 2.014746520763583959 ) ) ;
#123130=CARTESIAN_POINT ( 'NONE',  ( 1.863691559860299884, -1.706161385809309650, -1.259181899442491037 ) ) ;
#123132=CARTESIAN_POINT ( 'NONE',  ( 1.072527844217635584, 0.8224262283116140493, 1.844967818783457725 ) ) ;
#123137=CARTESIAN_POINT ( 'NONE',  ( 1.194844697948213463, -0.5240009448631496314, -2.097013730318515456 ) ) ;
#123139=CARTESIAN_POINT ( 'NONE',  ( 6.825078400183556049, 7.053092130845653784, 2.453807127456457238 ) ) ;
#123142=CARTESIAN_POINT ( 'NONE',  ( 6.016814611094169152, 0.2024578496369993375, 2.006372135924570088 ) ) ;
#123145=CARTESIAN_POINT ( 'NONE',  ( -0.04112450405316381286, -1.960553898366865555, -0.9795403211517728082 ) ) ;
#123147=CARTESIAN_POINT ( 'NONE',  ( 6.719591497160966931, -2.098179372288328182, 0.5198544864785522579 ) ) ;
#123151=CARTESIAN_POINT ( 'NONE',  ( 0.8256309606260933132, 0.7751641160983432366, -1.751937020314651150 ) ) ;
#123155=CARTESIAN_POINT ( 'NONE',  ( 3.017853972043908151, -0.8504761986376055960, -1.500546066986796490 ) ) ;
#123157=CARTESIAN_POINT ( 'NONE',  ( 0.7019891895669374549, -0.5885738721268447549, -1.669159149975569578 ) ) ;
#123158=CARTESIAN_POINT ( 'NONE',  ( 4.313639225654395837, -0.3805011380913872476, 2.173570407251994574 ) ) ;
#123162=CARTESIAN_POINT ( 'NONE',  ( 4.231183009085410340, 1.939187816756043237, 0.8583030597293441755 ) ) ;
#123163=CARTESIAN_POINT ( 'NONE',  ( 3.603138812553498216, -0.1455146663824242736, 2.011206757212272933 ) ) ;
#123167=CARTESIAN_POINT ( 'NONE',  ( 1.797508989346347619, -0.6330400025267440833, 1.760413054629046625 ) ) ;
#123179=CARTESIAN_POINT ( 'NONE',  ( 4.043311264919998038, 0.1072909356813686044, 2.118029240109862155 ) ) ;
#123180=CARTESIAN_POINT ( 'NONE',  ( -0.02948999725182251466, 0.2504340119564217870, -1.961592983597350459 ) ) ;
#123182=CARTESIAN_POINT ( 'NONE',  ( 5.589129042188730523, 1.739749244469630529, -0.9270521019464451618 ) ) ;
#123184=CARTESIAN_POINT ( 'NONE',  ( 0.6857920578585029459, 1.939116618559855842, -0.5408100507186993644 ) ) ;
#123186=CARTESIAN_POINT ( 'NONE',  ( 0.1580148589572556717, 1.223040929162301449, 1.728066982087714809 ) ) ;
#123188=CARTESIAN_POINT ( 'NONE',  ( 1.574760213118006735, 1.391939136705011348, -1.532762857463897843 ) ) ;
#123191=CARTESIAN_POINT ( 'NONE',  ( 3.873056903084231450, 1.968474739099084436, -0.7045419632574521085 ) ) ;
#123194=CARTESIAN_POINT ( 'NONE',  ( 2.203868028057700990, -1.825262823911228072, 0.04193083753635528516 ) ) ;
#123195=CARTESIAN_POINT ( 'NONE',  ( 1.488595082971344352, -1.720062743487455581, -0.5684112265044569678 ) ) ;
#123197=CARTESIAN_POINT ( 'NONE',  ( 5.057340365224886725, -1.863002784048470639, -1.182737378625432489 ) ) ;
#123199=CARTESIAN_POINT ( 'NONE',  ( 4.383934217864794647, 1.438874268414831015, 1.673263306058408340 ) ) ;
#123202=CARTESIAN_POINT ( 'NONE',  ( 3.193911838225035105, 1.215006091714765368, 1.476655219734591906 ) ) ;
#123204=CARTESIAN_POINT ( 'NONE',  ( 4.984861949208964305, 1.980195279717174905, 0.6042863919064264122 ) ) ;
#123206=CARTESIAN_POINT ( 'NONE',  ( 5.935146830689759234, -1.586316731616247200, -1.512381816529739353 ) ) ;
#123215=CARTESIAN_POINT ( 'NONE',  ( 5.840704046183605946, -2.018525344099521668, -0.4591754850708437696 ) ) ;
#123216=CARTESIAN_POINT ( 'NONE',  ( 4.688067719671657585, -0.9068681981775075229, 1.699704011162524120 ) ) ;
#123217=CARTESIAN_POINT ( 'NONE',  ( 1.405875298092047698, -1.122519365368032984, -1.674874950958963549 ) ) ;
#123221=CARTESIAN_POINT ( 'NONE',  ( 0.9201892814816803323, 1.302667801055312990, -1.762099327409505811 ) ) ;
#123222=CARTESIAN_POINT ( 'NONE',  ( 5.109893933574640279, -1.816543354971979163, 0.1824992186492402357 ) ) ;
#123229=CARTESIAN_POINT ( 'NONE',  ( 2.261056740009634414, 1.805359621025553363, -0.3608742708730780513 ) ) ;
#123230=CARTESIAN_POINT ( 'NONE',  ( 6.539320575229251808, 0.004279804010676873348, 1.996977849922920267 ) ) ;
#123231=CARTESIAN_POINT ( 'NONE',  ( 1.687308557152231270, -1.277188091954140514, -1.910694296540839332 ) ) ;
#123232=CARTESIAN_POINT ( 'NONE',  ( 6.702011072381410806, 0.7537920952922130269, -1.811353739714548272 ) ) ;
#123236=CARTESIAN_POINT ( 'NONE',  ( 0.4146172280090759665, 0.7909515328246279342, 1.913518691844050323 ) ) ;
#123238=CARTESIAN_POINT ( 'NONE',  ( 3.105106965723201551, -0.4054212715494521224, 2.050880055191468543 ) ) ;
#123239=CARTESIAN_POINT ( 'NONE',  ( 0.6724591444495706671, -1.759989063064151038, -0.6342292696241008665 ) ) ;
#123240=CARTESIAN_POINT ( 'NONE',  ( 1.704453651327157537, -1.458331393932917885, -1.392334588655015803 ) ) ;
#123244=CARTESIAN_POINT ( 'NONE',  ( 2.120290817172516551, 0.0009401564262049438847, 1.740626721131139698 ) ) ;
#123248=CARTESIAN_POINT ( 'NONE',  ( 2.912419603134624779, 1.249142870932816507, -1.189721958963300130 ) ) ;
#123249=CARTESIAN_POINT ( 'NONE',  ( 2.419692422129790632, -1.264489869534379141, -1.789777738334753732 ) ) ;
#123250=CARTESIAN_POINT ( 'NONE',  ( 5.619807753665406302, -2.153844256707802440, 0.4802137346974973409 ) ) ;
#123252=CARTESIAN_POINT ( 'NONE',  ( 2.606498238493897279, 2.170487999849361138, 0.05724136673956359972 ) ) ;
#123253=CARTESIAN_POINT ( 'NONE',  ( 1.365546509989667534, 1.798985258052044900, -0.3101867277976525505 ) ) ;
#123255=CARTESIAN_POINT ( 'NONE',  ( 4.434827806327999333, -1.698493238601869182, 1.263996378755541938 ) ) ;
#123258=CARTESIAN_POINT ( 'NONE',  ( 4.318134875187846333, 1.410584032999320225, -1.806939822960533348 ) ) ;
#123263=CARTESIAN_POINT ( 'NONE',  ( 6.604121268705382519, -0.9518609934017449037, 2.004712419625443776 ) ) ;
#123272=CARTESIAN_POINT ( 'NONE',  ( 4.781875055470904634, 1.674888562130649960, -1.122497055794105192 ) ) ;
#123274=CARTESIAN_POINT ( 'NONE',  ( 2.887610015510627459, -1.926180996541780877, 0.7380674418178012619 ) ) ;
#123276=CARTESIAN_POINT ( 'NONE',  ( -0.1409997244345879974, 6.947781918643359589, -2.595319453918026653 ) ) ;
#123280=CARTESIAN_POINT ( 'NONE',  ( 5.789076383285488347, 1.657349226701849476, 1.433863557930945332 ) ) ;
#123281=CARTESIAN_POINT ( 'NONE',  ( 3.129529892704606464, 0.4926417352555876872, 1.955172657653013957 ) ) ;
#123282=CARTESIAN_POINT ( 'NONE',  ( 2.770863647982471534, 1.747605724785822767, -0.5798694457997202178 ) ) ;
#123284=CARTESIAN_POINT ( 'NONE',  ( 6.528339890195161921, 1.048227956652090231, -1.494441373796271622 ) ) ;
#123286=CARTESIAN_POINT ( 'NONE',  ( 6.350461102289020054, 0.7023508724467423248, 2.150821023316491498 ) ) ;
#123287=CARTESIAN_POINT ( 'NONE',  ( 2.156984414944181694, -1.627247350590403707, 1.336999143475733121 ) ) ;
#123295=CARTESIAN_POINT ( 'NONE',  ( 2.285534418239891785, 0.09939759515392716793, -2.118372479656557061 ) ) ;
#123296=CARTESIAN_POINT ( 'NONE',  ( 4.500347021246276391, -1.045864285740649935, 1.959767921951799829 ) ) ;
#123297=CARTESIAN_POINT ( 'NONE',  ( 2.062683196291382082, -2.004346222996217897, -0.8864330828558324438 ) ) ;
#123298=CARTESIAN_POINT ( 'NONE',  ( 0.7685542157043163680, 1.090964843879228097, 1.918292034055509632 ) ) ;
#123300=CARTESIAN_POINT ( 'NONE',  ( 4.809014631063706524, -1.576880339463518022, 1.167019128429528374 ) ) ;
#123306=CARTESIAN_POINT ( 'NONE',  ( 3.463236921083117981, -1.731491641549892435, 1.224000437801611163 ) ) ;
#123308=CARTESIAN_POINT ( 'NONE',  ( 5.313408243115379292, -0.3210861823062813314, 2.137610926513198617 ) ) ;
#123309=CARTESIAN_POINT ( 'NONE',  ( 4.511176471348508521, -1.804767551675333204, 0.3638508048048467169 ) ) ;
#123312=CARTESIAN_POINT ( 'NONE',  ( 0.2041417395101949583, 1.512754574849054956, 0.8604388899705726068 ) ) ;
#123313=CARTESIAN_POINT ( 'NONE',  ( 6.827182134110178602, 3.710826266403470797, 2.225597045202745594 ) ) ;
#123317=CARTESIAN_POINT ( 'NONE',  ( 4.153314892778156242, -1.795761387672462961, -1.203114871582221079 ) ) ;
#123319=CARTESIAN_POINT ( 'NONE',  ( 6.063827332385394620, 1.649827434358666967, -1.158513616066357832 ) ) ;
#123321=CARTESIAN_POINT ( 'NONE',  ( 3.942369626403975147, 2.151062187213080623, 0.2142938780915065733 ) ) ;
#123322=CARTESIAN_POINT ( 'NONE',  ( 4.270748893545842861, -1.838291250766799223, -0.7124064801689540261 ) ) ;
#123323=CARTESIAN_POINT ( 'NONE',  ( 0.2752733618501881363, 2.042644424557562122, -0.7945232813236638991 ) ) ;
#123324=CARTESIAN_POINT ( 'NONE',  ( 0.6226543773679366067, -1.237902357568532841, -1.947274881911696953 ) ) ;
#123325=CARTESIAN_POINT ( 'NONE',  ( 3.989569841107299286, 1.489977244407629131, 1.423887585670815747 ) ) ;
#123326=CARTESIAN_POINT ( 'NONE',  ( 5.442900063589676485, -1.533566843616997133, -1.191469007954217618 ) ) ;
#123333=CARTESIAN_POINT ( 'NONE',  ( 1.835297179245497068, 0.2165863673247066801, 2.196102686035047213 ) ) ;
#123336=CARTESIAN_POINT ( 'NONE',  ( 6.983263157960366563, -0.003091553303710344557, 1.945923119799706669 ) ) ;
#123337=CARTESIAN_POINT ( 'NONE',  ( -0.1290005225502433017, 0.6921039065478848951, -2.255494067288220439 ) ) ;
#123344=CARTESIAN_POINT ( 'NONE',  ( 2.711851390082948399, -2.038666671984638690, 0.3009093235433103475 ) ) ;
#123349=CARTESIAN_POINT ( 'NONE',  ( 0.6376604129620618844, -1.456937097490097255, -1.457867103223365213 ) ) ;
#123351=CARTESIAN_POINT ( 'NONE',  ( 5.003375819710620398, -1.831856422778654681, 0.1858995714831001289 ) ) ;
#123355=CARTESIAN_POINT ( 'NONE',  ( -0.2409995289980003397, 4.087843961663322645, -2.555282842491034323 ) ) ;
#123357=CARTESIAN_POINT ( 'NONE',  ( 4.600333186373093852, -2.206333364838486411, -0.05604163552313382035 ) ) ;
#123358=CARTESIAN_POINT ( 'NONE',  ( 0.7202740732663616141, -1.155732025818452913, -1.826486478054230256 ) ) ;
#123360=CARTESIAN_POINT ( 'NONE',  ( 6.411931881972196610E-05, -0.8997486769052507327, 1.687471195204979457 ) ) ;
#123361=CARTESIAN_POINT ( 'NONE',  ( 0.5148617154710420918, 0.1531739628206352510, 2.010800830040265996 ) ) ;
#123366=CARTESIAN_POINT ( 'NONE',  ( 0.3384655940862451029, 0.3152513238553408814, 1.843739016257638141 ) ) ;
#123367=CARTESIAN_POINT ( 'NONE',  ( 2.571500236035813902, 1.429449181443824823, 1.422607194786096541 ) ) ;
#123371=CARTESIAN_POINT ( 'NONE',  ( 4.213572796808015219, -0.3603392467595716298, 2.074844637031019623 ) ) ;
#123376=CARTESIAN_POINT ( 'NONE',  ( 4.131121313247118287, 1.848376352210901574, 0.8146727144991843250 ) ) ;
#123380=CARTESIAN_POINT ( 'NONE',  ( 4.446650332099550518, 0.5718123500428309303, 2.084546224624775679 ) ) ;
#123386=CARTESIAN_POINT ( 'NONE',  ( 1.820994678651502330, -1.536134449795123480, 1.534618252339227329 ) ) ;
#123389=CARTESIAN_POINT ( 'NONE',  ( 2.067674361007607597, -1.131582805410412673, 1.452419944642673100 ) ) ;
#123392=CARTESIAN_POINT ( 'NONE',  ( 3.737968522918270864, 2.181131050170285857, 0.2133239450496857148 ) ) ;
#123393=CARTESIAN_POINT ( 'NONE',  ( 6.883263157960366918, 2.950764357809147143, 2.606098932787728639 ) ) ;
#123394=CARTESIAN_POINT ( 'NONE',  ( 4.170984489290855635, -2.109804223432755865, -0.8175660662063081174 ) ) ;
#123400=CARTESIAN_POINT ( 'NONE',  ( 5.008955365368598756, 1.539791945809299012, 0.8722439129504773181 ) ) ;
#123402=CARTESIAN_POINT ( 'NONE',  ( 0.6398468662271715734, -1.489381099377089512, -1.489160694218383485 ) ) ;
#123405=CARTESIAN_POINT ( 'NONE',  ( 0.6429344911094649895, -0.2373986304471594755, -1.955105650238073478 ) ) ;
#123408=CARTESIAN_POINT ( 'NONE',  ( 5.519718948577209794, -0.4320008574366646648, 1.759211659423996155 ) ) ;
#123413=CARTESIAN_POINT ( 'NONE',  ( 4.557402362779487959, 0.4096945884842878027, -1.825068887194372991 ) ) ;
#123415=CARTESIAN_POINT ( 'NONE',  ( 4.487213805514509879, 0.09639557921744396074, 2.068113308821089902 ) ) ;
#123427=CARTESIAN_POINT ( 'NONE',  ( 3.631260574587381829, 0.05062604155347744800, -1.961386756325018021 ) ) ;
#123428=CARTESIAN_POINT ( 'NONE',  ( 1.598982282203027516, 0.9961506480390787122, -1.752761228829377904 ) ) ;
#123429=CARTESIAN_POINT ( 'NONE',  ( -0.1108833634137010027, 1.377173795795206157, -2.152720132533675113 ) ) ;
#123432=CARTESIAN_POINT ( 'NONE',  ( 1.739302498465819191, -1.351291084634953066, -1.293660915597586003 ) ) ;
#123434=CARTESIAN_POINT ( 'NONE',  ( 4.465094144989894431, -1.614439531090381408, 1.202519638469838226 ) ) ;
#123437=CARTESIAN_POINT ( 'NONE',  ( 2.864987086846816577, -0.1587241086147250513, -2.111353475082369702 ) ) ;
#123439=CARTESIAN_POINT ( 'NONE',  ( 4.932118098221458524, 1.189261692661430114, 1.694535115018414917 ) ) ;
#123441=CARTESIAN_POINT ( 'NONE',  ( 6.720655732516684466, -0.001531948155393536137, 2.073773125298985054 ) ) ;
#123442=CARTESIAN_POINT ( 'NONE',  ( 6.720655732516665815, 6.034026441762381232, 2.768628153821062199 ) ) ;
#123443=CARTESIAN_POINT ( 'NONE',  ( 6.018537349360657984, 1.224031959697377658, -1.354583942311540667 ) ) ;
#123451=CARTESIAN_POINT ( 'NONE',  ( -0.02317427319796245069, -1.617030479356797334, -0.8165419217573687272 ) ) ;
#123461=CARTESIAN_POINT ( 'NONE',  ( 5.097279880301520905, -0.2930512725940071506, 1.994873791649566463 ) ) ;
#123463=SURFACE_STYLE_USAGE ( .BOTH. , #141790 ) ;
#123467=CARTESIAN_POINT ( 'NONE',  ( 2.887507918447276722, -1.839357967585793840, 0.7044240162308276210 ) ) ;
#123468=CARTESIAN_POINT ( 'NONE',  ( 4.165638788432171502, 1.319243065725501873, 1.525032742243138451 ) ) ;
#123470=CARTESIAN_POINT ( 'NONE',  ( 6.727182134110194944, 2.413774403037728167, 2.569658639860139093 ) ) ;
#123472=CARTESIAN_POINT ( 'NONE',  ( 4.365290731249091394, 2.125951747006165959, -0.5312598475561494116 ) ) ;
#123474=CARTESIAN_POINT ( 'NONE',  ( 3.223571483072392940, -1.856993652095505487, 0.5122080487700955143 ) ) ;
#123477=CARTESIAN_POINT ( 'NONE',  ( 0.1755611466353626804, -0.002217706044341590139, -2.244164702216360663 ) ) ;
#123483=CARTESIAN_POINT ( 'NONE',  ( 6.251489360189885325, 1.835807759842246423, -0.1425652098738516838 ) ) ;
#123484=CARTESIAN_POINT ( 'NONE',  ( 2.701816853162309684, 1.425160482578791354, 1.422027561765064174 ) ) ;
#123485=CARTESIAN_POINT ( 'NONE',  ( 5.308124166105086417, -1.975000179191854111, 1.175378216249231222 ) ) ;
#123487=CARTESIAN_POINT ( 'NONE',  ( 3.731172809088632025, 0.04972793443442201367, -1.860468898575567520 ) ) ;
#123492=CARTESIAN_POINT ( 'NONE',  ( 6.286679179808664308, 1.818834136932646839, -1.030939041669608924 ) ) ;
#123498=CARTESIAN_POINT ( 'NONE',  ( 5.900961842893762466, 1.406060569669766114, -0.9988219321918601068 ) ) ;
#123500=CARTESIAN_POINT ( 'NONE',  ( 0.9142546942676577082, -1.099255453910731983, -1.341178637715144673 ) ) ;
#123504=CARTESIAN_POINT ( 'NONE',  ( 5.454042025912737124, -0.7881617977381920603, 2.023119649181570168 ) ) ;
#123505=CARTESIAN_POINT ( 'NONE',  ( 5.285714101943871590, 1.228958891529348785, 1.350286652578087665 ) ) ;
#123506=CARTESIAN_POINT ( 'NONE',  ( 2.535929169054650156, 1.202975682259961765, 1.549578550289295586 ) ) ;
#123511=CARTESIAN_POINT ( 'NONE',  ( 3.879626234357834047, 0.2581020070546445888, -2.104639248629774251 ) ) ;
#123514=CARTESIAN_POINT ( 'NONE',  ( 2.166927730644189420, 1.536898783757352005, -1.387270004372019416 ) ) ;
#123517=CARTESIAN_POINT ( 'NONE',  ( 3.985193088136604889, -2.072824570928345711, -0.7989420372410382942 ) ) ;
#123519=CARTESIAN_POINT ( 'NONE',  ( 1.618275512070939115, 0.2312369868452644750, 2.287056861988717493 ) ) ;
#123521=CARTESIAN_POINT ( 'NONE',  ( 0.2682999959267086676, -0.8333247372044670920, -1.774235371720728649 ) ) ;
#123525=CARTESIAN_POINT ( 'NONE',  ( 6.392148736875968851, -0.4980823202534767624, -1.772533436741857260 ) ) ;
#123527=CARTESIAN_POINT ( 'NONE',  ( -0.2106725631049838343, 0.7236243445625335502, -2.087119268998542942 ) ) ;
#123528=CARTESIAN_POINT ( 'NONE',  ( 2.854212618329458717, 0.5792176767629078071, 1.624745991979989812 ) ) ;
#123529=CARTESIAN_POINT ( 'NONE',  ( 1.798064920797682653, -0.9548589541341389042, -1.776165177175797583 ) ) ;
#123531=CARTESIAN_POINT ( 'NONE',  ( 3.093345431676647994, 1.942085262481594965, -1.160266548027958367 ) ) ;
#123532=CARTESIAN_POINT ( 'NONE',  ( 4.811209553025526553, 1.832079168721172380, 1.038602630702612384 ) ) ;
#123534=CARTESIAN_POINT ( 'NONE',  ( 3.514700139928600198, 1.598748483301600354, 0.7592613872578843903 ) ) ;
#123536=CARTESIAN_POINT ( 'NONE',  ( 5.970342212645192603, -2.175549559325986149, -0.7227481681704952532 ) ) ;
#123537=CARTESIAN_POINT ( 'NONE',  ( 5.349485151062911115, 1.838858031828109363, -0.09410559872920226665 ) ) ;
#123540=CARTESIAN_POINT ( 'NONE',  ( 6.017560223340764125, -1.214513600917455083, -1.823921334435735231 ) ) ;
#123543=CARTESIAN_POINT ( 'NONE',  ( 6.285608408418759119, -1.950803066209889636, 0.6937918898708083093 ) ) ;
#123544=CARTESIAN_POINT ( 'NONE',  ( -0.04763828917917976857, -1.313539345393003321, 1.530161206715647149 ) ) ;
#123546=CARTESIAN_POINT ( 'NONE',  ( 4.020081831311307141, -0.9914672019816127557, -1.651657144357060014 ) ) ;
#123549=CARTESIAN_POINT ( 'NONE',  ( 6.363548717301088509, -1.704009271243651868, -1.262090224194649446 ) ) ;
#123559=CARTESIAN_POINT ( 'NONE',  ( 1.310910670669521272, -1.548711629584406113, 1.204245502051364936 ) ) ;
#123563=CARTESIAN_POINT ( 'NONE',  ( 0.4497679408741364071, 1.527348849510310247, 1.386460675282843447 ) ) ;
#123566=CARTESIAN_POINT ( 'NONE',  ( 0.5676901151186209971, 0.2185747425910676001, -2.251950761720759253 ) ) ;
#123571=CARTESIAN_POINT ( 'NONE',  ( 1.774454573425466863, -1.774572579973210384, -0.5916213571805841731 ) ) ;
#123572=CARTESIAN_POINT ( 'NONE',  ( 0.2461560209003906818, 1.715711078377361032, -0.2512605247984560086 ) ) ;
#123574=CARTESIAN_POINT ( 'NONE',  ( 4.142245973918059043, 0.5854081421233224836, 2.111838497463234710 ) ) ;
#123575=CARTESIAN_POINT ( 'NONE',  ( 4.331326240856082421, 0.1090238329626690705, 2.305124713103424483 ) ) ;
#123576=CARTESIAN_POINT ( 'NONE',  ( 6.591097270071800907, 1.795350502275098403, -1.011519373207786288 ) ) ;
#123577=CARTESIAN_POINT ( 'NONE',  ( 2.396341059777199689, 1.559625748545325319, -1.156842939599848741 ) ) ;
#123580=CARTESIAN_POINT ( 'NONE',  ( 4.851869265964163347, -1.501451181749386743, -1.497782127133556518 ) ) ;
#123581=CARTESIAN_POINT ( 'NONE',  ( 3.990861413484114273, -2.010826503599131065, 0.1511389102963680842 ) ) ;
#123585=CARTESIAN_POINT ( 'NONE',  ( 0.4514209555319322331, 0.5758240286459560542, -1.732582669633643047 ) ) ;
#123590=CARTESIAN_POINT ( 'NONE',  ( 5.524313221898556669, 1.229557446212639071, -1.653754484787550494 ) ) ;
#123595=CARTESIAN_POINT ( 'NONE',  ( 4.090493647085408746, -1.161108546167070488, 1.652349136562575760 ) ) ;
#123596=CARTESIAN_POINT ( 'NONE',  ( 5.672587799981195111, 0.8983335965149964464, 2.031727793752806210 ) ) ;
#123601=CARTESIAN_POINT ( 'NONE',  ( 4.662995224183227982, -1.840047010505897029, -0.9283316357228312832 ) ) ;
#123602=CARTESIAN_POINT ( 'NONE',  ( 3.850232551101364642, 0.2440307281281335339, -2.001511205109906655 ) ) ;
#123610=CARTESIAN_POINT ( 'NONE',  ( 3.901720107437017582, 0.2930258228103881923, 1.994564303527603499 ) ) ;
#123611=CARTESIAN_POINT ( 'NONE',  ( 2.747807751077631977, 0.6205313035267927546, 1.733543155639664990 ) ) ;
#123613=CARTESIAN_POINT ( 'NONE',  ( 1.559632053384899741, -1.981161107035840141, -1.183202272445786907 ) ) ;
#123615=CARTESIAN_POINT ( 'NONE',  ( 4.024825912876791811, 2.051136489140188424, 0.6822911077620784637 ) ) ;
#123619=CARTESIAN_POINT ( 'NONE',  ( 3.743815364168050053, -2.214071480395309433, -0.6165714402358390966 ) ) ;
#123621=CARTESIAN_POINT ( 'NONE',  ( 2.852262661058731386, 0.6285613048715790185, 1.762029509812724992 ) ) ;
#123622=CARTESIAN_POINT ( 'NONE',  ( 6.262572880032761802, -1.394454384559177695, 1.393866484745357459 ) ) ;
#123626=CARTESIAN_POINT ( 'NONE',  ( 0.1357705729100426029, -2.015811560716780360, 0.8986578214904348272 ) ) ;
#123632=CARTESIAN_POINT ( 'NONE',  ( 6.315303677655929704, -0.2418685481465185916, 1.956520841371222952 ) ) ;
#123633=CARTESIAN_POINT ( 'NONE',  ( 5.778008146871475681, 1.369946362297723264, 1.856932335381543897 ) ) ;
#123634=CARTESIAN_POINT ( 'NONE',  ( 6.584420904419787668, 1.070383488754884649, -1.522209605261907406 ) ) ;
#123635=CARTESIAN_POINT ( 'NONE',  ( 3.063389470891558997, 1.739959455442946279, 1.107334787568447165 ) ) ;
#123642=CARTESIAN_POINT ( 'NONE',  ( 5.652828992512394457, -0.5219723807755486389, -2.107401415877676598 ) ) ;
#123644=CARTESIAN_POINT ( 'NONE',  ( 5.425302022954732628, -1.172690680311109901, -1.419496581506813904 ) ) ;
#123647=CARTESIAN_POINT ( 'NONE',  ( 6.620655732516647518, 0.007553340620044743381, 1.826407896915738238 ) ) ;
#123648=CARTESIAN_POINT ( 'NONE',  ( 6.497619750234602698, -2.191128968173004843, 0.05151875470104508997 ) ) ;
#123649=CARTESIAN_POINT ( 'NONE',  ( 0.7373108528737730705, -1.318359053027039263, -1.327247110734230962 ) ) ;
#123650=CARTESIAN_POINT ( 'NONE',  ( 0.6325467830279264403, 1.161941506187497364, -1.941124190868536603 ) ) ;
#123655=CARTESIAN_POINT ( 'NONE',  ( 0.2934254677693093338, 1.784247535656303230, -0.6883866973072181317 ) ) ;
#123656=CARTESIAN_POINT ( 'NONE',  ( 1.621574733132331358, -0.9795727578338263575, -1.473812506242745179 ) ) ;
#123657=CARTESIAN_POINT ( 'NONE',  ( 5.971345465650553130, -1.727703365644253086, -1.033000238237492763 ) ) ;
#123659=CARTESIAN_POINT ( 'NONE',  ( 3.427252967507479209, -1.452606091845513037, -1.248918174067833009 ) ) ;
#123661=CARTESIAN_POINT ( 'NONE',  ( 4.721133488271325618, -1.758435714881977141, -0.8873337903104687729 ) ) ;
#123662=CARTESIAN_POINT ( 'NONE',  ( 6.222917004181202749, 1.493787235515126044, -1.359621011941100743 ) ) ;
#123664=CARTESIAN_POINT ( 'NONE',  ( 2.781945002432617997, -0.9632652739061451364, 1.603442845774772474 ) ) ;
#123665=CARTESIAN_POINT ( 'NONE',  ( 4.775862138867135620, 0.9967549737653296216, 1.407514542897546850 ) ) ;
#123667=CARTESIAN_POINT ( 'NONE',  ( 2.807470779205251343, 1.864772411128329477, 1.179945617918669143 ) ) ;
#123670=CARTESIAN_POINT ( 'NONE',  ( 6.795372052238223048, -1.752927774724974297, 0.8811163259476795240 ) ) ;
#123673=CARTESIAN_POINT ( 'NONE',  ( -0.2104748580754413345, 7.629137130509052511, -2.703678718140525739 ) ) ;
#123677=CARTESIAN_POINT ( 'NONE',  ( 2.400909748719297188, 0.4512941399696759337, 2.020426262116347349 ) ) ;
#123681=CARTESIAN_POINT ( 'NONE',  ( 0.2233145766990596859, 1.758413993963375610, 0.9933387185240820649 ) ) ;
#123683=B_SPLINE_CURVE_WITH_KNOTS ( 'NONE', 3,
 ( #210302, #62996, #66157, #192987, #161589, #15297, #82436, #129166, #195143, #31582, #162649, #213488, #61942, #44641, #46778, #110756, #97656, #164767, #163715, #130216, #181010, #32631, #128100, #194058, #45711, #47851, #197254, #112892, #111830, #29448, #48893, #178904, #95539, #113962, #13176, #79254, #30518, #96599, #14222, #98708, #84578, #101899, #167963, #118212, #1168, #17419, #83502, #116070, #117141, #200439, #33692, #152782, #67233, #35822, #100821, #151729, #20624, #133367, #52085, #102968, #183144, #185261, #70432, #184199, #150665, #19569, #2227, #86712, #149584, #199373, #3301, #68303, #134436, #182060, #34748, #4363, #166906, #51019, #135478, #202568, #18499, #169026, #85644, #132302, #36885, #69370, #136549, #201500, #53146, #165834, #119277, #49950, #198309, #99768, #33308, #115688, #178510, #14907, #130886, #65777, #149200, #113575, #196880, #47460, #81001, #62606, #48517, #181681, #114639, #112500, #177444, #83120, #179577, #32253, #95142, #98323, #29059, #775, #66841, #99393, #165446, #161192, #17041, #15972, #180631, #12780, #31199, #164388, #97273, #147089, #128768, #82058, #132985, #148150, #30122, #78853, #198986, #163327, #214151, #144974, #129839, #131927, #213112, #197937, #64744, #49563, #210979, #111440, #46382, #194744, #96211, #195820, #162262, #13849, #79925, #146032, #212041, #63683, #201126, #103669, #20253, #22377, #3988, #102592, #35439, #72196, #153478, #200067, #70057, #86337, #1853, #187027, #150286, #116757, #18110, #136168, #5050, #2919, #183830, #34374, #21306, #50631, #117838, #154547, #100447, #182756, #84196, #138305, #203264, #166520, #152408, #202186, #119975, #53844, #101516, #67913, #134059, #51718, #19188, #185955, #167587, #170786, #85263, #54910, #121061, #151350, #88488, #118899, #184883, #36508, #135110, #38661, #6128, #37587, #168649, #169717, #87414, #104739, #68992, #52764, #71126, #137242, #28441, #11104, #30590, #209293, #208238, #13253, #212507, #43649, #129241, #109765, #96674, #126021, #193061, #110821, #59870, #12180, #144376, #60941, #112964, #78252, #210375, #127097, #146487, #44714, #211441, #62015, #76122, #195214, #108691, #178976, #29516, #128171, #26292, #176828, #194133, #94533, #160572, #142225, #45783, #124960, #111900, #177903, #174719, #14296, #80391, #95609, #92407, #162725, #161658, #79324, #145441, #63073, #46850, #158446, #190922, #191983, #42586, #10046, #143302, #175773, #93467, #27366, #159506, #77180, #165, #117215, #33764, #166981, #180032, #64148, #16431, #101970, #51091, #35893, #183214, #165907, #200511, #84650, #66232, #130290, #31654, #17491, #18572, #82509, #197329, #47926, #34818, #50022, #115088, #1241, #48971, #181084, #164839, #32702, #97730, #65181, #132380, #151799, #98784, #83578, #131335, #81460, #147538, #114038, #148596, #99842, #163788, #168038, #198381, #149660, #116146, #100894, #118283, #182134, #67301, #134507, #133441, #199448, #150739, #2300, #68376, #52156, #184268, #19641, #213559, #15367, #85712, #196279, #169095, #121504, #104110, #123649, #87856, #86785, #106289, #91073, #136617, #7646, #202642, #3374, #156058, #56422, #57488, #70501, #187476, #73731, #186404, #38041, #204769, #20694, #122583, #152854, #4432, #188545, #6575, #54292, #120429, #139827, #22822, #39106, #170159, #189611, #153928, #21747, #172309 ),
 .UNSPECIFIED., .F., .F.,
 ( 4, 1, 1, 1, 1, 1, 1, 1, 1, 1, 1, 1, 1, 1, 1, 1, 1, 1, 1, 1, 1, 1, 1, 1, 1, 1, 1, 1, 1, 1, 1, 1, 1, 1, 1, 1, 1, 1, 1, 1, 1, 1, 1, 1, 1, 1, 1, 1, 1, 1, 1, 1, 1, 1, 1, 1, 1, 1, 1, 1, 1, 1, 1, 1, 1, 1, 1, 1, 1, 1, 1, 1, 1, 1, 1, 1, 1, 1, 1, 1, 1, 1, 1, 1, 1, 1, 1, 1, 1, 1, 1, 1, 1, 1, 1, 1, 1, 1, 1, 1, 1, 1, 1, 1, 1, 1, 1, 1, 1, 1, 1, 1, 1, 1, 1, 1, 1, 1, 1, 1, 1, 1, 1, 1, 1, 1, 1, 1, 1, 1, 1, 1, 1, 1, 1, 1, 1, 1, 1, 1, 1, 1, 1, 1, 1, 1, 1, 1, 1, 1, 1, 1, 1, 1, 1, 1, 1, 1, 1, 1, 1, 1, 1, 1, 1, 1, 1, 1, 1, 1, 1, 1, 1, 1, 1, 1, 1, 1, 1, 1, 1, 1, 1, 1, 1, 1, 1, 1, 1, 1, 1, 1, 1, 1, 1, 1, 1, 1, 1, 1, 1, 1, 1, 1, 1, 1, 1, 1, 1, 1, 1, 1, 1, 1, 1, 1, 1, 1, 1, 1, 1, 1, 1, 1, 1, 1, 1, 1, 1, 1, 1, 1, 1, 1, 1, 1, 1, 1, 1, 1, 1, 1, 1, 1, 1, 1, 1, 1, 1, 1, 1, 1, 1, 1, 1, 1, 1, 1, 1, 1, 1, 1, 1, 1, 1, 1, 1, 1, 1, 1, 1, 1, 1, 1, 1, 1, 1, 1, 1, 1, 1, 1, 1, 1, 1, 1, 1, 1, 1, 1, 1, 1, 1, 1, 1, 1, 1, 1, 1, 1, 1, 1, 1, 1, 1, 1, 1, 1, 1, 1, 1, 1, 1, 1, 1, 1, 1, 1, 1, 1, 1, 1, 1, 1, 1, 1, 1, 1, 1, 1, 1, 1, 1, 1, 1, 1, 1, 1, 1, 1, 1, 1, 1, 1, 1, 1, 1, 1, 1, 1, 1, 1, 1, 1, 1, 1, 1, 1, 1, 1, 1, 1, 1, 1, 1, 1, 1, 1, 1, 1, 1, 1, 1, 1, 1, 1, 1, 1, 1, 1, 1, 1, 1, 1, 4 ),
 ( 0.000000000000000000, 0.002600154539856827565, 0.005208839490340733125, 0.007813275572638063438, 0.01041576435696154809, 0.01302135854728175661, 0.01562456786780599440, 0.01822932761385693060, 0.02083324874646079461, 0.02343713590986815087, 0.02604192363554110393, 0.02864519953128016536, 0.03125045858075606309, 0.03385359029894085409, 0.03645870005206112291, 0.03906221013386886737, 0.04166657361863843057, 0.04427092160485841116, 0.04687444683368256759, 0.04947954930481244379, 0.05208268618576387260, 0.05468794662449812799, 0.05729120536831356497, 0.05989601299138836571, 0.06249988999545372931, 0.06510378435733490954, 0.06770858081828938502, 0.07031184975024351580, 0.07291710771924506118, 0.07552024060328325905, 0.07812534933470290099, 0.08072885870519988516, 0.08333322157114708695, 0.08593756915452624434, 0.08854109358761537429, 0.09114619558392741960, 0.09374933183658358538, 0.09635459170495851156, 0.09895784999447977681, 0.1015626569530685003, 0.1041665336043751944, 0.1067704272253022224, 0.1093752232910748662, 0.1119784915631429623, 0.1145837490571069844, 0.1171868814509031548, 0.1197919896162490533, 0.1223954986480551566, 0.1249998608471283579, 0.1276042081199000311, 0.1302077318846941445, 0.1328128334964322199, 0.1354159692195129883, 0.1380212286176593917, 0.1406244865514671982, 0.1432292929439143159, 0.1458331693420142072, 0.1484370623210626572, 0.1510418580899855479, 0.1536451258019158050, 0.1562503829188521542, 0.1588535149221727560, 0.1614586226195926788, 0.1640621314121666618, 0.1666664930431534797, 0.1692708401040713406, 0.1718743633000545112, 0.1744794646253388370, 0.1770825999186152189, 0.1796878589445308205, 0.1822911166222762891, 0.1848959225469683498, 0.1874997987909985397, 0.1901036912273387502, 0.1927084867977703619, 0.1953117540492253223, 0.1979170108871138589, 0.2005201425997050479, 0.2031252499273119572, 0.2057287585800815777, 0.2083331197417381819, 0.2109374666895270922, 0.2135409894161511279, 0.2161460905530729892, 0.2187492255162853672, 0.2213544842679382729, 0.2239577417892439637, 0.2265625473445374016, 0.2291664235336075273, 0.2317703155263790282, 0.2343751109966507595, 0.2369783778872631419, 0.2395836345440564008, 0.2421867660656364940, 0.2447918731215153465, 0.2473953817338825356, 0.2499997425249363969, 0.2526040894582959329, 0.2552076118149841921, 0.2578127128616094499, 0.2604158475944712281, 0.2630211061698037311, 0.2656243636342671688, 0.2682291689184919115, 0.2708330451516883230, 0.2734369368000036937, 0.2760417322684234342, 0.2786449988978000336, 0.2812502554714267355, 0.2838533869016899303, 0.2864584937839013135, 0.2890620024552456591, 0.2916663629743991848, 0.2942707099920074398, 0.2968742320781582733, 0.2994793331325310004, 0.3020824677347322962, 0.3046877262316646240, 0.3072909837388622112, 0.3098957888503254821, 0.3124996652267145181, 0.3151035566296633839, 0.3177083521945192612, 0.3203116186622446127, 0.3229168752506134110, 0.3255200066892336430, 0.3281251134958176330, 0.3307286223255002655, 0.3333329826714347410, 0.3359373298719517953, 0.3385408517869427647, 0.3411459529470890484, 0.3437490875183005223, 0.3463543460347343617, 0.3489576036842249041, 0.3515624087212146920, 0.3541662853398466204, 0.3567701765964986227, 0.3593749723560626386, 0.3619782387617029862, 0.3645834954627060198, 0.3671866270093405715, 0.3697917338383204244, 0.3723952429256875973, 0.3749996031970665444, 0.3776039506791386557, 0.3802074725223298923, 0.3828125738862612759, 0.3854157085261381011, 0.3880209671599602617, 0.3906242250512887426, 0.3932290301120778819, 0.3958329070719905363, 0.3984367982813996067, 0.4010415943339316058, 0.4036448607770379837, 0.4062501176885546794, 0.4088532494428480657, 0.4114583563922335485, 0.4140618658366201910, 0.4166662261320933647, 0.4192705739943561327, 0.4218740958650940009, 0.4244791975308115917, 0.4270823323389966175, 0.4296875911880828069, 0.4322908494207843844, 0.4348956546036337745, 0.4374995320038561619, 0.4401034232650644085, 0.4427082197088152427, 0.4453114862889279713, 0.4479167435088288185, 0.4505198755704162283, 0.4531249827382076711, 0.4557284926389418844, 0.4583328530571487147, 0.4609372013982309668, 0.4635407233958523388, 0.4661458254613498609, 0.4687489605374778323, 0.4713542196996960976, 0.4739574783732994345, 0.4765622837764619812, 0.4791661617160185016, 0.4817700531280592058, 0.4843748500612748420, 0.4869781168779269698, 0.4895833745040767959, 0.4921865069725880892, 0.4947916144567798824, 0.4973951249131855490, 0.4999994855527590265, 0.5026038344712867589, 0.5052073566951218453, 0.5078124592583899144, 0.5104155947020908579, 0.5130208542753056378, 0.5156241134893367883, 0.5182289192110610676, 0.5208327977889742888, 0.5234366894508762913, 0.5260414869718011976, 0.5286447541245218318, 0.5312500122547839654, 0.5338531452298473923, 0.5364582531284315392, 0.5390617642398328746, 0.5416661251994032700, 0.5442704747940029231, 0.5468739973433798252, 0.5494791005024090014, 0.5520822364133124438, 0.5546874964953879550, 0.5572907563493740835, 0.5598955624879079496, 0.5624994418032033261, 0.5651033338139942463, 0.5677081320208752224, 0.5703113996091939697, 0.5729166583414331271, 0.5755197919226788805, 0.5781249003336490500, 0.5807284121993739889, 0.5833327735775721834, 0.5859371239468746939, 0.5885406469211225122, 0.5911457507739076300, 0.5937488872516457628, 0.5963541479404496082, 0.5989574085339228748, 0.6015622151875171797, 0.6041660953392257172, 0.6067699877979360057, 0.6093747867890261238, 0.6119780549124759217, 0.6145833143445629254, 0.6171864486316270826, 0.6197915576529816617, 0.6223950703723655220, 0.6249994322678273928, 0.6276037835104713025, 0.6302073070089242446, 0.6328124116534677990, 0.6354155487976793637, 0.6380208101910863627, 0.6406240716235875876, 0.6432288788904997334, 0.6458327599776627626, 0.6484366529833293091, 0.6510414528568908565, 0.6536447216150126360, 0.6562499818448275235, 0.6588531169373553764, 0.6614582266671018562, 0.6640617403394915019, 0.6666661028508605868, 0.6692704550654967610, 0.6718739791874978051, 0.6744790847218130603, 0.6770822226321474568, 0.6796874848280434200, 0.6822907471991253026, 0.6848955551776233497, 0.6874994372992955238, 0.6901033309509650993, 0.6927081318052739078, 0.6953114012976200353, 0.6979166624230551674, 0.7005197984207056638, 0.7031249089568636368, 0.7057284236816204759, 0.7083327869075525252, 0.7109371401928469281, 0.7135406650377511539, 0.7161457715598668061, 0.7187489103359874232, 0.7213541734322722609, 0.7239574368415039318, 0.7265622456298695964, 0.7291661288851226663, 0.7317700232818561412, 0.7343748252152053624, 0.7369780955413426371, 0.7395833576603073611, 0.7421864946627563242, 0.7447916061033615920, 0.7473951219798656842, 0.7499994860190324353, 0.7526038404736700160, 0.7552073661408488237, 0.7578124737488122209, 0.7604156134903999886, 0.7630208775849919300, 0.7656241421319622820, 0.7682289518284949326, 0.7708328363164217434, 0.7734367315572975299, 0.7760415346680002990, 0.7786448059275148381, 0.7812500691379388185, 0.7838532072448821664, 0.7864583196879902927, 0.7890618368156444573, 0.7916662017667361884, 0.7942705574894247667, 0.7968740840782696511, 0.7994791928701499018, 0.8020823336769073997, 0.8046875988677468783, 0.8072908646520678966, 0.8098956753550886623, 0.8124995611748068169, 0.8151034573589240884, 0.8177082617453185209, 0.8203115340378186460, 0.8229167984376549727, 0.8255199377488137147, 0.8281250512925039109, 0.8307285697707365024, 0.8333329357324672504, 0.8359372928219411802, 0.8385408204318668401, 0.8411459305057594760, 0.8437490724774151518, 0.8463543388624672481, 0.8489576059837783406, 0.8515624177916331083, 0.8541663050422881875, 0.8567702022687715413, 0.8593750080292236193, 0.8619782814543437421, 0.8645835471415733720, 0.8671866877566964948, 0.8697918024990743957, 0.8723953224273439666, 0.8749996894984543028, 0.8776040480534781363, 0.8802075767839265819, 0.8828126882379567775, 0.8854158314742670566, 0.8880210991515266050, 0.8906243677094983768, 0.8932291807205616774, 0.8958330695013316802, 0.8984369678693342465, 0.9010417751022415933, 0.9036450497596462128, 0.9062503168322812996, 0.9088534588511494317, 0.9114585748903522022, 0.9140620963681507227, 0.9166664646474114164, 0.9192708247667824573, 0.9218743547172278952, 0.9244794676495572405, 0.9270826122503010858, 0.9296878813177945622, 0.9322911514121841048, 0.9348959657248061550, 0.9374998561347748227, 0.9401037557438677306, 0.9427085645475906661, 0.9453118405358371668, 0.9479171090940153865, 0.9505202526155902554, 0.9531253700418979014, 0.9557288931959170286, 0.9583332627756006028, 0.9609376244112938226, 0.9635411559431285022, 0.9661462708106475228, 0.9687494151757961580, 0.9713546862302190332, 0.9739579640138142924, 0.9765627705390533819, 0.9791666547386930208, 0.9817705986233274951, 0.9843753609709087193, 0.9869785915570626900, 0.9895841932699848131, 0.9921866851465583892, 0.9947911401134668097, 0.9973998225951543617, 1.000000000000000000 ),
 .UNSPECIFIED. ) ;
#123685=CARTESIAN_POINT ( 'NONE',  ( 6.777797683793751915, -1.903277019102869616, 0.4755351429900215310 ) ) ;
#123687=CARTESIAN_POINT ( 'NONE',  ( 5.184922634274871989, -1.076153828860962225, -1.704676470440001701 ) ) ;
#123688=CARTESIAN_POINT ( 'NONE',  ( 4.979654327277899917, -0.6834858053395581612, 1.789849564252174119 ) ) ;
#123689=CARTESIAN_POINT ( 'NONE',  ( 6.539320575229274901, 4.692178491785949923, 2.665866134390063813 ) ) ;
#123690=CARTESIAN_POINT ( 'NONE',  ( 2.208753784402537335, 1.959192758111829136, 0.9821998110004713789 ) ) ;
#123693=CARTESIAN_POINT ( 'NONE',  ( 2.355592738034977263, -1.419685808644566949, -1.281520755053264349 ) ) ;
#123696=CARTESIAN_POINT ( 'NONE',  ( 0.3160300859305562593, 1.034144755472726995, -1.730879882831819705 ) ) ;
#123698=CARTESIAN_POINT ( 'NONE',  ( 5.935146830689759234, -1.586316731616247200, -1.512381816529739353 ) ) ;
#123700=CARTESIAN_POINT ( 'NONE',  ( 2.994803049195310596, 1.480226043003279424, -0.8850232739186939535 ) ) ;
#123702=CARTESIAN_POINT ( 'NONE',  ( 6.310795917644286490, -0.5669512758468171487, -2.043305014803979525 ) ) ;
#123705=CARTESIAN_POINT ( 'NONE',  ( 0.6605093422152423788, -0.6574743052488278838, -1.848563176889833626 ) ) ;
#123708=CARTESIAN_POINT ( 'NONE',  ( 0.1399997263885795207, 2.876830203203218694, -2.488333633689450597 ) ) ;
#123711=CARTESIAN_POINT ( 'NONE',  ( 2.807043740381453656, 1.552634882062135624, -0.9328946631028020020 ) ) ;
#123716=CARTESIAN_POINT ( 'NONE',  ( 3.404753564208697014, -0.3562933990706117493, -1.775892323017129737 ) ) ;
#123719=CARTESIAN_POINT ( 'NONE',  ( 5.301151097710674165, -1.596257866726397134, 0.9565186216247966167 ) ) ;
#123721=CARTESIAN_POINT ( 'NONE',  ( 2.899894056866093361, -0.9465274319002868753, -1.665356295385928442 ) ) ;
#123722=CARTESIAN_POINT ( 'NONE',  ( 1.043660158496478196, 0.7440559408637310579, -1.667260813828251642 ) ) ;
#123731=CARTESIAN_POINT ( 'NONE',  ( 6.104353324094977218, 1.967046249225043342, 0.1001853051637753428 ) ) ;
#123734=CARTESIAN_POINT ( 'NONE',  ( 1.148509085094330029, -1.646982989033857869, 1.287593708729701802 ) ) ;
#123735=CARTESIAN_POINT ( 'NONE',  ( 6.440456187458303283, 1.905530750978209120, 0.2820203164855574207 ) ) ;
#123737=CARTESIAN_POINT ( 'NONE',  ( 2.871877888313049354, 0.9750061419492547232, 1.543211660213184899 ) ) ;
#123738=CARTESIAN_POINT ( 'NONE',  ( 2.912931060594741162, 1.598032330669514778, -1.522282275181946032 ) ) ;
#123740=CARTESIAN_POINT ( 'NONE',  ( 0.6328886395040033142, 1.767934563615305432, 0.7296191750566642931 ) ) ;
#123741=CARTESIAN_POINT ( 'NONE',  ( 1.574589453129974004, 1.325232347829819135, -1.457171473731319278 ) ) ;
#123742=CARTESIAN_POINT ( 'NONE',  ( 2.278764488077251738, 1.774667200368160280, -0.7891824313753895703 ) ) ;
#123746=CARTESIAN_POINT ( 'NONE',  ( 6.596546450148484730, 1.840605976333910654, 0.2736291870141689397 ) ) ;
#123751=CARTESIAN_POINT ( 'NONE',  ( 2.156058135970494227, 0.9403143569667195001, 1.979733194660021622 ) ) ;
#123755=CARTESIAN_POINT ( 'NONE',  ( 2.543341688579534576, -1.352695106659363766, -1.226303905950577366 ) ) ;
#123756=CARTESIAN_POINT ( 'NONE',  ( 6.016814611094169152, 0.2024578496369993375, 2.006372135924570088 ) ) ;
#123762=CARTESIAN_POINT ( 'NONE',  ( 2.209485269003717445, -0.4220890577730853632, 1.879544223609790565 ) ) ;
#123763=CARTESIAN_POINT ( 'NONE',  ( 6.227397112613878960, 0.1477489091250457076, -1.956280406615627854 ) ) ;
#123764=CIRCLE ( 'NONE', #158318, 0.05000000000000059258 ) ;
#123772=CARTESIAN_POINT ( 'NONE',  ( 5.313363446356571984, -1.745981802610725442, -1.112170280247841703 ) ) ;
#123773=CARTESIAN_POINT ( 'NONE',  ( -0.05938221139379848412, -1.422385081007140117, -1.168950373246782526 ) ) ;
#123775=CARTESIAN_POINT ( 'NONE',  ( 5.695955869756449630, 2.025510559372576402, 1.086827626776807554 ) ) ;
#123779=CARTESIAN_POINT ( 'NONE',  ( 6.550320078384911149, -1.775227793318678415, 1.449923619939506025 ) ) ;
#123783=CARTESIAN_POINT ( 'NONE',  ( 4.892492844921223494, 1.613610725055414141, -1.080192228897313145 ) ) ;
#123788=CARTESIAN_POINT ( 'NONE',  ( 6.082274476537278041, 0.9889857280602430967, 1.636697341158253272 ) ) ;
#123789=CARTESIAN_POINT ( 'NONE',  ( 0.4863796390984359008, -0.2058623683223875511, -1.712490539465325146 ) ) ;
#123790=CARTESIAN_POINT ( 'NONE',  ( 6.245327377194021423, 0.3399632236478037917, -1.987496870419297013 ) ) ;
#123794=CARTESIAN_POINT ( 'NONE',  ( 2.097712127064654819, -2.090152927352141532, 0.05235412406051109108 ) ) ;
#123795=CARTESIAN_POINT ( 'NONE',  ( 1.023854850961497309, 1.058662087540670704, -1.418139054142423472 ) ) ;
#123798=CARTESIAN_POINT ( 'NONE',  ( 3.873197071204284914, 2.158828169701370037, -0.7710026823131793661 ) ) ;
#123799=CARTESIAN_POINT ( 'NONE',  ( 2.519154997858559231, -1.001672848371559787, -1.422942596517995817 ) ) ;
#123802=CARTESIAN_POINT ( 'NONE',  ( 2.442404235307413796, 1.063479746408531046, 1.369289251230455751 ) ) ;
#123804=CARTESIAN_POINT ( 'NONE',  ( 2.101794631558097315, 0.7159089574285321111, -1.718054499674229074 ) ) ;
#123805=CARTESIAN_POINT ( 'NONE',  ( 2.858077868800662724, -0.6831540018236246237, 2.060947818793914532 ) ) ;
#123807=CARTESIAN_POINT ( 'NONE',  ( 3.415250174187448362, -1.861344788686780438, 0.7762291900053899241 ) ) ;
#123808=CARTESIAN_POINT ( 'NONE',  ( 2.968750000000002220, 0.7852924748298364399, -1.895863743164148074 ) ) ;
#123810=CARTESIAN_POINT ( 'NONE',  ( 1.096560174117457764, -0.4650716533593258761, -1.869300808490617305 ) ) ;
#123812=CARTESIAN_POINT ( 'NONE',  ( 4.131244869123442243, 2.031816273447330623, 0.8983479855831574268 ) ) ;
#123814=CARTESIAN_POINT ( 'NONE',  ( -0.2108831679770961920, 2.882544375557041239, -2.385815782126240236 ) ) ;
#123819=CARTESIAN_POINT ( 'NONE',  ( 5.818639523836858451, -0.7989930759073891053, -2.072897825184773168 ) ) ;
#123820=CARTESIAN_POINT ( 'NONE',  ( 5.107842384611220865, 0.6171798735227496113, -1.862306164846748491 ) ) ;
#123822=CARTESIAN_POINT ( 'NONE',  ( 5.360715614582075794, -1.643942929158914268, 1.554587190974612732 ) ) ;
#123824=CARTESIAN_POINT ( 'NONE',  ( 2.787610149020779193, -1.925555389141724527, 0.7399787145165384050 ) ) ;
#123829=CARTESIAN_POINT ( 'NONE',  ( 4.340975799156801429, -1.628549031532234403, 0.9200136957008757665 ) ) ;
#123830=CARTESIAN_POINT ( 'NONE',  ( 4.008270194328780178, -1.657810326508919685, 0.5087727743269004899 ) ) ;
#123831=CARTESIAN_POINT ( 'NONE',  ( 2.085156077859366519, -0.7432962182043149069, 1.573855765194108081 ) ) ;
#123832=CARTESIAN_POINT ( 'NONE',  ( 1.242159777398026410, 2.290014686995527793, 0.1064554428192917290 ) ) ;
#123833=CARTESIAN_POINT ( 'NONE',  ( 1.483733071427257411, 2.038639745401783721, -0.8453341458589253010 ) ) ;
#123834=CARTESIAN_POINT ( 'NONE',  ( 4.177344015168626079, 1.367166224251268547, 1.581858325755406858 ) ) ;
#123835=CARTESIAN_POINT ( 'NONE',  ( 6.035097030359367842, -1.408219244926838476, -1.337428300092268652 ) ) ;
#123839=CARTESIAN_POINT ( 'NONE',  ( 0.2291389764034670318, 2.011204493129043591, 0.1455304468792120720 ) ) ;
#123844=CARTESIAN_POINT ( 'NONE',  ( 4.248545464119923842, 0.4890907236730773766, 1.758887239191930796 ) ) ;
#123845=CARTESIAN_POINT ( 'NONE',  ( 1.905583573826599597, 1.834846665736546756, 1.225745012653912891 ) ) ;
#123851=CARTESIAN_POINT ( 'NONE',  ( 0.6154972907393120307, 1.653649208057221598, 1.159462664468139614 ) ) ;
#123853=CARTESIAN_POINT ( 'NONE',  ( 2.817075279929776688, -1.616631405580427838, -0.9216590669160623639 ) ) ;
#123858=CARTESIAN_POINT ( 'NONE',  ( 5.109893933574640279, -1.816543354971979163, 0.1824992186492402357 ) ) ;
#123863=CARTESIAN_POINT ( 'NONE',  ( 0.2448742905335095366, -1.679455039217644829, -0.4304099419733271592 ) ) ;
#123864=CARTESIAN_POINT ( 'NONE',  ( 6.562460610575872266, -1.685528226061007162, -0.7412392050258274079 ) ) ;
#123865=CARTESIAN_POINT ( 'NONE',  ( 4.565214137342485934, -2.059927483508086965, -1.040394749072820701 ) ) ;
#123867=CARTESIAN_POINT ( 'NONE',  ( 0.4739915956469250014, 1.184468288027096694, 1.686179815164081219 ) ) ;
#123869=CARTESIAN_POINT ( 'NONE',  ( 5.466298696655274902, 1.874607906009964964, 1.329618201824170898 ) ) ;
#123873=CARTESIAN_POINT ( 'NONE',  ( 5.559403950928493821, 0.3636877230743483236, -1.834782481876767291 ) ) ;
#123876=CARTESIAN_POINT ( 'NONE',  ( 2.847809051801777791, -1.287500320553297994, -1.414207669007704116 ) ) ;
#123878=CARTESIAN_POINT ( 'NONE',  ( 5.444034239667132624, 0.8972360612293399651, -2.016436982482258333 ) ) ;
#123879=CARTESIAN_POINT ( 'NONE',  ( 4.944582029040364368, -1.531444570474638667, 1.462332997386527556 ) ) ;
#123884=CARTESIAN_POINT ( 'NONE',  ( 1.817812757297363691, -0.2812075768990837665, 2.290339019377229945 ) ) ;
#123885=CARTESIAN_POINT ( 'NONE',  ( 3.859774877264535053, -0.5717695562157121270, 1.876676618968641019 ) ) ;
#123887=CARTESIAN_POINT ( 'NONE',  ( 6.157095870780715074, 1.689533437190817722, -1.182850423791491856 ) ) ;
#123891=CARTESIAN_POINT ( 'NONE',  ( 5.260953973667149342, -0.05432152012316109058, -2.015980820358989511 ) ) ;
#123895=CARTESIAN_POINT ( 'NONE',  ( 2.131898410887596906, 2.078612851201648404, -0.6269345663092191767 ) ) ;
#123901=CARTESIAN_POINT ( 'NONE',  ( 1.493510409444120057, 1.558468831475682492, 1.348393839584006493 ) ) ;
#123902=CARTESIAN_POINT ( 'NONE',  ( -0.02244404828160087226, 0.2256878572204877031, -2.222431841814066278 ) ) ;
#123903=CARTESIAN_POINT ( 'NONE',  ( 6.727182134110202050, 0.5964276595885747989, 1.864301751488647962 ) ) ;
#123907=CARTESIAN_POINT ( 'NONE',  ( 3.703681524037071071, 1.387051605615218008, 1.316649548728260344 ) ) ;
#123910=CARTESIAN_POINT ( 'NONE',  ( 5.612081123951941919, -0.7985520710115794341, -1.579504676149855458 ) ) ;
#123914=CARTESIAN_POINT ( 'NONE',  ( -0.03024393743376960902, -0.9005804071154848156, 1.690789300719280908 ) ) ;
#123916=CARTESIAN_POINT ( 'NONE',  ( 0.3442982867475213871, -0.9772804826688463731, 1.825211318103404867 ) ) ;
#123919=CARTESIAN_POINT ( 'NONE',  ( 5.647288160985431738, -1.475499438119257878, -1.149758287351684949 ) ) ;
#123920=CARTESIAN_POINT ( 'NONE',  ( 2.543341688579534576, -1.352695106659363766, -1.226303905950577366 ) ) ;
#123921=CARTESIAN_POINT ( 'NONE',  ( 5.830760709146560750, 2.125890151018691832, 0.5921790101122563765 ) ) ;
#123924=CARTESIAN_POINT ( 'NONE',  ( 2.875492298462109630, -0.2048798925258775439, 2.052495523891383566 ) ) ;
#123928=CARTESIAN_POINT ( 'NONE',  ( 0.6675187767142229944, 0.2125181155594977611, -2.151144519195991922 ) ) ;
#123930=CARTESIAN_POINT ( 'NONE',  ( 5.775854211382815073, -2.020734006234246927, 0.4499205674863211990 ) ) ;
#123932=CARTESIAN_POINT ( 'NONE',  ( 3.620547430246877862, 1.374377816306590727, -1.668374205817772182 ) ) ;
#123934=CARTESIAN_POINT ( 'NONE',  ( 3.070967880043346199, -1.527814596969854000, 1.321012706414641524 ) ) ;
#123935=CARTESIAN_POINT ( 'NONE',  ( 2.664445928352857429, -0.7481792696971515388, -1.813797970468238985 ) ) ;
#123936=CARTESIAN_POINT ( 'NONE',  ( 6.620655732516655512, 0.5568428858156619921, 2.325336003765938742 ) ) ;
#123940=CARTESIAN_POINT ( 'NONE',  ( 2.571500236035813902, 1.429449181443824823, 1.422607194786096541 ) ) ;
#123944=CARTESIAN_POINT ( 'NONE',  ( 5.783449990912790106, 0.1341079605299954347, -1.907733270042926810 ) ) ;
#123947=CARTESIAN_POINT ( 'NONE',  ( 2.900017720922347220, -0.9963201819552582883, -1.753021271517739343 ) ) ;
#123950=CARTESIAN_POINT ( 'NONE',  ( 5.860297766850644408, 0.7031890092840873407, 1.575098903243739024 ) ) ;
#123954=CARTESIAN_POINT ( 'NONE',  ( 3.883945074633635031, -0.9243716352356041721, 1.626130415258054018 ) ) ;
#123957=CARTESIAN_POINT ( 'NONE',  ( 2.096617048772158487, 2.047133997803842753, 0.3078910663548983795 ) ) ;
#123961=CARTESIAN_POINT ( 'NONE',  ( 0.2811518721992244951, 0.1772043297433387177, -1.802849762578159876 ) ) ;
#123967=EDGE_CURVE ( 'NONE', #63091, #168104, #106878, .T. ) ;
#123969=CARTESIAN_POINT ( 'NONE',  ( 5.536718839138406345, -1.507006759595967305, 1.182436279247323085 ) ) ;
#123976=CARTESIAN_POINT ( 'NONE',  ( 2.852577672069932735, 0.7271573612388192442, 2.035869728763760378 ) ) ;
#123980=CARTESIAN_POINT ( 'NONE',  ( 5.297797529045337406, -0.6555159417414997414, 1.704002486358429325 ) ) ;
#123982=CARTESIAN_POINT ( 'NONE',  ( 1.124223373062693820, 1.177560201100100734, -1.580856549663816280 ) ) ;
#123983=CARTESIAN_POINT ( 'NONE',  ( 3.621269620730773298, 1.642686141288721480, 0.9789267784374030557 ) ) ;
#123986=CARTESIAN_POINT ( 'NONE',  ( 4.879337363741727884, -0.09859167047137314122, 1.967224067494575346 ) ) ;
#123988=CARTESIAN_POINT ( 'NONE',  ( 5.741732329385339284, 1.940029712683045915, 0.09120231522616148445 ) ) ;
#123993=CARTESIAN_POINT ( 'NONE',  ( 3.457576163436149486, -1.449788379102138869, -1.247086912153513749 ) ) ;
#123996=CARTESIAN_POINT ( 'NONE',  ( 1.202499378025536858, -2.206952907257493823, 0.001246274542086866404 ) ) ;
#123998=CARTESIAN_POINT ( 'NONE',  ( 6.322908177684296582, 1.490210921086480234, -1.353605025193492128 ) ) ;
#124001=CARTESIAN_POINT ( 'NONE',  ( 1.592325325408463055, 1.022198633559557646, -1.800363622228559946 ) ) ;
#124011=CARTESIAN_POINT ( 'NONE',  ( 6.825078400183553384, 4.701740280048592346, 2.318362489372997270 ) ) ;
#124013=CARTESIAN_POINT ( 'NONE',  ( 5.344279299745758216, 0.3302840285365048478, -1.702201177978326818 ) ) ;
#124017=CARTESIAN_POINT ( 'NONE',  ( 1.885682352965558639, -1.950755244972163904, 0.6936349442826782452 ) ) ;
#124018=CARTESIAN_POINT ( 'NONE',  ( 3.093478398350542946, -0.4104027421963015732, 2.076914780291692519 ) ) ;
#124021=CARTESIAN_POINT ( 'NONE',  ( 1.252720943002823883, -0.4733663544725670302, -1.911600023467324716 ) ) ;
#124024=CARTESIAN_POINT ( 'NONE',  ( 0.1934256698341470238, 1.783621342183003389, -0.6902995980747894667 ) ) ;
#124025=CARTESIAN_POINT ( 'NONE',  ( 3.363489724395284597, 2.236470799849974878, -0.5019982374358539223 ) ) ;
#124026=CARTESIAN_POINT ( 'NONE',  ( 1.400715809426569702, 1.493624456287694580, -1.049586478250638777 ) ) ;
#124031=CARTESIAN_POINT ( 'NONE',  ( 3.093996842688331750, 1.280297628565935097, 1.553616095213964154 ) ) ;
#124032=CARTESIAN_POINT ( 'NONE',  ( 2.992962298452767289, 0.2353761085502041883, 1.947492218917420637 ) ) ;
#124036=CARTESIAN_POINT ( 'NONE',  ( 5.771452434752829319, 1.244600244801373767, 1.679635579212119145 ) ) ;
#124037=CARTESIAN_POINT ( 'NONE',  ( 5.032005376881601322, 0.9078957314892305286, -1.519088338465144128 ) ) ;
#124039=CARTESIAN_POINT ( 'NONE',  ( 0.6389542677898361056, -1.877638805159736579, 1.129783718924075364 ) ) ;
#124040=CARTESIAN_POINT ( 'NONE',  ( 5.665861931341662938, -1.099307624823061547, 1.349167961392354620 ) ) ;
#124043=CARTESIAN_POINT ( 'NONE',  ( 6.451773728000877561, -2.099535003536470157, -0.9362560538537908483 ) ) ;
#124044=CARTESIAN_POINT ( 'NONE',  ( 0.1333692844072767447, 1.351132181276387678, -2.308013766563504987 ) ) ;
#124046=CARTESIAN_POINT ( 'NONE',  ( 5.096919866207451300, 0.8898786499993548427, -1.487894112255260692 ) ) ;
#124047=CARTESIAN_POINT ( 'NONE',  ( 5.951682048281027981, 1.640226396406889942, 1.422642917226999426 ) ) ;
#124049=CARTESIAN_POINT ( 'NONE',  ( 0.1634790396850393235, 1.973143002845114458, -0.7684359545688070892 ) ) ;
#124050=CARTESIAN_POINT ( 'NONE',  ( 2.625000000000002665, -2.052068128417949833, 1.560916121760785068E-13 ) ) ;
#124051=CARTESIAN_POINT ( 'NONE',  ( 6.727182134110242906, 2.956326135258012577, 2.541581140702349195 ) ) ;
#124052=CARTESIAN_POINT ( 'NONE',  ( 3.961874236345910294, 1.911929771648058995, -0.2350156305768891229 ) ) ;
#124054=CARTESIAN_POINT ( 'NONE',  ( 1.260717678522350838, 2.218966152042425755, 0.1042569218142989779 ) ) ;
#124060=CARTESIAN_POINT ( 'NONE',  ( 2.737233380259511684, 2.092449130469396401, 0.7459289674271016857 ) ) ;
#124066=CARTESIAN_POINT ( 'NONE',  ( 0.9322677863709986079, -1.591319861332978425, -1.238319039483272599 ) ) ;
#124068=CARTESIAN_POINT ( 'NONE',  ( 6.531690654341108626, 1.975040822251827644, -0.5949189890239890977 ) ) ;
#124074=CARTESIAN_POINT ( 'NONE',  ( 1.229378055282577042, -1.117200307070218779, -1.372552531265440523 ) ) ;
#124075=CARTESIAN_POINT ( 'NONE',  ( 6.486931489777390425, -1.733547045345487758, 0.05303144115107599060 ) ) ;
#124076=CARTESIAN_POINT ( 'NONE',  ( 6.480030497237043718, -1.708793550445006248, -0.3294957622956768972 ) ) ;
#124077=CARTESIAN_POINT ( 'NONE',  ( 4.089605575727714104, -0.8772585143675699637, 2.118060962191004037 ) ) ;
#124079=CARTESIAN_POINT ( 'NONE',  ( 2.677489186553200007, -0.9463553590365643142, 1.579155189138586435 ) ) ;
#124083=CARTESIAN_POINT ( 'NONE',  ( 3.364083894888194592, 0.8197913233371353359, 1.631220078658943695 ) ) ;
#124084=CARTESIAN_POINT ( 'NONE',  ( 4.307267641921147749, 1.238321930042911578, -1.591317616567271775 ) ) ;
#124086=CARTESIAN_POINT ( 'NONE',  ( 3.344836307015612409, 0.5477570922035517320, 2.195101814764536030 ) ) ;
#124088=CARTESIAN_POINT ( 'NONE',  ( 5.614326327132292072, -0.9438296153482359507, -1.882684210903639022 ) ) ;
#124090=CARTESIAN_POINT ( 'NONE',  ( 2.910663983731573090, 0.6951178490613962868, 1.950330170896700022 ) ) ;
#124093=CARTESIAN_POINT ( 'NONE',  ( 4.899148033862871010, -0.2601683324335197223, -2.104413843559429065 ) ) ;
#124095=CARTESIAN_POINT ( 'NONE',  ( 0.5570954828270138215, -1.626785562868319435, -1.031698974670463009 ) ) ;
#124103=CARTESIAN_POINT ( 'NONE',  ( 0.6509960782678033686, 2.189857587618043055, 0.3722473809256007793 ) ) ;
#124104=CARTESIAN_POINT ( 'NONE',  ( 2.204260208318520764, -2.105514897310766020, 0.05069945311739902649 ) ) ;
#124107=CARTESIAN_POINT ( 'NONE',  ( 6.016418624437367413, 0.7528656616105857680, 1.702022903989255376 ) ) ;
#124109=CARTESIAN_POINT ( 'NONE',  ( -0.02319159430949970652, 0.003959926571647092407, -1.810968101872318714 ) ) ;
#124112=CARTESIAN_POINT ( 'NONE',  ( 0.6332531790259123827, 1.961634380476449335, 0.8060562103610890983 ) ) ;
#124115=CARTESIAN_POINT ( 'NONE',  ( 3.631260574587381829, 0.05062604155347744800, -1.961386756325018021 ) ) ;
#124116=CARTESIAN_POINT ( 'NONE',  ( 1.727627455807039691, -2.035446057602477321, 0.7283451284763039490 ) ) ;
#124120=CARTESIAN_POINT ( 'NONE',  ( 3.573892692743201760, -1.677664982382242931, -0.4625120326062928111 ) ) ;
#124125=CARTESIAN_POINT ( 'NONE',  ( 2.460314346279086628, 1.556669099887195484, 1.281166478716524670 ) ) ;
#124126=CARTESIAN_POINT ( 'NONE',  ( 6.825078400183572036, 7.051914997414900022, 2.742498282622223726 ) ) ;
#124128=CARTESIAN_POINT ( 'NONE',  ( 2.008605748815388559, 1.462198227207864853, -1.322556311574287768 ) ) ;
#124135=CARTESIAN_POINT ( 'NONE',  ( 2.596358364526121676, -1.036244631391324722, 1.733413072464027316 ) ) ;
#124137=CARTESIAN_POINT ( 'NONE',  ( 6.247156018452869830, -1.954037266989640420, 1.227234044731172036 ) ) ;
#124139=CARTESIAN_POINT ( 'NONE',  ( 3.467582345443523728, -0.3871886708083654427, 1.922995549214156608 ) ) ;
#124141=CARTESIAN_POINT ( 'NONE',  ( 1.055314813143366726, -1.277040974352643854, 1.560502084637045650 ) ) ;
#124143=CARTESIAN_POINT ( 'NONE',  ( 1.956417434996825522, -1.298217783395636316, 1.672616391537498526 ) ) ;
#124146=CARTESIAN_POINT ( 'NONE',  ( 2.097363409947244683, -1.840767647902554982, 0.04455809990146220728 ) ) ;
#124150=CARTESIAN_POINT ( 'NONE',  ( 2.742561299210785286, 1.174483946500170184, -1.765453564165630596 ) ) ;
#124151=CARTESIAN_POINT ( 'NONE',  ( 0.4097734724025984820, 1.271762808003698009, -1.331557029818277060 ) ) ;
#124155=CARTESIAN_POINT ( 'NONE',  ( 4.130192093715317370, 1.105610312200686174, -1.738907380658259560 ) ) ;
#124157=CARTESIAN_POINT ( 'NONE',  ( 1.821575194732877545, 1.059174331173462935, -1.505913648122420900 ) ) ;
#124162=CARTESIAN_POINT ( 'NONE',  ( 1.225528936851564721, -0.05108506852482053856, 2.206457870188942572 ) ) ;
#124163=CARTESIAN_POINT ( 'NONE',  ( 3.409705294423628352, -0.4451680670645007387, 2.218022689048837481 ) ) ;
#124165=CARTESIAN_POINT ( 'NONE',  ( 3.849720854566369255, -1.253557171431567863, -1.308061721885760198 ) ) ;
#124166=CARTESIAN_POINT ( 'NONE',  ( 2.571384127028350175, 1.358050290760448364, 1.351446277617992076 ) ) ;
#124167=CARTESIAN_POINT ( 'NONE',  ( 4.299325596424930396, -1.802881993240162961, 1.017688063649782482 ) ) ;
#124169=CARTESIAN_POINT ( 'NONE',  ( 2.711746521272298871, -1.950232680175187250, 0.2877518621813393018 ) ) ;
#124170=CARTESIAN_POINT ( 'NONE',  ( 1.536025370465494921, 0.9519229637394033272, -1.674701244428679292 ) ) ;
#124171=CARTESIAN_POINT ( 'NONE',  ( 3.432352559540859271, 1.824792983844251371, 0.4109263881779609551 ) ) ;
#124172=CARTESIAN_POINT ( 'NONE',  ( 2.403307275528394626, 1.852421531443759539, -1.376039175078101806 ) ) ;
#124173=CARTESIAN_POINT ( 'NONE',  ( 3.508111033888267283, 1.861241883637313688, 0.002260837353922766878 ) ) ;
#124179=CARTESIAN_POINT ( 'NONE',  ( 0.2234445423696731770, -0.1008541980360810469, 2.103780803345968398 ) ) ;
#124183=CARTESIAN_POINT ( 'NONE',  ( 6.731704548537910782, -1.406307105171537009, -1.641701734229366716 ) ) ;
#124184=CARTESIAN_POINT ( 'NONE',  ( 1.582450481569739331, 1.094613367649547309, 1.816135667671102016 ) ) ;
#124185=CARTESIAN_POINT ( 'NONE',  ( 0.2287787457191146345, 1.389782569690813929, -1.465877111898945095 ) ) ;
#124189=CARTESIAN_POINT ( 'NONE',  ( 1.124558466181435179, 1.288545020775376804, -1.735378439385642180 ) ) ;
#124194=CARTESIAN_POINT ( 'NONE',  ( 6.051970301643104122, 1.040788372175960541, 1.727066800951609249 ) ) ;
#124198=CARTESIAN_POINT ( 'NONE',  ( 0.8314075926023238861, 0.1693486111025067908, 2.256218002396610522 ) ) ;
#124202=CARTESIAN_POINT ( 'NONE',  ( 6.450795914701256351, -1.844717532910484570, -0.8146137538835170888 ) ) ;
#124207=CARTESIAN_POINT ( 'NONE',  ( 3.053030289171186684, -1.410389792183571966, -0.9926723171444253868 ) ) ;
#124211=CARTESIAN_POINT ( 'NONE',  ( 1.369957856843624366, -1.128201996292097498, 1.363478919461190708 ) ) ;
#124212=CARTESIAN_POINT ( 'NONE',  ( 2.332683495817444719, 1.313167467523576715, -1.525923137932885476 ) ) ;
#124214=CARTESIAN_POINT ( 'NONE',  ( 3.663272223086514234, -1.945104670120747059, -1.042327912031751458 ) ) ;
#124217=CARTESIAN_POINT ( 'NONE',  ( 4.881546266219149999, 0.2071824046101199135, -2.110321684233848583 ) ) ;
#124218=CARTESIAN_POINT ( 'NONE',  ( 2.636342400811112707, 0.6820146075395253638, 1.897692325672148073 ) ) ;
#124219=CARTESIAN_POINT ( 'NONE',  ( 3.234412676589659252, 1.145595053071927438, -1.403395578055862902 ) ) ;
#124224=CARTESIAN_POINT ( 'NONE',  ( 1.287742131874554552, -0.8442722623961744777, 1.669378388412197767 ) ) ;
#124226=CARTESIAN_POINT ( 'NONE',  ( 6.568987803155795113, -1.671525225137669102, -0.7347104647430282576 ) ) ;
#124228=CARTESIAN_POINT ( 'NONE',  ( 2.764735878068668384, -0.1456047134679704924, -1.910273805325033436 ) ) ;
#124235=CARTESIAN_POINT ( 'NONE',  ( 3.269896953881154644, 0.5115095171020591636, -2.057881918134551125 ) ) ;
#124236=CARTESIAN_POINT ( 'NONE',  ( -0.02968770228139669398, 7.629137130509076492, -2.426318643530885222 ) ) ;
#124238=CARTESIAN_POINT ( 'NONE',  ( 3.884019131438942285, -0.9746410142534560617, 1.713524893406521699 ) ) ;
#124239=CARTESIAN_POINT ( 'NONE',  ( -0.08764186210430401081, -2.012836238882615980, -0.04531326932211143105 ) ) ;
#124241=CARTESIAN_POINT ( 'NONE',  ( 0.03496603831146075092, -1.697522432243668389, 1.265142316669096934 ) ) ;
#124243=CARTESIAN_POINT ( 'NONE',  ( 2.014207461368537455, 2.064961549741591185, -0.1501100615294431728 ) ) ;
#124248=CARTESIAN_POINT ( 'NONE',  ( 3.697287448106700403, -0.6068447087972194121, 2.000623839779874125 ) ) ;
#124251=CARTESIAN_POINT ( 'NONE',  ( 0.6975727754284127835, 1.215713746931287753, 1.343078931132860587 ) ) ;
#124252=CARTESIAN_POINT ( 'NONE',  ( 5.725267921653402148, -0.05769419298589681389, 2.206291853148376170 ) ) ;
#124255=CARTESIAN_POINT ( 'NONE',  ( 4.137865722265689605, -1.519559189622637252, -1.600479987451455699 ) ) ;
#124258=CARTESIAN_POINT ( 'NONE',  ( 2.772007568003355793, 1.902874960710929431, -0.1895390408453850317 ) ) ;
#124260=CARTESIAN_POINT ( 'NONE',  ( 5.213363469605923228, -1.747142239327776903, -1.110534646669825376 ) ) ;
#124262=CARTESIAN_POINT ( 'NONE',  ( 2.483474991488154870, 1.976725341044349271, -0.8753317036461552014 ) ) ;
#124263=CARTESIAN_POINT ( 'NONE',  ( 6.462441986028243157, -2.002789442531027309, -0.8901952361822995652 ) ) ;
#124267=PRESENTATION_STYLE_ASSIGNMENT (( #125326 ) ) ;
#124271=CARTESIAN_POINT ( 'NONE',  ( -0.2102771530458276972, -0.008943344768330967198, -2.203482896658349066 ) ) ;
#124274=CARTESIAN_POINT ( 'NONE',  ( 5.717656431054087385, 0.4094431674900833595, -2.029196096928844284 ) ) ;
#124275=CARTESIAN_POINT ( 'NONE',  ( 4.881433204766033818, 1.796953459403265674, -0.6949688560347905275 ) ) ;
#124276=CARTESIAN_POINT ( 'NONE',  ( 0.4039230143318903177, -1.081087622585241714, -1.701935196855845822 ) ) ;
#124280=CARTESIAN_POINT ( 'NONE',  ( 6.615150229029130635, -2.225211831249251482, 0.5499996461680799476 ) ) ;
#124281=CARTESIAN_POINT ( 'NONE',  ( 4.881388680972561289, 1.702354803207173584, -0.6601141376258444771 ) ) ;
#124288=CARTESIAN_POINT ( 'NONE',  ( 2.911469271472226339, -0.9098125248445630975, -1.600700954789348263 ) ) ;
#124289=CARTESIAN_POINT ( 'NONE',  ( 5.801044709096109031, -0.2997443204828981189, -1.990672168044338886 ) ) ;
#124290=CARTESIAN_POINT ( 'NONE',  ( 1.195116192591906046, -1.458952948520657156, -1.775991855458454838 ) ) ;
#124291=CARTESIAN_POINT ( 'NONE',  ( 6.262552437187629550, -0.7028992384056665932, -1.831702256219314151 ) ) ;
#124295=CARTESIAN_POINT ( 'NONE',  ( 0.5200892513525963157, 2.048054262204841880, -0.3022008342252607838 ) ) ;
#124297=CARTESIAN_POINT ( 'NONE',  ( 2.261376066768826743, 2.049819659885134371, -0.4107522398083974791 ) ) ;
#124298=CARTESIAN_POINT ( 'NONE',  ( 1.569004590881704075, 0.1408476687595125731, -1.865417194689425795 ) ) ;
#124299=CARTESIAN_POINT ( 'NONE',  ( 2.126327167286511166, 0.3474154575464418748, -1.985796285822030161 ) ) ;
#124303=CARTESIAN_POINT ( 'NONE',  ( 2.524636229566870060, -1.623295675544262906, 0.6281775017502010394 ) ) ;
#124307=CARTESIAN_POINT ( 'NONE',  ( 2.824480366436402878, 1.624150206794371609, 0.5811974035451406007 ) ) ;
#124308=CARTESIAN_POINT ( 'NONE',  ( 2.366952063387484095, 0.1042156695447923470, -2.189191704635709890 ) ) ;
#124310=CARTESIAN_POINT ( 'NONE',  ( 5.742855475442601332, 0.4270144693867898300, 2.165010647329483895 ) ) ;
#124312=CARTESIAN_POINT ( 'NONE',  ( 1.938562956190786002, -1.164097522067691903, 1.832441342696682574 ) ) ;
#124313=CARTESIAN_POINT ( 'NONE',  ( 1.189776066567624691, -0.8228614858879386151, 1.629801898503015156 ) ) ;
#124314=CARTESIAN_POINT ( 'NONE',  ( 3.046228577489984879, 0.9562745863303960814, 1.889201325992972080 ) ) ;
#124315=CARTESIAN_POINT ( 'NONE',  ( 6.539320575229256249, 2.979067782826943844, 2.350490835693248126 ) ) ;
#124317=CARTESIAN_POINT ( 'NONE',  ( 4.142302782979132125, 0.6112592793995803575, 2.209291399377455889 ) ) ;
#124321=CARTESIAN_POINT ( 'NONE',  ( 6.551452540055466400, -1.985718062329771438, 0.9957849561875466993 ) ) ;
#124327=CARTESIAN_POINT ( 'NONE',  ( 4.342422763466713853, 0.4390309838058319425, -1.967887491402267486 ) ) ;
#124329=CARTESIAN_POINT ( 'NONE',  ( 3.397386871994355850, -1.821155587584430302, 0.9682287363927607471 ) ) ;
#124335=CARTESIAN_POINT ( 'NONE',  ( 6.158177532299373702, -1.552315630085840947, 1.547116483708823598 ) ) ;
#124336=CARTESIAN_POINT ( 'NONE',  ( 3.902970337090125863, -1.038992709432768891, -1.728002613881730598 ) ) ;
#124337=CARTESIAN_POINT ( 'NONE',  ( 3.561895345837225779, -1.234009368583251387, 1.366721199326895952 ) ) ;
#124340=CARTESIAN_POINT ( 'NONE',  ( 6.282242891264209206, -0.9739734823789309992, 1.543877162560060912 ) ) ;
#124342=CARTESIAN_POINT ( 'NONE',  ( 6.508658281791896094, 1.681912584842374159, -1.513523023287469016 ) ) ;
#124343=CARTESIAN_POINT ( 'NONE',  ( 1.576933964714849701, -2.000244969732989819, -0.6594162861879059312 ) ) ;
#124353=CARTESIAN_POINT ( 'NONE',  ( 3.814843914748572207, -0.6992408500761657653, -2.108525230111441218 ) ) ;
#124354=CARTESIAN_POINT ( 'NONE',  ( 0.7443833103580774768, 0.6396484562771962423, 2.096019810003430184 ) ) ;
#124355=CARTESIAN_POINT ( 'NONE',  ( 0.3291288957359936318, 2.113116833900237967, 0.6364493931270903682 ) ) ;
#124358=CARTESIAN_POINT ( 'NONE',  ( 4.088298575758734898, 1.051444423028622399, -1.656135347060924135 ) ) ;
#124361=DIRECTION ( 'NONE',  ( -1.000000000000000000, 0.000000000000000000, 0.000000000000000000 ) ) ;
#124366=CARTESIAN_POINT ( 'NONE',  ( 3.603867943843573673, 1.538443694073919898, 1.459757404076333698 ) ) ;
#124368=CARTESIAN_POINT ( 'NONE',  ( 5.524359596833869013, 1.291058806671550485, -1.733668313432787933 ) ) ;
#124369=CARTESIAN_POINT ( 'NONE',  ( 3.931074656914943954, -1.272613488525012659, -1.330884258478791438 ) ) ;
#124372=CARTESIAN_POINT ( 'NONE',  ( -0.04197470322641042723, -1.553021824201283208, -0.7857045047398486526 ) ) ;
#124377=CARTESIAN_POINT ( 'NONE',  ( 4.416967121957662279, 1.975198431823081302, 0.8787980929093119897 ) ) ;
#124378=CARTESIAN_POINT ( 'NONE',  ( 5.571638683613604037, 1.528505562557905595, -1.314797328242120367 ) ) ;
#124380=CARTESIAN_POINT ( 'NONE',  ( 3.643588467267334874, -1.635511012911139650, -1.413612897787956513 ) ) ;
#124381=CARTESIAN_POINT ( 'NONE',  ( 3.954335293022055886, 0.7064427249091516092, 1.840614667007954841 ) ) ;
#124383=CARTESIAN_POINT ( 'NONE',  ( 1.044460364342413072, 0.9324277726035223868, -2.110995228001291579 ) ) ;
#124384=CARTESIAN_POINT ( 'NONE',  ( 3.690745141589413691, -0.3983964448436724259, -2.021722667813256269 ) ) ;
#124385=CARTESIAN_POINT ( 'NONE',  ( 5.214377421777850685, 1.795891487756570815, 0.7396389662707256729 ) ) ;
#124393=CARTESIAN_POINT ( 'NONE',  ( 2.186817281270125424, -2.164169025584137263, -0.4306803264119417607 ) ) ;
#124395=CARTESIAN_POINT ( 'NONE',  ( 6.719590461409528537, 0.3385411321301828314, -1.932175811092277096 ) ) ;
#124396=CARTESIAN_POINT ( 'NONE',  ( -0.02880301295726198432, 7.629137130509075604, -2.873797191217826619 ) ) ;
#124401=CARTESIAN_POINT ( 'NONE',  ( 5.648353745280480176, -1.448853643138726000, 1.135948691490688667 ) ) ;
#124403=CARTESIAN_POINT ( 'NONE',  ( 2.588805925060005730, -0.3509353788873382229, -2.030617818815634745 ) ) ;
#124410=CARTESIAN_POINT ( 'NONE',  ( 1.217730312517154800, -2.010830008989676898, 0.4507304159913956831 ) ) ;
#124412=CARTESIAN_POINT ( 'NONE',  ( 5.231922985772964552, 1.814955821992572993, 0.3091130605668013231 ) ) ;
#124416=CARTESIAN_POINT ( 'NONE',  ( 6.610000000000030518, 1.266345627986571021, 2.115470293623383569 ) ) ;
#124418=CARTESIAN_POINT ( 'NONE',  ( 4.776106669258010307, 1.268914099295117781, 1.805409367619143390 ) ) ;
#124419=CARTESIAN_POINT ( 'NONE',  ( 0.6148119136215323133, 1.491057340773978668, -1.565211586912764741 ) ) ;
#124422=CARTESIAN_POINT ( 'NONE',  ( 0.4395310841842986482, -1.815173276516975243, 0.6020934215927520317 ) ) ;
#124423=CARTESIAN_POINT ( 'NONE',  ( 6.034394305845959927, 0.6080466156053351279, 1.816710885969755163 ) ) ;
#124425=CARTESIAN_POINT ( 'NONE',  ( 1.669710354559012622, -0.8274895997400324443, -2.144421126502197517 ) ) ;
#124427=CARTESIAN_POINT ( 'NONE',  ( 0.07536363704237906969, 4.084105538841027894, -2.698926661290324880 ) ) ;
#124428=CARTESIAN_POINT ( 'NONE',  ( 5.074826771331380826, -1.382354945563003312, 1.321565576914075502 ) ) ;
#124430=CARTESIAN_POINT ( 'NONE',  ( 0.7252172114964609007, -1.777616610744123804, 0.5828384007960025759 ) ) ;
#124431=CARTESIAN_POINT ( 'NONE',  ( 2.923064838257955156, -1.776166165677966591, 0.9548571111624851726 ) ) ;
#124433=CARTESIAN_POINT ( 'NONE',  ( 3.721394855333003626, -0.1548319924524182156, 2.100431540652194062 ) ) ;
#124438=CARTESIAN_POINT ( 'NONE',  ( 3.656514325482379757, 2.010451960178538222, 0.1936393378089220907 ) ) ;
#124441=CARTESIAN_POINT ( 'NONE',  ( 4.745497693432328745, -1.667575968047749546, -1.375352955852253922 ) ) ;
#124447=CARTESIAN_POINT ( 'NONE',  ( 1.539757937649718800, 2.006347644133343433, -0.8302594476135690682 ) ) ;
#124450=CARTESIAN_POINT ( 'NONE',  ( 1.100829259350871281, -0.4471758257712907247, 1.786007343351428966 ) ) ;
#124452=CARTESIAN_POINT ( 'NONE',  ( 3.597391730528697540, -0.6346259394694170330, 2.097678010650514402 ) ) ;
#124453=CARTESIAN_POINT ( 'NONE',  ( 6.883263157960404222, 3.695221384915627905, 2.468000959490519897 ) ) ;
#124454=CARTESIAN_POINT ( 'NONE',  ( 4.276442053719103242, -1.305714526237568229, 1.847550228136185302 ) ) ;
#124460=CARTESIAN_POINT ( 'NONE',  ( 4.692510491889085422, -0.3870912556891945577, -1.726709192852653230 ) ) ;
#124463=CARTESIAN_POINT ( 'NONE',  ( 0.5871190474453058528, -0.2578297629921856293, -2.090033075799145657 ) ) ;
#124466=CARTESIAN_POINT ( 'NONE',  ( 1.012081461190861065, 1.967466754592902989, -0.09309286250217158054 ) ) ;
#124468=CARTESIAN_POINT ( 'NONE',  ( 0.2386218892466463737, -1.902018210125755004, -0.4804332253167050149 ) ) ;
#124472=CARTESIAN_POINT ( 'NONE',  ( 5.278141497218024725, -1.038406966791558528, 1.555765341417144842 ) ) ;
#124474=B_SPLINE_CURVE_WITH_KNOTS ( 'NONE', 3,
 ( #181392, #167287, #33015, #17796, #99094, #35127, #165146, #82823, #149974, #1544, #67606 ),
 .UNSPECIFIED., .F., .F.,
 ( 4, 1, 1, 1, 1, 1, 1, 1, 4 ),
 ( 0.000000000000000000, 0.2255234228546724728, 0.3973271701647976828, 0.5245128843546777997, 0.6161923999872991331, 0.6815320185768301009, 0.7298552812456317040, 0.7704940248801678271, 1.000000000000000000 ),
 .UNSPECIFIED. ) ;
#124475=CARTESIAN_POINT ( 'NONE',  ( 4.170806909802426965, 1.467596682293986765, -1.460439952253207663 ) ) ;
#124484=CARTESIAN_POINT ( 'NONE',  ( 4.246505328441081417, -1.940195102956907336, -0.2900488188990399396 ) ) ;
#124485=CARTESIAN_POINT ( 'NONE',  ( 2.618517346670693247, 0.5404096030681635465, -1.942243668081746311 ) ) ;
#124489=CARTESIAN_POINT ( 'NONE',  ( 1.493192106177696044, 1.412881632968411516, 1.225925835885120829 ) ) ;
#124491=CARTESIAN_POINT ( 'NONE',  ( 2.513933912945048199, -0.6273889547634775576, 1.913045067402745936 ) ) ;
#124493=CARTESIAN_POINT ( 'NONE',  ( 3.550509549652399066, -1.420143166946661317, 1.570484981737807706 ) ) ;
#124495=CARTESIAN_POINT ( 'NONE',  ( 4.756339170418532269, -2.069830778647030023, -0.05414847147890837487 ) ) ;
#124497=CARTESIAN_POINT ( 'NONE',  ( 0.4684514965578719381, -1.969967889910573033, -0.7007429371770137472 ) ) ;
#124498=CARTESIAN_POINT ( 'NONE',  ( 6.720655732516665815, 3.683894443391816154, 2.687682123607849416 ) ) ;
#124499=CARTESIAN_POINT ( 'NONE',  ( 5.825187583072056974, -0.04236064406601056098, 1.825263316621673848 ) ) ;
#124503=MECHANICAL_DESIGN_GEOMETRIC_PRESENTATION_REPRESENTATION('',(#37991),#186713);
#124506=CARTESIAN_POINT ( 'NONE',  ( 5.690081826675051246, 1.142623417513729089, 1.533212917768103534 ) ) ;
#124511=PLANE ( 'NONE',  #151500 ) ;
#124516=CARTESIAN_POINT ( 'NONE',  ( 5.220327442464319567, 1.987051044970666647, 0.3419161450798278157 ) ) ;
#124523=CARTESIAN_POINT ( 'NONE',  ( 1.973436150528505406, -0.2460485697947655814, 1.953970194506114755 ) ) ;
#124524=CARTESIAN_POINT ( 'NONE',  ( 3.181267708840180841, 1.591331833097202830, 1.238305487465785948 ) ) ;
#124526=CARTESIAN_POINT ( 'NONE',  ( 6.727182134110239353, -0.007837387828812587484, 2.289081727344749684 ) ) ;
#124527=CARTESIAN_POINT ( 'NONE',  ( 3.363397379774799134, 2.138023915923603635, -0.4802275100637617977 ) ) ;
#124529=CARTESIAN_POINT ( 'NONE',  ( 2.204012588094861780, -1.926017964255047010, 0.04517517324725479899 ) ) ;
#124532=CARTESIAN_POINT ( 'NONE',  ( 0.2329586101569553480, 1.399178205689523224, -2.105666472772389941 ) ) ;
#124540=CARTESIAN_POINT ( 'NONE',  ( 6.304252605626877504, 1.359535501544101077, -1.241908024382516240 ) ) ;
#124541=CARTESIAN_POINT ( 'NONE',  ( 3.457684585873057159, -1.525941150838805216, -1.313146537923309376 ) ) ;
#124542=CARTESIAN_POINT ( 'NONE',  ( 4.411641467711771014, 0.6073606466481770161, 2.216650271500276492 ) ) ;
#124543=CARTESIAN_POINT ( 'NONE',  ( -0.02880301295729841352, 5.718910385480866054, -2.867850616339829628 ) ) ;
#124544=CARTESIAN_POINT ( 'NONE',  ( 2.746734941909965588, -0.3128536233567563163, -1.834277165529672793 ) ) ;
#124550=CARTESIAN_POINT ( 'NONE',  ( 6.392138156072928901, -0.5583118246898631787, -2.014728688386701272 ) ) ;
#124556=CARTESIAN_POINT ( 'NONE',  ( 6.481054518252093111, -0.09278056567359710405, -1.722521162943893014 ) ) ;
#124558=CARTESIAN_POINT ( 'NONE',  ( 1.933800834616914877, -1.393042465158848886, -1.032573028607612464 ) ) ;
#124561=CARTESIAN_POINT ( 'NONE',  ( 6.350449713519967787, -2.159805286613075470, -0.2212482231108928721 ) ) ;
#124562=CARTESIAN_POINT ( 'NONE',  ( 4.529811765687052016, -1.125283923072720071, -1.437579299059896343 ) ) ;
#124563=CARTESIAN_POINT ( 'NONE',  ( 2.623818369222921554, 1.924856029493416276, -0.3778354045670463401 ) ) ;
#124567=CARTESIAN_POINT ( 'NONE',  ( 4.196021508500130004, 1.385991406618786836, 1.604897850144955340 ) ) ;
#124571=CARTESIAN_POINT ( 'NONE',  ( 1.868117093089691760, -2.055091939184821026, 0.2493290443424806546 ) ) ;
#124574=CARTESIAN_POINT ( 'NONE',  ( 3.932468528151237042, -1.142516171320803853, -1.904832733444387971 ) ) ;
#124576=CARTESIAN_POINT ( 'NONE',  ( 1.969760627029959688, -2.255332599139341809, -0.4437108664413855763 ) ) ;
#124578=CARTESIAN_POINT ( 'NONE',  ( 6.912941059211402894, -1.598140348199797556, 1.303530876689311224 ) ) ;
#124583=FACE_OUTER_BOUND ( 'NONE', #103714, .T. ) ;
#124584=CARTESIAN_POINT ( 'NONE',  ( -0.1106727585416019261, 5.721739388512169455, -2.597565591738408841 ) ) ;
#124585=CARTESIAN_POINT ( 'NONE',  ( 3.223388876545678183, -1.662537434388009938, 0.4588695312727729125 ) ) ;
#124586=CARTESIAN_POINT ( 'NONE',  ( 2.553923023464285347, 1.082840749376843270, 1.700961377887353798 ) ) ;
#124587=CARTESIAN_POINT ( 'NONE',  ( 2.708015267422092531, 2.165615165066101966, 0.7711511238016451886 ) ) ;
#124588=CARTESIAN_POINT ( 'NONE',  ( 3.233911077135812384, -1.516719621523674677, -1.678889276187053081 ) ) ;
#124589=CARTESIAN_POINT ( 'NONE',  ( 5.180345272937711520, -1.170841012621581134, 1.750402278287941149 ) ) ;
#124592=CARTESIAN_POINT ( 'NONE',  ( 3.831107792978345472, -1.636083747181043879, 0.6751729126634566924 ) ) ;
#124595=CARTESIAN_POINT ( 'NONE',  ( 6.023008118121612853, -2.159854764417634687, 0.7684156934805678185 ) ) ;
#124596=CARTESIAN_POINT ( 'NONE',  ( 5.894452933195245770, 1.502573388107550034, -1.063714819228026132 ) ) ;
#124599=CARTESIAN_POINT ( 'NONE',  ( 6.175747540105122724, -1.175446681380667213, 1.849350104233343783 ) ) ;
#124602=CARTESIAN_POINT ( 'NONE',  ( 6.039524589772497620, 1.914416561877980261, -0.7887839105886890190 ) ) ;
#124603=CARTESIAN_POINT ( 'NONE',  ( 0.6379081216283178923, 2.014007883293071899, -0.1037844182863178755 ) ) ;
#124607=CARTESIAN_POINT ( 'NONE',  ( 3.492722931844041145, -0.3765888977748827471, -1.889173544197232824 ) ) ;
#124610=CARTESIAN_POINT ( 'NONE',  ( 0.3170205077604414945, -0.7560223448306638838, -2.088923821510160650 ) ) ;
#124619=CARTESIAN_POINT ( 'NONE',  ( 1.644895634054041933, -0.2845770130874228365, -1.940982728367894206 ) ) ;
#124622=CARTESIAN_POINT ( 'NONE',  ( 5.160583804383015227, -0.6592509027269661814, -1.847929681152965520 ) ) ;
#124624=EDGE_CURVE ( 'NONE', #89432, #87871, #171262, .T. ) ;
#124626=CARTESIAN_POINT ( 'NONE',  ( 6.508665849870632236, 1.605377118863276387, -1.447859449074364591 ) ) ;
#124630=CARTESIAN_POINT ( 'NONE',  ( 0.8427765623921362748, -1.607460297381148928, 0.9563107477488577146 ) ) ;
#124631=CARTESIAN_POINT ( 'NONE',  ( 5.712138547670210009, -1.368237114983595237, -1.064765744168968187 ) ) ;
#124633=CARTESIAN_POINT ( 'NONE',  ( 3.245827600587628758, 2.191739723504753101, -0.002129563554123526260 ) ) ;
#124634=CARTESIAN_POINT ( 'NONE',  ( 4.682853559034357183, -2.237096095179165633, -0.5655516052204231370 ) ) ;
#124636=CARTESIAN_POINT ( 'NONE',  ( 0.1806374041631699234, -1.998871265498179506, -0.5013196448642556202 ) ) ;
#124637=CARTESIAN_POINT ( 'NONE',  ( 2.765492612253204641, 1.039303555060458351, 1.640259502831205918 ) ) ;
#124640=CARTESIAN_POINT ( 'NONE',  ( 5.484674493353773883, -1.343714522216314489, 1.640574901390474460 ) ) ;
#124642=CARTESIAN_POINT ( 'NONE',  ( 3.305314717767214638, 1.277042846462652204, -1.560500556308255238 ) ) ;
#124646=CARTESIAN_POINT ( 'NONE',  ( 1.453431991042982041, 0.5316948868413253759, -1.746555546766684675 ) ) ;
#124651=CARTESIAN_POINT ( 'NONE',  ( 5.506733764336206427, 1.562011470896901288, -1.344504574768749627 ) ) ;
#124656=CARTESIAN_POINT ( 'NONE',  ( 4.231121231147261241, 1.847467856137770204, 0.8164654241873505747 ) ) ;
#124657=CARTESIAN_POINT ( 'NONE',  ( 5.813180279319686505, 1.817354232980341378, -1.277000798603223464 ) ) ;
#124661=CARTESIAN_POINT ( 'NONE',  ( 4.715729953790866347, -2.021515393979388175, 0.4000037541747498704 ) ) ;
#124662=CARTESIAN_POINT ( 'NONE',  ( 3.445935549842124690, -1.779626424299302956, -0.9480406757386842242 ) ) ;
#124669=CARTESIAN_POINT ( 'NONE',  ( 3.497422563753574298, 1.966343570655813666, 0.4444343670074250574 ) ) ;
#124670=CARTESIAN_POINT ( 'NONE',  ( 2.185277780439310202, -0.7877041259056734024, 1.664256631099890971 ) ) ;
#124671=CARTESIAN_POINT ( 'NONE',  ( 0.9444605492630732124, 0.9306326543588975264, -2.111904739147156818 ) ) ;
#124673=CARTESIAN_POINT ( 'NONE',  ( 3.954491917119377753, 0.7739500986865335275, 2.018479124525011770 ) ) ;
#124676=VERTEX_POINT ( 'NONE', #130820 ) ;
#124678=CARTESIAN_POINT ( 'NONE',  ( 1.850267049257280139, 0.5840378008528935849, 1.777222254475477659 ) ) ;
#124679=CARTESIAN_POINT ( 'NONE',  ( 6.192255011402767018, -1.961924197356275323, -0.1938383548326528261 ) ) ;
#124683=CARTESIAN_POINT ( 'NONE',  ( 0.06543086261080394150, -1.973449318085427340, -0.9880335165917543128 ) ) ;
#124687=FACE_OUTER_BOUND ( 'NONE', #98463, .T. ) ;
#124688=CARTESIAN_POINT ( 'NONE',  ( 5.823112234018508637, -0.04902082458170010926, 1.971020750367402430 ) ) ;
#124689=CARTESIAN_POINT ( 'NONE',  ( 5.285860113471884780, 1.546311580504238670, 1.713158476844111933 ) ) ;
#124690=CARTESIAN_POINT ( 'NONE',  ( 6.355886303346764521, -0.6260325832568144344, 1.752714347800623518 ) ) ;
#124691=CARTESIAN_POINT ( 'NONE',  ( 2.729405006034294257, 0.1058063225414084541, -2.059999219628326994 ) ) ;
#124698=CARTESIAN_POINT ( 'NONE',  ( 5.318865801915546143, -1.576246948875639209, 1.493384065191505350 ) ) ;
#124700=CARTESIAN_POINT ( 'NONE',  ( 3.720104550828434942, 1.749555917645674530, 0.5740644926693627692 ) ) ;
#124703=CARTESIAN_POINT ( 'NONE',  ( 6.409741707328596938, -1.031184584194230647, -1.933826218581576439 ) ) ;
#124705=CARTESIAN_POINT ( 'NONE',  ( 6.684454173705361768, -2.217265373380904681, -0.4495064082850850906 ) ) ;
#124711=CARTESIAN_POINT ( 'NONE',  ( 0.3558548230270657808, 0.6711484630133063289, 1.637870061858819559 ) ) ;
#124712=CARTESIAN_POINT ( 'NONE',  ( 4.899092244908956673, -0.2488113327579875855, -1.997608342807774218 ) ) ;
#124715=CARTESIAN_POINT ( 'NONE',  ( 4.436618261691759102, 2.064837277596673903, 0.4132364508900014943 ) ) ;
#124717=CARTESIAN_POINT ( 'NONE',  ( 3.233901216830310954, 1.915793140838128572, -0.003097617167701141160 ) ) ;
#124719=CARTESIAN_POINT ( 'NONE',  ( 3.736728436007582310, -1.897426337869069668, -0.5277852043128227200 ) ) ;
#124720=CARTESIAN_POINT ( 'NONE',  ( 5.906511930418064438, -2.010445946205151380, -0.1936997237232794822 ) ) ;
#124721=CARTESIAN_POINT ( 'NONE',  ( 2.289737743334671283, -0.8020533187339595749, 1.690132462187944107 ) ) ;
#124722=CARTESIAN_POINT ( 'NONE',  ( 5.145002536317147879, -1.476695180717332967, 0.8911356905443221788 ) ) ;
#124723=CARTESIAN_POINT ( 'NONE',  ( 0.9141475326900462273, -1.912571728325639153, 0.002704284578637640348 ) ) ;
#124724=CARTESIAN_POINT ( 'NONE',  ( 2.280145854635793334, 1.358931147977986420, 1.738775483816151768 ) ) ;
#124729=CARTESIAN_POINT ( 'NONE',  ( 6.689906388054261299, -1.280585065398877731, -1.486383542710856043 ) ) ;
#124735=ORIENTED_EDGE ( 'NONE', *, *, #185954, .F. ) ;
#124736=CARTESIAN_POINT ( 'NONE',  ( 2.559107912120599071, 1.664280205102614429, -1.231313097332722872 ) ) ;
#124740=CARTESIAN_POINT ( 'NONE',  ( 6.498696114369957755, -2.079444522786470184, -0.4142970760486197612 ) ) ;
#124745=CARTESIAN_POINT ( 'NONE',  ( 5.641953822799152363, -0.04667112846407085736, -2.015725140939367499 ) ) ;
#124746=CARTESIAN_POINT ( 'NONE',  ( 5.102711585370895975, 1.772601733252886280, 0.7270577078305997532 ) ) ;
#124747=CARTESIAN_POINT ( 'NONE',  ( 6.539320575229236709, 1.252639605590207150, 2.218328189723097754 ) ) ;
#124748=CARTESIAN_POINT ( 'NONE',  ( 3.087623348389135547, -0.8860277256741244667, 2.004638750299721828 ) ) ;
#124751=CARTESIAN_POINT ( 'NONE',  ( 5.906499476128409754, -2.003886227978883383, -0.1931989457738275962 ) ) ;
#124752=CARTESIAN_POINT ( 'NONE',  ( 2.267699027020404490, 0.5063876334258295975, -1.844086191983687284 ) ) ;
#124755=CARTESIAN_POINT ( 'NONE',  ( 6.538674910786447469, -1.636584463124007627, 1.342808005693174156 ) ) ;
#124757=CARTESIAN_POINT ( 'NONE',  ( 3.913685052542864362, -1.076426932671892711, -1.792217407939109552 ) ) ;
#124759=CARTESIAN_POINT ( 'NONE',  ( 2.467434050970338077, 1.692020480068063826, -0.3335236308374764369 ) ) ;
#124761=CARTESIAN_POINT ( 'NONE',  ( 6.363548717301088509, -1.704009271243651868, -1.262090224194649446 ) ) ;
#124770=CARTESIAN_POINT ( 'NONE',  ( 2.455456329753392897, -1.343237331403211776, -1.215579648594692808 ) ) ;
#124774=CARTESIAN_POINT ( 'NONE',  ( 3.545387212860445114, -1.672524232984048620, 0.6962571228125400413 ) ) ;
#124778=CARTESIAN_POINT ( 'NONE',  ( 3.824516763807362274, -1.251359258362509497, 1.377693585838150936 ) ) ;
#124780=CARTESIAN_POINT ( 'NONE',  ( 2.003404541029256691, -1.857510701737439929, 0.4675905980212178292 ) ) ;
#124781=CARTESIAN_POINT ( 'NONE',  ( 0.6041866639863550104, -0.6101368697832668664, -1.720745249832649870 ) ) ;
#124789=CARTESIAN_POINT ( 'NONE',  ( 6.069198383140281372, 1.735254367832469891, 0.9315073086425088578 ) ) ;
#124792=CARTESIAN_POINT ( 'NONE',  ( 0.4102503234837206469, 1.440240287209685111, -1.515647972008065780 ) ) ;
#124793=CARTESIAN_POINT ( 'NONE',  ( 0.1471128783409255958, -1.407412912164500263, -1.162481699956314785 ) ) ;
#124795=CARTESIAN_POINT ( 'NONE',  ( 1.395219695971817941, 1.379742824092672349, 1.195523663710513995 ) ) ;
#124796=CARTESIAN_POINT ( 'NONE',  ( 1.911028901235469535, 1.633884665098099598, -1.483674895440662667 ) ) ;
#124798=CARTESIAN_POINT ( 'NONE',  ( 1.230557176020010912, 1.282188879665364656, -1.419081615486268433 ) ) ;
#124799=( BOUNDED_SURFACE ( )  B_SPLINE_SURFACE ( 3, 3, ( 
 ( #77905, #28094, #179690, #113686, #95257, #208954, #126747, #162377, #161307, #80038, #144026, #176484, #128878, #94190, #192706, #212156, #146142, #96322, #44362, #160230, #196991, #114743, #210021, #31307, #60589, #11828, #16083, #213223, #97384, #164498, #63791, #64853, #61664, #78969, #145089, #129949, #15021, #211093, #32368, #195937, #62716, #127832, #81111, #131000, #48627, #112614, #180741, #98432, #45432, #178626, #82166, #111547, #110485, #177556, #194859, #30237, #29166, #46492, #151461, #150394, #119014, #167696, #184993, #100561, #19297, #136281, #166632, #51828, #3033, #49678, #17154, #52878, #117946, #183939, #101630, #85379, #181791, #69103, #199097, #182871, #36618, #202301, #21417, #200175, #20365, #84309, #116870, #53953, #201237, #86451, #35551, #133099, #135225, #37702, #102704, #149313, #168761, #148260, #99503, #33426, #152516, #165560, #1963, #68026, #4100, #134165, #50743, #70170, #34487, #120091, #186066, #893, #65892, #83229, #214260, #66960, #18225, #103779, #169830, #132038, #115803, #198049, #153591, #173051, #206589, #137353, #204436, #8389, #41996, #190335, #59277, #39842, #205518, #55022, #105949, #73384, #7308, #171973, #124377, #174132, #72310, #108103, #88599, #57151, #155724, #87526, #139490, #23564, #154656, #89673, #207658, #6239, #138416, #123317, #189280, #121172, #56089, #58218, #122246, #40919, #107025, #125434, #104851, #188205, #25705, #203369, #170896, #187140, #24632, #38769, #90739, #191398, #74471, #156802, #140578, #22488, #43063, #5162, #109176, #91813, #157872, #9465, #75536, #141647, #175189, #71237, #112371, #163197, #28924, #77663, #78722, #95009, #26775, #161056, #111307, #27851, #193550, #146961, #93948, #143784, #45193, #177309, #60342, #159988, #211916, #61418, #144849, #12651, #64617, #44119, #127582, #179446, #142705, #110240, #126502, #210855, #208715, #62481, #130756, #162131, #128645, #194609, #192467, #212976, #92878, #196750, #176249, #29992, #46253, #178382, #96078, #13719, #209779, #79793, #14780, #145906, #63552, #129708, #195690, #47326, #80872, #113440, #31067, #97144, #11590, #48391, #114505, #158923, #10520, #76594, #199926, #214022, #51571, #16902, #635, #68848, #20105, #53692, #17966, #52623, #116620, #149057, #86192, #19041, #118751, #84053, #165308, #167447, #69909, #183688, #181550, #35294, #180501, #131794, #65645, #184734, #197800, #182613, #34235, #117696, #100308, #82983, #85119, #66699, #2777, #133919, #33179, #98202, #49434, #32118, #115554, #132846, #198850, #50497, #166375, #81926, #101369, #164252, #151206, #134967, #15839, #150141, #200976, #36361, #102437, #152262, #1713, #67767, #148012, #168506, #3836, #136019, #202032, #99260, #209246, #104590, #77136, #120907, #23302, #139221, #153324, #205251, #170634, #154397, #11056, #176777, #210327, #171703, #60890, #55823, #88333, #28393, #172794, #127050, #89412, #22220, #106766, #12131, #123068, #186879, #189022, #119824, #70977, #4899, #193010, #137087, #121979, #187944, #56894, #39573, #5976, #27316, #72047, #159457, #73121, #38512, #37437, #203115, #185804, #54758, #138159, #204167, #105676, #155461, #21156, #40664, #103514, #93420, #143257, #169573, #7045, #44664, #110777, #94488, #160526, #78203, #144328, #87260, #80340, #47874, #196232, #146440, #98731, #148550, #46802, #16381, #63021 ),
 ( #212453, #95559, #129189, #32653, #96621, #113986, #179982, #99791, #79277, #162675, #116, #177856, #145394, #161610, #31603, #29468, #64098, #165858, #197277, #14245, #130239, #13200, #182083, #128121, #33714, #211392, #65132, #97679, #163737, #15318, #81406, #112915, #147489, #198333, #213511, #178926, #131290, #48917, #115038, #49973, #181037, #164789, #82460, #195167, #30541, #66182, #132328, #116092, #17443, #83526, #149609, #61965, #194081, #45734, #111852, #36908, #1191, #88891, #4383, #3323, #186356, #20646, #37992, #51042, #135500, #102990, #199396, #55310, #104064, #35843, #87808, #117165, #170110, #137640, #19593, #84602, #101922, #136570, #22774, #67255, #133390, #183169, #34773, #54243, #86735, #203659, #171184, #169048, #153881, #21697, #39058, #120381, #152804, #5450, #70455, #201523, #202591, #105144, #71529, #85666, #53171, #121459, #68328, #151752, #100845, #119299, #187429, #166931, #18524, #69393, #150690, #118236, #2252, #167988, #134459, #185285, #200463, #52110, #184221, #27056, #207941, #124661, #57440, #156012, #123601, #40130, #28137, #44405, #23853, #188498, #125722, #59562, #41211, #154945, #72607, #108390, #107318, #174414, #89961, #122537, #74759, #106240, #138707, #158153, #92099, #42276, #204723, #172266, #142996, #60630, #7599, #191682, #6529, #73684, #176525, #93163, #43343, #110525, #9746, #159200, #139782, #173342, #24922, #75820, #109463, #91027, #192748, #25991, #8677, #205809, #141928, #175470, #10801, #58506, #76875, #208994, #189566, #126793, #56374, #157088, #140861, #206875, #190618, #49714, #31350, #32405, #29210, #112657, #46536, #163478, #64892, #178666, #132077, #113727, #162418, #193823, #97425, #15060, #98471, #212196, #48665, #195980, #12930, #63834, #115843, #145127, #181829, #210065, #96364, #129992, #94232, #160270, #81152, #13995, #131039, #179731, #197028, #144070, #80080, #47613, #77949, #148299, #114782, #128917, #180779, #61705, #164536, #16122, #30278, #177598, #194898, #147237, #11872, #127873, #45472, #111588, #95300, #213265, #82205, #214296, #161349, #65929, #198087, #79011, #211133, #62757, #146181, #70203, #52912, #167733, #102740, #71272, #103811, #117983, #19334, #169860, #100596, #183975, #66998, #85413, #135258, #99538, #21449, #35586, #136316, #150433, #137386, #200209, #202335, #51861, #201272, #119045, #101665, #120125, #86483, #3066, #1998, #34524, #68063, #133136, #121206, #203401, #116908, #199135, #4135, #152548, #134199, #33462, #165600, #185029, #151497, #36654, #182908, #931, #69136, #50780, #17190, #168795, #20402, #53986, #83265, #166672, #87557, #153625, #18262, #186103, #37735, #84345, #5197, #55055, #149352, #188238, #190368, #187175, #138449, #72345, #191432, #204469, #189316, #40954, #124410, #107062, #172009, #25739, #155759, #9500, #140612, #39878, #104884, #56122, #38803, #6274, #73423, #23601, #139524, #89708, #88633, #58254, #170927, #42028, #91849, #22524, #7344, #108139, #141681, #75572, #158957, #205550, #90774, #154691, #57189, #173087, #24667, #123349, #207694, #59314, #156835, #125471, #105989, #8422, #74507, #122280, #206624, #174166, #157906, #43099, #92911, #109213, #175224, #26809, #10552, #76626, #142741, #208748, #60375, #178414, #46286, #164284, #143816, #161089, #64646, #27883, #209813, #160022, #30023, #93980, #128675 ),
 ( #14811, #15872, #31102, #63583, #163229, #145936, #112403, #195723, #81957, #196780, #210885, #96109, #48422, #193580, #62510, #11621, #162164, #13752, #192500, #114535, #194644, #80902, #28955, #148042, #78755, #146993, #144879, #79826, #211948, #129740, #213010, #179479, #47359, #95040, #130786, #113473, #97175, #180529, #214050, #32151, #98229, #126538, #44151, #45223, #110272, #77695, #176281, #61448, #127615, #111338, #177343, #12679, #182647, #103547, #18000, #168542, #84090, #19076, #151240, #150177, #152297, #118786, #35327, #34268, #66736, #100341, #165339, #153362, #169608, #149089, #99292, #36398, #184772, #166406, #65678, #197834, #85157, #1745, #2809, #669, #33208, #199959, #16933, #49467, #68880, #135000, #167480, #115585, #83015, #53728, #185838, #132879, #102476, #131825, #198881, #87293, #3870, #20139, #21190, #201011, #69943, #50527, #67802, #133951, #52657, #86225, #51605, #181579, #136055, #117730, #116650, #202068, #119860, #37470, #183719, #101407, #106798, #138194, #123101, #26549, #55858, #92657, #120943, #7080, #40695, #4933, #71009, #8169, #73153, #190116, #24398, #41770, #54795, #139259, #172826, #203151, #59053, #107883, #39608, #91591, #186915, #173910, #141428, #23336, #88368, #105711, #140347, #137122, #38546, #104623, #170671, #22258, #57992, #90510, #207434, #174967, #156575, #157643, #25485, #42840, #124155, #74253, #72083, #122014, #89446, #155497, #154434, #204204, #9240, #171739, #56928, #205290, #108947, #6014, #189058, #75312, #187982, #206366, #125211, #191173, #60122, #160833, #196532, #79574, #44969, #94784, #43901, #64396, #10297, #130540, #126281, #161912, #111077, #62262, #12424, #28698, #209550, #29772, #80651, #78504, #61194, #210636, #177082, #95856, #146742, #144622, #128423, #13502, #192239, #27620, #63327, #194390, #46032, #112154, #178157, #110015, #145693, #127353, #193322, #47102, #212761, #31908, #211692, #30847, #129488, #195470, #48174, #113217, #96925, #179222, #143556, #162975, #114287, #14554, #159760, #180284, #158699, #176028, #93721, #76371, #11359, #142478, #208486, #77439, #100090, #82767, #150988, #66485, #134750, #51347, #99036, #15619, #197579, #164044, #131578, #198631, #148841, #50279, #413, #213807, #183463, #81709, #35069, #2553, #147790, #132625, #18814, #52408, #200759, #69696, #116398, #1487, #65428, #182386, #83826, #17737, #34016, #118535, #184518, #166151, #36139, #165092, #67552, #149919, #97985, #133696, #199701, #16683, #117471, #3617, #101140, #102222, #167228, #84901, #68628, #49223, #168292, #19888, #85973, #152048, #135799, #201823, #53468, #119605, #185590, #115342, #181334, #32961, #155247, #24151, #123901, #7904, #71827, #189870, #20940, #206111, #173656, #55605, #120686, #137937, #172569, #58807, #37219, #124961, #87035, #103293, #90254, #56679, #25230, #207183, #205034, #41512, #140086, #75060, #156321, #188806, #73993, #122844, #171488, #106543, #141172, #107625, #121760, #23079, #91333, #104366, #187727, #70756, #89195, #139011, #169354, #157391, #39356, #57743, #154181, #153108, #203958, #8985, #105452, #40442, #4682, #6828, #136869, #202894, #72907, #5749, #38289, #54539, #186662, #170411, #22000, #88111, #10048, #161659, #29517, #77181, #190923, #108692, #144377, #143303, #210376, #126022, #158447, #110822, #76123, #174720, #194134 ),
 ( #129242, #95610, #146488, #128172, #195215, #191984, #209294, #60942, #45784, #13254, #127098, #14297, #62017, #44715, #142226, #111901, #177904, #46851, #94534, #145442, #193062, #79327, #178977, #176829, #160573, #211442, #92408, #59871, #63074, #12181, #78253, #112965, #30591, #208239, #96676, #27368, #11105, #162726, #80392, #64149, #28442, #212508, #42587, #159507, #26293, #43650, #109766, #175774, #93468, #120155, #22558, #136345, #131336, #202367, #130291, #81461, #15368, #137413, #147539, #132381, #198382, #70233, #50023, #115089, #186131, #98785, #169887, #83579, #197330, #47927, #213560, #196280, #163789, #16432, #181085, #82510, #32703, #31655, #4163, #114040, #54016, #37766, #180033, #164840, #103838, #87585, #21476, #104917, #148597, #33765, #97731, #166, #116147, #182135, #66233, #153657, #5226, #99843, #71300, #48972, #165908, #17492, #65182, #152576, #203432, #55086, #121235, #38834, #187205, #170958, #88663, #154723, #6306, #139556, #74540, #10583, #175253, #176311, #110303, #89742, #107096, #76657, #188270, #155791, #106020, #124441, #39911, #140640, #27915, #207723, #173119, #8452, #172041, #192529, #138479, #44183, #23634, #75602, #24700, #190399, #206653, #156866, #123380, #157936, #208778, #58285, #189345, #42057, #9529, #108170, #57220, #125501, #40985, #109245, #25769, #73454, #204501, #7375, #56151, #205583, #90802, #174196, #91881, #141713, #59347, #191464, #122313, #43129, #26839, #92942, #158987, #142772, #60408, #126569, #94011, #160050, #72380, #193609, #30053, #211975, #145965, #96143, #48453, #98256, #210914, #180558, #12709, #129770, #79856, #11654, #63615, #162194, #78785, #178445, #131855, #144907, #62541, #13781, #195753, #45251, #128703, #47390, #164313, #114566, #115615, #49494, #28987, #46316, #15904, #127645, #95073, #111369, #113503, #177373, #179511, #181610, #147021, #112432, #31131, #161122, #197862, #77727, #33239, #194672, #14840, #97206, #163258, #80930, #213044, #64673, #130819, #148074, #196810, #32180, #81986, #214080, #65707, #99322, #143849, #209841, #61480, #66767, #34300, #69976, #135032, #201045, #118817, #184804, #198913, #36433, #1780, #199991, #53764, #4967, #38581, #2843, #37507, #101438, #133983, #71045, #3906, #103583, #68912, #150208, #152328, #54831, #168571, #166443, #20171, #165372, #116680, #50559, #169641, #182679, #167512, #19109, #136087, #51639, #16965, #83046, #102509, #117763, #86258, #100373, #132908, #85187, #18035, #149121, #202104, #119897, #52688, #703, #84122, #153396, #137161, #67837, #185871, #183753, #35363, #186949, #21224, #87329, #120981, #203185, #151270, #122050, #73190, #7117, #140380, #41807, #139296, #125248, #8201, #56962, #72120, #206400, #58025, #9275, #106834, #173945, #24436, #39642, #172865, #108980, #171777, #174999, #154471, #123137, #90547, #104657, #170705, #124189, #189095, #25518, #74286, #91626, #6049, #157677, #156611, #190152, #75346, #141462, #205325, #207469, #138228, #59088, #191208, #40728, #188014, #107920, #42872, #22290, #88403, #204241, #105750, #55893, #23373, #89483, #155538, #39273, #37130, #21916, #186583, #121680, #202813, #20858, #120605, #103210, #3539, #153025, #187645, #154096, #168207, #69611, #5666, #150907, #19806, #117387, #135718, #185507, #149837, #71745, #85890, #38211, #200676, #105367, #36058 ),
 ( #183383, #171404, #83743, #167148, #34989, #54462, #2468, #201743, #1406, #134673, #67467, #199617, #151967, #119519, #133613, #51262, #86958, #53384, #104284, #169272, #170330, #101059, #88025, #4600, #70674, #137860, #203881, #118454, #55525, #18735, #84818, #68544, #102139, #52325, #184441, #136784, #44628, #22995, #110745, #72826, #89112, #76043, #42501, #159422, #192976, #190841, #175689, #125948, #60854, #142145, #174636, #59789, #108609, #157308, #92331, #127017, #93386, #107543, #8898, #11022, #90180, #173577, #56598, #74979, #124876, #155166, #77097, #25146, #191904, #140006, #6750, #189783, #43566, #41434, #26213, #158373, #91248, #109686, #208159, #207097, #206028, #24075, #57664, #122761, #138929, #204947, #106462, #188721, #27279, #143224, #123822, #40359, #172487, #9965, #141087, #209214, #156243, #7820, #58726, #73913, #160491, #179945, #113949, #64058, #12098, #210289, #164750, #82422, #45698, #81369, #28357, #61929, #198293, #114997, #147449, #132288, #31568, #180994, #111813, #195127, #129151, #97643, #213473, #46765, #78, #196195, #30505, #128088, #163700, #15283, #32615, #80304, #131253, #130201, #49935, #47838, #98693, #65096, #66143, #197240, #48879, #16341, #148511, #96586, #176743, #94452, #78166, #112876, #162635, #144296, #29434, #178890, #194046, #14209, #177818, #95525, #161575, #146402, #13162, #79239, #145358, #212416, #211358, #62983, #25919, #187358, #38988, #40060, #72534, #158084, #157018, #190548, #7528, #88817, #90953, #207867, #107250, #105073, #173271, #103994, #55238, #203586, #108321, #121385, #106170, #172196, #41140, #23785, #154874, #8604, #138632, #140788, #57368, #171112, #21624, #22704, #170038, #137569, #204655, #6457, #56304, #122466, #5377, #189496, #87732, #24851, #74687, #153806, #188425, #206802, #58435, #124588, #75749, #89891, #73611, #71456, #155942, #139710, #205734, #123531, #42204, #174341, #92027, #9672, #141859, #59491, #125648, #191610, #111515, #127797, #44330, #209989, #163409, #110452, #94158, #61631, #193752, #76801, #176453, #45399, #195904, #146109, #147166, #81079, #60557, #77875, #47540, #159130, #126716, #142922, #95221, #10731, #177521, #213193, #178592, #143997, #29133, #208922, #14985, #109392, #64820, #161271, #12857, #160197, #128841, #179657, #78932, #11800, #145054, #211057, #194822, #31277, #62682, #46458, #112580, #192676, #28065, #162341, #30201, #96289, #13924, #80004, #212120, #63758, #129918, #113653, #97352, #130966, #43272, #175397, #26982, #93089, #165528, #36585, #35519, #69070, #100528, #181757, #183908, #86418, #200143, #198017, #51797, #196958, #148227, #82135, #201206, #214229, #199066, #50712, #134136, #116838, #33391, #101596, #17120, #19265, #150364, #49645, #114714, #65857, #48596, #16051, #83197, #99469, #149279, #860, #98400, #67994, #180709, #117915, #167664, #32332, #66926, #85347, #151428, #3001, #168730, #133068, #166603, #164465, #182839, #34456, #18192, #84277, #135190, #52845, #1934, #118980, #115768, #184959, #102672, #132007, #20332, #152485, #4067, #70137, #41957, #203336, #187104, #154626, #72275, #169795, #54989, #138384, #74440, #24599, #25670, #174097, #153558, #170866, #140542, #37668, #5129, #21384, #188174, #103744, #204402, #91777, #57119, #22456, #56055, #87493, #108069, #202269, #157834, #71204, #139453 ),
 ( #90708, #9431, #40888, #73350, #173018, #155690, #122212, #205485, #136249, #206556, #6206, #39808, #58184, #121141, #105914, #137320, #171939, #23530, #53920, #124342, #89638, #156770, #38738, #120057, #88568, #8356, #7273, #104820, #123286, #186032, #189249, #106993, #190300, #192429, #76557, #44084, #175154, #163160, #179413, #158887, #109141, #46221, #128608, #176213, #75501, #207621, #28890, #27815, #94974, #10483, #43029, #209744, #26740, #59238, #78688, #12615, #177274, #125397, #92843, #63521, #195658, #142667, #194575, #141612, #208678, #97108, #13686, #112338, #31034, #144813, #79756, #60307, #93912, #159953, #210820, #178350, #11557, #113407, #161020, #143749, #126466, #62445, #29958, #145872, #193516, #96044, #162097, #110203, #45157, #191362, #77627, #61386, #127545, #111271, #211880, #129673, #47292, #17927, #16867, #199886, #34195, #51531, #64581, #117656, #132809, #1674, #101329, #183649, #49399, #167410, #212944, #35253, #151167, #33142, #98169, #115518, #150102, #36321, #14745, #146927, #182573, #181513, #100270, #164217, #196713, #149021, #48354, #130722, #84011, #166335, #116578, #114465, #180465, #2738, #134931, #15804, #133879, #80837, #32081, #102399, #19002, #85083, #184700, #67728, #68809, #81890, #99222, #165272, #200936, #52584, #82947, #118712, #147976, #596, #213986, #65606, #131756, #197761, #198813, #66662, #50459, #87220, #72008, #190049, #4860, #41701, #69870, #170595, #204130, #168467, #20065, #171665, #22181, #139184, #187906, #205214, #3796, #56856, #138121, #155422, #40625, #123030, #203075, #106728, #152225, #188981, #90438, #186842, #37397, #54719, #89373, #86154, #135979, #201994, #53652, #119784, #7006, #39536, #156506, #124086, #121940, #172755, #24330, #206296, #73083, #105637, #8095, #23261, #88297, #74184, #57921, #140277, #38474, #154358, #185765, #21114, #104551, #103472, #5937, #55783, #169534, #153284, #70939, #137049, #120868, #148516, #62986, #213477, #129155, #29438, #125148, #82, #130206, #163705, #80307, #13165, #108880, #79243, #207371, #198298, #66147, #191105, #141357, #81372, #15287, #211361, #107811, #196199, #147455, #157577, #145362, #31571, #65101, #131257, #82426, #195131, #14212, #75245, #46768, #96589, #30508, #112882, #197244, #48883, #95529, #115002, #177821, #146407, #178894, #173836, #162638, #212420, #161578, #64061, #16345, #47841, #113952, #179948, #97646, #58991, #181000, #32620, #98697, #164756, #132292, #25413, #42773, #91518, #9170, #165824, #67221, #83492, #101888, #17408, #52074, #87769, #185250, #150654, #200428, #149574, #170076, #116060, #21663, #1158, #53134, #2217, #167953, #118201, #134425, #100811, #135466, #186322, #184189, #166896, #19557, #68292, #201488, #37957, #35811, #85633, #119265, #133356, #199363, #169015, #151719, #3290, #69358, #36874, #51009, #102956, #18488, #84566, #152770, #117130, #104030, #183132, #34738, #20613, #86701, #153845, #4351, #136537, #70419, #202556, #54208, #5416, #120346, #71495, #137606, #49939, #182050, #33680, #99755, #154911, #205773, #57401, #140826, #123566, #188462, #42241, #172232, #25956, #157053, #204690, #121422, #88856, #55273, #22738, #89925, #40093, #155976, #106206, #105107, #74721, #187392, #173306, #23820, #56340, #7563, #6495, #76839, #93126, #72570, #138670, #174376, #108354, #73649 ),
 ( #206838, #90990, #39024, #122501, #191643, #109427, #139748, #92061, #171147, #189529, #10764, #141893, #158119, #159165, #58471, #207904, #41177, #107284, #24885, #124626, #9710, #8642, #27018, #190584, #75786, #59525, #125685, #43308, #175433, #203622, #97388, #30241, #61667, #46495, #164502, #193787, #16086, #44366, #145092, #178629, #142958, #208960, #146145, #211096, #113691, #162380, #179694, #192711, #31310, #112619, #129953, #15024, #163444, #177559, #81115, #126751, #147201, #64858, #161310, #11833, #29171, #63795, #60593, #110489, #176488, #28099, #94194, #195941, #13958, #131003, #98437, #96325, #213226, #196995, #180745, #47577, #80042, #48630, #212160, #62720, #114747, #32372, #160234, #12893, #128881, #77911, #210026, #78972, #144030, #194862, #127835, #45436, #111550, #95261, #184998, #199101, #120094, #34490, #36623, #100565, #896, #99506, #186071, #101634, #135228, #166637, #66964, #165563, #37706, #167700, #201241, #51831, #50746, #83232, #116875, #181796, #169833, #103782, #17158, #115808, #52882, #119017, #182874, #82170, #214263, #35554, #18229, #19302, #149317, #49681, #1966, #33429, #65896, #85382, #151466, #183944, #132042, #133103, #70173, #202305, #84313, #102707, #148264, #150398, #198052, #20370, #168765, #68030, #3037, #86455, #134170, #200178, #117949, #69106, #152519, #4104, #136285, #53956, #89678, #121175, #24636, #90745, #25709, #139494, #190338, #123321, #154659, #205522, #43067, #72314, #109180, #137357, #23570, #57156, #21420, #87529, #156806, #155728, #206593, #40926, #58222, #71241, #124380, #189284, #8393, #108108, #42000, #56093, #174135, #5167, #91817, #157875, #39847, #104854, #122249, #74475, #153596, #203374, #55026, #187144, #38773, #140582, #107030, #9468, #191401, #173056, #75540, #141650, #59280, #207661, #125440, #170899, #22491, #7312, #88603, #6245, #138419, #105954, #73391, #204439, #188208, #171978, #208719, #161061, #62484, #26778, #31071, #177313, #63555, #77667, #212980, #127586, #129711, #144852, #210858, #128648, #194613, #60345, #46256, #11593, #209782, #195694, #126506, #97147, #44122, #110244, #111310, #143787, #14783, #13723, #47330, #78725, #159992, #162135, #64620, #178385, #176253, #29996, #175192, #192470, #27854, #179450, #93951, #28927, #95012, #112374, #12654, #61421, #79796, #193554, #211920, #96081, #45196, #92882, #145909, #158927, #113444, #163200, #80875, #146965, #130759, #76597, #196755, #10523, #48395, #142710, #164255, #16906, #35297, #68851, #2780, #86195, #66702, #17970, #81929, #132849, #100311, #34239, #198853, #151209, #200979, #99263, #134971, #115557, #84057, #182616, #114508, #166378, #50501, #181554, #116623, #20108, #33182, #165311, #150144, #1716, #148015, #82986, #67771, #52626, #118754, #3839, #152266, #131797, #149061, #184738, #15843, #197803, #214026, #133922, #65650, #199929, #69912, #101374, #638, #51575, #49438, #136022, #180504, #202035, #117700, #183691, #167449, #19044, #85123, #36366, #102441, #168509, #32122, #98205, #104593, #105679, #5980, #139224, #41742, #72051, #171707, #56897, #169576, #137091, #172798, #87263, #154401, #38515, #138162, #170638, #21159, #205255, #119828, #123072, #24369, #103517, #22223, #189026, #8138, #156546, #25453, #204170, #23305, #153328, #55826, #39576, #187948, #121982, #90481, #140318, #88337 ) ),
 .UNSPECIFIED., .T., .F., .F. ) 
 B_SPLINE_SURFACE_WITH_KNOTS ( ( 4, 3, 4 ),
 ( 4, 1, 1, 1, 1, 1, 1, 1, 1, 1, 1, 1, 1, 1, 1, 1, 1, 1, 1, 1, 1, 1, 1, 1, 1, 1, 1, 1, 1, 1, 1, 1, 1, 1, 1, 1, 1, 1, 1, 1, 1, 1, 1, 1, 1, 1, 1, 1, 1, 1, 1, 1, 1, 1, 1, 1, 1, 1, 1, 1, 1, 1, 1, 1, 1, 1, 1, 1, 1, 1, 1, 1, 1, 1, 1, 1, 1, 1, 1, 1, 1, 1, 1, 1, 1, 1, 1, 1, 1, 1, 1, 1, 1, 1, 1, 1, 1, 1, 1, 1, 1, 1, 1, 1, 1, 1, 1, 1, 1, 1, 1, 1, 1, 1, 1, 1, 1, 1, 1, 1, 1, 1, 1, 1, 1, 1, 1, 1, 1, 1, 1, 1, 1, 1, 1, 1, 1, 1, 1, 1, 1, 1, 1, 1, 1, 1, 1, 1, 1, 1, 1, 1, 1, 1, 1, 1, 1, 1, 1, 1, 1, 1, 1, 1, 1, 1, 1, 1, 1, 1, 1, 1, 1, 1, 1, 1, 1, 1, 1, 1, 1, 1, 1, 1, 1, 1, 1, 1, 1, 1, 1, 1, 1, 1, 1, 1, 1, 1, 1, 1, 1, 1, 1, 1, 1, 1, 1, 1, 1, 1, 1, 1, 1, 1, 1, 1, 1, 1, 1, 1, 1, 1, 1, 1, 1, 1, 1, 1, 1, 1, 1, 1, 1, 1, 1, 1, 1, 1, 1, 1, 1, 1, 1, 1, 1, 1, 1, 1, 1, 1, 1, 1, 1, 1, 1, 1, 1, 1, 1, 1, 1, 1, 1, 1, 1, 1, 1, 1, 1, 1, 1, 1, 1, 1, 1, 1, 1, 1, 1, 1, 1, 1, 1, 1, 1, 1, 1, 1, 1, 1, 1, 1, 1, 1, 1, 1, 1, 1, 1, 1, 1, 1, 1, 1, 1, 1, 1, 1, 1, 1, 1, 1, 1, 1, 1, 1, 1, 1, 1, 1, 1, 1, 1, 1, 1, 1, 1, 1, 1, 1, 1, 1, 1, 1, 1, 1, 1, 1, 1, 1, 1, 1, 1, 1, 1, 1, 1, 1, 1, 1, 1, 1, 1, 1, 1, 1, 1, 1, 1, 1, 1, 1, 1, 1, 1, 1, 1, 1, 1, 1, 1, 1, 1, 1, 1, 1, 1, 1, 1, 1, 1, 1, 1, 1, 4 ),
 ( 0.000000000000000000, 0.5000000000000000000, 1.000000000000000000 ),
 ( 0.000000000000000000, 0.002599909708945224215, 0.005208776875251038344, 0.007813105021672143990, 0.01041684075506122895, 0.01302033053878596733, 0.01562516449037322508, 0.01822901888718816976, 0.02083333248856494152, 0.02343767784666880849, 0.02604151204071371642, 0.02864616705684025488, 0.03124974664057501156, 0.03385445107693609706, 0.03645811663825353210, 0.03906264587105176544, 0.04166673705245293319, 0.04427082116499847508, 0.04687535697974040683, 0.04947901875943551409, 0.05208372524935509645, 0.05468730636643894666, 0.05729195276349181160, 0.05989578571700067411, 0.06250012971910297310, 0.06510448174046053194, 0.06770830932160050442, 0.07031296016926287529, 0.07291653972921435800, 0.07552124384959360559, 0.07812490789241745281, 0.08072943556986492131, 0.08333352577934262373, 0.08593760861062926804, 0.08854214333088818167, 0.09114580385899402615, 0.09375050919907033931, 0.09635408915385039463, 0.09895873428887830281, 0.1015625661591952889, 0.1041669088510773916, 0.1067712598504420435, 0.1093750861808121810, 0.1119797359579501050, 0.1145833143474069837, 0.1171880172914337714, 0.1197916802446672702, 0.1223962066585842084, 0.1250002958591681090, 0.1276043774339237491, 0.1302089111537957367, 0.1328125705047451810, 0.1354172747579587832, 0.1380208536162275679, 0.1406254975582941213, 0.1432293284131295197, 0.1458336698625422867, 0.1484380199076493767, 0.1510418450546419100, 0.1536464938294531402, 0.1562500711155297428, 0.1588547729514310503, 0.1614584348822658832, 0.1640629601007041471, 0.1666670483599762276, 0.1692711287458052438, 0.1718756615333107141, 0.1744793197742946778, 0.1770840230088624179, 0.1796876008377196188, 0.1822922436549848091, 0.1848960735616705098, 0.1875004138364584350, 0.1901047629951247708, 0.1927085870260826783, 0.1953132348667029061, 0.1979168111164897881, 0.2005215119124719170, 0.2031251728880697216, 0.2057296969790492203, 0.2083337843645647058, 0.2109378636290424602, 0.2135423955521746908, 0.2161460527503557827, 0.2187507550344668650, 0.2213543319009846355, 0.2239589736615800464, 0.2265628026874214052, 0.2291671418554001027, 0.2317714901954165685, 0.2343753131776551424, 0.2369799601521939414, 0.2395835354327550959, 0.2421882352569974250, 0.2447918953444941648, 0.2473964183760076208, 0.2500005049552969649, 0.2526045831659717300, 0.2552091142926994904, 0.2578127705152143956, 0.2604174719170327390, 0.2630210478882585856, 0.2656256886602897938, 0.2682295168725681855, 0.2708338550015275126, 0.2734382025906618163, 0.2760420245914711468, 0.2786466707680146371, 0.2812502451463897990, 0.2838549440670474211, 0.2864586033335557724, 0.2890631253735708728, 0.2916672112141422968, 0.2942712884385379479, 0.2968758188368077477, 0.2994794741507696423, 0.3020841747384366283, 0.3046877498813952978, 0.3072923897329448151, 0.3098962171989202430, 0.3125005543566263810, 0.3151049012626256918, 0.3177087223492732204, 0.3203133677958864278, 0.3229169413390938770, 0.3255216394243000688, 0.3281252979369121969, 0.3307298190533745630, 0.3333339042227165261, 0.3359379805283350118, 0.3385425102660742369, 0.3411461647385755636, 0.3437508645802123675, 0.3463544389619092612, 0.3489590779610384774, 0.3515629047479519320, 0.3541672410021501904, 0.3567715872927431642, 0.3593754075324762653, 0.3619800523172059803, 0.3645836250922447341, 0.3671883224101137877, 0.3697919802359038166, 0.3723965004967392245, 0.3750005850623230885, 0.3776046605166471504, 0.3802091896617659783, 0.3828128433598806946, 0.3854175425235913388, 0.3880211162110140388, 0.3906257544257662473, 0.3932295806008425099, 0.3958339160192597128, 0.3984382617621595180, 0.4010420812222079689, 0.4036467254130849946, 0.4062502974869375283, 0.4088549941055670267, 0.4114586513115932598, 0.4140631707847102772, 0.4166672548139925825, 0.4192713294844879757, 0.4218758581048823730, 0.4244795110956688933, 0.4270842096495421902, 0.4296877827096635682, 0.4322924202080664635, 0.4348962458385162155, 0.4375005804888632555, 0.4401049257517701263, 0.4427087444993486054, 0.4453133881643903114, 0.4479169596040251111, 0.4505216555914985932, 0.4531253122448062887, 0.4557298309980991058, 0.4583339145585244578, 0.4609379885126426157, 0.4635425166761967808, 0.4661461690266998081, 0.4687508670388120247, 0.4713544395385928509, 0.4739590763886608604, 0.4765629015416836811, 0.4791672354916582388, 0.4817715803422617515, 0.4843753984445725025, 0.4869800416517858221, 0.4895836125241597725, 0.4921883079485492862, 0.4947919641161733773, 0.4973964822175238609, 0.5000005653765271507, 0.5026046386817077938, 0.5052091664562964324, 0.5078128182335502894, 0.5104175157719683664, 0.5130210877783591972, 0.5156257240480961457, 0.5182295487908826770, 0.5208338821081714975, 0.5234382266141532902, 0.5260420441383883983, 0.5286466869557716608, 0.5312502573278325979, 0.5338549522572011430, 0.5364586080061681805, 0.5390631255234488162, 0.5416672083484578293, 0.5442712810721315186, 0.5468758085256230084, 0.5494794597966533578, 0.5520841569294364648, 0.5546877285093810839, 0.5572923642667827471, 0.5598961886665174692, 0.5625005214187991376, 0.5651048656478350196, 0.5677086826611791315, 0.5703133251567252815, 0.5729168950954143247, 0.5755215895978186280, 0.5781252449951498340, 0.5807297619962258350, 0.5833338445546641937, 0.5859379167642547737, 0.5885424439645127181, 0.5911460947963396162, 0.5937507915915425372, 0.5963543628119793993, 0.5989589981250363904, 0.6015628222488997867, 0.6041671545038470592, 0.6067714985236103420, 0.6093753150932430529, 0.6119799573349418154, 0.6145835269071964202, 0.6171882210506893784, 0.6197918761634028106, 0.6223963927161352272, 0.6250004750754242222, 0.6276045468383509851, 0.6302090738532378777, 0.6328127243128783830, 0.6354174208385534595, 0.6380209917664191321, 0.6406256267031188445, 0.6432294506182901772, 0.6458337824435727015, 0.6484381263217364744, 0.6510419425148348260, 0.6536465845706755928, 0.6562501538434313275, 0.6588548476960643940, 0.6614585025911776661, 0.6640630187634258830, 0.6666671009909873602, 0.6692711723746683772, 0.6718756992720475996, 0.6744793494265174383, 0.6770840457507175669, 0.6796876164529486175, 0.6822922510812780006, 0.6848960748549377531, 0.6875004063182246217, 0.6901047501224634173, 0.6927085660062048955, 0.6953132079441787239, 0.6979167769843723779, 0.7005214706141982273, 0.7031251253587310623, 0.7057296412183544643, 0.7083337233816132672, 0.7109377944534676086, 0.7135423213012055399, 0.7161459712175226588, 0.7187506674083037339, 0.7213542379518396164, 0.7239588723397878400, 0.7265626960391206035, 0.7291670272080824633, 0.7317713710060759214, 0.7343751866476402324, 0.7369798285357428425, 0.7395833974103146469, 0.7421880908853900616, 0.7447917455463664016, 0.7473962611612280371, 0.7500003433276148934, 0.7526044141550642941, 0.7552089410210337528, 0.7578125907662203176, 0.7604172868916432293, 0.7630208573434285046, 0.7656254915589897347, 0.7682293152511859846, 0.7708336461934980344, 0.7734379900529331220, 0.7760418055195050790, 0.7786464474257392965, 0.7812500162016354777, 0.7838547095900232353, 0.7864583642344741277, 0.7890628796724428184, 0.7916669619093961163, 0.7942710325598689725, 0.7968755595119511037, 0.7994792091530360523, 0.8020839052811703507, 0.8046874757081575735, 0.8072921098193328593, 0.8098959335715922858, 0.8125002643549369408, 0.8151046083435100620, 0.8177084237022821389, 0.8203130656946604482, 0.8229166344388356702, 0.8255213278086077633, 0.8281249825035741363, 0.8307294978325265866, 0.8333335802074958165, 0.8359376507484286289, 0.8385421778545157911, 0.8411458274585372763, 0.8437505236574627254, 0.8463540941266142204, 0.8489587282014147140, 0.8515625520809478877, 0.8541668827730166669, 0.8567712269584367712, 0.8593750422766117669, 0.8619796844231587540, 0.8645832532025788941, 0.8671879466218186394, 0.8697916014343529678, 0.8723961167221769841, 0.8750001993026245151, 0.8776042698014647758, 0.8802087971294628721, 0.8828124467634709260, 0.8854171431012803906, 0.8880207136795719158, 0.8906253477860208712, 0.8932291718600525732, 0.8958335025285494302, 0.8984378469785403443, 0.9010416623233333810, 0.9036463046920883979, 0.9062498735737328781, 0.9088545671105374701, 0.9114582221077071056, 0.9140627374223044832, 0.9166668202757080053, 0.9192708907999164181, 0.9218754184177497812, 0.9244790681488107564, 0.9270837646936044285, 0.9296873354480212903, 0.9322919696541906998, 0.9348957939899811276, 0.9375001247025137596, 0.9401044694846933947, 0.9427082849236875228, 0.9453129275835465695, 0.9479164966330613229, 0.9505211903504858784, 0.9531248456066239161, 0.9557293610412391782, 0.9583334441921064206, 0.9609375147049603605, 0.9635420428945489224, 0.9661456931510739032, 0.9687503890924937799, 0.9713539588735070618, 0.9739585961357111188, 0.9765624261165479769, 0.9791667493207181217, 0.9817710620974646751, 0.9843748983037424738, 0.9869797303524157073, 0.9895832060093603388, 0.9921869237806116848, 0.9947912468131487884, 0.9974000922265050528, 0.9999999999999998890 ),
 .UNSPECIFIED. ) 
 GEOMETRIC_REPRESENTATION_ITEM ( )  RATIONAL_B_SPLINE_SURFACE ( (
 ( 1.000000000000000000, 1.000000000000000000, 1.000000000000000000, 0.9999999999999997780, 1.000000000000000000, 1.000000000000000444, 0.9999999999999996669, 0.9999999999999996669, 1.000000000000000444, 1.000000000000000000, 1.000000000000000000, 1.000000000000000000, 1.000000000000000222, 1.000000000000000222, 0.9999999999999997780, 1.000000000000000000, 1.000000000000000222, 1.000000000000000000, 1.000000000000000222, 0.9999999999999994449, 1.000000000000000222, 0.9999999999999997780, 1.000000000000000444, 1.000000000000000000, 1.000000000000000000, 1.000000000000000222, 0.9999999999999997780, 1.000000000000000222, 1.000000000000000000, 1.000000000000000222, 0.9999999999999997780, 1.000000000000000000, 1.000000000000000000, 0.9999999999999997780, 1.000000000000000000, 1.000000000000000000, 1.000000000000000222, 1.000000000000000000, 0.9999999999999997780, 1.000000000000000222, 0.9999999999999997780, 1.000000000000000000, 0.9999999999999997780, 1.000000000000000444, 0.9999999999999996669, 1.000000000000000222, 1.000000000000000000, 1.000000000000000000, 1.000000000000000444, 0.9999999999999996669, 1.000000000000000222, 1.000000000000000444, 1.000000000000000000, 0.9999999999999997780, 1.000000000000000444, 1.000000000000000222, 1.000000000000000000, 1.000000000000000000, 1.000000000000000222, 1.000000000000000000, 1.000000000000000222, 0.9999999999999997780, 1.000000000000000222, 1.000000000000000000, 1.000000000000000000, 1.000000000000000444, 0.9999999999999996669, 1.000000000000000000, 0.9999999999999997780, 1.000000000000000222, 0.9999999999999996669, 1.000000000000000000, 1.000000000000000222, 0.9999999999999997780, 1.000000000000000444, 0.9999999999999997780, 1.000000000000000000, 0.9999999999999997780, 1.000000000000000222, 0.9999999999999996669, 1.000000000000000000, 1.000000000000000222, 0.9999999999999996669, 1.000000000000000444, 0.9999999999999997780, 1.000000000000000000, 1.000000000000000222, 0.9999999999999996669, 1.000000000000000222, 1.000000000000000000, 0.9999999999999997780, 1.000000000000000222, 0.9999999999999997780, 1.000000000000000000, 1.000000000000000222, 0.9999999999999997780, 1.000000000000000000, 1.000000000000000000, 0.9999999999999997780, 1.000000000000000000, 1.000000000000000222, 0.9999999999999997780, 1.000000000000000000, 1.000000000000000000, 1.000000000000000000, 0.9999999999999997780, 1.000000000000000222, 0.9999999999999997780, 0.9999999999999997780, 1.000000000000000444, 1.000000000000000000, 1.000000000000000000, 0.9999999999999997780, 1.000000000000000222, 1.000000000000000000, 1.000000000000000000, 1.000000000000000000, 1.000000000000000000, 1.000000000000000222, 1.000000000000000222, 0.9999999999999997780, 1.000000000000000000, 0.9999999999999997780, 1.000000000000000444, 0.9999999999999996669, 1.000000000000000666, 1.000000000000000000, 0.9999999999999997780, 1.000000000000000222, 1.000000000000000000, 1.000000000000000000, 1.000000000000000000, 0.9999999999999994449, 1.000000000000000666, 0.9999999999999996669, 1.000000000000000000, 1.000000000000000222, 0.9999999999999997780, 1.000000000000000222, 0.9999999999999997780, 1.000000000000000222, 0.9999999999999996669, 1.000000000000000444, 1.000000000000000000, 1.000000000000000222, 0.9999999999999996669, 1.000000000000000000, 1.000000000000000222, 0.9999999999999997780, 1.000000000000000000, 0.9999999999999997780, 1.000000000000000000, 1.000000000000000000, 1.000000000000000222, 0.9999999999999997780, 1.000000000000000222, 0.9999999999999997780, 1.000000000000000000, 1.000000000000000000, 1.000000000000000222, 0.9999999999999997780, 1.000000000000000444, 1.000000000000000000, 0.9999999999999997780, 1.000000000000000000, 1.000000000000000000, 1.000000000000000222, 0.9999999999999997780, 1.000000000000000222, 1.000000000000000000, 1.000000000000000000, 1.000000000000000000, 1.000000000000000222, 1.000000000000000000, 0.9999999999999997780, 1.000000000000000000, 1.000000000000000000, 1.000000000000000000, 1.000000000000000444, 0.9999999999999996669, 1.000000000000000222, 1.000000000000000000, 1.000000000000000222, 0.9999999999999997780, 1.000000000000000000, 0.9999999999999997780, 1.000000000000000000, 0.9999999999999997780, 1.000000000000000000, 1.000000000000000444, 0.9999999999999994449, 1.000000000000000444, 1.000000000000000000, 1.000000000000000222, 1.000000000000000222, 0.9999999999999997780, 1.000000000000000222, 0.9999999999999997780, 1.000000000000000222, 1.000000000000000222, 1.000000000000000222, 0.9999999999999997780, 1.000000000000000000, 1.000000000000000444, 0.9999999999999996669, 1.000000000000000000, 0.9999999999999997780, 1.000000000000000222, 1.000000000000000222, 1.000000000000000000, 0.9999999999999997780, 1.000000000000000222, 0.9999999999999997780, 1.000000000000000222, 0.9999999999999997780, 0.9999999999999997780, 1.000000000000000000, 1.000000000000000000, 1.000000000000000000, 1.000000000000000000, 1.000000000000000000, 1.000000000000000222, 1.000000000000000000, 1.000000000000000000, 1.000000000000000222, 1.000000000000000000, 0.9999999999999997780, 1.000000000000000000, 1.000000000000000000, 1.000000000000000000, 0.9999999999999997780, 1.000000000000000000, 0.9999999999999997780, 1.000000000000000000, 1.000000000000000222, 0.9999999999999996669, 1.000000000000000444, 1.000000000000000000, 0.9999999999999997780, 1.000000000000000222, 1.000000000000000000, 0.9999999999999997780, 1.000000000000000222, 1.000000000000000000, 1.000000000000000222, 1.000000000000000000, 0.9999999999999997780, 1.000000000000000222, 1.000000000000000000, 1.000000000000000000, 1.000000000000000222, 1.000000000000000000, 1.000000000000000000, 1.000000000000000222, 0.9999999999999997780, 0.9999999999999996669, 1.000000000000000444, 0.9999999999999994449, 1.000000000000000444, 0.9999999999999997780, 1.000000000000000222, 1.000000000000000000, 1.000000000000000000, 1.000000000000000000, 1.000000000000000000, 1.000000000000000444, 0.9999999999999996669, 1.000000000000000444, 1.000000000000000000, 0.9999999999999997780, 1.000000000000000444, 0.9999999999999994449, 1.000000000000000444, 0.9999999999999997780, 0.9999999999999997780, 1.000000000000000222, 1.000000000000000444, 0.9999999999999997780, 1.000000000000000444, 0.9999999999999997780, 1.000000000000000000, 1.000000000000000444, 0.9999999999999997780, 0.9999999999999997780, 1.000000000000000000, 1.000000000000000000, 1.000000000000000000, 0.9999999999999997780, 1.000000000000000444, 1.000000000000000222, 0.9999999999999997780, 1.000000000000000444, 1.000000000000000000, 1.000000000000000222, 1.000000000000000000, 1.000000000000000000, 1.000000000000000222, 0.9999999999999997780, 1.000000000000000222, 1.000000000000000222, 0.9999999999999997780, 1.000000000000000222, 1.000000000000000000, 1.000000000000000000, 1.000000000000000222, 0.9999999999999997780, 1.000000000000000444, 0.9999999999999997780, 0.9999999999999997780, 1.000000000000000222, 0.9999999999999997780, 1.000000000000000000, 1.000000000000000000, 0.9999999999999997780, 1.000000000000000222, 0.9999999999999996669, 1.000000000000000444, 0.9999999999999997780, 1.000000000000000222, 1.000000000000000222, 0.9999999999999997780, 1.000000000000000222, 0.9999999999999997780, 1.000000000000000000, 0.9999999999999997780, 1.000000000000000444, 0.9999999999999996669, 1.000000000000000222, 0.9999999999999996669, 1.000000000000000444, 1.000000000000000000, 0.9999999999999997780, 1.000000000000000222, 0.9999999999999996669, 1.000000000000000222, 1.000000000000000222, 0.9999999999999996669, 1.000000000000000444, 1.000000000000000222, 0.9999999999999997780, 1.000000000000000222, 0.9999999999999997780, 1.000000000000000222, 1.000000000000000000, 1.000000000000000222, 0.9999999999999996669, 1.000000000000000444, 1.000000000000000000, 1.000000000000000000, 1.000000000000000222, 0.9999999999999997780, 0.9999999999999997780, 1.000000000000000444, 1.000000000000000000, 1.000000000000000000, 0.9999999999999996669, 1.000000000000000000, 1.000000000000000222, 1.000000000000000000, 1.000000000000000000, 1.000000000000000222, 0.9999999999999997780, 1.000000000000000000, 0.9999999999999997780, 0.9999999999999997780, 1.000000000000000222, 0.9999999999999997780, 1.000000000000000000, 1.000000000000000000, 0.9999999999999997780, 1.000000000000000222, 1.000000000000000000, 1.000000000000000222, 1.000000000000000000, 1.000000000000000444, 1.000000000000000000, 1.000000000000000000, 0.9999999999999997780, 0.9999999999999997780, 1.000000000000000222, 1.000000000000000000, 1.000000000000000000, 1.000000000000000000, 0.9999999999999997780, 1.000000000000000222, 1.000000000000000000, 1.000000000000000000),
 ( 0.3333333333333333703, 0.3333333333333333703, 0.3333333333333333703, 0.3333333333333333148, 0.3333333333333334259, 0.3333333333333334814, 0.3333333333333332593, 0.3333333333333332593, 0.3333333333333334814, 0.3333333333333333703, 0.3333333333333333703, 0.3333333333333334259, 0.3333333333333334259, 0.3333333333333334259, 0.3333333333333332593, 0.3333333333333334259, 0.3333333333333334259, 0.3333333333333333703, 0.3333333333333334259, 0.3333333333333332038, 0.3333333333333334259, 0.3333333333333333148, 0.3333333333333334259, 0.3333333333333333703, 0.3333333333333333703, 0.3333333333333334259, 0.3333333333333333148, 0.3333333333333334259, 0.3333333333333333703, 0.3333333333333333703, 0.3333333333333333148, 0.3333333333333334259, 0.3333333333333333703, 0.3333333333333333703, 0.3333333333333333148, 0.3333333333333333148, 0.3333333333333334259, 0.3333333333333333148, 0.3333333333333334259, 0.3333333333333333703, 0.3333333333333333703, 0.3333333333333333703, 0.3333333333333332593, 0.3333333333333334814, 0.3333333333333332593, 0.3333333333333333703, 0.3333333333333333703, 0.3333333333333333703, 0.3333333333333335369, 0.3333333333333332593, 0.3333333333333333703, 0.3333333333333335369, 0.3333333333333333703, 0.3333333333333333703, 0.3333333333333335369, 0.3333333333333333703, 0.3333333333333334259, 0.3333333333333334259, 0.3333333333333333703, 0.3333333333333333703, 0.3333333333333333703, 0.3333333333333333703, 0.3333333333333333703, 0.3333333333333333148, 0.3333333333333334259, 0.3333333333333334814, 0.3333333333333333148, 0.3333333333333333703, 0.3333333333333333148, 0.3333333333333334259, 0.3333333333333332593, 0.3333333333333334259, 0.3333333333333333703, 0.3333333333333334259, 0.3333333333333333703, 0.3333333333333333703, 0.3333333333333333703, 0.3333333333333333148, 0.3333333333333334814, 0.3333333333333332038, 0.3333333333333334259, 0.3333333333333334259, 0.3333333333333333148, 0.3333333333333334259, 0.3333333333333333703, 0.3333333333333333148, 0.3333333333333333703, 0.3333333333333333148, 0.3333333333333334814, 0.3333333333333333148, 0.3333333333333333148, 0.3333333333333334259, 0.3333333333333333148, 0.3333333333333333148, 0.3333333333333334814, 0.3333333333333333148, 0.3333333333333334259, 0.3333333333333333703, 0.3333333333333333148, 0.3333333333333333703, 0.3333333333333334259, 0.3333333333333333148, 0.3333333333333334259, 0.3333333333333333148, 0.3333333333333333703, 0.3333333333333333148, 0.3333333333333333703, 0.3333333333333333703, 0.3333333333333333148, 0.3333333333333334259, 0.3333333333333334259, 0.3333333333333333148, 0.3333333333333333703, 0.3333333333333333703, 0.3333333333333334259, 0.3333333333333333703, 0.3333333333333333703, 0.3333333333333334259, 0.3333333333333333703, 0.3333333333333334259, 0.3333333333333333148, 0.3333333333333333703, 0.3333333333333333148, 0.3333333333333335369, 0.3333333333333333148, 0.3333333333333335369, 0.3333333333333333703, 0.3333333333333332593, 0.3333333333333334259, 0.3333333333333334259, 0.3333333333333333148, 0.3333333333333333703, 0.3333333333333333148, 0.3333333333333335369, 0.3333333333333333148, 0.3333333333333333703, 0.3333333333333333703, 0.3333333333333334259, 0.3333333333333334259, 0.3333333333333333703, 0.3333333333333334259, 0.3333333333333332593, 0.3333333333333334814, 0.3333333333333333148, 0.3333333333333333703, 0.3333333333333333148, 0.3333333333333333148, 0.3333333333333334259, 0.3333333333333332593, 0.3333333333333333148, 0.3333333333333333703, 0.3333333333333333148, 0.3333333333333333703, 0.3333333333333334259, 0.3333333333333333703, 0.3333333333333334259, 0.3333333333333333148, 0.3333333333333333703, 0.3333333333333333703, 0.3333333333333333703, 0.3333333333333333148, 0.3333333333333335369, 0.3333333333333333148, 0.3333333333333333703, 0.3333333333333333148, 0.3333333333333334259, 0.3333333333333334259, 0.3333333333333333703, 0.3333333333333334259, 0.3333333333333333703, 0.3333333333333333703, 0.3333333333333334259, 0.3333333333333333703, 0.3333333333333333703, 0.3333333333333333703, 0.3333333333333334259, 0.3333333333333333148, 0.3333333333333333148, 0.3333333333333335369, 0.3333333333333333148, 0.3333333333333334259, 0.3333333333333333148, 0.3333333333333334259, 0.3333333333333333703, 0.3333333333333333148, 0.3333333333333333148, 0.3333333333333333703, 0.3333333333333333148, 0.3333333333333334259, 0.3333333333333334259, 0.3333333333333332038, 0.3333333333333335369, 0.3333333333333333703, 0.3333333333333334259, 0.3333333333333334259, 0.3333333333333333703, 0.3333333333333334259, 0.3333333333333332593, 0.3333333333333334814, 0.3333333333333333703, 0.3333333333333334259, 0.3333333333333333148, 0.3333333333333333148, 0.3333333333333335369, 0.3333333333333332593, 0.3333333333333333703, 0.3333333333333332593, 0.3333333333333335369, 0.3333333333333333703, 0.3333333333333333703, 0.3333333333333333703, 0.3333333333333334259, 0.3333333333333332593, 0.3333333333333334814, 0.3333333333333332593, 0.3333333333333333703, 0.3333333333333333703, 0.3333333333333333703, 0.3333333333333334259, 0.3333333333333333148, 0.3333333333333334259, 0.3333333333333334259, 0.3333333333333333703, 0.3333333333333333148, 0.3333333333333334259, 0.3333333333333333148, 0.3333333333333333703, 0.3333333333333333148, 0.3333333333333333703, 0.3333333333333333703, 0.3333333333333333148, 0.3333333333333333703, 0.3333333333333333703, 0.3333333333333333703, 0.3333333333333334259, 0.3333333333333333703, 0.3333333333333333703, 0.3333333333333334814, 0.3333333333333332593, 0.3333333333333333703, 0.3333333333333334259, 0.3333333333333333148, 0.3333333333333334259, 0.3333333333333333703, 0.3333333333333334814, 0.3333333333333333703, 0.3333333333333333148, 0.3333333333333334259, 0.3333333333333333703, 0.3333333333333333703, 0.3333333333333333703, 0.3333333333333334259, 0.3333333333333333148, 0.3333333333333334259, 0.3333333333333333148, 0.3333333333333333148, 0.3333333333333335369, 0.3333333333333332038, 0.3333333333333335369, 0.3333333333333333148, 0.3333333333333333703, 0.3333333333333334259, 0.3333333333333333703, 0.3333333333333333148, 0.3333333333333333703, 0.3333333333333334259, 0.3333333333333333703, 0.3333333333333334259, 0.3333333333333333148, 0.3333333333333333703, 0.3333333333333334259, 0.3333333333333333148, 0.3333333333333333703, 0.3333333333333333703, 0.3333333333333333148, 0.3333333333333334259, 0.3333333333333334259, 0.3333333333333333703, 0.3333333333333335369, 0.3333333333333333148, 0.3333333333333333703, 0.3333333333333333703, 0.3333333333333333148, 0.3333333333333333703, 0.3333333333333333703, 0.3333333333333333703, 0.3333333333333333148, 0.3333333333333333703, 0.3333333333333334814, 0.3333333333333333703, 0.3333333333333333703, 0.3333333333333335369, 0.3333333333333333703, 0.3333333333333333703, 0.3333333333333334259, 0.3333333333333334259, 0.3333333333333333703, 0.3333333333333333703, 0.3333333333333333703, 0.3333333333333333703, 0.3333333333333333148, 0.3333333333333334259, 0.3333333333333333703, 0.3333333333333333703, 0.3333333333333333703, 0.3333333333333333148, 0.3333333333333334814, 0.3333333333333333148, 0.3333333333333333148, 0.3333333333333334814, 0.3333333333333333148, 0.3333333333333333148, 0.3333333333333334259, 0.3333333333333333148, 0.3333333333333334259, 0.3333333333333333148, 0.3333333333333334259, 0.3333333333333332593, 0.3333333333333335369, 0.3333333333333333148, 0.3333333333333333148, 0.3333333333333334259, 0.3333333333333333703, 0.3333333333333333703, 0.3333333333333333148, 0.3333333333333334259, 0.3333333333333333148, 0.3333333333333334259, 0.3333333333333333148, 0.3333333333333334259, 0.3333333333333334259, 0.3333333333333333703, 0.3333333333333334259, 0.3333333333333333703, 0.3333333333333333703, 0.3333333333333334259, 0.3333333333333333148, 0.3333333333333335369, 0.3333333333333334259, 0.3333333333333333148, 0.3333333333333333703, 0.3333333333333333148, 0.3333333333333334814, 0.3333333333333333703, 0.3333333333333333703, 0.3333333333333332593, 0.3333333333333334814, 0.3333333333333333703, 0.3333333333333333148, 0.3333333333333334259, 0.3333333333333332593, 0.3333333333333334814, 0.3333333333333333703, 0.3333333333333334259, 0.3333333333333333703, 0.3333333333333333148, 0.3333333333333333703, 0.3333333333333334259, 0.3333333333333333703, 0.3333333333333334259, 0.3333333333333333703, 0.3333333333333333703, 0.3333333333333333148, 0.3333333333333333148, 0.3333333333333333703, 0.3333333333333333703, 0.3333333333333333703, 0.3333333333333333703, 0.3333333333333333703, 0.3333333333333333148, 0.3333333333333334814, 0.3333333333333333148, 0.3333333333333334814, 0.3333333333333333703, 0.3333333333333334259, 0.3333333333333334259, 0.3333333333333333703, 0.3333333333333332593, 0.3333333333333333703, 0.3333333333333333703, 0.3333333333333333703, 0.3333333333333333148, 0.3333333333333333703, 0.3333333333333332593, 0.3333333333333334259, 0.3333333333333333703, 0.3333333333333333703),
 ( 0.3333333333333333703, 0.3333333333333333703, 0.3333333333333333703, 0.3333333333333333148, 0.3333333333333334259, 0.3333333333333334814, 0.3333333333333332593, 0.3333333333333332593, 0.3333333333333334814, 0.3333333333333333703, 0.3333333333333333703, 0.3333333333333334259, 0.3333333333333334259, 0.3333333333333334259, 0.3333333333333332593, 0.3333333333333334259, 0.3333333333333334259, 0.3333333333333333703, 0.3333333333333334259, 0.3333333333333332038, 0.3333333333333334259, 0.3333333333333333148, 0.3333333333333334259, 0.3333333333333333703, 0.3333333333333333703, 0.3333333333333334259, 0.3333333333333333148, 0.3333333333333334259, 0.3333333333333333703, 0.3333333333333333703, 0.3333333333333333148, 0.3333333333333334259, 0.3333333333333333703, 0.3333333333333333703, 0.3333333333333333148, 0.3333333333333333148, 0.3333333333333334259, 0.3333333333333333148, 0.3333333333333334259, 0.3333333333333333703, 0.3333333333333333703, 0.3333333333333333703, 0.3333333333333332593, 0.3333333333333334814, 0.3333333333333332593, 0.3333333333333333703, 0.3333333333333333703, 0.3333333333333333703, 0.3333333333333335369, 0.3333333333333332593, 0.3333333333333333703, 0.3333333333333335369, 0.3333333333333333703, 0.3333333333333333703, 0.3333333333333335369, 0.3333333333333333703, 0.3333333333333334259, 0.3333333333333334259, 0.3333333333333333703, 0.3333333333333333703, 0.3333333333333333703, 0.3333333333333333703, 0.3333333333333333703, 0.3333333333333333148, 0.3333333333333334259, 0.3333333333333334814, 0.3333333333333333148, 0.3333333333333333703, 0.3333333333333333148, 0.3333333333333334259, 0.3333333333333332593, 0.3333333333333334259, 0.3333333333333333703, 0.3333333333333334259, 0.3333333333333333703, 0.3333333333333333703, 0.3333333333333333703, 0.3333333333333333148, 0.3333333333333334814, 0.3333333333333332038, 0.3333333333333334259, 0.3333333333333334259, 0.3333333333333333148, 0.3333333333333334259, 0.3333333333333333703, 0.3333333333333333148, 0.3333333333333333703, 0.3333333333333333148, 0.3333333333333334814, 0.3333333333333333148, 0.3333333333333333148, 0.3333333333333334259, 0.3333333333333333148, 0.3333333333333333148, 0.3333333333333334814, 0.3333333333333333148, 0.3333333333333334259, 0.3333333333333333703, 0.3333333333333333148, 0.3333333333333333703, 0.3333333333333334259, 0.3333333333333333148, 0.3333333333333334259, 0.3333333333333333148, 0.3333333333333333703, 0.3333333333333333148, 0.3333333333333333703, 0.3333333333333333703, 0.3333333333333333148, 0.3333333333333334259, 0.3333333333333334259, 0.3333333333333333148, 0.3333333333333333703, 0.3333333333333333703, 0.3333333333333334259, 0.3333333333333333703, 0.3333333333333333703, 0.3333333333333334259, 0.3333333333333333703, 0.3333333333333334259, 0.3333333333333333148, 0.3333333333333333703, 0.3333333333333333148, 0.3333333333333335369, 0.3333333333333333148, 0.3333333333333335369, 0.3333333333333333703, 0.3333333333333332593, 0.3333333333333334259, 0.3333333333333334259, 0.3333333333333333148, 0.3333333333333333703, 0.3333333333333333148, 0.3333333333333335369, 0.3333333333333333148, 0.3333333333333333703, 0.3333333333333333703, 0.3333333333333334259, 0.3333333333333334259, 0.3333333333333333703, 0.3333333333333334259, 0.3333333333333332593, 0.3333333333333334814, 0.3333333333333333148, 0.3333333333333333703, 0.3333333333333333148, 0.3333333333333333148, 0.3333333333333334259, 0.3333333333333332593, 0.3333333333333333148, 0.3333333333333333703, 0.3333333333333333148, 0.3333333333333333703, 0.3333333333333334259, 0.3333333333333333703, 0.3333333333333334259, 0.3333333333333333148, 0.3333333333333333703, 0.3333333333333333703, 0.3333333333333333703, 0.3333333333333333148, 0.3333333333333335369, 0.3333333333333333148, 0.3333333333333333703, 0.3333333333333333148, 0.3333333333333334259, 0.3333333333333334259, 0.3333333333333333703, 0.3333333333333334259, 0.3333333333333333703, 0.3333333333333333703, 0.3333333333333334259, 0.3333333333333333703, 0.3333333333333333703, 0.3333333333333333703, 0.3333333333333334259, 0.3333333333333333148, 0.3333333333333333148, 0.3333333333333335369, 0.3333333333333333148, 0.3333333333333334259, 0.3333333333333333148, 0.3333333333333334259, 0.3333333333333333703, 0.3333333333333333148, 0.3333333333333333148, 0.3333333333333333703, 0.3333333333333333148, 0.3333333333333334259, 0.3333333333333334259, 0.3333333333333332038, 0.3333333333333335369, 0.3333333333333333703, 0.3333333333333334259, 0.3333333333333334259, 0.3333333333333333703, 0.3333333333333334259, 0.3333333333333332593, 0.3333333333333334814, 0.3333333333333333703, 0.3333333333333334259, 0.3333333333333333148, 0.3333333333333333148, 0.3333333333333335369, 0.3333333333333332593, 0.3333333333333333703, 0.3333333333333332593, 0.3333333333333335369, 0.3333333333333333703, 0.3333333333333333703, 0.3333333333333333703, 0.3333333333333334259, 0.3333333333333332593, 0.3333333333333334814, 0.3333333333333332593, 0.3333333333333333703, 0.3333333333333333703, 0.3333333333333333703, 0.3333333333333334259, 0.3333333333333333148, 0.3333333333333334259, 0.3333333333333334259, 0.3333333333333333703, 0.3333333333333333148, 0.3333333333333334259, 0.3333333333333333148, 0.3333333333333333703, 0.3333333333333333148, 0.3333333333333333703, 0.3333333333333333703, 0.3333333333333333148, 0.3333333333333333703, 0.3333333333333333703, 0.3333333333333333703, 0.3333333333333334259, 0.3333333333333333703, 0.3333333333333333703, 0.3333333333333334814, 0.3333333333333332593, 0.3333333333333333703, 0.3333333333333334259, 0.3333333333333333148, 0.3333333333333334259, 0.3333333333333333703, 0.3333333333333334814, 0.3333333333333333703, 0.3333333333333333148, 0.3333333333333334259, 0.3333333333333333703, 0.3333333333333333703, 0.3333333333333333703, 0.3333333333333334259, 0.3333333333333333148, 0.3333333333333334259, 0.3333333333333333148, 0.3333333333333333148, 0.3333333333333335369, 0.3333333333333332038, 0.3333333333333335369, 0.3333333333333333148, 0.3333333333333333703, 0.3333333333333334259, 0.3333333333333333703, 0.3333333333333333148, 0.3333333333333333703, 0.3333333333333334259, 0.3333333333333333703, 0.3333333333333334259, 0.3333333333333333148, 0.3333333333333333703, 0.3333333333333334259, 0.3333333333333333148, 0.3333333333333333703, 0.3333333333333333703, 0.3333333333333333148, 0.3333333333333334259, 0.3333333333333334259, 0.3333333333333333703, 0.3333333333333335369, 0.3333333333333333148, 0.3333333333333333703, 0.3333333333333333703, 0.3333333333333333148, 0.3333333333333333703, 0.3333333333333333703, 0.3333333333333333703, 0.3333333333333333148, 0.3333333333333333703, 0.3333333333333334814, 0.3333333333333333703, 0.3333333333333333703, 0.3333333333333335369, 0.3333333333333333703, 0.3333333333333333703, 0.3333333333333334259, 0.3333333333333334259, 0.3333333333333333703, 0.3333333333333333703, 0.3333333333333333703, 0.3333333333333333703, 0.3333333333333333148, 0.3333333333333334259, 0.3333333333333333703, 0.3333333333333333703, 0.3333333333333333703, 0.3333333333333333148, 0.3333333333333334814, 0.3333333333333333148, 0.3333333333333333148, 0.3333333333333334814, 0.3333333333333333148, 0.3333333333333333148, 0.3333333333333334259, 0.3333333333333333148, 0.3333333333333334259, 0.3333333333333333148, 0.3333333333333334259, 0.3333333333333332593, 0.3333333333333335369, 0.3333333333333333148, 0.3333333333333333148, 0.3333333333333334259, 0.3333333333333333703, 0.3333333333333333703, 0.3333333333333333148, 0.3333333333333334259, 0.3333333333333333148, 0.3333333333333334259, 0.3333333333333333148, 0.3333333333333334259, 0.3333333333333334259, 0.3333333333333333703, 0.3333333333333334259, 0.3333333333333333703, 0.3333333333333333703, 0.3333333333333334259, 0.3333333333333333148, 0.3333333333333335369, 0.3333333333333334259, 0.3333333333333333148, 0.3333333333333333703, 0.3333333333333333148, 0.3333333333333334814, 0.3333333333333333703, 0.3333333333333333703, 0.3333333333333332593, 0.3333333333333334814, 0.3333333333333333703, 0.3333333333333333148, 0.3333333333333334259, 0.3333333333333332593, 0.3333333333333334814, 0.3333333333333333703, 0.3333333333333334259, 0.3333333333333333703, 0.3333333333333333148, 0.3333333333333333703, 0.3333333333333334259, 0.3333333333333333703, 0.3333333333333334259, 0.3333333333333333703, 0.3333333333333333703, 0.3333333333333333148, 0.3333333333333333148, 0.3333333333333333703, 0.3333333333333333703, 0.3333333333333333703, 0.3333333333333333703, 0.3333333333333333703, 0.3333333333333333148, 0.3333333333333334814, 0.3333333333333333148, 0.3333333333333334814, 0.3333333333333333703, 0.3333333333333334259, 0.3333333333333334259, 0.3333333333333333703, 0.3333333333333332593, 0.3333333333333333703, 0.3333333333333333703, 0.3333333333333333703, 0.3333333333333333148, 0.3333333333333333703, 0.3333333333333332593, 0.3333333333333334259, 0.3333333333333333703, 0.3333333333333333703),
 ( 1.000000000000000000, 1.000000000000000000, 1.000000000000000000, 0.9999999999999997780, 1.000000000000000000, 1.000000000000000444, 0.9999999999999996669, 0.9999999999999996669, 1.000000000000000444, 1.000000000000000000, 1.000000000000000000, 1.000000000000000000, 1.000000000000000222, 1.000000000000000222, 0.9999999999999997780, 1.000000000000000000, 1.000000000000000222, 1.000000000000000000, 1.000000000000000222, 0.9999999999999994449, 1.000000000000000222, 0.9999999999999997780, 1.000000000000000444, 1.000000000000000000, 1.000000000000000000, 1.000000000000000222, 0.9999999999999997780, 1.000000000000000222, 1.000000000000000000, 1.000000000000000222, 0.9999999999999997780, 1.000000000000000000, 1.000000000000000000, 0.9999999999999997780, 1.000000000000000000, 1.000000000000000000, 1.000000000000000222, 1.000000000000000000, 0.9999999999999997780, 1.000000000000000222, 0.9999999999999997780, 1.000000000000000000, 0.9999999999999997780, 1.000000000000000444, 0.9999999999999996669, 1.000000000000000222, 1.000000000000000000, 1.000000000000000000, 1.000000000000000444, 0.9999999999999996669, 1.000000000000000222, 1.000000000000000444, 1.000000000000000000, 0.9999999999999997780, 1.000000000000000444, 1.000000000000000222, 1.000000000000000000, 1.000000000000000000, 1.000000000000000222, 1.000000000000000000, 1.000000000000000222, 0.9999999999999997780, 1.000000000000000222, 1.000000000000000000, 1.000000000000000000, 1.000000000000000444, 0.9999999999999996669, 1.000000000000000000, 0.9999999999999997780, 1.000000000000000222, 0.9999999999999996669, 1.000000000000000000, 1.000000000000000222, 0.9999999999999997780, 1.000000000000000444, 0.9999999999999997780, 1.000000000000000000, 0.9999999999999997780, 1.000000000000000222, 0.9999999999999996669, 1.000000000000000000, 1.000000000000000222, 0.9999999999999996669, 1.000000000000000444, 0.9999999999999997780, 1.000000000000000000, 1.000000000000000222, 0.9999999999999996669, 1.000000000000000222, 1.000000000000000000, 0.9999999999999997780, 1.000000000000000222, 0.9999999999999997780, 1.000000000000000000, 1.000000000000000222, 0.9999999999999997780, 1.000000000000000000, 1.000000000000000000, 0.9999999999999997780, 1.000000000000000000, 1.000000000000000222, 0.9999999999999997780, 1.000000000000000000, 1.000000000000000000, 1.000000000000000000, 0.9999999999999997780, 1.000000000000000222, 0.9999999999999997780, 0.9999999999999997780, 1.000000000000000444, 1.000000000000000000, 1.000000000000000000, 0.9999999999999997780, 1.000000000000000222, 1.000000000000000000, 1.000000000000000000, 1.000000000000000000, 1.000000000000000000, 1.000000000000000222, 1.000000000000000222, 0.9999999999999997780, 1.000000000000000000, 0.9999999999999997780, 1.000000000000000444, 0.9999999999999996669, 1.000000000000000666, 1.000000000000000000, 0.9999999999999997780, 1.000000000000000222, 1.000000000000000000, 1.000000000000000000, 1.000000000000000000, 0.9999999999999994449, 1.000000000000000666, 0.9999999999999996669, 1.000000000000000000, 1.000000000000000222, 0.9999999999999997780, 1.000000000000000222, 0.9999999999999997780, 1.000000000000000222, 0.9999999999999996669, 1.000000000000000444, 1.000000000000000000, 1.000000000000000222, 0.9999999999999996669, 1.000000000000000000, 1.000000000000000222, 0.9999999999999997780, 1.000000000000000000, 0.9999999999999997780, 1.000000000000000000, 1.000000000000000000, 1.000000000000000222, 0.9999999999999997780, 1.000000000000000222, 0.9999999999999997780, 1.000000000000000000, 1.000000000000000000, 1.000000000000000222, 0.9999999999999997780, 1.000000000000000444, 1.000000000000000000, 0.9999999999999997780, 1.000000000000000000, 1.000000000000000000, 1.000000000000000222, 0.9999999999999997780, 1.000000000000000222, 1.000000000000000000, 1.000000000000000000, 1.000000000000000000, 1.000000000000000222, 1.000000000000000000, 0.9999999999999997780, 1.000000000000000000, 1.000000000000000000, 1.000000000000000000, 1.000000000000000444, 0.9999999999999996669, 1.000000000000000222, 1.000000000000000000, 1.000000000000000222, 0.9999999999999997780, 1.000000000000000000, 0.9999999999999997780, 1.000000000000000000, 0.9999999999999997780, 1.000000000000000000, 1.000000000000000444, 0.9999999999999994449, 1.000000000000000444, 1.000000000000000000, 1.000000000000000222, 1.000000000000000222, 0.9999999999999997780, 1.000000000000000222, 0.9999999999999997780, 1.000000000000000222, 1.000000000000000222, 1.000000000000000222, 0.9999999999999997780, 1.000000000000000000, 1.000000000000000444, 0.9999999999999996669, 1.000000000000000000, 0.9999999999999997780, 1.000000000000000222, 1.000000000000000222, 1.000000000000000000, 0.9999999999999997780, 1.000000000000000222, 0.9999999999999997780, 1.000000000000000222, 0.9999999999999997780, 0.9999999999999997780, 1.000000000000000000, 1.000000000000000000, 1.000000000000000000, 1.000000000000000000, 1.000000000000000000, 1.000000000000000222, 1.000000000000000000, 1.000000000000000000, 1.000000000000000222, 1.000000000000000000, 0.9999999999999997780, 1.000000000000000000, 1.000000000000000000, 1.000000000000000000, 0.9999999999999997780, 1.000000000000000000, 0.9999999999999997780, 1.000000000000000000, 1.000000000000000222, 0.9999999999999996669, 1.000000000000000444, 1.000000000000000000, 0.9999999999999997780, 1.000000000000000222, 1.000000000000000000, 0.9999999999999997780, 1.000000000000000222, 1.000000000000000000, 1.000000000000000222, 1.000000000000000000, 0.9999999999999997780, 1.000000000000000222, 1.000000000000000000, 1.000000000000000000, 1.000000000000000222, 1.000000000000000000, 1.000000000000000000, 1.000000000000000222, 0.9999999999999997780, 0.9999999999999996669, 1.000000000000000444, 0.9999999999999994449, 1.000000000000000444, 0.9999999999999997780, 1.000000000000000222, 1.000000000000000000, 1.000000000000000000, 1.000000000000000000, 1.000000000000000000, 1.000000000000000444, 0.9999999999999996669, 1.000000000000000444, 1.000000000000000000, 0.9999999999999997780, 1.000000000000000444, 0.9999999999999994449, 1.000000000000000444, 0.9999999999999997780, 0.9999999999999997780, 1.000000000000000222, 1.000000000000000444, 0.9999999999999997780, 1.000000000000000444, 0.9999999999999997780, 1.000000000000000000, 1.000000000000000444, 0.9999999999999997780, 0.9999999999999997780, 1.000000000000000000, 1.000000000000000000, 1.000000000000000000, 0.9999999999999997780, 1.000000000000000444, 1.000000000000000222, 0.9999999999999997780, 1.000000000000000444, 1.000000000000000000, 1.000000000000000222, 1.000000000000000000, 1.000000000000000000, 1.000000000000000222, 0.9999999999999997780, 1.000000000000000222, 1.000000000000000222, 0.9999999999999997780, 1.000000000000000222, 1.000000000000000000, 1.000000000000000000, 1.000000000000000222, 0.9999999999999997780, 1.000000000000000444, 0.9999999999999997780, 0.9999999999999997780, 1.000000000000000222, 0.9999999999999997780, 1.000000000000000000, 1.000000000000000000, 0.9999999999999997780, 1.000000000000000222, 0.9999999999999996669, 1.000000000000000444, 0.9999999999999997780, 1.000000000000000222, 1.000000000000000222, 0.9999999999999997780, 1.000000000000000222, 0.9999999999999997780, 1.000000000000000000, 0.9999999999999997780, 1.000000000000000444, 0.9999999999999996669, 1.000000000000000222, 0.9999999999999996669, 1.000000000000000444, 1.000000000000000000, 0.9999999999999997780, 1.000000000000000222, 0.9999999999999996669, 1.000000000000000222, 1.000000000000000222, 0.9999999999999996669, 1.000000000000000444, 1.000000000000000222, 0.9999999999999997780, 1.000000000000000222, 0.9999999999999997780, 1.000000000000000222, 1.000000000000000000, 1.000000000000000222, 0.9999999999999996669, 1.000000000000000444, 1.000000000000000000, 1.000000000000000000, 1.000000000000000222, 0.9999999999999997780, 0.9999999999999997780, 1.000000000000000444, 1.000000000000000000, 1.000000000000000000, 0.9999999999999996669, 1.000000000000000000, 1.000000000000000222, 1.000000000000000000, 1.000000000000000000, 1.000000000000000222, 0.9999999999999997780, 1.000000000000000000, 0.9999999999999997780, 0.9999999999999997780, 1.000000000000000222, 0.9999999999999997780, 1.000000000000000000, 1.000000000000000000, 0.9999999999999997780, 1.000000000000000222, 1.000000000000000000, 1.000000000000000222, 1.000000000000000000, 1.000000000000000444, 1.000000000000000000, 1.000000000000000000, 0.9999999999999997780, 0.9999999999999997780, 1.000000000000000222, 1.000000000000000000, 1.000000000000000000, 1.000000000000000000, 0.9999999999999997780, 1.000000000000000222, 1.000000000000000000, 1.000000000000000000),
 ( 0.3333333333333333703, 0.3333333333333333703, 0.3333333333333333703, 0.3333333333333333148, 0.3333333333333334259, 0.3333333333333334814, 0.3333333333333332593, 0.3333333333333332593, 0.3333333333333334814, 0.3333333333333333703, 0.3333333333333333703, 0.3333333333333334259, 0.3333333333333334259, 0.3333333333333334259, 0.3333333333333332593, 0.3333333333333334259, 0.3333333333333334259, 0.3333333333333333703, 0.3333333333333334259, 0.3333333333333332038, 0.3333333333333334259, 0.3333333333333333148, 0.3333333333333334259, 0.3333333333333333703, 0.3333333333333333703, 0.3333333333333334259, 0.3333333333333333148, 0.3333333333333334259, 0.3333333333333333703, 0.3333333333333333703, 0.3333333333333333148, 0.3333333333333334259, 0.3333333333333333703, 0.3333333333333333703, 0.3333333333333333148, 0.3333333333333333148, 0.3333333333333334259, 0.3333333333333333148, 0.3333333333333334259, 0.3333333333333333703, 0.3333333333333333703, 0.3333333333333333703, 0.3333333333333332593, 0.3333333333333334814, 0.3333333333333332593, 0.3333333333333333703, 0.3333333333333333703, 0.3333333333333333703, 0.3333333333333335369, 0.3333333333333332593, 0.3333333333333333703, 0.3333333333333335369, 0.3333333333333333703, 0.3333333333333333703, 0.3333333333333335369, 0.3333333333333333703, 0.3333333333333334259, 0.3333333333333334259, 0.3333333333333333703, 0.3333333333333333703, 0.3333333333333333703, 0.3333333333333333703, 0.3333333333333333703, 0.3333333333333333148, 0.3333333333333334259, 0.3333333333333334814, 0.3333333333333333148, 0.3333333333333333703, 0.3333333333333333148, 0.3333333333333334259, 0.3333333333333332593, 0.3333333333333334259, 0.3333333333333333703, 0.3333333333333334259, 0.3333333333333333703, 0.3333333333333333703, 0.3333333333333333703, 0.3333333333333333148, 0.3333333333333334814, 0.3333333333333332038, 0.3333333333333334259, 0.3333333333333334259, 0.3333333333333333148, 0.3333333333333334259, 0.3333333333333333703, 0.3333333333333333148, 0.3333333333333333703, 0.3333333333333333148, 0.3333333333333334814, 0.3333333333333333148, 0.3333333333333333148, 0.3333333333333334259, 0.3333333333333333148, 0.3333333333333333148, 0.3333333333333334814, 0.3333333333333333148, 0.3333333333333334259, 0.3333333333333333703, 0.3333333333333333148, 0.3333333333333333703, 0.3333333333333334259, 0.3333333333333333148, 0.3333333333333334259, 0.3333333333333333148, 0.3333333333333333703, 0.3333333333333333148, 0.3333333333333333703, 0.3333333333333333703, 0.3333333333333333148, 0.3333333333333334259, 0.3333333333333334259, 0.3333333333333333148, 0.3333333333333333703, 0.3333333333333333703, 0.3333333333333334259, 0.3333333333333333703, 0.3333333333333333703, 0.3333333333333334259, 0.3333333333333333703, 0.3333333333333334259, 0.3333333333333333148, 0.3333333333333333703, 0.3333333333333333148, 0.3333333333333335369, 0.3333333333333333148, 0.3333333333333335369, 0.3333333333333333703, 0.3333333333333332593, 0.3333333333333334259, 0.3333333333333334259, 0.3333333333333333148, 0.3333333333333333703, 0.3333333333333333148, 0.3333333333333335369, 0.3333333333333333148, 0.3333333333333333703, 0.3333333333333333703, 0.3333333333333334259, 0.3333333333333334259, 0.3333333333333333703, 0.3333333333333334259, 0.3333333333333332593, 0.3333333333333334814, 0.3333333333333333148, 0.3333333333333333703, 0.3333333333333333148, 0.3333333333333333148, 0.3333333333333334259, 0.3333333333333332593, 0.3333333333333333148, 0.3333333333333333703, 0.3333333333333333148, 0.3333333333333333703, 0.3333333333333334259, 0.3333333333333333703, 0.3333333333333334259, 0.3333333333333333148, 0.3333333333333333703, 0.3333333333333333703, 0.3333333333333333703, 0.3333333333333333148, 0.3333333333333335369, 0.3333333333333333148, 0.3333333333333333703, 0.3333333333333333148, 0.3333333333333334259, 0.3333333333333334259, 0.3333333333333333703, 0.3333333333333334259, 0.3333333333333333703, 0.3333333333333333703, 0.3333333333333334259, 0.3333333333333333703, 0.3333333333333333703, 0.3333333333333333703, 0.3333333333333334259, 0.3333333333333333148, 0.3333333333333333148, 0.3333333333333335369, 0.3333333333333333148, 0.3333333333333334259, 0.3333333333333333148, 0.3333333333333334259, 0.3333333333333333703, 0.3333333333333333148, 0.3333333333333333148, 0.3333333333333333703, 0.3333333333333333148, 0.3333333333333334259, 0.3333333333333334259, 0.3333333333333332038, 0.3333333333333335369, 0.3333333333333333703, 0.3333333333333334259, 0.3333333333333334259, 0.3333333333333333703, 0.3333333333333334259, 0.3333333333333332593, 0.3333333333333334814, 0.3333333333333333703, 0.3333333333333334259, 0.3333333333333333148, 0.3333333333333333148, 0.3333333333333335369, 0.3333333333333332593, 0.3333333333333333703, 0.3333333333333332593, 0.3333333333333335369, 0.3333333333333333703, 0.3333333333333333703, 0.3333333333333333703, 0.3333333333333334259, 0.3333333333333332593, 0.3333333333333334814, 0.3333333333333332593, 0.3333333333333333703, 0.3333333333333333703, 0.3333333333333333703, 0.3333333333333334259, 0.3333333333333333148, 0.3333333333333334259, 0.3333333333333334259, 0.3333333333333333703, 0.3333333333333333148, 0.3333333333333334259, 0.3333333333333333148, 0.3333333333333333703, 0.3333333333333333148, 0.3333333333333333703, 0.3333333333333333703, 0.3333333333333333148, 0.3333333333333333703, 0.3333333333333333703, 0.3333333333333333703, 0.3333333333333334259, 0.3333333333333333703, 0.3333333333333333703, 0.3333333333333334814, 0.3333333333333332593, 0.3333333333333333703, 0.3333333333333334259, 0.3333333333333333148, 0.3333333333333334259, 0.3333333333333333703, 0.3333333333333334814, 0.3333333333333333703, 0.3333333333333333148, 0.3333333333333334259, 0.3333333333333333703, 0.3333333333333333703, 0.3333333333333333703, 0.3333333333333334259, 0.3333333333333333148, 0.3333333333333334259, 0.3333333333333333148, 0.3333333333333333148, 0.3333333333333335369, 0.3333333333333332038, 0.3333333333333335369, 0.3333333333333333148, 0.3333333333333333703, 0.3333333333333334259, 0.3333333333333333703, 0.3333333333333333148, 0.3333333333333333703, 0.3333333333333334259, 0.3333333333333333703, 0.3333333333333334259, 0.3333333333333333148, 0.3333333333333333703, 0.3333333333333334259, 0.3333333333333333148, 0.3333333333333333703, 0.3333333333333333703, 0.3333333333333333148, 0.3333333333333334259, 0.3333333333333334259, 0.3333333333333333703, 0.3333333333333335369, 0.3333333333333333148, 0.3333333333333333703, 0.3333333333333333703, 0.3333333333333333148, 0.3333333333333333703, 0.3333333333333333703, 0.3333333333333333703, 0.3333333333333333148, 0.3333333333333333703, 0.3333333333333334814, 0.3333333333333333703, 0.3333333333333333703, 0.3333333333333335369, 0.3333333333333333703, 0.3333333333333333703, 0.3333333333333334259, 0.3333333333333334259, 0.3333333333333333703, 0.3333333333333333703, 0.3333333333333333703, 0.3333333333333333703, 0.3333333333333333148, 0.3333333333333334259, 0.3333333333333333703, 0.3333333333333333703, 0.3333333333333333703, 0.3333333333333333148, 0.3333333333333334814, 0.3333333333333333148, 0.3333333333333333148, 0.3333333333333334814, 0.3333333333333333148, 0.3333333333333333148, 0.3333333333333334259, 0.3333333333333333148, 0.3333333333333334259, 0.3333333333333333148, 0.3333333333333334259, 0.3333333333333332593, 0.3333333333333335369, 0.3333333333333333148, 0.3333333333333333148, 0.3333333333333334259, 0.3333333333333333703, 0.3333333333333333703, 0.3333333333333333148, 0.3333333333333334259, 0.3333333333333333148, 0.3333333333333334259, 0.3333333333333333148, 0.3333333333333334259, 0.3333333333333334259, 0.3333333333333333703, 0.3333333333333334259, 0.3333333333333333703, 0.3333333333333333703, 0.3333333333333334259, 0.3333333333333333148, 0.3333333333333335369, 0.3333333333333334259, 0.3333333333333333148, 0.3333333333333333703, 0.3333333333333333148, 0.3333333333333334814, 0.3333333333333333703, 0.3333333333333333703, 0.3333333333333332593, 0.3333333333333334814, 0.3333333333333333703, 0.3333333333333333148, 0.3333333333333334259, 0.3333333333333332593, 0.3333333333333334814, 0.3333333333333333703, 0.3333333333333334259, 0.3333333333333333703, 0.3333333333333333148, 0.3333333333333333703, 0.3333333333333334259, 0.3333333333333333703, 0.3333333333333334259, 0.3333333333333333703, 0.3333333333333333703, 0.3333333333333333148, 0.3333333333333333148, 0.3333333333333333703, 0.3333333333333333703, 0.3333333333333333703, 0.3333333333333333703, 0.3333333333333333703, 0.3333333333333333148, 0.3333333333333334814, 0.3333333333333333148, 0.3333333333333334814, 0.3333333333333333703, 0.3333333333333334259, 0.3333333333333334259, 0.3333333333333333703, 0.3333333333333332593, 0.3333333333333333703, 0.3333333333333333703, 0.3333333333333333703, 0.3333333333333333148, 0.3333333333333333703, 0.3333333333333332593, 0.3333333333333334259, 0.3333333333333333703, 0.3333333333333333703),
 ( 0.3333333333333333703, 0.3333333333333333703, 0.3333333333333333703, 0.3333333333333333148, 0.3333333333333334259, 0.3333333333333334814, 0.3333333333333332593, 0.3333333333333332593, 0.3333333333333334814, 0.3333333333333333703, 0.3333333333333333703, 0.3333333333333334259, 0.3333333333333334259, 0.3333333333333334259, 0.3333333333333332593, 0.3333333333333334259, 0.3333333333333334259, 0.3333333333333333703, 0.3333333333333334259, 0.3333333333333332038, 0.3333333333333334259, 0.3333333333333333148, 0.3333333333333334259, 0.3333333333333333703, 0.3333333333333333703, 0.3333333333333334259, 0.3333333333333333148, 0.3333333333333334259, 0.3333333333333333703, 0.3333333333333333703, 0.3333333333333333148, 0.3333333333333334259, 0.3333333333333333703, 0.3333333333333333703, 0.3333333333333333148, 0.3333333333333333148, 0.3333333333333334259, 0.3333333333333333148, 0.3333333333333334259, 0.3333333333333333703, 0.3333333333333333703, 0.3333333333333333703, 0.3333333333333332593, 0.3333333333333334814, 0.3333333333333332593, 0.3333333333333333703, 0.3333333333333333703, 0.3333333333333333703, 0.3333333333333335369, 0.3333333333333332593, 0.3333333333333333703, 0.3333333333333335369, 0.3333333333333333703, 0.3333333333333333703, 0.3333333333333335369, 0.3333333333333333703, 0.3333333333333334259, 0.3333333333333334259, 0.3333333333333333703, 0.3333333333333333703, 0.3333333333333333703, 0.3333333333333333703, 0.3333333333333333703, 0.3333333333333333148, 0.3333333333333334259, 0.3333333333333334814, 0.3333333333333333148, 0.3333333333333333703, 0.3333333333333333148, 0.3333333333333334259, 0.3333333333333332593, 0.3333333333333334259, 0.3333333333333333703, 0.3333333333333334259, 0.3333333333333333703, 0.3333333333333333703, 0.3333333333333333703, 0.3333333333333333148, 0.3333333333333334814, 0.3333333333333332038, 0.3333333333333334259, 0.3333333333333334259, 0.3333333333333333148, 0.3333333333333334259, 0.3333333333333333703, 0.3333333333333333148, 0.3333333333333333703, 0.3333333333333333148, 0.3333333333333334814, 0.3333333333333333148, 0.3333333333333333148, 0.3333333333333334259, 0.3333333333333333148, 0.3333333333333333148, 0.3333333333333334814, 0.3333333333333333148, 0.3333333333333334259, 0.3333333333333333703, 0.3333333333333333148, 0.3333333333333333703, 0.3333333333333334259, 0.3333333333333333148, 0.3333333333333334259, 0.3333333333333333148, 0.3333333333333333703, 0.3333333333333333148, 0.3333333333333333703, 0.3333333333333333703, 0.3333333333333333148, 0.3333333333333334259, 0.3333333333333334259, 0.3333333333333333148, 0.3333333333333333703, 0.3333333333333333703, 0.3333333333333334259, 0.3333333333333333703, 0.3333333333333333703, 0.3333333333333334259, 0.3333333333333333703, 0.3333333333333334259, 0.3333333333333333148, 0.3333333333333333703, 0.3333333333333333148, 0.3333333333333335369, 0.3333333333333333148, 0.3333333333333335369, 0.3333333333333333703, 0.3333333333333332593, 0.3333333333333334259, 0.3333333333333334259, 0.3333333333333333148, 0.3333333333333333703, 0.3333333333333333148, 0.3333333333333335369, 0.3333333333333333148, 0.3333333333333333703, 0.3333333333333333703, 0.3333333333333334259, 0.3333333333333334259, 0.3333333333333333703, 0.3333333333333334259, 0.3333333333333332593, 0.3333333333333334814, 0.3333333333333333148, 0.3333333333333333703, 0.3333333333333333148, 0.3333333333333333148, 0.3333333333333334259, 0.3333333333333332593, 0.3333333333333333148, 0.3333333333333333703, 0.3333333333333333148, 0.3333333333333333703, 0.3333333333333334259, 0.3333333333333333703, 0.3333333333333334259, 0.3333333333333333148, 0.3333333333333333703, 0.3333333333333333703, 0.3333333333333333703, 0.3333333333333333148, 0.3333333333333335369, 0.3333333333333333148, 0.3333333333333333703, 0.3333333333333333148, 0.3333333333333334259, 0.3333333333333334259, 0.3333333333333333703, 0.3333333333333334259, 0.3333333333333333703, 0.3333333333333333703, 0.3333333333333334259, 0.3333333333333333703, 0.3333333333333333703, 0.3333333333333333703, 0.3333333333333334259, 0.3333333333333333148, 0.3333333333333333148, 0.3333333333333335369, 0.3333333333333333148, 0.3333333333333334259, 0.3333333333333333148, 0.3333333333333334259, 0.3333333333333333703, 0.3333333333333333148, 0.3333333333333333148, 0.3333333333333333703, 0.3333333333333333148, 0.3333333333333334259, 0.3333333333333334259, 0.3333333333333332038, 0.3333333333333335369, 0.3333333333333333703, 0.3333333333333334259, 0.3333333333333334259, 0.3333333333333333703, 0.3333333333333334259, 0.3333333333333332593, 0.3333333333333334814, 0.3333333333333333703, 0.3333333333333334259, 0.3333333333333333148, 0.3333333333333333148, 0.3333333333333335369, 0.3333333333333332593, 0.3333333333333333703, 0.3333333333333332593, 0.3333333333333335369, 0.3333333333333333703, 0.3333333333333333703, 0.3333333333333333703, 0.3333333333333334259, 0.3333333333333332593, 0.3333333333333334814, 0.3333333333333332593, 0.3333333333333333703, 0.3333333333333333703, 0.3333333333333333703, 0.3333333333333334259, 0.3333333333333333148, 0.3333333333333334259, 0.3333333333333334259, 0.3333333333333333703, 0.3333333333333333148, 0.3333333333333334259, 0.3333333333333333148, 0.3333333333333333703, 0.3333333333333333148, 0.3333333333333333703, 0.3333333333333333703, 0.3333333333333333148, 0.3333333333333333703, 0.3333333333333333703, 0.3333333333333333703, 0.3333333333333334259, 0.3333333333333333703, 0.3333333333333333703, 0.3333333333333334814, 0.3333333333333332593, 0.3333333333333333703, 0.3333333333333334259, 0.3333333333333333148, 0.3333333333333334259, 0.3333333333333333703, 0.3333333333333334814, 0.3333333333333333703, 0.3333333333333333148, 0.3333333333333334259, 0.3333333333333333703, 0.3333333333333333703, 0.3333333333333333703, 0.3333333333333334259, 0.3333333333333333148, 0.3333333333333334259, 0.3333333333333333148, 0.3333333333333333148, 0.3333333333333335369, 0.3333333333333332038, 0.3333333333333335369, 0.3333333333333333148, 0.3333333333333333703, 0.3333333333333334259, 0.3333333333333333703, 0.3333333333333333148, 0.3333333333333333703, 0.3333333333333334259, 0.3333333333333333703, 0.3333333333333334259, 0.3333333333333333148, 0.3333333333333333703, 0.3333333333333334259, 0.3333333333333333148, 0.3333333333333333703, 0.3333333333333333703, 0.3333333333333333148, 0.3333333333333334259, 0.3333333333333334259, 0.3333333333333333703, 0.3333333333333335369, 0.3333333333333333148, 0.3333333333333333703, 0.3333333333333333703, 0.3333333333333333148, 0.3333333333333333703, 0.3333333333333333703, 0.3333333333333333703, 0.3333333333333333148, 0.3333333333333333703, 0.3333333333333334814, 0.3333333333333333703, 0.3333333333333333703, 0.3333333333333335369, 0.3333333333333333703, 0.3333333333333333703, 0.3333333333333334259, 0.3333333333333334259, 0.3333333333333333703, 0.3333333333333333703, 0.3333333333333333703, 0.3333333333333333703, 0.3333333333333333148, 0.3333333333333334259, 0.3333333333333333703, 0.3333333333333333703, 0.3333333333333333703, 0.3333333333333333148, 0.3333333333333334814, 0.3333333333333333148, 0.3333333333333333148, 0.3333333333333334814, 0.3333333333333333148, 0.3333333333333333148, 0.3333333333333334259, 0.3333333333333333148, 0.3333333333333334259, 0.3333333333333333148, 0.3333333333333334259, 0.3333333333333332593, 0.3333333333333335369, 0.3333333333333333148, 0.3333333333333333148, 0.3333333333333334259, 0.3333333333333333703, 0.3333333333333333703, 0.3333333333333333148, 0.3333333333333334259, 0.3333333333333333148, 0.3333333333333334259, 0.3333333333333333148, 0.3333333333333334259, 0.3333333333333334259, 0.3333333333333333703, 0.3333333333333334259, 0.3333333333333333703, 0.3333333333333333703, 0.3333333333333334259, 0.3333333333333333148, 0.3333333333333335369, 0.3333333333333334259, 0.3333333333333333148, 0.3333333333333333703, 0.3333333333333333148, 0.3333333333333334814, 0.3333333333333333703, 0.3333333333333333703, 0.3333333333333332593, 0.3333333333333334814, 0.3333333333333333703, 0.3333333333333333148, 0.3333333333333334259, 0.3333333333333332593, 0.3333333333333334814, 0.3333333333333333703, 0.3333333333333334259, 0.3333333333333333703, 0.3333333333333333148, 0.3333333333333333703, 0.3333333333333334259, 0.3333333333333333703, 0.3333333333333334259, 0.3333333333333333703, 0.3333333333333333703, 0.3333333333333333148, 0.3333333333333333148, 0.3333333333333333703, 0.3333333333333333703, 0.3333333333333333703, 0.3333333333333333703, 0.3333333333333333703, 0.3333333333333333148, 0.3333333333333334814, 0.3333333333333333148, 0.3333333333333334814, 0.3333333333333333703, 0.3333333333333334259, 0.3333333333333334259, 0.3333333333333333703, 0.3333333333333332593, 0.3333333333333333703, 0.3333333333333333703, 0.3333333333333333703, 0.3333333333333333148, 0.3333333333333333703, 0.3333333333333332593, 0.3333333333333334259, 0.3333333333333333703, 0.3333333333333333703),
 ( 1.000000000000000000, 1.000000000000000000, 1.000000000000000000, 0.9999999999999997780, 1.000000000000000000, 1.000000000000000444, 0.9999999999999996669, 0.9999999999999996669, 1.000000000000000444, 1.000000000000000000, 1.000000000000000000, 1.000000000000000000, 1.000000000000000222, 1.000000000000000222, 0.9999999999999997780, 1.000000000000000000, 1.000000000000000222, 1.000000000000000000, 1.000000000000000222, 0.9999999999999994449, 1.000000000000000222, 0.9999999999999997780, 1.000000000000000444, 1.000000000000000000, 1.000000000000000000, 1.000000000000000222, 0.9999999999999997780, 1.000000000000000222, 1.000000000000000000, 1.000000000000000222, 0.9999999999999997780, 1.000000000000000000, 1.000000000000000000, 0.9999999999999997780, 1.000000000000000000, 1.000000000000000000, 1.000000000000000222, 1.000000000000000000, 0.9999999999999997780, 1.000000000000000222, 0.9999999999999997780, 1.000000000000000000, 0.9999999999999997780, 1.000000000000000444, 0.9999999999999996669, 1.000000000000000222, 1.000000000000000000, 1.000000000000000000, 1.000000000000000444, 0.9999999999999996669, 1.000000000000000222, 1.000000000000000444, 1.000000000000000000, 0.9999999999999997780, 1.000000000000000444, 1.000000000000000222, 1.000000000000000000, 1.000000000000000000, 1.000000000000000222, 1.000000000000000000, 1.000000000000000222, 0.9999999999999997780, 1.000000000000000222, 1.000000000000000000, 1.000000000000000000, 1.000000000000000444, 0.9999999999999996669, 1.000000000000000000, 0.9999999999999997780, 1.000000000000000222, 0.9999999999999996669, 1.000000000000000000, 1.000000000000000222, 0.9999999999999997780, 1.000000000000000444, 0.9999999999999997780, 1.000000000000000000, 0.9999999999999997780, 1.000000000000000222, 0.9999999999999996669, 1.000000000000000000, 1.000000000000000222, 0.9999999999999996669, 1.000000000000000444, 0.9999999999999997780, 1.000000000000000000, 1.000000000000000222, 0.9999999999999996669, 1.000000000000000222, 1.000000000000000000, 0.9999999999999997780, 1.000000000000000222, 0.9999999999999997780, 1.000000000000000000, 1.000000000000000222, 0.9999999999999997780, 1.000000000000000000, 1.000000000000000000, 0.9999999999999997780, 1.000000000000000000, 1.000000000000000222, 0.9999999999999997780, 1.000000000000000000, 1.000000000000000000, 1.000000000000000000, 0.9999999999999997780, 1.000000000000000222, 0.9999999999999997780, 0.9999999999999997780, 1.000000000000000444, 1.000000000000000000, 1.000000000000000000, 0.9999999999999997780, 1.000000000000000222, 1.000000000000000000, 1.000000000000000000, 1.000000000000000000, 1.000000000000000000, 1.000000000000000222, 1.000000000000000222, 0.9999999999999997780, 1.000000000000000000, 0.9999999999999997780, 1.000000000000000444, 0.9999999999999996669, 1.000000000000000666, 1.000000000000000000, 0.9999999999999997780, 1.000000000000000222, 1.000000000000000000, 1.000000000000000000, 1.000000000000000000, 0.9999999999999994449, 1.000000000000000666, 0.9999999999999996669, 1.000000000000000000, 1.000000000000000222, 0.9999999999999997780, 1.000000000000000222, 0.9999999999999997780, 1.000000000000000222, 0.9999999999999996669, 1.000000000000000444, 1.000000000000000000, 1.000000000000000222, 0.9999999999999996669, 1.000000000000000000, 1.000000000000000222, 0.9999999999999997780, 1.000000000000000000, 0.9999999999999997780, 1.000000000000000000, 1.000000000000000000, 1.000000000000000222, 0.9999999999999997780, 1.000000000000000222, 0.9999999999999997780, 1.000000000000000000, 1.000000000000000000, 1.000000000000000222, 0.9999999999999997780, 1.000000000000000444, 1.000000000000000000, 0.9999999999999997780, 1.000000000000000000, 1.000000000000000000, 1.000000000000000222, 0.9999999999999997780, 1.000000000000000222, 1.000000000000000000, 1.000000000000000000, 1.000000000000000000, 1.000000000000000222, 1.000000000000000000, 0.9999999999999997780, 1.000000000000000000, 1.000000000000000000, 1.000000000000000000, 1.000000000000000444, 0.9999999999999996669, 1.000000000000000222, 1.000000000000000000, 1.000000000000000222, 0.9999999999999997780, 1.000000000000000000, 0.9999999999999997780, 1.000000000000000000, 0.9999999999999997780, 1.000000000000000000, 1.000000000000000444, 0.9999999999999994449, 1.000000000000000444, 1.000000000000000000, 1.000000000000000222, 1.000000000000000222, 0.9999999999999997780, 1.000000000000000222, 0.9999999999999997780, 1.000000000000000222, 1.000000000000000222, 1.000000000000000222, 0.9999999999999997780, 1.000000000000000000, 1.000000000000000444, 0.9999999999999996669, 1.000000000000000000, 0.9999999999999997780, 1.000000000000000222, 1.000000000000000222, 1.000000000000000000, 0.9999999999999997780, 1.000000000000000222, 0.9999999999999997780, 1.000000000000000222, 0.9999999999999997780, 0.9999999999999997780, 1.000000000000000000, 1.000000000000000000, 1.000000000000000000, 1.000000000000000000, 1.000000000000000000, 1.000000000000000222, 1.000000000000000000, 1.000000000000000000, 1.000000000000000222, 1.000000000000000000, 0.9999999999999997780, 1.000000000000000000, 1.000000000000000000, 1.000000000000000000, 0.9999999999999997780, 1.000000000000000000, 0.9999999999999997780, 1.000000000000000000, 1.000000000000000222, 0.9999999999999996669, 1.000000000000000444, 1.000000000000000000, 0.9999999999999997780, 1.000000000000000222, 1.000000000000000000, 0.9999999999999997780, 1.000000000000000222, 1.000000000000000000, 1.000000000000000222, 1.000000000000000000, 0.9999999999999997780, 1.000000000000000222, 1.000000000000000000, 1.000000000000000000, 1.000000000000000222, 1.000000000000000000, 1.000000000000000000, 1.000000000000000222, 0.9999999999999997780, 0.9999999999999996669, 1.000000000000000444, 0.9999999999999994449, 1.000000000000000444, 0.9999999999999997780, 1.000000000000000222, 1.000000000000000000, 1.000000000000000000, 1.000000000000000000, 1.000000000000000000, 1.000000000000000444, 0.9999999999999996669, 1.000000000000000444, 1.000000000000000000, 0.9999999999999997780, 1.000000000000000444, 0.9999999999999994449, 1.000000000000000444, 0.9999999999999997780, 0.9999999999999997780, 1.000000000000000222, 1.000000000000000444, 0.9999999999999997780, 1.000000000000000444, 0.9999999999999997780, 1.000000000000000000, 1.000000000000000444, 0.9999999999999997780, 0.9999999999999997780, 1.000000000000000000, 1.000000000000000000, 1.000000000000000000, 0.9999999999999997780, 1.000000000000000444, 1.000000000000000222, 0.9999999999999997780, 1.000000000000000444, 1.000000000000000000, 1.000000000000000222, 1.000000000000000000, 1.000000000000000000, 1.000000000000000222, 0.9999999999999997780, 1.000000000000000222, 1.000000000000000222, 0.9999999999999997780, 1.000000000000000222, 1.000000000000000000, 1.000000000000000000, 1.000000000000000222, 0.9999999999999997780, 1.000000000000000444, 0.9999999999999997780, 0.9999999999999997780, 1.000000000000000222, 0.9999999999999997780, 1.000000000000000000, 1.000000000000000000, 0.9999999999999997780, 1.000000000000000222, 0.9999999999999996669, 1.000000000000000444, 0.9999999999999997780, 1.000000000000000222, 1.000000000000000222, 0.9999999999999997780, 1.000000000000000222, 0.9999999999999997780, 1.000000000000000000, 0.9999999999999997780, 1.000000000000000444, 0.9999999999999996669, 1.000000000000000222, 0.9999999999999996669, 1.000000000000000444, 1.000000000000000000, 0.9999999999999997780, 1.000000000000000222, 0.9999999999999996669, 1.000000000000000222, 1.000000000000000222, 0.9999999999999996669, 1.000000000000000444, 1.000000000000000222, 0.9999999999999997780, 1.000000000000000222, 0.9999999999999997780, 1.000000000000000222, 1.000000000000000000, 1.000000000000000222, 0.9999999999999996669, 1.000000000000000444, 1.000000000000000000, 1.000000000000000000, 1.000000000000000222, 0.9999999999999997780, 0.9999999999999997780, 1.000000000000000444, 1.000000000000000000, 1.000000000000000000, 0.9999999999999996669, 1.000000000000000000, 1.000000000000000222, 1.000000000000000000, 1.000000000000000000, 1.000000000000000222, 0.9999999999999997780, 1.000000000000000000, 0.9999999999999997780, 0.9999999999999997780, 1.000000000000000222, 0.9999999999999997780, 1.000000000000000000, 1.000000000000000000, 0.9999999999999997780, 1.000000000000000222, 1.000000000000000000, 1.000000000000000222, 1.000000000000000000, 1.000000000000000444, 1.000000000000000000, 1.000000000000000000, 0.9999999999999997780, 0.9999999999999997780, 1.000000000000000222, 1.000000000000000000, 1.000000000000000000, 1.000000000000000000, 0.9999999999999997780, 1.000000000000000222, 1.000000000000000000, 1.000000000000000000) ) ) 
 REPRESENTATION_ITEM ( '' )  SURFACE ( )  );
#124801=CARTESIAN_POINT ( 'NONE',  ( 0.7308274648059713829, -1.853293357156562404, -0.6670056901108140091 ) ) ;
#124802=CARTESIAN_POINT ( 'NONE',  ( 2.296341162515431744, 1.558512652156778699, -1.158513924970270059 ) ) ;
#124806=CARTESIAN_POINT ( 'NONE',  ( 6.702007135557183304, 0.7127468228822000373, -1.719244972783180225 ) ) ;
#124810=CARTESIAN_POINT ( 'NONE',  ( 3.034921719543516971, -1.931671641359738567, 1.035203715903771915 ) ) ;
#124813=CARTESIAN_POINT ( 'NONE',  ( 2.859763506297557711, 1.816872213737670938, -0.1792109616642542924 ) ) ;
#124817=CARTESIAN_POINT ( 'NONE',  ( 1.119610834840406577, -1.879747399699664978, 0.4211694731556160365 ) ) ;
#124818=CARTESIAN_POINT ( 'NONE',  ( 5.401206054008879320, -1.684469800357458302, 1.005230755432365175 ) ) ;
#124822=CARTESIAN_POINT ( 'NONE',  ( 4.476244563333130699, -2.125884358948509689, -0.5320566845071761364 ) ) ;
#124825=CARTESIAN_POINT ( 'NONE',  ( 5.559458666840932928, 1.689222788819956245, 1.196583256836199149 ) ) ;
#124828=CARTESIAN_POINT ( 'NONE',  ( 4.852278370791485607, 0.2271405875100707961, -2.287421213010778942 ) ) ;
#124832=CARTESIAN_POINT ( 'NONE',  ( 0.09422489544355044933, -2.291893678819735491, -0.04953789299679511871 ) ) ;
#124835=CARTESIAN_POINT ( 'NONE',  ( 4.927648248775200912, 0.9969592527751047761, -1.666372862991059245 ) ) ;
#124839=CARTESIAN_POINT ( 'NONE',  ( 5.660397963661894849, 1.910509065610028090, 0.08734628876111423523 ) ) ;
#124840=CARTESIAN_POINT ( 'NONE',  ( 6.247054435025749086, -1.454095476552646593, 0.9272665607438534963 ) ) ;
#124841=CARTESIAN_POINT ( 'NONE',  ( 5.524625123954316486, 0.3981063221985549072, 1.976670730632006601 ) ) ;
#124845=CARTESIAN_POINT ( 'NONE',  ( 1.992240001063511290, -0.5588421479580056861, -2.014483121414586186 ) ) ;
#124846=CARTESIAN_POINT ( 'NONE',  ( 0.6019893773144822102, -0.5904995772347610972, -1.668576399176853853 ) ) ;
#124847=CARTESIAN_POINT ( 'NONE',  ( 5.748672702226536479, 1.986101125435947301, -0.3474646712962395911 ) ) ;
#124848=ADVANCED_FACE ( 'NONE', ( #50560 ), #192374, .F. ) ;
#124850=CARTESIAN_POINT ( 'NONE',  ( 2.748291532463055020, 0.7732563850255981253, 2.158024254592408209 ) ) ;
#124851=CARTESIAN_POINT ( 'NONE',  ( 1.974151807821213245, -0.08369685440555743594, -1.738446472377056740 ) ) ;
#124855=CARTESIAN_POINT ( 'NONE',  ( 2.741176079829604539, -1.657949034129829302, -0.5072451560675111937 ) ) ;
#124857=CARTESIAN_POINT ( 'NONE',  ( 1.715070751487054013, -1.593955780799067412, -0.9604075334226671590 ) ) ;
#124858=CARTESIAN_POINT ( 'NONE',  ( 2.506498380571024143, 2.170641363890627229, 0.05523593993728668355 ) ) ;
#124859=CARTESIAN_POINT ( 'NONE',  ( 4.012907874177486178, 0.1037781579101039742, 2.014008197856680393 ) ) ;
#124860=CARTESIAN_POINT ( 'NONE',  ( 4.156250000000002665, -1.895863743163992199, 0.7852924748302037017 ) ) ;
#124862=CARTESIAN_POINT ( 'NONE',  ( 0.5867820057828515568, -0.2326963965399355405, -1.912219011898611765 ) ) ;
#124864=CARTESIAN_POINT ( 'NONE',  ( 3.779691724966814270, 0.2693221142107836696, -2.204936161957889329 ) ) ;
#124870=CARTESIAN_POINT ( 'NONE',  ( 5.906509255234578148, -2.210603606603298132, -0.2184946463264207661 ) ) ;
#124872=CARTESIAN_POINT ( 'NONE',  ( 4.562918044398325712, 1.517878595006398212, -1.242988302126393663 ) ) ;
#124876=CARTESIAN_POINT ( 'NONE',  ( 5.817715961848279882, -2.209163325107537101, 0.4873710261694869095 ) ) ;
#124879=CARTESIAN_POINT ( 'NONE',  ( 1.838405449727827268, -1.105357634037696046, 1.741336484761913272 ) ) ;
#124885=CARTESIAN_POINT ( 'NONE',  ( 4.077312411328878561, 1.762187477035919603, -0.6278270876356045749 ) ) ;
#124886=CARTESIAN_POINT ( 'NONE',  ( 3.058897358425614055, -1.030606816589432873, 1.394497854932384762 ) ) ;
#124887=CARTESIAN_POINT ( 'NONE',  ( 0.02941885139840036759, -2.092310700284722103, 0.9370380844745775928 ) ) ;
#124888=CARTESIAN_POINT ( 'NONE',  ( 1.220068447022312652, -2.152735442661047216, 0.4846846590640523367 ) ) ;
#124889=CARTESIAN_POINT ( 'NONE',  ( 4.388279639374990104, -0.4598052185818923832, -2.039381826187444791 ) ) ;
#124890=CARTESIAN_POINT ( 'NONE',  ( 5.648367429523982963, -1.529681991043756017, 1.196244224141077561 ) ) ;
#124893=CARTESIAN_POINT ( 'NONE',  ( 0.2812500008225146120, 0.7852924545924094835, 1.895863743164083681 ) ) ;
#124894=CARTESIAN_POINT ( 'NONE',  ( 0.01820432788856435335, -1.842448466851685840, 0.8197770699841927522 ) ) ;
#124901=CARTESIAN_POINT ( 'NONE',  ( 4.512205841073367196, -0.7830535718562798841, -1.649371741558727678 ) ) ;
#124902=CARTESIAN_POINT ( 'NONE',  ( 1.887996149947854807, 1.521953097117642706, 1.598203399828190152 ) ) ;
#124907=CARTESIAN_POINT ( 'NONE',  ( 1.371359653073561891, -1.734546099648653472, -1.034550878434212784 ) ) ;
#124910=CARTESIAN_POINT ( 'NONE',  ( 2.975287861635074194, -0.1872683251897942214, 1.851525965346143554 ) ) ;
#124915=( GEOMETRIC_REPRESENTATION_CONTEXT ( 3 ) GLOBAL_UNCERTAINTY_ASSIGNED_CONTEXT ( ( #80768 ) ) GLOBAL_UNIT_ASSIGNED_CONTEXT ( ( #78182, #46779, #162650 ) ) REPRESENTATION_CONTEXT ( 'NONE', 'WORKASPACE' ) );
#124917=CARTESIAN_POINT ( 'NONE',  ( 4.055160972438559774, -1.518969423100406946, -1.012540670841777013 ) ) ;
#124922=CARTESIAN_POINT ( 'NONE',  ( 0.7899210882133401723, -1.648783996043493350, 0.5366646198887611297 ) ) ;
#124923=CARTESIAN_POINT ( 'NONE',  ( 5.912015133600425187, 1.233162958052456348, -1.367321061651972869 ) ) ;
#124925=CARTESIAN_POINT ( 'NONE',  ( 4.494930827260392725, -0.5027447494639860626, -2.252120713733107404 ) ) ;
#124927=CARTESIAN_POINT ( 'NONE',  ( 6.643834073375672666, 0.8340821395082242962, -1.994398315854857495 ) ) ;
#124929=CARTESIAN_POINT ( 'NONE',  ( 5.501416862357105586, 2.263058191380825424, 0.4008149593560642598 ) ) ;
#124932=CARTESIAN_POINT ( 'NONE',  ( 5.348468966913380029, 0.5439794105128460400, 1.789823788735760646 ) ) ;
#124934=CARTESIAN_POINT ( 'NONE',  ( 2.707167837304753633, 1.638089068140319071, -0.9866689735503200165 ) ) ;
#124936=CARTESIAN_POINT ( 'NONE',  ( 3.492985898914053866, -0.4302566696539159574, -2.164365734511737305 ) ) ;
#124937=CARTESIAN_POINT ( 'NONE',  ( 4.821547164884887771, -1.499609098395672246, -1.495007082409164356 ) ) ;
#124940=CARTESIAN_POINT ( 'NONE',  ( 6.983263157960371892, 7.629137130509070275, 2.546189081643289942 ) ) ;
#124941=CARTESIAN_POINT ( 'NONE',  ( -0.2110808730066962846, 5.724502961415374180, -2.391230805320884834 ) ) ;
#124944=CARTESIAN_POINT ( 'NONE',  ( 1.975998049093165232, 2.207973392102855925, -0.6707195784038646469 ) ) ;
#124945=CARTESIAN_POINT ( 'NONE',  ( 2.435929278166943490, 1.204617592564939166, 1.548422000036096202 ) ) ;
#124947=CARTESIAN_POINT ( 'NONE',  ( 6.649293052619501765, 1.797374026962361482, -1.011582863395175114 ) ) ;
#124951=CARTESIAN_POINT ( 'NONE',  ( 4.522672878804367969, 0.3494810548456111499, 1.985869246038343583 ) ) ;
#124956=CARTESIAN_POINT ( 'NONE',  ( 2.518641040286667465, 0.9249485440519630286, 1.964284900515224530 ) ) ;
#124960=CARTESIAN_POINT ( 'NONE',  ( 2.354581831802166736, -1.448805955455864769, 1.183207591018392568 ) ) ;
#124961=CARTESIAN_POINT ( 'NONE',  ( 1.264995835974036975, -1.861883480270887903, -0.8836341380922418942 ) ) ;
#124962=DIRECTION ( 'NONE',  ( 1.039099362110107450E-15, 1.000000000000000000, -4.583713267641621330E-32 ) ) ;
#124963=CARTESIAN_POINT ( 'NONE',  ( 6.727182134110257117, 2.064761932694148872, 2.218145506119094890 ) ) ;
#124967=CARTESIAN_POINT ( 'NONE',  ( 2.947808941170467545, -1.285945688040548207, -1.415481726668985196 ) ) ;
#124968=CARTESIAN_POINT ( 'NONE',  ( 5.313276456144085280, -0.2569279779609782155, 1.750970204404985964 ) ) ;
#124969=CARTESIAN_POINT ( 'NONE',  ( 1.734869227892420707, 1.784761669998648381, 0.6870963898520031643 ) ) ;
#124972=CARTESIAN_POINT ( 'NONE',  ( 0.1806861152609346710, 1.591142543434557632, -1.066548322639774504 ) ) ;
#124974=CARTESIAN_POINT ( 'NONE',  ( 0.6782873735513493818, -1.106163567672680204, -1.749894625276714688 ) ) ;
#124976=CARTESIAN_POINT ( 'NONE',  ( 5.928550619183988957, 1.803260976426118489, 0.4972845834502263584 ) ) ;
#124977=CARTESIAN_POINT ( 'NONE',  ( 2.209345402013741300, -0.4006574107652469130, 1.781019818369505847 ) ) ;
#124978=CARTESIAN_POINT ( 'NONE',  ( 5.356176587289051660, 2.204499490778097481, -0.1052899746726426722 ) ) ;
#124982=CARTESIAN_POINT ( 'NONE',  ( 2.682143534289625375, -1.185536078076434796, -1.687771684069488076 ) ) ;
#124987=CARTESIAN_POINT ( 'NONE',  ( 0.4566077865506939504, 0.8268718848777978359, 1.997384878126715391 ) ) ;
#124989=CARTESIAN_POINT ( 'NONE',  ( 4.967269779104159788, 1.799668380515653920, 1.023422521214325309 ) ) ;
#124991=CARTESIAN_POINT ( 'NONE',  ( 2.442841770826277514, 0.4709965094221583159, 2.109507199432036018 ) ) ;
#124993=CARTESIAN_POINT ( 'NONE',  ( 3.035811672558884400, -1.945802561663440455, 0.5409189654149139104 ) ) ;
#124994=CARTESIAN_POINT ( 'NONE',  ( 2.207404936347991065, -1.573848641742966459, -1.171066219227391070 ) ) ;
#124995=CARTESIAN_POINT ( 'NONE',  ( 6.620655732516642189, 2.417337544263608251, 2.554705107920357321 ) ) ;
#125001=CARTESIAN_POINT ( 'NONE',  ( 0.9543149826918421175, -1.275552737861269437, 1.561884623745241951 ) ) ;
#125003=CARTESIAN_POINT ( 'NONE',  ( 6.603104432341277530, -0.4828188497946246382, 2.145653685147373313 ) ) ;
#125005=CARTESIAN_POINT ( 'NONE',  ( 5.888906298306327614, -1.818048641159516254, -0.5935555146628914702 ) ) ;
#125009=CARTESIAN_POINT ( 'NONE',  ( 3.550407796516129366, -1.352142120786763213, 1.496064415113136592 ) ) ;
#125012=CARTESIAN_POINT ( 'NONE',  ( 6.106443901014584341, -0.6257089282217034309, -1.607472872393211683 ) ) ;
#125017=CARTESIAN_POINT ( 'NONE',  ( 4.200366636497298245, -0.5845007089231197828, -1.776970133648393624 ) ) ;
#125019=CARTESIAN_POINT ( 'NONE',  ( 1.375928118113247445, -2.020660359122231409, 0.4497719141252009556 ) ) ;
#125023=CARTESIAN_POINT ( 'NONE',  ( 0.08751785467620704084, -0.5350655163729299835, 1.944078888069140865 ) ) ;
#125025=CARTESIAN_POINT ( 'NONE',  ( 0.4393641590584134171, -1.719983824569010444, 0.5688467837753272693 ) ) ;
#125030=CARTESIAN_POINT ( 'NONE',  ( 0.8011316787140990714, -1.684513426579350659, 1.005393624328714264 ) ) ;
#125032=CARTESIAN_POINT ( 'NONE',  ( 4.780823714695519477, 1.590225366507077354, -1.067722475238532365 ) ) ;
#125040=CARTESIAN_POINT ( 'NONE',  ( 3.010779355932476253, 1.566693023359872372, -1.489686202715050145 ) ) ;
#125045=CARTESIAN_POINT ( 'NONE',  ( 4.418855976699648025, 1.669273799801282765, 0.7395231729718022562 ) ) ;
#125047=CARTESIAN_POINT ( 'NONE',  ( 1.493369529629706705, 1.490176471889271603, 1.290657618255620864 ) ) ;
#125048=CARTESIAN_POINT ( 'NONE',  ( 3.955252344019274169, -1.661368509396843995, 0.9470704235666274062 ) ) ;
#125051=CARTESIAN_POINT ( 'NONE',  ( 4.914487397858644080, 0.7518983826605809551, 1.820584232156793769 ) ) ;
#125053=CARTESIAN_POINT ( 'NONE',  ( 6.233930015136599501, 1.921560620327814606, 0.2806146417165931717 ) ) ;
#125057=CARTESIAN_POINT ( 'NONE',  ( 6.381110825713084189, -1.939362502171553482, -0.8581636585355473246 ) ) ;
#125059=CARTESIAN_POINT ( 'NONE',  ( 3.580628178849315280, -1.282259035790348722, 1.418852674340838060 ) ) ;
#125063=CARTESIAN_POINT ( 'NONE',  ( 5.022139790744326149, -2.003173700978663874, 0.1997323756105211789 ) ) ;
#125066=CARTESIAN_POINT ( 'NONE',  ( 6.410779360540267646, 1.349177972556347971, -1.230185023894624141 ) ) ;
#125067=CARTESIAN_POINT ( 'NONE',  ( 2.066927875543830950, 1.535623996113824496, -1.388825173883188713 ) ) ;
#125072=CARTESIAN_POINT ( 'NONE',  ( 6.420764531294745225, 1.746252128813120086, 0.6712297951826234899 ) ) ;
#125079=CARTESIAN_POINT ( 'NONE',  ( 6.825078400183526739, -0.0002198122173602961866, 1.955566246027613531 ) ) ;
#125081=CARTESIAN_POINT ( 'NONE',  ( 4.834428552630634535, 0.5376618173574229109, -1.648781088846348108 ) ) ;
#125083=CARTESIAN_POINT ( 'NONE',  ( 2.764580022184208730, -0.7881864689132519475, -1.914544693583389634 ) ) ;
#125084=CARTESIAN_POINT ( 'NONE',  ( 3.163770493730236666, 1.345063228294058000, 1.635049775249038051 ) ) ;
#125087=CARTESIAN_POINT ( 'NONE',  ( 2.254690153889327586, -0.5205305878250593432, -1.899364841092534339 ) ) ;
#125091=CARTESIAN_POINT ( 'NONE',  ( 4.154423454741348110, -1.699848520643287175, 1.538017723768041023 ) ) ;
#125092=CARTESIAN_POINT ( 'NONE',  ( 1.734698295210383767, 0.1775668987445792879, 1.817036636966688823 ) ) ;
#125096=CARTESIAN_POINT ( 'NONE',  ( 2.724860606552154785, 1.455292111517191511, -1.391298800531393765 ) ) ;
#125097=CARTESIAN_POINT ( 'NONE',  ( 2.254674508890702089, -0.5182927192734412269, -1.892014123021222627 ) ) ;
#125100=CARTESIAN_POINT ( 'NONE',  ( 0.1751657365761885576, 5.722053558346082092, -2.638081460773045617 ) ) ;
#125101=CARTESIAN_POINT ( 'NONE',  ( 5.121074860632232273, -1.985326386471301552, 0.6553513102709652705 ) ) ;
#125102=CARTESIAN_POINT ( 'NONE',  ( 3.766244448481158802, -1.188900867318806176, 1.311211162958977328 ) ) ;
#125105=CARTESIAN_POINT ( 'NONE',  ( 6.386719491623852996, 1.997645938776301477, -1.124140632904375936 ) ) ;
#125106=CARTESIAN_POINT ( 'NONE',  ( 5.331890987662370129, 1.715487909331077310, 0.2919898797263379975 ) ) ;
#125108=CARTESIAN_POINT ( 'NONE',  ( 6.153027625867640182, 1.178261263523974645, 1.973664585577431518 ) ) ;
#125109=CARTESIAN_POINT ( 'NONE',  ( 0.1333692844072802142, 2.017199222642913625, -2.468757726274827036 ) ) ;
#125110=CARTESIAN_POINT ( 'NONE',  ( 5.712138547670210009, -1.368237114983595237, -1.064765744168968187 ) ) ;
#125111=CARTESIAN_POINT ( 'NONE',  ( 5.687976231080541289, -1.372897218612447290, -1.682037316681925132 ) ) ;
#125113=CARTESIAN_POINT ( 'NONE',  ( 0.07561343334091479018, 1.573685453729951833, 1.416787448489342127 ) ) ;
#125114=CARTESIAN_POINT ( 'NONE',  ( 5.281250000000004441, 0.7852924748302615443, 1.895863743163964665 ) ) ;
#125115=CARTESIAN_POINT ( 'NONE',  ( 6.827182134110224787, 2.426453598513299337, 2.470348285387702347 ) ) ;
#125116=CARTESIAN_POINT ( 'NONE',  ( 3.909137014540211119, 1.651653515444248876, 0.9912706138347370244 ) ) ;
#125118=CARTESIAN_POINT ( 'NONE',  ( 0.5225339808294949817, -2.210013125053798433, 0.2238140636349055246 ) ) ;
#125123=CARTESIAN_POINT ( 'NONE',  ( 2.579030809547431247, -1.529751724882743247, 1.610829425214066246 ) ) ;
#125128=CARTESIAN_POINT ( 'NONE',  ( 0.6158615555539399544, 0.1511424999406512648, 2.010826230049263863 ) ) ;
#125130=CARTESIAN_POINT ( 'NONE',  ( 5.266109189975630045, -2.053049664954803788, 0.1989083462991206031 ) ) ;
#125136=CARTESIAN_POINT ( 'NONE',  ( 1.774285776001020221, -1.678457933910833644, -0.5611888468203419800 ) ) ;
#125137=CARTESIAN_POINT ( 'NONE',  ( 0.03578008775950020093, -1.617816776142148250, 1.203357013023528932 ) ) ;
#125138=CARTESIAN_POINT ( 'NONE',  ( 5.776847720190436242, 1.604795045139913556, -0.6741588622883755155 ) ) ;
#125139=CARTESIAN_POINT ( 'NONE',  ( 3.913864042289341150, -1.178888685321772156, -1.965896434285055117 ) ) ;
#125141=CARTESIAN_POINT ( 'NONE',  ( 2.202840038917678545, -0.4038221959529255112, 1.796142596185656526 ) ) ;
#125145=CARTESIAN_POINT ( 'NONE',  ( 3.188313505853744179, -1.798300186086329688, -0.3134973320952222364 ) ) ;
#125146=CARTESIAN_POINT ( 'NONE',  ( 4.131482539099665452, 0.5404898895830790861, 1.942541833525657680 ) ) ;
#125148=CARTESIAN_POINT ( 'NONE',  ( 2.800010096142038218, -0.7105090101824761417, 2.148112714708799942 ) ) ;
#125149=CARTESIAN_POINT ( 'NONE',  ( 5.420966337283807945, 1.944620675078809757, 0.8088979906116978702 ) ) ;
#125151=CARTESIAN_POINT ( 'NONE',  ( 2.260293373024503616, -2.069953001785612479, 0.04851313490940312168 ) ) ;
#125154=CARTESIAN_POINT ( 'NONE',  ( 4.371814246616528621, 0.4635510597098578267, -2.069045912693792566 ) ) ;
#125156=CARTESIAN_POINT ( 'NONE',  ( 0.5043604530000692643, -0.6477430859608296343, -1.814464506502324159 ) ) ;
#125162=CARTESIAN_POINT ( 'NONE',  ( 5.836213162209912930, -1.179542664122106510, -1.762073437084572314 ) ) ;
#125163=CARTESIAN_POINT ( 'NONE',  ( 1.729655969393493642, -1.983145177596838948, 0.7090631796887718608 ) ) ;
#125166=CARTESIAN_POINT ( 'NONE',  ( 6.332830178222744522, -1.766687566082520533, -0.5848361604409312298 ) ) ;
#125171=CARTESIAN_POINT ( 'NONE',  ( 0.3520121086563637314, -1.504009422257305495, -1.495223887398588358 ) ) ;
#125173=CARTESIAN_POINT ( 'NONE',  ( 3.103904542773823660, 0.7086415210641981988, -1.829580771271981154 ) ) ;
#125174=CARTESIAN_POINT ( 'NONE',  ( 1.042116488573753497, 0.8753402851892390091, -1.976733581976031218 ) ) ;
#125178=CARTESIAN_POINT ( 'NONE',  ( 2.132362993881876889, -1.555188906917738700, 0.7812613976432846163 ) ) ;
#125183=CARTESIAN_POINT ( 'NONE',  ( 2.161482305958133399, -0.5350050527693461788, -1.943774068525660148 ) ) ;
#125184=CARTESIAN_POINT ( 'NONE',  ( 6.825078400183518745, 4.686743419949856104, 2.806861564458093650 ) ) ;
#125186=CARTESIAN_POINT ( 'NONE',  ( 2.448066223300342514, 1.970991375097268961, 0.05018580263361701460 ) ) ;
#125187=CARTESIAN_POINT ( 'NONE',  ( 6.135011676971934058, 1.786887936952135991, 0.6819008164158719687 ) ) ;
#125192=CARTESIAN_POINT ( 'NONE',  ( 1.576825605243727502, -1.426663165427190405, 1.429853764617691647 ) ) ;
#125194=CARTESIAN_POINT ( 'NONE',  ( 5.930798096255836427, 2.221851032742766741, 0.6229754028606748761 ) ) ;
#125195=CARTESIAN_POINT ( 'NONE',  ( 6.531700620877029628, 1.877769495358465157, -0.5682946464737671510 ) ) ;
#125196=CARTESIAN_POINT ( 'NONE',  ( 3.028120845615460688, 1.045410262836780069, 1.659804706804830277 ) ) ;
#125198=CARTESIAN_POINT ( 'NONE',  ( 0.4400775573648734174, -1.704940109561555950, -1.076314675215600314 ) ) ;
#125200=CARTESIAN_POINT ( 'NONE',  ( 0.8314520141109645879, -1.673154641659507558, -1.297526329946703472 ) ) ;
#125203=CARTESIAN_POINT ( 'NONE',  ( 2.132514540308296791, -1.644867172388216003, 0.8273176719292076875 ) ) ;
#125207=CARTESIAN_POINT ( 'NONE',  ( 2.531617689938488791, -0.2033970545941807817, 2.110794199748195599 ) ) ;
#125211=CARTESIAN_POINT ( 'NONE',  ( 3.813790581289760784, -2.030913156241159978, 0.3485601269093330234 ) ) ;
#125213=CARTESIAN_POINT ( 'NONE',  ( 1.399689850468607277, -0.6632477835330424787, -1.717811453623831808 ) ) ;
#125215=CARTESIAN_POINT ( 'NONE',  ( -0.02224634325202321655, 2.854569189074110280, -2.777010687634806629 ) ) ;
#125216=( BOUNDED_SURFACE ( )  B_SPLINE_SURFACE ( 3, 3, ( 
 ( #129347, #161767, #158555, #41622, #208347, #107736, #173761, #25338, #11215, #42696, #128283, #91439, #10152, #94642, #191029, #210486, #62123, #44826, #159618, #27475, #157500, #28553, #58915, #110931, #125072, #45889, #112010, #26404, #76226, #59978, #43759, #192092, #77296, #178010, #9095, #115198, #46956, #147645, #113073, #99950, #167090, #68488, #150847, #2411, #114146, #34927, #149773, #197438, #83684, #65288, #101001, #166014, #179079, #195325, #196389, #17600, #50135, #133551, #117325, #18681, #1348, #84760, #212616, #30701, #98892, #67410, #199559, #148704, #164945, #96782, #49078, #131435, #48032, #130399, #51203, #162833, #183323, #64256, #66345, #181191, #32818, #14411, #132489, #80501, #81561, #146598, #82619, #180138, #31766, #97836, #198491, #163901, #15477, #213663, #16537, #273, #116258, #182247, #33872, #89050, #37068, #201681, #85828, #171340, #102080, #35999, #200618, #40290, #55462, #202751, #10689, #103149, #53327, #185448, #169210, #20801, #118392, #86897, #151907, #87963, #106400, #120543, #134616, #152964, #69548, #168148, #71685, #4538, #155107, #52265, #19748, #70612, #119460, #3481, #184380, #72767, #136727, #135658, #54404, #121617, #22934, #159091, #186522, #38152, #188661, #104224, #187586, #39212, #170271, #21856, #154037, #5603, #105303, #137798, #6692, #203817, #138866, #93050, #204884, #56536, #122698, #172424, #26943, #97305, #79961, #163364, #208883, #110412, #145011, #213148, #192637, #146064, #76759, #180664, #142881, #44290, #114670, #13882, #212077, #176415, #162295, #63716, #126674, #164420, #28022, #78888, #112534, #94119, #160160, #196912, #77832, #11758, #143953, #129874, #195857, #47497, #209948, #179610, #32289, #128798, #130919, #127756, #113606, #64778, #96244, #98355, #48552, #31231, #60513, #61587, #193713, #14940, #81035, #147122, #45356, #111475, #177480, #29095, #95179, #161228, #194780, #12815, #211017, #30156, #46417, #62640, #178546, #100479, #17075, #165479, #52797, #131958, #152441, #99425, #70089, #168683, #83153, #67945, #181714, #16004, #35474, #184916, #185985, #120009, #807, #53876, #20287, #202222, #151384, #66875, #36540, #51747, #86372, #136204, #84231, #19220, #85298, #4020, #33343, #150319, #65811, #37619, #200098, #18143, #1885, #2954, #133020, #199019, #149233, #50666, #214183, #116792, #182789, #34407, #134090, #166555, #117870, #183861, #103699, #101552, #82089, #167621, #148182, #118936, #197968, #49599, #69025, #115723, #135142, #201158, #102627, #141570, #139405, #170820, #41915, #207578, #6159, #8312, #104771, #74397, #124298, #57075, #7227, #23487, #153513, #90659, #187060, #24552, #121093, #58139, #174052, #22411, #138335, #88520, #171890, #39759, #38693, #106950, #156721, #89594, #21338, #122161, #87444, #140498, #59198, #42985, #125354, #191317, #154582, #9386, #190257, #155643, #108026, #105864, #5082, #188128, #71157, #206508, #169750, #137274, #203294, #54941, #72228, #75457, #25625, #73303, #91737, #205439, #204351, #157790, #56009, #123239, #189204, #40841, #172973, #47249, #30990, #14700, #211835, #146884, #126423, #109095, #12571, #63472, #113363, #62402, #78643, #175111, #177230, #193474, #110160, #44041, #145830, #10441, #97065, #192387, #163118, #179368, #176172, #160980, #60266, #26698, #128565, #129627, #64537, #212904, #93868 ),
 ( #210779, #27772, #130681, #159906, #112291, #13642, #143707, #142624, #80794, #195612, #196670, #158844, #94931, #92799, #11513, #77584, #209699, #76513, #208633, #61343, #127502, #45117, #29916, #28843, #111227, #144769, #194530, #46177, #178307, #95998, #162052, #79714, #213946, #1626, #20020, #34153, #48310, #16818, #197717, #164177, #199842, #99174, #2692, #114421, #15762, #82903, #115478, #65567, #180421, #200891, #148976, #32039, #116534, #35206, #85037, #69824, #550, #49359, #102352, #17880, #101282, #167365, #66615, #98126, #132762, #81847, #18953, #86109, #135932, #3750, #147930, #181470, #168424, #68764, #50415, #151126, #198765, #152180, #134884, #131714, #33099, #165226, #52537, #117607, #118671, #184654, #182523, #36275, #100223, #166291, #83965, #150054, #67685, #133831, #51484, #183599, #201950, #55737, #71961, #203030, #137002, #24283, #103426, #124037, #70892, #41653, #140228, #54671, #39488, #153239, #53606, #6959, #156458, #157531, #91469, #186796, #25369, #206249, #173793, #122978, #38425, #8044, #23214, #57875, #107767, #121892, #205167, #56808, #190003, #4810, #187861, #37352, #9125, #171620, #204084, #105586, #188937, #104504, #170548, #120819, #22132, #185719, #88245, #154315, #5888, #89327, #138071, #155374, #73040, #75201, #139138, #119740, #40576, #169488, #90389, #21071, #87169, #106682, #172705, #74134, #179109, #207324, #113103, #110963, #142370, #13388, #30731, #192128, #194278, #76261, #45923, #95746, #28588, #193212, #209438, #125102, #62157, #158587, #210521, #92548, #29660, #145581, #208379, #109906, #60011, #143441, #11250, #10187, #78393, #128315, #61082, #58945, #161797, #77328, #195355, #112043, #191060, #162863, #126164, #178044, #79464, #211578, #63212, #46987, #129376, #96814, #43793, #141312, #44859, #14442, #42725, #94676, #176971, #108833, #127242, #160718, #175917, #27508, #174859, #26438, #93608, #159653, #12312, #144513, #147678, #132523, #31796, #80532, #99981, #34960, #36032, #184413, #65317, #118427, #84792, #52298, #1381, #131466, #101031, #116288, #150880, #200649, #148736, #83717, #149807, #2443, #97871, #304, #130433, #102110, #50167, #82652, #66375, #67442, #197467, #49111, #163931, #115231, #64287, #213695, #181221, #15506, #198521, #81593, #32848, #98924, #168181, #164977, #146628, #16569, #212645, #117358, #196419, #48063, #182278, #114176, #33903, #180170, #166047, #17631, #133587, #199591, #167122, #51234, #183356, #18709, #68517, #134644, #188694, #121651, #71718, #88000, #3511, #155140, #37104, #89083, #185479, #122731, #24044, #20832, #202786, #86930, #21890, #104256, #103184, #171375, #6721, #154072, #85862, #186555, #151937, #138900, #206000, #107515, #189753, #41405, #152997, #73885, #40330, #5637, #169244, #137831, #4573, #70647, #136757, #19780, #54436, #57636, #120578, #69581, #56572, #123795, #139978, #38184, #135692, #170302, #201717, #53358, #119492, #203852, #55497, #106435, #187618, #39246, #72800, #105338, #204919, #172457, #22968, #90148, #156216, #7792, #94424, #190812, #28328, #124846, #61901, #177791, #174610, #142117, #26186, #175663, #43538, #42472, #110715, #160463, #93357, #25118, #125919, #91221, #78139, #145328, #46736, #129123, #195100, #92301, #13133, #128062, #27250, #194018, #109661, #79210, #144270, #157282, #173544, #158345, #210263 ),
 ( #126989, #77068, #8871, #159394, #10993, #9939, #108582, #45668, #74950, #95499, #76014, #211329, #111785, #208130, #143197, #59759, #141061, #192948, #29407, #207068, #62954, #191878, #58698, #209188, #60828, #44600, #176715, #12071, #161546, #49910, #83461, #213448, #146374, #54, #64031, #2183, #179919, #116031, #17377, #147423, #212389, #50975, #149541, #34709, #162607, #98667, #67189, #15257, #31541, #96560, #97617, #163674, #130177, #32590, #113923, #81344, #65070, #68260, #131226, #150623, #197214, #134392, #1127, #200395, #18456, #48854, #112848, #114968, #178864, #30475, #84533, #82396, #180968, #199329, #14183, #164722, #165794, #47810, #133326, #117097, #66117, #16311, #148485, #80276, #33648, #196169, #182017, #132260, #183098, #100778, #198267, #99722, #166861, #54172, #136502, #69323, #203590, #38992, #186286, #118170, #4316, #184156, #171115, #23788, #139714, #7531, #73614, #185215, #106173, #6461, #120312, #154878, #202523, #172199, #22708, #35778, #52044, #53098, #88821, #121389, #204658, #188429, #89895, #72538, #155946, #135433, #101854, #170041, #138636, #56308, #5381, #21627, #167922, #37924, #103998, #119232, #201455, #122469, #19520, #40064, #36839, #85597, #151685, #102921, #87735, #3255, #168982, #71459, #20582, #86667, #152734, #70386, #153810, #137572, #55242, #187362, #105077, #160200, #26985, #209992, #111518, #59494, #208925, #60560, #61634, #157021, #125651, #41143, #29136, #175400, #207871, #191613, #192679, #42207, #108324, #8607, #174344, #124592, #74690, #43275, #206805, #190551, #25922, #161274, #92030, #95224, #158087, #12860, #28068, #78935, #177524, #9676, #205738, #75752, #57371, #123534, #189499, #93092, #58438, #77878, #107254, #141862, #44333, #140791, #110455, #11803, #159133, #109396, #10734, #173274, #126719, #76804, #176456, #142925, #94161, #127800, #144000, #193755, #45402, #24854, #90956, #162344, #82138, #132010, #64823, #211060, #97355, #62685, #49648, #119775, #21105, #103463, #169525, #63761, #201985, #99472, #147169, #33394, #14988, #53642, #115771, #128844, #145057, #146112, #181760, #214232, #86145, #69860, #185755, #165531, #37388, #13927, #194825, #48599, #17123, #152216, #98403, #114717, #46461, #213196, #81082, #212123, #80007, #3785, #112583, #135969, #129921, #178595, #30204, #195907, #196961, #96292, #47543, #164468, #113656, #179660, #31280, #163412, #130969, #180712, #32335, #16054, #148230, #65860, #198020, #91505, #207360, #155412, #90426, #156495, #157566, #38464, #6995, #137038, #125136, #56847, #89364, #73073, #74173, #138110, #204121, #104540, #55773, #70929, #154349, #203065, #174892, #54708, #139174, #123019, #120859, #186832, #58980, #88285, #170585, #22170, #172745, #24320, #206285, #5927, #190038, #42762, #205205, #141345, #121930, #124074, #187897, #153273, #71999, #23251, #171654, #188970, #191093, #8084, #57909, #39527, #105625, #40614, #106718, #108868, #140265, #41690, #107801, #173826, #25403, #9159, #75235, #87209, #4850, #12346, #195391, #143476, #93639, #192162, #63247, #208411, #142403, #92582, #146664, #161833, #94709, #114208, #209472, #159682, #77362, #61114, #127274, #10221, #193246, #43822, #194314, #212678, #78426, #26472, #44893, #175948, #60045, #178077, #110999, #47021, #158624, #126200, #177004, #11283, #109939, #76295, #179143 ),
 ( #13421, #28621, #27544, #160751, #144548, #79496, #210555, #145615, #62191, #128347, #196453, #45955, #112076, #29695, #95776, #80565, #113136, #211611, #30766, #129408, #96846, #162893, #14476, #64319, #130463, #48096, #69618, #180206, #147710, #3548, #117394, #34996, #213728, #51270, #183391, #101068, #167155, #84827, #65351, #68553, #135728, #17667, #19813, #16604, #2476, #336, #31828, #165009, #116320, #50202, #33940, #151974, #18742, #150915, #66409, #131498, #67476, #197502, #201750, #32881, #134680, #200683, #132554, #49145, #118462, #52334, #102148, #15540, #166079, #184448, #82685, #98958, #115261, #36066, #181254, #81625, #97903, #85900, #168214, #100015, #53391, #148767, #198553, #182311, #83753, #149844, #163964, #1414, #133622, #199624, #91255, #105374, #119528, #88032, #54468, #20865, #56604, #170338, #73919, #185514, #86964, #154104, #186589, #70681, #37138, #57671, #5673, #103219, #187653, #106468, #156249, #141094, #71751, #120612, #173584, #89119, #172495, #24081, #137867, #169279, #104290, #121686, #90186, #203887, #7827, #55531, #155173, #74986, #153033, #39279, #4607, #136793, #25154, #140012, #122768, #206037, #202819, #38217, #171413, #41442, #21923, #188728, #23001, #8906, #6757, #72832, #157315, #40366, #123829, #138935, #204956, #189791, #107550, #207106, #174643, #60861, #94458, #26220, #158378, #178897, #59796, #92336, #108616, #124885, #30511, #28363, #125953, #145365, #96592, #109691, #111822, #208165, #177824, #13168, #160498, #110750, #127022, #42510, #194051, #76049, #128093, #9971, #161581, #62989, #191909, #27285, #43572, #192981, #143229, #142150, #210294, #45703, #44635, #190849, #11027, #175695, #29441, #162641, #146410, #14215, #80310, #93391, #112885, #79246, #176748, #211364, #209219, #58733, #95532, #159428, #77105, #12103, #129158, #195135, #46771, #78173, #144301, #61935, #35814, #15290, #212423, #116063, #166899, #2220, #165827, #182053, #64065, #66150, #82429, #213480, #147459, #34741, #113955, #134428, #81375, #52078, #150657, #65104, #49942, #163708, #130209, #17411, #18491, #167956, #101891, #197247, #132295, #47844, #48886, #100814, #115005, #84570, #33683, #68295, #118205, #198301, #1161, #67224, #200431, #131260, #99759, #179951, #19560, #83495, #85, #149577, #199366, #181003, #32623, #98700, #164759, #196202, #16349, #148519, #133359, #51012, #117133, #183136, #184192, #85636, #31574, #97649, #70424, #173310, #188466, #189533, #57405, #202560, #41181, #37961, #107288, #119269, #53138, #3294, #123571, #72574, #5420, #24889, #120350, #4356, #54212, #186326, #104034, #135471, #170080, #102960, #105111, #151722, #137610, #69362, #21667, #86705, #185254, #88860, #87774, #106210, #201492, #36878, #153849, #136541, #169019, #20617, #89929, #71499, #152774, #203626, #138674, #40098, #55277, #121426, #187396, #205777, #39028, #204694, #56344, #171152, #22742, #154915, #6499, #122505, #172236, #23824, #155980, #7567, #73653, #139752, #43312, #124630, #8646, #145096, #111554, #94198, #177563, #74725, #190588, #159169, #12897, #206843, #160238, #90994, #194866, #157057, #58475, #128885, #28103, #11837, #42245, #176492, #77915, #140830, #178633, #108358, #93130, #126755, #174380, #25960, #211100, #92065, #158123, #9714, #144034, #210030, #61671, #75790, #193791, #46499, #142962 ),
 ( #10769, #127839, #45440, #95265, #141898, #76843, #207908, #112623, #60597, #208964, #192716, #29175, #59529, #125689, #191647, #109431, #175437, #27022, #44370, #110493, #161313, #78976, #62724, #196999, #96329, #149321, #1968, #117951, #200180, #51833, #163448, #84315, #199104, #32376, #133106, #114751, #150400, #899, #13962, #30245, #31314, #66967, #99510, #182877, #166640, #68032, #50749, #134172, #47581, #162384, #148268, #116878, #34493, #198055, #214267, #80046, #98441, #180749, #97392, #179699, #100567, #146149, #18231, #113695, #212164, #63799, #15028, #82174, #195945, #129957, #49685, #81119, #147205, #213230, #64862, #164506, #131007, #48634, #16090, #65900, #132046, #115812, #181800, #33433, #165567, #17162, #83236, #188209, #135230, #37707, #19304, #7313, #153597, #186072, #103783, #170900, #20372, #86457, #201243, #152521, #167702, #36625, #102709, #52884, #169834, #185000, #168767, #4106, #139495, #70175, #73392, #136287, #205523, #6246, #57157, #89680, #202307, #183946, #53957, #35556, #101636, #155729, #5168, #120095, #56094, #85384, #21421, #22492, #119019, #88604, #138420, #71242, #87530, #137358, #151468, #104856, #203375, #38774, #55027, #72315, #39848, #121176, #187145, #154660, #204440, #122250, #105955, #171979, #23571, #3039, #69108, #192471, #123322, #12655, #189285, #90746, #161062, #60346, #44125, #156807, #208720, #126507, #173057, #210860, #24637, #125441, #158928, #8394, #74477, #28929, #124381, #140584, #206594, #110245, #176254, #27855, #58223, #11594, #78726, #175194, #177315, #174136, #159993, #157876, #40927, #108109, #59282, #207663, #191402, #95013, #93952, #77668, #9469, #190339, #10524, #42001, #144853, #25710, #143788, #209783, #75541, #91818, #61422, #127589, #45197, #141651, #109181, #193555, #43068, #26779, #92883, #111311, #76598, #142711, #107031, #165313, #98206, #14785, #66704, #47331, #145910, #129712, #113445, #195695, #194615, #179451, #96082, #48396, #16908, #146966, #62485, #31072, #211922, #178386, #164256, #97148, #197805, #128649, #162136, #163202, #80876, #79798, #46257, #99265, #212982, #112375, #196756, #131798, #181555, #29997, #64621, #130760, #13725, #65651, #82988, #149063, #114509, #63556, #33183, #180505, #32125, #640, #15844, #81930, #148016, #214027, #49440, #115559, #195198, #143286, #94519, #64132, #46835, #208221, #31638, #11088, #47911, #161642, #79310, #43632, #95594, #13237, #59853, #97715, #126005, #12165, #45766, #191966, #109747, #130276, #77165, #175757, #27349, #145426, #211427, #129224, #93451, #112949, #180017, #62000, #196264, #60924, #178960, #44698, #76103, #209277, #160557, #78237, #144359, #114021, #63057, #30575, #110805, #159489, #111884, #127081, #10028, #193044, #96656, #162709, #176810, #28426, #14281, #80376, #146471, #210360, #128156, #212490, #194116, #177888, #29501, #142206, #131321, #65166, #15351, #69426, #84632, #17476, #36943, #132364, #16414, #150, #198366, #66216, #147522, #116130, #115073, #117199, #135532, #149642, #163773, #50006, #98767, #197314, #100878, #182118, #118267, #81444, #48955, #33747, #82494, #181069, #213543, #101953, #99825, #32687, #83560, #150723, #200495, #185320, #165891, #164823, #3356, #133425, #2283, #68359, #1224, #148581, #67286, #199432, #134492, #51074, #52139, #183197, #34803, #119333, #166965 ),
 ( #18555, #184251, #35878, #53202, #168020, #19624, #85695, #151783, #201556, #38024, #139811, #4414, #24954, #186387, #157117, #41241, #170144, #154974, #54275, #103024, #122566, #57472, #58533, #206902, #87840, #22806, #152839, #153911, #205839, #5481, #123632, #138736, #107348, #8706, #171212, #106273, #172294, #173370, #120412, #88921, #70485, #140891, #72639, #105175, #6559, #89988, #71562, #137669, #104095, #203690, #86768, #21730, #55337, #121489, #204754, #187461, #39089, #56405, #124688, #188528, #190646, #40159, #169079, #189595, #20678, #74790, #23882, #136601, #156039, #202625, #7628, #73713, #91056, #43370, #128947, #14017, #93195, #95329, #191712, #161378, #211160, #144098, #94259, #110551, #26019, #177629, #59593, #111617, #207967, #145154, #46562, #109492, #10827, #175499, #44434, #126819, #125750, #193851, #29237, #176553, #108421, #209020, #174443, #12962, #80104, #130015, #212225, #63859, #27087, #28163, #210093, #79039, #159226, #192776, #96391, #62784, #92129, #42306, #76901, #194925, #112682, #178692, #30306, #162442, #146208, #158183, #143025, #9775, #160298, #75848, #141955, #61732, #11901, #60656, #77975, #45501, #127900, #153376, #196006, #97449, #167494, #51620, #150191, #47641, #137139, #19090, #113752, #52670, #185853, #21205, #6029, #85170, #133965, #38563, #168555, #37485, #103562, #151254, #179756, #183736, #201028, #169622, #2824, #87307, #68894, #20154, #154450, #31373, #84104, #136069, #118800, #102491, #4947, #202083, #71024, #166424, #18015, #184786, #120959, #1760, #53742, #67818, #88381, #199972, #117745, #22272, #119875, #203166, #35343, #69957, #54811, #101422, #72098, #135014, #36412, #86240, #152311, #3887, #104638, #186931, #170685, #187996, #9256, #75326, #42854, #171756, #26564, #93735, #190131, #192252, #189075, #174981, #172842, #204221, #123115, #74267, #8183, #206379, #110029, #141443, #108961, #24414, #23351, #25499, #89461, #27634, #205305, #207449, #92670, #90527, #155514, #76386, #158714, #60136, #39621, #124169, #10311, #40708, #56943, #7096, #142494, #105726, #73168, #55873, #43915, #59068, #58005, #11373, #106812, #156589, #140360, #41787, #107900, #122030, #173926, #139274, #91607, #176042, #157658, #138208, #125229, #191187, #126293, #208501, #159774, #31921, #194404, #144635, #28712, #114300, #44982, #193337, #143571, #197595, #212774, #145708, #165106, #46046, #210650, #128438, #112167, #178170, #61209, #29786, #94798, #30861, #49238, #63342, #77453, #95871, #12439, #111091, #14570, #161926, #98000, #209563, #177097, #13516, #62277, #160847, #127366, #15636, #79588, #78518, #211706, #64410, #180299, #99051, #129501, #195482, #131593, #47115, #130555, #196546, #113233, #179237, #96938, #162989, #48189, #80665, #164057, #146756, #81723, #32975, #147806, #213824, #65442, #115357, #181349, #37237, #19904, #103308, #148856, #50295, #84915, #153124, #132640, #85989, #16698, #120702, #82783, #198646, #54556, #168306, #152063, #116413, #102235, #3633, #66501, #104382, #182404, #18831, #52426, #34033, #100106, #136884, #17755, #166166, #83844, #69712, #135815, #201838, #149933, #119621, #186677, #68643, #70770, #67568, #53483, #51364, #430, #1502, #167243, #101157, #151003, #202911, #185605, #169370, #117487, #133712, #118551, #199718, #38305, #183478, #20954, #87052, #35086 ),
 ( #2573, #134766, #4695, #200774, #184533, #36156, #173672, #42601, #88126, #203973, #24166, #92422, #71845, #25247, #170429, #59887, #22016, #137953, #208253, #107640, #91347, #55620, #41528, #157409, #5764, #43664, #121777, #172587, #206128, #187744, #39372, #76138, #171502, #105469, #23094, #9000, #75075, #141188, #89210, #58823, #126036, #7923, #10062, #6844, #207198, #205052, #154196, #155263, #106559, #40456, #90269, #142241, #124976, #190937, #56694, #72922, #57758, #139028, #191999, #122861, #108707, #174736, #188822, #156338, #26309, #158462, #74009, #140101, #123919, #189886, #12196, #176844, #60957, #146505, #77197, #11120, #175790, #15381, #30605, #177918, #197344, #78266, #28457, #160589, #144391, #210392, #93482, #62034, #127114, #63089, #81475, #95624, #109781, #128188, #44731, #143316, #46866, #194149, #64163, #27381, #209310, #45797, #94551, #193081, #159521, #47940, #111918, #110838, #29532, #96693, #212522, #131348, #161674, #13268, #163805, #79341, #162741, #14314, #145459, #211454, #129258, #80407, #147552, #195228, #65196, #112979, #178990, #130306, #196293, #114054, #180047, #31669, #213574, #97746, #32717, #70515, #50040, #19655, #118297, #201587, #185352, #169111, #151815, #86801, #66248, #48986, #166996, #3388, #53234, #2316, #18587, #115104, #117229, #133458, #116163, #198398, #85730, #164853, #36974, #132396, #103057, #119364, #182149, #100907, #180, #181102, #68392, #69458, #4445, #152867, #33779, #183227, #98799, #99858, #135563, #165920, #20707, #84665, #136630, #16445, #34833, #52171, #184283, #82525, #17505, #150754, #148611, #83593, #134521, #51104, #200525, #35909, #149675, #1256, #67314, #199462, #101984, #168053, #121521, #5509, #122597, #203719, #187491, #39121, #158216, #105204, #26051, #171241, #9805, #24988, #92164, #108455, #22837, #75880, #88951, #202657, #54306, #174475, #172325, #55367, #74824, #120444, #155005, #41275, #137699, #107384, #157151, #90019, #40191, #56438, #186418, #123664, #71590, #57505, #153941, #91091, #206938, #6590, #72669, #138767, #204785, #188560, #106303, #139842, #189627, #23914, #38056, #156076, #7662, #104127, #73747, #170173, #205871, #173407, #21761, #8743, #140924, #58567, #87869, #124721, #190681, #42340, #93226, #141987, #80138, #110585, #208001, #210126, #128981, #178726, #163537, #176587, #76932, #196039, #111650, #194960, #46596, #28199, #59627, #126853, #144133, #112714, #94293, #30341, #160333, #177662, #97480, #125784, #27120, #79071, #61768, #45536, #162477, #145189, #14049, #191746, #175531, #127936, #63891, #43401, #211195, #109524, #31406, #159258, #10859, #179786, #62821, #96426, #143058, #12996, #146241, #209053, #15122, #60689, #193888, #29270, #192811, #44469, #47673, #11937, #78009, #95362, #212257, #130046, #113784, #161412, #184027, #36709, #133192, #135313, #132134, #118041, #115900, #147290, #65984, #17246, #165659, #149410, #52965, #18322, #51918, #181885, #114837, #182966, #32462, #185085, #148355, #84405, #200266, #33521, #180835, #19388, #35643, #3123, #131096, #67056, #101722, #198141, #214354, #98531, #167793, #48723, #197085, #213322, #201327, #2052, #992, #168853, #49773, #99593, #83323, #199194, #50842, #64944, #116969, #164592, #34581, #102795, #100653, #119103, #16178, #81210, #166731, #82262, #85467, #150493, #68125 ) ),
 .UNSPECIFIED., .T., .F., .T. ) 
 B_SPLINE_SURFACE_WITH_KNOTS ( ( 4, 3, 4 ),
 ( 4, 1, 1, 1, 1, 1, 1, 1, 1, 1, 1, 1, 1, 1, 1, 1, 1, 1, 1, 1, 1, 1, 1, 1, 1, 1, 1, 1, 1, 1, 1, 1, 1, 1, 1, 1, 1, 1, 1, 1, 1, 1, 1, 1, 1, 1, 1, 1, 1, 1, 1, 1, 1, 1, 1, 1, 1, 1, 1, 1, 1, 1, 1, 1, 1, 1, 1, 1, 1, 1, 1, 1, 1, 1, 1, 1, 1, 1, 1, 1, 1, 1, 1, 1, 1, 1, 1, 1, 1, 1, 1, 1, 1, 1, 1, 1, 1, 1, 1, 1, 1, 1, 1, 1, 1, 1, 1, 1, 1, 1, 1, 1, 1, 1, 1, 1, 1, 1, 1, 1, 1, 1, 1, 1, 1, 1, 1, 1, 1, 1, 1, 1, 1, 1, 1, 1, 1, 1, 1, 1, 1, 1, 1, 1, 1, 1, 1, 1, 1, 1, 1, 1, 1, 1, 1, 1, 1, 1, 1, 1, 1, 1, 1, 1, 1, 1, 1, 1, 1, 1, 1, 1, 1, 1, 1, 1, 1, 1, 1, 1, 1, 1, 1, 1, 1, 1, 1, 1, 1, 1, 1, 1, 1, 1, 1, 1, 1, 1, 1, 1, 1, 1, 1, 1, 1, 1, 1, 1, 1, 1, 1, 1, 1, 1, 1, 1, 1, 1, 1, 1, 1, 1, 1, 1, 1, 1, 1, 1, 1, 1, 1, 1, 1, 1, 1, 1, 1, 1, 1, 1, 1, 1, 1, 1, 1, 1, 1, 1, 1, 1, 1, 1, 1, 1, 1, 1, 1, 1, 1, 1, 1, 1, 1, 1, 1, 1, 1, 1, 1, 1, 1, 1, 1, 1, 1, 1, 1, 1, 1, 1, 1, 1, 1, 1, 1, 1, 1, 1, 1, 1, 1, 1, 1, 1, 1, 1, 1, 1, 1, 1, 1, 1, 1, 1, 1, 1, 1, 1, 1, 1, 1, 1, 1, 1, 1, 1, 1, 1, 1, 1, 1, 1, 1, 1, 1, 1, 1, 1, 1, 1, 1, 1, 1, 1, 1, 1, 1, 1, 1, 1, 1, 1, 1, 1, 1, 1, 1, 1, 1, 1, 1, 1, 1, 1, 1, 1, 1, 1, 1, 1, 1, 1, 1, 1, 1, 1, 1, 1, 1, 1, 1, 1, 1, 1, 1, 1, 1, 1, 1, 1, 1, 1, 1, 1, 4 ),
 ( 0.000000000000000000, 0.5000000000000000000, 1.000000000000000000 ),
 ( 0.000000000000000000, 0.002600154539856827565, 0.005208839490340733125, 0.007813275572638063438, 0.01041576435696154809, 0.01302135854728175661, 0.01562456786780599440, 0.01822932761385693060, 0.02083324874646079461, 0.02343713590986815087, 0.02604192363554110393, 0.02864519953128016536, 0.03125045858075606309, 0.03385359029894085409, 0.03645870005206112291, 0.03906221013386886737, 0.04166657361863843057, 0.04427092160485841116, 0.04687444683368256759, 0.04947954930481244379, 0.05208268618576387260, 0.05468794662449812799, 0.05729120536831356497, 0.05989601299138836571, 0.06249988999545372931, 0.06510378435733490954, 0.06770858081828938502, 0.07031184975024351580, 0.07291710771924506118, 0.07552024060328325905, 0.07812534933470290099, 0.08072885870519988516, 0.08333322157114708695, 0.08593756915452624434, 0.08854109358761537429, 0.09114619558392741960, 0.09374933183658358538, 0.09635459170495851156, 0.09895784999447977681, 0.1015626569530685003, 0.1041665336043751944, 0.1067704272253022224, 0.1093752232910748662, 0.1119784915631429623, 0.1145837490571069844, 0.1171868814509031548, 0.1197919896162490533, 0.1223954986480551566, 0.1249998608471283579, 0.1276042081199000311, 0.1302077318846941445, 0.1328128334964322199, 0.1354159692195129883, 0.1380212286176593917, 0.1406244865514671982, 0.1432292929439143159, 0.1458331693420142072, 0.1484370623210626572, 0.1510418580899855479, 0.1536451258019158050, 0.1562503829188521542, 0.1588535149221727560, 0.1614586226195926788, 0.1640621314121666618, 0.1666664930431534797, 0.1692708401040713406, 0.1718743633000545112, 0.1744794646253388370, 0.1770825999186152189, 0.1796878589445308205, 0.1822911166222762891, 0.1848959225469683498, 0.1874997987909985397, 0.1901036912273387502, 0.1927084867977703619, 0.1953117540492253223, 0.1979170108871138589, 0.2005201425997050479, 0.2031252499273119572, 0.2057287585800815777, 0.2083331197417381819, 0.2109374666895270922, 0.2135409894161511279, 0.2161460905530729892, 0.2187492255162853672, 0.2213544842679382729, 0.2239577417892439637, 0.2265625473445374016, 0.2291664235336075273, 0.2317703155263790282, 0.2343751109966507595, 0.2369783778872631419, 0.2395836345440564008, 0.2421867660656364940, 0.2447918731215153465, 0.2473953817338825356, 0.2499997425249363969, 0.2526040894582959329, 0.2552076118149841921, 0.2578127128616094499, 0.2604158475944712281, 0.2630211061698037311, 0.2656243636342671688, 0.2682291689184919115, 0.2708330451516883230, 0.2734369368000036937, 0.2760417322684234342, 0.2786449988978000336, 0.2812502554714267355, 0.2838533869016899303, 0.2864584937839013135, 0.2890620024552456591, 0.2916663629743991848, 0.2942707099920074398, 0.2968742320781582733, 0.2994793331325310004, 0.3020824677347322962, 0.3046877262316646240, 0.3072909837388622112, 0.3098957888503254821, 0.3124996652267145181, 0.3151035566296633839, 0.3177083521945192612, 0.3203116186622446127, 0.3229168752506134110, 0.3255200066892336430, 0.3281251134958176330, 0.3307286223255002655, 0.3333329826714347410, 0.3359373298719517953, 0.3385408517869427647, 0.3411459529470890484, 0.3437490875183005223, 0.3463543460347343617, 0.3489576036842249041, 0.3515624087212146920, 0.3541662853398466204, 0.3567701765964986227, 0.3593749723560626386, 0.3619782387617029862, 0.3645834954627060198, 0.3671866270093405715, 0.3697917338383204244, 0.3723952429256875973, 0.3749996031970665444, 0.3776039506791386557, 0.3802074725223298923, 0.3828125738862612759, 0.3854157085261381011, 0.3880209671599602617, 0.3906242250512887426, 0.3932290301120778819, 0.3958329070719905363, 0.3984367982813996067, 0.4010415943339316058, 0.4036448607770379837, 0.4062501176885546794, 0.4088532494428480657, 0.4114583563922335485, 0.4140618658366201910, 0.4166662261320933647, 0.4192705739943561327, 0.4218740958650940009, 0.4244791975308115917, 0.4270823323389966175, 0.4296875911880828069, 0.4322908494207843844, 0.4348956546036337745, 0.4374995320038561619, 0.4401034232650644085, 0.4427082197088152427, 0.4453114862889279713, 0.4479167435088288185, 0.4505198755704162283, 0.4531249827382076711, 0.4557284926389418844, 0.4583328530571487147, 0.4609372013982309668, 0.4635407233958523388, 0.4661458254613498609, 0.4687489605374778323, 0.4713542196996960976, 0.4739574783732994345, 0.4765622837764619812, 0.4791661617160185016, 0.4817700531280592058, 0.4843748500612748420, 0.4869781168779269698, 0.4895833745040767959, 0.4921865069725880892, 0.4947916144567798824, 0.4973951249131855490, 0.4999994855527590265, 0.5026038344712867589, 0.5052073566951218453, 0.5078124592583899144, 0.5104155947020908579, 0.5130208542753056378, 0.5156241134893367883, 0.5182289192110610676, 0.5208327977889742888, 0.5234366894508762913, 0.5260414869718011976, 0.5286447541245218318, 0.5312500122547839654, 0.5338531452298473923, 0.5364582531284315392, 0.5390617642398328746, 0.5416661251994032700, 0.5442704747940029231, 0.5468739973433798252, 0.5494791005024090014, 0.5520822364133124438, 0.5546874964953879550, 0.5572907563493740835, 0.5598955624879079496, 0.5624994418032033261, 0.5651033338139942463, 0.5677081320208752224, 0.5703113996091939697, 0.5729166583414331271, 0.5755197919226788805, 0.5781249003336490500, 0.5807284121993739889, 0.5833327735775721834, 0.5859371239468746939, 0.5885406469211225122, 0.5911457507739076300, 0.5937488872516457628, 0.5963541479404496082, 0.5989574085339228748, 0.6015622151875171797, 0.6041660953392257172, 0.6067699877979360057, 0.6093747867890261238, 0.6119780549124759217, 0.6145833143445629254, 0.6171864486316270826, 0.6197915576529816617, 0.6223950703723655220, 0.6249994322678273928, 0.6276037835104713025, 0.6302073070089242446, 0.6328124116534677990, 0.6354155487976793637, 0.6380208101910863627, 0.6406240716235875876, 0.6432288788904997334, 0.6458327599776627626, 0.6484366529833293091, 0.6510414528568908565, 0.6536447216150126360, 0.6562499818448275235, 0.6588531169373553764, 0.6614582266671018562, 0.6640617403394915019, 0.6666661028508605868, 0.6692704550654967610, 0.6718739791874978051, 0.6744790847218130603, 0.6770822226321474568, 0.6796874848280434200, 0.6822907471991253026, 0.6848955551776233497, 0.6874994372992955238, 0.6901033309509650993, 0.6927081318052739078, 0.6953114012976200353, 0.6979166624230551674, 0.7005197984207056638, 0.7031249089568636368, 0.7057284236816204759, 0.7083327869075525252, 0.7109371401928469281, 0.7135406650377511539, 0.7161457715598668061, 0.7187489103359874232, 0.7213541734322722609, 0.7239574368415039318, 0.7265622456298695964, 0.7291661288851226663, 0.7317700232818561412, 0.7343748252152053624, 0.7369780955413426371, 0.7395833576603073611, 0.7421864946627563242, 0.7447916061033615920, 0.7473951219798656842, 0.7499994860190324353, 0.7526038404736700160, 0.7552073661408488237, 0.7578124737488122209, 0.7604156134903999886, 0.7630208775849919300, 0.7656241421319622820, 0.7682289518284949326, 0.7708328363164217434, 0.7734367315572975299, 0.7760415346680002990, 0.7786448059275148381, 0.7812500691379388185, 0.7838532072448821664, 0.7864583196879902927, 0.7890618368156444573, 0.7916662017667361884, 0.7942705574894247667, 0.7968740840782696511, 0.7994791928701499018, 0.8020823336769073997, 0.8046875988677468783, 0.8072908646520678966, 0.8098956753550886623, 0.8124995611748068169, 0.8151034573589240884, 0.8177082617453185209, 0.8203115340378186460, 0.8229167984376549727, 0.8255199377488137147, 0.8281250512925039109, 0.8307285697707365024, 0.8333329357324672504, 0.8359372928219411802, 0.8385408204318668401, 0.8411459305057594760, 0.8437490724774151518, 0.8463543388624672481, 0.8489576059837783406, 0.8515624177916331083, 0.8541663050422881875, 0.8567702022687715413, 0.8593750080292236193, 0.8619782814543437421, 0.8645835471415733720, 0.8671866877566964948, 0.8697918024990743957, 0.8723953224273439666, 0.8749996894984543028, 0.8776040480534781363, 0.8802075767839265819, 0.8828126882379567775, 0.8854158314742670566, 0.8880210991515266050, 0.8906243677094983768, 0.8932291807205616774, 0.8958330695013316802, 0.8984369678693342465, 0.9010417751022415933, 0.9036450497596462128, 0.9062503168322812996, 0.9088534588511494317, 0.9114585748903522022, 0.9140620963681507227, 0.9166664646474114164, 0.9192708247667824573, 0.9218743547172278952, 0.9244794676495572405, 0.9270826122503010858, 0.9296878813177945622, 0.9322911514121841048, 0.9348959657248061550, 0.9374998561347748227, 0.9401037557438677306, 0.9427085645475906661, 0.9453118405358371668, 0.9479171090940153865, 0.9505202526155902554, 0.9531253700418979014, 0.9557288931959170286, 0.9583332627756006028, 0.9609376244112938226, 0.9635411559431285022, 0.9661462708106475228, 0.9687494151757961580, 0.9713546862302190332, 0.9739579640138142924, 0.9765627705390533819, 0.9791666547386930208, 0.9817705986233274951, 0.9843753609709087193, 0.9869785915570626900, 0.9895841932699848131, 0.9921866851465583892, 0.9947911401134668097, 0.9973998225951543617, 1.000000000000000000 ),
 .UNSPECIFIED. ) 
 GEOMETRIC_REPRESENTATION_ITEM ( )  RATIONAL_B_SPLINE_SURFACE ( (
 ( 1.000000000000000000, 1.000000000000000000, 1.000000000000000222, 1.000000000000000000, 0.9999999999999996669, 1.000000000000000444, 0.9999999999999997780, 1.000000000000000000, 1.000000000000000222, 0.9999999999999996669, 1.000000000000000222, 0.9999999999999996669, 1.000000000000000000, 0.9999999999999997780, 1.000000000000000222, 0.9999999999999997780, 1.000000000000000222, 1.000000000000000222, 0.9999999999999997780, 1.000000000000000222, 1.000000000000000222, 0.9999999999999996669, 1.000000000000000444, 0.9999999999999997780, 1.000000000000000000, 1.000000000000000222, 1.000000000000000000, 1.000000000000000000, 1.000000000000000000, 1.000000000000000000, 1.000000000000000222, 1.000000000000000000, 1.000000000000000000, 0.9999999999999997780, 1.000000000000000000, 1.000000000000000000, 1.000000000000000000, 1.000000000000000000, 0.9999999999999997780, 1.000000000000000222, 1.000000000000000000, 1.000000000000000000, 1.000000000000000444, 0.9999999999999997780, 1.000000000000000222, 0.9999999999999996669, 1.000000000000000444, 0.9999999999999997780, 1.000000000000000000, 0.9999999999999997780, 1.000000000000000000, 1.000000000000000222, 0.9999999999999997780, 1.000000000000000444, 0.9999999999999997780, 1.000000000000000000, 0.9999999999999996669, 1.000000000000000444, 0.9999999999999997780, 1.000000000000000444, 1.000000000000000000, 1.000000000000000444, 0.9999999999999996669, 1.000000000000000000, 0.9999999999999996669, 1.000000000000000444, 0.9999999999999997780, 1.000000000000000000, 1.000000000000000000, 1.000000000000000000, 1.000000000000000000, 0.9999999999999996669, 1.000000000000000000, 1.000000000000000222, 0.9999999999999997780, 1.000000000000000000, 0.9999999999999997780, 0.9999999999999997780, 1.000000000000000000, 1.000000000000000222, 0.9999999999999997780, 1.000000000000000000, 1.000000000000000222, 1.000000000000000222, 1.000000000000000222, 0.9999999999999997780, 1.000000000000000000, 1.000000000000000222, 0.9999999999999997780, 1.000000000000000222, 1.000000000000000222, 0.9999999999999997780, 0.9999999999999997780, 0.9999999999999997780, 1.000000000000000444, 1.000000000000000000, 1.000000000000000000, 1.000000000000000000, 1.000000000000000222, 0.9999999999999997780, 1.000000000000000000, 1.000000000000000444, 0.9999999999999996669, 1.000000000000000444, 1.000000000000000000, 1.000000000000000000, 1.000000000000000222, 0.9999999999999997780, 1.000000000000000444, 0.9999999999999996669, 1.000000000000000444, 1.000000000000000000, 0.9999999999999997780, 1.000000000000000222, 0.9999999999999996669, 1.000000000000000222, 1.000000000000000000, 1.000000000000000222, 0.9999999999999997780, 1.000000000000000222, 0.9999999999999996669, 1.000000000000000222, 1.000000000000000222, 1.000000000000000222, 1.000000000000000000, 0.9999999999999997780, 1.000000000000000000, 0.9999999999999997780, 1.000000000000000000, 0.9999999999999997780, 0.9999999999999997780, 1.000000000000000222, 1.000000000000000222, 1.000000000000000222, 0.9999999999999997780, 0.9999999999999997780, 1.000000000000000444, 0.9999999999999997780, 1.000000000000000000, 0.9999999999999997780, 1.000000000000000000, 0.9999999999999997780, 1.000000000000000222, 1.000000000000000000, 1.000000000000000000, 1.000000000000000222, 1.000000000000000000, 0.9999999999999997780, 1.000000000000000444, 1.000000000000000000, 1.000000000000000000, 1.000000000000000444, 0.9999999999999997780, 1.000000000000000222, 0.9999999999999997780, 1.000000000000000444, 1.000000000000000000, 1.000000000000000222, 0.9999999999999997780, 0.9999999999999997780, 1.000000000000000000, 1.000000000000000444, 0.9999999999999996669, 1.000000000000000000, 1.000000000000000222, 1.000000000000000222, 0.9999999999999997780, 1.000000000000000222, 0.9999999999999997780, 1.000000000000000222, 1.000000000000000000, 1.000000000000000000, 0.9999999999999997780, 1.000000000000000444, 0.9999999999999997780, 1.000000000000000222, 0.9999999999999996669, 1.000000000000000444, 0.9999999999999996669, 1.000000000000000222, 1.000000000000000000, 1.000000000000000000, 1.000000000000000000, 1.000000000000000444, 1.000000000000000222, 0.9999999999999997780, 1.000000000000000444, 0.9999999999999997780, 1.000000000000000000, 0.9999999999999996669, 1.000000000000000000, 0.9999999999999996669, 1.000000000000000000, 1.000000000000000222, 1.000000000000000000, 0.9999999999999997780, 1.000000000000000222, 1.000000000000000000, 1.000000000000000222, 0.9999999999999996669, 1.000000000000000000, 1.000000000000000000, 1.000000000000000000, 0.9999999999999997780, 1.000000000000000000, 1.000000000000000000, 1.000000000000000222, 1.000000000000000000, 1.000000000000000000, 0.9999999999999997780, 1.000000000000000000, 1.000000000000000222, 0.9999999999999997780, 1.000000000000000000, 1.000000000000000222, 1.000000000000000000, 1.000000000000000000, 0.9999999999999997780, 0.9999999999999997780, 1.000000000000000000, 1.000000000000000000, 0.9999999999999997780, 1.000000000000000000, 1.000000000000000000, 1.000000000000000000, 1.000000000000000222, 1.000000000000000000, 1.000000000000000000, 0.9999999999999997780, 1.000000000000000000, 0.9999999999999997780, 1.000000000000000444, 0.9999999999999997780, 1.000000000000000222, 0.9999999999999997780, 1.000000000000000444, 0.9999999999999994449, 1.000000000000000444, 0.9999999999999997780, 1.000000000000000222, 1.000000000000000000, 1.000000000000000000, 0.9999999999999997780, 1.000000000000000000, 1.000000000000000000, 0.9999999999999997780, 1.000000000000000000, 1.000000000000000000, 0.9999999999999997780, 1.000000000000000222, 1.000000000000000000, 1.000000000000000222, 0.9999999999999997780, 1.000000000000000222, 0.9999999999999997780, 1.000000000000000222, 0.9999999999999997780, 1.000000000000000444, 0.9999999999999996669, 1.000000000000000222, 0.9999999999999997780, 1.000000000000000000, 1.000000000000000000, 1.000000000000000000, 1.000000000000000222, 1.000000000000000222, 1.000000000000000000, 1.000000000000000444, 1.000000000000000222, 0.9999999999999997780, 1.000000000000000222, 0.9999999999999996669, 1.000000000000000444, 0.9999999999999997780, 0.9999999999999997780, 1.000000000000000222, 1.000000000000000000, 1.000000000000000222, 1.000000000000000000, 1.000000000000000000, 1.000000000000000222, 1.000000000000000000, 0.9999999999999997780, 1.000000000000000222, 0.9999999999999997780, 1.000000000000000000, 1.000000000000000222, 1.000000000000000000, 0.9999999999999997780, 0.9999999999999997780, 1.000000000000000000, 0.9999999999999997780, 1.000000000000000000, 1.000000000000000000, 1.000000000000000000, 1.000000000000000222, 0.9999999999999997780, 1.000000000000000000, 1.000000000000000222, 1.000000000000000000, 0.9999999999999997780, 1.000000000000000000, 1.000000000000000000, 1.000000000000000222, 0.9999999999999997780, 1.000000000000000222, 1.000000000000000000, 1.000000000000000000, 1.000000000000000222, 1.000000000000000000, 1.000000000000000000, 1.000000000000000222, 1.000000000000000000, 1.000000000000000444, 0.9999999999999996669, 1.000000000000000444, 0.9999999999999997780, 1.000000000000000000, 1.000000000000000222, 0.9999999999999996669, 1.000000000000000444, 1.000000000000000000, 1.000000000000000000, 1.000000000000000222, 1.000000000000000444, 1.000000000000000000, 0.9999999999999996669, 1.000000000000000444, 0.9999999999999997780, 0.9999999999999997780, 0.9999999999999997780, 1.000000000000000222, 1.000000000000000000, 0.9999999999999996669, 1.000000000000000222, 1.000000000000000000, 1.000000000000000444, 0.9999999999999997780, 1.000000000000000000, 1.000000000000000222, 1.000000000000000222, 1.000000000000000222, 1.000000000000000222, 1.000000000000000000, 1.000000000000000000, 1.000000000000000000, 1.000000000000000000, 1.000000000000000000, 1.000000000000000444, 1.000000000000000000, 0.9999999999999997780, 1.000000000000000000, 1.000000000000000222, 1.000000000000000000, 1.000000000000000222, 1.000000000000000222, 1.000000000000000000, 0.9999999999999997780, 0.9999999999999997780, 1.000000000000000222, 0.9999999999999997780, 1.000000000000000000, 1.000000000000000222, 1.000000000000000000, 1.000000000000000222, 1.000000000000000000, 0.9999999999999997780, 1.000000000000000000, 0.9999999999999997780, 1.000000000000000222, 1.000000000000000000, 0.9999999999999997780, 0.9999999999999997780, 1.000000000000000222, 1.000000000000000000, 1.000000000000000222, 0.9999999999999996669, 1.000000000000000000, 1.000000000000000222, 0.9999999999999997780, 1.000000000000000000, 1.000000000000000000, 1.000000000000000222, 1.000000000000000222, 1.000000000000000000, 1.000000000000000222, 1.000000000000000222),
 ( 0.3333333333333333703, 0.3333333333333333703, 0.3333333333333333703, 0.3333333333333333703, 0.3333333333333333148, 0.3333333333333334259, 0.3333333333333333703, 0.3333333333333333148, 0.3333333333333334259, 0.3333333333333333148, 0.3333333333333334259, 0.3333333333333332038, 0.3333333333333333703, 0.3333333333333332593, 0.3333333333333333703, 0.3333333333333332593, 0.3333333333333334814, 0.3333333333333334259, 0.3333333333333333703, 0.3333333333333334259, 0.3333333333333334259, 0.3333333333333332038, 0.3333333333333335369, 0.3333333333333333148, 0.3333333333333333148, 0.3333333333333334259, 0.3333333333333333703, 0.3333333333333333148, 0.3333333333333334259, 0.3333333333333333148, 0.3333333333333335369, 0.3333333333333333148, 0.3333333333333334259, 0.3333333333333333148, 0.3333333333333334259, 0.3333333333333333703, 0.3333333333333333148, 0.3333333333333333703, 0.3333333333333334259, 0.3333333333333333703, 0.3333333333333334259, 0.3333333333333333703, 0.3333333333333334814, 0.3333333333333333148, 0.3333333333333334259, 0.3333333333333332593, 0.3333333333333335369, 0.3333333333333332593, 0.3333333333333334259, 0.3333333333333333148, 0.3333333333333333703, 0.3333333333333334259, 0.3333333333333333148, 0.3333333333333334814, 0.3333333333333332593, 0.3333333333333333703, 0.3333333333333332593, 0.3333333333333335369, 0.3333333333333333148, 0.3333333333333334259, 0.3333333333333334259, 0.3333333333333334259, 0.3333333333333333148, 0.3333333333333333148, 0.3333333333333333703, 0.3333333333333333703, 0.3333333333333333703, 0.3333333333333334259, 0.3333333333333333148, 0.3333333333333333703, 0.3333333333333333703, 0.3333333333333332593, 0.3333333333333334259, 0.3333333333333333703, 0.3333333333333333703, 0.3333333333333333148, 0.3333333333333333148, 0.3333333333333334259, 0.3333333333333333148, 0.3333333333333334259, 0.3333333333333333148, 0.3333333333333334259, 0.3333333333333333703, 0.3333333333333334259, 0.3333333333333333703, 0.3333333333333333703, 0.3333333333333333148, 0.3333333333333335369, 0.3333333333333332593, 0.3333333333333334814, 0.3333333333333333703, 0.3333333333333333703, 0.3333333333333333148, 0.3333333333333333703, 0.3333333333333334259, 0.3333333333333334259, 0.3333333333333333148, 0.3333333333333333703, 0.3333333333333334259, 0.3333333333333333148, 0.3333333333333333703, 0.3333333333333334814, 0.3333333333333332038, 0.3333333333333334814, 0.3333333333333333703, 0.3333333333333333148, 0.3333333333333334259, 0.3333333333333333148, 0.3333333333333334259, 0.3333333333333332593, 0.3333333333333333703, 0.3333333333333334259, 0.3333333333333333148, 0.3333333333333333703, 0.3333333333333333148, 0.3333333333333334259, 0.3333333333333333703, 0.3333333333333333703, 0.3333333333333333703, 0.3333333333333334259, 0.3333333333333332038, 0.3333333333333334259, 0.3333333333333334259, 0.3333333333333333703, 0.3333333333333333703, 0.3333333333333332593, 0.3333333333333333703, 0.3333333333333333148, 0.3333333333333334259, 0.3333333333333332593, 0.3333333333333334259, 0.3333333333333333703, 0.3333333333333334259, 0.3333333333333334259, 0.3333333333333333148, 0.3333333333333334259, 0.3333333333333334259, 0.3333333333333332593, 0.3333333333333334259, 0.3333333333333333703, 0.3333333333333333703, 0.3333333333333333148, 0.3333333333333334259, 0.3333333333333333703, 0.3333333333333334259, 0.3333333333333334259, 0.3333333333333333703, 0.3333333333333333703, 0.3333333333333334814, 0.3333333333333333703, 0.3333333333333333703, 0.3333333333333335369, 0.3333333333333332593, 0.3333333333333334259, 0.3333333333333333148, 0.3333333333333334259, 0.3333333333333334259, 0.3333333333333334259, 0.3333333333333332593, 0.3333333333333333148, 0.3333333333333333703, 0.3333333333333334259, 0.3333333333333333148, 0.3333333333333333703, 0.3333333333333333148, 0.3333333333333334259, 0.3333333333333333148, 0.3333333333333334259, 0.3333333333333333148, 0.3333333333333334259, 0.3333333333333333703, 0.3333333333333334259, 0.3333333333333333703, 0.3333333333333334259, 0.3333333333333333148, 0.3333333333333333703, 0.3333333333333333703, 0.3333333333333334259, 0.3333333333333333703, 0.3333333333333334259, 0.3333333333333333703, 0.3333333333333333703, 0.3333333333333334259, 0.3333333333333334814, 0.3333333333333333703, 0.3333333333333333703, 0.3333333333333334814, 0.3333333333333333148, 0.3333333333333333703, 0.3333333333333333148, 0.3333333333333333703, 0.3333333333333333148, 0.3333333333333334259, 0.3333333333333334259, 0.3333333333333333703, 0.3333333333333333703, 0.3333333333333333703, 0.3333333333333333703, 0.3333333333333334259, 0.3333333333333332593, 0.3333333333333333703, 0.3333333333333333703, 0.3333333333333333703, 0.3333333333333333148, 0.3333333333333333703, 0.3333333333333333148, 0.3333333333333334259, 0.3333333333333333148, 0.3333333333333333703, 0.3333333333333333703, 0.3333333333333334259, 0.3333333333333333703, 0.3333333333333333148, 0.3333333333333333703, 0.3333333333333333703, 0.3333333333333333148, 0.3333333333333333703, 0.3333333333333333148, 0.3333333333333333703, 0.3333333333333333703, 0.3333333333333334814, 0.3333333333333333148, 0.3333333333333334259, 0.3333333333333334259, 0.3333333333333333703, 0.3333333333333334259, 0.3333333333333333703, 0.3333333333333334259, 0.3333333333333332593, 0.3333333333333334259, 0.3333333333333333148, 0.3333333333333334259, 0.3333333333333333148, 0.3333333333333334259, 0.3333333333333332593, 0.3333333333333335369, 0.3333333333333332038, 0.3333333333333334259, 0.3333333333333333703, 0.3333333333333333148, 0.3333333333333334259, 0.3333333333333333148, 0.3333333333333333148, 0.3333333333333333148, 0.3333333333333334814, 0.3333333333333332593, 0.3333333333333334259, 0.3333333333333333148, 0.3333333333333333148, 0.3333333333333334814, 0.3333333333333333703, 0.3333333333333334259, 0.3333333333333333148, 0.3333333333333333703, 0.3333333333333332593, 0.3333333333333334814, 0.3333333333333333148, 0.3333333333333334259, 0.3333333333333333148, 0.3333333333333334259, 0.3333333333333333703, 0.3333333333333333703, 0.3333333333333334259, 0.3333333333333333148, 0.3333333333333334814, 0.3333333333333333703, 0.3333333333333333703, 0.3333333333333334814, 0.3333333333333333703, 0.3333333333333332593, 0.3333333333333334259, 0.3333333333333332593, 0.3333333333333334814, 0.3333333333333333148, 0.3333333333333333703, 0.3333333333333333703, 0.3333333333333334259, 0.3333333333333333703, 0.3333333333333333703, 0.3333333333333333148, 0.3333333333333334259, 0.3333333333333334259, 0.3333333333333333703, 0.3333333333333334259, 0.3333333333333333148, 0.3333333333333333703, 0.3333333333333334259, 0.3333333333333333703, 0.3333333333333333148, 0.3333333333333334259, 0.3333333333333333703, 0.3333333333333333148, 0.3333333333333333148, 0.3333333333333334259, 0.3333333333333333148, 0.3333333333333333703, 0.3333333333333333703, 0.3333333333333333703, 0.3333333333333334259, 0.3333333333333334259, 0.3333333333333333148, 0.3333333333333334259, 0.3333333333333333148, 0.3333333333333334814, 0.3333333333333332593, 0.3333333333333334814, 0.3333333333333333703, 0.3333333333333333703, 0.3333333333333334259, 0.3333333333333333703, 0.3333333333333333703, 0.3333333333333333703, 0.3333333333333333703, 0.3333333333333334814, 0.3333333333333333148, 0.3333333333333334259, 0.3333333333333333148, 0.3333333333333333703, 0.3333333333333333703, 0.3333333333333333703, 0.3333333333333335369, 0.3333333333333333703, 0.3333333333333333148, 0.3333333333333334814, 0.3333333333333334259, 0.3333333333333333148, 0.3333333333333333148, 0.3333333333333335369, 0.3333333333333332593, 0.3333333333333333703, 0.3333333333333333148, 0.3333333333333333703, 0.3333333333333333703, 0.3333333333333332593, 0.3333333333333334259, 0.3333333333333332593, 0.3333333333333335369, 0.3333333333333333148, 0.3333333333333333703, 0.3333333333333334259, 0.3333333333333333703, 0.3333333333333333703, 0.3333333333333334814, 0.3333333333333333148, 0.3333333333333333148, 0.3333333333333334259, 0.3333333333333333148, 0.3333333333333333703, 0.3333333333333334814, 0.3333333333333333703, 0.3333333333333333703, 0.3333333333333333703, 0.3333333333333333703, 0.3333333333333334814, 0.3333333333333333703, 0.3333333333333334814, 0.3333333333333333703, 0.3333333333333333703, 0.3333333333333333148, 0.3333333333333334259, 0.3333333333333333148, 0.3333333333333334259, 0.3333333333333333148, 0.3333333333333333703, 0.3333333333333334814, 0.3333333333333333148, 0.3333333333333333148, 0.3333333333333333703, 0.3333333333333333703, 0.3333333333333333703, 0.3333333333333334259, 0.3333333333333333148, 0.3333333333333333703, 0.3333333333333334259, 0.3333333333333333148, 0.3333333333333333703, 0.3333333333333332593, 0.3333333333333333703, 0.3333333333333334259, 0.3333333333333333703, 0.3333333333333333703, 0.3333333333333333703, 0.3333333333333333703, 0.3333333333333334814, 0.3333333333333333703, 0.3333333333333334259, 0.3333333333333334259),
 ( 0.3333333333333333703, 0.3333333333333333703, 0.3333333333333333703, 0.3333333333333333703, 0.3333333333333333148, 0.3333333333333334259, 0.3333333333333333703, 0.3333333333333333148, 0.3333333333333334259, 0.3333333333333333148, 0.3333333333333334259, 0.3333333333333332038, 0.3333333333333333703, 0.3333333333333332593, 0.3333333333333333703, 0.3333333333333332593, 0.3333333333333334814, 0.3333333333333334259, 0.3333333333333333703, 0.3333333333333334259, 0.3333333333333334259, 0.3333333333333332038, 0.3333333333333335369, 0.3333333333333333148, 0.3333333333333333148, 0.3333333333333334259, 0.3333333333333333703, 0.3333333333333333148, 0.3333333333333334259, 0.3333333333333333148, 0.3333333333333335369, 0.3333333333333333148, 0.3333333333333334259, 0.3333333333333333148, 0.3333333333333334259, 0.3333333333333333703, 0.3333333333333333148, 0.3333333333333333703, 0.3333333333333334259, 0.3333333333333333703, 0.3333333333333334259, 0.3333333333333333703, 0.3333333333333334814, 0.3333333333333333148, 0.3333333333333334259, 0.3333333333333332593, 0.3333333333333335369, 0.3333333333333332593, 0.3333333333333334259, 0.3333333333333333148, 0.3333333333333333703, 0.3333333333333334259, 0.3333333333333333148, 0.3333333333333334814, 0.3333333333333332593, 0.3333333333333333703, 0.3333333333333332593, 0.3333333333333335369, 0.3333333333333333148, 0.3333333333333334259, 0.3333333333333334259, 0.3333333333333334259, 0.3333333333333333148, 0.3333333333333333148, 0.3333333333333333703, 0.3333333333333333703, 0.3333333333333333703, 0.3333333333333334259, 0.3333333333333333148, 0.3333333333333333703, 0.3333333333333333703, 0.3333333333333332593, 0.3333333333333334259, 0.3333333333333333703, 0.3333333333333333703, 0.3333333333333333148, 0.3333333333333333148, 0.3333333333333334259, 0.3333333333333333148, 0.3333333333333334259, 0.3333333333333333148, 0.3333333333333334259, 0.3333333333333333703, 0.3333333333333334259, 0.3333333333333333703, 0.3333333333333333703, 0.3333333333333333148, 0.3333333333333335369, 0.3333333333333332593, 0.3333333333333334814, 0.3333333333333333703, 0.3333333333333333703, 0.3333333333333333148, 0.3333333333333333703, 0.3333333333333334259, 0.3333333333333334259, 0.3333333333333333148, 0.3333333333333333703, 0.3333333333333334259, 0.3333333333333333148, 0.3333333333333333703, 0.3333333333333334814, 0.3333333333333332038, 0.3333333333333334814, 0.3333333333333333703, 0.3333333333333333148, 0.3333333333333334259, 0.3333333333333333148, 0.3333333333333334259, 0.3333333333333332593, 0.3333333333333333703, 0.3333333333333334259, 0.3333333333333333148, 0.3333333333333333703, 0.3333333333333333148, 0.3333333333333334259, 0.3333333333333333703, 0.3333333333333333703, 0.3333333333333333703, 0.3333333333333334259, 0.3333333333333332038, 0.3333333333333334259, 0.3333333333333334259, 0.3333333333333333703, 0.3333333333333333703, 0.3333333333333332593, 0.3333333333333333703, 0.3333333333333333148, 0.3333333333333334259, 0.3333333333333332593, 0.3333333333333334259, 0.3333333333333333703, 0.3333333333333334259, 0.3333333333333334259, 0.3333333333333333148, 0.3333333333333334259, 0.3333333333333334259, 0.3333333333333332593, 0.3333333333333334259, 0.3333333333333333703, 0.3333333333333333703, 0.3333333333333333148, 0.3333333333333334259, 0.3333333333333333703, 0.3333333333333334259, 0.3333333333333334259, 0.3333333333333333703, 0.3333333333333333703, 0.3333333333333334814, 0.3333333333333333703, 0.3333333333333333703, 0.3333333333333335369, 0.3333333333333332593, 0.3333333333333334259, 0.3333333333333333148, 0.3333333333333334259, 0.3333333333333334259, 0.3333333333333334259, 0.3333333333333332593, 0.3333333333333333148, 0.3333333333333333703, 0.3333333333333334259, 0.3333333333333333148, 0.3333333333333333703, 0.3333333333333333148, 0.3333333333333334259, 0.3333333333333333148, 0.3333333333333334259, 0.3333333333333333148, 0.3333333333333334259, 0.3333333333333333703, 0.3333333333333334259, 0.3333333333333333703, 0.3333333333333334259, 0.3333333333333333148, 0.3333333333333333703, 0.3333333333333333703, 0.3333333333333334259, 0.3333333333333333703, 0.3333333333333334259, 0.3333333333333333703, 0.3333333333333333703, 0.3333333333333334259, 0.3333333333333334814, 0.3333333333333333703, 0.3333333333333333703, 0.3333333333333334814, 0.3333333333333333148, 0.3333333333333333703, 0.3333333333333333148, 0.3333333333333333703, 0.3333333333333333148, 0.3333333333333334259, 0.3333333333333334259, 0.3333333333333333703, 0.3333333333333333703, 0.3333333333333333703, 0.3333333333333333703, 0.3333333333333334259, 0.3333333333333332593, 0.3333333333333333703, 0.3333333333333333703, 0.3333333333333333703, 0.3333333333333333148, 0.3333333333333333703, 0.3333333333333333148, 0.3333333333333334259, 0.3333333333333333148, 0.3333333333333333703, 0.3333333333333333703, 0.3333333333333334259, 0.3333333333333333703, 0.3333333333333333148, 0.3333333333333333703, 0.3333333333333333703, 0.3333333333333333148, 0.3333333333333333703, 0.3333333333333333148, 0.3333333333333333703, 0.3333333333333333703, 0.3333333333333334814, 0.3333333333333333148, 0.3333333333333334259, 0.3333333333333334259, 0.3333333333333333703, 0.3333333333333334259, 0.3333333333333333703, 0.3333333333333334259, 0.3333333333333332593, 0.3333333333333334259, 0.3333333333333333148, 0.3333333333333334259, 0.3333333333333333148, 0.3333333333333334259, 0.3333333333333332593, 0.3333333333333335369, 0.3333333333333332038, 0.3333333333333334259, 0.3333333333333333703, 0.3333333333333333148, 0.3333333333333334259, 0.3333333333333333148, 0.3333333333333333148, 0.3333333333333333148, 0.3333333333333334814, 0.3333333333333332593, 0.3333333333333334259, 0.3333333333333333148, 0.3333333333333333148, 0.3333333333333334814, 0.3333333333333333703, 0.3333333333333334259, 0.3333333333333333148, 0.3333333333333333703, 0.3333333333333332593, 0.3333333333333334814, 0.3333333333333333148, 0.3333333333333334259, 0.3333333333333333148, 0.3333333333333334259, 0.3333333333333333703, 0.3333333333333333703, 0.3333333333333334259, 0.3333333333333333148, 0.3333333333333334814, 0.3333333333333333703, 0.3333333333333333703, 0.3333333333333334814, 0.3333333333333333703, 0.3333333333333332593, 0.3333333333333334259, 0.3333333333333332593, 0.3333333333333334814, 0.3333333333333333148, 0.3333333333333333703, 0.3333333333333333703, 0.3333333333333334259, 0.3333333333333333703, 0.3333333333333333703, 0.3333333333333333148, 0.3333333333333334259, 0.3333333333333334259, 0.3333333333333333703, 0.3333333333333334259, 0.3333333333333333148, 0.3333333333333333703, 0.3333333333333334259, 0.3333333333333333703, 0.3333333333333333148, 0.3333333333333334259, 0.3333333333333333703, 0.3333333333333333148, 0.3333333333333333148, 0.3333333333333334259, 0.3333333333333333148, 0.3333333333333333703, 0.3333333333333333703, 0.3333333333333333703, 0.3333333333333334259, 0.3333333333333334259, 0.3333333333333333148, 0.3333333333333334259, 0.3333333333333333148, 0.3333333333333334814, 0.3333333333333332593, 0.3333333333333334814, 0.3333333333333333703, 0.3333333333333333703, 0.3333333333333334259, 0.3333333333333333703, 0.3333333333333333703, 0.3333333333333333703, 0.3333333333333333703, 0.3333333333333334814, 0.3333333333333333148, 0.3333333333333334259, 0.3333333333333333148, 0.3333333333333333703, 0.3333333333333333703, 0.3333333333333333703, 0.3333333333333335369, 0.3333333333333333703, 0.3333333333333333148, 0.3333333333333334814, 0.3333333333333334259, 0.3333333333333333148, 0.3333333333333333148, 0.3333333333333335369, 0.3333333333333332593, 0.3333333333333333703, 0.3333333333333333148, 0.3333333333333333703, 0.3333333333333333703, 0.3333333333333332593, 0.3333333333333334259, 0.3333333333333332593, 0.3333333333333335369, 0.3333333333333333148, 0.3333333333333333703, 0.3333333333333334259, 0.3333333333333333703, 0.3333333333333333703, 0.3333333333333334814, 0.3333333333333333148, 0.3333333333333333148, 0.3333333333333334259, 0.3333333333333333148, 0.3333333333333333703, 0.3333333333333334814, 0.3333333333333333703, 0.3333333333333333703, 0.3333333333333333703, 0.3333333333333333703, 0.3333333333333334814, 0.3333333333333333703, 0.3333333333333334814, 0.3333333333333333703, 0.3333333333333333703, 0.3333333333333333148, 0.3333333333333334259, 0.3333333333333333148, 0.3333333333333334259, 0.3333333333333333148, 0.3333333333333333703, 0.3333333333333334814, 0.3333333333333333148, 0.3333333333333333148, 0.3333333333333333703, 0.3333333333333333703, 0.3333333333333333703, 0.3333333333333334259, 0.3333333333333333148, 0.3333333333333333703, 0.3333333333333334259, 0.3333333333333333148, 0.3333333333333333703, 0.3333333333333332593, 0.3333333333333333703, 0.3333333333333334259, 0.3333333333333333703, 0.3333333333333333703, 0.3333333333333333703, 0.3333333333333333703, 0.3333333333333334814, 0.3333333333333333703, 0.3333333333333334259, 0.3333333333333334259),
 ( 1.000000000000000000, 1.000000000000000000, 1.000000000000000222, 1.000000000000000000, 0.9999999999999996669, 1.000000000000000444, 0.9999999999999997780, 1.000000000000000000, 1.000000000000000222, 0.9999999999999996669, 1.000000000000000222, 0.9999999999999996669, 1.000000000000000000, 0.9999999999999997780, 1.000000000000000222, 0.9999999999999997780, 1.000000000000000222, 1.000000000000000222, 0.9999999999999997780, 1.000000000000000222, 1.000000000000000222, 0.9999999999999996669, 1.000000000000000444, 0.9999999999999997780, 1.000000000000000000, 1.000000000000000222, 1.000000000000000000, 1.000000000000000000, 1.000000000000000000, 1.000000000000000000, 1.000000000000000222, 1.000000000000000000, 1.000000000000000000, 0.9999999999999997780, 1.000000000000000000, 1.000000000000000000, 1.000000000000000000, 1.000000000000000000, 0.9999999999999997780, 1.000000000000000222, 1.000000000000000000, 1.000000000000000000, 1.000000000000000444, 0.9999999999999997780, 1.000000000000000222, 0.9999999999999996669, 1.000000000000000444, 0.9999999999999997780, 1.000000000000000000, 0.9999999999999997780, 1.000000000000000000, 1.000000000000000222, 0.9999999999999997780, 1.000000000000000444, 0.9999999999999997780, 1.000000000000000000, 0.9999999999999996669, 1.000000000000000444, 0.9999999999999997780, 1.000000000000000444, 1.000000000000000000, 1.000000000000000444, 0.9999999999999996669, 1.000000000000000000, 0.9999999999999996669, 1.000000000000000444, 0.9999999999999997780, 1.000000000000000000, 1.000000000000000000, 1.000000000000000000, 1.000000000000000000, 0.9999999999999996669, 1.000000000000000000, 1.000000000000000222, 0.9999999999999997780, 1.000000000000000000, 0.9999999999999997780, 0.9999999999999997780, 1.000000000000000000, 1.000000000000000222, 0.9999999999999997780, 1.000000000000000000, 1.000000000000000222, 1.000000000000000222, 1.000000000000000222, 0.9999999999999997780, 1.000000000000000000, 1.000000000000000222, 0.9999999999999997780, 1.000000000000000222, 1.000000000000000222, 0.9999999999999997780, 0.9999999999999997780, 0.9999999999999997780, 1.000000000000000444, 1.000000000000000000, 1.000000000000000000, 1.000000000000000000, 1.000000000000000222, 0.9999999999999997780, 1.000000000000000000, 1.000000000000000444, 0.9999999999999996669, 1.000000000000000444, 1.000000000000000000, 1.000000000000000000, 1.000000000000000222, 0.9999999999999997780, 1.000000000000000444, 0.9999999999999996669, 1.000000000000000444, 1.000000000000000000, 0.9999999999999997780, 1.000000000000000222, 0.9999999999999996669, 1.000000000000000222, 1.000000000000000000, 1.000000000000000222, 0.9999999999999997780, 1.000000000000000222, 0.9999999999999996669, 1.000000000000000222, 1.000000000000000222, 1.000000000000000222, 1.000000000000000000, 0.9999999999999997780, 1.000000000000000000, 0.9999999999999997780, 1.000000000000000000, 0.9999999999999997780, 0.9999999999999997780, 1.000000000000000222, 1.000000000000000222, 1.000000000000000222, 0.9999999999999997780, 0.9999999999999997780, 1.000000000000000444, 0.9999999999999997780, 1.000000000000000000, 0.9999999999999997780, 1.000000000000000000, 0.9999999999999997780, 1.000000000000000222, 1.000000000000000000, 1.000000000000000000, 1.000000000000000222, 1.000000000000000000, 0.9999999999999997780, 1.000000000000000444, 1.000000000000000000, 1.000000000000000000, 1.000000000000000444, 0.9999999999999997780, 1.000000000000000222, 0.9999999999999997780, 1.000000000000000444, 1.000000000000000000, 1.000000000000000222, 0.9999999999999997780, 0.9999999999999997780, 1.000000000000000000, 1.000000000000000444, 0.9999999999999996669, 1.000000000000000000, 1.000000000000000222, 1.000000000000000222, 0.9999999999999997780, 1.000000000000000222, 0.9999999999999997780, 1.000000000000000222, 1.000000000000000000, 1.000000000000000000, 0.9999999999999997780, 1.000000000000000444, 0.9999999999999997780, 1.000000000000000222, 0.9999999999999996669, 1.000000000000000444, 0.9999999999999996669, 1.000000000000000222, 1.000000000000000000, 1.000000000000000000, 1.000000000000000000, 1.000000000000000444, 1.000000000000000222, 0.9999999999999997780, 1.000000000000000444, 0.9999999999999997780, 1.000000000000000000, 0.9999999999999996669, 1.000000000000000000, 0.9999999999999996669, 1.000000000000000000, 1.000000000000000222, 1.000000000000000000, 0.9999999999999997780, 1.000000000000000222, 1.000000000000000000, 1.000000000000000222, 0.9999999999999996669, 1.000000000000000000, 1.000000000000000000, 1.000000000000000000, 0.9999999999999997780, 1.000000000000000000, 1.000000000000000000, 1.000000000000000222, 1.000000000000000000, 1.000000000000000000, 0.9999999999999997780, 1.000000000000000000, 1.000000000000000222, 0.9999999999999997780, 1.000000000000000000, 1.000000000000000222, 1.000000000000000000, 1.000000000000000000, 0.9999999999999997780, 0.9999999999999997780, 1.000000000000000000, 1.000000000000000000, 0.9999999999999997780, 1.000000000000000000, 1.000000000000000000, 1.000000000000000000, 1.000000000000000222, 1.000000000000000000, 1.000000000000000000, 0.9999999999999997780, 1.000000000000000000, 0.9999999999999997780, 1.000000000000000444, 0.9999999999999997780, 1.000000000000000222, 0.9999999999999997780, 1.000000000000000444, 0.9999999999999994449, 1.000000000000000444, 0.9999999999999997780, 1.000000000000000222, 1.000000000000000000, 1.000000000000000000, 0.9999999999999997780, 1.000000000000000000, 1.000000000000000000, 0.9999999999999997780, 1.000000000000000000, 1.000000000000000000, 0.9999999999999997780, 1.000000000000000222, 1.000000000000000000, 1.000000000000000222, 0.9999999999999997780, 1.000000000000000222, 0.9999999999999997780, 1.000000000000000222, 0.9999999999999997780, 1.000000000000000444, 0.9999999999999996669, 1.000000000000000222, 0.9999999999999997780, 1.000000000000000000, 1.000000000000000000, 1.000000000000000000, 1.000000000000000222, 1.000000000000000222, 1.000000000000000000, 1.000000000000000444, 1.000000000000000222, 0.9999999999999997780, 1.000000000000000222, 0.9999999999999996669, 1.000000000000000444, 0.9999999999999997780, 0.9999999999999997780, 1.000000000000000222, 1.000000000000000000, 1.000000000000000222, 1.000000000000000000, 1.000000000000000000, 1.000000000000000222, 1.000000000000000000, 0.9999999999999997780, 1.000000000000000222, 0.9999999999999997780, 1.000000000000000000, 1.000000000000000222, 1.000000000000000000, 0.9999999999999997780, 0.9999999999999997780, 1.000000000000000000, 0.9999999999999997780, 1.000000000000000000, 1.000000000000000000, 1.000000000000000000, 1.000000000000000222, 0.9999999999999997780, 1.000000000000000000, 1.000000000000000222, 1.000000000000000000, 0.9999999999999997780, 1.000000000000000000, 1.000000000000000000, 1.000000000000000222, 0.9999999999999997780, 1.000000000000000222, 1.000000000000000000, 1.000000000000000000, 1.000000000000000222, 1.000000000000000000, 1.000000000000000000, 1.000000000000000222, 1.000000000000000000, 1.000000000000000444, 0.9999999999999996669, 1.000000000000000444, 0.9999999999999997780, 1.000000000000000000, 1.000000000000000222, 0.9999999999999996669, 1.000000000000000444, 1.000000000000000000, 1.000000000000000000, 1.000000000000000222, 1.000000000000000444, 1.000000000000000000, 0.9999999999999996669, 1.000000000000000444, 0.9999999999999997780, 0.9999999999999997780, 0.9999999999999997780, 1.000000000000000222, 1.000000000000000000, 0.9999999999999996669, 1.000000000000000222, 1.000000000000000000, 1.000000000000000444, 0.9999999999999997780, 1.000000000000000000, 1.000000000000000222, 1.000000000000000222, 1.000000000000000222, 1.000000000000000222, 1.000000000000000000, 1.000000000000000000, 1.000000000000000000, 1.000000000000000000, 1.000000000000000000, 1.000000000000000444, 1.000000000000000000, 0.9999999999999997780, 1.000000000000000000, 1.000000000000000222, 1.000000000000000000, 1.000000000000000222, 1.000000000000000222, 1.000000000000000000, 0.9999999999999997780, 0.9999999999999997780, 1.000000000000000222, 0.9999999999999997780, 1.000000000000000000, 1.000000000000000222, 1.000000000000000000, 1.000000000000000222, 1.000000000000000000, 0.9999999999999997780, 1.000000000000000000, 0.9999999999999997780, 1.000000000000000222, 1.000000000000000000, 0.9999999999999997780, 0.9999999999999997780, 1.000000000000000222, 1.000000000000000000, 1.000000000000000222, 0.9999999999999996669, 1.000000000000000000, 1.000000000000000222, 0.9999999999999997780, 1.000000000000000000, 1.000000000000000000, 1.000000000000000222, 1.000000000000000222, 1.000000000000000000, 1.000000000000000222, 1.000000000000000222),
 ( 0.3333333333333333703, 0.3333333333333333703, 0.3333333333333333703, 0.3333333333333333703, 0.3333333333333333148, 0.3333333333333334259, 0.3333333333333333703, 0.3333333333333333148, 0.3333333333333334259, 0.3333333333333333148, 0.3333333333333334259, 0.3333333333333332038, 0.3333333333333333703, 0.3333333333333332593, 0.3333333333333333703, 0.3333333333333332593, 0.3333333333333334814, 0.3333333333333334259, 0.3333333333333333703, 0.3333333333333334259, 0.3333333333333334259, 0.3333333333333332038, 0.3333333333333335369, 0.3333333333333333148, 0.3333333333333333148, 0.3333333333333334259, 0.3333333333333333703, 0.3333333333333333148, 0.3333333333333334259, 0.3333333333333333148, 0.3333333333333335369, 0.3333333333333333148, 0.3333333333333334259, 0.3333333333333333148, 0.3333333333333334259, 0.3333333333333333703, 0.3333333333333333148, 0.3333333333333333703, 0.3333333333333334259, 0.3333333333333333703, 0.3333333333333334259, 0.3333333333333333703, 0.3333333333333334814, 0.3333333333333333148, 0.3333333333333334259, 0.3333333333333332593, 0.3333333333333335369, 0.3333333333333332593, 0.3333333333333334259, 0.3333333333333333148, 0.3333333333333333703, 0.3333333333333334259, 0.3333333333333333148, 0.3333333333333334814, 0.3333333333333332593, 0.3333333333333333703, 0.3333333333333332593, 0.3333333333333335369, 0.3333333333333333148, 0.3333333333333334259, 0.3333333333333334259, 0.3333333333333334259, 0.3333333333333333148, 0.3333333333333333148, 0.3333333333333333703, 0.3333333333333333703, 0.3333333333333333703, 0.3333333333333334259, 0.3333333333333333148, 0.3333333333333333703, 0.3333333333333333703, 0.3333333333333332593, 0.3333333333333334259, 0.3333333333333333703, 0.3333333333333333703, 0.3333333333333333148, 0.3333333333333333148, 0.3333333333333334259, 0.3333333333333333148, 0.3333333333333334259, 0.3333333333333333148, 0.3333333333333334259, 0.3333333333333333703, 0.3333333333333334259, 0.3333333333333333703, 0.3333333333333333703, 0.3333333333333333148, 0.3333333333333335369, 0.3333333333333332593, 0.3333333333333334814, 0.3333333333333333703, 0.3333333333333333703, 0.3333333333333333148, 0.3333333333333333703, 0.3333333333333334259, 0.3333333333333334259, 0.3333333333333333148, 0.3333333333333333703, 0.3333333333333334259, 0.3333333333333333148, 0.3333333333333333703, 0.3333333333333334814, 0.3333333333333332038, 0.3333333333333334814, 0.3333333333333333703, 0.3333333333333333148, 0.3333333333333334259, 0.3333333333333333148, 0.3333333333333334259, 0.3333333333333332593, 0.3333333333333333703, 0.3333333333333334259, 0.3333333333333333148, 0.3333333333333333703, 0.3333333333333333148, 0.3333333333333334259, 0.3333333333333333703, 0.3333333333333333703, 0.3333333333333333703, 0.3333333333333334259, 0.3333333333333332038, 0.3333333333333334259, 0.3333333333333334259, 0.3333333333333333703, 0.3333333333333333703, 0.3333333333333332593, 0.3333333333333333703, 0.3333333333333333148, 0.3333333333333334259, 0.3333333333333332593, 0.3333333333333334259, 0.3333333333333333703, 0.3333333333333334259, 0.3333333333333334259, 0.3333333333333333148, 0.3333333333333334259, 0.3333333333333334259, 0.3333333333333332593, 0.3333333333333334259, 0.3333333333333333703, 0.3333333333333333703, 0.3333333333333333148, 0.3333333333333334259, 0.3333333333333333703, 0.3333333333333334259, 0.3333333333333334259, 0.3333333333333333703, 0.3333333333333333703, 0.3333333333333334814, 0.3333333333333333703, 0.3333333333333333703, 0.3333333333333335369, 0.3333333333333332593, 0.3333333333333334259, 0.3333333333333333148, 0.3333333333333334259, 0.3333333333333334259, 0.3333333333333334259, 0.3333333333333332593, 0.3333333333333333148, 0.3333333333333333703, 0.3333333333333334259, 0.3333333333333333148, 0.3333333333333333703, 0.3333333333333333148, 0.3333333333333334259, 0.3333333333333333148, 0.3333333333333334259, 0.3333333333333333148, 0.3333333333333334259, 0.3333333333333333703, 0.3333333333333334259, 0.3333333333333333703, 0.3333333333333334259, 0.3333333333333333148, 0.3333333333333333703, 0.3333333333333333703, 0.3333333333333334259, 0.3333333333333333703, 0.3333333333333334259, 0.3333333333333333703, 0.3333333333333333703, 0.3333333333333334259, 0.3333333333333334814, 0.3333333333333333703, 0.3333333333333333703, 0.3333333333333334814, 0.3333333333333333148, 0.3333333333333333703, 0.3333333333333333148, 0.3333333333333333703, 0.3333333333333333148, 0.3333333333333334259, 0.3333333333333334259, 0.3333333333333333703, 0.3333333333333333703, 0.3333333333333333703, 0.3333333333333333703, 0.3333333333333334259, 0.3333333333333332593, 0.3333333333333333703, 0.3333333333333333703, 0.3333333333333333703, 0.3333333333333333148, 0.3333333333333333703, 0.3333333333333333148, 0.3333333333333334259, 0.3333333333333333148, 0.3333333333333333703, 0.3333333333333333703, 0.3333333333333334259, 0.3333333333333333703, 0.3333333333333333148, 0.3333333333333333703, 0.3333333333333333703, 0.3333333333333333148, 0.3333333333333333703, 0.3333333333333333148, 0.3333333333333333703, 0.3333333333333333703, 0.3333333333333334814, 0.3333333333333333148, 0.3333333333333334259, 0.3333333333333334259, 0.3333333333333333703, 0.3333333333333334259, 0.3333333333333333703, 0.3333333333333334259, 0.3333333333333332593, 0.3333333333333334259, 0.3333333333333333148, 0.3333333333333334259, 0.3333333333333333148, 0.3333333333333334259, 0.3333333333333332593, 0.3333333333333335369, 0.3333333333333332038, 0.3333333333333334259, 0.3333333333333333703, 0.3333333333333333148, 0.3333333333333334259, 0.3333333333333333148, 0.3333333333333333148, 0.3333333333333333148, 0.3333333333333334814, 0.3333333333333332593, 0.3333333333333334259, 0.3333333333333333148, 0.3333333333333333148, 0.3333333333333334814, 0.3333333333333333703, 0.3333333333333334259, 0.3333333333333333148, 0.3333333333333333703, 0.3333333333333332593, 0.3333333333333334814, 0.3333333333333333148, 0.3333333333333334259, 0.3333333333333333148, 0.3333333333333334259, 0.3333333333333333703, 0.3333333333333333703, 0.3333333333333334259, 0.3333333333333333148, 0.3333333333333334814, 0.3333333333333333703, 0.3333333333333333703, 0.3333333333333334814, 0.3333333333333333703, 0.3333333333333332593, 0.3333333333333334259, 0.3333333333333332593, 0.3333333333333334814, 0.3333333333333333148, 0.3333333333333333703, 0.3333333333333333703, 0.3333333333333334259, 0.3333333333333333703, 0.3333333333333333703, 0.3333333333333333148, 0.3333333333333334259, 0.3333333333333334259, 0.3333333333333333703, 0.3333333333333334259, 0.3333333333333333148, 0.3333333333333333703, 0.3333333333333334259, 0.3333333333333333703, 0.3333333333333333148, 0.3333333333333334259, 0.3333333333333333703, 0.3333333333333333148, 0.3333333333333333148, 0.3333333333333334259, 0.3333333333333333148, 0.3333333333333333703, 0.3333333333333333703, 0.3333333333333333703, 0.3333333333333334259, 0.3333333333333334259, 0.3333333333333333148, 0.3333333333333334259, 0.3333333333333333148, 0.3333333333333334814, 0.3333333333333332593, 0.3333333333333334814, 0.3333333333333333703, 0.3333333333333333703, 0.3333333333333334259, 0.3333333333333333703, 0.3333333333333333703, 0.3333333333333333703, 0.3333333333333333703, 0.3333333333333334814, 0.3333333333333333148, 0.3333333333333334259, 0.3333333333333333148, 0.3333333333333333703, 0.3333333333333333703, 0.3333333333333333703, 0.3333333333333335369, 0.3333333333333333703, 0.3333333333333333148, 0.3333333333333334814, 0.3333333333333334259, 0.3333333333333333148, 0.3333333333333333148, 0.3333333333333335369, 0.3333333333333332593, 0.3333333333333333703, 0.3333333333333333148, 0.3333333333333333703, 0.3333333333333333703, 0.3333333333333332593, 0.3333333333333334259, 0.3333333333333332593, 0.3333333333333335369, 0.3333333333333333148, 0.3333333333333333703, 0.3333333333333334259, 0.3333333333333333703, 0.3333333333333333703, 0.3333333333333334814, 0.3333333333333333148, 0.3333333333333333148, 0.3333333333333334259, 0.3333333333333333148, 0.3333333333333333703, 0.3333333333333334814, 0.3333333333333333703, 0.3333333333333333703, 0.3333333333333333703, 0.3333333333333333703, 0.3333333333333334814, 0.3333333333333333703, 0.3333333333333334814, 0.3333333333333333703, 0.3333333333333333703, 0.3333333333333333148, 0.3333333333333334259, 0.3333333333333333148, 0.3333333333333334259, 0.3333333333333333148, 0.3333333333333333703, 0.3333333333333334814, 0.3333333333333333148, 0.3333333333333333148, 0.3333333333333333703, 0.3333333333333333703, 0.3333333333333333703, 0.3333333333333334259, 0.3333333333333333148, 0.3333333333333333703, 0.3333333333333334259, 0.3333333333333333148, 0.3333333333333333703, 0.3333333333333332593, 0.3333333333333333703, 0.3333333333333334259, 0.3333333333333333703, 0.3333333333333333703, 0.3333333333333333703, 0.3333333333333333703, 0.3333333333333334814, 0.3333333333333333703, 0.3333333333333334259, 0.3333333333333334259),
 ( 0.3333333333333333703, 0.3333333333333333703, 0.3333333333333333703, 0.3333333333333333703, 0.3333333333333333148, 0.3333333333333334259, 0.3333333333333333703, 0.3333333333333333148, 0.3333333333333334259, 0.3333333333333333148, 0.3333333333333334259, 0.3333333333333332038, 0.3333333333333333703, 0.3333333333333332593, 0.3333333333333333703, 0.3333333333333332593, 0.3333333333333334814, 0.3333333333333334259, 0.3333333333333333703, 0.3333333333333334259, 0.3333333333333334259, 0.3333333333333332038, 0.3333333333333335369, 0.3333333333333333148, 0.3333333333333333148, 0.3333333333333334259, 0.3333333333333333703, 0.3333333333333333148, 0.3333333333333334259, 0.3333333333333333148, 0.3333333333333335369, 0.3333333333333333148, 0.3333333333333334259, 0.3333333333333333148, 0.3333333333333334259, 0.3333333333333333703, 0.3333333333333333148, 0.3333333333333333703, 0.3333333333333334259, 0.3333333333333333703, 0.3333333333333334259, 0.3333333333333333703, 0.3333333333333334814, 0.3333333333333333148, 0.3333333333333334259, 0.3333333333333332593, 0.3333333333333335369, 0.3333333333333332593, 0.3333333333333334259, 0.3333333333333333148, 0.3333333333333333703, 0.3333333333333334259, 0.3333333333333333148, 0.3333333333333334814, 0.3333333333333332593, 0.3333333333333333703, 0.3333333333333332593, 0.3333333333333335369, 0.3333333333333333148, 0.3333333333333334259, 0.3333333333333334259, 0.3333333333333334259, 0.3333333333333333148, 0.3333333333333333148, 0.3333333333333333703, 0.3333333333333333703, 0.3333333333333333703, 0.3333333333333334259, 0.3333333333333333148, 0.3333333333333333703, 0.3333333333333333703, 0.3333333333333332593, 0.3333333333333334259, 0.3333333333333333703, 0.3333333333333333703, 0.3333333333333333148, 0.3333333333333333148, 0.3333333333333334259, 0.3333333333333333148, 0.3333333333333334259, 0.3333333333333333148, 0.3333333333333334259, 0.3333333333333333703, 0.3333333333333334259, 0.3333333333333333703, 0.3333333333333333703, 0.3333333333333333148, 0.3333333333333335369, 0.3333333333333332593, 0.3333333333333334814, 0.3333333333333333703, 0.3333333333333333703, 0.3333333333333333148, 0.3333333333333333703, 0.3333333333333334259, 0.3333333333333334259, 0.3333333333333333148, 0.3333333333333333703, 0.3333333333333334259, 0.3333333333333333148, 0.3333333333333333703, 0.3333333333333334814, 0.3333333333333332038, 0.3333333333333334814, 0.3333333333333333703, 0.3333333333333333148, 0.3333333333333334259, 0.3333333333333333148, 0.3333333333333334259, 0.3333333333333332593, 0.3333333333333333703, 0.3333333333333334259, 0.3333333333333333148, 0.3333333333333333703, 0.3333333333333333148, 0.3333333333333334259, 0.3333333333333333703, 0.3333333333333333703, 0.3333333333333333703, 0.3333333333333334259, 0.3333333333333332038, 0.3333333333333334259, 0.3333333333333334259, 0.3333333333333333703, 0.3333333333333333703, 0.3333333333333332593, 0.3333333333333333703, 0.3333333333333333148, 0.3333333333333334259, 0.3333333333333332593, 0.3333333333333334259, 0.3333333333333333703, 0.3333333333333334259, 0.3333333333333334259, 0.3333333333333333148, 0.3333333333333334259, 0.3333333333333334259, 0.3333333333333332593, 0.3333333333333334259, 0.3333333333333333703, 0.3333333333333333703, 0.3333333333333333148, 0.3333333333333334259, 0.3333333333333333703, 0.3333333333333334259, 0.3333333333333334259, 0.3333333333333333703, 0.3333333333333333703, 0.3333333333333334814, 0.3333333333333333703, 0.3333333333333333703, 0.3333333333333335369, 0.3333333333333332593, 0.3333333333333334259, 0.3333333333333333148, 0.3333333333333334259, 0.3333333333333334259, 0.3333333333333334259, 0.3333333333333332593, 0.3333333333333333148, 0.3333333333333333703, 0.3333333333333334259, 0.3333333333333333148, 0.3333333333333333703, 0.3333333333333333148, 0.3333333333333334259, 0.3333333333333333148, 0.3333333333333334259, 0.3333333333333333148, 0.3333333333333334259, 0.3333333333333333703, 0.3333333333333334259, 0.3333333333333333703, 0.3333333333333334259, 0.3333333333333333148, 0.3333333333333333703, 0.3333333333333333703, 0.3333333333333334259, 0.3333333333333333703, 0.3333333333333334259, 0.3333333333333333703, 0.3333333333333333703, 0.3333333333333334259, 0.3333333333333334814, 0.3333333333333333703, 0.3333333333333333703, 0.3333333333333334814, 0.3333333333333333148, 0.3333333333333333703, 0.3333333333333333148, 0.3333333333333333703, 0.3333333333333333148, 0.3333333333333334259, 0.3333333333333334259, 0.3333333333333333703, 0.3333333333333333703, 0.3333333333333333703, 0.3333333333333333703, 0.3333333333333334259, 0.3333333333333332593, 0.3333333333333333703, 0.3333333333333333703, 0.3333333333333333703, 0.3333333333333333148, 0.3333333333333333703, 0.3333333333333333148, 0.3333333333333334259, 0.3333333333333333148, 0.3333333333333333703, 0.3333333333333333703, 0.3333333333333334259, 0.3333333333333333703, 0.3333333333333333148, 0.3333333333333333703, 0.3333333333333333703, 0.3333333333333333148, 0.3333333333333333703, 0.3333333333333333148, 0.3333333333333333703, 0.3333333333333333703, 0.3333333333333334814, 0.3333333333333333148, 0.3333333333333334259, 0.3333333333333334259, 0.3333333333333333703, 0.3333333333333334259, 0.3333333333333333703, 0.3333333333333334259, 0.3333333333333332593, 0.3333333333333334259, 0.3333333333333333148, 0.3333333333333334259, 0.3333333333333333148, 0.3333333333333334259, 0.3333333333333332593, 0.3333333333333335369, 0.3333333333333332038, 0.3333333333333334259, 0.3333333333333333703, 0.3333333333333333148, 0.3333333333333334259, 0.3333333333333333148, 0.3333333333333333148, 0.3333333333333333148, 0.3333333333333334814, 0.3333333333333332593, 0.3333333333333334259, 0.3333333333333333148, 0.3333333333333333148, 0.3333333333333334814, 0.3333333333333333703, 0.3333333333333334259, 0.3333333333333333148, 0.3333333333333333703, 0.3333333333333332593, 0.3333333333333334814, 0.3333333333333333148, 0.3333333333333334259, 0.3333333333333333148, 0.3333333333333334259, 0.3333333333333333703, 0.3333333333333333703, 0.3333333333333334259, 0.3333333333333333148, 0.3333333333333334814, 0.3333333333333333703, 0.3333333333333333703, 0.3333333333333334814, 0.3333333333333333703, 0.3333333333333332593, 0.3333333333333334259, 0.3333333333333332593, 0.3333333333333334814, 0.3333333333333333148, 0.3333333333333333703, 0.3333333333333333703, 0.3333333333333334259, 0.3333333333333333703, 0.3333333333333333703, 0.3333333333333333148, 0.3333333333333334259, 0.3333333333333334259, 0.3333333333333333703, 0.3333333333333334259, 0.3333333333333333148, 0.3333333333333333703, 0.3333333333333334259, 0.3333333333333333703, 0.3333333333333333148, 0.3333333333333334259, 0.3333333333333333703, 0.3333333333333333148, 0.3333333333333333148, 0.3333333333333334259, 0.3333333333333333148, 0.3333333333333333703, 0.3333333333333333703, 0.3333333333333333703, 0.3333333333333334259, 0.3333333333333334259, 0.3333333333333333148, 0.3333333333333334259, 0.3333333333333333148, 0.3333333333333334814, 0.3333333333333332593, 0.3333333333333334814, 0.3333333333333333703, 0.3333333333333333703, 0.3333333333333334259, 0.3333333333333333703, 0.3333333333333333703, 0.3333333333333333703, 0.3333333333333333703, 0.3333333333333334814, 0.3333333333333333148, 0.3333333333333334259, 0.3333333333333333148, 0.3333333333333333703, 0.3333333333333333703, 0.3333333333333333703, 0.3333333333333335369, 0.3333333333333333703, 0.3333333333333333148, 0.3333333333333334814, 0.3333333333333334259, 0.3333333333333333148, 0.3333333333333333148, 0.3333333333333335369, 0.3333333333333332593, 0.3333333333333333703, 0.3333333333333333148, 0.3333333333333333703, 0.3333333333333333703, 0.3333333333333332593, 0.3333333333333334259, 0.3333333333333332593, 0.3333333333333335369, 0.3333333333333333148, 0.3333333333333333703, 0.3333333333333334259, 0.3333333333333333703, 0.3333333333333333703, 0.3333333333333334814, 0.3333333333333333148, 0.3333333333333333148, 0.3333333333333334259, 0.3333333333333333148, 0.3333333333333333703, 0.3333333333333334814, 0.3333333333333333703, 0.3333333333333333703, 0.3333333333333333703, 0.3333333333333333703, 0.3333333333333334814, 0.3333333333333333703, 0.3333333333333334814, 0.3333333333333333703, 0.3333333333333333703, 0.3333333333333333148, 0.3333333333333334259, 0.3333333333333333148, 0.3333333333333334259, 0.3333333333333333148, 0.3333333333333333703, 0.3333333333333334814, 0.3333333333333333148, 0.3333333333333333148, 0.3333333333333333703, 0.3333333333333333703, 0.3333333333333333703, 0.3333333333333334259, 0.3333333333333333148, 0.3333333333333333703, 0.3333333333333334259, 0.3333333333333333148, 0.3333333333333333703, 0.3333333333333332593, 0.3333333333333333703, 0.3333333333333334259, 0.3333333333333333703, 0.3333333333333333703, 0.3333333333333333703, 0.3333333333333333703, 0.3333333333333334814, 0.3333333333333333703, 0.3333333333333334259, 0.3333333333333334259),
 ( 1.000000000000000000, 1.000000000000000000, 1.000000000000000222, 1.000000000000000000, 0.9999999999999996669, 1.000000000000000444, 0.9999999999999997780, 1.000000000000000000, 1.000000000000000222, 0.9999999999999996669, 1.000000000000000222, 0.9999999999999996669, 1.000000000000000000, 0.9999999999999997780, 1.000000000000000222, 0.9999999999999997780, 1.000000000000000222, 1.000000000000000222, 0.9999999999999997780, 1.000000000000000222, 1.000000000000000222, 0.9999999999999996669, 1.000000000000000444, 0.9999999999999997780, 1.000000000000000000, 1.000000000000000222, 1.000000000000000000, 1.000000000000000000, 1.000000000000000000, 1.000000000000000000, 1.000000000000000222, 1.000000000000000000, 1.000000000000000000, 0.9999999999999997780, 1.000000000000000000, 1.000000000000000000, 1.000000000000000000, 1.000000000000000000, 0.9999999999999997780, 1.000000000000000222, 1.000000000000000000, 1.000000000000000000, 1.000000000000000444, 0.9999999999999997780, 1.000000000000000222, 0.9999999999999996669, 1.000000000000000444, 0.9999999999999997780, 1.000000000000000000, 0.9999999999999997780, 1.000000000000000000, 1.000000000000000222, 0.9999999999999997780, 1.000000000000000444, 0.9999999999999997780, 1.000000000000000000, 0.9999999999999996669, 1.000000000000000444, 0.9999999999999997780, 1.000000000000000444, 1.000000000000000000, 1.000000000000000444, 0.9999999999999996669, 1.000000000000000000, 0.9999999999999996669, 1.000000000000000444, 0.9999999999999997780, 1.000000000000000000, 1.000000000000000000, 1.000000000000000000, 1.000000000000000000, 0.9999999999999996669, 1.000000000000000000, 1.000000000000000222, 0.9999999999999997780, 1.000000000000000000, 0.9999999999999997780, 0.9999999999999997780, 1.000000000000000000, 1.000000000000000222, 0.9999999999999997780, 1.000000000000000000, 1.000000000000000222, 1.000000000000000222, 1.000000000000000222, 0.9999999999999997780, 1.000000000000000000, 1.000000000000000222, 0.9999999999999997780, 1.000000000000000222, 1.000000000000000222, 0.9999999999999997780, 0.9999999999999997780, 0.9999999999999997780, 1.000000000000000444, 1.000000000000000000, 1.000000000000000000, 1.000000000000000000, 1.000000000000000222, 0.9999999999999997780, 1.000000000000000000, 1.000000000000000444, 0.9999999999999996669, 1.000000000000000444, 1.000000000000000000, 1.000000000000000000, 1.000000000000000222, 0.9999999999999997780, 1.000000000000000444, 0.9999999999999996669, 1.000000000000000444, 1.000000000000000000, 0.9999999999999997780, 1.000000000000000222, 0.9999999999999996669, 1.000000000000000222, 1.000000000000000000, 1.000000000000000222, 0.9999999999999997780, 1.000000000000000222, 0.9999999999999996669, 1.000000000000000222, 1.000000000000000222, 1.000000000000000222, 1.000000000000000000, 0.9999999999999997780, 1.000000000000000000, 0.9999999999999997780, 1.000000000000000000, 0.9999999999999997780, 0.9999999999999997780, 1.000000000000000222, 1.000000000000000222, 1.000000000000000222, 0.9999999999999997780, 0.9999999999999997780, 1.000000000000000444, 0.9999999999999997780, 1.000000000000000000, 0.9999999999999997780, 1.000000000000000000, 0.9999999999999997780, 1.000000000000000222, 1.000000000000000000, 1.000000000000000000, 1.000000000000000222, 1.000000000000000000, 0.9999999999999997780, 1.000000000000000444, 1.000000000000000000, 1.000000000000000000, 1.000000000000000444, 0.9999999999999997780, 1.000000000000000222, 0.9999999999999997780, 1.000000000000000444, 1.000000000000000000, 1.000000000000000222, 0.9999999999999997780, 0.9999999999999997780, 1.000000000000000000, 1.000000000000000444, 0.9999999999999996669, 1.000000000000000000, 1.000000000000000222, 1.000000000000000222, 0.9999999999999997780, 1.000000000000000222, 0.9999999999999997780, 1.000000000000000222, 1.000000000000000000, 1.000000000000000000, 0.9999999999999997780, 1.000000000000000444, 0.9999999999999997780, 1.000000000000000222, 0.9999999999999996669, 1.000000000000000444, 0.9999999999999996669, 1.000000000000000222, 1.000000000000000000, 1.000000000000000000, 1.000000000000000000, 1.000000000000000444, 1.000000000000000222, 0.9999999999999997780, 1.000000000000000444, 0.9999999999999997780, 1.000000000000000000, 0.9999999999999996669, 1.000000000000000000, 0.9999999999999996669, 1.000000000000000000, 1.000000000000000222, 1.000000000000000000, 0.9999999999999997780, 1.000000000000000222, 1.000000000000000000, 1.000000000000000222, 0.9999999999999996669, 1.000000000000000000, 1.000000000000000000, 1.000000000000000000, 0.9999999999999997780, 1.000000000000000000, 1.000000000000000000, 1.000000000000000222, 1.000000000000000000, 1.000000000000000000, 0.9999999999999997780, 1.000000000000000000, 1.000000000000000222, 0.9999999999999997780, 1.000000000000000000, 1.000000000000000222, 1.000000000000000000, 1.000000000000000000, 0.9999999999999997780, 0.9999999999999997780, 1.000000000000000000, 1.000000000000000000, 0.9999999999999997780, 1.000000000000000000, 1.000000000000000000, 1.000000000000000000, 1.000000000000000222, 1.000000000000000000, 1.000000000000000000, 0.9999999999999997780, 1.000000000000000000, 0.9999999999999997780, 1.000000000000000444, 0.9999999999999997780, 1.000000000000000222, 0.9999999999999997780, 1.000000000000000444, 0.9999999999999994449, 1.000000000000000444, 0.9999999999999997780, 1.000000000000000222, 1.000000000000000000, 1.000000000000000000, 0.9999999999999997780, 1.000000000000000000, 1.000000000000000000, 0.9999999999999997780, 1.000000000000000000, 1.000000000000000000, 0.9999999999999997780, 1.000000000000000222, 1.000000000000000000, 1.000000000000000222, 0.9999999999999997780, 1.000000000000000222, 0.9999999999999997780, 1.000000000000000222, 0.9999999999999997780, 1.000000000000000444, 0.9999999999999996669, 1.000000000000000222, 0.9999999999999997780, 1.000000000000000000, 1.000000000000000000, 1.000000000000000000, 1.000000000000000222, 1.000000000000000222, 1.000000000000000000, 1.000000000000000444, 1.000000000000000222, 0.9999999999999997780, 1.000000000000000222, 0.9999999999999996669, 1.000000000000000444, 0.9999999999999997780, 0.9999999999999997780, 1.000000000000000222, 1.000000000000000000, 1.000000000000000222, 1.000000000000000000, 1.000000000000000000, 1.000000000000000222, 1.000000000000000000, 0.9999999999999997780, 1.000000000000000222, 0.9999999999999997780, 1.000000000000000000, 1.000000000000000222, 1.000000000000000000, 0.9999999999999997780, 0.9999999999999997780, 1.000000000000000000, 0.9999999999999997780, 1.000000000000000000, 1.000000000000000000, 1.000000000000000000, 1.000000000000000222, 0.9999999999999997780, 1.000000000000000000, 1.000000000000000222, 1.000000000000000000, 0.9999999999999997780, 1.000000000000000000, 1.000000000000000000, 1.000000000000000222, 0.9999999999999997780, 1.000000000000000222, 1.000000000000000000, 1.000000000000000000, 1.000000000000000222, 1.000000000000000000, 1.000000000000000000, 1.000000000000000222, 1.000000000000000000, 1.000000000000000444, 0.9999999999999996669, 1.000000000000000444, 0.9999999999999997780, 1.000000000000000000, 1.000000000000000222, 0.9999999999999996669, 1.000000000000000444, 1.000000000000000000, 1.000000000000000000, 1.000000000000000222, 1.000000000000000444, 1.000000000000000000, 0.9999999999999996669, 1.000000000000000444, 0.9999999999999997780, 0.9999999999999997780, 0.9999999999999997780, 1.000000000000000222, 1.000000000000000000, 0.9999999999999996669, 1.000000000000000222, 1.000000000000000000, 1.000000000000000444, 0.9999999999999997780, 1.000000000000000000, 1.000000000000000222, 1.000000000000000222, 1.000000000000000222, 1.000000000000000222, 1.000000000000000000, 1.000000000000000000, 1.000000000000000000, 1.000000000000000000, 1.000000000000000000, 1.000000000000000444, 1.000000000000000000, 0.9999999999999997780, 1.000000000000000000, 1.000000000000000222, 1.000000000000000000, 1.000000000000000222, 1.000000000000000222, 1.000000000000000000, 0.9999999999999997780, 0.9999999999999997780, 1.000000000000000222, 0.9999999999999997780, 1.000000000000000000, 1.000000000000000222, 1.000000000000000000, 1.000000000000000222, 1.000000000000000000, 0.9999999999999997780, 1.000000000000000000, 0.9999999999999997780, 1.000000000000000222, 1.000000000000000000, 0.9999999999999997780, 0.9999999999999997780, 1.000000000000000222, 1.000000000000000000, 1.000000000000000222, 0.9999999999999996669, 1.000000000000000000, 1.000000000000000222, 0.9999999999999997780, 1.000000000000000000, 1.000000000000000000, 1.000000000000000222, 1.000000000000000222, 1.000000000000000000, 1.000000000000000222, 1.000000000000000222) ) ) 
 REPRESENTATION_ITEM ( '' )  SURFACE ( )  );
#125220=CARTESIAN_POINT ( 'NONE',  ( 1.366164030173490973, 2.173753390890633685, -0.3800739277931909355 ) ) ;
#125221=CARTESIAN_POINT ( 'NONE',  ( 2.530887537405112298, 2.193952394701288000, 0.5517939747049571686 ) ) ;
#125224=CARTESIAN_POINT ( 'NONE',  ( 1.986290607305480460, -1.112306265806988437, 1.429831149274364721 ) ) ;
#125226=CARTESIAN_POINT ( 'NONE',  ( 3.274530738273524033, -0.3788105498489474088, -1.877706502262687760 ) ) ;
#125227=CARTESIAN_POINT ( 'NONE',  ( 4.316890830952234914, -1.536253448065309613, 1.388129241271539138 ) ) ;
#125229=CARTESIAN_POINT ( 'NONE',  ( 2.272288244244465627, -1.214158342444570327, 1.553133305774859974 ) ) ;
#125230=CARTESIAN_POINT ( 'NONE',  ( 0.4813100693330485957, 1.798698175156054457, -0.6901501906162701427 ) ) ;
#125231=CARTESIAN_POINT ( 'NONE',  ( 3.731198135974967300, -1.728734619261709904, 0.7151963084984153118 ) ) ;
#125232=CARTESIAN_POINT ( 'NONE',  ( 1.893647147081824356, 2.006347305559322169, -1.140069799644787940 ) ) ;
#125234=CARTESIAN_POINT ( 'NONE',  ( 3.437814515362676016, 1.178941034414218603, 1.440021488233768521 ) ) ;
#125239=CARTESIAN_POINT ( 'NONE',  ( 0.7332070197069834316, 0.1568218392365756941, 2.100289424198895194 ) ) ;
#125242=CARTESIAN_POINT ( 'NONE',  ( 6.661405305706385782, 0.3767857563467743032, -2.128362917677539379 ) ) ;
#125243=CARTESIAN_POINT ( 'NONE',  ( 2.021885665735908333, -0.4598567139443253682, 2.069992740399699382 ) ) ;
#125244=CARTESIAN_POINT ( 'NONE',  ( -0.1403647893034008221, -1.563942476893056543, -1.277904792927646582 ) ) ;
#125248=CARTESIAN_POINT ( 'NONE',  ( 1.476082264964494906, 1.286352913914396545, 1.737049067733025032 ) ) ;
#125250=CARTESIAN_POINT ( 'NONE',  ( 6.825078400183526739, 3.708013787890347857, 2.270222819304415385 ) ) ;
#125253=CARTESIAN_POINT ( 'NONE',  ( 4.803922858132807505, -1.082837210388952309, -1.700963621564715700 ) ) ;
#125257=CARTESIAN_POINT ( 'NONE',  ( 0.1985910703563107393, -2.262096406685298877, -0.05156929113746439725 ) ) ;
#125261=CARTESIAN_POINT ( 'NONE',  ( 6.239861269555550649, 2.010826412442122013, -0.1511553674920090573 ) ) ;
#125265=CARTESIAN_POINT ( 'NONE',  ( 3.387030231456603424, 1.558874866368621159, -0.7386201850746020314 ) ) ;
#125268=CARTESIAN_POINT ( 'NONE',  ( 0.8953273879380260203, -0.6444125412686675380, 1.648433012593934155 ) ) ;
#125269=CARTESIAN_POINT ( 'NONE',  ( 2.086589530005359183, -1.236640506920426263, 1.588416314350507674 ) ) ;
#125271=CARTESIAN_POINT ( 'NONE',  ( 4.630015379333586978, -1.354682855507854278, -1.741961856448564383 ) ) ;
#125275=CARTESIAN_POINT ( 'NONE',  ( 2.719513590175401063, 1.792643918890064247, 1.132349250948051500 ) ) ;
#125276=CARTESIAN_POINT ( 'NONE',  ( 3.462517696756307384, -1.944077823024586538, -0.5350690621670484148 ) ) ;
#125277=CARTESIAN_POINT ( 'NONE',  ( 3.462975342835975301, -1.477922853017235916, 1.047338699574466014 ) ) ;
#125281=CARTESIAN_POINT ( 'NONE',  ( 0.1450994221751950586, -1.442925249786636943, -1.190247126510869613 ) ) ;
#125284=CARTESIAN_POINT ( 'NONE',  ( 6.094357461763901362, -1.817385979143220309, -0.1739998769475574192 ) ) ;
#125286=CARTESIAN_POINT ( 'NONE',  ( 2.905391412282500863, -1.844872930762898600, 0.5157873856561823178 ) ) ;
#125295=CARTESIAN_POINT ( 'NONE',  ( 2.724977724663907530, 1.532976055022855499, -1.465462182430438798 ) ) ;
#125296=CARTESIAN_POINT ( 'NONE',  ( -0.02988540731099428513, 1.418068428043406382, -1.986943242881351601 ) ) ;
#125298=CARTESIAN_POINT ( 'NONE',  ( 4.604731966549804767, 1.525920046185350376, -1.248162976031294003 ) ) ;
#125299=CARTESIAN_POINT ( 'NONE',  ( -0.05247892273943338681, -1.838936383286099652, 0.8197664084235550819 ) ) ;
#125300=CARTESIAN_POINT ( 'NONE',  ( 6.368375629516933145, -2.076896536817146810, -0.4110353314962181259 ) ) ;
#125302=CARTESIAN_POINT ( 'NONE',  ( 1.645070734656968625, -0.3017366986639741788, -2.048123538821471801 ) ) ;
#125303=CARTESIAN_POINT ( 'NONE',  ( 2.589705103518041618, -1.936761303218867969, -0.1426656448052856518 ) ) ;
#125307=CARTESIAN_POINT ( 'NONE',  ( 3.662131271747073757, -1.403999256393541284, 1.549221476816674548 ) ) ;
#125310=CARTESIAN_POINT ( 'NONE',  ( 0.9788403037365877024, -1.637337388150851725, -0.7752084675131820646 ) ) ;
#125312=CARTESIAN_POINT ( 'NONE',  ( 5.742855475442601332, 0.4270144693867898300, 2.165010647329483895 ) ) ;
#125314=CARTESIAN_POINT ( 'NONE',  ( 4.647634198631804381, -1.703412986257560879, -1.402924735643434673 ) ) ;
#125317=CARTESIAN_POINT ( 'NONE',  ( 2.648957786072099641, 0.2360777847093403214, 1.897596177352772306 ) ) ;
#125319=CARTESIAN_POINT ( 'NONE',  ( 5.160626937512653001, -0.6942339714755951796, -1.950645400549338104 ) ) ;
#125321=CARTESIAN_POINT ( 'NONE',  ( 2.325270847726228940, -0.0006328605136555342939, 2.161883445422786654 ) ) ;
#125322=CARTESIAN_POINT ( 'NONE',  ( 4.581673536070863584, -1.032772929490553215, 1.932928240684625099 ) ) ;
#125324=ORIENTED_EDGE ( 'NONE', *, *, #58676, .F. ) ;
#125326=SURFACE_STYLE_USAGE ( .BOTH. , #126392 ) ;
#125331=CARTESIAN_POINT ( 'NONE',  ( 5.787960296632533641, -1.308950758395693414, -1.603975846202657429 ) ) ;
#125332=CARTESIAN_POINT ( 'NONE',  ( 4.811117629317255506, 1.676929503210132122, 0.9481960042460689797 ) ) ;
#125333=CARTESIAN_POINT ( 'NONE',  ( 6.468375645409351726, -2.076397406075684682, -0.4129765506453788038 ) ) ;
#125336=CARTESIAN_POINT ( 'NONE',  ( 5.383641442822343137, -1.871314765454759055, 0.6142198095173864170 ) ) ;
#125337=CARTESIAN_POINT ( 'NONE',  ( 6.562434020506859866, -2.092894318229638895, -0.9354203566987564500 ) ) ;
#125338=CARTESIAN_POINT ( 'NONE',  ( 4.934128534657983067, 0.9357288403324083292, -1.567518238613223813 ) ) ;
#125344=CARTESIAN_POINT ( 'NONE',  ( 2.718100415690410721, 1.734538518968967935, 0.6181264464550640936 ) ) ;
#125345=CARTESIAN_POINT ( 'NONE',  ( -0.07552757677437360595, -0.8618087116909570744, -1.817275918844815541 ) ) ;
#125346=CARTESIAN_POINT ( 'NONE',  ( 1.283028839759347894, -2.242172747002548316, 0.5046827817699239827 ) ) ;
#125347=CARTESIAN_POINT ( 'NONE',  ( 5.401206054008879320, -1.684469800357458302, 1.005230755432365175 ) ) ;
#125351=CARTESIAN_POINT ( 'NONE',  ( 0.5728211633247158874, 1.428863753495920763, -1.498466819491943269 ) ) ;
#125353=CARTESIAN_POINT ( 'NONE',  ( 1.118821681092090126, -0.04763362108583040627, 2.090370170816723494 ) ) ;
#125354=CARTESIAN_POINT ( 'NONE',  ( 1.111929834214450796, -0.8377583890188080584, -1.672643128629976772 ) ) ;
#125355=CARTESIAN_POINT ( 'NONE',  ( 1.792342068719571468, -1.899328565777322231, 0.6766080823841430503 ) ) ;
#125358=CARTESIAN_POINT ( 'NONE',  ( 2.225747907193951214, 1.688420964825324555, 0.4218146122960535482 ) ) ;
#125361=CARTESIAN_POINT ( 'NONE',  ( 2.367434161175852925, 1.691737554211050210, -0.3355112704105273624 ) ) ;
#125362=CARTESIAN_POINT ( 'NONE',  ( 3.105210138592546798, -0.4252477525170209605, 2.149737936336936883 ) ) ;
#125363=CARTESIAN_POINT ( 'NONE',  ( 0.1583034150156861219, 0.9959709328331721734, 1.419360398433693549 ) ) ;
#125364=CARTESIAN_POINT ( 'NONE',  ( 4.951907052881864502, 0.6945806438464275923, -2.094803410698709900 ) ) ;
#125366=CARTESIAN_POINT ( 'NONE',  ( 2.448294946665624749, -0.9317531996627312907, 1.961122280359078873 ) ) ;
#125367=CARTESIAN_POINT ( 'NONE',  ( 1.277666653898035021, 1.085793613588705853, 1.467558327050644484 ) ) ;
#125368=CARTESIAN_POINT ( 'NONE',  ( 3.766910327102332978, -0.2117226681838789426, -2.106763584193247940 ) ) ;
#125372=CARTESIAN_POINT ( 'NONE',  ( 3.984120879971131401, -2.267471576223866414, -0.3361144993852988594 ) ) ;
#125374=CARTESIAN_POINT ( 'NONE',  ( 6.727182134110200273, -0.004969159814478123736, 2.189081792362323586 ) ) ;
#125376=CARTESIAN_POINT ( 'NONE',  ( 6.164703477482621707, 0.6939275443377226349, 2.110173311658748663 ) ) ;
#125382=CARTESIAN_POINT ( 'NONE',  ( 4.096327398540238640, -0.3419367296172080017, 1.987046374476949095 ) ) ;
#125384=CARTESIAN_POINT ( 'NONE',  ( 3.678632908625163012, 1.312080992568062321, -1.591389186695492342 ) ) ;
#125389=CARTESIAN_POINT ( 'NONE',  ( 6.316381784907312280, 2.043361914081378128, 0.7923855730916644635 ) ) ;
#125390=CARTESIAN_POINT ( 'NONE',  ( 3.709611425391425854, 1.915599900965975433, 0.6298755557959597740 ) ) ;
#125391=CARTESIAN_POINT ( 'NONE',  ( 1.927068723821170559, -1.203646435588998420, -1.393412863611859454 ) ) ;
#125393=CARTESIAN_POINT ( 'NONE',  ( 0.09417432218480553674, -0.3651332853754212238, -1.691417143215419028 ) ) ;
#125395=CARTESIAN_POINT ( 'NONE',  ( 0.05395445667428447334, -1.494411465983748855, 1.746745294031383455 ) ) ;
#125397=CARTESIAN_POINT ( 'NONE',  ( 5.840765815766128632, 0.4347934677991367458, 2.220198762108383850 ) ) ;
#125399=CARTESIAN_POINT ( 'NONE',  ( 1.893330831959182836, 1.831869315246800189, -1.038985425167998633 ) ) ;
#125408=CARTESIAN_POINT ( 'NONE',  ( 2.795431959603801086, -0.1677860356435970368, -2.215157990583861203 ) ) ;
#125410=CARTESIAN_POINT ( 'NONE',  ( 0.06543086261080394150, -1.973449318085427340, -0.9880335165917543128 ) ) ;
#125413=CARTESIAN_POINT ( 'NONE',  ( 4.633228507203630997, 0.002057781214020309134, -1.962046631861932067 ) ) ;
#125421=CARTESIAN_POINT ( 'NONE',  ( 3.357788437482766675, -1.608272433257527556, -1.382313803475518244 ) ) ;
#125423=CARTESIAN_POINT ( 'NONE',  ( 5.120075222393803749, -1.153228217640640985, -1.828211184805514922 ) ) ;
#125424=CARTESIAN_POINT ( 'NONE',  ( 3.561895345837225779, -1.234009368583251165, 1.366721199326895952 ) ) ;
#125425=CARTESIAN_POINT ( 'NONE',  ( 4.856657812281613751, -1.900414607462055816, -0.6748505307947461063 ) ) ;
#125429=CARTESIAN_POINT ( 'NONE',  ( 6.527322169609689695, -1.143008000885838760, -1.312471774050189444 ) ) ;
#125430=CARTESIAN_POINT ( 'NONE',  ( 6.727182134110170075, 7.629137130509032971, 2.310944104600751281 ) ) ;
#125434=CARTESIAN_POINT ( 'NONE',  ( 4.012696165952275962, 1.530467462299599513, -1.526897427004340280 ) ) ;
#125437=CARTESIAN_POINT ( 'NONE',  ( 5.097029748277864591, 1.038832625704217527, -1.727738606215820205 ) ) ;
#125440=CARTESIAN_POINT ( 'NONE',  ( 3.151412294154242844, -1.766339975446712174, -1.245920677233211871 ) ) ;
#125441=CARTESIAN_POINT ( 'NONE',  ( 4.042224286460029958, 1.961553563453529492, 0.1965975345302218569 ) ) ;
#125443=CARTESIAN_POINT ( 'NONE',  ( 0.7984239956072606281, -0.8271026589724904676, 2.154427444091823851 ) ) ;
#125444=CARTESIAN_POINT ( 'NONE',  ( 2.073578556082512403, 1.972924284924733929, -0.5953725496260859895 ) ) ;
#125445=CARTESIAN_POINT ( 'NONE',  ( 5.091328012616338938, -0.6953414466571452568, 1.813493487445563046 ) ) ;
#125454=CARTESIAN_POINT ( 'NONE',  ( 2.380145745526092593, 1.357289424207007489, 1.739932290444376584 ) ) ;
#125456=CARTESIAN_POINT ( 'NONE',  ( 6.666857073735664052, 1.455856877570886887, -1.315125143065517532 ) ) ;
#125462=CARTESIAN_POINT ( 'NONE',  ( 5.367088761235753402, 1.773375748883701419, -0.4946613714205680967 ) ) ;
#125467=CARTESIAN_POINT ( 'NONE',  ( 6.310795917644286490, -0.5669512758468171487, -2.043305014803979525 ) ) ;
#125471=CARTESIAN_POINT ( 'NONE',  ( 0.5673477787482993362, 0.2024836561579176908, -2.050924697174760780 ) ) ;
#125474=CARTESIAN_POINT ( 'NONE',  ( 2.189708182147569460, -1.212837473668834098, -1.411683579110091458 ) ) ;
#125475=CARTESIAN_POINT ( 'NONE',  ( 4.352959896991869471, 0.3989296284454147412, -1.797357466088687961 ) ) ;
#125479=CARTESIAN_POINT ( 'NONE',  ( 6.610000000000029630, 4.695285100415147461, 2.562642482393460153 ) ) ;
#125481=CARTESIAN_POINT ( 'NONE',  ( 4.266400587755204477, 1.039063272370500668, 1.946970035688735390 ) ) ;
#125482=CARTESIAN_POINT ( 'NONE',  ( 5.817715961848279882, -2.209163325107537101, 0.4873710261694869095 ) ) ;
#125484=CARTESIAN_POINT ( 'NONE',  ( 0.07037084582631887575, 0.7337836260858082715, 1.766209603411242668 ) ) ;
#125485=CARTESIAN_POINT ( 'NONE',  ( 6.262892222096183126, -0.1014175117164286682, -1.913191589401983528 ) ) ;
#125488=CARTESIAN_POINT ( 'NONE',  ( 5.619756671179352736, -0.4603523440993939619, 1.855926886426211952 ) ) ;
#125489=CARTESIAN_POINT ( 'NONE',  ( 6.539320575229279342, 7.629137130509070275, 2.496737603865983868 ) ) ;
#125490=CARTESIAN_POINT ( 'NONE',  ( 1.287742131874554552, -0.8442722623961744777, 1.669378388412197767 ) ) ;
#125491=CARTESIAN_POINT ( 'NONE',  ( 2.114470590943520634, 1.957170936680457052, 0.4852650170619755565 ) ) ;
#125493=CARTESIAN_POINT ( 'NONE',  ( 3.879594643445562152, 1.983085605235184845, -0.7095211871808704274 ) ) ;
#125497=CARTESIAN_POINT ( 'NONE',  ( 3.094014924146833323, 1.284692261361711774, 1.558518293110554565 ) ) ;
#125501=CARTESIAN_POINT ( 'NONE',  ( 4.288457955665158750, -2.137403104576699242, -0.3218062170811594735 ) ) ;
#125507=CARTESIAN_POINT ( 'NONE',  ( 1.891327416536987105, 0.2117802020594385659, 2.160802721360413070 ) ) ;
#125510=CARTESIAN_POINT ( 'NONE',  ( 0.8371598888798935656, 0.7463826720714299423, -1.683355135116317847 ) ) ;
#125513=CARTESIAN_POINT ( 'NONE',  ( 1.646283778714407342, 0.6915601415973006150, 2.079641132013386517 ) ) ;
#125514=CARTESIAN_POINT ( 'NONE',  ( 6.883263157960376688, 2.059069814638575302, 2.260828084523508252 ) ) ;
#125515=CARTESIAN_POINT ( 'NONE',  ( 3.608526635699527141, -0.9147260449715814978, -2.069530211360113725 ) ) ;
#125517=CARTESIAN_POINT ( 'NONE',  ( 4.469935555517978720, -0.9463019959239076240, 1.780667052345537238 ) ) ;
#125523=CARTESIAN_POINT ( 'NONE',  ( 4.270580540438973394, -1.650736559713336771, -0.6384287733962620282 ) ) ;
#125526=CARTESIAN_POINT ( 'NONE',  ( 1.061710303787483989, 0.4109483673962707750, -2.065292405001526443 ) ) ;
#125535=CARTESIAN_POINT ( 'NONE',  ( 3.871829239884491791, 1.038646522470688671, 1.555605274479121114 ) ) ;
#125536=CARTESIAN_POINT ( 'NONE',  ( 4.557524383921963462, 1.659614545607337677, 1.237363147772299721 ) ) ;
#125544=CARTESIAN_POINT ( 'NONE',  ( 3.842202535371820993, -0.9690557767615382012, 1.705768119890891610 ) ) ;
#125546=CARTESIAN_POINT ( 'NONE',  ( 1.686874821769188237, -1.117660090026689979, -1.677749154088927774 ) ) ;
#125548=CARTESIAN_POINT ( 'NONE',  ( 6.639320575229278099, 0.5905802482995252678, 1.949996947996739172 ) ) ;
#125549=CARTESIAN_POINT ( 'NONE',  ( 0.5966796567213605851, 1.558732183387041781, -1.033768272189788950 ) ) ;
#125551=CARTESIAN_POINT ( 'NONE',  ( 3.023692480417307316, -0.3885771752702297799, 1.975188976417296072 ) ) ;
#125553=CARTESIAN_POINT ( 'NONE',  ( 3.691103677939993499, 1.816986910410453682, 1.086596289330623799 ) ) ;
#125555=CARTESIAN_POINT ( 'NONE',  ( 5.020015195830264787, 2.048331326439792210, -0.3003445753073652469 ) ) ;
#125557=CARTESIAN_POINT ( 'NONE',  ( 0.1168898295945815374, -0.09829507837614966104, 2.088553102151818219 ) ) ;
#125559=CARTESIAN_POINT ( 'NONE',  ( 4.998959831394860664, 1.517082468864182632, -1.015166198912627049 ) ) ;
#125560=ORIENTED_EDGE ( 'NONE', *, *, #69557, .T. ) ;
#125567=CARTESIAN_POINT ( 'NONE',  ( 6.639320575229252341, 0.005161017367553630275, 1.896863882003448021 ) ) ;
#125584=CARTESIAN_POINT ( 'NONE',  ( 1.938274800925225527, -1.057869798513750847, 1.661026717510836637 ) ) ;
#125585=CARTESIAN_POINT ( 'NONE',  ( 3.796500049179197589, 1.423950305759081214, -1.427950143821264506 ) ) ;
#125587=CARTESIAN_POINT ( 'NONE',  ( 6.727182134110194056, 3.682851444631680682, 2.702965647100654234 ) ) ;
#125588=CARTESIAN_POINT ( 'NONE',  ( 3.574349206294104242, -2.111947977397998777, -0.5846811180381800144 ) ) ;
#125590=CARTESIAN_POINT ( 'NONE',  ( 1.905176762840081528, 1.600281962709374062, 1.072135106281972616 ) ) ;
#125593=CARTESIAN_POINT ( 'NONE',  ( 0.2331563151865451988, 4.092570554693980789, -2.500672995626152861 ) ) ;
#125600=CARTESIAN_POINT ( 'NONE',  ( 5.513187957602974976, -1.795010045117376496, 0.4093405989887277663 ) ) ;
#125601=CARTESIAN_POINT ( 'NONE',  ( 2.631496214491501728, -0.1952657482040425496, 2.003584891602292473 ) ) ;
#125602=CARTESIAN_POINT ( 'NONE',  ( 4.218341386676929261, -1.908100849112413178, -1.281069462185228325 ) ) ;
#125603=CARTESIAN_POINT ( 'NONE',  ( -0.1291982275798625457, 6.946856551170387029, -2.669038260222480918 ) ) ;
#125604=CARTESIAN_POINT ( 'NONE',  ( 2.992830011424299830, 0.2227009285440742226, 1.847472864794322156 ) ) ;
#125606=DIRECTION ( 'NONE',  ( 2.949029909160572061E-17, 1.000000000000000000, -8.673600428462391266E-15 ) ) ;
#125607=CARTESIAN_POINT ( 'NONE',  ( 6.381121926128928479, -1.751337275642101510, -0.7685668267764720341 ) ) ;
#125611=CARTESIAN_POINT ( 'NONE',  ( 5.548407312280490444, -1.647412313956169605, 1.287198389022710998 ) ) ;
#125616=CARTESIAN_POINT ( 'NONE',  ( 5.865779507164840645, 1.698138087647281358, -0.3015940010741220978 ) ) ;
#125618=CARTESIAN_POINT ( 'NONE',  ( 1.863478119473166439, -0.08537559288352389308, -1.732189446134152266 ) ) ;
#125623=CARTESIAN_POINT ( 'NONE',  ( 5.735278773323231327, -0.04571225511484919291, -2.170743740471086980 ) ) ;
#125624=CARTESIAN_POINT ( 'NONE',  ( 4.775911370473768791, 1.053640644303525331, 1.490772598166143048 ) ) ;
#125625=CARTESIAN_POINT ( 'NONE',  ( 2.694135368495911731, 0.9291169126603683326, -1.727816930623335745 ) ) ;
#125629=CARTESIAN_POINT ( 'NONE',  ( 2.121885542695590487, -0.4617877489709980576, 2.069441001874790409 ) ) ;
#125632=CARTESIAN_POINT ( 'NONE',  ( 0.5497785174156321064, 1.531638494488884339, 1.392999266381978130 ) ) ;
#125635=CARTESIAN_POINT ( 'NONE',  ( 3.299698294838341539, 2.007417196159299255, -0.9513305067451423014 ) ) ;
#125637=CARTESIAN_POINT ( 'NONE',  ( 1.055823836731560439, -1.452736638576918038, 1.781478128903237756 ) ) ;
#125639=CARTESIAN_POINT ( 'NONE',  ( 6.825054090417398633, -1.883341039872712397, -0.8414091007707087400 ) ) ;
#125643=CARTESIAN_POINT ( 'NONE',  ( 6.356982874815331641, 0.3076174260261410054, -1.815216213958574132 ) ) ;
#125644=CARTESIAN_POINT ( 'NONE',  ( -0.2104748580754201015, 5.720428293583295520, -2.697747842008205943 ) ) ;
#125645=CARTESIAN_POINT ( 'NONE',  ( 2.484998412088899489, 1.578176246201369093, -0.6962595882179720697 ) ) ;
#125646=CARTESIAN_POINT ( 'NONE',  ( 0.7609543035823238544, -0.05432987398422234326, -2.015980609757315190 ) ) ;
#125647=CARTESIAN_POINT ( 'NONE',  ( 3.182589804937531852, 1.813683736837278460, 1.412227471172630588 ) ) ;
#125648=CARTESIAN_POINT ( 'NONE',  ( 2.970297248839429027, 1.207737455218102829, 1.912895951805194894 ) ) ;
#125649=CARTESIAN_POINT ( 'NONE',  ( 5.602208710206744158, -2.106257355024013567, -0.001338375500582050358 ) ) ;
#125651=CARTESIAN_POINT ( 'NONE',  ( 4.024454502147566615, 1.679793015868607409, 0.5571282570626963082 ) ) ;
#125653=CARTESIAN_POINT ( 'NONE',  ( 6.374598633881160659, -0.1077809834691043772, -2.289980472931157252 ) ) ;
#125654=CARTESIAN_POINT ( 'NONE',  ( 5.806566994037906326, 1.625791660643903791, 0.8640615347050364381 ) ) ;
#125658=CARTESIAN_POINT ( 'NONE',  ( 4.541096662771787251, -1.693051203114638525, -1.391418086139440957 ) ) ;
#125661=CARTESIAN_POINT ( 'NONE',  ( 6.144996677366851401, -0.2998803957653916608, -2.048400609436632269 ) ) ;
#125662=CARTESIAN_POINT ( 'NONE',  ( 0.3215004009857677092, -1.429452135790244549, -1.422604240635255479 ) ) ;
#125664=CARTESIAN_POINT ( 'NONE',  ( 3.352094138168077553, 1.926676517159428670, -0.0006976933946620245131 ) ) ;
#125667=CARTESIAN_POINT ( 'NONE',  ( -0.1750823283547575382, -0.9565501389544858180, -2.002587789130043205 ) ) ;
#125677=CARTESIAN_POINT ( 'NONE',  ( 0.9066075625437097774, 0.5660373911110065936, 1.878450800843839419 ) ) ;
#125682=CARTESIAN_POINT ( 'NONE',  ( 5.107842384611220865, 0.6171798735227496113, -1.862306164846748491 ) ) ;
#125685=CARTESIAN_POINT ( 'NONE',  ( 6.385629968321593353, 1.486944277142748572, 1.569300510047972219 ) ) ;
#125689=CARTESIAN_POINT ( 'NONE',  ( 6.714144427970111906, -0.9273952116407166990, -1.739565242892411545 ) ) ;
#125690=CARTESIAN_POINT ( 'NONE',  ( 6.643864291637132879, -0.08952462543848457854, -1.731637005886511593 ) ) ;
#125692=CARTESIAN_POINT ( 'NONE',  ( 2.718528139169604341, 2.064530135181973591, 0.7356957861901700646 ) ) ;
#125693=CARTESIAN_POINT ( 'NONE',  ( 4.981611329956401768, 2.155202031093924830, -0.8251229701327715826 ) ) ;
#125694=CARTESIAN_POINT ( 'NONE',  ( 6.432896526414161542, 0.1972406338010060101, 2.051297006214629182 ) ) ;
#125695=CARTESIAN_POINT ( 'NONE',  ( 1.851409727902778357, 1.936748846533197677, -0.1429498737708263245 ) ) ;
#125698=CARTESIAN_POINT ( 'NONE',  ( 5.220985865760717992, 1.604251394084664550, -1.386888226476624242 ) ) ;
#125701=CARTESIAN_POINT ( 'NONE',  ( 3.902970337090125863, -1.038992709432768891, -1.728002613881730598 ) ) ;
#125710=CARTESIAN_POINT ( 'NONE',  ( 6.086805585656668960, -0.2997611930264115765, -2.038837977671539736 ) ) ;
#125715=CARTESIAN_POINT ( 'NONE',  ( 4.494788958170754078, -1.959534436568559190, -0.4887017053271830447 ) ) ;
#125722=CARTESIAN_POINT ( 'NONE',  ( 4.557529213136806590, 0.4535224272249741562, -2.010195360780684393 ) ) ;
#125723=CARTESIAN_POINT ( 'NONE',  ( 2.707657903872981553, 1.899618770239443366, 0.6767133375917554483 ) ) ;
#125729=CARTESIAN_POINT ( 'NONE',  ( 3.110703712691643918, 0.7282687159771012997, -1.880146464672841411 ) ) ;
#125730=CARTESIAN_POINT ( 'NONE',  ( 2.325889007780062023, 1.785771638016835361, 0.4476198290149570602 ) ) ;
#125731=CARTESIAN_POINT ( 'NONE',  ( 1.436587813502993249, 1.134030013130071346, -2.009770128656597876 ) ) ;
#125733=CARTESIAN_POINT ( 'NONE',  ( 4.200566210393744448, -0.6737006675727378324, -2.054019326127386691 ) ) ;
#125735=CARTESIAN_POINT ( 'NONE',  ( 3.620768967900461099, 0.5618574718093732878, -2.228542275653460969 ) ) ;
#125739=CARTESIAN_POINT ( 'NONE',  ( 1.041631754505952134, 0.7616270086890539748, -1.708776438048253077 ) ) ;
#125741=CARTESIAN_POINT ( 'NONE',  ( 5.418811373015061328, 1.821287777658405549, 0.7551675066918785983 ) ) ;
#125745=CARTESIAN_POINT ( 'NONE',  ( 0.7334016978863610037, 0.1661181961954381059, 2.200687262777756725 ) ) ;
#125750=CARTESIAN_POINT ( 'NONE',  ( 5.155133900154169169, -1.665016652684460530, -1.055383500247959461 ) ) ;
#125751=CARTESIAN_POINT ( 'NONE',  ( 5.110162711920646750, -2.297000869944005430, 0.2220405423442091408 ) ) ;
#125752=CARTESIAN_POINT ( 'NONE',  ( 6.039480578167179203, 1.719269793624801590, -0.7129749698730929452 ) ) ;
#125753=CARTESIAN_POINT ( 'NONE',  ( 3.204023084367659813, 0.7466497159868844546, -1.922840047214324333 ) ) ;
#125762=CARTESIAN_POINT ( 'NONE',  ( 5.828641854062238892, -1.381805371539744698, 1.674691576451936781 ) ) ;
#125764=CARTESIAN_POINT ( 'NONE',  ( 3.931074656914943954, -1.272613488525012659, -1.330884258478791438 ) ) ;
#125766=CARTESIAN_POINT ( 'NONE',  ( 6.720655732516628511, 2.062125556784020652, 2.233254568942647733 ) ) ;
#125767=CARTESIAN_POINT ( 'NONE',  ( 6.321842903100939104, 1.263506803105146847, -1.790488031206059372 ) ) ;
#125768=DIRECTION ( 'NONE',  ( 2.949029909160572061E-17, 1.000000000000000000, -8.673600428462579015E-15 ) ) ;
#125769=CARTESIAN_POINT ( 'NONE',  ( 6.825078400183548055, -0.008500281443135982926, 2.244262395727573356 ) ) ;
#125776=CARTESIAN_POINT ( 'NONE',  ( 0.6019893773144822102, -0.5904995772347610972, -1.668576399176853853 ) ) ;
#125777=CARTESIAN_POINT ( 'NONE',  ( 5.373694559265936199, 0.3904673514037678150, -1.974700560916352154 ) ) ;
#125779=CARTESIAN_POINT ( 'NONE',  ( 4.295997052264050708, -0.8081792604435251715, 1.944918383092561376 ) ) ;
#125780=CARTESIAN_POINT ( 'NONE',  ( 3.655789272196503514, 1.066996606607173659, 1.590710377612122750 ) ) ;
#125782=CARTESIAN_POINT ( 'NONE',  ( 4.475032023839897732, 1.799880929630924165, 0.8001706733358445733 ) ) ;
#125783=CARTESIAN_POINT ( 'NONE',  ( 5.871354875427445386, -1.734483768580237673, -1.034654692648151464 ) ) ;
#125784=CARTESIAN_POINT ( 'NONE',  ( 1.797508989346347619, -0.6330400025267440833, 1.760413054629046625 ) ) ;
#125785=CARTESIAN_POINT ( 'NONE',  ( 4.687984124052484880, -0.8092498044112338418, 1.523260386444349468 ) ) ;
#125786=CARTESIAN_POINT ( 'NONE',  ( 1.564566645345835116, 0.6029492335615972420, 1.814891859350221459 ) ) ;
#125788=CARTESIAN_POINT ( 'NONE',  ( 2.139570144280181108, -1.970530345926827742, 0.9937953903183869286 ) ) ;
#125791=CARTESIAN_POINT ( 'NONE',  ( 6.812952578306354035, -1.517200236233799071, 1.243500037895750143 ) ) ;
#125799=CARTESIAN_POINT ( 'NONE',  ( 1.785682506433339478, -1.950172559450613852, 0.6955597780969878796 ) ) ;
#125804=CARTESIAN_POINT ( 'NONE',  ( 0.06511101446048017660, -1.620675302784078786, 1.204964419619258376 ) ) ;
#125810=CARTESIAN_POINT ( 'NONE',  ( 5.764999918528635803, -2.016288307888712161, -0.002809016773450134351 ) ) ;
#125811=CARTESIAN_POINT ( 'NONE',  ( 4.452287505575288407, -1.246817998045848697, 1.454578644467845017 ) ) ;
#125812=CARTESIAN_POINT ( 'NONE',  ( 2.753686713869853531, 2.180749500395392282, -0.2175628297749406803 ) ) ;
#125815=CARTESIAN_POINT ( 'NONE',  ( 5.150644359860614863, 1.984129689857921486, 0.3399971717471597654 ) ) ;
#125816=CARTESIAN_POINT ( 'NONE',  ( 1.107505169401588274, 1.450017293480215352, 1.247013401884336403 ) ) ;
#125820=CARTESIAN_POINT ( 'NONE',  ( 6.485961931490698440, -2.116758087377061504, 0.05204923864161013075 ) ) ;
#125822=CARTESIAN_POINT ( 'NONE',  ( 3.843375017719421916, 0.7025675959630849343, -1.969317001441653670 ) ) ;
#125824=CARTESIAN_POINT ( 'NONE',  ( 1.711479192339813382, -1.712302428074402583, 0.2063632002643790431 ) ) ;
#125834=CARTESIAN_POINT ( 'NONE',  ( 2.683996807801437789, 0.9705641499191748345, 1.529316921005590357 ) ) ;
#125839=CARTESIAN_POINT ( 'NONE',  ( 3.984856247070994506, -1.691632632888851351, -0.6484230535298250997 ) ) ;
#125843=CARTESIAN_POINT ( 'NONE',  ( 4.035495103658576888, 1.752908062920730092, -0.6255878229263853729 ) ) ;
#125844=CARTESIAN_POINT ( 'NONE',  ( 1.528765853866232538, -1.617345627753681514, 1.026210199876474105 ) ) ;
#125845=CARTESIAN_POINT ( 'NONE',  ( 0.4459769555512117511, 1.820297760642339391, 0.1397589855641478973 ) ) ;
#125855=CARTESIAN_POINT ( 'NONE',  ( 6.227403457816463650, 0.1483525144864000778, -1.963943935631215165 ) ) ;
#125858=CARTESIAN_POINT ( 'NONE',  ( 0.005962723626575306898, -0.8962717426808585186, -1.887145544106306083 ) ) ;
#125860=CARTESIAN_POINT ( 'NONE',  ( 5.825206220505295462, -0.04701585971965925592, 1.925982856303788182 ) ) ;
#125862=CARTESIAN_POINT ( 'NONE',  ( 1.360069071312763223, 0.7361036424862777983, 1.670779996689908398 ) ) ;
#125863=CARTESIAN_POINT ( 'NONE',  ( 1.664966938652842954, -1.558911317520403239, 1.562347339584921002 ) ) ;
#125865=CARTESIAN_POINT ( 'NONE',  ( 0.5801457039020865292, 0.9447208859736742070, 1.662703529197881558 ) ) ;
#125866=CARTESIAN_POINT ( 'NONE',  ( 0.4144234639597261238, 0.7504023841088992564, 1.821203888109582447 ) ) ;
#125867=CARTESIAN_POINT ( 'NONE',  ( 2.647912457843327960, 0.6564901929842799078, 1.827849683178353057 ) ) ;
#125869=CARTESIAN_POINT ( 'NONE',  ( 0.5618747747782488755, 1.677749815653075460, -1.117659098820653174 ) ) ;
#125871=CARTESIAN_POINT ( 'NONE',  ( 6.086726144739807332, 1.793049480792831440, 0.4976782122840143763 ) ) ;
#125877=CARTESIAN_POINT ( 'NONE',  ( 2.665787806004877414, 1.174844384069907655, 1.849873475113596566 ) ) ;
#125881=CARTESIAN_POINT ( 'NONE',  ( 2.402731849113007190, 1.466575434288765800, -1.087121784572639527 ) ) ;
#125886=CARTESIAN_POINT ( 'NONE',  ( -0.02968770228140015649, 0.7448490463385791793, -1.910291535987144629 ) ) ;
#125888=CARTESIAN_POINT ( 'NONE',  ( 1.189925737956001095, -0.8670580458889056708, 1.720419655784347412 ) ) ;
#125889=CARTESIAN_POINT ( 'NONE',  ( 5.664887785843471413, 1.487927489739076181, -1.278645765186999128 ) ) ;
#125893=CARTESIAN_POINT ( 'NONE',  ( 5.302338810847701644, 1.659911028786088538, -1.431018553749352051 ) ) ;
#125896=CARTESIAN_POINT ( 'NONE',  ( 4.223533608758993196, 0.2584441732129874603, -2.054024224480345939 ) ) ;
#125901=CARTESIAN_POINT ( 'NONE',  ( 3.850415763719742479, 0.2810032917593773272, -2.281380581095279858 ) ) ;
#125905=CARTESIAN_POINT ( 'NONE',  ( 0.02392203315931124008, -1.416205114373503715, -1.803417470570017000 ) ) ;
#125906=FACE_OUTER_BOUND ( 'NONE', #162259, .T. ) ;
#125908=CARTESIAN_POINT ( 'NONE',  ( 5.261643664715593971, 0.9589319835984220219, 1.688605554185283575 ) ) ;
#125912=CARTESIAN_POINT ( 'NONE',  ( 5.607647405131535479, 1.452367144367059826, 1.244281684088064166 ) ) ;
#125913=CARTESIAN_POINT ( 'NONE',  ( 6.018504615762162224, 1.154743246034171555, -1.281328459571188239 ) ) ;
#125914=CARTESIAN_POINT ( 'NONE',  ( 4.540250091716044878, 0.7762272601403925609, 1.861345588084816871 ) ) ;
#125918=CARTESIAN_POINT ( 'NONE',  ( 1.394599547902091174, 1.708230453586807585, -1.204993862942314031 ) ) ;
#125919=CARTESIAN_POINT ( 'NONE',  ( 0.3734444151584931926, 1.013553851667288841, 1.450680648178425125 ) ) ;
#125920=CARTESIAN_POINT ( 'NONE',  ( 5.309220276109914316, 1.198862193007979471, -1.621181151826488254 ) ) ;
#125922=CARTESIAN_POINT ( 'NONE',  ( 3.504133162399528434, -0.9285911969159079682, -2.095928835653658062 ) ) ;
#125924=CARTESIAN_POINT ( 'NONE',  ( 2.132362993881876889, -1.555188906917738700, 0.7812613976432846163 ) ) ;
#125925=CARTESIAN_POINT ( 'NONE',  ( 2.883181758455736432, -1.960942133159260692, -0.8077274430827171559 ) ) ;
#125926=CARTESIAN_POINT ( 'NONE',  ( 2.495074604456462009, 1.680611355344446389, 0.4256512511701947554 ) ) ;
#125928=CARTESIAN_POINT ( 'NONE',  ( 1.609564491371988426, 0.5446964562696824386, -1.779540750359181800 ) ) ;
#125929=CARTESIAN_POINT ( 'NONE',  ( 2.471331864234734610, 1.938535094165691142, 0.9779774689679074928 ) ) ;
#125930=CARTESIAN_POINT ( 'NONE',  ( 3.467982673848205355, -0.9896861206786079501, 1.756853968756578066 ) ) ;
#125931=CARTESIAN_POINT ( 'NONE',  ( 5.031250000000002665, -0.7852924748302606561, -1.895863743163967108 ) ) ;
#125933=CARTESIAN_POINT ( 'NONE',  ( 0.3758376374219556393, 1.106279473776916378, 1.576890456013874120 ) ) ;
#125935=CARTESIAN_POINT ( 'NONE',  ( 3.937882119624159127, -2.125045857649208614, 0.6470787896058221023 ) ) ;
#125937=CARTESIAN_POINT ( 'NONE',  ( -0.2110808730066962846, 2.887681559854797797, -2.286017728802595350 ) ) ;
#125941=CARTESIAN_POINT ( 'NONE',  ( 6.012022869640524014, -0.7491050530544652863, 2.091446645375413027 ) ) ;
#125942=CARTESIAN_POINT ( 'NONE',  ( 4.264078424595136418, -1.956757550135434620, 0.1421211968542570592 ) ) ;
#125948=CARTESIAN_POINT ( 'NONE',  ( 6.116559975520791781, 1.526041019664432508, -1.670398689176689544 ) ) ;
#125949=CARTESIAN_POINT ( 'NONE',  ( 2.699736158553706300, -1.526808845971421968, -1.387057796406083732 ) ) ;
#125951=EDGE_LOOP ( 'NONE', ( #193965, #156078 ) ) ;
#125953=CARTESIAN_POINT ( 'NONE',  ( 4.024554299415397551, 1.775361691451295520, 0.5892213400080713592 ) ) ;
#125954=CARTESIAN_POINT ( 'NONE',  ( 3.006226939181593227, -1.670314528538990873, 0.4657782236400943021 ) ) ;
#125955=CARTESIAN_POINT ( 'NONE',  ( 6.480031355044912900, -2.148842909532014289, -0.4297212958329286736 ) ) ;
#125956=CARTESIAN_POINT ( 'NONE',  ( 1.114635189304619356, -0.9934212416997322270, -1.970578525975318573 ) ) ;
#125957=CARTESIAN_POINT ( 'NONE',  ( 6.158146451363091245, -1.371594178524730534, 1.374984930127883143 ) ) ;
#125960=CARTESIAN_POINT ( 'NONE',  ( -0.05211191391743182078, -1.802403943428915412, -0.9041556775107384425 ) ) ;
#125963=CARTESIAN_POINT ( 'NONE',  ( 6.381482430641396419, -0.5404875331735843336, -1.942542459342583294 ) ) ;
#125967=CARTESIAN_POINT ( 'NONE',  ( 4.195794211080963620, -0.6966935528937777677, 1.687730213881050600 ) ) ;
#125968=CARTESIAN_POINT ( 'NONE',  ( 2.169229845753062325, -2.017539712319418310, -0.8944986170207609444 ) ) ;
#125973=CARTESIAN_POINT ( 'NONE',  ( 1.388932113579334660, -1.919223592974130588, -0.6296790815572687050 ) ) ;
#125976=CARTESIAN_POINT ( 'NONE',  ( 2.430303444995636664, -1.149418499707482999, 1.463420418157684422 ) ) ;
#125978=CARTESIAN_POINT ( 'NONE',  ( 5.818982467333652764, 0.9914020171761170896, -1.755767668913270407 ) ) ;
#125981=CARTESIAN_POINT ( 'NONE',  ( 3.844227010333609584, 1.817057058749595777, 0.1772887374331885701 ) ) ;
#125986=CARTESIAN_POINT ( 'NONE',  ( 6.345077344222471716, -1.080897578067066878, 1.701688803805063266 ) ) ;
#125987=CARTESIAN_POINT ( 'NONE',  ( 5.578019757025042047, -1.797138167560994759, -0.3993771437491022702 ) ) ;
#125988=CARTESIAN_POINT ( 'NONE',  ( 4.512551404143492206, -0.9841529367882025925, -2.087457756972084244 ) ) ;
#125990=CARTESIAN_POINT ( 'NONE',  ( 0.5970370245043071789, 1.714778692204623312, -1.142632759096851913 ) ) ;
#125991=CARTESIAN_POINT ( 'NONE',  ( 1.909617033088998328, -0.9174269660217245770, -1.711723090954318405 ) ) ;
#125992=CARTESIAN_POINT ( 'NONE',  ( 5.852921341749488526, -1.041456137194999521, 2.048983711149698461 ) ) ;
#125995=CARTESIAN_POINT ( 'NONE',  ( 4.135518821028766112, -1.289757458839156934, -1.355179912160727085 ) ) ;
#125997=CARTESIAN_POINT ( 'NONE',  ( 2.425908952446104827, -1.891012092455180760, 0.2844710172774585488 ) ) ;
#126000=CARTESIAN_POINT ( 'NONE',  ( 3.950008152305323428, 0.7444041667201054535, -2.077678867657362538 ) ) ;
#126002=CARTESIAN_POINT ( 'NONE',  ( 6.883263157960371359, 7.052674735402435502, 2.544342468817725855 ) ) ;
#126005=CARTESIAN_POINT ( 'NONE',  ( 1.950399328871486704, 0.6145138020485548802, 1.873222726689319106 ) ) ;
#126006=CARTESIAN_POINT ( 'NONE',  ( 2.257223126251302947, -1.783628160338263768, 1.464130300071916135 ) ) ;
#126007=CARTESIAN_POINT ( 'NONE',  ( 2.945700582358207864, 1.385421296276163838, 1.389331660621349274 ) ) ;
#126009=CARTESIAN_POINT ( 'NONE',  ( 6.069198595068595381, 1.816300881853601723, 0.9774375683993684616 ) ) ;
#126011=CARTESIAN_POINT ( 'NONE',  ( 3.977750132953357998, -0.7672935630990398437, 1.865046046545227654 ) ) ;
#126014=CARTESIAN_POINT ( 'NONE',  ( 4.206267736153862735, 1.236801365491456028, -1.592660703826812352 ) ) ;
#126019=CARTESIAN_POINT ( 'NONE',  ( 2.290094988384860919, -1.415387839477784571, -1.646397135256922661 ) ) ;
#126021=CARTESIAN_POINT ( 'NONE',  ( 2.846779338809723559, -1.557328454271855955, 1.035869100625155692 ) ) ;
#126022=CARTESIAN_POINT ( 'NONE',  ( 0.2454759580562664856, -1.591291808662575580, -1.309149871672641297 ) ) ;
#126024=CARTESIAN_POINT ( 'NONE',  ( 6.727182134110200273, 2.469373133786161745, 2.195552656936059055 ) ) ;
#126027=CARTESIAN_POINT ( 'NONE',  ( 3.932203299393256302, -0.9856607118853939475, -1.638553295466014026 ) ) ;
#126028=CARTESIAN_POINT ( 'NONE',  ( 3.731107905939319735, -1.635417248454105854, 0.6770700851450436319 ) ) ;
#126029=CARTESIAN_POINT ( 'NONE',  ( 2.227084300891319035, 1.708885092217244051, 0.8583199515034345417 ) ) ;
#126032=CARTESIAN_POINT ( 'NONE',  ( -0.1357414145864926924, -1.858833624763186032, -0.4630600859806994762 ) ) ;
#126034=CARTESIAN_POINT ( 'NONE',  ( 0.9243811426856913815, 1.018911950503737174, 1.802186752163869699 ) ) ;
#126036=CARTESIAN_POINT ( 'NONE',  ( 6.139502064137229986, -1.356240498024411600, -1.288626068300227523 ) ) ;
#126037=CARTESIAN_POINT ( 'NONE',  ( 1.224926655537651676, -0.04696546880481740349, 1.825250005322680780 ) ) ;
#126038=CARTESIAN_POINT ( 'NONE',  ( 6.147136880733683917, -1.866598994669689926, 1.177069016086537356 ) ) ;
#126041=CARTESIAN_POINT ( 'NONE',  ( 3.473143217414649708, 1.863520296645693186, 0.8845801619412340111 ) ) ;
#126051=CARTESIAN_POINT ( 'NONE',  ( 5.846161131210033446, -0.9342735719010831774, 1.847668428805064655 ) ) ;
#126054=CARTESIAN_POINT ( 'NONE',  ( 3.163507678178357541, 0.3205598832158839118, -2.137589075770351066 ) ) ;
#126056=CARTESIAN_POINT ( 'NONE',  ( 2.789718171214683462, 1.917044005781431748, -0.6357942740662542169 ) ) ;
#126062=CARTESIAN_POINT ( 'NONE',  ( 1.762908039156896978, -0.1037823317905466058, -2.014007988105172231 ) ) ;
#126064=CARTESIAN_POINT ( 'NONE',  ( 5.618738332679400038, -0.05485954975367920983, 2.191026952110195491 ) ) ;
#126065=( BOUNDED_CURVE ( )  B_SPLINE_CURVE ( 3, ( #67197, #17386, #152743, #4324 ),
 .UNSPECIFIED., .F., .T. ) 
 B_SPLINE_CURVE_WITH_KNOTS ( ( 4, 4 ),
 ( 0.5000000000000017764, 1.000000000000000000 ),
 .UNSPECIFIED. ) 
 CURVE ( )  GEOMETRIC_REPRESENTATION_ITEM ( )  RATIONAL_B_SPLINE_CURVE ( ( 0.9999999999999976685, 0.3333333333333333703, 0.3333333333333357573, 1.000000000000000000 ) ) 
 REPRESENTATION_ITEM ( '' )  );
#126067=CARTESIAN_POINT ( 'NONE',  ( 4.675980034926481288, 1.890745994642643479, -0.2862527531290667837 ) ) ;
#126072=CARTESIAN_POINT ( 'NONE',  ( 3.251577527157409886, 1.966640965408305686, -0.4445242805125593222 ) ) ;
#126074=CARTESIAN_POINT ( 'NONE',  ( 5.807552366672524613, -0.4147409827905921831, 1.674012740457442305 ) ) ;
#126078=CARTESIAN_POINT ( 'NONE',  ( 4.059713336928523653, 1.856696190431494475, -0.2264497139414511362 ) ) ;
#126080=CARTESIAN_POINT ( 'NONE',  ( 1.463825199929311260, -0.5068179562870354093, 2.007114080642191656 ) ) ;
#126082=VERTEX_POINT ( 'NONE', #138776 ) ;
#126083=CARTESIAN_POINT ( 'NONE',  ( 6.111934181110398434, -0.6035781192351510338, 1.708109960999981469 ) ) ;
#126085=CARTESIAN_POINT ( 'NONE',  ( -0.1234324464992678227, -0.4448297287729073846, -1.973926538189611835 ) ) ;
#126086=CARTESIAN_POINT ( 'NONE',  ( 0.5624193892179689680, 0.5266301872345402479, 1.733300928327138113 ) ) ;
#126091=CARTESIAN_POINT ( 'NONE',  ( 0.8362905744919849615, -1.092891352686057527, 1.629061181365853539 ) ) ;
#126093=CARTESIAN_POINT ( 'NONE',  ( 4.534732036847580083, -1.536008458380673458, 1.144414559590371638 ) ) ;
#126102=CARTESIAN_POINT ( 'NONE',  ( 1.815512348505427642, -0.2646426633909418347, 2.145385951886819242 ) ) ;
#126105=CARTESIAN_POINT ( 'NONE',  ( -0.1049925189658337810, -2.058569791948822392, -0.5088776734372552069 ) ) ;
#126106=CARTESIAN_POINT ( 'NONE',  ( 4.260648785556298890, -1.352668379831567069, 1.226179085325199258 ) ) ;
#126108=CARTESIAN_POINT ( 'NONE',  ( 0.9484320465981105341, 0.5679970104440315026, 1.887783002132171539 ) ) ;
#126109=CARTESIAN_POINT ( 'NONE',  ( 3.990413957267644474, -1.096855775730350757, 1.566394476586838724 ) ) ;
#126112=CARTESIAN_POINT ( 'NONE',  ( 4.176189586714727398, -1.010410353755032409, -1.690456409470885824 ) ) ;
#126114=CARTESIAN_POINT ( 'NONE',  ( 5.530791563722144311, -1.753914071513791528, 0.8342105869050663314 ) ) ;
#126115=VERTEX_POINT ( 'NONE', #123673 ) ;
#126118=CARTESIAN_POINT ( 'NONE',  ( 6.117454236943913770, 1.763945953808215394, 1.176740244630887222 ) ) ;
#126120=CARTESIAN_POINT ( 'NONE',  ( 4.125576785117724299, -0.3237648511281773778, 1.884507068624697190 ) ) ;
#126122=CARTESIAN_POINT ( 'NONE',  ( 0.2005908178989434243, -2.206344910233990486, -0.05143828380192031619 ) ) ;
#126124=CARTESIAN_POINT ( 'NONE',  ( 5.162748661275342599, 0.5863960615675645194, 1.925778112416365317 ) ) ;
#126126=CARTESIAN_POINT ( 'NONE',  ( 5.690036971771410101, -0.8169618954828453683, 1.632782195682795257 ) ) ;
#126127=CARTESIAN_POINT ( 'NONE',  ( 5.788296071918774821, -0.7303023681345042206, -1.879805717804765353 ) ) ;
#126128=CARTESIAN_POINT ( 'NONE',  ( 1.451716722110554025, 1.566445173006292935, 1.353826630019476562 ) ) ;
#126140=CARTESIAN_POINT ( 'NONE',  ( 3.709331991548686425, 1.648016779243220320, 0.5399856063554776542 ) ) ;
#126143=CARTESIAN_POINT ( 'NONE',  ( 2.166927730644189420, 1.536898783757352005, -1.387270004372019416 ) ) ;
#126144=CARTESIAN_POINT ( 'NONE',  ( 3.603210856581297694, -0.1536155211374414797, 2.111693916904446855 ) ) ;
#126147=CARTESIAN_POINT ( 'NONE',  ( 1.217558188649459527, 0.3894938459214473125, -1.930362121600463610 ) ) ;
#126152=CARTESIAN_POINT ( 'NONE',  ( 3.486539624822242889, -0.4467316994782115636, -2.248153690150441975 ) ) ;
#126153=CARTESIAN_POINT ( 'NONE',  ( 0.2404813148422607350, 0.3085585699703840001, 1.799268721412583094 ) ) ;
#126154=CARTESIAN_POINT ( 'NONE',  ( 2.812653035604309348, -0.5591599321941118639, -1.828790038765286452 ) ) ;
#126158=CARTESIAN_POINT ( 'NONE',  ( 2.267839937129061401, 0.5327387516648759425, -1.941401684534331817 ) ) ;
#126159=CARTESIAN_POINT ( 'NONE',  ( 2.096468001391890823, 1.939661435718213811, 0.2929505381348077031 ) ) ;
#126162=CARTESIAN_POINT ( 'NONE',  ( 0.07516593201273896740, 4.087024598281757015, -2.598925129725014660 ) ) ;
#126163=CARTESIAN_POINT ( 'NONE',  ( 5.279275078172800839, 1.403616728028998395, 1.549557787628618399 ) ) ;
#126164=CARTESIAN_POINT ( 'NONE',  ( 3.361912448646987794, 0.7947379027260987883, 1.581431320561203169 ) ) ;
#126166=CARTESIAN_POINT ( 'NONE',  ( 6.615150229029130635, -2.225211831249251482, 0.5499996461680799476 ) ) ;
#126167=CARTESIAN_POINT ( 'NONE',  ( 5.753775850233431299, 0.7111499035084413167, 1.588595604753391122 ) ) ;
#126169=CARTESIAN_POINT ( 'NONE',  ( 6.065094409921147900, -1.233312222785312384, 1.939673083280533783 ) ) ;
#126171=CARTESIAN_POINT ( 'NONE',  ( 5.255145817263100483, -1.720984288211702795, -0.2101651147246290929 ) ) ;
#126172=CARTESIAN_POINT ( 'NONE',  ( 6.092256315220226703, 1.075607590566488803, -1.885974292122821527 ) ) ;
#126174=CARTESIAN_POINT ( 'NONE',  ( 6.438686429976131720, -1.555646628146038157, 1.282773817382940384 ) ) ;
#126175=CARTESIAN_POINT ( 'NONE',  ( 5.187500000000002665, -1.451031289060905172, 1.451031289061322838 ) ) ;
#126177=CARTESIAN_POINT ( 'NONE',  ( 3.012629298554883484, 1.396463203792638996, -1.327218363718547511 ) ) ;
#126179=CARTESIAN_POINT ( 'NONE',  ( 0.2236696677372449760, 1.935810370009845460, 1.089285801332658732 ) ) ;
#126184=CARTESIAN_POINT ( 'NONE',  ( 2.350487294161308860, 1.044453463271700633, -1.960417310804033031 ) ) ;
#126191=CARTESIAN_POINT ( 'NONE',  ( 1.160779977835691312, 1.203355533934968635, 1.617816888933524710 ) ) ;
#126193=CARTESIAN_POINT ( 'NONE',  ( 6.039522989413334209, 1.907243403200251208, -0.7859975451465596175 ) ) ;
#126200=CARTESIAN_POINT ( 'NONE',  ( 0.2448899766094528307, -1.362147681959727574, -1.129672978174221631 ) ) ;
#126201=CARTESIAN_POINT ( 'NONE',  ( 5.994686951402704800, -1.719894441074249158, 0.2214109503040090354 ) ) ;
#126202=CARTESIAN_POINT ( 'NONE',  ( 5.636210787324313465, 0.3477544615747550361, 1.705165986005853229 ) ) ;
#126203=CARTESIAN_POINT ( 'NONE',  ( 2.788958495631514545, 1.964664059585927491, -1.180940832111162520 ) ) ;
#126205=CARTESIAN_POINT ( 'NONE',  ( 2.220424023188283247, -0.0004634451795330202239, 1.841320589463534052 ) ) ;
#126208=CARTESIAN_POINT ( 'NONE',  ( 2.555444900642935391, 0.4891320457309326075, -1.758753460580727790 ) ) ;
#126209=CARTESIAN_POINT ( 'NONE',  ( 3.516250148862578584, -1.862017090670412767, 0.7743150488077471527 ) ) ;
#126212=CARTESIAN_POINT ( 'NONE',  ( 5.825249245718299385, -0.05505390245461554838, 2.105416907300653673 ) ) ;
#126216=CARTESIAN_POINT ( 'NONE',  ( 2.436061438456170958, 1.271862942251865691, 1.633573898902056731 ) ) ;
#126219=CARTESIAN_POINT ( 'NONE',  ( 4.653055333535057514, 0.3633016933833124185, 2.088981207656291250 ) ) ;
#126220=CARTESIAN_POINT ( 'NONE',  ( 1.506341009219732907, -0.6927896466909737594, -1.797792356224122923 ) ) ;
#126227=CARTESIAN_POINT ( 'NONE',  ( 5.765915565743810589, 0.6138260544302427402, -2.029845472315944921 ) ) ;
#126228=CARTESIAN_POINT ( 'NONE',  ( 2.590967463960031303, -0.3587740299011917267, -2.075001757462133778 ) ) ;
#126231=CARTESIAN_POINT ( 'NONE',  ( 6.280112003059028503, -1.032894792506684034, -1.547752956576850858 ) ) ;
#126239=CARTESIAN_POINT ( 'NONE',  ( 2.383191274269541360, -0.003000794896521400724, 1.962046632024143866 ) ) ;
#126240=CARTESIAN_POINT ( 'NONE',  ( 1.481558191429487970, 1.997200094811113491, -0.8276061316847342919 ) ) ;
#126246=CARTESIAN_POINT ( 'NONE',  ( 3.672919734203412112, -0.7009596788165352033, -1.586013134846143480 ) ) ;
#126247=CARTESIAN_POINT ( 'NONE',  ( 2.413636602577839518, 1.137377966863511780, -1.317326450295707607 ) ) ;
#126251=CARTESIAN_POINT ( 'NONE',  ( 2.179064334209149578, -0.9478932651061505732, -1.779355105811925020 ) ) ;
#126252=DIRECTION ( 'NONE',  ( 1.214306433183764966E-17, 1.000000000000000000, 5.200010849845536803E-32 ) ) ;
#126254=CARTESIAN_POINT ( 'NONE',  ( 1.780087957478289074, -1.056366978776434484, 1.664393130878606852 ) ) ;
#126256=CARTESIAN_POINT ( 'NONE',  ( 5.748291730981218706, 0.9368611416523886515, -1.667099895225135686 ) ) ;
#126263=CARTESIAN_POINT ( 'NONE',  ( 1.488931934708405569, -1.918476728873222070, -0.6315473366199951810 ) ) ;
#126265=CARTESIAN_POINT ( 'NONE',  ( 6.159233218726320125, -1.974841252017808468, -1.193533401095113300 ) ) ;
#126266=CARTESIAN_POINT ( 'NONE',  ( 5.758247127753066685, -1.962046631956643195, -0.001586170976335121285 ) ) ;
#126267=CARTESIAN_POINT ( 'NONE',  ( 2.940231979924610162, -1.012623612260230566, 1.680088604585870060 ) ) ;
#126269=CARTESIAN_POINT ( 'NONE',  ( 0.6158615555539398434, 0.1511424999406512648, 2.010826230049263863 ) ) ;
#126271=CARTESIAN_POINT ( 'NONE',  ( 1.323616076398025587, -1.537765720040217055, -1.455736727087880489 ) ) ;
#126274=CARTESIAN_POINT ( 'NONE',  ( 1.534833434108737515, -1.332603482217321389, -1.270662175854364362 ) ) ;
#126277=CARTESIAN_POINT ( 'NONE',  ( 2.584367824843319283, 1.138156186954141003, 1.789115803205274080 ) ) ;
#126281=CARTESIAN_POINT ( 'NONE',  ( 3.602854949731192136, 1.626725521824391230, -1.265059968925500211 ) ) ;
#126283=CARTESIAN_POINT ( 'NONE',  ( 0.4328342922346357646, -1.301571265828086688, -1.302605208699902928 ) ) ;
#126286=CARTESIAN_POINT ( 'NONE',  ( 0.7860941533469123499, 1.484900681275106438, 1.632775826992872492 ) ) ;
#126287=CARTESIAN_POINT ( 'NONE',  ( 2.566018446761752170, 2.219231934913689308, -0.4390887803658559130 ) ) ;
#126289=CARTESIAN_POINT ( 'NONE',  ( 2.039049738775432719, 0.002999869061550211602, 1.811767226593180569 ) ) ;
#126290=CARTESIAN_POINT ( 'NONE',  ( 3.626117945992116898, 1.907004414510531598, 0.1821707851048308124 ) ) ;
#126291=CARTESIAN_POINT ( 'NONE',  ( 4.492674960910642667, 2.029786422369950216, 0.4070406814440513665 ) ) ;
#126293=CARTESIAN_POINT ( 'NONE',  ( 2.237131214483905950, -1.761753319436863086, 0.8849394531919276830 ) ) ;
#126294=CARTESIAN_POINT ( 'NONE',  ( 6.674445239480702341, -1.183187502913226608, 1.521125075997560527 ) ) ;
#126295=CARTESIAN_POINT ( 'NONE',  ( 2.975316878787794828, 1.776827963633962559, -0.5852370025475408521 ) ) ;
#126296=CARTESIAN_POINT ( 'NONE',  ( 1.735461890456877487, 0.2295834678119219041, 2.296248630371207966 ) ) ;
#126298=CARTESIAN_POINT ( 'NONE',  ( 2.646735056387524043, -0.3148485976074810733, -1.834047879892097388 ) ) ;
#126300=CARTESIAN_POINT ( 'NONE',  ( 6.602015036461629904, 0.7930265726678319416, -1.904331891608399996 ) ) ;
#126305=CARTESIAN_POINT ( 'NONE',  ( 0.3640743269037312602, 2.082829956593022835, -0.3111531555848711106 ) ) ;
#126307=CARTESIAN_POINT ( 'NONE',  ( 6.151685507011436904, 0.6340151041426717038, -2.066508600247290772 ) ) ;
#126308=CARTESIAN_POINT ( 'NONE',  ( -0.1930879795662324705, -0.4444491470046680326, -1.977061965688177825 ) ) ;
#126315=CARTESIAN_POINT ( 'NONE',  ( 4.575407832915947104, 1.497500392235491029, 1.350737390116145242 ) ) ;
#126318=CARTESIAN_POINT ( 'NONE',  ( 6.069229152942410721, 0.1638285306290178100, -2.155560115052157055 ) ) ;
#126325=CARTESIAN_POINT ( 'NONE',  ( 0.3510145263703016716, 0.1867627727243931779, -1.906451055755745250 ) ) ;
#126329=CARTESIAN_POINT ( 'NONE',  ( 1.259898821826772819, 0.6958341084943464594, 1.578493908868659146 ) ) ;
#126333=CARTESIAN_POINT ( 'NONE',  ( 0.7898890640410756170, -1.755383811729524624, -0.2245491444978504059 ) ) ;
#126334=CARTESIAN_POINT ( 'NONE',  ( 2.367839801511921305, 0.5346396131555611886, -1.940748983941695371 ) ) ;
#126336=CARTESIAN_POINT ( 'NONE',  ( 3.874219531129017291, 1.223701582695544854, 1.836212042189053761 ) ) ;
#126337=CARTESIAN_POINT ( 'NONE',  ( 5.366168305121062687, -2.161276524852562275, 0.2057630808787509757 ) ) ;
#126341=CARTESIAN_POINT ( 'NONE',  ( 2.754661888675050019, 2.104750880745378083, 0.2572054321872129790 ) ) ;
#126342=CARTESIAN_POINT ( 'NONE',  ( 3.357046149680571023, 0.04665894677104672622, -2.016035383867887276 ) ) ;
#126343=CARTESIAN_POINT ( 'NONE',  ( 3.533306822026711647, -0.1277962806783480842, 1.807111865170844656 ) ) ;
#126347=CARTESIAN_POINT ( 'NONE',  ( 0.5494049127674709432, 0.5909524230637287490, -1.774924738581270089 ) ) ;
#126350=CARTESIAN_POINT ( 'NONE',  ( 6.270122753791413928, 0.9430518052575274091, 1.563124558401955300 ) ) ;
#126352=CARTESIAN_POINT ( 'NONE',  ( 1.903404652330241476, -1.857121539659777998, 0.4695605108672970540 ) ) ;
#126358=CARTESIAN_POINT ( 'NONE',  ( 5.787991602622606813, -0.9759734195362681497, 1.928925553883020338 ) ) ;
#126361=CARTESIAN_POINT ( 'NONE',  ( 3.515986968957810266, -0.6120941298391361363, 2.030368431519948391 ) ) ;
#126362=CARTESIAN_POINT ( 'NONE',  ( -0.1296875068448159751, 0.001480089298542403009, -1.826395826379861864 ) ) ;
#126364=CARTESIAN_POINT ( 'NONE',  ( 4.534422775129973715, 1.932726017421485976, 0.3875534085790635630 ) ) ;
#126365=CARTESIAN_POINT ( 'NONE',  ( 6.064708884584704585, 0.6063723501847050334, 1.813766235492550560 ) ) ;
#126367=CARTESIAN_POINT ( 'NONE',  ( 5.981681833671104620, -0.7110503908294771858, 1.994531755910114112 ) ) ;
#126369=CARTESIAN_POINT ( 'NONE',  ( 0.6958625912084138720, -1.462932864358768459, -1.465259690088885014 ) ) ;
#126370=CARTESIAN_POINT ( 'NONE',  ( 2.783070106938976274, 1.373617692895822806, 1.372961415081490610 ) ) ;
#126374=CARTESIAN_POINT ( 'NONE',  ( 3.732441334599644556, 0.3067963083541249691, 2.067875747930392638 ) ) ;
#126377=CARTESIAN_POINT ( 'NONE',  ( 0.3986853379376364415, -0.2198743563824180347, -1.798016573952045283 ) ) ;
#126379=CARTESIAN_POINT ( 'NONE',  ( 5.074942902252104204, -2.077123540546990110, -0.7459609299403435756 ) ) ;
#126381=CARTESIAN_POINT ( 'NONE',  ( 2.573496151666111231, 0.1090403232480302298, -2.204208057042057245 ) ) ;
#126383=CARTESIAN_POINT ( 'NONE',  ( 1.471198412684338264, -1.640640410176617658, -0.9821394255850326438 ) ) ;
#126385=CARTESIAN_POINT ( 'NONE',  ( 5.740704066448026666, -2.019076491677873619, -0.4572469816465085657 ) ) ;
#126388=CARTESIAN_POINT ( 'NONE',  ( 2.993221558690632556, 1.854768100113469265, -1.110066390340218367 ) ) ;
#126389=CARTESIAN_POINT ( 'NONE',  ( 4.827760788416924242, 1.126602223531171898, -1.879657820484957664 ) ) ;
#126392=SURFACE_SIDE_STYLE ('',( #136440 ) ) ;
#126399=CARTESIAN_POINT ( 'NONE',  ( 6.016483110937820733, 0.8336820848486149460, 1.895147399281302825 ) ) ;
#126400=CARTESIAN_POINT ( 'NONE',  ( 3.844294682379956640, 1.917307101836130512, 0.1879692045662837430 ) ) ;
#126401=CARTESIAN_POINT ( 'NONE',  ( 0.3687678296072604556, -0.2496303596870551866, -2.000855358883571800 ) ) ;
#126404=CARTESIAN_POINT ( 'NONE',  ( 4.961744348476156752, -0.5292939252423340957, 1.896881419486784681 ) ) ;
#126405=CARTESIAN_POINT ( 'NONE',  ( 0.4280004979528989617, 1.123059939108238314, -1.881669248891951085 ) ) ;
#126406=CARTESIAN_POINT ( 'NONE',  ( 3.861776535121093090, 1.811678901967550326, -0.2252020330209548171 ) ) ;
#126413=CARTESIAN_POINT ( 'NONE',  ( 3.157574601152390414, 0.8305207305269333151, 1.643389852989694200 ) ) ;
#126414=CARTESIAN_POINT ( 'NONE',  ( 5.220952493833380004, 1.521736800665099976, -1.318127947290965052 ) ) ;
#126415=CARTESIAN_POINT ( 'NONE',  ( 1.054597461939084768, 2.025951976169305890, -1.085350914182762638 ) ) ;
#126416=CARTESIAN_POINT ( 'NONE',  ( 5.805508902378371694, -1.544246397408255866, -1.209716981170713357 ) ) ;
#126420=CARTESIAN_POINT ( 'NONE',  ( 0.4321921490204432281, 1.190796696626210682, 1.693455153822187587 ) ) ;
#126422=CARTESIAN_POINT ( 'NONE',  ( 1.593426000515285157, -0.7013512306414200204, 1.969750900790192549 ) ) ;
#126423=CARTESIAN_POINT ( 'NONE',  ( 0.5142528298564854605, 1.293200884458247657, -1.351890787750304135 ) ) ;
#126426=CARTESIAN_POINT ( 'NONE',  ( -0.1102773484824015326, 7.629137130509110243, -2.803480817674379288 ) ) ;
#126427=CARTESIAN_POINT ( 'NONE',  ( 1.680815414582544243, 1.200268842161634097, 1.260572391871515263 ) ) ;
#126431=CARTESIAN_POINT ( 'NONE',  ( 3.070621489812708660, -1.593986286245190565, -0.6595977741803840111 ) ) ;
#126432=CARTESIAN_POINT ( 'NONE',  ( 2.753686713869853531, 2.180749500395392282, -0.2175628297749406803 ) ) ;
#126433=CARTESIAN_POINT ( 'NONE',  ( 5.672569038193632451, -1.402732290180560337, 1.703733612381942653 ) ) ;
#126435=CARTESIAN_POINT ( 'NONE',  ( 2.465899347143265086, -0.4792435138091205027, 2.117354166282244599 ) ) ;
#126436=CARTESIAN_POINT ( 'NONE',  ( 1.084280211047653264, -1.780658692889337091, -0.4022698149812459212 ) ) ;
#126437=CARTESIAN_POINT ( 'NONE',  ( 3.081382859721363499, 1.672078201027054734, 1.298909159995583318 ) ) ;
#126438=CARTESIAN_POINT ( 'NONE',  ( 6.639320575229240795, 2.471732717405307422, 2.181477732991484064 ) ) ;
#126441=CARTESIAN_POINT ( 'NONE',  ( 4.019262574452024062, -2.193609252165360513, 0.6655472109698862271 ) ) ;
#126445=CARTESIAN_POINT ( 'NONE',  ( 6.112022827852052309, -0.7509524718064889415, 2.090657394127520163 ) ) ;
#126452=CARTESIAN_POINT ( 'NONE',  ( 4.184220324914634581, 1.621181886760931778, 1.198861198883696799 ) ) ;
#126454=CARTESIAN_POINT ( 'NONE',  ( 2.061455334089828284, 1.712470851095546642, 1.149345886162132402 ) ) ;
#126459=CARTESIAN_POINT ( 'NONE',  ( 5.173855182012670362, -1.219361875273092366, 1.820681821249593657 ) ) ;
#126460=CARTESIAN_POINT ( 'NONE',  ( 2.496720397819631732, -1.994071314890283553, 0.2986276487200872354 ) ) ;
#126461=CARTESIAN_POINT ( 'NONE',  ( 1.962219809069129184, -1.683971100191889336, -0.7449956418128443891 ) ) ;
#126464=CARTESIAN_POINT ( 'NONE',  ( 6.317409609008933558, -0.2203418483949574069, 1.812181760327068680 ) ) ;
#126466=CARTESIAN_POINT ( 'NONE',  ( 5.436487035374818255, 2.228047177662040301, 0.3926572465528885281 ) ) ;
#126468=CARTESIAN_POINT ( 'NONE',  ( 1.875742097524640384, 2.014971663898405652, -0.6126918839576761533 ) ) ;
#126478=CARTESIAN_POINT ( 'NONE',  ( 1.687894460584405731, 2.027760172737497424, -0.6205009303206151516 ) ) ;
#126479=CARTESIAN_POINT ( 'NONE',  ( 2.777807369331359411, 0.3217554308703252652, -2.197856884423950774 ) ) ;
#126483=CARTESIAN_POINT ( 'NONE',  ( 4.053139552913617827, 1.658577106941661272, -1.047563642765911185 ) ) ;
#126492=CARTESIAN_POINT ( 'NONE',  ( 2.953504815971871977, -1.868289524550557523, 1.003269902519101864 ) ) ;
#126494=CARTESIAN_POINT ( 'NONE',  ( 4.821240550277555492, -0.1094919189667045711, 2.159058991224649393 ) ) ;
#126495=CARTESIAN_POINT ( 'NONE',  ( 4.370544011308346910, -0.004580445953385886559, -1.841430844414258861 ) ) ;
#126498=CARTESIAN_POINT ( 'NONE',  ( 6.193256023596829252, -0.5794974496134881470, 1.641157367357688246 ) ) ;
#126502=CARTESIAN_POINT ( 'NONE',  ( 3.081113354808207916, -0.1575343947536785305, -2.156009052512488200 ) ) ;
#126504=CARTESIAN_POINT ( 'NONE',  ( 6.151720201709268920, -0.2930281871833945173, -1.994563951915592881 ) ) ;
#126506=CARTESIAN_POINT ( 'NONE',  ( 2.588937169860201504, -0.3686131662095324946, -2.129881858774537395 ) ) ;
#126507=CARTESIAN_POINT ( 'NONE',  ( 4.112542095708375811, 1.396345452295008727, -1.391819494878621111 ) ) ;
#126510=CARTESIAN_POINT ( 'NONE',  ( -0.04112450405316381286, -1.960553898366865555, -0.9795403211517728082 ) ) ;
#126511=CARTESIAN_POINT ( 'NONE',  ( 0.1129635547038260190, -0.9897495874401724958, -2.082026327295583012 ) ) ;
#126512=CARTESIAN_POINT ( 'NONE',  ( 4.651864714057460048, 0.7465859729765094155, 1.793013943324140769 ) ) ;
#126522=CARTESIAN_POINT ( 'NONE',  ( 2.731697238759897672, -2.059418846490802313, 0.7933392487004319316 ) ) ;
#126524=CARTESIAN_POINT ( 'NONE',  ( 6.772321408939014020, -0.9219223515295159599, -1.731591420108986812 ) ) ;
#126528=CARTESIAN_POINT ( 'NONE',  ( 0.07499057489260704812, 2.034159190454051913, -2.372362849262329210 ) ) ;
#126530=CARTESIAN_POINT ( 'NONE',  ( 5.560457619783242933, -1.666209093894938764, -0.7835883864039174806 ) ) ;
#126535=CARTESIAN_POINT ( 'NONE',  ( 5.994406619193555663, -1.133004004027007294, 1.792352430775605798 ) ) ;
#126538=CARTESIAN_POINT ( 'NONE',  ( 6.221960870361377793, -1.141027836104959281, -1.715851070140647527 ) ) ;
#126540=CARTESIAN_POINT ( 'NONE',  ( 2.365471783816187834, -0.4113058309756181807, 1.814853103561973935 ) ) ;
#126541=CARTESIAN_POINT ( 'NONE',  ( 5.073706409418358376, -1.018251046719556685, 1.533866337327425278 ) ) ;
#126548=CARTESIAN_POINT ( 'NONE',  ( 4.178501018151202118, -1.271701901513167421, 1.803451139310302986 ) ) ;
#126549=CARTESIAN_POINT ( 'NONE',  ( 5.606774309801295431, 1.718512474747270868, -1.471603694038286836 ) ) ;
#126551=CARTESIAN_POINT ( 'NONE',  ( 5.924035771748266122, -1.796794102754266431, 0.2306889152782486963 ) ) ;
#126552=CARTESIAN_POINT ( 'NONE',  ( 6.368375084315238688, -1.880202862833039834, -0.3662410793365057926 ) ) ;
#126555=CARTESIAN_POINT ( 'NONE',  ( 5.918603479541379997, -0.6925943527147163659, -1.782627650866043911 ) ) ;
#126557=CARTESIAN_POINT ( 'NONE',  ( 0.1802491246630563426, -1.813337052076903877, -0.4591185353455888296 ) ) ;
#126559=CARTESIAN_POINT ( 'NONE',  ( 0.8840003597419334724, -2.016708404047353742, 0.004841148455551891328 ) ) ;
#126561=CARTESIAN_POINT ( 'NONE',  ( 3.528042858452341335, -1.254676591636105121, -1.691379958841844111 ) ) ;
#126565=CARTESIAN_POINT ( 'NONE',  ( 3.199477664157297063, 1.824241505505564964, -0.8673461216518009165 ) ) ;
#126569=CARTESIAN_POINT ( 'NONE',  ( 3.901784996602038813, -0.6316019492740264640, 2.067237329103743804 ) ) ;
#126575=CARTESIAN_POINT ( 'NONE',  ( 1.029994877853340762, 2.092549206400303063, -0.5788440209302682105 ) ) ;
#126578=CARTESIAN_POINT ( 'NONE',  ( 0.9074547957551477584, -0.8278116715597811925, -1.644758345054016191 ) ) ;
#126580=CARTESIAN_POINT ( 'NONE',  ( 1.874823134854076923, -0.1115055541827478930, -2.188858692977871279 ) ) ;
#126582=CARTESIAN_POINT ( 'NONE',  ( 3.098750496328426252, -0.6552482397011113457, -2.165565034296774272 ) ) ;
#126588=CARTESIAN_POINT ( 'NONE',  ( 4.077242326343363032, 1.667005924876462597, -0.5946135600440533020 ) ) ;
#126590=CARTESIAN_POINT ( 'NONE',  ( 1.290213853529555976, -0.9470325862265884798, 1.881093767389901750 ) ) ;
#126594=CARTESIAN_POINT ( 'NONE',  ( 6.169546029190324354, 1.392557221580101201, 1.458547251757099428 ) ) ;
#126595=CARTESIAN_POINT ( 'NONE',  ( 5.062699594374425516, 0.5334270428436416189, 1.731249764757249343 ) ) ;
#126597=CARTESIAN_POINT ( 'NONE',  ( 3.186256133050053840, -1.842714570631575510, -0.3211874441736498054 ) ) ;
#126598=CARTESIAN_POINT ( 'NONE',  ( 4.610256228194366201, 2.069909489248497714, -0.04556564433023241323 ) ) ;
#126606=CARTESIAN_POINT ( 'NONE',  ( 3.666413850373055006, -0.7928392042928497085, -1.794698522912529182 ) ) ;
#126607=CARTESIAN_POINT ( 'NONE',  ( 0.8607036144342284922, -0.7282710370301350711, 1.880145570116364073 ) ) ;
#126611=CARTESIAN_POINT ( 'NONE',  ( 1.194370141144196706, -0.4488658031855938813, -1.815784161679114384 ) ) ;
#126613=CARTESIAN_POINT ( 'NONE',  ( 3.445567785929729343, -1.858493022056451949, 0.7744065704922193927 ) ) ;
#126615=CARTESIAN_POINT ( 'NONE',  ( 3.603210856581297694, -0.1536155211374414797, 2.111693916904446855 ) ) ;
#126617=CARTESIAN_POINT ( 'NONE',  ( 5.283670394142272464, -1.967056725255760474, 0.6460906113585006549 ) ) ;
#126619=CARTESIAN_POINT ( 'NONE',  ( 6.632766914392992597, -1.868179159523954302, 0.9385789683672930428 ) ) ;
#126621=CARTESIAN_POINT ( 'NONE',  ( 5.579063851370913873, -0.04688903583028104782, -1.825137680102270288 ) ) ;
#126626=CARTESIAN_POINT ( 'NONE',  ( 6.159228477734898455, -1.889628185881117695, -1.139594184263223120 ) ) ;
#126628=CARTESIAN_POINT ( 'NONE',  ( 5.057238878282278804, -1.638088962530854786, 0.9864336689310859718 ) ) ;
#126637=EDGE_CURVE ( 'NONE', #139360, #57181, #61162, .T. ) ;
#126641=CARTESIAN_POINT ( 'NONE',  ( 0.1399997263886037790, 2.025166351305721868, -2.415484119839182320 ) ) ;
#126644=CARTESIAN_POINT ( 'NONE',  ( 2.237097273892864724, -0.09148514208244534762, -1.967424487969974711 ) ) ;
#126645=CARTESIAN_POINT ( 'NONE',  ( 3.357046149680571023, 0.04665894677104672622, -2.016035383867887276 ) ) ;
#126648=CARTESIAN_POINT ( 'NONE',  ( 6.827182134110167055, 4.690515317746113411, 2.651606140002475076 ) ) ;
#126649=CARTESIAN_POINT ( 'NONE',  ( 3.750093249908572623, 0.7883579158753216687, 2.044908353623323016 ) ) ;
#126651=CARTESIAN_POINT ( 'NONE',  ( 1.729391032145210394, -1.814785505609041838, 0.6465514451386763506 ) ) ;
#126654=CARTESIAN_POINT ( 'NONE',  ( 0.2329586101569320611, 0.7537478099126624365, -1.931748487665209124 ) ) ;
#126662=CARTESIAN_POINT ( 'NONE',  ( 6.515202330376022921, -1.784155196879381622, 0.4545711315065634195 ) ) ;
#126663=CARTESIAN_POINT ( 'NONE',  ( 3.440093027223433797, -1.200828029685986786, -1.615568007891918789 ) ) ;
#126664=CARTESIAN_POINT ( 'NONE',  ( 4.376513399274863936, -0.3984044028133710835, 2.263477716089700387 ) ) ;
#126665=CARTESIAN_POINT ( 'NONE',  ( -0.1290005225502641184, 1.996213967822700663, -2.587563282167547385 ) ) ;
#126666=CARTESIAN_POINT ( 'NONE',  ( 2.500643731865523023, 0.4022941478849762498, 1.816780921579076225 ) ) ;
#126673=CARTESIAN_POINT ( 'NONE',  ( 5.056232447125663221, -1.513354532948107956, 1.442795048270538727 ) ) ;
#126674=CARTESIAN_POINT ( 'NONE',  ( 3.643291952642300213, -1.415932857957047375, -1.222571138756740838 ) ) ;
#126680=CARTESIAN_POINT ( 'NONE',  ( 5.848237035817564156, 1.723274176396558888, 0.07769637638467204177 ) ) ;
#126682=CARTESIAN_POINT ( 'NONE',  ( 1.424001084297383146, -1.255706242181073851, -1.196294345734474129 ) ) ;
#126686=CARTESIAN_POINT ( 'NONE',  ( 5.541899213757757181, 1.452536422000339611, 1.613792965789240696 ) ) ;
#126687=CARTESIAN_POINT ( 'NONE',  ( 4.441915170580639227, 0.7783198120194650960, -1.651611053696280695 ) ) ;
#126688=CARTESIAN_POINT ( 'NONE',  ( 2.500770564479499303, 0.4249116886347775734, 1.915039037836663738 ) ) ;
#126689=CARTESIAN_POINT ( 'NONE',  ( 0.2459221440733790898, 2.093483123843339122, -0.3155690596675052584 ) ) ;
#126693=CARTESIAN_POINT ( 'NONE',  ( 2.491022521637117570, -2.029929026191950481, -0.6131127883793398015 ) ) ;
#126697=CARTESIAN_POINT ( 'NONE',  ( 1.112269271232646739, 2.068042923180101411, -0.09779880236997220977 ) ) ;
#126700=CARTESIAN_POINT ( 'NONE',  ( 3.563320577568354075, -1.815308083731239419, 1.279909030408127091 ) ) ;
#126702=CARTESIAN_POINT ( 'NONE',  ( 0.6338907866723633155, 0.6742984703760960263, 2.197570948669794966 ) ) ;
#126704=CARTESIAN_POINT ( 'NONE',  ( 5.524308913217452321, 1.011932313297726038, 1.797175476313887188 ) ) ;
#126707=CARTESIAN_POINT ( 'NONE',  ( 0.1331565106231606399, 5.723858289613107608, -2.539976893513963052 ) ) ;
#126708=CARTESIAN_POINT ( 'NONE',  ( 5.530750200611445067, -1.661959182355336795, 0.7928504710919548337 ) ) ;
#126712=CARTESIAN_POINT ( 'NONE',  ( -0.1106727585415836906, 0.7252806920327293794, -2.087287528096515299 ) ) ;
#126713=CARTESIAN_POINT ( 'NONE',  ( 3.065164753754692661, 0.2545988855646770244, -1.705743084088023664 ) ) ;
#126714=CARTESIAN_POINT ( 'NONE',  ( 1.305875433988498813, -1.124247956386617231, -1.673852571057246053 ) ) ;
#126715=CARTESIAN_POINT ( 'NONE',  ( 3.164923336591000336, 1.459680849325554197, 1.775737417650694816 ) ) ;
#126716=CARTESIAN_POINT ( 'NONE',  ( 2.583610768588519235, 2.069371435550710459, -0.9147937799905188072 ) ) ;
#126717=CARTESIAN_POINT ( 'NONE',  ( 5.496739094006439785, -0.5105849265115348645, -2.043105244204785453 ) ) ;
#126719=CARTESIAN_POINT ( 'NONE',  ( 3.250976011129117715, -1.444759545231928843, -1.021753751062564497 ) ) ;
#126721=CARTESIAN_POINT ( 'NONE',  ( 6.550320078384911149, -1.775227793318678415, 1.449923619939506025 ) ) ;
#126722=CARTESIAN_POINT ( 'NONE',  ( 4.277188459880359339, 1.204364621523913437, 1.392669941884729035 ) ) ;
#126726=CARTESIAN_POINT ( 'NONE',  ( 4.558633756138521065, -1.956834287480881285, -0.9866608250781593314 ) ) ;
#126730=CARTESIAN_POINT ( 'NONE',  ( 5.301260566756325510, -1.777534899005998481, 1.061244097098137606 ) ) ;
#126731=CARTESIAN_POINT ( 'NONE',  ( 0.4621254960020632074, -1.116205757145168231, 1.679226196708947239 ) ) ;
#126733=CARTESIAN_POINT ( 'NONE',  ( 3.141151230849213327, -1.698683669661217754, 0.9087857633808916757 ) ) ;
#126736=CARTESIAN_POINT ( 'NONE',  ( 0.3346308043965214307, -1.195296165414746037, -1.872270659723746622 ) ) ;
#126745=CARTESIAN_POINT ( 'NONE',  ( 1.381223342121252085, -0.05156877537583307025, 1.961363007973878858 ) ) ;
#126747=CARTESIAN_POINT ( 'NONE',  ( 6.737200384369169903, -1.933438233944267060, 0.9670071574134844195 ) ) ;
#126748=CARTESIAN_POINT ( 'NONE',  ( 5.459412808053472510, 1.602871733476991079, 1.130958114227413436 ) ) ;
#126751=CARTESIAN_POINT ( 'NONE',  ( 5.875883356151954118, 1.283970044810868849, 1.738936680771227206 ) ) ;
#126755=CARTESIAN_POINT ( 'NONE',  ( 0.3857445262360514882, -0.8876765639535091346, 1.646530163845527195 ) ) ;
#126756=CARTESIAN_POINT ( 'NONE',  ( 6.309869086801066729, -1.462580435118435496, 0.9307709330467325293 ) ) ;
#126759=CARTESIAN_POINT ( 'NONE',  ( 2.964592600559623037, -2.025863808726846127, -0.8364240203130177687 ) ) ;
#126760=CARTESIAN_POINT ( 'NONE',  ( 4.507023749723728656, 1.786828103088284658, -1.460221407940938798 ) ) ;
#126761=CARTESIAN_POINT ( 'NONE',  ( 6.116494506269664733, 1.387434351230539598, -1.523912472565646770 ) ) ;
#126762=CARTESIAN_POINT ( 'NONE',  ( 0.9900592867461569524, -0.4711592545371501295, -1.883805795384153381 ) ) ;
#126767=CARTESIAN_POINT ( 'NONE',  ( 4.588201236890728119, 1.223260742344203900, 1.732012071221388450 ) ) ;
#126769=CARTESIAN_POINT ( 'NONE',  ( 2.127577483945505055, 0.4445034925110411539, 1.966644524931899563 ) ) ;
#126771=CARTESIAN_POINT ( 'NONE',  ( 5.262800499965147871, -1.601618428465928057, 1.518362080380669221 ) ) ;
#126774=CARTESIAN_POINT ( 'NONE',  ( 0.2932112110246976044, 1.350478442433366677, 1.228755397233910696 ) ) ;
#126781=CARTESIAN_POINT ( 'NONE',  ( 5.155176885484381799, -1.739861089072095357, -1.104300716835506346 ) ) ;
#126784=CARTESIAN_POINT ( 'NONE',  ( -0.2108831679770960255, 0.2438762813419328990, -1.931650693707862132 ) ) ;
#126787=CARTESIAN_POINT ( 'NONE',  ( 5.022131231807676066, -2.009760515157756444, 0.1999713455246488469 ) ) ;
#126793=CARTESIAN_POINT ( 'NONE',  ( 3.731368383135937883, -1.904846641313600708, 0.7871492865094924518 ) ) ;
#126794=CARTESIAN_POINT ( 'NONE',  ( 2.531875153343257523, -1.674887184936912909, 1.122499117612890673 ) ) ;
#126796=CARTESIAN_POINT ( 'NONE',  ( 6.727182134110200273, 7.629137130509069387, 2.789055895399249696 ) ) ;
#126800=CARTESIAN_POINT ( 'NONE',  ( 2.952499795743710020, 1.423742661936340470, 1.427719607385954381 ) ) ;
#126801=CARTESIAN_POINT ( 'NONE',  ( 2.589598559577494186, -1.836209955096680613, -0.1354230481333124070 ) ) ;
#126802=CARTESIAN_POINT ( 'NONE',  ( 0.7862591250819307431, 1.553807182831347777, 1.706378029075397151 ) ) ;
#126804=CARTESIAN_POINT ( 'NONE',  ( 3.040462492942562545, 2.144887288335277198, 0.2678724578094940356 ) ) ;
#126808=CARTESIAN_POINT ( 'NONE',  ( 0.9713206009373563932, 1.803875226702996049, -0.4951341686536685494 ) ) ;
#126810=CARTESIAN_POINT ( 'NONE',  ( 5.893431036533754330, 1.492594341498763466, 1.288039297220463730 ) ) ;
#126814=CARTESIAN_POINT ( 'NONE',  ( 0.3291288957359936318, 2.113116833900237967, 0.6364493931270903682 ) ) ;
#126815=CARTESIAN_POINT ( 'NONE',  ( 6.514133371570012265, 2.065101995627930620, -0.1482383472809906122 ) ) ;
#126818=DIRECTION ( 'NONE',  ( 1.040834085586084257E-15, 1.000000000000000000, -4.622230424712076367E-32 ) ) ;
#126819=CARTESIAN_POINT ( 'NONE',  ( 5.172717120832922788, -1.856099020970953806, -0.6648386725634397587 ) ) ;
#126820=CARTESIAN_POINT ( 'NONE',  ( 6.187761630889374587, 1.931537729788906477, -0.5904018810464291001 ) ) ;
#126822=CARTESIAN_POINT ( 'NONE',  ( 4.811288673970230967, 2.006026520401600788, 1.140621419682581239 ) ) ;
#126823=CARTESIAN_POINT ( 'NONE',  ( 1.797792903779442009, -1.491087995953117140, -1.425289625791379411 ) ) ;
#126830=CARTESIAN_POINT ( 'NONE',  ( 5.564936049989869460, 1.647787920686558438, -1.413916910601682897 ) ) ;
#126833=CARTESIAN_POINT ( 'NONE',  ( 3.878315922200573862, -0.1843894689829879696, -1.832007427040844183 ) ) ;
#126834=CARTESIAN_POINT ( 'NONE',  ( -0.1604749557937330817, 7.629137130509052511, -2.703579865625728385 ) ) ;
#126835=CARTESIAN_POINT ( 'NONE',  ( 6.620655732516672387, 6.040129668214249570, 2.321170174800915031 ) ) ;
#126836=CARTESIAN_POINT ( 'NONE',  ( 5.601184584505256581, -0.5335315006234629953, 2.125516261704554211 ) ) ;
#126838=CARTESIAN_POINT ( 'NONE',  ( 6.209908689894510836, -2.246332978858367468, 0.2696892186580777673 ) ) ;
#126843=CARTESIAN_POINT ( 'NONE',  ( 0.6371259318241145886, -1.247223858821765230, -1.255979444004810430 ) ) ;
#126846=CARTESIAN_POINT ( 'NONE',  ( 5.022139790744326149, -2.003173700978663874, 0.1997323756105211789 ) ) ;
#126848=CARTESIAN_POINT ( 'NONE',  ( 3.610471823009605341, -0.8516972358460070947, -1.926234778997274244 ) ) ;
#126849=CARTESIAN_POINT ( 'NONE',  ( 3.286649939900693429, 1.508079230315559016, -1.181058552281685659 ) ) ;
#126851=CARTESIAN_POINT ( 'NONE',  ( 4.299236425489592506, -1.714783525531939690, 0.9686585690476202659 ) ) ;
#126852=CARTESIAN_POINT ( 'NONE',  ( 5.836196223694859242, -1.125476168604349514, -1.676936384952235404 ) ) ;
#126853=CARTESIAN_POINT ( 'NONE',  ( 1.938157646728836614, 1.849873822469105145, 0.2772664081076986475 ) ) ;
#126854=CARTESIAN_POINT ( 'NONE',  ( 4.600069218058569831, -1.724633479392148949, -0.03822871362766516734 ) ) ;
#126855=CARTESIAN_POINT ( 'NONE',  ( 1.089939655121434203, 1.141396045679959004, 1.534244836814010693 ) ) ;
#126856=ORIENTED_EDGE ( 'NONE', *, *, #162518, .T. ) ;
#126857=CARTESIAN_POINT ( 'NONE',  ( 1.559489335033688251, -1.894147805384650995, -1.132260830144316888 ) ) ;
#126867=CARTESIAN_POINT ( 'NONE',  ( 2.541538742049511246, 1.893869637037654208, -0.8368498079355383146 ) ) ;
#126872=CARTESIAN_POINT ( 'NONE',  ( 6.164709077089638001, 0.6648188651474650213, 2.013622499735030491 ) ) ;
#126878=CARTESIAN_POINT ( 'NONE',  ( 4.639999869408336863, 0.002810260262744306969, -2.016288307263448321 ) ) ;
#126879=CARTESIAN_POINT ( 'NONE',  ( 4.645656780685024856, 1.893963204498310571, -0.2871864570129621375 ) ) ;
#126880=CARTESIAN_POINT ( 'NONE',  ( 2.489988787850425656, -2.185901284972164405, -0.1580625509675498419 ) ) ;
#126881=CARTESIAN_POINT ( 'NONE',  ( 0.1335669894368343991, 6.947499997881672940, -2.748639729795236963 ) ) ;
#126883=CARTESIAN_POINT ( 'NONE',  ( 5.273694575261410833, 0.3885250917745143862, -1.975199337908732256 ) ) ;
#126886=CARTESIAN_POINT ( 'NONE',  ( 6.415624682135008250, -1.382911306069923407, -1.603242893440869343 ) ) ;
#126888=CARTESIAN_POINT ( 'NONE',  ( 3.439088004391201991, -1.584594249056283877, -1.364047514679037620 ) ) ;
#126890=CARTESIAN_POINT ( 'NONE',  ( 2.133451061308448526, -1.123891114067215424, -1.308414479858905022 ) ) ;
#126892=CARTESIAN_POINT ( 'NONE',  ( 6.187751663909415001, 2.028806014889028120, -0.6170373231123224000 ) ) ;
#126899=ORIENTED_EDGE ( 'NONE', *, *, #91211, .T. ) ;
#126901=CARTESIAN_POINT ( 'NONE',  ( 2.262115610809340094, 1.811117530136572285, 0.04320712765945587674 ) ) ;
#126907=CARTESIAN_POINT ( 'NONE',  ( 3.861793950654641261, 0.6069239149280086787, -1.706917045096454366 ) ) ;
#126908=CARTESIAN_POINT ( 'NONE',  ( 6.539320575229251808, 0.004279804010676873348, 1.996977849922920267 ) ) ;
#126912=CARTESIAN_POINT ( 'NONE',  ( 3.894834723524211118, 0.2711828204805393772, 1.841042229387960472 ) ) ;
#126914=CARTESIAN_POINT ( 'NONE',  ( 1.212342387966048651, 1.846533033048233463, 0.5095510818057205071 ) ) ;
#126915=CARTESIAN_POINT ( 'NONE',  ( 0.7272432748211544729, -1.735090175422876246, 0.5678700757711930835 ) ) ;
#126922=CARTESIAN_POINT ( 'NONE',  ( 5.418793955257063644, -1.429144796294969932, 1.355356204701572143 ) ) ;
#126926=CARTESIAN_POINT ( 'NONE',  ( 0.2344723086637650333, 0.3594713984965206000, 2.059332689821891105 ) ) ;
#126928=CARTESIAN_POINT ( 'NONE',  ( 5.684577344524033293, -1.879503395548718148, -0.4217397607521166103 ) ) ;
#126930=CARTESIAN_POINT ( 'NONE',  ( 0.9557436305893591832, 1.823730570757614800, -0.08488363409227266121 ) ) ;
#126931=CARTESIAN_POINT ( 'NONE',  ( 2.104404934925046877, -2.206339196854599116, 0.05594281105186085790 ) ) ;
#126933=CARTESIAN_POINT ( 'NONE',  ( 0.4395310841842986482, -1.815173276516975243, 0.6020934215927520317 ) ) ;
#126935=CARTESIAN_POINT ( 'NONE',  ( 0.8714670931111346830, -0.2923345663568870378, 1.947617037577647592 ) ) ;
#126936=CARTESIAN_POINT ( 'NONE',  ( 2.384236373620087335, -0.3343274798127248149, -1.912924682550071864 ) ) ;
#126938=CARTESIAN_POINT ( 'NONE',  ( 0.9485920322965735174, 1.351945250224910744, 1.495824703658617416 ) ) ;
#126940=CARTESIAN_POINT ( 'NONE',  ( 5.541811466629937399, 1.248470921604339923, 1.380218479220591155 ) ) ;
#126946=CARTESIAN_POINT ( 'NONE',  ( 1.013517375116283592, -2.137022957946862700, 0.4851717564131745597 ) ) ;
#126950=CARTESIAN_POINT ( 'NONE',  ( 2.877373901574116211, 1.733520850877915187, -0.5729475677913041798 ) ) ;
#126956=CARTESIAN_POINT ( 'NONE',  ( 1.312975575179779586, 1.698600376263710743, 0.9089255565387382996 ) ) ;
#126957=CARTESIAN_POINT ( 'NONE',  ( 5.489096970993415425, 0.1405823987245969631, 1.956747174436481274 ) ) ;
#126961=CARTESIAN_POINT ( 'NONE',  ( 4.968408144156593487, -2.063508908063705238, -0.7385586828293493333 ) ) ;
#126965=CARTESIAN_POINT ( 'NONE',  ( 4.153231765667256603, 1.751622898902647663, -1.103220242290925190 ) ) ;
#126969=CARTESIAN_POINT ( 'NONE',  ( 4.272342533241332063, 2.053246469231550630, -1.033699615426456830 ) ) ;
#126976=CARTESIAN_POINT ( 'NONE',  ( 3.943253339372253308, 0.6530871051511869529, -1.828966769512891277 ) ) ;
#126981=CARTESIAN_POINT ( 'NONE',  ( 4.974826827724895928, -1.381046924789817831, 1.323090558688621909 ) ) ;
#126982=CARTESIAN_POINT ( 'NONE',  ( 6.704117942027653321, -1.724248281341285827, 0.04880198193529976941 ) ) ;
#126983=CARTESIAN_POINT ( 'NONE',  ( 4.891814693739657827, -2.006371927678828104, 0.2024599332275459629 ) ) ;
#126985=CARTESIAN_POINT ( 'NONE',  ( 1.418904949497600487, 1.480075412272121582, -1.637148382315711359 ) ) ;
#126988=CARTESIAN_POINT ( 'NONE',  ( 1.447338344653009701, 0.6056102050338266762, -2.000996673686726179 ) ) ;
#126989=CARTESIAN_POINT ( 'NONE',  ( 6.925078400183545035, 0.003529629153843985134, 1.755452343125718073 ) ) ;
#126990=CARTESIAN_POINT ( 'NONE',  ( 5.660779783930850684, 1.203351582566011047, 1.617819807990819481 ) ) ;
#126992=CARTESIAN_POINT ( 'NONE',  ( 3.047136720273002641, -1.874302040764055599, -1.319397901421492714 ) ) ;
#126993=CARTESIAN_POINT ( 'NONE',  ( 1.411604581429444893, 1.170971978790593448, -1.287647580301202410 ) ) ;
#126994=CARTESIAN_POINT ( 'NONE',  ( 2.619513681940002670, 1.793805257907291395, 1.130712135851599465 ) ) ;
#126996=CARTESIAN_POINT ( 'NONE',  ( 1.580929310206186100, 1.169321551402967119, -1.280364243709716243 ) ) ;
#126998=CARTESIAN_POINT ( 'NONE',  ( 2.224856516622634395, -1.700045390792026989, -0.7576570785256631080 ) ) ;
#126999=CARTESIAN_POINT ( 'NONE',  ( 1.715514515588032030, -1.861668902569445283, -1.117036959414873465 ) ) ;
#127000=CARTESIAN_POINT ( 'NONE',  ( 2.923064838257955156, -1.776166165677966591, 0.9548571111624851726 ) ) ;
#127001=CARTESIAN_POINT ( 'NONE',  ( 4.968750000000002665, 0.7852924748297213098, -1.895863743164188042 ) ) ;
#127004=CARTESIAN_POINT ( 'NONE',  ( 6.428350398238483088, 1.106843121268024976, -1.576624894639609309 ) ) ;
#127006=CARTESIAN_POINT ( 'NONE',  ( 3.551236150222897958, 0.3290391446359001715, 2.196816492004387111 ) ) ;
#127012=CARTESIAN_POINT ( 'NONE',  ( 6.075711799444424521, -0.9231013878284710650, 1.475285791177717076 ) ) ;
#127013=CARTESIAN_POINT ( 'NONE',  ( 4.193769882565239193, -1.351282707657221582, -1.422545440481419510 ) ) ;
#127017=CARTESIAN_POINT ( 'NONE',  ( 5.975896723952917711, 1.340560379189212226, 1.822362705929107429 ) ) ;
#127018=CARTESIAN_POINT ( 'NONE',  ( 2.418490130824833440, 0.8798743164511336756, 1.865715637115851866 ) ) ;
#127022=CARTESIAN_POINT ( 'NONE',  ( 3.848780967690920374, -1.530814235938406931, 1.074699354247290017 ) ) ;
#127023=CARTESIAN_POINT ( 'NONE',  ( 2.971044740931504613, -1.708945904174772989, -0.2933555621278273184 ) ) ;
#127025=CARTESIAN_POINT ( 'NONE',  ( 0.1876184131640425135, 1.704306722208508873, 1.533282888375518960 ) ) ;
#127026=CARTESIAN_POINT ( 'NONE',  ( 0.6400319944965120467, -1.562016764346199960, -1.559085968200937256 ) ) ;
#127027=CARTESIAN_POINT ( 'NONE',  ( 3.590839768554392908, -0.4196827604958653923, -2.120402733634827452 ) ) ;
#127028=CARTESIAN_POINT ( 'NONE',  ( 5.173749199105643903, -1.077276334994947460, 1.615559063095718839 ) ) ;
#127033=CARTESIAN_POINT ( 'NONE',  ( 6.029922689959810178, -1.701949372586025744, 1.081063231324945528 ) ) ;
#127037=CARTESIAN_POINT ( 'NONE',  ( 3.281694405262673087, 1.158851912627656189, 1.410738560442346801 ) ) ;
#127038=CARTESIAN_POINT ( 'NONE',  ( 1.677102584378454608, -2.095606157416990190, -0.6917391671936305997 ) ) ;
#127043=CARTESIAN_POINT ( 'NONE',  ( 1.511979465466501527, -0.6765842426028411127, 1.903255196800458071 ) ) ;
#127044=CARTESIAN_POINT ( 'NONE',  ( 1.401209248766785542, -0.3145075555085960484, -2.096923750572597722 ) ) ;
#127048=CARTESIAN_POINT ( 'NONE',  ( 2.025991663365491746, 0.9512761431412205537, 1.599265494891942030 ) ) ;
#127050=CARTESIAN_POINT ( 'NONE',  ( 0.9894095316701527754, 1.906041449620498929, -1.019753361306941386 ) ) ;
#127051=CARTESIAN_POINT ( 'NONE',  ( 5.713517581197447015, 1.944070655204039433, 0.5350908816983344085 ) ) ;
#127055=CARTESIAN_POINT ( 'NONE',  ( 4.512205841073367196, -0.7830535718562798841, -1.649371741558727678 ) ) ;
#127060=CARTESIAN_POINT ( 'NONE',  ( 6.186875009713125984, -1.117664052418202658, -1.677746505241828334 ) ) ;
#127061=CARTESIAN_POINT ( 'NONE',  ( 5.331922971087851515, 1.814509544241477146, 0.3110680438872318043 ) ) ;
#127062=CARTESIAN_POINT ( 'NONE',  ( -0.02299388927992032997, 1.367829385570513923, -2.164798317653505944 ) ) ;
#127063=CARTESIAN_POINT ( 'NONE',  ( 4.020403473283917783, -1.184823721361260018, -1.980193191683382148 ) ) ;
#127065=CARTESIAN_POINT ( 'NONE',  ( 5.835289683280778128, -1.956920075724715602, 0.9183947573421016308 ) ) ;
#127066=CARTESIAN_POINT ( 'NONE',  ( 1.786567547031367775, 1.688677558619257058, -0.9590575663266877049 ) ) ;
#127067=CARTESIAN_POINT ( 'NONE',  ( 4.604990120689349098, 0.9883660700816098155, -2.075160223314168828 ) ) ;
#127071=CARTESIAN_POINT ( 'NONE',  ( 4.434354141042872399, 1.834536173243521917, 0.3649259964926266364 ) ) ;
#127074=CARTESIAN_POINT ( 'NONE',  ( 2.513799616133075343, -0.5961229146635020903, 1.817204401178821760 ) ) ;
#127077=CARTESIAN_POINT ( 'NONE',  ( 4.301547675229603129, 1.771612934706376707, 1.315755017190944676 ) ) ;
#127081=CARTESIAN_POINT ( 'NONE',  ( 1.405477211469996934, -0.4828617686813937993, 1.911177332403845464 ) ) ;
#127082=CARTESIAN_POINT ( 'NONE',  ( 1.273011573350724568, -1.461848840328241694, 1.785463964174689000 ) ) ;
#127083=CARTESIAN_POINT ( 'NONE',  ( 3.016010921186715432, 1.952665002612500533, -0.1895750030070641190 ) ) ;
#127085=CARTESIAN_POINT ( 'NONE',  ( 6.350444629809289587, -2.052082384739264409, -0.2080662788188895607 ) ) ;
#127087=CARTESIAN_POINT ( 'NONE',  ( 4.118375227313908482, 1.978554835517082555, 0.3886342876525810119 ) ) ;
#127093=CARTESIAN_POINT ( 'NONE',  ( 1.797964266608031547, -1.570508639683061647, -1.499219477302183412 ) ) ;
#127097=CARTESIAN_POINT ( 'NONE',  ( 2.671000074538076863, 0.09590037325727870932, -1.868228684465601752 ) ) ;
#127098=CARTESIAN_POINT ( 'NONE',  ( 6.766866382711775429, -1.973269837180600561, -0.8828958408187634888 ) ) ;
#127100=CARTESIAN_POINT ( 'NONE',  ( 6.827182134110164391, 0.6048993162116442779, 1.764860727632423076 ) ) ;
#127103=( BOUNDED_CURVE ( )  B_SPLINE_CURVE ( 3, ( #110363, #30107, #157999, #177429 ),
 .UNSPECIFIED., .F., .T. ) 
 B_SPLINE_CURVE_WITH_KNOTS ( ( 4, 4 ),
 ( 0.5000000000000022204, 1.000000000000000000 ),
 .UNSPECIFIED. ) 
 CURVE ( )  GEOMETRIC_REPRESENTATION_ITEM ( )  RATIONAL_B_SPLINE_CURVE ( ( 0.9999999999999972244, 0.3333333333333334259, 0.3333333333333363679, 1.000000000000000222 ) ) 
 REPRESENTATION_ITEM ( '' )  );
#127104=CARTESIAN_POINT ( 'NONE',  ( 1.963391044528959073, -1.536740334223782645, -1.137898036029337812 ) ) ;
#127105=CARTESIAN_POINT ( 'NONE',  ( 4.645211000723334926, -1.368906681764755939, -1.121767690593698186 ) ) ;
#127106=CARTESIAN_POINT ( 'NONE',  ( 1.295406243800485635, 1.766531960031037407, -0.7327172462580702206 ) ) ;
#127109=CARTESIAN_POINT ( 'NONE',  ( 6.310162246266422414, 1.098484216484491904, -1.569160930707512502 ) ) ;
#127111=CARTESIAN_POINT ( 'NONE',  ( 1.416557266959647787, 0.8372786474034592530, 1.893679232998768391 ) ) ;
#127114=CARTESIAN_POINT ( 'NONE',  ( 5.295714669793899709, -0.6724083694377264164, 1.745798414713333413 ) ) ;
#127115=CARTESIAN_POINT ( 'NONE',  ( 1.365546509989667534, 1.798985258052044900, -0.3101867277976525505 ) ) ;
#127116=CARTESIAN_POINT ( 'NONE',  ( 6.182275136424624229, -1.184133725572718676, 1.862117674348878760 ) ) ;
#127119=CARTESIAN_POINT ( 'NONE',  ( 2.506364121320878713, 2.062161341495666100, 0.05312637652370164748 ) ) ;
#127125=CARTESIAN_POINT ( 'NONE',  ( 5.459458695672200435, 1.690470114046587646, 1.195012289465044564 ) ) ;
#127127=CARTESIAN_POINT ( 'NONE',  ( 2.372553944209778720, -1.331880425775422205, 1.702409713178254069 ) ) ;
#127129=CARTESIAN_POINT ( 'NONE',  ( 3.404948832191158736, -0.3961486058311721736, -1.980257767865372109 ) ) ;
#127135=CARTESIAN_POINT ( 'NONE',  ( 0.8840003597419334724, -2.016708404047353742, 0.004841148455551891328 ) ) ;
#127137=CARTESIAN_POINT ( 'NONE',  ( 6.110890996357365879, -0.2699588104537915534, 2.174781792473476472 ) ) ;
#127139=CARTESIAN_POINT ( 'NONE',  ( 4.746305163667582150, 0.9781546018433548983, -1.643150005489722787 ) ) ;
#127143=CARTESIAN_POINT ( 'NONE',  ( 3.234000073275579812, 2.016598147164900823, -0.002828922958116042007 ) ) ;
#127146=CARTESIAN_POINT ( 'NONE',  ( 5.596639136713698726, -0.4230586844520961010, -1.671955901692462998 ) ) ;
#127150=CARTESIAN_POINT ( 'NONE',  ( 3.831198023013999698, -1.729401117988647929, 0.7132991360168300377 ) ) ;
#127153=CARTESIAN_POINT ( 'NONE',  ( 1.235311698660218616, -0.04697018572753957483, -2.069874154031334790 ) ) ;
#127157=CARTESIAN_POINT ( 'NONE',  ( 5.830666647502705580, 1.211628268937942066, -1.346810592849301047 ) ) ;
#127160=CARTESIAN_POINT ( 'NONE',  ( -0.1583346312582509796, -1.114004300041637974, -1.428896152673633013 ) ) ;
#127163=CARTESIAN_POINT ( 'NONE',  ( 3.539196308827243787, -1.659330947522210886, -1.431560661003590695 ) ) ;
#127166=CARTESIAN_POINT ( 'NONE',  ( 0.9944974185457016169, 1.932217576897478528, 0.3389098420027157332 ) ) ;
#127168=B_SPLINE_CURVE_WITH_KNOTS ( 'NONE', 3,
 ( #157162, #156086, #122607, #72681, #56448, #6601, #203730, #40202, #119375, #70525 ),
 .UNSPECIFIED., .F., .F.,
 ( 4, 1, 1, 1, 1, 1, 1, 4 ),
 ( 0.000000000000000000, 0.09790276019723312406, 0.1918320694002237370, 0.2608036337010187777, 0.3626611837559554630, 0.5214803378330250538, 0.7337833476510040587, 1.000000000000000000 ),
 .UNSPECIFIED. ) ;
#127169=CARTESIAN_POINT ( 'NONE',  ( 5.097249261280999200, -0.2764669589378037085, 1.895409748447648202 ) ) ;
#127175=ORIENTED_EDGE ( 'NONE', *, *, #193200, .T. ) ;
#127178=CARTESIAN_POINT ( 'NONE',  ( 1.340939272977889729, 0.4221563536682856332, 2.119910705745978508 ) ) ;
#127181=CARTESIAN_POINT ( 'NONE',  ( 1.658932825283397250, -1.563847321437005666, -0.9416461389453802955 ) ) ;
#127182=CARTESIAN_POINT ( 'NONE',  ( 0.1586465271753433603, 2.115359532055087310, 0.1496401998123952359 ) ) ;
#127183=CARTESIAN_POINT ( 'NONE',  ( 5.209893869493905427, -1.816617279468687229, 0.1804919988709560719 ) ) ;
#127186=CARTESIAN_POINT ( 'NONE',  ( 0.7023363917650466970, -0.6599406036866415359, -1.857761218813491988 ) ) ;
#127187=CARTESIAN_POINT ( 'NONE',  ( 3.410326831400651404, -1.910418641682644969, -0.08914582809275289899 ) ) ;
#127189=CARTESIAN_POINT ( 'NONE',  ( 4.193778028305522376, -1.356587754280412339, -1.428115657216560974 ) ) ;
#127191=CARTESIAN_POINT ( 'NONE',  ( 5.688998805639625012, 1.473442329711650345, 1.265259504309938610 ) ) ;
#127197=CARTESIAN_POINT ( 'NONE',  ( 4.248624793116656306, 1.876006594227698221, 0.3698101955103145211 ) ) ;
#127200=CARTESIAN_POINT ( 'NONE',  ( 0.2181801407958559869, -2.163675782650812618, 0.4331315337846516900 ) ) ;
#127202=CARTESIAN_POINT ( 'NONE',  ( 5.690095194620785612, 1.200872180055783112, 1.615535318972769474 ) ) ;
#127204=CARTESIAN_POINT ( 'NONE',  ( 5.654876981934024549, -1.436564326775534806, 1.126588154728463742 ) ) ;
#127205=CARTESIAN_POINT ( 'NONE',  ( 2.471216696211364638, 1.848302923701108158, 0.9330170062570308787 ) ) ;
#127217=CARTESIAN_POINT ( 'NONE',  ( 4.148821288392518625, 0.8220224570679548481, 1.526945684688446381 ) ) ;
#127219=CARTESIAN_POINT ( 'NONE',  ( 1.428671948192638208, -1.316369429293560156, 1.597808059233512656 ) ) ;
#127220=CARTESIAN_POINT ( 'NONE',  ( 3.339577153505444151, 0.5119293057267596536, -2.054306502313862470 ) ) ;
#127224=CARTESIAN_POINT ( 'NONE',  ( 6.877786287229037399, -2.009644702432196617, 0.4970176993947388322 ) ) ;
#127228=DIRECTION ( 'NONE',  ( -0.9999980456341538426, 0.000000000000000000, -0.001977050295967298574 ) ) ;
#127229=CARTESIAN_POINT ( 'NONE',  ( 3.662334778960428139, -1.540015086033737601, 1.698051401694438800 ) ) ;
#127230=CARTESIAN_POINT ( 'NONE',  ( 0.3459771380207553593, 1.820543102168985961, 0.1377627428671979182 ) ) ;
#127231=CARTESIAN_POINT ( 'NONE',  ( 3.849791259674230748, -1.322437695595569673, -1.381667681676468140 ) ) ;
#127236=CARTESIAN_POINT ( 'NONE',  ( 1.687745526430058263, 1.925312447093192825, -0.5882657090081342410 ) ) ;
#127237=CARTESIAN_POINT ( 'NONE',  ( 2.342563710341159400, -1.922903400459201828, -0.3876519335672747313 ) ) ;
#127241=CARTESIAN_POINT ( 'NONE',  ( 5.050766879278534738, -1.765858898356540196, -1.118837652998798005 ) ) ;
#127242=CARTESIAN_POINT ( 'NONE',  ( 3.080641367082480819, -0.1285219475026712632, -1.765225098288242256 ) ) ;
#127245=CARTESIAN_POINT ( 'NONE',  ( 5.947306879541199187, 0.6707566017311801243, -2.191947003353618584 ) ) ;
#127246=CARTESIAN_POINT ( 'NONE',  ( 4.505614311517684101, -0.7474637548481823934, -1.571778613660354207 ) ) ;
#127249=CARTESIAN_POINT ( 'NONE',  ( 4.762897148713774342, -1.733524727309469382, -0.04171941676067019572 ) ) ;
#127250=CARTESIAN_POINT ( 'NONE',  ( 4.897030219210679824, 0.3665305452156160659, 2.139867649710110786 ) ) ;
#127252=CARTESIAN_POINT ( 'NONE',  ( -0.1704767588886099972, -1.641208087572191276, -1.337381612054800772 ) ) ;
#127253=CARTESIAN_POINT ( 'NONE',  ( 5.906250000000004441, 1.895863743163945125, -0.7852924748303062863 ) ) ;
#127255=CARTESIAN_POINT ( 'NONE',  ( 2.977471715415116460, 1.829795069231574534, -0.6025905002205227401 ) ) ;
#127257=CARTESIAN_POINT ( 'NONE',  ( 0.5928132819080602633, -1.229099697874297181, 1.850090981381287358 ) ) ;
#127259=CARTESIAN_POINT ( 'NONE',  ( -0.1411974294641838990, 5.723166529328228336, -2.494358352568406545 ) ) ;
#127262=CARTESIAN_POINT ( 'NONE',  ( 2.825082509308895151, 1.607285200359307886, -1.533455307168646975 ) ) ;
#127268=CARTESIAN_POINT ( 'NONE',  ( 0.3697678102792775756, -0.2496098759999023087, -2.000856779379902139 ) ) ;
#127270=CARTESIAN_POINT ( 'NONE',  ( 5.230950406320217461, -1.941087326682365832, -0.6980428833110083886 ) ) ;
#127274=CARTESIAN_POINT ( 'NONE',  ( 0.5086179708909451813, 1.535567861042252957, 0.8796773807029609760 ) ) ;
#127275=CARTESIAN_POINT ( 'NONE',  ( 5.678250988984351544, 1.318717643421193575, 1.126304846749843769 ) ) ;
#127276=CARTESIAN_POINT ( 'NONE',  ( 5.196709787541290204, 1.427093291641279293, 0.9959802872364865722 ) ) ;
#127278=CARTESIAN_POINT ( 'NONE',  ( 2.542860532589632960, -1.904047414228837942, 1.276277502183044810 ) ) ;
#127280=CARTESIAN_POINT ( 'NONE',  ( 1.710644026344819046, -0.2265308078298749472, 1.827073587482845207 ) ) ;
#127282=CARTESIAN_POINT ( 'NONE',  ( 2.256629077056008015, -1.412982602626071671, 1.155960151518524937 ) ) ;
#127283=CARTESIAN_POINT ( 'NONE',  ( 3.129529892704606464, 0.4926417352555876872, 1.955172657653013957 ) ) ;
#127286=CARTESIAN_POINT ( 'NONE',  ( 4.559663772078708988, 0.4639327178320976630, -2.054050964449795291 ) ) ;
#127289=CARTESIAN_POINT ( 'NONE',  ( 2.014207461368537455, 2.064961549741591185, -0.1501100615294431728 ) ) ;
#127292=CARTESIAN_POINT ( 'NONE',  ( 4.178469031319306914, 1.000645923475869559, 1.869553197578948334 ) ) ;
#127294=CARTESIAN_POINT ( 'NONE',  ( 6.463509179248937642, 0.3066564278407272748, -1.799597105106438777 ) ) ;
#127302=CARTESIAN_POINT ( 'NONE',  ( 6.135037582782754129, 1.979230198018981701, 0.7618025574447004900 ) ) ;
#127303=CARTESIAN_POINT ( 'NONE',  ( 0.9386647947689167326, 2.074798300807283447, 0.3599966696490787266 ) ) ;
#127306=CARTESIAN_POINT ( 'NONE',  ( 6.262542430310119812, -0.6688554880303022587, -1.736790604091620560 ) ) ;
#127315=CARTESIAN_POINT ( 'NONE',  ( 2.576550507925364109, 1.283677811227203147, -1.483670167215108693 ) ) ;
#127316=CARTESIAN_POINT ( 'NONE',  ( 1.358524781292804517, 0.8764843271744371389, 1.976213614152767750 ) ) ;
#127320=CARTESIAN_POINT ( 'NONE',  ( 3.198323437492247123, -1.162659817912135019, -1.286436312214979338 ) ) ;
#127321=CARTESIAN_POINT ( 'NONE',  ( 2.396107360292961008, 1.398095582919863133, -1.036136137726038520 ) ) ;
#127325=CARTESIAN_POINT ( 'NONE',  ( 2.319685276966905629, -1.560262528187049025, 1.276846253076675541 ) ) ;
#127326=CARTESIAN_POINT ( 'NONE',  ( 6.825078400183572036, 7.051914997414900022, 2.742498282622223726 ) ) ;
#127329=CARTESIAN_POINT ( 'NONE',  ( 0.9539096209374531288, 1.969307747869667446, -0.09461285551524113713 ) ) ;
#127330=CARTESIAN_POINT ( 'NONE',  ( 6.117437049485344502, 1.593764408019750389, 1.056661447057717362 ) ) ;
#127335=CARTESIAN_POINT ( 'NONE',  ( 1.418624149192078576, -0.7290977765982089576, -1.883658722702468591 ) ) ;
#127336=CARTESIAN_POINT ( 'NONE',  ( 4.823409937486792032, -0.1187154998047341425, 2.304658580708033533 ) ) ;
#127337=CARTESIAN_POINT ( 'NONE',  ( 5.670351692713981429, -0.8806477319739226539, -1.753155087565357428 ) ) ;
#127338=CARTESIAN_POINT ( 'NONE',  ( 2.869914117416060062, -1.941089286637355693, 0.2830422620509198128 ) ) ;
#127342=CARTESIAN_POINT ( 'NONE',  ( 0.9017390913304748068, -2.064370131783893392, 0.4699791444322827250 ) ) ;
#127345=CARTESIAN_POINT ( 'NONE',  ( 1.499689682683522207, -0.6613356838569836027, -1.718437284301529200 ) ) ;
#127347=CARTESIAN_POINT ( 'NONE',  ( 3.134000194803722383, 2.016708403948695771, -0.004836970814638129855 ) ) ;
#127349=CARTESIAN_POINT ( 'NONE',  ( 2.883181758455736432, -1.960942133159260692, -0.8077274430827171559 ) ) ;
#127353=CARTESIAN_POINT ( 'NONE',  ( 3.128252755821586906, 1.147704512706015922, -1.711389856620056493 ) ) ;
#127355=CARTESIAN_POINT ( 'NONE',  ( 0.2394788589213901198, 1.836227513651207177, 0.1364553164684492448 ) ) ;
#127357=CARTESIAN_POINT ( 'NONE',  ( -0.02244404828157658613, 7.629137130509074716, -2.789100637983293662 ) ) ;
#127359=CARTESIAN_POINT ( 'NONE',  ( 0.3291288957359936318, 2.113116833900237967, 0.6364493931270903682 ) ) ;
#127360=CARTESIAN_POINT ( 'NONE',  ( 2.812116484403729633, -2.238188867732244791, 0.3292703641907517298 ) ) ;
#127362=CARTESIAN_POINT ( 'NONE',  ( 2.285178059325339461, 0.08539987017499665878, -1.809671756684204214 ) ) ;
#127363=CARTESIAN_POINT ( 'NONE',  ( 3.010844082872287331, 0.05196181304293297915, 1.915202476457795511 ) ) ;
#127364=CARTESIAN_POINT ( 'NONE',  ( 4.070807014193541740, 1.466255041752505539, -1.461937513464212079 ) ) ;
#127366=CARTESIAN_POINT ( 'NONE',  ( 1.569145635881466605, 0.1472162271188414695, -1.966034296795520664 ) ) ;
#127367=CARTESIAN_POINT ( 'NONE',  ( 6.393193437440540805, 1.674708767708126045, -0.9521171982297592651 ) ) ;
#127368=CARTESIAN_POINT ( 'NONE',  ( 3.133525119713890472, -1.255248497922526463, -1.387151338369890574 ) ) ;
#127369=CARTESIAN_POINT ( 'NONE',  ( 2.438448314377542392, 1.086391669559241047, -2.035977865114136254 ) ) ;
#127371=CARTESIAN_POINT ( 'NONE',  ( 2.347915429038241353, -0.7989592750466242288, 1.680985684562475990 ) ) ;
#127373=CARTESIAN_POINT ( 'NONE',  ( 6.443808500197930833, 1.419581301535753015, 1.496705048937081006 ) ) ;
#127377=CARTESIAN_POINT ( 'NONE',  ( 6.211965580189116487, -2.090513352778848422, 0.2539706045930691380 ) ) ;
#127379=CARTESIAN_POINT ( 'NONE',  ( 6.274726406708529325, -2.050348626090079840, -0.6846857035173321560 ) ) ;
#127380=CARTESIAN_POINT ( 'NONE',  ( 6.498695841808301843, -1.981098178724240322, -0.3918999010058578092 ) ) ;
#127387=CARTESIAN_POINT ( 'NONE',  ( 4.768767694835816862, -0.2516295123269947642, -2.000731945836851544 ) ) ;
#127391=B_SPLINE_CURVE_WITH_KNOTS ( 'NONE', 3,
 ( #66931, #151433, #18197, #103749, #117920, #85352 ),
 .UNSPECIFIED., .F., .F.,
 ( 4, 1, 1, 4 ),
 ( 0.000000000000000000, 0.5978647917419361857, 0.6978647917419360525, 1.000000000000000000 ),
 .UNSPECIFIED. ) ;
#127393=CARTESIAN_POINT ( 'NONE',  ( 5.805597153138060129, -0.5296426447994294628, 2.095691122003799478 ) ) ;
#127398=CARTESIAN_POINT ( 'NONE',  ( 0.1752026701883572513, 1.419887415397131925, 1.286083148499452600 ) ) ;
#127401=CARTESIAN_POINT ( 'NONE',  ( 1.998289267358617671, -0.4583927764671858474, -1.662768097037459869 ) ) ;
#127405=CARTESIAN_POINT ( 'NONE',  ( 0.9481069621972251227, 0.5063937300482551640, 1.695761627633844304 ) ) ;
#127406=CARTESIAN_POINT ( 'NONE',  ( 1.629542719884415680, -0.2443838731654828789, 1.998128341252780604 ) ) ;
#127408=CARTESIAN_POINT ( 'NONE',  ( 4.137865722265689605, -1.519559189622637252, -1.600479987451455699 ) ) ;
#127410=CARTESIAN_POINT ( 'NONE',  ( 4.909118719746323301, -1.747747579089290237, 1.287847701716714255 ) ) ;
#127414=CARTESIAN_POINT ( 'NONE',  ( 3.018346832952636394, -2.117961878424143407, 0.1061830045200745365 ) ) ;
#127415=CARTESIAN_POINT ( 'NONE',  ( 3.409779952838042583, -1.203371721269937744, -1.617806234278630573 ) ) ;
#127416=CARTESIAN_POINT ( 'NONE',  ( 2.953145165254339233, -1.595657772652997464, 0.8577772064107972438 ) ) ;
#127423=CARTESIAN_POINT ( 'NONE',  ( 5.900976575431972293, 1.489821718068456979, -1.054992404821846863 ) ) ;
#127425=CARTESIAN_POINT ( 'NONE',  ( 1.446349702961244876, -1.352062789758176731, 1.357433777346368498 ) ) ;
#127434=CARTESIAN_POINT ( 'NONE',  ( 4.997027575558513846, 1.799266821141291661, -1.197868618907194316 ) ) ;
#127437=CARTESIAN_POINT ( 'NONE',  ( 3.551138032611600437, 0.3147205237276836653, 2.097014573754731881 ) ) ;
#127440=CARTESIAN_POINT ( 'NONE',  ( 4.077382496314372773, 1.857369029195341525, -0.6610406152272005897 ) ) ;
#127441=CARTESIAN_POINT ( 'NONE',  ( 6.187759705938407073, 1.828009178079874841, -0.5617473972939349691 ) ) ;
#127443=CARTESIAN_POINT ( 'NONE',  ( 5.612555052430599822, 2.041346303960121400, 0.5620598648080311621 ) ) ;
#127445=CARTESIAN_POINT ( 'NONE',  ( 6.830521637698823589, -1.212721230272953754, 1.552361911452035503 ) ) ;
#127446=CARTESIAN_POINT ( 'NONE',  ( 2.150241637240562831, -1.501185980473922488, 1.231905181128474691 ) ) ;
#127450=CARTESIAN_POINT ( 'NONE',  ( 3.082061393860520138, -2.059794914563463308, -0.3567947225071969042 ) ) ;
#127453=CARTESIAN_POINT ( 'NONE',  ( 0.06471810551328219252, -1.456173922333989790, 1.077237379209189827 ) ) ;
#127455=CARTESIAN_POINT ( 'NONE',  ( 5.110101661328442901, -2.196521081226535443, 0.2136625748923453583 ) ) ;
#127457=CARTESIAN_POINT ( 'NONE',  ( 3.663272223086514234, -1.945104670120747059, -1.042327912031751458 ) ) ;
#127460=CARTESIAN_POINT ( 'NONE',  ( 1.893074787327468700, -0.09523556418119562272, -1.910042277862213034 ) ) ;
#127461=CIRCLE ( 'NONE', #155053, 0.05000000000000056483 ) ;
#127463=CARTESIAN_POINT ( 'NONE',  ( 5.775854211382815073, -2.020734006234246927, 0.4499205674863211990 ) ) ;
#127465=CARTESIAN_POINT ( 'NONE',  ( 2.958072429731006370, 2.151414462573512765, -0.2105227563667099733 ) ) ;
#127466=CARTESIAN_POINT ( 'NONE',  ( 5.179302069984247581, 1.471482994053765925, 1.624232740060495228 ) ) ;
#127475=CARTESIAN_POINT ( 'NONE',  ( 0.2467204944939948574, 1.994070950632735428, -0.2986300710981006357 ) ) ;
#127478=CARTESIAN_POINT ( 'NONE',  ( 5.155165671438199482, 1.724248240607465732, -1.145533019084030268 ) ) ;
#127479=CARTESIAN_POINT ( 'NONE',  ( 3.035679594228014810, -1.294101122711612151, -1.427291446562365618 ) ) ;
#127480=CARTESIAN_POINT ( 'NONE',  ( -0.1409997244346088141, -0.002808977843308038680, -2.000147647483838220 ) ) ;
#127484=CARTESIAN_POINT ( 'NONE',  ( 3.713681502677267154, 0.4829771288026918907, -1.909149233777557075 ) ) ;
#127485=CARTESIAN_POINT ( 'NONE',  ( 0.006183538434290089709, -0.9405624870862170361, -1.977291442860461768 ) ) ;
#127486=CARTESIAN_POINT ( 'NONE',  ( 3.844227010333609584, 1.817057058749595777, 0.1772887374331885701 ) ) ;
#127492=CARTESIAN_POINT ( 'NONE',  ( 1.452429406588066740, -1.579491434881035827, -0.9459884711465746943 ) ) ;
#127493=CARTESIAN_POINT ( 'NONE',  ( 4.623295736497193609, 1.753618999902604614, 0.9886709913553303197 ) ) ;
#127494=CARTESIAN_POINT ( 'NONE',  ( 0.5096300131263042932, 2.292432092913086361, 0.1664806320332279099 ) ) ;
#127495=CARTESIAN_POINT ( 'NONE',  ( 5.700043108275813175, 0.7984002208856562088, -1.792138013221859394 ) ) ;
#127501=CARTESIAN_POINT ( 'NONE',  ( 1.628582148955775910, 0.2080868244966528613, 2.080379227509927542 ) ) ;
#127502=CARTESIAN_POINT ( 'NONE',  ( 6.491055376221456008, 1.537463663300852490, -0.8764918771043300749 ) ) ;
#127504=CARTESIAN_POINT ( 'NONE',  ( -0.2102771530458459603, 1.310786636098780544, -2.452585248267840967 ) ) ;
#127505=CARTESIAN_POINT ( 'NONE',  ( 1.768729326414076430, 1.665373798791164317, -0.5055230280728554293 ) ) ;
#127510=CARTESIAN_POINT ( 'NONE',  ( 2.121340078736310364, -1.673401575455361723, 0.4176718278932553541 ) ) ;
#127511=CARTESIAN_POINT ( 'NONE',  ( 1.945129482973105839, -1.762486321751283835, -1.302348873264857820 ) ) ;
#127512=CARTESIAN_POINT ( 'NONE',  ( 4.319099500008596770, 2.017107695584336557, 0.8957252843501888329 ) ) ;
#127514=CARTESIAN_POINT ( 'NONE',  ( 2.711994142844989408, 0.5828001693900261015, -2.091290491527279194 ) ) ;
#127515=CARTESIAN_POINT ( 'NONE',  ( 1.137010146156680834, -1.651496384925277283, 0.7785749969668461778 ) ) ;
#127516=CARTESIAN_POINT ( 'NONE',  ( 3.309862381128574338, -1.264700674563856264, -1.697971918580774675 ) ) ;
#127517=CARTESIAN_POINT ( 'NONE',  ( 6.539320575229228716, 1.281788455817688188, 2.013036689384885225 ) ) ;
#127520=CARTESIAN_POINT ( 'NONE',  ( 3.140441720415044546, 0.5589363893779492054, 2.223061277538174174 ) ) ;
#127524=CARTESIAN_POINT ( 'NONE',  ( 5.760436963792294307, 2.218610086356072930, 0.1113587401332209043 ) ) ;
#127528=CARTESIAN_POINT ( 'NONE',  ( 6.825078400183575589, 7.629137130509070275, 2.455651831298297338 ) ) ;
#127530=CARTESIAN_POINT ( 'NONE',  ( 3.727185537919291747, 2.006959858346604619, 0.1948421285040344286 ) ) ;
#127532=CARTESIAN_POINT ( 'NONE',  ( 2.659094170149599368, 1.659314987522000795, -1.224949181800268017 ) ) ;
#127537=CARTESIAN_POINT ( 'NONE',  ( 4.699289266375740404, -0.5861454505808120219, 2.111544493182772708 ) ) ;
#127538=CARTESIAN_POINT ( 'NONE',  ( 2.408827471728996361, -1.163269702728772392, -1.646838680093346996 ) ) ;
#127539=CARTESIAN_POINT ( 'NONE',  ( 1.874305484616908934, -0.09156810461483089192, -1.839108553062768214 ) ) ;
#127542=CARTESIAN_POINT ( 'NONE',  ( 6.704125975539116489, -1.825092170400946845, 0.04854515157103055090 ) ) ;
#127543=CARTESIAN_POINT ( 'NONE',  ( 0.1066027571702803795, -0.1042336552941041522, 2.296444677329109840 ) ) ;
#127545=CARTESIAN_POINT ( 'NONE',  ( 5.225545412997908201, -2.150153479602398221, 0.7043797957921889008 ) ) ;
#127547=CARTESIAN_POINT ( 'NONE',  ( 0.3640743269037312602, 2.082829956593022835, -0.3111531555848711106 ) ) ;
#127559=CARTESIAN_POINT ( 'NONE',  ( 1.793382672576701919, -0.1090974814243403090, -2.117938670719583527 ) ) ;
#127560=CARTESIAN_POINT ( 'NONE',  ( 3.393049125975013069, -2.141818966976690497, -0.5891788363768469816 ) ) ;
#127564=CARTESIAN_POINT ( 'NONE',  ( 3.982823771651412770, 1.862158852298421152, 0.6176278068941787325 ) ) ;
#127572=CARTESIAN_POINT ( 'NONE',  ( 3.111701630267147412, 1.674174984267240429, 1.301503359413098249 ) ) ;
#127574=CARTESIAN_POINT ( 'NONE',  ( 4.346650381253648554, 0.5737703434565506466, 2.084106190491950006 ) ) ;
#127575=CARTESIAN_POINT ( 'NONE',  ( 4.352959896991869471, 0.3989296284454147412, -1.797357466088687961 ) ) ;
#127578=CARTESIAN_POINT ( 'NONE',  ( 5.788919933143140462, 1.322006966288125085, 1.131936178618123456 ) ) ;
#127582=CARTESIAN_POINT ( 'NONE',  ( 3.151412294154242844, -1.766339975446712174, -1.245920677233211871 ) ) ;
#127583=CARTESIAN_POINT ( 'NONE',  ( 5.307970166423544356, -1.730600239375930549, 1.034008556546859969 ) ) ;
#127586=CARTESIAN_POINT ( 'NONE',  ( 2.782270202741622178, -1.112240752214749273, 1.853481441253836071 ) ) ;
#127589=CARTESIAN_POINT ( 'NONE',  ( 3.374254075663080332, -1.176934739253515438, 1.581319453489488325 ) ) ;
#127590=CARTESIAN_POINT ( 'NONE',  ( 4.845229750085990439, 0.6055439843271113176, -1.845326283916528753 ) ) ;
#127599=CARTESIAN_POINT ( 'NONE',  ( 1.747397587315655088, -1.864034986486883039, 1.180896971623420999 ) ) ;
#127601=CARTESIAN_POINT ( 'NONE',  ( 6.139501739389007007, 1.813922436357641388, -0.7475906808915923074 ) ) ;
#127605=CARTESIAN_POINT ( 'NONE',  ( 0.07479286986305369589, 0.004866263145587855152, -1.855573292446037970 ) ) ;
#127606=CARTESIAN_POINT ( 'NONE',  ( 6.721333373144884327, -0.1645177889858795151, 2.170883633896856679 ) ) ;
#127607=CARTESIAN_POINT ( 'NONE',  ( 5.841722611436678925, 1.839261846420519708, 0.08593139445873397564 ) ) ;
#127612=CARTESIAN_POINT ( 'NONE',  ( 6.170199167347634628, 2.114832956739281400, -0.1575216572810705096 ) ) ;
#127615=CARTESIAN_POINT ( 'NONE',  ( 6.098915436037096960, 1.687290577560787375, -1.182889608693861394 ) ) ;
#127617=CARTESIAN_POINT ( 'NONE',  ( 2.259996020855909116, -1.860750554326926487, 0.04185779618384557338 ) ) ;
#127618=CARTESIAN_POINT ( 'NONE',  ( 4.054132754448328768, -1.361571661076573792, 1.239656203754435193 ) ) ;
#127624=CARTESIAN_POINT ( 'NONE',  ( 3.088704478669739295, -2.174299887604825177, -0.3769171259565203269 ) ) ;
#127625=CARTESIAN_POINT ( 'NONE',  ( 5.782586711780850486, -2.205454299129143703, -0.5038293679325082097 ) ) ;
#127627=CARTESIAN_POINT ( 'NONE',  ( 5.396671993488243224, -1.769204348786549641, -0.3888369506312178703 ) ) ;
#127628=CARTESIAN_POINT ( 'NONE',  ( 6.473869786608328347, -0.8128310455158479497, 1.733272608194774689 ) ) ;
#127630=CARTESIAN_POINT ( 'NONE',  ( 6.174654088403855212, -1.776896415251895789, -0.5849557326117056366 ) ) ;
#127631=CARTESIAN_POINT ( 'NONE',  ( 5.549440478958018730, -1.726947976793649975, 0.8215754744917985741 ) ) ;
#127633=CARTESIAN_POINT ( 'NONE',  ( 0.9888773766892227091, 1.651582696977689890, -0.8784067438419729257 ) ) ;
#127634=CARTESIAN_POINT ( 'NONE',  ( 1.534389036647098692, 0.6371565916030231813, 1.913260934284975345 ) ) ;
#127636=CARTESIAN_POINT ( 'NONE',  ( 3.967482597722607363, 0.2578578757282763978, -2.090148584218749939 ) ) ;
#127641=CARTESIAN_POINT ( 'NONE',  ( 2.865494903669623117, -1.653614387114977990, -1.159512146270498478 ) ) ;
#127645=CARTESIAN_POINT ( 'NONE',  ( 3.268983376858981327, -1.995845357749256976, -0.8305886511386084692 ) ) ;
#127651=CARTESIAN_POINT ( 'NONE',  ( 0.4851436980863755299, 2.077851564382672933, 0.6296362999115376891 ) ) ;
#127655=CARTESIAN_POINT ( 'NONE',  ( 2.015410700679621137, -2.124826835150806392, 0.5361769018528695918 ) ) ;
#127657=CARTESIAN_POINT ( 'NONE',  ( 2.079355054740182229, -0.1115493103639639688, -2.259872350005930119 ) ) ;
#127659=CARTESIAN_POINT ( 'NONE',  ( 4.610564714392807240, 1.931124171932835809, 0.5807562064495259690 ) ) ;
#127665=CARTESIAN_POINT ( 'NONE',  ( 4.745210919507984570, -1.367539302148174318, -1.123239564495488674 ) ) ;
#127667=CARTESIAN_POINT ( 'NONE',  ( 1.132014994273435216, -1.335988328115779167, -1.627952913800976731 ) ) ;
#127671=CARTESIAN_POINT ( 'NONE',  ( 6.380482474105581225, -0.5405081658083621399, -1.942537888137134461 ) ) ;
#127675=CARTESIAN_POINT ( 'NONE',  ( 4.205816867194319464, -1.865656749788859647, 0.1373567816406878750 ) ) ;
#127676=CARTESIAN_POINT ( 'NONE',  ( 2.993098612437726125, 0.2488643248897918769, 2.055149816265568585 ) ) ;
#127682=CARTESIAN_POINT ( 'NONE',  ( 6.420800710400103917, 2.015122584031241004, 0.7829223626853940576 ) ) ;
#127685=CARTESIAN_POINT ( 'NONE',  ( 3.490630252122446375, 1.913478943654752129, 0.4322817992908413176 ) ) ;
#127686=CARTESIAN_POINT ( 'NONE',  ( 1.370470000664014254, -0.4925687793003556969, 1.954872606163795989 ) ) ;
#127690=CARTESIAN_POINT ( 'NONE',  ( 1.528351178377739927, 1.801267752838480840, 0.5040548479407629401 ) ) ;
#127692=CARTESIAN_POINT ( 'NONE',  ( 3.568611400213494989, 0.7284950617309441379, 1.876934371664749301 ) ) ;
#127694=CARTESIAN_POINT ( 'NONE',  ( 2.724332569758937339, 2.101576450279537767, 0.2563457491038360070 ) ) ;
#127696=CARTESIAN_POINT ( 'NONE',  ( 4.158688916442685013, -0.6465363538536235133, -1.966910096795893681 ) ) ;
#127698=CARTESIAN_POINT ( 'NONE',  ( 0.1872078708128835645, 1.551958633911882934, 1.401156373025253421 ) ) ;
#127700=CARTESIAN_POINT ( 'NONE',  ( 5.245057492501287832, -1.564903486862476489, 0.9398553879134128319 ) ) ;
#127705=CARTESIAN_POINT ( 'NONE',  ( 6.018643902988223715, 1.486383190695803158, -1.631276885294789203 ) ) ;
#127707=CARTESIAN_POINT ( 'NONE',  ( 5.637344576021464881, -0.04253375892994575719, 1.911971901805488816 ) ) ;
#127718=CARTESIAN_POINT ( 'NONE',  ( -0.02319159430947542386, 0.2540490248266329965, -1.846305437520213477 ) ) ;
#127725=CARTESIAN_POINT ( 'NONE',  ( 2.641402650619076198, 1.802640082279869382, -0.7936183362749064107 ) ) ;
#127727=CARTESIAN_POINT ( 'NONE',  ( 3.778922869151004171, 1.701937167235707982, -1.081084515101193633 ) ) ;
#127730=CARTESIAN_POINT ( 'NONE',  ( 6.727182134110236689, 0.5535242275785922095, 2.340336476220133743 ) ) ;
#127731=CARTESIAN_POINT ( 'NONE',  ( 3.521585679250069045, -1.305302140894725627, -1.760141160621036649 ) ) ;
#127733=CARTESIAN_POINT ( 'NONE',  ( 2.502848596126582059, 1.548454276800725449, -1.145803370841493418 ) ) ;
#127736=CARTESIAN_POINT ( 'NONE',  ( -0.1296875068447882473, 5.724785194352729256, -2.420566058096422779 ) ) ;
#127737=CARTESIAN_POINT ( 'NONE',  ( 0.2333540202161349941, 2.877056899079268870, -2.534299598574590640 ) ) ;
#127744=CARTESIAN_POINT ( 'NONE',  ( 5.267088776126935379, 1.772936381825638952, -0.4966186330585887210 ) ) ;
#127745=CARTESIAN_POINT ( 'NONE',  ( 1.611978021082097978, -0.6760664726842831040, 1.896312242100234524 ) ) ;
#127746=CARTESIAN_POINT ( 'NONE',  ( 4.446792056507931079, 1.496784378905056334, 1.744297655265887537 ) ) ;
#127747=CARTESIAN_POINT ( 'NONE',  ( -0.1291982275798392032, 1.351143144720265532, -2.329141727150272789 ) ) ;
#127748=CARTESIAN_POINT ( 'NONE',  ( 2.412761291957177701, -1.442071615443579091, 1.176286876380010726 ) ) ;
#127751=CARTESIAN_POINT ( 'NONE',  ( 5.185773951807310489, 1.841398108398510480, -0.5159224025059682139 ) ) ;
#127755=CARTESIAN_POINT ( 'NONE',  ( 4.933190498422773018, -1.479524406611672394, -1.477502780037798447 ) ) ;
#127756=CARTESIAN_POINT ( 'NONE',  ( 3.309304339999539657, -0.3661640501408692794, 1.834289908569000538 ) ) ;
#127762=CARTESIAN_POINT ( 'NONE',  ( 6.621745524129793559, -1.670984818007285266, 0.4274731708342211500 ) ) ;
#127765=CARTESIAN_POINT ( 'NONE',  ( 1.951430075251599838, -1.585913025431864742, -0.7019457847057923860 ) ) ;
#127768=CARTESIAN_POINT ( 'NONE',  ( 5.858309005574939832, -2.171239809575730817, -0.007779773244297875576 ) ) ;
#127769=CARTESIAN_POINT ( 'NONE',  ( 4.881388680972560401, 1.702354803207173584, -0.6601141376258444771 ) ) ;
#127770=CARTESIAN_POINT ( 'NONE',  ( 2.606241817087478374, 1.961221450604538008, 0.05310280016677935283 ) ) ;
#127771=CARTESIAN_POINT ( 'NONE',  ( 0.2634788376212302552, 1.973769265480609381, -0.7665230665306818070 ) ) ;
#127775=CARTESIAN_POINT ( 'NONE',  ( 2.824977599723184074, 1.534285384246200090, -1.463936014953904463 ) ) ;
#127780=CARTESIAN_POINT ( 'NONE',  ( 0.7431355771655088205, -0.2497938498803170537, -2.055034051290441255 ) ) ;
#127783=CARTESIAN_POINT ( 'NONE',  ( 4.002737143027909283, -2.197200394838841664, -0.3254818186308478523 ) ) ;
#127785=CARTESIAN_POINT ( 'NONE',  ( 0.9151166212276349299, -1.463470719828030120, -1.772635753884302057 ) ) ;
#127787=CARTESIAN_POINT ( 'NONE',  ( 5.998899845030374323, 0.3968100507469035643, 2.023884403326465797 ) ) ;
#127790=CARTESIAN_POINT ( 'NONE',  ( 0.2331563151865486683, 0.005903526429595904942, -1.945944850731482934 ) ) ;
#127791=CARTESIAN_POINT ( 'NONE',  ( 5.126429434416579056, 0.1410513515392505246, 1.835921608166577013 ) ) ;
#127793=CARTESIAN_POINT ( 'NONE',  ( 2.819059531128511598, -0.1711090930666993304, 1.716262065957876004 ) ) ;
#127794=CARTESIAN_POINT ( 'NONE',  ( 1.675017921984035096, 1.752138005693338441, -0.9981273289914743829 ) ) ;
#127795=CARTESIAN_POINT ( 'NONE',  ( 2.637635294750583004, 0.7773225462509441019, 2.163377341885423188 ) ) ;
#127797=CARTESIAN_POINT ( 'NONE',  ( 2.917521460708580872, -0.2248114924257374192, 2.251233801775154308 ) ) ;
#127798=CARTESIAN_POINT ( 'NONE',  ( 5.004563900840214963, -0.7087877200973876635, -1.983347251131000855 ) ) ;
#127800=CARTESIAN_POINT ( 'NONE',  ( 3.163107763524728444, 0.2631224511941733790, -1.749944513356870734 ) ) ;
#127804=CARTESIAN_POINT ( 'NONE',  ( 6.585440809757122871, -0.9837151097084917417, 2.068200907652519405 ) ) ;
#127805=CARTESIAN_POINT ( 'NONE',  ( 4.329911453333429527, 1.806054511993939515, 0.3568155486674411958 ) ) ;
#127810=CARTESIAN_POINT ( 'NONE',  ( 4.470767510317084970, 0.001397387737574890204, -2.191629466793604486 ) ) ;
#127815=CARTESIAN_POINT ( 'NONE',  ( 3.422408909100621344, 1.221451249705886477, -1.489789856891531761 ) ) ;
#127818=CARTESIAN_POINT ( 'NONE',  ( 0.5104038411899833871, -0.7921320118633947693, 2.075572886547627505 ) ) ;
#127827=CARTESIAN_POINT ( 'NONE',  ( 2.102700294964424454, -0.3804589880251930123, 1.698169956227519872 ) ) ;
#127829=CARTESIAN_POINT ( 'NONE',  ( 0.6077679335219284829, 0.6189715888181289705, -1.861716921216026055 ) ) ;
#127832=CARTESIAN_POINT ( 'NONE',  ( 6.121977807712331909, -1.196819783530624015, -1.799967629666970881 ) ) ;
#127835=CARTESIAN_POINT ( 'NONE',  ( 5.260679775997886054, -1.568431141927080219, 1.487858469166832176 ) ) ;
#127836=CARTESIAN_POINT ( 'NONE',  ( -0.2106725631050020975, 5.721452923065615259, -2.597767226077936087 ) ) ;
#127839=CARTESIAN_POINT ( 'NONE',  ( 6.919227946136824237, -0.1375138451006757134, 1.940497564164916922 ) ) ;
#127840=CARTESIAN_POINT ( 'NONE',  ( 5.835191860132536767, -1.097891704307648597, 1.341895879554096727 ) ) ;
#127842=CARTESIAN_POINT ( 'NONE',  ( 3.544632465004614374, -1.790652189326558563, 1.263247045326252094 ) ) ;
#127843=CARTESIAN_POINT ( 'NONE',  ( 3.100898361104642120, -0.6683016296473989204, -2.208703637169514788 ) ) ;
#127844=CARTESIAN_POINT ( 'NONE',  ( 5.571578285044489043, 1.987195396197571462, -0.5455906853745869922 ) ) ;
#127845=CARTESIAN_POINT ( 'NONE',  ( 1.288897009404812666, 1.470358960358808309, 1.268651691623223110 ) ) ;
#127850=CARTESIAN_POINT ( 'NONE',  ( 4.570628194609677841, 0.8141925398062774821, 1.958264201954627026 ) ) ;
#127852=CARTESIAN_POINT ( 'NONE',  ( 1.863907939170056149, -0.1017519224979606118, -2.013985838549677609 ) ) ;
#127854=CARTESIAN_POINT ( 'NONE',  ( 5.895608061265788180, 1.667329832391790667, 1.445732890734657161 ) ) ;
#127863=CARTESIAN_POINT ( 'NONE',  ( 4.715729953790866347, -2.021515393979388175, 0.4000037541747498704 ) ) ;
#127868=CARTESIAN_POINT ( 'NONE',  ( 4.881513094923572105, 0.1956549798781386795, -2.010156034525738988 ) ) ;
#127873=CARTESIAN_POINT ( 'NONE',  ( 2.747006664573675039, -1.714185755289293622, 1.143718651939158670 ) ) ;
#127874=CARTESIAN_POINT ( 'NONE',  ( 2.742814741689561853, 2.006446121045248887, -0.2004354718553730264 ) ) ;
#127876=CARTESIAN_POINT ( 'NONE',  ( 6.727182134110222478, 4.688348259194305534, 2.751590707055273199 ) ) ;
#127880=CARTESIAN_POINT ( 'NONE',  ( 2.636092105226188309, 0.1017362925337349233, -2.013677536115268563 ) ) ;
#127881=CARTESIAN_POINT ( 'NONE',  ( 1.956743257466783570, 0.3155556147324266036, -1.813728304320901596 ) ) ;
#127882=CARTESIAN_POINT ( 'NONE',  ( 1.313548042387347348, 2.037171730821058624, 1.084164666379479502 ) ) ;
#127884=CARTESIAN_POINT ( 'NONE',  ( 2.741676502816026595, -1.599691942034554337, -1.453933697666408120 ) ) ;
#127890=CARTESIAN_POINT ( 'NONE',  ( 0.7252172114964609007, -1.777616610744123804, 0.5828384007960025759 ) ) ;
#127891=CARTESIAN_POINT ( 'NONE',  ( 5.225445458360559847, -1.872321802520343414, 0.6175577138636638708 ) ) ;
#127895=CARTESIAN_POINT ( 'NONE',  ( 0.5752038918783763943, -2.079344756725898691, -0.7397341299467049547 ) ) ;
#127896=CARTESIAN_POINT ( 'NONE',  ( 6.795378861676105053, -1.851214886592133846, 0.9271815693319698237 ) ) ;
#127899=CARTESIAN_POINT ( 'NONE',  ( 6.539320575229251808, 7.629137130509035636, 2.803262396134009737 ) ) ;
#127900=CARTESIAN_POINT ( 'NONE',  ( 4.452002833372045387, 1.971050344634683427, -0.04741254548742446229 ) ) ;
#127901=CARTESIAN_POINT ( 'NONE',  ( 0.03560581989598374242, -0.09759080014098624190, 2.118463022953632091 ) ) ;
#127903=CARTESIAN_POINT ( 'NONE',  ( 4.600386337014011673, -2.307077041318765342, -0.05981084109947519545 ) ) ;
#127904=CARTESIAN_POINT ( 'NONE',  ( 2.483324480268500611, -0.004404232681418790429, 2.062741127353195925 ) ) ;
#127911=CARTESIAN_POINT ( 'NONE',  ( 4.281792510435393773, -2.078899500905183828, 0.6263114880437108400 ) ) ;
#127913=CARTESIAN_POINT ( 'NONE',  ( 3.843160323004328305, 0.6166970922517557296, -1.735048075492843456 ) ) ;
#127916=CARTESIAN_POINT ( 'NONE',  ( 5.003566749295822014, -2.181051155298455058, 0.2145382695054529609 ) ) ;
#127918=CARTESIAN_POINT ( 'NONE',  ( 6.385631343721732911, 1.554564302923328700, 1.644106664497286596 ) ) ;
#127927=CARTESIAN_POINT ( 'NONE',  ( 1.252431388357349684, -1.398210551426328330, 1.084949785890441110 ) ) ;
#127928=CARTESIAN_POINT ( 'NONE',  ( 4.846344381697188730, 1.033023791896072519, -1.727689222339493069 ) ) ;
#127930=CARTESIAN_POINT ( 'NONE',  ( 4.612399560509667928, -0.8980232107528103302, -1.905027153144087437 ) ) ;
#127931=CARTESIAN_POINT ( 'NONE',  ( 2.020959903547480341, -1.710230010390185296, 0.8631189023672394267 ) ) ;
#127933=CARTESIAN_POINT ( 'NONE',  ( 2.892966452247947906, 0.2382023302623069438, 1.955005545544076240 ) ) ;
#127935=CARTESIAN_POINT ( 'NONE',  ( 5.853772736177474734, -1.465772220379698343, -1.389892856972896329 ) ) ;
#127936=CARTESIAN_POINT ( 'NONE',  ( 1.621729638615863944, -1.036547396872866678, -1.557007864774778705 ) ) ;
#127937=CARTESIAN_POINT ( 'NONE',  ( 5.408750372623219782, 1.302234988713904640, -1.131221429639968745 ) ) ;
#127938=CARTESIAN_POINT ( 'NONE',  ( 1.423922367354793606, -1.897583212610975734, 0.2371896777705190806 ) ) ;
#127940=CARTESIAN_POINT ( 'NONE',  ( 0.9618826090718561872, 0.4271145061440981272, -2.164990749644220447 ) ) ;
#127948=CARTESIAN_POINT ( 'NONE',  ( 1.873570696236816158, -0.2555354716398828274, 2.054483085851127377 ) ) ;
#127953=CARTESIAN_POINT ( 'NONE',  ( 6.059260758684835046, -1.791542317298041365, 1.134111293253435182 ) ) ;
#127957=CARTESIAN_POINT ( 'NONE',  ( 6.848121815800094936, -0.8396676627679277027, 1.771385694100804375 ) ) ;
#127959=CARTESIAN_POINT ( 'NONE',  ( 4.833361152654930493, -1.319026006086077230, 1.524810761284051575 ) ) ;
#127960=CARTESIAN_POINT ( 'NONE',  ( 4.557778266838360182, 1.108094384514320963, 1.562507240529472874 ) ) ;
#127962=CARTESIAN_POINT ( 'NONE',  ( 2.454835928891830221, -1.908367152989149718, -1.077367144120815023 ) ) ;
#127966=CARTESIAN_POINT ( 'NONE',  ( 4.939702229944241907, -1.910329301133410151, 0.6354416197995541582 ) ) ;
#127969=CARTESIAN_POINT ( 'NONE',  ( 6.011343318556897408, -1.993460012771612222, 0.7135861072808927785 ) ) ;
#127971=CARTESIAN_POINT ( 'NONE',  ( 3.245728744149275702, 2.090933975402937683, -0.002398190518447183318 ) ) ;
#127973=CARTESIAN_POINT ( 'NONE',  ( 1.465380626080296400, 1.700101026837578466, -0.2896415544312477830 ) ) ;
#127975=CARTESIAN_POINT ( 'NONE',  ( 4.834296457332984076, -1.136628438424293508, -1.790084250976264002 ) ) ;
#127983=CARTESIAN_POINT ( 'NONE',  ( 1.348006360704995910, 0.8929448326314154416, -1.575985355173844527 ) ) ;
#127988=CARTESIAN_POINT ( 'NONE',  ( 3.158660791640830467, 0.4427227019567353539, 1.756387338163778233 ) ) ;
#127992=CARTESIAN_POINT ( 'NONE',  ( 4.246440214068532448, -1.840602306905499086, -0.2743259802632999622 ) ) ;
#127993=CARTESIAN_POINT ( 'NONE',  ( 1.423292265346193464, -1.388624197914482883, -1.319832876491247697 ) ) ;
#127994=CARTESIAN_POINT ( 'NONE',  ( 6.422877973628248860, 1.797746274024723201, 0.6925914001822802701 ) ) ;
#128000=CARTESIAN_POINT ( 'NONE',  ( 6.121921657745279077, 1.940899573806122325, -0.3330216297181831653 ) ) ;
#128004=CARTESIAN_POINT ( 'NONE',  ( -0.02919842301645457147, -0.002306431287177941429, -2.073770398395402115 ) ) ;
#128006=CARTESIAN_POINT ( 'NONE',  ( 5.016589502704805525, 1.328544886203905318, -1.395186341261208884 ) ) ;
#128009=CARTESIAN_POINT ( 'NONE',  ( 1.588595499965880453, -0.2641367610144580991, -1.806243275932853276 ) ) ;
#128010=CARTESIAN_POINT ( 'NONE',  ( 2.121956728516772639, -2.140194184088719531, 0.5379336890513550795 ) ) ;
#128011=CARTESIAN_POINT ( 'NONE',  ( 0.1582721923853447621, 1.907395734848855051, 0.1385995803297388196 ) ) ;
#128013=CARTESIAN_POINT ( 'NONE',  ( 0.3792734414799744380, -0.1002090192285705339, 1.967142940827655284 ) ) ;
#128014=CARTESIAN_POINT ( 'NONE',  ( 3.052217916795424202, -1.468930141372110088, 1.270444820450331358 ) ) ;
#128015=CARTESIAN_POINT ( 'NONE',  ( 0.7552322466577044979, -2.000550463317086525, -0.2495714061315074117 ) ) ;
#128017=CARTESIAN_POINT ( 'NONE',  ( 5.383604208181901107, -1.767738693978682996, 0.5818682867176503404 ) ) ;
#128023=CARTESIAN_POINT ( 'NONE',  ( 1.083813775577105565, -0.9808430935620198188, 1.959877696171570927 ) ) ;
#128027=CARTESIAN_POINT ( 'NONE',  ( 2.525780997283606499, -1.050937884436175418, -1.492673824175783093 ) ) ;
#128031=CARTESIAN_POINT ( 'NONE',  ( 6.509000000000010111, 6.037005099786168394, 2.594901386363585694 ) ) ;
#128033=CARTESIAN_POINT ( 'NONE',  ( 0.7153026426200872478, -0.2839029868492106701, 1.905349893463634814 ) ) ;
#128034=CARTESIAN_POINT ( 'NONE',  ( 5.541838416980684023, 1.314774629379747539, 1.456173869884537675 ) ) ;
#128037=CARTESIAN_POINT ( 'NONE',  ( 4.704715985517350596, 1.906866092115505840, 1.080010033982371498 ) ) ;
#128039=CARTESIAN_POINT ( 'NONE',  ( 4.329010850845236291, -1.929826300244817272, -0.7499136367685385052 ) ) ;
#128043=CARTESIAN_POINT ( 'NONE',  ( 4.360180292246352174, 0.0003893357360621601550, -2.298851035006874266 ) ) ;
#128048=CARTESIAN_POINT ( 'NONE',  ( 6.620655732516647518, 0.007553340620044743381, 1.826407896915738238 ) ) ;
#128050=CARTESIAN_POINT ( 'NONE',  ( 3.451055654028605701, 0.4708835965685866376, -1.883881102318455847 ) ) ;
#128054=CARTESIAN_POINT ( 'NONE',  ( 5.502191098127390489, -0.8541586074963626318, 1.711093258865265643 ) ) ;
#128055=CARTESIAN_POINT ( 'NONE',  ( 6.299779570463345912, -0.5759050694413189175, 1.625906498142214884 ) ) ;
#128056=CARTESIAN_POINT ( 'NONE',  ( 4.997279897388729353, -0.2910847460899004258, 1.995267753224789997 ) ) ;
#128058=CARTESIAN_POINT ( 'NONE',  ( 2.245003380770736801, 0.4850519687749441644, 2.152760086278446394 ) ) ;
#128061=CARTESIAN_POINT ( 'NONE',  ( 1.746151220907150359, 0.6571888886500141247, 1.984721739902342019 ) ) ;
#128062=CARTESIAN_POINT ( 'NONE',  ( 0.2152203129428611750, -1.737008003653650157, 0.3383841826808623443 ) ) ;
#128063=CARTESIAN_POINT ( 'NONE',  ( 5.924453975591452703, -1.462443569488897754, -1.388487997949397368 ) ) ;
#128065=CARTESIAN_POINT ( 'NONE',  ( 2.607731988003787915, -2.267127051869659571, 0.3377934734241551662 ) ) ;
#128066=CARTESIAN_POINT ( 'NONE',  ( 1.042430265417312985, -1.369658564370433540, -1.073568199598630146 ) ) ;
#128069=CARTESIAN_POINT ( 'NONE',  ( 0.9656601056488465229, 1.412931828189394556, 1.004572000263863840 ) ) ;
#128072=CARTESIAN_POINT ( 'NONE',  ( 0.9421113726552653445, 1.458074577165750396, 1.608915699534870569 ) ) ;
#128073=CARTESIAN_POINT ( 'NONE',  ( 1.956267901341804283, -1.236798062192035363, 1.592663274815858676 ) ) ;
#128074=CARTESIAN_POINT ( 'NONE',  ( 4.500000000000003553, -2.561000571632643674E-13, -2.052068128417943171 ) ) ;
#128076=CARTESIAN_POINT ( 'NONE',  ( 6.129514107576198967, -1.813157573415961066, 0.6514091821806231586 ) ) ;
#128078=CARTESIAN_POINT ( 'NONE',  ( 2.883289241188752072, -2.054055030226094480, -0.8463503915563088675 ) ) ;
#128083=CARTESIAN_POINT ( 'NONE',  ( 5.935049520445493165, -1.266825670006064275, -1.193719461430408968 ) ) ;
#128084=CARTESIAN_POINT ( 'NONE',  ( 3.947668504265917644, 1.419370528949075005, 1.354593381527373186 ) ) ;
#128088=CARTESIAN_POINT ( 'NONE',  ( 4.710415318105323657, -0.9616676431317521256, -2.047968690232481848 ) ) ;
#128089=CARTESIAN_POINT ( 'NONE',  ( 1.855998075696059901, -0.6969055236651957586, 1.941492863836144611 ) ) ;
#128093=CARTESIAN_POINT ( 'NONE',  ( 3.778450875046265534, -1.801938340082277712, -0.5016190811713144848 ) ) ;
#128094=CARTESIAN_POINT ( 'NONE',  ( 2.496349097179047405, -1.714988558773246741, 0.2561001183170578677 ) ) ;
#128095=CARTESIAN_POINT ( 'NONE',  ( 6.603104432341277530, -0.4828188497946246382, 2.145653685147373313 ) ) ;
#128096=CARTESIAN_POINT ( 'NONE',  ( 0.1302870565101400258, -1.360178740744298675, -1.738515015553928622 ) ) ;
#128097=CARTESIAN_POINT ( 'NONE',  ( 3.450221060135277629, 2.161883445724331665, 0.001893877739161941697 ) ) ;
#128098=CARTESIAN_POINT ( 'NONE',  ( 4.329980137697307718, 1.904743498531726198, 0.3774997404530285317 ) ) ;
#128100=CARTESIAN_POINT ( 'NONE',  ( 6.555916519444559221, 1.865492442988415656, -0.1378669075578625169 ) ) ;
#128104=CARTESIAN_POINT ( 'NONE',  ( -0.1049925189658337810, -2.058569791948822392, -0.5088776734372552069 ) ) ;
#128106=CARTESIAN_POINT ( 'NONE',  ( 6.223279759862190730, 1.994869330463379331, 0.2930738960792296233 ) ) ;
#128110=CARTESIAN_POINT ( 'NONE',  ( 2.807047293222181494, 1.542382716246639474, 0.9765254425028799812 ) ) ;
#128111=CARTESIAN_POINT ( 'NONE',  ( 2.555956245031346885, 0.5892994983645870599, -2.126554282292691500 ) ) ;
#128116=CARTESIAN_POINT ( 'NONE',  ( 0.4924518904856821089, -1.118466686806585342, 1.681619975139287515 ) ) ;
#128117=CARTESIAN_POINT ( 'NONE',  ( 0.6980877996264934771, 1.427081234210248573, 1.568565553304770877 ) ) ;
#128119=CARTESIAN_POINT ( 'NONE',  ( 1.481066496106745234, -0.05241980694788496431, 1.860401082089859770 ) ) ;
#128121=CARTESIAN_POINT ( 'NONE',  ( 6.438362351209899082, 2.038089008908655853, 0.3048918457534201543 ) ) ;
#128122=CARTESIAN_POINT ( 'NONE',  ( 6.223279759862189842, 1.994869330463379553, 0.2930738960792296233 ) ) ;
#128126=CARTESIAN_POINT ( 'NONE',  ( 3.896943178251357054, 1.541351720387572843, -0.9781566455248569270 ) ) ;
#128130=CARTESIAN_POINT ( 'NONE',  ( 6.731795954091533751, -1.842168972580451314, -0.8196458303668037182 ) ) ;
#128131=CARTESIAN_POINT ( 'NONE',  ( 6.228435704027582176, 0.1854037366294820077, 1.831779187086844729 ) ) ;
#128133=CARTESIAN_POINT ( 'NONE',  ( 4.389522222404328211, 2.062498103173298514, -1.035318202965694434 ) ) ;
#128135=CARTESIAN_POINT ( 'NONE',  ( 6.169229141836320096, 0.1658205177522271700, -2.155315574850395155 ) ) ;
#128137=CARTESIAN_POINT ( 'NONE',  ( 0.6615421549095920062, 0.9584981283930308349, 1.688995467024148045 ) ) ;
#128142=CARTESIAN_POINT ( 'NONE',  ( 4.218341386676929261, -1.908100849112413178, -1.281069462185228325 ) ) ;
#128145=CARTESIAN_POINT ( 'NONE',  ( 5.137510444216992767, -1.323429205136433140, -1.322332877454430955 ) ) ;
#128147=CARTESIAN_POINT ( 'NONE',  ( 2.109489925670060551, 1.480643174185194200, 1.210387159491378650 ) ) ;
#128150=CARTESIAN_POINT ( 'NONE',  ( 3.528125218122651230, -1.314342534882004809, -1.772652456903674567 ) ) ;
#128151=CARTESIAN_POINT ( 'NONE',  ( 6.883263157960407774, 1.288564682660230831, 1.962666442651111565 ) ) ;
#128156=CARTESIAN_POINT ( 'NONE',  ( 1.212115688179933759, -0.8827433895065642799, -1.762721879769993283 ) ) ;
#128157=CARTESIAN_POINT ( 'NONE',  ( 1.062054608305310177, 0.4471719227481777414, -2.263690193671878514 ) ) ;
#128158=CARTESIAN_POINT ( 'NONE',  ( 2.312880826517309085, -1.518475810973318074, 1.242258525517292433 ) ) ;
#128160=CARTESIAN_POINT ( 'NONE',  ( 5.102416002207363022, 2.056666295747246576, 0.1571963825151497518 ) ) ;
#128167=CARTESIAN_POINT ( 'NONE',  ( 1.253040875654364505, -0.5252153140962511069, -2.106489908942406952 ) ) ;
#128171=CARTESIAN_POINT ( 'NONE',  ( 2.495189509527053762, 1.443206194050347557, 1.189963633554675937 ) ) ;
#128172=CARTESIAN_POINT ( 'NONE',  ( 6.889893180375397996, -0.9309023296741396614, 1.948985471107896439 ) ) ;
#128173=CARTESIAN_POINT ( 'NONE',  ( 0.07755575628181492209, 4.082361791518872352, -2.743585103993382734 ) ) ;
#128174=CARTESIAN_POINT ( 'NONE',  ( 6.827182134110195477, 0.006757161851597691914, 1.710856279483467413 ) ) ;
#128177=CARTESIAN_POINT ( 'NONE',  ( 2.033716200607054159, -1.854476301366870583, 0.4660679227486629883 ) ) ;
#128179=CARTESIAN_POINT ( 'NONE',  ( 4.117836676938036788, -0.9100935957705791335, -1.517748890920249671 ) ) ;
#128180=CARTESIAN_POINT ( 'NONE',  ( 2.262237773093742188, 1.911903731097279513, 0.04523801603947830152 ) ) ;
#128183=CARTESIAN_POINT ( 'NONE',  ( 5.870691181925934643, -0.2860506952705432204, -1.894010149965511758 ) ) ;
#128185=CARTESIAN_POINT ( 'NONE',  ( 0.2388460773940295212, -2.007853281042128568, -0.5044432775610437902 ) ) ;
#128188=CARTESIAN_POINT ( 'NONE',  ( 5.207814216083940018, -1.861544245658670604, 0.1842191830812092979 ) ) ;
#128189=CARTESIAN_POINT ( 'NONE',  ( 1.875362892791394787, 1.747422460009705913, -0.5287960245906262458 ) ) ;
#128191=CARTESIAN_POINT ( 'NONE',  ( 4.705825944637973990, -0.5905853116198942487, 2.126329296355852883 ) ) ;
#128194=CARTESIAN_POINT ( 'NONE',  ( 3.297386996040070795, -1.820318649397782318, 0.9700563119749375796 ) ) ;
#128203=CARTESIAN_POINT ( 'NONE',  ( 5.090316257491098284, 1.067296284200716983, -1.773933887923849984 ) ) ;
#128205=CARTESIAN_POINT ( 'NONE',  ( 2.618638089201937635, 1.414096770131420655, -1.634928933042498533 ) ) ;
#128207=CARTESIAN_POINT ( 'NONE',  ( 3.703775025860293724, 1.464345522003915878, 1.391222453660536873 ) ) ;
#128208=CARTESIAN_POINT ( 'NONE',  ( 6.720655732516672920, 1.239197277384354035, 2.287559680360019332 ) ) ;
#128210=ADVANCED_FACE ( 'NONE', ( #47573 ), #124799, .T. ) ;
#128214=CARTESIAN_POINT ( 'NONE',  ( 1.358611653602972646, -1.916354379050893009, -0.6279873632355145174 ) ) ;
#128215=CARTESIAN_POINT ( 'NONE',  ( 6.075747529084263299, -1.173811750163206158, 1.850510016281024850 ) ) ;
#128217=CARTESIAN_POINT ( 'NONE',  ( 4.922078805074791674, -1.902621863305080430, 0.1933406509087298719 ) ) ;
#128221=CARTESIAN_POINT ( 'NONE',  ( 2.812125237574263803, 1.117814398428567557, -1.678018709429726307 ) ) ;
#128224=CARTESIAN_POINT ( 'NONE',  ( 5.139545982361763521, -1.221863454424999329, -1.217595815693907957 ) ) ;
#128230=CARTESIAN_POINT ( 'NONE',  ( 1.288034235163344254, -1.310400469390052836, -1.602789277989056016 ) ) ;
#128233=CARTESIAN_POINT ( 'NONE',  ( 5.074790875859057415, -1.308146702057958910, 1.253318493144810697 ) ) ;
#128236=CARTESIAN_POINT ( 'NONE',  ( 6.094382945298186804, -0.9628849012233617888, 1.534170072110131899 ) ) ;
#128239=CARTESIAN_POINT ( 'NONE',  ( 3.521585679250069045, -1.305302140894725627, -1.760141160621036649 ) ) ;
#128241=CARTESIAN_POINT ( 'NONE',  ( 0.2210476084268316321, -1.750679471464357650, -0.8856473702157914296 ) ) ;
#128243=CARTESIAN_POINT ( 'NONE',  ( 4.499565103457034532, -1.877818951341524878, 0.3776799693050793549 ) ) ;
#128252=CARTESIAN_POINT ( 'NONE',  ( 2.131903390035182255, -1.411712784473453830, -1.637176306262012826 ) ) ;
#128255=CARTESIAN_POINT ( 'NONE',  ( 1.571042225754931465, 0.1381101175703668971, -1.820421783975199048 ) ) ;
#128256=CARTESIAN_POINT ( 'NONE',  ( -0.1577409392781377873, -1.310076727147227560, -1.668215054097483385 ) ) ;
#128258=CARTESIAN_POINT ( 'NONE',  ( 5.227504313999177477, -1.733024862908550290, 0.5741523302658231298 ) ) ;
#128260=CARTESIAN_POINT ( 'NONE',  ( 2.759904966095374501, 0.6844231338998980618, -1.785916880244736715 ) ) ;
#128262=CARTESIAN_POINT ( 'NONE',  ( 3.490635713810024132, 1.920951117756137583, 0.4340392168088512692 ) ) ;
#128264=CARTESIAN_POINT ( 'NONE',  ( 6.515186996419942034, -1.882659881547473546, 0.4762376372081030262 ) ) ;
#128268=CARTESIAN_POINT ( 'NONE',  ( 5.783468009189684622, 0.1541500780414573890, -2.115021274163720211 ) ) ;
#128270=CARTESIAN_POINT ( 'NONE',  ( 3.984940423737866055, -1.785409543757199291, -0.6854135386504257577 ) ) ;
#128276=CARTESIAN_POINT ( 'NONE',  ( 4.846344381697188730, 1.033023791896072519, -1.727689222339493069 ) ) ;
#128278=CARTESIAN_POINT ( 'NONE',  ( 5.584540971669589737, -1.782103179330214449, -0.3958202769075992444 ) ) ;
#128279=CARTESIAN_POINT ( 'NONE',  ( 0.3618904354094238940, -0.5536326762660361833, 1.994880328902041589 ) ) ;
#128283=CARTESIAN_POINT ( 'NONE',  ( 6.666881909320486521, -1.711340306973156977, -0.7558587634414122292 ) ) ;
#128289=FILL_AREA_STYLE_COLOUR ( '', #41627 ) ;
#128291=CARTESIAN_POINT ( 'NONE',  ( 3.392920078539514162, -0.7062313252990999324, -1.584032799413936710 ) ) ;
#128293=CARTESIAN_POINT ( 'NONE',  ( 1.182579820358391931, 1.236233925375467058, -1.660450453320160058 ) ) ;
#128294=CARTESIAN_POINT ( 'NONE',  ( 1.986098615764248398, -2.116669865667855088, 0.05555418577087371801 ) ) ;
#128298=CARTESIAN_POINT ( 'NONE',  ( 1.076931260867712625, 1.817606662292377218, 0.7587987759381797925 ) ) ;
#128303=CARTESIAN_POINT ( 'NONE',  ( 2.027642443044708198, -1.499220162234589093, -1.734095823995058794 ) ) ;
#128304=CARTESIAN_POINT ( 'NONE',  ( 0.9085097582094739943, 1.384192474337717194, -1.190531929384466503 ) ) ;
#128305=CARTESIAN_POINT ( 'NONE',  ( 3.006014587165442453, -0.7710369221427433306, 1.750240277048662030 ) ) ;
#128309=CARTESIAN_POINT ( 'NONE',  ( 2.144791297303435762, 1.953827510466410455, 0.4849535144586021307 ) ) ;
#128310=CARTESIAN_POINT ( 'NONE',  ( 1.657006586592904673, 1.606862555911577006, -1.125131163738995577 ) ) ;
#128314=CARTESIAN_POINT ( 'NONE',  ( 5.296857843117306786, 1.708683220140273740, 1.204356289764816568 ) ) ;
#128315=CARTESIAN_POINT ( 'NONE',  ( 3.520126680498508520, 1.123421168108656776, -1.367553765667248955 ) ) ;
#128318=CARTESIAN_POINT ( 'NONE',  ( 6.369073578265099123, 2.195482680428318290, -0.6590174882785122534 ) ) ;
#128319=CARTESIAN_POINT ( 'NONE',  ( 4.857210178628561970, 1.720700030253617951, -0.2597475362437673407 ) ) ;
#128322=CARTESIAN_POINT ( 'NONE',  ( 4.903498277369322977, 0.2971982615034232111, 1.707963748468165122 ) ) ;
#128324=CARTESIAN_POINT ( 'NONE',  ( 5.160662515399747186, -0.7266353732918430230, -2.046117350891932141 ) ) ;
#128326=CARTESIAN_POINT ( 'NONE',  ( -0.2349522205629230309, -0.1529240981989663239, -2.083514258294770105 ) ) ;
#128327=CARTESIAN_POINT ( 'NONE',  ( 4.843750000000003553, 1.895863743164186710, 0.7852924748297296365 ) ) ;
#128329=CARTESIAN_POINT ( 'NONE',  ( 3.100521554045695627, -0.5575540177290801980, -1.843951249938739378 ) ) ;
#128331=CARTESIAN_POINT ( 'NONE',  ( 0.4170203200158085211, -0.7540967040414385814, -2.089506846138278195 ) ) ;
#128333=CARTESIAN_POINT ( 'NONE',  ( 6.883263157960408662, 2.979503955789930547, 2.299731230128279513 ) ) ;
#128336=CARTESIAN_POINT ( 'NONE',  ( 2.157158246434082827, 0.4899616716134093108, 2.166440146811992040 ) ) ;
#128337=CARTESIAN_POINT ( 'NONE',  ( -0.02900071798687918478, 7.629137130509076492, -2.773797386654376584 ) ) ;
#128341=CARTESIAN_POINT ( 'NONE',  ( 1.020157974382044364, -1.821741137083273010, 0.8647263380179845971 ) ) ;
#128343=CARTESIAN_POINT ( 'NONE',  ( 5.758276963478038191, -2.062851381910678850, -0.003602753815758196875 ) ) ;
#128347=CARTESIAN_POINT ( 'NONE',  ( 6.784453417974287248, -1.834524189944960693, -0.3643881242741816573 ) ) ;
#128348=CARTESIAN_POINT ( 'NONE',  ( 6.223290642006293893, 1.716731611696775683, 0.2442158411369663995 ) ) ;
#128349=CARTESIAN_POINT ( 'NONE',  ( 5.811982450300033243, 1.162468279597946630, -1.295502344845029574 ) ) ;
#128350=CARTESIAN_POINT ( 'NONE',  ( 3.105313311461850745, -0.4450742334846323756, 2.248595817482400783 ) ) ;
#128352=CARTESIAN_POINT ( 'NONE',  ( 1.130510352786683326, -1.665311210022573540, 0.7854980884962547982 ) ) ;
#128354=CARTESIAN_POINT ( 'NONE',  ( 2.449991753796490368, 1.825138167369045661, 0.04731899098397300552 ) ) ;
#128355=CARTESIAN_POINT ( 'NONE',  ( 2.813125141109920069, 1.117832431973438734, -1.678005364621336426 ) ) ;
#128356=CARTESIAN_POINT ( 'NONE',  ( 1.412352946837617473, 1.469754387505791460, -1.625674263109680329 ) ) ;
#128358=CARTESIAN_POINT ( 'NONE',  ( 4.629967194361879201, -1.293677666091449296, -1.661686202823991820 ) ) ;
#128362=CARTESIAN_POINT ( 'NONE',  ( 1.117730493923989599, 0.4056601665377962407, -2.030061024271647252 ) ) ;
#128365=CARTESIAN_POINT ( 'NONE',  ( 4.160867320283115234, 0.5667376361006767338, 2.043264482828925033 ) ) ;
#128366=CARTESIAN_POINT ( 'NONE',  ( 0.2406815423939384080, 0.3279693432677989184, 1.898232506199586167 ) ) ;
#128373=CARTESIAN_POINT ( 'NONE',  ( 6.398696098476772676, -2.079943653215409416, -0.4123558718646391785 ) ) ;
#128374=CARTESIAN_POINT ( 'NONE',  ( 1.202331507228219243, -2.106147100265920002, -0.0002331622408376087278 ) ) ;
#128377=CARTESIAN_POINT ( 'NONE',  ( 5.102340918953698790, 1.855823733615385551, 0.1392438295388219172 ) ) ;
#128384=CARTESIAN_POINT ( 'NONE',  ( 2.119516022818414669, 0.3384452847540948550, -1.932298432780136244 ) ) ;
#128385=B_SPLINE_CURVE_WITH_KNOTS ( 'NONE', 3,
 ( #192274, #142514, #74290, #73195, #206404, #90552, #10331, #77474, #91630, #41811 ),
 .UNSPECIFIED., .F., .F.,
 ( 4, 1, 1, 1, 1, 1, 1, 4 ),
 ( 0.000000000000000000, 0.09272347919791326665, 0.1850049962306132278, 0.2567072177207115891, 0.3610482009861257779, 0.5209239196176974618, 0.7336689415868371533, 1.000000000000000000 ),
 .UNSPECIFIED. ) ;
#128386=CARTESIAN_POINT ( 'NONE',  ( 0.6730137850648570952, -2.035850703004048246, -0.7271551459356735414 ) ) ;
#128390=CARTESIAN_POINT ( 'NONE',  ( 3.022450238936627009, 1.725798670860735351, -0.1664453034943418896 ) ) ;
#128391=CARTESIAN_POINT ( 'NONE',  ( 1.833560160614732704, 1.721085009045751901, 0.2571270737643116533 ) ) ;
#128395=CARTESIAN_POINT ( 'NONE',  ( 1.212267286723569981, -1.587592435625035270, -1.242539042498117086 ) ) ;
#128396=CARTESIAN_POINT ( 'NONE',  ( 6.925078400183548588, 2.417948008941684268, 2.525058136801380027 ) ) ;
#128398=CARTESIAN_POINT ( 'NONE',  ( 1.024223545076022424, 1.176019522272594875, -1.582147633265261977 ) ) ;
#128399=CARTESIAN_POINT ( 'NONE',  ( 5.449440537890920311, -1.726199344983204265, 0.8234401749890255529 ) ) ;
#128404=CARTESIAN_POINT ( 'NONE',  ( 1.735027068915934167, 1.885295237280168790, 0.7248928932378613244 ) ) ;
#128406=CARTESIAN_POINT ( 'NONE',  ( 4.471882758057180496, 2.239461445850467580, -0.5561450820626266944 ) ) ;
#128407=CARTESIAN_POINT ( 'NONE',  ( 5.898874287966751950, 0.3812104124719677412, 1.924297140916144233 ) ) ;
#128409=CARTESIAN_POINT ( 'NONE',  ( 1.797631089865757259, -1.417250949620936895, -1.356651810197152086 ) ) ;
#128413=CARTESIAN_POINT ( 'NONE',  ( 1.780608593570524034, -0.5699985197749558585, -2.039088110117696750 ) ) ;
#128416=CARTESIAN_POINT ( 'NONE',  ( 0.9020086522944226193, 1.395640307904035593, -1.200911154268270664 ) ) ;
#128419=CARTESIAN_POINT ( 'NONE',  ( 3.428091063814618700, -2.088597262255381448, 0.3661859999234198249 ) ) ;
#128423=CARTESIAN_POINT ( 'NONE',  ( 3.321608758505911307, -1.986990267296639745, 0.5463351552400242950 ) ) ;
#128425=CARTESIAN_POINT ( 'NONE',  ( 0.6437974683802077935, 0.5340323341261629109, 1.762076181610471526 ) ) ;
#128431=CARTESIAN_POINT ( 'NONE',  ( 2.689068300184436655, -0.3842959826076980390, -2.229375072012912629 ) ) ;
#128433=CARTESIAN_POINT ( 'NONE',  ( 2.478518767674630308, -1.246658584539367176, 1.314663817856591699 ) ) ;
#128434=CARTESIAN_POINT ( 'NONE',  ( 3.503066848181853654, -0.1354201214893405170, 1.910964455010273344 ) ) ;
#128435=CARTESIAN_POINT ( 'NONE',  ( 4.264170421968140445, -2.065031762457261610, 0.1491743435546449281 ) ) ;
#128438=CARTESIAN_POINT ( 'NONE',  ( 1.938291742056476030, 1.949724373066508143, 0.2912656003557292927 ) ) ;
#128439=CARTESIAN_POINT ( 'NONE',  ( 0.4637318561061140043, 1.905900585730261110, -0.2794304195078872732 ) ) ;
#128440=CARTESIAN_POINT ( 'NONE',  ( 2.641296366799699147, -1.384790685969448099, -1.257831364775918503 ) ) ;
#128441=CARTESIAN_POINT ( 'NONE',  ( 0.9971819109757291688, -0.5654680449962052879, -2.237236815885994989 ) ) ;
#128443=CARTESIAN_POINT ( 'NONE',  ( 2.857670863715315424, -0.5868061553097079219, 1.766171933019081042 ) ) ;
#128445=CARTESIAN_POINT ( 'NONE',  ( 6.812941044521420686, -1.596950470092706853, 1.305146078352089845 ) ) ;
#128448=CARTESIAN_POINT ( 'NONE',  ( 6.827182134110199030, -0.004087946457608306570, 2.088967824442849341 ) ) ;
#128450=CARTESIAN_POINT ( 'NONE',  ( 6.134075720976177593, 1.071308383804179476, -1.877395391766012445 ) ) ;
#128451=CARTESIAN_POINT ( 'NONE',  ( 0.03542360567958083295, -0.09470281839311225913, 2.017672626582614814 ) ) ;
#128456=CARTESIAN_POINT ( 'NONE',  ( 6.825078400183554272, 2.980425674467934272, 2.309322343017068402 ) ) ;
#128459=CARTESIAN_POINT ( 'NONE',  ( 5.155482549980198392, 1.942097955248718533, -0.5424665614216088727 ) ) ;
#128464=CARTESIAN_POINT ( 'NONE',  ( 5.928642344448160628, 2.082074431819755045, 0.5810635428650026135 ) ) ;
#128469=CARTESIAN_POINT ( 'NONE',  ( 6.345327396762703742, 0.3419173589993273477, -1.987050850726256979 ) ) ;
#128472=CARTESIAN_POINT ( 'NONE',  ( 1.769703478646069028, 0.8846387809394311574, 1.480598516496567152 ) ) ;
#128476=CARTESIAN_POINT ( 'NONE',  ( 6.309813054293936574, -1.856383540575656799, 0.2289572138471432372 ) ) ;
#128478=CARTESIAN_POINT ( 'NONE',  ( 1.067042177248921364, -1.585704042599777264, 1.240073755948613243 ) ) ;
#128479=CARTESIAN_POINT ( 'NONE',  ( 3.522699392456357881, 1.401646575410384843, -1.704459333586107794 ) ) ;
#128480=CARTESIAN_POINT ( 'NONE',  ( 5.946172770594575496, -0.9833217254726284162, 1.935730195829394429 ) ) ;
#128483=AXIS2_PLACEMENT_3D ( 'NONE', #59875, #93472, #191988 ) ;
#128485=CARTESIAN_POINT ( 'NONE',  ( 2.789816089392273213, 2.012775272720100705, -0.6673941125509493810 ) ) ;
#128486=CARTESIAN_POINT ( 'NONE',  ( 2.935172905452135161, -1.650095542580119812, -1.158671029019647358 ) ) ;
#128487=CARTESIAN_POINT ( 'NONE',  ( 2.689504281738527514, 1.718874962283756691, -0.5722189708131807384 ) ) ;
#128488=ORIENTED_EDGE ( 'NONE', *, *, #103113, .F. ) ;
#128491=CARTESIAN_POINT ( 'NONE',  ( 0.08069323953814251660, -0.1329233695197447052, -1.840450602299897431 ) ) ;
#128494=CARTESIAN_POINT ( 'NONE',  ( 1.217839795352684273, 0.9409426854420616104, -1.668592810110066438 ) ) ;
#128501=CARTESIAN_POINT ( 'NONE',  ( 4.909125497034264818, 1.879091090907711425, 1.068517025386829467 ) ) ;
#128504=CARTESIAN_POINT ( 'NONE',  ( 3.392942708002244068, -2.044739723715986113, -0.5619712599038150236 ) ) ;
#128505=CARTESIAN_POINT ( 'NONE',  ( -0.1296875068448125057, 2.889142263448498227, -2.315371602238533555 ) ) ;
#128507=CARTESIAN_POINT ( 'NONE',  ( 4.675049781410951510, 0.003005680196035282782, -1.971530341645504780 ) ) ;
#128511=CARTESIAN_POINT ( 'NONE',  ( 0.8364851226981102617, -1.151554295457988930, 1.720357586142134076 ) ) ;
#128512=CARTESIAN_POINT ( 'NONE',  ( 2.800647771853786772, 1.640754720439155268, 1.038516083699735582 ) ) ;
#128516=CARTESIAN_POINT ( 'NONE',  ( 2.976600611693449139, -0.1542612496043833104, -2.085005227243463821 ) ) ;
#128519=CARTESIAN_POINT ( 'NONE',  ( 0.8557779741884026237, 0.7350315055517571139, -1.655818919202347361 ) ) ;
#128521=CARTESIAN_POINT ( 'NONE',  ( 4.196070124731249074, -0.8457972711899945928, 2.038567251995755836 ) ) ;
#128522=CARTESIAN_POINT ( 'NONE',  ( 2.678998284833411070, -2.111460168698295004, -0.6414983429729387288 ) ) ;
#128525=CARTESIAN_POINT ( 'NONE',  ( 2.297387027313551044, 1.747684631587187454, -0.7765785915121098393 ) ) ;
#128527=CARTESIAN_POINT ( 'NONE',  ( 4.316890830952234914, -1.536253448065309613, 1.388129241271539138 ) ) ;
#128529=CARTESIAN_POINT ( 'NONE',  ( 2.922914210685311431, 2.035003303901411265, 0.7295308445595325431 ) ) ;
#128530=CARTESIAN_POINT ( 'NONE',  ( 4.441096743985088580, -1.694418930461354611, -1.389946530008886905 ) ) ;
#128537=CARTESIAN_POINT ( 'NONE',  ( 0.3170300144729014669, 1.034162889623980286, -1.730867746391979933 ) ) ;
#128541=CARTESIAN_POINT ( 'NONE',  ( 4.979381509686323426, -0.1069728651886258930, 2.067640925720988232 ) ) ;
#128542=CARTESIAN_POINT ( 'NONE',  ( 2.947785801820240970, 0.6929415146892035082, -1.797737524126517217 ) ) ;
#128543=CARTESIAN_POINT ( 'NONE',  ( 6.099228927766127129, -0.2589519472634767006, 2.101251757753983984 ) ) ;
#128546=CARTESIAN_POINT ( 'NONE',  ( 3.485164662121999601, 0.04367138265829079852, 1.969119211374547707 ) ) ;
#128547=CARTESIAN_POINT ( 'NONE',  ( 6.228533256425053288, 0.2185279184554402288, 2.281841813635554495 ) ) ;
#128548=CARTESIAN_POINT ( 'NONE',  ( 4.424309136736732206, 1.121156565774838354, -1.440799707636587712 ) ) ;
#128555=CARTESIAN_POINT ( 'NONE',  ( 1.979791773625012352, -1.805961398883266344, -0.3578489297004632808 ) ) ;
#128556=CARTESIAN_POINT ( 'NONE',  ( 5.519794446587845016, -0.4848760706452569513, 1.953846845731139759 ) ) ;
#128557=CARTESIAN_POINT ( 'NONE',  ( 0.3339538366646053191, -1.498446967350696379, 1.742810101306817794 ) ) ;
#128558=CARTESIAN_POINT ( 'NONE',  ( 6.034033239799157400, 1.165729394902741189, 1.577711426528668692 ) ) ;
#128564=CARTESIAN_POINT ( 'NONE',  ( 2.050439074220523406, -1.614099552242785895, 1.328842424969446823 ) ) ;
#128565=CARTESIAN_POINT ( 'NONE',  ( 0.1275333129481092398, -1.147091320445620566, -1.478225367208672703 ) ) ;
#128568=CARTESIAN_POINT ( 'NONE',  ( 1.294060738426667134, 1.423250580516822072, -1.001416416642088469 ) ) ;
#128573=CARTESIAN_POINT ( 'NONE',  ( 2.209205535023693212, -0.3792257637574465434, 1.682495413129220907 ) ) ;
#128574=CARTESIAN_POINT ( 'NONE',  ( 1.435386855117400717, -1.590506285900999295, -1.507976327226906443 ) ) ;
#128575=CARTESIAN_POINT ( 'NONE',  ( 4.494872972331320327, -0.4818267175418550208, -2.153482813429814069 ) ) ;
#128577=CARTESIAN_POINT ( 'NONE',  ( 0.8663802385432646247, -2.160743160283730813, 0.2111063225179575509 ) ) ;
#128578=CARTESIAN_POINT ( 'NONE',  ( 0.06470675514189982991, -1.629034059718449834, -0.8243793580787887043 ) ) ;
#128579=CARTESIAN_POINT ( 'NONE',  ( 3.221969581791602977, 0.9480887764680032692, -1.893252576601434756 ) ) ;
#128580=CARTESIAN_POINT ( 'NONE',  ( 6.539320575229234933, 1.301352213286063320, 1.914891792149053140 ) ) ;
#128582=CARTESIAN_POINT ( 'NONE',  ( 4.036908492867667064, -1.994400080153370558, 1.130107982421886481 ) ) ;
#128587=CARTESIAN_POINT ( 'NONE',  ( 5.742908703533418091, 2.140221812536883927, 0.5945068574613203705 ) ) ;
#128593=CARTESIAN_POINT ( 'NONE',  ( 4.289685514112329123, 1.556909497225898109, -1.281360267751927129 ) ) ;
#128595=CARTESIAN_POINT ( 'NONE',  ( 1.903259321421392425, -1.744647275545135212, 1.099889041785537813 ) ) ;
#128600=CARTESIAN_POINT ( 'NONE',  ( 4.839868765920234850, 2.185429510258177110, 0.1630863781024796955 ) ) ;
#128601=CARTESIAN_POINT ( 'NONE',  ( 2.760388869050140137, 1.913803604375517109, -0.6351994527180188088 ) ) ;
#128602=CARTESIAN_POINT ( 'NONE',  ( 1.839159199666509981, 0.7036077657225293658, -1.701706503975081830 ) ) ;
#128605=CARTESIAN_POINT ( 'NONE',  ( 5.666980381186065507, -1.651371415153819688, -0.7785968546244539379 ) ) ;
#128606=CARTESIAN_POINT ( 'NONE',  ( 6.346327303948391396, 0.3419391630616851474, -1.987045965717588958 ) ) ;
#128608=CARTESIAN_POINT ( 'NONE',  ( 6.104402428500737443, -0.8075561382203682026, -2.113670588390024196 ) ) ;
#128610=CARTESIAN_POINT ( 'NONE',  ( 0.5750072486576313091, -1.983761410860336527, -0.7076436626956124076 ) ) ;
#128621=CARTESIAN_POINT ( 'NONE',  ( 1.846092968827160119, -1.388944967848893430, -1.602481653760478020 ) ) ;
#128622=CARTESIAN_POINT ( 'NONE',  ( 2.742673093864269163, 1.230450920196803022, -1.849320754654346866 ) ) ;
#128626=CARTESIAN_POINT ( 'NONE',  ( 3.648837080137564470, -0.3802854374791163616, -1.924481129451253603 ) ) ;
#128633=CARTESIAN_POINT ( 'NONE',  ( 2.777707764728345907, 0.3069055913166895966, -2.098134212408508059 ) ) ;
#128635=CARTESIAN_POINT ( 'NONE',  ( 4.399409362686744096, 1.734418756986338295, 1.290045131933370781 ) ) ;
#128636=CARTESIAN_POINT ( 'NONE',  ( 3.333393596924072444, 0.8250370302015205271, -1.646115572170883334 ) ) ;
#128640=CARTESIAN_POINT ( 'NONE',  ( 6.246048974015395494, 0.5531718476652900396, 1.650163303580793217 ) ) ;
#128645=CARTESIAN_POINT ( 'NONE',  ( 2.975616057669258741, 2.053088362031017855, -0.6768339029224537118 ) ) ;
#128646=CARTESIAN_POINT ( 'NONE',  ( 4.253279712585047001, -1.993766238088546361, -0.2985801555873274227 ) ) ;
#128648=CARTESIAN_POINT ( 'NONE',  ( 2.711983997553393699, -2.138339778157403615, 0.3160903847422363300 ) ) ;
#128649=CARTESIAN_POINT ( 'NONE',  ( 2.776590643643538581, -1.885432240069355503, -0.5755950866291289492 ) ) ;
#128650=CARTESIAN_POINT ( 'NONE',  ( 6.509000000000010999, 0.004788705324892603143, 2.000274819378269786 ) ) ;
#128651=CARTESIAN_POINT ( 'NONE',  ( 4.458499667006603495, -1.736235857128598070, -0.8702183630341918663 ) ) ;
#128660=CARTESIAN_POINT ( 'NONE',  ( 0.9388347430083656686, 2.174419798330699649, 0.3756190385216377492 ) ) ;
#128662=CARTESIAN_POINT ( 'NONE',  ( 5.893401036868160858, -1.775023410133094615, 0.8355650083611900758 ) ) ;
#128666=CARTESIAN_POINT ( 'NONE',  ( 0.07499057489264347731, 7.629137130509110243, -2.555503484197537922 ) ) ;
#128667=CARTESIAN_POINT ( 'NONE',  ( 5.947170714876300224, 0.5300644225827764178, -1.763184533696081857 ) ) ;
#128672=CARTESIAN_POINT ( 'NONE',  ( 6.328397690248316110, -1.000878058022572903, -1.869571840794107986 ) ) ;
#128675=CARTESIAN_POINT ( 'NONE',  ( 0.07516593201271813685, 0.0004601587237540622779, -2.044269526395313452 ) ) ;
#128677=CARTESIAN_POINT ( 'NONE',  ( 1.662329954472214322, -0.6657413170317361129, -1.738099805993092106 ) ) ;
#128678=CARTESIAN_POINT ( 'NONE',  ( 3.140019216317342376, 0.4501627324021878485, 1.785233193441162491 ) ) ;
#128683=CARTESIAN_POINT ( 'NONE',  ( 3.334799921508072806, 2.153101868192684343, 0.4835390122766567433 ) ) ;
#128684=CARTESIAN_POINT ( 'NONE',  ( 5.747450795320371064, -1.778423256021565813, -1.398359773074304480 ) ) ;
#128686=CARTESIAN_POINT ( 'NONE',  ( 5.554893708145399067, 0.3617622393776204204, 1.774916939089685730 ) ) ;
#128687=CARTESIAN_POINT ( 'NONE',  ( 5.946487413881851758, -1.349596479577100272, 1.359900094196204279 ) ) ;
#128689=CARTESIAN_POINT ( 'NONE',  ( 5.981297838379462384, 1.727768277425823396, -0.7175292643646775659 ) ) ;
#128692=CARTESIAN_POINT ( 'NONE',  ( 6.086734230332795370, -0.2636980280019511902, -1.749942407053702409 ) ) ;
#128693=CARTESIAN_POINT ( 'NONE',  ( 0.9894706735516716201, -0.4852629857438545691, 1.957171443305204761 ) ) ;
#128695=CARTESIAN_POINT ( 'NONE',  ( 3.352270206574393008, 2.106257355090755290, -0.0002192025019883553090 ) ) ;
#128700=CARTESIAN_POINT ( 'NONE',  ( 3.023699206349286239, -0.3898671064326043045, 1.981619672226095918 ) ) ;
#128703=CARTESIAN_POINT ( 'NONE',  ( 3.427187520701843404, 0.04928524951339217919, 2.161187641841005647 ) ) ;
#128708=CARTESIAN_POINT ( 'NONE',  ( 1.012457490462664644, 2.168662962709181574, -0.1065306264821704596 ) ) ;
#128712=CARTESIAN_POINT ( 'NONE',  ( 2.525153347276567484, -2.043736813514348771, 0.7916865192442237298 ) ) ;
#128714=CARTESIAN_POINT ( 'NONE',  ( 2.817521562391828827, -0.2228243041610066255, 2.251526839675880520 ) ) ;
#128722=CARTESIAN_POINT ( 'NONE',  ( 3.795971232924668648, -1.767634583600716569, -0.08911788016389800282 ) ) ;
#128724=CARTESIAN_POINT ( 'NONE',  ( 6.821333372217227797, -0.1664864972488830641, 2.170661319153658564 ) ) ;
#128730=CARTESIAN_POINT ( 'NONE',  ( 3.854256360616271415, 0.6726810918341770140, 1.745705178215435582 ) ) ;
#128731=CARTESIAN_POINT ( 'NONE',  ( 3.643477671580112709, 1.873648065284461817, -0.8808079623299628347 ) ) ;
#128735=CARTESIAN_POINT ( 'NONE',  ( 5.998930166150279852, 1.769978137569449883, -1.240765152474863298 ) ) ;
#128737=CARTESIAN_POINT ( 'NONE',  ( 2.998438581075290710, 1.946722116546204306, 0.2428724957088539971 ) ) ;
#128738=CARTESIAN_POINT ( 'NONE',  ( 0.5618747747782488755, 1.677749815653075460, -1.117659098820653174 ) ) ;
#128742=CARTESIAN_POINT ( 'NONE',  ( 0.6845637836509765872, -0.2226890396202323152, -1.857165095135074218 ) ) ;
#128744=CARTESIAN_POINT ( 'NONE',  ( 2.636979257498579088, 1.897111442976556317, 0.6741904779793208569 ) ) ;
#128746=CARTESIAN_POINT ( 'NONE',  ( 1.775175926465226039, 1.840253878465339055, -1.046873989079605050 ) ) ;
#128749=CARTESIAN_POINT ( 'NONE',  ( 3.859880467719906783, -0.6038372105774907350, 1.980330894321411517 ) ) ;
#128751=CARTESIAN_POINT ( 'NONE',  ( 5.384749270845579083, 1.844215719714219492, -0.9846981469126301345 ) ) ;
#128753=CARTESIAN_POINT ( 'NONE',  ( 5.543921259432438298, 0.7380120197021734496, -1.669944898041133552 ) ) ;
#128758=CARTESIAN_POINT ( 'NONE',  ( 6.651417122894856426, -1.768357563224710605, -1.319949637914811458 ) ) ;
#128760=CARTESIAN_POINT ( 'NONE',  ( 5.162724115531083235, 0.5589384127702141658, 1.828758346017298919 ) ) ;
#128768=CARTESIAN_POINT ( 'NONE',  ( 4.657402308249613654, 0.4116239899518738810, -1.824517662812553009 ) ) ;
#128776=CARTESIAN_POINT ( 'NONE',  ( 0.9363041846261275225, -1.098647377812447923, 1.634312829373037568 ) ) ;
#128777=CARTESIAN_POINT ( 'NONE',  ( 2.917592388753763810, -1.356314522985989646, -1.492243612603139979 ) ) ;
#128780=CARTESIAN_POINT ( 'NONE',  ( 3.134921595499224445, -1.932508288125428741, 1.033376004005027715 ) ) ;
#128782=CARTESIAN_POINT ( 'NONE',  ( 6.825078400183556937, 1.282741234726336943, 1.971047034039685952 ) ) ;
#128783=CARTESIAN_POINT ( 'NONE',  ( 0.2329586101569866563, 2.046406029004425253, -2.262590835625963415 ) ) ;
#128788=CARTESIAN_POINT ( 'NONE',  ( 4.985823801847525161, -1.827980399782932697, -0.2200341325891697619 ) ) ;
#128789=CARTESIAN_POINT ( 'NONE',  ( 1.981109662258444537, -1.841391200710382980, -0.8139001868950055396 ) ) ;
#128790=CARTESIAN_POINT ( 'NONE',  ( 3.778943494763619793, -2.265100756353163103, 0.3889815702934427688 ) ) ;
#128791=CARTESIAN_POINT ( 'NONE',  ( -0.02880301295726198432, 7.629137130509075604, -2.873797191217826619 ) ) ;
#128792=CARTESIAN_POINT ( 'NONE',  ( 1.955673630663162132, -0.6329532555123269510, 1.750116298748620958 ) ) ;
#128794=CARTESIAN_POINT ( 'NONE',  ( 5.308822938259078583, -0.4706598425541131947, -1.853433239416848455 ) ) ;
#128797=CARTESIAN_POINT ( 'NONE',  ( 4.317973780707057507, 1.284968578774790426, -1.649195526182813509 ) ) ;
#128798=CARTESIAN_POINT ( 'NONE',  ( 3.344469905398727239, 0.4532862802011444758, 1.814783984445811127 ) ) ;
#128800=CARTESIAN_POINT ( 'NONE',  ( 5.970224376651540155, -1.750504005202535796, -0.5711807346103907612 ) ) ;
#128804=CARTESIAN_POINT ( 'NONE',  ( 5.285687151129126349, 1.162661966624499277, 1.274325963116212934 ) ) ;
#128808=CARTESIAN_POINT ( 'NONE',  ( 6.227749967195368441, 0.7672974224810541477, -1.865044430435198741 ) ) ;
#128809=FILL_AREA_STYLE ('',( #61597 ) ) ;
#128810=CARTESIAN_POINT ( 'NONE',  ( 4.891568528303794849, -1.987603774517988642, 0.8738605845971869623 ) ) ;
#128811=CARTESIAN_POINT ( 'NONE',  ( 4.740742070742828496, 0.3150700179065483719, 1.798135100120237251 ) ) ;
#128812=CARTESIAN_POINT ( 'NONE',  ( 1.621847549879054107, 1.933622029546874010, -0.3300716771732490895 ) ) ;
#128813=CARTESIAN_POINT ( 'NONE',  ( 0.4744016597374626221, -2.101792896462660210, -0.2546084012580717704 ) ) ;
#128817=CARTESIAN_POINT ( 'NONE',  ( 2.860144583491229131, 0.7611018733697445526, -1.979373954265637892 ) ) ;
#128822=CARTESIAN_POINT ( 'NONE',  ( 0.4442981077158770775, -0.9790059121952739973, 1.824179074426744762 ) ) ;
#128823=CARTESIAN_POINT ( 'NONE',  ( 6.983263157960330147, 7.052490050591996962, 2.551961896892048109 ) ) ;
#128825=CARTESIAN_POINT ( 'NONE',  ( 2.456000923045877027, -1.648014358291004733, -1.489564561520567487 ) ) ;
#128827=CARTESIAN_POINT ( 'NONE',  ( 0.9502802867703894485, -2.080962668894706269, -0.9767702978288366200 ) ) ;
#128829=CARTESIAN_POINT ( 'NONE',  ( 5.823111402427982419, -1.862227451873458728, -0.8870778100700682511 ) ) ;
#128833=CARTESIAN_POINT ( 'NONE',  ( 0.1333542156527660338, 0.2446709926765543996, -2.080993637364982884 ) ) ;
#128834=CARTESIAN_POINT ( 'NONE',  ( 5.267088776126935379, 1.772936381825638952, -0.4966186330585887210 ) ) ;
#128837=CARTESIAN_POINT ( 'NONE',  ( 2.010387792931751516, 1.280683741330263858, -1.155484876777863379 ) ) ;
#128838=CARTESIAN_POINT ( 'NONE',  ( 0.9367328597341374463, -1.586666764284098807, 1.244388658875786424 ) ) ;
#128839=CARTESIAN_POINT ( 'NONE',  ( 2.338912275282720277, 0.6088908215152682990, -2.216548965993940801 ) ) ;
#128841=CARTESIAN_POINT ( 'NONE',  ( 2.302381833152538082, -2.261912932826372735, 0.05377845686085034466 ) ) ;
#128842=CARTESIAN_POINT ( 'NONE',  ( 3.615936863914733124, -2.074906038012876763, 0.3600020511305370707 ) ) ;
#128844=CARTESIAN_POINT ( 'NONE',  ( 2.706023412207391843, -0.6731984680253579878, -1.636901589742848051 ) ) ;
#128847=CARTESIAN_POINT ( 'NONE',  ( 5.196947908113320302, 1.872795242347685463, 1.321741379092307600 ) ) ;
#128848=CARTESIAN_POINT ( 'NONE',  ( 4.206863059814883066, -0.3125640686512491384, 1.814249101404527220 ) ) ;
#128853=CARTESIAN_POINT ( 'NONE',  ( 2.531617689938488791, -0.2033970545941807817, 2.110794199748195599 ) ) ;
#128854=CARTESIAN_POINT ( 'NONE',  ( 4.769572470968366673, 1.260305947291120221, 1.792593939366843303 ) ) ;
#128859=CARTESIAN_POINT ( 'NONE',  ( 2.736843622788497132, 0.2362483484473417716, 1.911901653511848931 ) ) ;
#128862=CARTESIAN_POINT ( 'NONE',  ( 6.117454236943913770, 1.763945953808215394, 1.176740244630887222 ) ) ;
#128872=CARTESIAN_POINT ( 'NONE',  ( 2.032363155619838935, -1.554395792557780487, 0.7831100076771575491 ) ) ;
#128874=CARTESIAN_POINT ( 'NONE',  ( 0.6253529088778921885, 0.1960189665039281104, -1.952063659030292220 ) ) ;
#128878=CARTESIAN_POINT ( 'NONE',  ( 6.631704542599726082, -1.407888343591977121, -1.640466528430361670 ) ) ;
#128881=CARTESIAN_POINT ( 'NONE',  ( 5.366167234668930419, 1.061923416652654550, 1.882811416686725359 ) ) ;
#128885=CARTESIAN_POINT ( 'NONE',  ( 0.5615140978009087736, 1.851110617189118734, -0.2680550677405246773 ) ) ;
#128886=CARTESIAN_POINT ( 'NONE',  ( 6.555961055344926791, 1.506409351870329649, -0.8582156258899288348 ) ) ;
#128888=CARTESIAN_POINT ( 'NONE',  ( 3.105210138592546798, -0.4252477525170209605, 2.149737936336936883 ) ) ;
#128889=CARTESIAN_POINT ( 'NONE',  ( 3.557953228543974777, 0.5631008447647236625, -2.237707790512387440 ) ) ;
#128890=CARTESIAN_POINT ( 'NONE',  ( 5.677046966798700467, -0.04615325445976201785, -2.060428132270344381 ) ) ;
#128891=CARTESIAN_POINT ( 'NONE',  ( 1.710778446297245958, -0.2380136870633246249, 1.927241887951787858 ) ) ;
#128894=CARTESIAN_POINT ( 'NONE',  ( 4.553055379497691568, 0.3652949536288411791, 2.088752307168060707 ) ) ;
#128896=CARTESIAN_POINT ( 'NONE',  ( 2.145157927413956944, 0.8647252629472859109, 1.821741647932619390 ) ) ;
#128898=CARTESIAN_POINT ( 'NONE',  ( 4.102700518754747172, -0.6894086160392081108, -2.096397988278507096 ) ) ;
#128899=DIRECTION ( 'NONE',  ( 1.016547956922408957E-15, 1.000000000000000000, -4.622230424712075819E-32 ) ) ;
#128907=CARTESIAN_POINT ( 'NONE',  ( 4.100502863055309533, -0.6448639507273239424, -1.957478828838697504 ) ) ;
#128912=CARTESIAN_POINT ( 'NONE',  ( 2.912765130361310018, -0.5885411476599323732, -1.932001019476004888 ) ) ;
#128917=CARTESIAN_POINT ( 'NONE',  ( 2.922786580453646366, 1.940006684909411971, 0.6957959148722169251 ) ) ;
#128918=CARTESIAN_POINT ( 'NONE',  ( 3.235000160576475992, 2.016597019841442240, -0.002811030766311505089 ) ) ;
#128921=CARTESIAN_POINT ( 'NONE',  ( 3.239470508323912146, 0.4852670486454255250, -1.957170429962351577 ) ) ;
#128925=CARTESIAN_POINT ( 'NONE',  ( 3.022814370378481552, 2.006652721595225675, -0.1948103792988181704 ) ) ;
#128926=CARTESIAN_POINT ( 'NONE',  ( 1.745803608711377075, 0.5764907460206626366, 1.748616612666432868 ) ) ;
#128929=CARTESIAN_POINT ( 'NONE',  ( 6.498651167236064730, -0.5841124237929047336, -2.128106146270396071 ) ) ;
#128931=CARTESIAN_POINT ( 'NONE',  ( 2.161604200734370096, 0.3718190433680613749, -2.129227089361292791 ) ) ;
#128933=CARTESIAN_POINT ( 'NONE',  ( 4.997310516409209313, -0.3076690597460414733, 2.094731796426703152 ) ) ;
#128935=CARTESIAN_POINT ( 'NONE',  ( 1.586564105604048480, -0.2713065988851799393, -1.850747533123621391 ) ) ;
#128937=CARTESIAN_POINT ( 'NONE',  ( 4.909034519618480807, 1.714790629392642707, 0.9726076082038226378 ) ) ;
#128942=CARTESIAN_POINT ( 'NONE',  ( 5.795568699328918605, 1.593732954614892616, 1.376895199011922477 ) ) ;
#128946=CARTESIAN_POINT ( 'NONE',  ( 6.639320575229230137, 7.629137130509035636, 2.603262396134010892 ) ) ;
#128947=CARTESIAN_POINT ( 'NONE',  ( 5.541858398712612654, 0.7996551022716179569, -1.802186847774432943 ) ) ;
#128948=CARTESIAN_POINT ( 'NONE',  ( -0.1049925189658337810, -2.058569791948822392, -0.5088776734372552069 ) ) ;
#128950=CARTESIAN_POINT ( 'NONE',  ( 4.617980755673473325, -2.263821322725892315, 0.4470779566097658475 ) ) ;
#128951=CARTESIAN_POINT ( 'NONE',  ( 2.377848133335142222, -2.001750602163259174, 0.4968105773679451498 ) ) ;
#128958=CARTESIAN_POINT ( 'NONE',  ( 4.299414767360295819, -1.890980460948383790, 1.066717558251949471 ) ) ;
#128961=CARTESIAN_POINT ( 'NONE',  ( 3.579498943475650563, -0.9044721095569520086, 1.603693017070174864 ) ) ;
#128964=CARTESIAN_POINT ( 'NONE',  ( 5.530878137806295669, -1.981686641427220286, 0.9361944923952856268 ) ) ;
#128966=CARTESIAN_POINT ( 'NONE',  ( 6.526273518496622295, 1.309208030111205900, -1.845092234498114658 ) ) ;
#128973=CARTESIAN_POINT ( 'NONE',  ( 0.5843626980001519478, -0.2102794380555508547, -1.757238120818458649 ) ) ;
#128974=CARTESIAN_POINT ( 'NONE',  ( 4.758451920691616266, 2.007841679651333422, 0.1459793341078066131 ) ) ;
#128976=CARTESIAN_POINT ( 'NONE',  ( 4.155375932019107488, -1.749630165425161143, -1.171798067238625229 ) ) ;
#128977=CARTESIAN_POINT ( 'NONE',  ( 1.599098272587581748, -0.2325377738172547115, 1.901345697680896007 ) ) ;
#128979=CARTESIAN_POINT ( 'NONE',  ( 3.666418788940009943, -0.7958718277518551654, -1.801768233320384605 ) ) ;
#128980=CARTESIAN_POINT ( 'NONE',  ( 5.537369811128121988, -0.04535447194144863470, 2.019437878860441238 ) ) ;
#128981=CARTESIAN_POINT ( 'NONE',  ( 2.131529507118444133, -1.219933349377068099, -1.418231869465089057 ) ) ;
#128982=CARTESIAN_POINT ( 'NONE',  ( 1.943732651021431224, 1.350599318427040840, 1.423195245143428433 ) ) ;
#128983=CARTESIAN_POINT ( 'NONE',  ( 4.055083665587292607, -1.435586732866575010, -0.9558459365816800446 ) ) ;
#128984=CARTESIAN_POINT ( 'NONE',  ( 0.9317291061951762376, -1.865162313430932750, 0.4216105838140621342 ) ) ;
#128986=CARTESIAN_POINT ( 'NONE',  ( 0.8915962724085277902, 1.944627461026976034, -1.043433064090833140 ) ) ;
#128990=CARTESIAN_POINT ( 'NONE',  ( 6.772336237553374438, -1.148929780121176414, 1.476827877338216632 ) ) ;
#128994=CARTESIAN_POINT ( 'NONE',  ( 6.842638490404138629, -2.029097751484234546, -0.4099019697717393163 ) ) ;
#128996=CARTESIAN_POINT ( 'NONE',  ( 0.3970419974134197783, 0.3524218036512065111, 2.039982198586967943 ) ) ;
#129001=CARTESIAN_POINT ( 'NONE',  ( 5.988958055669808545, -2.013456733998910231, -0.6654305520411086805 ) ) ;
#129006=CARTESIAN_POINT ( 'NONE',  ( 6.373494408814909917, -0.2414686440028299685, 1.946897059556201848 ) ) ;
#129008=CARTESIAN_POINT ( 'NONE',  ( 3.848982377512806696, -0.9961485462514391154, 1.752762419822328610 ) ) ;
#129009=CARTESIAN_POINT ( 'NONE',  ( 3.327253086410830729, -1.454009962414861912, -1.247479002808443704 ) ) ;
#129011=CARTESIAN_POINT ( 'NONE',  ( 1.593588134247824639, -0.7342643958434189599, 2.065040727587868830 ) ) ;
#129014=CARTESIAN_POINT ( 'NONE',  ( 5.572526294291941795, 0.8198877612898677336, 1.838878804361820274 ) ) ;
#129017=CARTESIAN_POINT ( 'NONE',  ( 6.134383104757832328, 0.6643169034818379171, 2.010352329694592655 ) ) ;
#129020=CARTESIAN_POINT ( 'NONE',  ( 3.017214641935324071, -2.014214092474704731, 0.5601794093188486867 ) ) ;
#129022=CARTESIAN_POINT ( 'NONE',  ( 1.606044756371062920, -0.6162743471601249690, -1.611104689205801188 ) ) ;
#129024=CARTESIAN_POINT ( 'NONE',  ( 5.150683391976684788, 2.089615912265533559, 0.3601871064465370087 ) ) ;
#129035=CARTESIAN_POINT ( 'NONE',  ( 2.015983567491559381, -1.811083833189537806, 0.04518873659950343319 ) ) ;
#129041=CARTESIAN_POINT ( 'NONE',  ( 2.824650661615616620, 1.310593810787925362, -1.250744805450889618 ) ) ;
#129047=CARTESIAN_POINT ( 'NONE',  ( 4.228838981530287811, -1.735973604985484142, -0.6712095357626171044 ) ) ;
#129049=CARTESIAN_POINT ( 'NONE',  ( 1.862754361789496160, -0.09592165986596230820, -1.913344494172765753 ) ) ;
#129050=CARTESIAN_POINT ( 'NONE',  ( 0.2877648253245302379, -0.8656086203641421006, 1.607325130595547602 ) ) ;
#129057=CARTESIAN_POINT ( 'NONE',  ( 4.557443512217212778, 1.579177641033597368, 1.176567834677658908 ) ) ;
#129060=CARTESIAN_POINT ( 'NONE',  ( -0.1399997263889594112, -0.002789056014654289761, -2.000146600338557956 ) ) ;
#129061=CARTESIAN_POINT ( 'NONE',  ( 0.09384556119819162379, -2.090229486699231032, -0.04899896570133810414 ) ) ;
#129063=CARTESIAN_POINT ( 'NONE',  ( 5.280268953417031952, -1.070192140894361099, 1.601580209743416860 ) ) ;
#129066=CARTESIAN_POINT ( 'NONE',  ( 1.676486011727536418, -1.732352342712149440, -0.5761224636358779350 ) ) ;
#129067=CARTESIAN_POINT ( 'NONE',  ( 2.297764732281985633, 1.706874461811638044, 1.398895601573101111 ) ) ;
#129069=CARTESIAN_POINT ( 'NONE',  ( -0.03509584499547176162, -1.534781374734139670, 1.140672443274578729 ) ) ;
#129072=CARTESIAN_POINT ( 'NONE',  ( 0.1507525579465497367, -0.4251589684514142653, -1.929747299214799483 ) ) ;
#129073=CARTESIAN_POINT ( 'NONE',  ( 1.733828471206948496, 1.921180395534723528, 0.2831599317468564969 ) ) ;
#129074=CARTESIAN_POINT ( 'NONE',  ( 1.141953626738337890, -0.04666616626641807014, -2.015725262716171695 ) ) ;
#129076=CARTESIAN_POINT ( 'NONE',  ( 5.787920722453932854, -1.179413039982403433, -1.439513333959110852 ) ) ;
#129082=CARTESIAN_POINT ( 'NONE',  ( 1.909981697816802049, -1.036543071415759298, -1.930953618257096993 ) ) ;
#129086=CARTESIAN_POINT ( 'NONE',  ( 1.506192966688112422, -0.6554880476431452774, -1.704135612709246184 ) ) ;
#129090=CARTESIAN_POINT ( 'NONE',  ( 6.609000000000053276, 6.037706995087852135, 2.494900065673964829 ) ) ;
#129093=CARTESIAN_POINT ( 'NONE',  ( 1.523919215901398783, -1.069746099203742418, -1.602010878309991559 ) ) ;
#129094=CARTESIAN_POINT ( 'NONE',  ( 3.959774770350584561, -0.5736532364168048792, 1.875976257969473648 ) ) ;
#129098=CARTESIAN_POINT ( 'NONE',  ( 4.792620198997869174, 1.822056328612733145, -1.217503271791681163 ) ) ;
#129100=CARTESIAN_POINT ( 'NONE',  ( 3.731357587288412159, 0.05568397596692271218, -2.069689236595618542 ) ) ;
#129104=CARTESIAN_POINT ( 'NONE',  ( 3.868082235913085309, -0.2263641512248204812, -2.287543476887623051 ) ) ;
#129109=CARTESIAN_POINT ( 'NONE',  ( 6.620655732516613767, 2.976578140159558128, 2.379908536877679559 ) ) ;
#129111=CARTESIAN_POINT ( 'NONE',  ( 3.960829289611409898, 0.2367351755836170912, -1.927401316828970979 ) ) ;
#129114=CARTESIAN_POINT ( 'NONE',  ( 5.185773951807310489, 1.841398108398510480, -0.5159224025059682139 ) ) ;
#129116=CARTESIAN_POINT ( 'NONE',  ( 6.686556848510641693, -1.692700875910668312, -0.3300756604382968362 ) ) ;
#129117=CARTESIAN_POINT ( 'NONE',  ( 4.188685576152741064, 1.555700494002542067, -1.282988152656767911 ) ) ;
#129119=CARTESIAN_POINT ( 'NONE',  ( 0.9618826090718561872, 0.4271145061440981272, -2.164990749644220447 ) ) ;
#129122=CARTESIAN_POINT ( 'NONE',  ( 0.04111360010001801485, -1.617408405202691135, -1.324400026677017728 ) ) ;
#129123=CARTESIAN_POINT ( 'NONE',  ( 0.2855648877363594629, -0.8402267237041045611, 1.557686187855854554 ) ) ;
#129124=CARTESIAN_POINT ( 'NONE',  ( 6.029922689959810178, -1.701949372586025744, 1.081063231324945528 ) ) ;
#129126=CARTESIAN_POINT ( 'NONE',  ( 3.275583346405244622, 1.454120551940318418, 1.771997285204220507 ) ) ;
#129127=CARTESIAN_POINT ( 'NONE',  ( 1.499541640181512481, -0.6240335575410212998, -1.624780663456944385 ) ) ;
#129130=CARTESIAN_POINT ( 'NONE',  ( 1.282125424323858898, -1.693001012030776353, 0.3732380902255887367 ) ) ;
#129133=CARTESIAN_POINT ( 'NONE',  ( 1.557326333469456481, 1.775469013113859074, -1.249449068179921518 ) ) ;
#129134=CARTESIAN_POINT ( 'NONE',  ( 2.360564879530482330, -1.931125380751706810, -0.5807522007576990664 ) ) ;
#129135=CARTESIAN_POINT ( 'NONE',  ( 5.437500000000002665, 1.451031289060892737, -1.451031289061332608 ) ) ;
#129137=CARTESIAN_POINT ( 'NONE',  ( 0.2176306489089273599, -1.889907718300526174, 0.3723054783561028369 ) ) ;
#129139=CARTESIAN_POINT ( 'NONE',  ( 3.199698422319953384, 2.006668028495290024, -0.9531968752462171013 ) ) ;
#129140=ORIENTED_EDGE ( 'NONE', *, *, #109079, .F. ) ;
#129146=CARTESIAN_POINT ( 'NONE',  ( 5.214300491592821274, 1.611006010870178251, 0.6591642633846701571 ) ) ;
#129147=CARTESIAN_POINT ( 'NONE',  ( 3.631260574587381829, 0.05062604155347744800, -1.961386756325018021 ) ) ;
#129151=CARTESIAN_POINT ( 'NONE',  ( 4.833442251172010984, -2.071103420340114187, 0.9108926349224757413 ) ) ;
#129153=CARTESIAN_POINT ( 'NONE',  ( 1.645062733043511027, -0.3006328960593112054, -2.040525779345269797 ) ) ;
#129155=CARTESIAN_POINT ( 'NONE',  ( 2.835161494786802461, 0.2760463380651246856, 2.245541603805699005 ) ) ;
#129158=CARTESIAN_POINT ( 'NONE',  ( 3.215925951850879816, -0.9189154559356220719, -1.629173103855706906 ) ) ;
#129159=CARTESIAN_POINT ( 'NONE',  ( 2.056849044198369114, -1.066344721839644460, 1.367450411802049182 ) ) ;
#129160=CARTESIAN_POINT ( 'NONE',  ( 6.023007056224171762, -2.064090639567913499, 0.7368321019862942300 ) ) ;
#129161=CARTESIAN_POINT ( 'NONE',  ( 6.229535257468108433, -2.175718461381468405, 0.7693011637898824473 ) ) ;
#129162=CARTESIAN_POINT ( 'NONE',  ( 4.452137864729129646, 2.161286467946467837, -0.05003489268536746859 ) ) ;
#129163=CARTESIAN_POINT ( 'NONE',  ( 4.734287085814634644, 0.3336016870040105498, 1.912933106389144822 ) ) ;
#129166=CARTESIAN_POINT ( 'NONE',  ( 6.819622122755134797, -1.814287395386984691, 0.4549875680220638596 ) ) ;
#129169=CARTESIAN_POINT ( 'NONE',  ( -0.1341500063891595818, -0.1486117279969369209, -1.983907055413631992 ) ) ;
#129173=CARTESIAN_POINT ( 'NONE',  ( 5.889296118903345700, -0.7283762112263308941, -1.880435897373772258 ) ) ;
#129177=CARTESIAN_POINT ( 'NONE',  ( 3.545350327189537687, -1.383302465072188792, -1.191577590537174158 ) ) ;
#129183=CARTESIAN_POINT ( 'NONE',  ( 0.4397206748869232351, -1.916487937148562137, 0.6377882026268544280 ) ) ;
#129184=CARTESIAN_POINT ( 'NONE',  ( 1.700013272279196963, 1.464590769506744161, 1.533662747278791816 ) ) ;
#129187=CARTESIAN_POINT ( 'NONE',  ( 1.850234720775156605, -1.851392121210411634, -0.1886080954226591611 ) ) ;
#129189=CARTESIAN_POINT ( 'NONE',  ( 6.807514186891733488, -0.4511856701074740683, 2.018123631040650068 ) ) ;
#129190=CARTESIAN_POINT ( 'NONE',  ( 5.906875006520014182, -1.122496024291631755, -1.674889250513518446 ) ) ;
#129192=ORIENTED_EDGE ( 'NONE', *, *, #199481, .T. ) ;
#129195=CARTESIAN_POINT ( 'NONE',  ( 3.738726038629454074, 0.2694068579384528150, 1.805578518607708016 ) ) ;
#129200=CARTESIAN_POINT ( 'NONE',  ( 6.679064532090532857, -0.9478974852125362505, -1.779352858464311016 ) ) ;
#129201=CARTESIAN_POINT ( 'NONE',  ( 5.771403949166884040, 1.100151190403714452, 1.476150860297696932 ) ) ;
#129202=CARTESIAN_POINT ( 'NONE',  ( -0.02319159430949970999, 4.096340798889516854, -2.366022381217198767 ) ) ;
#129203=CARTESIAN_POINT ( 'NONE',  ( 2.983396891919448013, -0.1703749763015352803, -2.301462837838092135 ) ) ;
#129205=CARTESIAN_POINT ( 'NONE',  ( 5.536455037250767930, 2.128579029500421438, 0.3755436860354774420 ) ) ;
#129207=CARTESIAN_POINT ( 'NONE',  ( 1.681094245561355560, 1.340559147886428271, 1.405378567840375403 ) ) ;
#129210=CARTESIAN_POINT ( 'NONE',  ( 5.009243775243890973, 2.291699508649183592, 0.1762380284849179579 ) ) ;
#129213=CARTESIAN_POINT ( 'NONE',  ( 5.084763247618332649, -0.2297073032716222263, -1.856415652357709778 ) ) ;
#129214=CARTESIAN_POINT ( 'NONE',  ( 0.7735182334044669039, 0.3705173918269571431, -1.875978362188877036 ) ) ;
#129218=CARTESIAN_POINT ( 'NONE',  ( 3.686314334879085663, -1.088174899301070253, 1.919869060924610293 ) ) ;
#129219=CARTESIAN_POINT ( 'NONE',  ( 6.883263157960402445, 0.5924656843266817852, 1.899575500811432338 ) ) ;
#129224=CARTESIAN_POINT ( 'NONE',  ( 1.757037784194936725, -1.688679813833958709, -1.016973138862599102 ) ) ;
#129226=CARTESIAN_POINT ( 'NONE',  ( 1.606910496583548786, -0.8321943236449917958, -2.152478949753482862 ) ) ;
#129227=CARTESIAN_POINT ( 'NONE',  ( 2.119516022818414669, 0.3384452847540948550, -1.932298432780136244 ) ) ;
#129228=CARTESIAN_POINT ( 'NONE',  ( 5.840703832811390050, -2.011083492259890360, -0.4572853040550031167 ) ) ;
#129236=CARTESIAN_POINT ( 'NONE',  ( 0.8663802385432646247, -2.160743160283730813, 0.2111063225179575509 ) ) ;
#129241=CARTESIAN_POINT ( 'NONE',  ( 2.899504437521780442, -0.5904213222340527478, 1.774967144274109287 ) ) ;
#129242=CARTESIAN_POINT ( 'NONE',  ( 6.925078400183550364, -0.007619068086212391067, 2.144148427808051594 ) ) ;
#129243=CARTESIAN_POINT ( 'NONE',  ( 0.07735805125222078305, -0.0005418671161615954465, -2.088975025666544472 ) ) ;
#129244=CARTESIAN_POINT ( 'NONE',  ( 6.827182134110233669, 2.063332311267600971, 2.217821918593851027 ) ) ;
#129246=CARTESIAN_POINT ( 'NONE',  ( 2.121601645288184290, -0.4173985973947492711, 1.866012167355892926 ) ) ;
#129248=CARTESIAN_POINT ( 'NONE',  ( 3.748697311245871688, -1.446992627045262214, 1.018796548582428185 ) ) ;
#129249=CARTESIAN_POINT ( 'NONE',  ( 1.699719973799845185, 1.319605273547658220, 1.384218846220357291 ) ) ;
#129253=CARTESIAN_POINT ( 'NONE',  ( 5.712480180419416520, 1.847460191615752700, 0.5061846876120765781 ) ) ;
#129255=CARTESIAN_POINT ( 'NONE',  ( 0.2564123431100414074, -2.069877475643782994, -0.05227228806716639753 ) ) ;
#129257=CARTESIAN_POINT ( 'NONE',  ( 2.250376613284802207, 0.9954810856505689198, -1.872389709364124188 ) ) ;
#129258=CARTESIAN_POINT ( 'NONE',  ( 4.733189744967194024, -1.710186631362722531, 0.7584244158565585092 ) ) ;
#129259=CARTESIAN_POINT ( 'NONE',  ( 1.945663734523142230, 0.6997465788082489757, -1.686465609443507763 ) ) ;
#129261=CARTESIAN_POINT ( 'NONE',  ( 4.916741810085082598, 1.523553907054091328, -1.596827639139485777 ) ) ;
#129264=CARTESIAN_POINT ( 'NONE',  ( 1.346217686498082378, -0.9293675016086970775, 1.841534056632480265 ) ) ;
#129269=CARTESIAN_POINT ( 'NONE',  ( 0.1753634416057498202, 0.7014533214223102053, -2.226873008360684913 ) ) ;
#129271=CARTESIAN_POINT ( 'NONE',  ( 3.842288295254093100, -1.023014542950370975, 1.799900136785845817 ) ) ;
#129273=CARTESIAN_POINT ( 'NONE',  ( 2.688937055384227115, -0.3666181952855402382, -2.130111032054008646 ) ) ;
#129275=CARTESIAN_POINT ( 'NONE',  ( 1.787766293494430725, 1.931992495155916867, -0.5885693585916639270 ) ) ;
#129276=CARTESIAN_POINT ( 'NONE',  ( 6.720655732516647163, -0.007268404184145297979, 2.273772995263834140 ) ) ;
#129281=CARTESIAN_POINT ( 'NONE',  ( 1.305875433988498813, -1.124247956386617009, -1.673852571057245830 ) ) ;
#129282=CARTESIAN_POINT ( 'NONE',  ( 5.513277522340928272, -2.138352208816508782, 0.4792397250529822905 ) ) ;
#129284=CARTESIAN_POINT ( 'NONE',  ( 4.500206361630255003, -0.8965733778899236395, 1.689174240301967389 ) ) ;
#129288=CARTESIAN_POINT ( 'NONE',  ( 2.425407844734633223, -1.496065234337567329, -1.352141214786584777 ) ) ;
#129291=CARTESIAN_POINT ( 'NONE',  ( 5.579022813628022881, -0.04626586813367798007, -1.724316369773688962 ) ) ;
#129292=CARTESIAN_POINT ( 'NONE',  ( -0.1394461523061377994, 7.629137130509062281, -2.880276239818948536 ) ) ;
#129298=CARTESIAN_POINT ( 'NONE',  ( 0.8310238944931707117, -1.948087850137161459, -0.7009411469260096172 ) ) ;
#129300=CARTESIAN_POINT ( 'NONE',  ( 4.582537834466095639, -1.179681096148448738, 1.374793604838970396 ) ) ;
#129303=CARTESIAN_POINT ( 'NONE',  ( 6.322923312362423331, 1.337123347216003788, -1.222299563558794766 ) ) ;
#129306=CARTESIAN_POINT ( 'NONE',  ( 3.011879173929287834, -1.080601074572758558, -1.906429682232862799 ) ) ;
#129308=CARTESIAN_POINT ( 'NONE',  ( 0.1331565106231328843, 0.003911343561965873426, -1.946049565259087455 ) ) ;
#129311=CARTESIAN_POINT ( 'NONE',  ( 5.237857731762096236, 1.913213232725724966, -0.09853679971996709419 ) ) ;
#129319=CARTESIAN_POINT ( 'NONE',  ( 1.674925575805393585, -2.052671086741376882, -0.6780288057936025847 ) ) ;
#129322=CARTESIAN_POINT ( 'NONE',  ( 1.623764174509664260, -1.011042645414115260, -1.519837739365454743 ) ) ;
#129324=CARTESIAN_POINT ( 'NONE',  ( 5.086841682847768276, -0.2248377094848166835, -1.811598703993194670 ) ) ;
#129326=CARTESIAN_POINT ( 'NONE',  ( 2.900541297466651347, -1.884798985816903860, -0.3226963764228693576 ) ) ;
#129328=CARTESIAN_POINT ( 'NONE',  ( 3.473067387030086994, 1.779531822584624834, 0.8443681024216052045 ) ) ;
#129330=CARTESIAN_POINT ( 'NONE',  ( 5.231954969198427285, 1.913977456902911767, 0.3281912247276967398 ) ) ;
#129334=CARTESIAN_POINT ( 'NONE',  ( 5.379186226027963258, -1.918017450862268714, -0.9047448674902383026 ) ) ;
#129336=CARTESIAN_POINT ( 'NONE',  ( 3.193911838225035105, 1.215006091714765368, 1.476655219734591906 ) ) ;
#129339=CARTESIAN_POINT ( 'NONE',  ( 0.2533207856364183552, -1.770817270756098960, 1.316655756711228253 ) ) ;
#129340=CARTESIAN_POINT ( 'NONE',  ( 4.828775420069912450, 1.386532772215205878, -1.459704157296830784 ) ) ;
#129342=CARTESIAN_POINT ( 'NONE',  ( 5.356004772612798170, 1.823420152956479523, -0.09349780940721279243 ) ) ;
#129343=CARTESIAN_POINT ( 'NONE',  ( 1.258353326579707776, -2.070544811992577561, -0.001879966208345739808 ) ) ;
#129347=CARTESIAN_POINT ( 'NONE',  ( 6.825078400183573812, 0.002648415797040087893, 1.855566311045192540 ) ) ;
#129356=CARTESIAN_POINT ( 'NONE',  ( 1.797802452481820135, -1.496673605676283714, -1.430578824989765518 ) ) ;
#129357=CARTESIAN_POINT ( 'NONE',  ( 2.355205625472241771, 0.1007552864207492405, -2.114937101796029673 ) ) ;
#129360=CARTESIAN_POINT ( 'NONE',  ( 0.7429342955292950190, -0.2353911671746557188, -1.955230025236649682 ) ) ;
#129365=CARTESIAN_POINT ( 'NONE',  ( 2.677988851928223557, -1.177355775514120850, 1.966668201240986402 ) ) ;
#129366=CARTESIAN_POINT ( 'NONE',  ( 1.224926655537651676, -0.04696546880481740349, 1.825250005322680780 ) ) ;
#129367=CARTESIAN_POINT ( 'NONE',  ( 2.004032382285144021, -0.8144628449315849394, 1.730399521388835460 ) ) ;
#129370=CARTESIAN_POINT ( 'NONE',  ( 2.039316462420410758, 0.004210374635823382894, 2.013376229890501357 ) ) ;
#129371=CARTESIAN_POINT ( 'NONE',  ( 2.026150138982992566, 1.004015975608811173, 1.685199498757394831 ) ) ;
#129375=CARTESIAN_POINT ( 'NONE',  ( 5.226549702048478352, 0.1529751191454275516, 2.085101625929087099 ) ) ;
#129376=CARTESIAN_POINT ( 'NONE',  ( 3.256490041505883504, -1.340903482672378466, 1.155240514129013407 ) ) ;
#129379=CARTESIAN_POINT ( 'NONE',  ( 6.228533256425053288, 0.2185279184554402288, 2.281841813635554495 ) ) ;
#129380=CARTESIAN_POINT ( 'NONE',  ( 4.558407276396470920, -1.556374654738747587, -0.7788941851257675797 ) ) ;
#129383=CARTESIAN_POINT ( 'NONE',  ( 4.780456778825039166, -1.700172319169111157, 0.3389010404759411621 ) ) ;
#129385=CARTESIAN_POINT ( 'NONE',  ( 4.369693832449129012, -0.3752608539947903665, 2.138364329090262306 ) ) ;
#129387=CARTESIAN_POINT ( 'NONE',  ( 5.841029835422532734, -1.731992920607817288, -1.032484497598872064 ) ) ;
#129388=CARTESIAN_POINT ( 'NONE',  ( 6.250000000000084377, 2.349784478886278158E-12, 2.052068128417940063 ) ) ;
#129390=CARTESIAN_POINT ( 'NONE',  ( 3.575144680771982220, 0.04857402364528973226, -1.925943534667476476 ) ) ;
#129392=CARTESIAN_POINT ( 'NONE',  ( -0.05755013669183139946, -1.372491973113322050, -1.747462644287574030 ) ) ;
#129394=CARTESIAN_POINT ( 'NONE',  ( 6.983263157960410972, 2.978556228996271482, 2.299637001123565838 ) ) ;
#129397=CARTESIAN_POINT ( 'NONE',  ( 1.577126836321657954, -1.567749618368704967, 1.573888218047289067 ) ) ;
#129398=CARTESIAN_POINT ( 'NONE',  ( 6.883263157960391787, -0.001104538646235289417, 1.946037152736757925 ) ) ;
#129402=CARTESIAN_POINT ( 'NONE',  ( 0.0006249722829775038483, -1.976948959267275541, 0.3961041280396286890 ) ) ;
#129404=CARTESIAN_POINT ( 'NONE',  ( 5.107907679073590224, 0.6501100083472023394, -1.957599679411163196 ) ) ;
#129408=CARTESIAN_POINT ( 'NONE',  ( 6.608674649642057197, 1.385883050205028333, -1.256505298338560062 ) ) ;
#129409=CARTESIAN_POINT ( 'NONE',  ( 5.555191991570319843, -1.093772777934084894, 1.345723482730563525 ) ) ;
#129410=CARTESIAN_POINT ( 'NONE',  ( 5.073663595168481422, -0.9608294848038684277, 1.450969404730037660 ) ) ;
#129412=CARTESIAN_POINT ( 'NONE',  ( 2.999882145774832143, -2.289621049425132338, 0.1149546659729560466 ) ) ;
#129414=CARTESIAN_POINT ( 'NONE',  ( 1.323879276782027548, 1.773944146221797524, 0.4926282247687193139 ) ) ;
#129418=CARTESIAN_POINT ( 'NONE',  ( 2.098414945899258033, -0.4839449910110822373, -1.760204267430766301 ) ) ;
#129419=CARTESIAN_POINT ( 'NONE',  ( 2.567029916978436077, -1.034165006014248211, 1.730866473406714068 ) ) ;
#129420=CARTESIAN_POINT ( 'NONE',  ( 1.359612608069910911, 2.158557413232742750, -0.3773744582575569440 ) ) ;
#129422=CARTESIAN_POINT ( 'NONE',  ( 4.700279962202062123, -2.105436441984291029, -0.05427613729028049616 ) ) ;
#129425=CARTESIAN_POINT ( 'NONE',  ( 0.9946828900261883710, 2.039433816042154124, 0.3556643922909968891 ) ) ;
#129428=CARTESIAN_POINT ( 'NONE',  ( 3.176547234745368264, 0.9552152173708803318, 1.893241096743401464 ) ) ;
#129429=CARTESIAN_POINT ( 'NONE',  ( 0.2934164811014350893, 1.426665091747752356, 1.294802382297273180 ) ) ;
#129430=ORIENTED_EDGE ( 'NONE', *, *, #1218, .F. ) ;
#129437=CARTESIAN_POINT ( 'NONE',  ( 6.170199167347634628, 2.114832956739281400, -0.1575216572810705096 ) ) ;
#129438=CARTESIAN_POINT ( 'NONE',  ( 0.8156195060344322290, -0.3088407994138153700, 2.083069475825300110 ) ) ;
#129441=CARTESIAN_POINT ( 'NONE',  ( 5.717585430250381684, 0.3647202891138579539, -1.824662122815931875 ) ) ;
#129448=CARTESIAN_POINT ( 'NONE',  ( 1.926150285298435572, 1.005797860886543660, 1.684270608208485065 ) ) ;
#129449=CARTESIAN_POINT ( 'NONE',  ( 0.9717996764858798375, 2.083101276202529384, -0.5774176476955604764 ) ) ;
#129453=CARTESIAN_POINT ( 'NONE',  ( 3.110371403566422277, 0.6269696901312575843, -1.616694140604297614 ) ) ;
#129454=CARTESIAN_POINT ( 'NONE',  ( 2.308218407481243961, 1.554217257889878301, 0.7831649204469055547 ) ) ;
#129457=CARTESIAN_POINT ( 'NONE',  ( 1.985689569138231914, 1.418919563317089017, 1.494737215543304965 ) ) ;
#129458=CARTESIAN_POINT ( 'NONE',  ( 1.405624810022429561, 0.3905361843517705100, 1.977748161624798939 ) ) ;
#129461=CARTESIAN_POINT ( 'NONE',  ( 1.498834128701274748, 1.612947343535120925, -1.133365233443942355 ) ) ;
#129462=CARTESIAN_POINT ( 'NONE',  ( 5.941656858135131891, -1.798430535887390658, 0.6506349336675710804 ) ) ;
#129468=CARTESIAN_POINT ( 'NONE',  ( 1.295575897195440307, 1.865243415117883385, -0.7750591016795584931 ) ) ;
#129471=CARTESIAN_POINT ( 'NONE',  ( 4.612551310933718618, -0.9822873175598394457, -2.088206479280288796 ) ) ;
#129472=CARTESIAN_POINT ( 'NONE',  ( 5.934033239752055877, 1.167398200610193282, 1.576599764842034457 ) ) ;
#129473=CARTESIAN_POINT ( 'NONE',  ( 1.780054392102415672, -1.085390340960286082, -1.633940563308281968 ) ) ;
#129477=CARTESIAN_POINT ( 'NONE',  ( 1.147838861943322630, 2.084982156806517661, -0.3680304603586990742 ) ) ;
#129480=CARTESIAN_POINT ( 'NONE',  ( 0.8316833483592298570, 1.813467871694788069, 0.3170515863319539052 ) ) ;
#129482=CARTESIAN_POINT ( 'NONE',  ( 4.504835797669192843, 0.5730007755406724135, 2.094059341655955198 ) ) ;
#129484=CARTESIAN_POINT ( 'NONE',  ( 1.635180430577408028, 1.980530345366804834, 0.7584260845197098311 ) ) ;
#129488=CARTESIAN_POINT ( 'NONE',  ( 3.005207323352117488, 1.739114039596071803, 1.105284290502930089 ) ) ;
#129490=CARTESIAN_POINT ( 'NONE',  ( 0.8020088176248600931, 1.394402496181508466, -1.202495849378336423 ) ) ;
#129492=CARTESIAN_POINT ( 'NONE',  ( -0.02264175331117677936, 4.084751018978694859, -2.643765695431527174 ) ) ;
#129494=CARTESIAN_POINT ( 'NONE',  ( 0.2060869173217265982, -0.5842117877600698783, 2.128085570573131413 ) ) ;
#129495=CARTESIAN_POINT ( 'NONE',  ( 2.126610404160976575, 1.303795175273964269, -1.848758590024823123 ) ) ;
#129497=CARTESIAN_POINT ( 'NONE',  ( 2.619172825086816037, 1.532478635541080214, 0.9657477217557136617 ) ) ;
#129498=CARTESIAN_POINT ( 'NONE',  ( 1.956118367686721538, -1.175378340988470827, 1.512710158094223933 ) ) ;
#129499=CARTESIAN_POINT ( 'NONE',  ( 3.367693471486675083, -0.4065805204805824635, 2.029877954327436118 ) ) ;
#129501=CARTESIAN_POINT ( 'NONE',  ( 1.428526753364509627, 1.899469058273341338, 0.5276583995704342556 ) ) ;
#129502=CARTESIAN_POINT ( 'NONE',  ( 0.2176306489089273599, -1.889907718300526174, 0.3723054783561028369 ) ) ;
#129503=CARTESIAN_POINT ( 'NONE',  ( 2.588565208901713266, -0.3177388942022137397, -1.843305967786903032 ) ) ;
#129504=CARTESIAN_POINT ( 'NONE',  ( 1.120229914364691659, -2.250463172007353130, 0.5101417434775123994 ) ) ;
#129506=CARTESIAN_POINT ( 'NONE',  ( 2.980726927023560346, 1.751358449955683350, 0.6298351686941299210 ) ) ;
#129508=CARTESIAN_POINT ( 'NONE',  ( 5.406706549104464798, 0.5953045380993631230, 1.974924460807401028 ) ) ;
#129513=CARTESIAN_POINT ( 'NONE',  ( 6.704139028598911310, -2.105588161048920437, 0.04759252156865538541 ) ) ;
#129515=CARTESIAN_POINT ( 'NONE',  ( 5.466167184710096549, 1.060119519021487378, 1.883692621652333532 ) ) ;
#129516=CARTESIAN_POINT ( 'NONE',  ( 0.05299788485858129838, 0.3494575625802974206, 1.989167885679890002 ) ) ;
#129523=CARTESIAN_POINT ( 'NONE',  ( 5.260953973667149342, -0.05432152012316109058, -2.015980820358989511 ) ) ;
#129528=CARTESIAN_POINT ( 'NONE',  ( 5.911032513020411550, 1.904272706209766630, 1.023102869888978583 ) ) ;
#129533=CARTESIAN_POINT ( 'NONE',  ( 5.747672784407955149, 1.986098415631059932, -0.3474865836668520336 ) ) ;
#129535=CARTESIAN_POINT ( 'NONE',  ( 2.174029202910219283, -1.062355927555928226, 1.358808029953484597 ) ) ;
#129540=CARTESIAN_POINT ( 'NONE',  ( 6.186763334926775215, -0.2743023915687745617, -1.850177433978140051 ) ) ;
#129541=CARTESIAN_POINT ( 'NONE',  ( 0.7330649400898289203, 1.860844449999502492, 0.7684416140155255759 ) ) ;
#129542=CARTESIAN_POINT ( 'NONE',  ( 3.012930935654754450, 1.599341701681813444, -1.520756135150652222 ) ) ;
#129543=CARTESIAN_POINT ( 'NONE',  ( 5.577072259002747501, 2.003115288890752410, 0.8377749483753393900 ) ) ;
#129547=CARTESIAN_POINT ( 'NONE',  ( 3.123802294713691641, -0.4116375371931815796, 2.079978743196985391 ) ) ;
#129548=CARTESIAN_POINT ( 'NONE',  ( 1.827750133516142128, 0.7691037069590834774, -1.864176919362303675 ) ) ;
#129549=CARTESIAN_POINT ( 'NONE',  ( 2.425776345151516633, -1.791340243523626974, 0.2692766639123735373 ) ) ;
#129554=CARTESIAN_POINT ( 'NONE',  ( 1.323292448300671165, -1.390094005022534773, -1.318457861805687914 ) ) ;
#129560=CARTESIAN_POINT ( 'NONE',  ( 5.524359596833869013, 1.291058806671550485, -1.733668313432787711 ) ) ;
#129563=CARTESIAN_POINT ( 'NONE',  ( 2.320699612028754188, -0.8158636990020677882, -1.957571985684476212 ) ) ;
#129567=CARTESIAN_POINT ( 'NONE',  ( 3.567610853275906546, 1.924076846980572464, -0.4285291244595054727 ) ) ;
#129568=CARTESIAN_POINT ( 'NONE',  ( 5.888906298306328502, -1.818048641159516476, -0.5935555146628914702 ) ) ;
#129571=CARTESIAN_POINT ( 'NONE',  ( 0.6782873735513493818, -1.106163567672680204, -1.749894625276714688 ) ) ;
#129572=CARTESIAN_POINT ( 'NONE',  ( 2.396341059777199689, 1.559625748545325319, -1.156842939599848741 ) ) ;
#129577=CARTESIAN_POINT ( 'NONE',  ( 2.906283313408718705, 1.513773858955402618, -1.442204806208322809 ) ) ;
#129580=CARTESIAN_POINT ( 'NONE',  ( 6.059226159983991167, -1.612925389857391645, 1.026989893868179404 ) ) ;
#129582=CARTESIAN_POINT ( 'NONE',  ( 4.494872972331320327, -0.4818267175418550208, -2.153482813429814069 ) ) ;
#129584=CARTESIAN_POINT ( 'NONE',  ( 2.872332416675418276, 1.179501869419818494, 1.864919306664609921 ) ) ;
#129585=CARTESIAN_POINT ( 'NONE',  ( 1.664566505720616929, 0.6010121217654046388, 1.815428919054395518 ) ) ;
#129588=CARTESIAN_POINT ( 'NONE',  ( 4.615722581382986967, 0.4567890626981512270, -2.019179087418949692 ) ) ;
#129590=CARTESIAN_POINT ( 'NONE',  ( 1.534274790466340299, 1.065227450066742687, -1.880959520452238465 ) ) ;
#129591=CARTESIAN_POINT ( 'NONE',  ( 4.792620198997869174, 1.822056328612733145, -1.217503271791681163 ) ) ;
#129601=CARTESIAN_POINT ( 'NONE',  ( -0.06968618116158857567, -1.560424145883563929, -1.276814929289785239 ) ) ;
#129603=CARTESIAN_POINT ( 'NONE',  ( 4.680570891794395116, 1.277791010243028991, -1.628752506732597638 ) ) ;
#129604=CARTESIAN_POINT ( 'NONE',  ( 3.545458749278436184, -1.459459766114965973, -1.257631776117454914 ) ) ;
#129605=CARTESIAN_POINT ( 'NONE',  ( 5.958642064211575828, -2.010625215935774257, -0.6636248059145292144 ) ) ;
#129609=CARTESIAN_POINT ( 'NONE',  ( 4.135575292396717728, 1.855891543885644479, -0.6595280497384666818 ) ) ;
#129610=CARTESIAN_POINT ( 'NONE',  ( 5.876963737413220201, 2.120050906709324501, -0.8721662429640556491 ) ) ;
#129611=CARTESIAN_POINT ( 'NONE',  ( 3.527797039230845311, -1.088449851438414218, -1.465592618984489670 ) ) ;
#129617=CARTESIAN_POINT ( 'NONE',  ( 1.012948470060770934, -1.796336717620912626, 0.4034172393945419377 ) ) ;
#129618=CARTESIAN_POINT ( 'NONE',  ( 5.467046525086633579, -1.584481552701553220, 1.241800460852604759 ) ) ;
#129620=CARTESIAN_POINT ( 'NONE',  ( 5.748750450937779810, 2.265299150918558269, -0.3897391249057541862 ) ) ;
#129621=CARTESIAN_POINT ( 'NONE',  ( 5.313317156408340125, -1.655227327604656740, -1.052681782574490743 ) ) ;
#129626=CARTESIAN_POINT ( 'NONE',  ( 1.698888801382715252, 1.740066399362389271, 1.158727311120285819 ) ) ;
#129627=CARTESIAN_POINT ( 'NONE',  ( 0.1099206271272800961, -0.7955684105149689600, -1.691499381818922343 ) ) ;
#129628=CARTESIAN_POINT ( 'NONE',  ( 5.929623787841700633, 0.9553189508899215809, -1.690649115374833311 ) ) ;
#129629=CARTESIAN_POINT ( 'NONE',  ( -0.1106727585416019261, 4.087503477334416324, -2.558207815289376796 ) ) ;
#129630=CARTESIAN_POINT ( 'NONE',  ( 0.4326491639514402077, -1.228936893156933330, -1.232681022120321934 ) ) ;
#129634=CARTESIAN_POINT ( 'NONE',  ( 1.470901328764297800, 0.1297424413324743397, -1.720050270840302487 ) ) ;
#129636=CARTESIAN_POINT ( 'NONE',  ( 2.033021410476544943, -1.955939774129427988, 0.9887309579383956049 ) ) ;
#129637=CARTESIAN_POINT ( 'NONE',  ( 3.809358915828209735, 1.892446193107431451, 1.135094405146239049 ) ) ;
#129640=CARTESIAN_POINT ( 'NONE',  ( 1.692468234204123734, 1.072632775294654062, -1.887553939074837261 ) ) ;
#129642=CARTESIAN_POINT ( 'NONE',  ( 2.061849949441786123, 1.306762352624482038, 1.665877332585569803 ) ) ;
#129646=CARTESIAN_POINT ( 'NONE',  ( 2.367065275503206667, 0.1088462660112088087, -2.289894902259086429 ) ) ;
#129650=CARTESIAN_POINT ( 'NONE',  ( 6.287741706623968696, 2.126563164181693555, -0.6417273904879957636 ) ) ;
#129657=CARTESIAN_POINT ( 'NONE',  ( 3.024064729735044921, -1.777011313454954999, 0.9530116517338580451 ) ) ;
#129659=CARTESIAN_POINT ( 'NONE',  ( 2.184505357994303232, 1.191016756910455943, -1.683754781088636632 ) ) ;
#129663=CARTESIAN_POINT ( 'NONE',  ( 5.015667846030231303, -1.170523448010954315, -1.852474865436819274 ) ) ;
#129664=CARTESIAN_POINT ( 'NONE',  ( 2.971327447312217984, -1.987046587055636637, -0.3419355124290662240 ) ) ;
#129665=CARTESIAN_POINT ( 'NONE',  ( 2.595044651933966495, -0.5755060336137384214, 1.749081985381637061 ) ) ;
#129670=CARTESIAN_POINT ( 'NONE',  ( 5.737271026523679041, -1.649412122839075234, 0.7826820710771440481 ) ) ;
#129671=CARTESIAN_POINT ( 'NONE',  ( 6.592432824109000222, -0.4393352932590722792, 1.975308225066509049 ) ) ;
#129673=CARTESIAN_POINT ( 'NONE',  ( 5.172873261720807747, -2.128565284095069288, -0.7672878325792488186 ) ) ;
#129675=CARTESIAN_POINT ( 'NONE',  ( 1.084755975048516285, -2.055113062490296016, -0.4597243831155339300 ) ) ;
#129686=CARTESIAN_POINT ( 'NONE',  ( 1.916421503514931679, -2.120014230100770725, 0.05699577502370903326 ) ) ;
#129687=CARTESIAN_POINT ( 'NONE',  ( 2.848112528106065078, -1.494902295879830589, -1.643281164644925907 ) ) ;
#129691=CARTESIAN_POINT ( 'NONE',  ( 2.892962425504439050, 0.2373818416543191367, 1.947367909387688112 ) ) ;
#129698=CARTESIAN_POINT ( 'NONE',  ( 2.601940685209406467, 1.502730264585940168, 1.496503045097858919 ) ) ;
#129700=CARTESIAN_POINT ( 'NONE',  ( 4.100566281481184738, -0.6756360485904688851, -2.053482476349233643 ) ) ;
#129701=CARTESIAN_POINT ( 'NONE',  ( 2.981803241483144795, -1.814435276338403735, -0.3121031562058202424 ) ) ;
#129704=CARTESIAN_POINT ( 'NONE',  ( 5.542807930227759527, -1.375536301258666105, -1.066015508636003251 ) ) ;
#129705=CARTESIAN_POINT ( 'NONE',  ( 6.727182134110231360, 6.039168392632435989, 2.405853653942995773 ) ) ;
#129708=CARTESIAN_POINT ( 'NONE',  ( 2.676834871759771417, -2.068302492614528365, -0.6285112194897370941 ) ) ;
#129709=CARTESIAN_POINT ( 'NONE',  ( 4.200545946899570282, -1.388273439763810790, -1.462221600879671790 ) ) ;
#129711=CARTESIAN_POINT ( 'NONE',  ( 2.764712544972968811, -1.491509591961351910, 1.564943835847030229 ) ) ;
#129712=CARTESIAN_POINT ( 'NONE',  ( 3.057844483195955032, 1.962173284599289858, -0.1898399627659839439 ) ) ;
#129714=CARTESIAN_POINT ( 'NONE',  ( 4.968278857500742163, -1.829972417919925265, -0.6506317318197059052 ) ) ;
#129724=CARTESIAN_POINT ( 'NONE',  ( 1.448561363430532989, 2.204290700723564811, 0.1073905156721635390 ) ) ;
#129726=CARTESIAN_POINT ( 'NONE',  ( 4.750807836863311095, -0.4258335417525476729, -1.914832529679215023 ) ) ;
#129731=CARTESIAN_POINT ( 'NONE',  ( 3.943160212656390051, 0.6185462545997170158, -1.734258544408360248 ) ) ;
#129737=CARTESIAN_POINT ( 'NONE',  ( 5.924112389714110805, -2.104401743431310923, 0.2612745606217213856 ) ) ;
#129740=CARTESIAN_POINT ( 'NONE',  ( 6.432896526414161542, 0.1972406338010060101, 2.051297006214629182 ) ) ;
#129742=CARTESIAN_POINT ( 'NONE',  ( 2.453354322281832811, 1.436274109216955752, 1.183453651933939588 ) ) ;
#129743=CARTESIAN_POINT ( 'NONE',  ( 3.983814121021773680, -1.821778379405362136, -0.2661574599523569007 ) ) ;
#129748=CARTESIAN_POINT ( 'NONE',  ( 3.739080281021701868, 0.3231575147602770426, 2.182976880621155136 ) ) ;
#129749=CARTESIAN_POINT ( 'NONE',  ( 5.712299329104530088, -1.009927678917849736, -2.024548151048012556 ) ) ;
#129751=CARTESIAN_POINT ( 'NONE',  ( 5.976795019380008789, -1.274598912183276589, 1.287626877918945922 ) ) ;
#129752=CARTESIAN_POINT ( 'NONE',  ( 5.753135696777640362, 0.1336808224800915823, -1.911095040969860825 ) ) ;
#129754=CARTESIAN_POINT ( 'NONE',  ( 6.561405567229332547, 0.3174558530528898692, -1.843364171016811603 ) ) ;
#129755=CARTESIAN_POINT ( 'NONE',  ( 5.793359732304666387, -1.682316520808274429, 0.7960761923023454978 ) ) ;
#129758=CARTESIAN_POINT ( 'NONE',  ( 6.819227944281511355, -0.1297537616256147774, 1.740395163524804945 ) ) ;
#129759=CARTESIAN_POINT ( 'NONE',  ( 1.604704241733472037, 1.883313803065278513, 0.7212895827233902768 ) ) ;
#129761=CARTESIAN_POINT ( 'NONE',  ( 2.578859754595532294, -2.015555182639038101, -0.6107849380157669428 ) ) ;
#129767=CARTESIAN_POINT ( 'NONE',  ( 2.935811755974365500, -1.945362344549756539, 0.5428778075214285570 ) ) ;
#129770=CARTESIAN_POINT ( 'NONE',  ( 3.655696586050953378, 0.5291108212043382775, -2.095698868369605616 ) ) ;
#129775=CARTESIAN_POINT ( 'NONE',  ( 0.7136160920222310855, -1.834322530278935215, -1.161324927271490060 ) ) ;
#129780=CARTESIAN_POINT ( 'NONE',  ( 2.120887600855193345, 0.003649250790785373531, 2.191739723551556551 ) ) ;
#129782=CARTESIAN_POINT ( 'NONE',  ( 2.483610925836767791, 2.068663895631245531, -0.9166773448976636152 ) ) ;
#129789=CARTESIAN_POINT ( 'NONE',  ( 2.987294507434365087, 1.248747198882380394, 1.254300180652974550 ) ) ;
#129792=CARTESIAN_POINT ( 'NONE',  ( 6.756857042228312515, -1.710155547305733492, 1.394389531264042414 ) ) ;
#129796=CARTESIAN_POINT ( 'NONE',  ( 5.519157712072518152, -1.821736412749059397, 0.8647389720048551665 ) ) ;
#129797=CARTESIAN_POINT ( 'NONE',  ( 4.886864132303106345, -1.708302746381512804, -0.6034029335190493892 ) ) ;
#129799=CARTESIAN_POINT ( 'NONE',  ( 3.520239479114235959, 1.187513476551487424, -1.445374034619355985 ) ) ;
#129800=CARTESIAN_POINT ( 'NONE',  ( 3.467693386974544545, -0.4085244671708112008, 2.029378838279243258 ) ) ;
#129807=CARTESIAN_POINT ( 'NONE',  ( 1.248149539447914513, 0.9399939672071170316, -1.665319807275446928 ) ) ;
#129808=CARTESIAN_POINT ( 'NONE',  ( 3.191801227909254912, -1.315628469008291557, -1.455533501494077342 ) ) ;
#129809=CARTESIAN_POINT ( 'NONE',  ( 0.7728142736522191081, -2.006652962095498260, 0.1948079406639269262 ) ) ;
#129812=CARTESIAN_POINT ( 'NONE',  ( 6.257099195183372764, -1.689481296825417811, -1.015638971094455556 ) ) ;
#129814=CARTESIAN_POINT ( 'NONE',  ( 2.092043371607322566, 1.241737408274107501, 1.584530653180368009 ) ) ;
#129816=CARTESIAN_POINT ( 'NONE',  ( 2.706785462534053277, 1.994624666228937526, 0.7104243659002054123 ) ) ;
#129818=CARTESIAN_POINT ( 'NONE',  ( 3.350112325975619587, -0.8415805752714689003, 1.891790567983504312 ) ) ;
#129820=CARTESIAN_POINT ( 'NONE',  ( 5.876921326125680523, 1.932075295558054240, -0.7991432938223922422 ) ) ;
#129822=CARTESIAN_POINT ( 'NONE',  ( 4.752862199841776381, -1.465721779273346792, 1.088108411805274622 ) ) ;
#129829=CARTESIAN_POINT ( 'NONE',  ( 5.197880135092803222, 1.287283252470315720, 1.414272151883423589 ) ) ;
#129835=CARTESIAN_POINT ( 'NONE',  ( 0.3449248370967008537, 0.5783895242766275979, -1.748133987124582012 ) ) ;
#129839=CARTESIAN_POINT ( 'NONE',  ( 4.481629103029507455, 1.220264704679861811, 1.417821649906551906 ) ) ;
#129840=CARTESIAN_POINT ( 'NONE',  ( -0.02319159430947542733, 0.7471999394491578572, -1.895068635927643630 ) ) ;
#129846=CARTESIAN_POINT ( 'NONE',  ( 1.270285106180467416, -0.8805531663822261379, -1.761673308874162069 ) ) ;
#129847=CARTESIAN_POINT ( 'NONE',  ( 2.442982655898734645, -1.755780842375562312, -0.9913809985205720432 ) ) ;
#129851=CARTESIAN_POINT ( 'NONE',  ( 1.992365796559266267, -0.5863786240636535974, -2.111471653062434672 ) ) ;
#129862=CARTESIAN_POINT ( 'NONE',  ( 4.739718475747470627, 1.836682745182907972, 0.1304020654292817605 ) ) ;
#129863=CARTESIAN_POINT ( 'NONE',  ( 1.488932678171340118, -1.912290114023627252, -0.6292827167945020950 ) ) ;
#129864=CARTESIAN_POINT ( 'NONE',  ( 3.058317229773829471, 1.972480788633700577, -1.179572646267361025 ) ) ;
#129866=CARTESIAN_POINT ( 'NONE',  ( 2.184208379282841950, 1.076359544750982389, -1.517863362848305808 ) ) ;
#129869=CARTESIAN_POINT ( 'NONE',  ( 5.484596585704371918, -1.208295678440996390, 1.482354609825987435 ) ) ;
#129873=CARTESIAN_POINT ( 'NONE',  ( 5.319903205935248458, 1.244510898466891780, -1.679860476595731233 ) ) ;
#129874=CARTESIAN_POINT ( 'NONE',  ( 3.449935675575486638, 1.870836310073907827, 0.001118452434160921221 ) ) ;
#129876=CARTESIAN_POINT ( 'NONE',  ( 6.233933901472759942, 1.822226914158030286, 0.2631550708301691466 ) ) ;
#129879=CARTESIAN_POINT ( 'NONE',  ( 5.021954727502539129, -0.9268850835505036967, -1.454474922752227339 ) ) ;
#129881=CARTESIAN_POINT ( 'NONE',  ( 0.4922575064417636925, -1.726078246012904938, 0.1672019070194027679 ) ) ;
#129884=CARTESIAN_POINT ( 'NONE',  ( 5.102462520977921301, 2.164757797245045357, 0.1666947352320021780 ) ) ;
#129885=CARTESIAN_POINT ( 'NONE',  ( 3.492628380820805400, -0.3572889717703279788, -1.790209119249221548 ) ) ;
#129886=CARTESIAN_POINT ( 'NONE',  ( 1.305434336737832490, -1.543085766649286317, -1.211208057394968618 ) ) ;
#129887=CARTESIAN_POINT ( 'NONE',  ( 0.1756132116073009508, 1.572246328413629435, 1.418195661691145304 ) ) ;
#129888=CARTESIAN_POINT ( 'NONE',  ( 0.6918693526153978368, -0.8198495674218098106, 2.140808456117601732 ) ) ;
#129892=CARTESIAN_POINT ( 'NONE',  ( 2.280079029133400326, 2.079044457705871096, -0.4163345062310334632 ) ) ;
#129896=CARTESIAN_POINT ( 'NONE',  ( 6.977413708759169886, -0.1587332643391472231, 2.136494379638858909 ) ) ;
#129897=CARTESIAN_POINT ( 'NONE',  ( 6.983263157960349687, 0.5706719223780298833, 2.105707282093812083 ) ) ;
#129900=CARTESIAN_POINT ( 'NONE',  ( 1.998975601324129769, -2.179183720934555701, -0.4297205562568666148 ) ) ;
#129902=CARTESIAN_POINT ( 'NONE',  ( 0.4230186368967851496, -1.631317381931682631, -1.619748931356496113 ) ) ;
#129904=CARTESIAN_POINT ( 'NONE',  ( 5.787952559958898568, -1.304071791706362449, -1.598039198280821749 ) ) ;
#129910=CARTESIAN_POINT ( 'NONE',  ( 5.372543328820884589, -0.05112055865702340440, -1.840719716649619198 ) ) ;
#129914=CARTESIAN_POINT ( 'NONE',  ( 2.238867094643140376, -1.542287835237671212, 0.7722583484809567578 ) ) ;
#129915=CARTESIAN_POINT ( 'NONE',  ( 1.499232818411553536, -0.2420282084563407654, 2.001858358113464575 ) ) ;
#129916=CARTESIAN_POINT ( 'NONE',  ( 2.180727191476996563, 1.779927251244978192, 1.454631630963822309 ) ) ;
#129918=CARTESIAN_POINT ( 'NONE',  ( 1.950798113461976735, 0.7085273209575352338, 2.148688966898488761 ) ) ;
#129919=CARTESIAN_POINT ( 'NONE',  ( 4.266313661023513504, 0.9922932564179194337, 1.857654695958657953 ) ) ;
#129921=CARTESIAN_POINT ( 'NONE',  ( 2.266550661271060640, -1.615954428537921483, -0.7220204016161780869 ) ) ;
#129926=CARTESIAN_POINT ( 'NONE',  ( 6.064703480017706205, 0.6958612881963457397, 2.109637055116654558 ) ) ;
#129927=CARTESIAN_POINT ( 'NONE',  ( 3.275498427308475069, 1.390425696708731396, 1.693851754907250928 ) ) ;
#129930=CARTESIAN_POINT ( 'NONE',  ( 6.569000932001921811, -1.639521903533578850, 1.344440124909966450 ) ) ;
#129935=CARTESIAN_POINT ( 'NONE',  ( 5.730757696090861941, 1.422813033107739988, -1.572628729999878905 ) ) ;
#129940=CARTESIAN_POINT ( 'NONE',  ( 6.251489360189885325, 1.835807759842246423, -0.1425652098738516838 ) ) ;
#129944=CARTESIAN_POINT ( 'NONE',  ( 2.296107463031165086, 1.396982486531380463, -1.037807123096459838 ) ) ;
#129949=CARTESIAN_POINT ( 'NONE',  ( 6.227428301493934448, -2.037140905555033576, 0.7235935974677574212 ) ) ;
#129953=CARTESIAN_POINT ( 'NONE',  ( 5.963787895669664607, 2.130530397400759668, -0.3648857593604309391 ) ) ;
#129957=CARTESIAN_POINT ( 'NONE',  ( 5.729747329291909885, -1.248464225167019714, -1.525673545143470200 ) ) ;
#129958=CARTESIAN_POINT ( 'NONE',  ( 5.395702507230883072, 0.1292110896585068891, 1.729053200853872596 ) ) ;
#129960=CARTESIAN_POINT ( 'NONE',  ( 2.103317784989285677, -0.4765762082987561321, 2.138964651187735821 ) ) ;
#129961=CARTESIAN_POINT ( 'NONE',  ( 3.487651025411703021, 2.087124329425969371, -0.9845696281253720761 ) ) ;
#129962=CARTESIAN_POINT ( 'NONE',  ( 6.345006307232072373, -1.743395995315766056, 1.098490678494741912 ) ) ;
#129963=CARTESIAN_POINT ( 'NONE',  ( 1.745936028080337765, 0.6089015219087092756, 1.844080840262368071 ) ) ;
#129969=CARTESIAN_POINT ( 'NONE',  ( 3.480829117359967917, -1.421471314662653196, 1.573842340227212366 ) ) ;
#129971=CARTESIAN_POINT ( 'NONE',  ( 1.951796282902381163, -1.844710420878793444, -0.8146254186931353169 ) ) ;
#129973=CARTESIAN_POINT ( 'NONE',  ( 4.506973327934083784, 1.708129512224244806, -1.397202154207459524 ) ) ;
#129976=CARTESIAN_POINT ( 'NONE',  ( -0.01727558406095473439, -0.1313277740116538805, -1.795991579427682616 ) ) ;
#129982=CARTESIAN_POINT ( 'NONE',  ( 4.346593572148568896, 0.5479209435249388083, 1.986652789453833057 ) ) ;
#129988=CARTESIAN_POINT ( 'NONE',  ( 3.545573561795499540, -1.865266050240913520, 0.7750044584247675061 ) ) ;
#129992=CARTESIAN_POINT ( 'NONE',  ( 3.168876024238317601, -1.903602637213364979, -0.7901525784780991657 ) ) ;
#129996=CARTESIAN_POINT ( 'NONE',  ( 1.763359053103892293, 0.9455654613358072114, 1.579637215005654349 ) ) ;
#129997=CARTESIAN_POINT ( 'NONE',  ( 6.639307388351803674, -1.973492857608965423, 0.9879489342229507143 ) ) ;
#129999=CARTESIAN_POINT ( 'NONE',  ( 2.987745815084281276, 1.526290923294726820, 1.530918043534036599 ) ) ;
#130001=CARTESIAN_POINT ( 'NONE',  ( 1.622280145275534435, 1.995268681201247452, 0.2910785328335343536 ) ) ;
#130003=CARTESIAN_POINT ( 'NONE',  ( 0.8131078318618142342, -0.2785150557334699073, 1.849687307983488571 ) ) ;
#130005=CARTESIAN_POINT ( 'NONE',  ( 4.170748999387418721, -1.839122178589139178, -0.7105754535856413368 ) ) ;
#130006=CARTESIAN_POINT ( 'NONE',  ( 4.540250091716044878, 0.7762272601403925609, 1.861345588084816871 ) ) ;
#130010=CARTESIAN_POINT ( 'NONE',  ( 6.024072228909682636, -1.168613738950954550, -1.751890494488865357 ) ) ;
#130011=CARTESIAN_POINT ( 'NONE',  ( 6.531696417657103737, 1.982406992490031383, -0.5971068152322634992 ) ) ;
#130015=CARTESIAN_POINT ( 'NONE',  ( 4.996930482532231821, 1.639556309048403770, -1.094490209086243171 ) ) ;
#130016=CARTESIAN_POINT ( 'NONE',  ( 6.363536886121980984, -1.624614756573187435, -1.199887179878684540 ) ) ;
#130018=CARTESIAN_POINT ( 'NONE',  ( 4.582853619701852566, -2.237698958467302823, -0.5636369891960175682 ) ) ;
#130019=CARTESIAN_POINT ( 'NONE',  ( 2.237243932873288710, -0.09700783546583501005, -2.060382906607181930 ) ) ;
#130026=CARTESIAN_POINT ( 'NONE',  ( 4.721225823269111110, -1.937324205527543253, -0.9803755122778281539 ) ) ;
#130029=CARTESIAN_POINT ( 'NONE',  ( 2.647807870277216757, 0.6224553824519338807, 1.732961026760751366 ) ) ;
#130031=CARTESIAN_POINT ( 'NONE',  ( 5.319949580897746166, 1.306013235697962571, -1.759773446019400778 ) ) ;
#130033=CARTESIAN_POINT ( 'NONE',  ( 6.034080775264698993, 1.121385855563570288, -1.965008656891243044 ) ) ;
#130038=CARTESIAN_POINT ( 'NONE',  ( 6.221911924188020748, -0.9849534058487903199, -1.470084644806458174 ) ) ;
#130040=CARTESIAN_POINT ( 'NONE',  ( 4.072905994182826284, -1.490248019560231452, 1.353564014653575009 ) ) ;
#130042=CARTESIAN_POINT ( 'NONE',  ( 3.188603428895543601, -2.074531711476882201, -0.3615289903074799249 ) ) ;
#130043=CARTESIAN_POINT ( 'NONE',  ( 2.478032317504985649, -1.910654254087537307, -0.1382841363062360662 ) ) ;
#130045=CARTESIAN_POINT ( 'NONE',  ( 3.543367420142525148, 1.781686863328624026, -0.8397465311346365979 ) ) ;
#130046=CARTESIAN_POINT ( 'NONE',  ( 1.164687902950040321, -1.689591380799923215, -0.8031939614948147010 ) ) ;
#130047=CARTESIAN_POINT ( 'NONE',  ( 1.644895634054041933, -0.2845770130874228365, -1.940982728367894206 ) ) ;
#130048=CARTESIAN_POINT ( 'NONE',  ( 4.019902842142981214, -0.8889698729942583366, -1.477996400630256613 ) ) ;
#130049=CARTESIAN_POINT ( 'NONE',  ( -0.2108831679770960255, -0.001785917861228669690, -1.896958272444612792 ) ) ;
#130051=CARTESIAN_POINT ( 'NONE',  ( 1.682535984017709874, -1.178549783888741320, 1.865657194899547733 ) ) ;
#130058=CARTESIAN_POINT ( 'NONE',  ( 6.666853767972947153, 1.538155548931797956, -1.385880503156889487 ) ) ;
#130059=CARTESIAN_POINT ( 'NONE',  ( 0.8540665308606997241, -0.7467690478978536994, 1.931163149162813619 ) ) ;
#130065=CARTESIAN_POINT ( 'NONE',  ( 5.391314312714450274, -0.05227466736787074464, -2.120015263102632552 ) ) ;
#130069=CARTESIAN_POINT ( 'NONE',  ( 6.285602425426498385, -1.847771260692541162, 0.6596951833430019230 ) ) ;
#130071=CARTESIAN_POINT ( 'NONE',  ( 4.657577273293715514, -0.4389639308803178208, -1.967586094827819654 ) ) ;
#130072=CARTESIAN_POINT ( 'NONE',  ( 3.995261062014230813, -0.3217480215693402368, 1.888325751980689082 ) ) ;
#130074=CARTESIAN_POINT ( 'NONE',  ( 1.734175692058033347, 2.168326105380265378, 0.3173973903456903112 ) ) ;
#130079=CARTESIAN_POINT ( 'NONE',  ( 5.519199075762924345, -1.913696209152406125, 0.9060895950074706606 ) ) ;
#130081=CARTESIAN_POINT ( 'NONE',  ( 2.577772492168933116, -1.072305133946813260, 1.794659622045821079 ) ) ;
#130083=CARTESIAN_POINT ( 'NONE',  ( 0.4281588809218932479, 1.648258183568848789, 0.5080355103465240552 ) ) ;
#130095=CARTESIAN_POINT ( 'NONE',  ( 1.857782056280156580, 0.6927856907082428073, -1.673962145341382435 ) ) ;
#130100=CARTESIAN_POINT ( 'NONE',  ( 6.639320575229255006, 0.6011172813700341733, 1.850849092781511107 ) ) ;
#130105=CARTESIAN_POINT ( 'NONE',  ( 3.156551239342288095, -0.5378050974185369926, -1.781664776597549293 ) ) ;
#130106=CARTESIAN_POINT ( 'NONE',  ( 0.2631137269465182449, 1.787087189245086583, -0.6902753917677264539 ) ) ;
#130107=CARTESIAN_POINT ( 'NONE',  ( 6.721714886968523928, -1.868385559882647318, 0.4688378381374983528 ) ) ;
#130116=CARTESIAN_POINT ( 'NONE',  ( 4.188306824812327633, 1.057184280071225890, -1.661461291525099693 ) ) ;
#130117=CARTESIAN_POINT ( 'NONE',  ( 1.664851754375612058, 0.6682523891239250391, 2.012492909199379731 ) ) ;
#130122=CARTESIAN_POINT ( 'NONE',  ( 5.683573789218531402, -0.9880169931659465998, 1.956149625775935430 ) ) ;
#130124=CARTESIAN_POINT ( 'NONE',  ( 5.209954918934378121, -1.917094737882633959, 0.1888984193934347133 ) ) ;
#130127=CARTESIAN_POINT ( 'NONE',  ( 0.7685542157043163680, 1.090964843879228097, 1.918292034055509632 ) ) ;
#130132=CARTESIAN_POINT ( 'NONE',  ( 6.209808219158968967, 0.5752867347804692111, -1.883509059051315271 ) ) ;
#130133=CARTESIAN_POINT ( 'NONE',  ( 1.083423466712875260, -0.8719414265662344121, 1.735365470925637199 ) ) ;
#130134=CARTESIAN_POINT ( 'NONE',  ( 0.8958609827393304581, 0.1455075039201655374, 2.010896580075637541 ) ) ;
#130136=CARTESIAN_POINT ( 'NONE',  ( 5.313276548598107496, -1.570925495967404828, -0.9973500568975323111 ) ) ;
#130141=CARTESIAN_POINT ( 'NONE',  ( 1.857222401600963302, 0.3706860215506869172, -2.159823580554325329 ) ) ;
#130145=CARTESIAN_POINT ( 'NONE',  ( 2.015964598666186269, -0.8597642540715648707, -1.610575774528985704 ) ) ;
#130148=CARTESIAN_POINT ( 'NONE',  ( 6.609000000000047059, 2.429201845222619394, 2.481963755843877628 ) ) ;
#130150=CARTESIAN_POINT ( 'NONE',  ( 6.604126001430527637, -1.825160783932573860, 0.05055279568313279792 ) ) ;
#130151=CARTESIAN_POINT ( 'NONE',  ( 4.610177715184628155, 1.961415711727178213, -0.04403062578262756377 ) ) ;
#130154=CARTESIAN_POINT ( 'NONE',  ( 4.353197867323560288, 0.4795420089713005041, -2.138300074133951068 ) ) ;
#130156=CARTESIAN_POINT ( 'NONE',  ( 3.678634981485491728, 1.317094234756083893, -1.597214816249421743 ) ) ;
#130159=CARTESIAN_POINT ( 'NONE',  ( 4.553568368667338717, -1.501836741657993191, 1.740358071397982265 ) ) ;
#130165=CARTESIAN_POINT ( 'NONE',  ( 4.154194137148957466, -1.438218894771810641, 1.305048227774636915 ) ) ;
#130168=CARTESIAN_POINT ( 'NONE',  ( 4.201352949932454450, 1.705870964349815333, -0.8646410313453978258 ) ) ;
#130170=CARTESIAN_POINT ( 'NONE',  ( 5.121954690102882957, -0.9251313946504275965, -1.455449238992040373 ) ) ;
#130171=CARTESIAN_POINT ( 'NONE',  ( 4.663296154398564042, 1.879804967172087782, -0.7303043177912388328 ) ) ;
#130172=CARTESIAN_POINT ( 'NONE',  ( 4.676596114989339803, 1.702786692269612212, 1.544373632959222586 ) ) ;
#130174=CARTESIAN_POINT ( 'NONE',  ( 0.8739773845415178544, 2.125910683164092152, -0.5920798734769525673 ) ) ;
#130177=CARTESIAN_POINT ( 'NONE',  ( 6.028513167084792457, 1.705988696259161719, 0.4703064415670314413 ) ) ;
#130179=CARTESIAN_POINT ( 'NONE',  ( 1.553083273963658639, -1.967900166212281476, -1.175304309182874096 ) ) ;
#130180=CARTESIAN_POINT ( 'NONE',  ( 1.429236002152774576, 0.8600564655791165247, -1.512861638240108997 ) ) ;
#130182=CARTESIAN_POINT ( 'NONE',  ( 0.9129801003131752246, 0.4962884120854795245, 1.661303041287894411 ) ) ;
#130185=CARTESIAN_POINT ( 'NONE',  ( 1.029994877853340762, 2.092549206400303063, -0.5788440209302682105 ) ) ;
#130186=CARTESIAN_POINT ( 'NONE',  ( 2.272673044126482189, -0.3494851828299732621, -1.985868527484459634 ) ) ;
#130188=CARTESIAN_POINT ( 'NONE',  ( 6.305299685587768543, 1.603216850002240124, 1.067941234924398852 ) ) ;
#130190=CARTESIAN_POINT ( 'NONE',  ( 2.022025532713614737, -0.4812968563913700981, 2.168513943247989850 ) ) ;
#130196=CARTESIAN_POINT ( 'NONE',  ( 5.020954538418783031, -1.650374644951870806, 0.5528329121840831473 ) ) ;
#130197=CARTESIAN_POINT ( 'NONE',  ( 4.017981030900905637, 1.947309607215493621, -0.2378496960543720617 ) ) ;
#130201=CARTESIAN_POINT ( 'NONE',  ( 4.604895111943496211, 1.752856212930454127, -1.430419756957083566 ) ) ;
#130202=CARTESIAN_POINT ( 'NONE',  ( 1.258340527071156956, -2.062851378465610175, -0.001992840727984764547 ) ) ;
#130206=CARTESIAN_POINT ( 'NONE',  ( 2.764839853141934256, -1.560785778453818828, 1.638175023747280523 ) ) ;
#130209=CARTESIAN_POINT ( 'NONE',  ( 2.723731132150861711, -1.073666234122659713, -1.531540996774889640 ) ) ;
#130210=CARTESIAN_POINT ( 'NONE',  ( 1.529482971743981734, -1.465093928883187901, 0.9274137557628134854 ) ) ;
#130211=CARTESIAN_POINT ( 'NONE',  ( 5.179302069984247581, 1.471482994053765925, 1.624232740060495228 ) ) ;
#130212=CARTESIAN_POINT ( 'NONE',  ( 0.3587983166186413109, 0.8468606107991830667, 2.038007455039527294 ) ) ;
#130213=CARTESIAN_POINT ( 'NONE',  ( 3.995124980148881288, 1.827535992889782523, -1.154293374375232828 ) ) ;
#130214=CARTESIAN_POINT ( 'NONE',  ( 4.435450497376713486, 0.8291751068889623433, -1.756158939159500276 ) ) ;
#130216=CARTESIAN_POINT ( 'NONE',  ( 6.608674649642057197, 1.385883050205028333, -1.256505298338560062 ) ) ;
#130217=CARTESIAN_POINT ( 'NONE',  ( 0.4999999999999185651, 1.979557137443526406E-12, -2.052068128417952941 ) ) ;
#130222=CARTESIAN_POINT ( 'NONE',  ( 6.117814597332064785, 0.2004318333163370436, 2.006446488866588496 ) ) ;
#130226=CARTESIAN_POINT ( 'NONE',  ( 3.246530741642670304, 0.4443377543969920795, 1.770662692542070538 ) ) ;
#130228=CARTESIAN_POINT ( 'NONE',  ( -0.1296875068448159474, 0.7431874094961617994, -1.910093690679348200 ) ) ;
#130234=CARTESIAN_POINT ( 'NONE',  ( -0.05247081622378191312, -1.844958069526716926, 0.8224554107575526851 ) ) ;
#130235=CARTESIAN_POINT ( 'NONE',  ( 0.7859742890132662696, 2.042544534415400737, -0.5693509180391894686 ) ) ;
#130239=CARTESIAN_POINT ( 'NONE',  ( 6.491097285755237145, 1.794469726164525492, -1.013322515520258538 ) ) ;
#130244=CARTESIAN_POINT ( 'NONE',  ( -0.2108831679771203116, 0.7314853703891763814, -1.979988191570913880 ) ) ;
#130247=CARTESIAN_POINT ( 'NONE',  ( 0.07680821025393863577, 5.725641208404781857, -2.404836704152548688 ) ) ;
#130250=CARTESIAN_POINT ( 'NONE',  ( 5.800157620552712778, -1.823839058171864203, 0.8595007112896931867 ) ) ;
#130251=CARTESIAN_POINT ( 'NONE',  ( 5.068220161613846031, -1.734768455660203434, -0.6171159064975312303 ) ) ;
#130253=CARTESIAN_POINT ( 'NONE',  ( 3.387651152892924955, 2.086375235072422285, -0.9864360317304238235 ) ) ;
#130255=CARTESIAN_POINT ( 'NONE',  ( 5.712251288600169730, -0.9662322189689104279, -1.933677227328117532 ) ) ;
#130257=CARTESIAN_POINT ( 'NONE',  ( 1.083423466712875260, -0.8719414265662344121, 1.735365470925637199 ) ) ;
#130261=CARTESIAN_POINT ( 'NONE',  ( 4.429307823785958220, 1.078883539000154324, 2.029420160895245129 ) ) ;
#130262=CARTESIAN_POINT ( 'NONE',  ( 0.07516593201275459379, 0.0004601587237918110533, -2.044269526395313008 ) ) ;
#130264=CARTESIAN_POINT ( 'NONE',  ( 4.733189744967194024, -1.710186631362722531, 0.7584244158565585092 ) ) ;
#130266=CARTESIAN_POINT ( 'NONE',  ( 1.072351618572921605, 0.7776387867773439933, 1.747342548420704800 ) ) ;
#130269=CARTESIAN_POINT ( 'NONE',  ( 2.631697372267821855, -2.058793095894187353, 0.7952504953367269813 ) ) ;
#130276=CARTESIAN_POINT ( 'NONE',  ( 1.862511354659317053, -1.396895987378836690, 1.391268958170795100 ) ) ;
#130277=CARTESIAN_POINT ( 'NONE',  ( 1.149971759812302263, -1.820915985741960785, -1.417348977311111202 ) ) ;
#130278=CARTESIAN_POINT ( 'NONE',  ( 1.099968687278202406, 0.7983322178258808188, -1.792280776234013828 ) ) ;
#130279=CARTESIAN_POINT ( 'NONE',  ( 5.084863090169797317, 1.972218467801799102, 0.6036872243675943661 ) ) ;
#130286=CARTESIAN_POINT ( 'NONE',  ( 1.288188150525194642, -1.375441891341127265, -1.679832657438373511 ) ) ;
#130290=CARTESIAN_POINT ( 'NONE',  ( 1.651402116136031051, 0.5479989942898423338, -1.788454331708405620 ) ) ;
#130291=CARTESIAN_POINT ( 'NONE',  ( 5.993488848236776967, 1.632462841753023808, 1.416962642945495565 ) ) ;
#130293=CARTESIAN_POINT ( 'NONE',  ( -0.02264175331117677936, 7.629137130509094256, -2.689100833419917347 ) ) ;
#130295=CARTESIAN_POINT ( 'NONE',  ( 2.543496672408153358, -1.783599581865771500, 0.6900697577220117340 ) ) ;
#130297=CARTESIAN_POINT ( 'NONE',  ( 4.574921169738827231, -0.001286399002502561879, -1.770032026507301515 ) ) ;
#130298=CARTESIAN_POINT ( 'NONE',  ( 0.4692111731946085884, -1.615589042895089200, -1.022764193708516789 ) ) ;
#130301=CARTESIAN_POINT ( 'NONE',  ( 4.956599115817130752, -1.805213640821627052, -0.6413244422398997058 ) ) ;
#130302=CARTESIAN_POINT ( 'NONE',  ( 6.602011381505620946, 0.7551138498248446407, -1.819252348156335852 ) ) ;
#130304=CARTESIAN_POINT ( 'NONE',  ( 1.986737319265439394, -1.300789755646198476, 1.674730562594067829 ) ) ;
#130306=CARTESIAN_POINT ( 'NONE',  ( 4.610133579271312954, -0.8000244862099057386, -1.691074300901610261 ) ) ;
#130307=CARTESIAN_POINT ( 'NONE',  ( 0.5041868517345666767, -0.6120625888205477594, -1.720162557568189809 ) ) ;
#130309=CARTESIAN_POINT ( 'NONE',  ( 4.582781371344160526, -2.140174514510746029, -0.5380331057033281850 ) ) ;
#130312=CARTESIAN_POINT ( 'NONE',  ( 1.820832581213110313, -1.460207654653251419, 1.457104742506893036 ) ) ;
#130320=CARTESIAN_POINT ( 'NONE',  ( 3.807136610393092813, -1.694265131726957252, 1.189645435975445809 ) ) ;
#130322=CARTESIAN_POINT ( 'NONE',  ( 1.405796033167511894, -0.5266655099175953092, 2.096309153942426562 ) ) ;
#130324=CARTESIAN_POINT ( 'NONE',  ( 2.051431352050979040, -1.803145959232739237, 0.9099833227969624794 ) ) ;
#130328=CARTESIAN_POINT ( 'NONE',  ( 0.07479286986305369589, 0.004866263145587855152, -1.855573292446037970 ) ) ;
#130332=CARTESIAN_POINT ( 'NONE',  ( 0.1984543448181053105, 1.387095780679182377, -1.463931301963219855 ) ) ;
#130333=CARTESIAN_POINT ( 'NONE',  ( 5.267185993530860699, 2.112242253262315739, -0.5839428218426812034 ) ) ;
#130335=CARTESIAN_POINT ( 'NONE',  ( 4.113462262696740979, 1.539102623358613586, 1.134910093507961237 ) ) ;
#130339=CARTESIAN_POINT ( 'NONE',  ( 2.284780001213771783, 1.617805504991537635, -1.203372706716873575 ) ) ;
#130341=CARTESIAN_POINT ( 'NONE',  ( 0.3106431952284515741, 1.574884954006963600, -1.665989127006389126 ) ) ;
#130343=CARTESIAN_POINT ( 'NONE',  ( 3.733171248123872132, -1.593707704047672591, 0.6599822260907485250 ) ) ;
#130344=FACE_OUTER_BOUND ( 'NONE', #100884, .T. ) ;
#130350=CARTESIAN_POINT ( 'NONE',  ( 5.197853184559683370, 1.220981990389960581, 1.338314830865680261 ) ) ;
#130353=DIRECTION ( 'NONE',  ( 1.214306433183764966E-17, 1.000000000000000000, 5.200009205990155575E-32 ) ) ;
#130354=CARTESIAN_POINT ( 'NONE',  ( 6.111934181110398434, -0.6035781192351510338, 1.708109960999981469 ) ) ;
#130357=CARTESIAN_POINT ( 'NONE',  ( 2.748186945943337012, 0.7392028471469233031, 2.063141171074922120 ) ) ;
#130361=CARTESIAN_POINT ( 'NONE',  ( 5.846130809274892925, -0.8361890816445856078, 1.662715158673214066 ) ) ;
#130363=CARTESIAN_POINT ( 'NONE',  ( 3.814002402653454027, 1.021707883093534885, -1.620180217528136568 ) ) ;
#130369=CARTESIAN_POINT ( 'NONE',  ( 1.604591590977550108, -0.7782141685120853580, -2.016947388195994062 ) ) ;
#130373=CARTESIAN_POINT ( 'NONE',  ( 2.397230751819504402, 1.409552409829779140, 1.160114028286141075 ) ) ;
#130375=CARTESIAN_POINT ( 'NONE',  ( 3.821172736587064023, -0.1348131347885111742, 1.820669774636254568 ) ) ;
#130377=CARTESIAN_POINT ( 'NONE',  ( 2.601700882821424976, 1.355260107747566334, 1.349524769375435973 ) ) ;
#130379=CARTESIAN_POINT ( 'NONE',  ( 4.053143702687862060, 1.665121224333296235, -1.051576502219366605 ) ) ;
#130381=CARTESIAN_POINT ( 'NONE',  ( 4.845229750085990439, 0.6055439843271113176, -1.845326283916528753 ) ) ;
#130382=ORIENTED_EDGE ( 'NONE', *, *, #17999, .T. ) ;
#130385=CARTESIAN_POINT ( 'NONE',  ( 4.763993809689464065, 0.6627061821620899851, -2.014485251161435286 ) ) ;
#130391=CARTESIAN_POINT ( 'NONE',  ( 3.615888430654935259, -0.5820857220382947839, 1.927115488332105553 ) ) ;
#130393=CARTESIAN_POINT ( 'NONE',  ( 5.285714101943871590, 1.228958891529348785, 1.350286652578087665 ) ) ;
#130394=CARTESIAN_POINT ( 'NONE',  ( 0.6607010325807397555, -0.6960017893198193750, -1.950014918625786020 ) ) ;
#130399=CARTESIAN_POINT ( 'NONE',  ( 5.559403950928493821, 0.3636877230743483236, -1.834782481876767291 ) ) ;
#130403=B_SPLINE_CURVE_WITH_KNOTS ( 'NONE', 3,
 ( #55979, #118901, #188095, #39727, #105833, #117840, #183832, #35441, #101518, #167589 ),
 .UNSPECIFIED., .F., .F.,
 ( 4, 1, 1, 1, 1, 1, 1, 4 ),
 ( 0.000000000000000000, 0.09489293188423997272, 0.1878783894049059211, 0.2584743716234961797, 0.3617987437640678983, 0.5212292184658617877, 0.7337638816394396191, 1.000000000000000000 ),
 .UNSPECIFIED. ) ;
#130410=CARTESIAN_POINT ( 'NONE',  ( 0.9013344411078340057, -1.777497804657724334, 1.061070337243313455 ) ) ;
#130411=CARTESIAN_POINT ( 'NONE',  ( 1.968512934334982978, -2.077085554295199810, -0.4095441970272342136 ) ) ;
#130415=CARTESIAN_POINT ( 'NONE',  ( 0.3913703952206915027, -1.802969083500185477, 0.7928767443170018359 ) ) ;
#130419=DIRECTION ( 'NONE',  ( 1.014813233446432150E-15, 1.000000000000000000, -4.583713267641621330E-32 ) ) ;
#130420=CARTESIAN_POINT ( 'NONE',  ( 2.801036929584544311, 1.937030572335847856, 1.225446795713614589 ) ) ;
#130421=CARTESIAN_POINT ( 'NONE',  ( 0.6799654140086827114, -1.016662149479659494, 1.516215539243186639 ) ) ;
#130422=CARTESIAN_POINT ( 'NONE',  ( 2.672007700615218528, 1.902801012812182169, -0.1915479950082218386 ) ) ;
#130427=CARTESIAN_POINT ( 'NONE',  ( 1.740491373288379995, 1.155656410672186496, -1.648304894270665510 ) ) ;
#130428=CARTESIAN_POINT ( 'NONE',  ( 1.516376426791886445, 0.7900930292849810410, 1.795789229542772647 ) ) ;
#130432=CARTESIAN_POINT ( 'NONE',  ( 4.400388060213418662, 1.616114658936588011, -1.326231919226998901 ) ) ;
#130433=CARTESIAN_POINT ( 'NONE',  ( 2.482954129442132452, 1.619277697627572676, -0.7147633530761726695 ) ) ;
#130435=CARTESIAN_POINT ( 'NONE',  ( 5.332074485713341971, 2.257618135992002895, 0.3962004586785839444 ) ) ;
#130436=CARTESIAN_POINT ( 'NONE',  ( 4.382551862494687533, 1.553031517084975555, -0.7855321229453329224 ) ) ;
#130439=CARTESIAN_POINT ( 'NONE',  ( 4.393670956608656475, 0.08463240572039069931, 1.731882585348672343 ) ) ;
#130440=CARTESIAN_POINT ( 'NONE',  ( 4.404835846824251888, 0.5749587956990888094, 2.093619418667266530 ) ) ;
#130442=CARTESIAN_POINT ( 'NONE',  ( 5.296111364736042937, -0.9110065213352031011, -1.799124599017036585 ) ) ;
#130443=CARTESIAN_POINT ( 'NONE',  ( 0.5312500000000220934, -0.7852924748305555314, -1.895863743164076576 ) ) ;
#130445=CARTESIAN_POINT ( 'NONE',  ( 3.346621647027960833, 0.4665833272349695360, 1.868923817322089453 ) ) ;
#130447=CARTESIAN_POINT ( 'NONE',  ( 6.135052730014136202, 2.072377209612641824, 0.8004311911904669063 ) ) ;
#130449=CARTESIAN_POINT ( 'NONE',  ( 6.883263157960370471, 7.053006342242538196, 2.444342378444531949 ) ) ;
#130452=CARTESIAN_POINT ( 'NONE',  ( 1.735333443468607184, 2.074102030253548445, 0.7956244722606919950 ) ) ;
#130459=CARTESIAN_POINT ( 'NONE',  ( 4.352046829380719295, -0.7922827022245787498, 1.904640004429495326 ) ) ;
#130463=CARTESIAN_POINT ( 'NONE',  ( 6.520764494017629254, 1.745421825204738431, 0.6730592012400560264 ) ) ;
#130464=CARTESIAN_POINT ( 'NONE',  ( 6.082590270738484683, -0.5753628732939282120, 1.636087478734444600 ) ) ;
#130465=CARTESIAN_POINT ( 'NONE',  ( 4.792390001771311248, 1.443284891743993770, -0.9723301709525405956 ) ) ;
#130467=CARTESIAN_POINT ( 'NONE',  ( 3.087719631786550956, -0.9270648334414759439, 2.096714421332421807 ) ) ;
#130469=CARTESIAN_POINT ( 'NONE',  ( 1.288719586054212884, 1.393062650230517674, 1.203921758438614376 ) ) ;
#130471=CARTESIAN_POINT ( 'NONE',  ( 2.045663570152244315, 0.7015605659913305425, -1.685594894050304493 ) ) ;
#130472=CARTESIAN_POINT ( 'NONE',  ( 3.217422812353257555, 1.967887761762876941, 0.4390297752325384995 ) ) ;
#130473=CARTESIAN_POINT ( 'NONE',  ( 0.9553299046189435151, 0.4242123182428610972, -2.149831459026855907 ) ) ;
#130475=CARTESIAN_POINT ( 'NONE',  ( 4.542079205076994697, 0.9026690382304535243, -1.902845716346044158 ) ) ;
#130479=CARTESIAN_POINT ( 'NONE',  ( 1.891162872569674080, 0.2007839719405465906, 2.060584128686280714 ) ) ;
#130482=CARTESIAN_POINT ( 'NONE',  ( 3.158948766716848766, 0.5171890032967979556, 2.056314737185329644 ) ) ;
#130486=CARTESIAN_POINT ( 'NONE',  ( 0.1352084326644766299, -1.761967750658991028, 0.7794309377431463126 ) ) ;
#130494=CARTESIAN_POINT ( 'NONE',  ( 3.779560859189102562, 0.2429267963163626032, -2.005027992008329818 ) ) ;
#130495=CARTESIAN_POINT ( 'NONE',  ( 1.501149451381103672, 1.721883814275385616, -1.212229816669802895 ) ) ;
#130498=CARTESIAN_POINT ( 'NONE',  ( 5.524199568661091853, 0.9153802634506421620, 1.620121770064205213 ) ) ;
#130503=CARTESIAN_POINT ( 'NONE',  ( 0.4093245661422850734, 1.881582470445356314, 1.064130679222355491 ) ) ;
#130507=CARTESIAN_POINT ( 'NONE',  ( 2.864235035935404738, -0.5475380835847867278, 1.645162456946830831 ) ) ;
#130508=CARTESIAN_POINT ( 'NONE',  ( 1.095196197045473774, -1.740516465796032586, -0.003461242977918776564 ) ) ;
#130509=CARTESIAN_POINT ( 'NONE',  ( 6.410760325301650298, 1.714854236211732941, -1.544436965994408828 ) ) ;
#130512=CARTESIAN_POINT ( 'NONE',  ( 2.530605077378933920, 1.998055600607269833, 0.5039824654343558752 ) ) ;
#130513=CARTESIAN_POINT ( 'NONE',  ( 1.194685229111978497, -1.276845315561925931, -1.560263297373874813 ) ) ;
#130514=CARTESIAN_POINT ( 'NONE',  ( 6.925078400183521055, 0.5534609092465185842, 2.295239920751692253 ) ) ;
#130516=CARTESIAN_POINT ( 'NONE',  ( 0.6726557866889815163, -1.855577277548149828, -0.6663020492489196700 ) ) ;
#130517=CARTESIAN_POINT ( 'NONE',  ( 4.517770118113122457, -0.5046507728132009207, 1.844564425022446885 ) ) ;
#130522=CARTESIAN_POINT ( 'NONE',  ( 0.1705770660650838266, 0.7750864355984161680, 1.865232097879976125 ) ) ;
#130523=CARTESIAN_POINT ( 'NONE',  ( 4.858593139428769803, 0.8780750695473713563, 2.134189430172124702 ) ) ;
#130524=CARTESIAN_POINT ( 'NONE',  ( 5.916451087343006954, 0.7937011933104149985, 1.794315766958521241 ) ) ;
#130525=CARTESIAN_POINT ( 'NONE',  ( 1.533958681542445301, 1.164210590399002321, 1.578835587694705334 ) ) ;
#130529=CARTESIAN_POINT ( 'NONE',  ( 0.1459223332197969736, 2.093306735845179567, -0.3175718533311999714 ) ) ;
#130532=CARTESIAN_POINT ( 'NONE',  ( 1.112948326906910035, -1.796673262952220629, 0.4014371099074555693 ) ) ;
#130534=CARTESIAN_POINT ( 'NONE',  ( 4.206061555090504278, 0.7368182104705008895, -2.042320221205825792 ) ) ;
#130536=CARTESIAN_POINT ( 'NONE',  ( 2.355864820516640812, -1.574449018071517825, -1.420800595792824028 ) ) ;
#130540=CARTESIAN_POINT ( 'NONE',  ( 3.620434630758031069, 1.310268768930487937, -1.590567769477232662 ) ) ;
#130542=CARTESIAN_POINT ( 'NONE',  ( 0.3449248370967008537, 0.5783895242766275979, -1.748133987124582012 ) ) ;
#130544=CARTESIAN_POINT ( 'NONE',  ( -0.02264175331117417728, 0.7142767504201595896, -2.172799776233569791 ) ) ;
#130548=CARTESIAN_POINT ( 'NONE',  ( 1.441102657128832121, 0.4411821743415585417, 2.218815533503415871 ) ) ;
#130550=CARTESIAN_POINT ( 'NONE',  ( 1.388595261843462714, -1.720809334905664567, -0.5665428721913360333 ) ) ;
#130551=CARTESIAN_POINT ( 'NONE',  ( 1.586979130512996772, 1.594871783843774260, 1.060967117046989427 ) ) ;
#130552=CARTESIAN_POINT ( 'NONE',  ( 2.945825538390862697, 1.462269270728074222, 1.465923284304726737 ) ) ;
#130555=CARTESIAN_POINT ( 'NONE',  ( 1.358210660854881402, 0.7971155783631430625, 1.803302576489584697 ) ) ;
#130556=CARTESIAN_POINT ( 'NONE',  ( 5.268162717194916134, 0.9514403766726580169, 1.675093392909310142 ) ) ;
#130558=CARTESIAN_POINT ( 'NONE',  ( 0.7687468715882056491, 1.142267183891092053, 2.005099294460314319 ) ) ;
#130561=CARTESIAN_POINT ( 'NONE',  ( 5.793442459296725744, -1.866233137118753715, 0.8787832743982221251 ) ) ;
#130565=CARTESIAN_POINT ( 'NONE',  ( 6.247117736759643769, -1.781108002423707592, 1.123397916191863244 ) ) ;
#130567=CARTESIAN_POINT ( 'NONE',  ( 6.432923066502826082, 0.2047513753351773713, 2.151863363619124225 ) ) ;
#130568=CARTESIAN_POINT ( 'NONE',  ( 0.3625324912872701089, 0.1813134127766780901, -1.832273687604975665 ) ) ;
#130569=CARTESIAN_POINT ( 'NONE',  ( 5.373696804382912973, 0.3918686645382524203, -1.981109099827490949 ) ) ;
#130577=CARTESIAN_POINT ( 'NONE',  ( 3.309780021317248355, -1.205041885261768808, -1.616693488061982098 ) ) ;
#130582=CARTESIAN_POINT ( 'NONE',  ( 5.014612968065254250, 1.493337269798940881, -1.563205770552501761 ) ) ;
#130587=CARTESIAN_POINT ( 'NONE',  ( 5.941029844038744123, -1.730876725876070221, -1.034150010194856417 ) ) ;
#130590=CARTESIAN_POINT ( 'NONE',  ( 1.576317393346495344, -1.636983117988626946, -0.5438251031371076349 ) ) ;
#130595=CARTESIAN_POINT ( 'NONE',  ( 6.573518820989787237, 1.789947451694915204, -0.5432430119688207437 ) ) ;
#130596=CARTESIAN_POINT ( 'NONE',  ( 1.207682405589046937, 1.525905122249699319, 1.313188400431253955 ) ) ;
#130598=CARTESIAN_POINT ( 'NONE',  ( 3.311752114541001379, -0.4323003076652854881, 2.163846791405985570 ) ) ;
#130599=CARTESIAN_POINT ( 'NONE',  ( 4.961888193860729324, -0.5853885669280403103, 2.090577497978749477 ) ) ;
#130602=CARTESIAN_POINT ( 'NONE',  ( 2.578903501431661915, -1.460476376761214556, 1.537597662120089081 ) ) ;
#130603=CARTESIAN_POINT ( 'NONE',  ( 1.528922965942226986, -1.701935853630029083, 1.081086586856384590 ) ) ;
#130604=CARTESIAN_POINT ( 'NONE',  ( 1.722643027415799999, 1.340613184126436597, -1.218586174478804907 ) ) ;
#130610=CARTESIAN_POINT ( 'NONE',  ( 1.710024596074321002, 1.099767263899156244, -1.568400350156524459 ) ) ;
#130616=CARTESIAN_POINT ( 'NONE',  ( 5.049776242366147194, 0.6816224847111511664, -2.051488706027407183 ) ) ;
#130620=CARTESIAN_POINT ( 'NONE',  ( 1.881254504445781794, -1.940830296247602949, -0.8548571619346672090 ) ) ;
#130621=CARTESIAN_POINT ( 'NONE',  ( -0.1296875068447882473, 5.724785194352729256, -2.420566058096422779 ) ) ;
#130622=CARTESIAN_POINT ( 'NONE',  ( 3.303940151695891281, -1.969246965329603638, 0.09337747576219912471 ) ) ;
#130623=CARTESIAN_POINT ( 'NONE',  ( 5.168181644781757456, 1.909928461159452251, -0.09994665148223277895 ) ) ;
#130626=CARTESIAN_POINT ( 'NONE',  ( 0.3794556558127279988, -0.1030994254981997954, 2.067933115924729837 ) ) ;
#130627=CARTESIAN_POINT ( 'NONE',  ( 1.833828351339358287, 1.920785844388651409, 0.2851290042146270576 ) ) ;
#130632=CARTESIAN_POINT ( 'NONE',  ( 2.501997717985538383, -0.8009308590465279432, -1.931334861377894008 ) ) ;
#130635=CARTESIAN_POINT ( 'NONE',  ( 5.901015568784107934, -0.2851453878830525479, -1.890788771128081969 ) ) ;
#130637=CARTESIAN_POINT ( 'NONE',  ( 4.266400587755204477, 1.039063272370500668, 1.946970035688735612 ) ) ;
#130638=CARTESIAN_POINT ( 'NONE',  ( 2.046200460737709559, 0.8445575735530999051, -2.038961412367201298 ) ) ;
#130640=CARTESIAN_POINT ( 'NONE',  ( 1.770022778749248182, 1.907080152163560971, -0.1419829583147319274 ) ) ;
#130644=CARTESIAN_POINT ( 'NONE',  ( 3.982925052038261526, 1.964963782255540359, 0.6523228965355857278 ) ) ;
#130646=CARTESIAN_POINT ( 'NONE',  ( 2.149508875876861236, -1.735919364271593768, -1.288018159417112729 ) ) ;
#130647=CARTESIAN_POINT ( 'NONE',  ( 4.054362073078698891, -1.623213109359676443, 1.472610181411204922 ) ) ;
#130655=CARTESIAN_POINT ( 'NONE',  ( 0.5455463417442986129, -1.458554840210561476, 1.392547631435703037 ) ) ;
#130658=CARTESIAN_POINT ( 'NONE',  ( 4.557524383921963462, 1.659614545607337677, 1.237363147772299721 ) ) ;
#130659=CARTESIAN_POINT ( 'NONE',  ( 3.281779325460960628, 1.222525406819600757, 1.488901545882119759 ) ) ;
#130660=CARTESIAN_POINT ( 'NONE',  ( 5.519199075762924345, -1.913696209152406125, 0.9060895950074706606 ) ) ;
#130664=CARTESIAN_POINT ( 'NONE',  ( 3.836728334651629879, -1.896773656598240709, -0.5296851528490874594 ) ) ;
#130665=CARTESIAN_POINT ( 'NONE',  ( 5.999983301813878178, -0.8195729662384824143, -2.140910441102741313 ) ) ;
#130666=CARTESIAN_POINT ( 'NONE',  ( 4.055160972438559774, -1.518969423100406946, -1.012540670841777013 ) ) ;
#130673=CARTESIAN_POINT ( 'NONE',  ( 5.379157392057874354, -1.821786014368693252, -0.8570216514257876783 ) ) ;
#130674=CARTESIAN_POINT ( 'NONE',  ( 6.188148266813070286, 1.908752161701723571, 1.280650486962619627 ) ) ;
#130675=CARTESIAN_POINT ( 'NONE',  ( 4.504711789546460565, 0.5192035298374733099, 1.891763301562799260 ) ) ;
#130680=CARTESIAN_POINT ( 'NONE',  ( 0.3805629577237649719, -0.2597898305938106112, -2.074488238918821725 ) ) ;
#130681=CARTESIAN_POINT ( 'NONE',  ( 6.807488043635657959, -0.3792581958518992935, 1.734866861734218446 ) ) ;
#130683=CARTESIAN_POINT ( 'NONE',  ( 6.386669098100576036, 1.688287130807873293, -0.9594923298414399504 ) ) ;
#130684=CARTESIAN_POINT ( 'NONE',  ( -0.2102771530458276972, 0.6786276403282426317, -2.283427277113641019 ) ) ;
#130685=CARTESIAN_POINT ( 'NONE',  ( 1.329236136963531489, 0.8583591509643221373, -1.513936452999464555 ) ) ;
#130688=CARTESIAN_POINT ( 'NONE',  ( 1.400563108759992792, 1.411875272319111696, -0.9905557981151734692 ) ) ;
#130689=CARTESIAN_POINT ( 'NONE',  ( 2.138457411672203712, 0.4836887423533155483, 2.137355272389021899 ) ) ;
#130690=CARTESIAN_POINT ( 'NONE',  ( 3.985166894971280183, -0.2153072539897090687, -2.196357064762343825 ) ) ;
#130692=CARTESIAN_POINT ( 'NONE',  ( 1.569424903267138571, 1.913428125876670549, 1.025899993198212901 ) ) ;
#130694=CARTESIAN_POINT ( 'NONE',  ( 2.554045646286424276, 1.136978842527110123, 1.786019645988563997 ) ) ;
#130696=CARTESIAN_POINT ( 'NONE',  ( 3.070184882724129594, -1.363667385223182871, 1.842535374393680980 ) ) ;
#130701=CARTESIAN_POINT ( 'NONE',  ( 5.303485788544977098, 1.959706058537356910, -1.045853978123905570 ) ) ;
#130708=CARTESIAN_POINT ( 'NONE',  ( 3.006482587178582300, -1.942541511447487990, 0.5404910644229294903 ) ) ;
#130710=CARTESIAN_POINT ( 'NONE',  ( 1.885666897375902096, -1.943580278752204515, 0.6908589954031388869 ) ) ;
#130715=CARTESIAN_POINT ( 'NONE',  ( 4.681673494351117348, -1.034495392153191418, 1.931897795048514554 ) ) ;
#130716=CARTESIAN_POINT ( 'NONE',  ( 1.969375177810539945, -1.978050944945686673, -0.3905967402937361443 ) ) ;
#130717=CARTESIAN_POINT ( 'NONE',  ( 0.5558949066124979632, -1.334021266253348381, 1.269314063962425854 ) ) ;
#130719=CARTESIAN_POINT ( 'NONE',  ( 5.139593076133685656, -1.292025762983131099, -1.289991942498528665 ) ) ;
#130720=CARTESIAN_POINT ( 'NONE',  ( 6.293592298849589817, 1.492257802130890765, -1.356297202127904944 ) ) ;
#130722=CARTESIAN_POINT ( 'NONE',  ( 4.610415411315283762, -0.9635332438130711497, -2.047219928730920291 ) ) ;
#130724=CARTESIAN_POINT ( 'NONE',  ( 0.7332070197069834316, 0.1568218392365756941, 2.100289424198895194 ) ) ;
#130726=CARTESIAN_POINT ( 'NONE',  ( 5.160626937512653001, -0.6942339714755951796, -1.950645400549338104 ) ) ;
#130734=CARTESIAN_POINT ( 'NONE',  ( 1.740644586495963431, 1.216819214799185866, -1.736574482785017359 ) ) ;
#130735=CARTESIAN_POINT ( 'NONE',  ( 1.934110000270176322, -2.153362505827714823, 0.5451143137677332273 ) ) ;
#130739=CARTESIAN_POINT ( 'NONE',  ( 3.683996026499200660, -1.166640140252427793, -1.577160851978461009 ) ) ;
#130745=CARTESIAN_POINT ( 'NONE',  ( 2.654661980655496301, 2.105093816413053709, 0.2552270188876659129 ) ) ;
#130747=CARTESIAN_POINT ( 'NONE',  ( 6.109812101310618360, 0.5708666350849945781, -1.876949146916474298 ) ) ;
#130748=CARTESIAN_POINT ( 'NONE',  ( 4.575171270262055501, 0.003154952768896768234, -2.161883445794945846 ) ) ;
#130749=CARTESIAN_POINT ( 'NONE',  ( 2.911469271472226339, -0.9098125248445630975, -1.600700954789348263 ) ) ;
#130752=CARTESIAN_POINT ( 'NONE',  ( 5.507646315527288117, -0.7876679103963373230, -1.551952608056671457 ) ) ;
#130756=CARTESIAN_POINT ( 'NONE',  ( 3.010779355932476253, 1.566693023359872372, -1.489686202715050145 ) ) ;
#130757=CARTESIAN_POINT ( 'NONE',  ( 5.044295983762377311, 1.882185518538554314, -0.7230303062365079914 ) ) ;
#130759=CARTESIAN_POINT ( 'NONE',  ( 1.920999885407469243, 2.016935458891587096, 0.7782144962657986387 ) ) ;
#130760=CARTESIAN_POINT ( 'NONE',  ( 2.530492563074437928, 1.911271491015430035, 0.4824842627236708426 ) ) ;
#130762=CARTESIAN_POINT ( 'NONE',  ( 4.142085694530703854, 0.5209831505245207106, 1.870798910701749973 ) ) ;
#130771=CARTESIAN_POINT ( 'NONE',  ( 0.7455094363101981703, -1.891729906373079029, 1.136061337225414913 ) ) ;
#130773=CARTESIAN_POINT ( 'NONE',  ( 4.803538753074391821, -1.513872852549098091, -1.247617340562396926 ) ) ;
#130776=CARTESIAN_POINT ( 'NONE',  ( 0.1745949693968692484, 0.009193469831055355729, -1.755468632744116242 ) ) ;
#130777=CARTESIAN_POINT ( 'NONE',  ( 3.714658492009088153, -0.1339090230784937274, 1.836323816731308067 ) ) ;
#130783=CARTESIAN_POINT ( 'NONE',  ( 4.922192346260840345, -2.110166376318895587, 0.2103620946037400852 ) ) ;
#130786=CARTESIAN_POINT ( 'NONE',  ( 6.345006307232072373, -1.743395995315766056, 1.098490678494741912 ) ) ;
#130788=CARTESIAN_POINT ( 'NONE',  ( 1.099803389655891195, 0.7588869020343449456, -1.699499299819209108 ) ) ;
#130789=CARTESIAN_POINT ( 'NONE',  ( 3.192734241421916419, 1.453351889590439816, 1.130385295574042104 ) ) ;
#130795=CARTESIAN_POINT ( 'NONE',  ( 3.405080638938757343, 1.739790774466195789, -1.357627211771177178 ) ) ;
#130796=CARTESIAN_POINT ( 'NONE',  ( 5.026804934256954738, 2.162974397647707825, 0.6633081500663459140 ) ) ;
#130798=CARTESIAN_POINT ( 'NONE',  ( 5.414259967653319627, -1.811767230315189048, 0.008324397547932599339 ) ) ;
#130800=CARTESIAN_POINT ( 'NONE',  ( 5.067565384200278800, 1.291559945344708638, 1.415018661930996569 ) ) ;
#130803=CARTESIAN_POINT ( 'NONE',  ( 6.104356062600288624, -0.6750377415852754082, -1.744797942764392928 ) ) ;
#130805=CARTESIAN_POINT ( 'NONE',  ( 5.441811508714582857, 1.250024229543914567, 1.378945535785504051 ) ) ;
#130807=CARTESIAN_POINT ( 'NONE',  ( 0.1626889888870358680, -1.668787113083155305, -0.8454427722031019332 ) ) ;
#130809=CARTESIAN_POINT ( 'NONE',  ( 1.270720652900014791, -0.3006520276036573902, -1.993892820393451615 ) ) ;
#130811=CARTESIAN_POINT ( 'NONE',  ( 2.455815469989936606, 0.5610288669116151317, -2.029897440403311215 ) ) ;
#130816=CARTESIAN_POINT ( 'NONE',  ( 1.318624316974380317, -0.7310098426952565953, -1.883032709213072975 ) ) ;
#130819=CARTESIAN_POINT ( 'NONE',  ( 2.899875653925917174, -0.6810940995312758650, 2.051530325002319799 ) ) ;
#130820=CARTESIAN_POINT ( 'NONE',  ( 6.883263157960367806, 7.629137130509066722, 2.653810918356712900 ) ) ;
#130827=CARTESIAN_POINT ( 'NONE',  ( 1.382659466718983543, -0.3261178763579902218, -2.167053615394160637 ) ) ;
#130829=CARTESIAN_POINT ( 'NONE',  ( 2.571453329723889958, 0.1116048768269807673, -2.259888279461387040 ) ) ;
#130836=CARTESIAN_POINT ( 'NONE',  ( 3.075218854414006220, 1.681628227459546432, -0.5517178611392310472 ) ) ;
#130838=CARTESIAN_POINT ( 'NONE',  ( 6.475609205405274515, 2.113627995098281254, -0.6344055572156809264 ) ) ;
#130841=CARTESIAN_POINT ( 'NONE',  ( 5.185172808627552143, 1.650094130669476522, 1.158673036085342112 ) ) ;
#130843=CARTESIAN_POINT ( 'NONE',  ( 2.131529507118444133, -1.219933349377068099, -1.418231869465089057 ) ) ;
#130844=CARTESIAN_POINT ( 'NONE',  ( 3.661042849074844785, 1.635018244968543977, -1.269851595989857085 ) ) ;
#130849=CARTESIAN_POINT ( 'NONE',  ( 1.582132296805271787, 0.9858968508435607125, 1.638552900098678045 ) ) ;
#130850=CARTESIAN_POINT ( 'NONE',  ( 2.980854556682940526, 1.846358069237159949, 0.6635599008937702603 ) ) ;
#130851=CARTESIAN_POINT ( 'NONE',  ( 1.229842044428463010, -1.821462008879136896, -0.8645945014377558469 ) ) ;
#130856=CARTESIAN_POINT ( 'NONE',  ( 6.415303688471941435, -0.2438443212883933120, 1.956177878852760177 ) ) ;
#130859=CARTESIAN_POINT ( 'NONE',  ( 1.880608475893473353, -0.5680388087716014001, -2.039528425668888811 ) ) ;
#130861=CARTESIAN_POINT ( 'NONE',  ( 3.525891238081061640, 2.020528833579691597, -0.4508363271973143682 ) ) ;
#130863=CARTESIAN_POINT ( 'NONE',  ( 5.490208796768200727, -0.5072484191241812823, -2.028029781992314096 ) ) ;
#130865=CARTESIAN_POINT ( 'NONE',  ( 4.735264887803245060, -1.668767028523497675, 0.7406363711058363553 ) ) ;
#130871=CARTESIAN_POINT ( 'NONE',  ( 6.071336392737415544, 0.1682094380959769098, -2.200428349287026908 ) ) ;
#130873=( BOUNDED_CURVE ( )  B_SPLINE_CURVE ( 3, ( #76962, #112746, #178758, #13023 ),
 .UNSPECIFIED., .F., .T. ) 
 B_SPLINE_CURVE_WITH_KNOTS ( ( 4, 4 ),
 ( 0.5000000000000018874, 1.000000000000000000 ),
 .UNSPECIFIED. ) 
 CURVE ( )  GEOMETRIC_REPRESENTATION_ITEM ( )  RATIONAL_B_SPLINE_CURVE ( ( 0.9999999999999974465, 0.3333333333333333703, 0.3333333333333358683, 1.000000000000000000 ) ) 
 REPRESENTATION_ITEM ( '' )  );
#130874=EDGE_CURVE ( 'NONE', #167392, #117162, #126065, .T. ) ;
#130876=CARTESIAN_POINT ( 'NONE',  ( 4.775979982822478931, 1.890921987351320777, -0.2842533987747336566 ) ) ;
#130883=CARTESIAN_POINT ( 'NONE',  ( 0.4679805871025365382, -1.733519288248483559, -0.6209854868195128219 ) ) ;
#130886=CARTESIAN_POINT ( 'NONE',  ( 5.219927230130699591, -0.9996001844756461363, -1.580852690948472361 ) ) ;
#130889=CARTESIAN_POINT ( 'NONE',  ( -0.2108831679770960255, -0.001785917861228669690, -1.896958272444612792 ) ) ;
#130892=CARTESIAN_POINT ( 'NONE',  ( 0.9187298884396404297, -1.430263011927451311, 1.354180262349208075 ) ) ;
#130893=CARTESIAN_POINT ( 'NONE',  ( 2.618767733003044551, 0.2496279305150179983, 2.000855661889962445 ) ) ;
#130898=CARTESIAN_POINT ( 'NONE',  ( 2.097856687836355150, -2.190910012095201420, 0.05558666267656967030 ) ) ;
#130908=ORIENTED_EDGE ( 'NONE', *, *, #84677, .F. ) ;
#130909=CARTESIAN_POINT ( 'NONE',  ( 5.214338956685347526, 1.703448749313410282, 0.6994016148276983591 ) ) ;
#130910=CARTESIAN_POINT ( 'NONE',  ( 2.227199469478642335, 1.799111979166287512, 0.9032904990664193390 ) ) ;
#130911=CARTESIAN_POINT ( 'NONE',  ( 2.759436883174094746, -2.292065780239035178, -0.1713596109048869109 ) ) ;
#130913=CARTESIAN_POINT ( 'NONE',  ( 1.938117168453708627, -1.000761817645494212, 1.568762535561243121 ) ) ;
#130915=CARTESIAN_POINT ( 'NONE',  ( 6.117437049485344502, 1.593764408019750389, 1.056661447057717362 ) ) ;
#130918=CARTESIAN_POINT ( 'NONE',  ( 5.372635804747151411, -0.05242855794247149731, -2.090268718351683930 ) ) ;
#130919=CARTESIAN_POINT ( 'NONE',  ( 3.326877442632663939, 0.04465521416292458912, 1.870282673472216439 ) ) ;
#130921=CARTESIAN_POINT ( 'NONE',  ( 6.181194517112824194, 1.274813594131599226, 1.328792456347933637 ) ) ;
#130925=CARTESIAN_POINT ( 'NONE',  ( 4.652814366283819503, -1.382804000779764619, 1.030830748262304253 ) ) ;
#130932=CARTESIAN_POINT ( 'NONE',  ( 4.997030173247643425, 0.3645372836193886967, 2.140096573681660619 ) ) ;
#130933=CARTESIAN_POINT ( 'NONE',  ( 3.264084022359412529, 0.8216391472936382945, 1.630427331384458833 ) ) ;
#130934=CARTESIAN_POINT ( 'NONE',  ( 1.533958681542445301, 1.164210590399002321, 1.578835587694705334 ) ) ;
#130935=CARTESIAN_POINT ( 'NONE',  ( 6.016841150788749815, 0.2099786098018930069, 2.106937748889408546 ) ) ;
#130936=CARTESIAN_POINT ( 'NONE',  ( 5.899983332490822185, -0.8214817842997054198, -2.140285636048167017 ) ) ;
#130940=CARTESIAN_POINT ( 'NONE',  ( 1.858217301831434964, 0.8087058978607818416, -1.960417502992222838 ) ) ;
#130946=CARTESIAN_POINT ( 'NONE',  ( 6.684450694706582929, 1.257157530024972658, -1.769884466434832548 ) ) ;
#130947=CARTESIAN_POINT ( 'NONE',  ( 6.983263157960363010, -0.009046620988246899253, 2.153544821522495489 ) ) ;
#130950=CARTESIAN_POINT ( 'NONE',  ( 2.069254833283964867, -1.714886923611224745, 1.411838272681579687 ) ) ;
#130952=CARTESIAN_POINT ( 'NONE',  ( -0.1335965759122420549, -0.1551069838626080166, -2.263292908747056131 ) ) ;
#130954=CARTESIAN_POINT ( 'NONE',  ( 5.875849835592577897, -2.013560656311346619, 0.4463529024570592751 ) ) ;
#130959=CARTESIAN_POINT ( 'NONE',  ( 0.2331563151865729544, 2.882199166944008795, -2.434502449063076224 ) ) ;
#130960=CARTESIAN_POINT ( 'NONE',  ( 4.194743914777058436, 1.481411246205705412, 1.093257649623424754 ) ) ;
#130962=CARTESIAN_POINT ( 'NONE',  ( 2.274029058727170316, -1.063862581237082550, 1.357477553621669442 ) ) ;
#130963=CARTESIAN_POINT ( 'NONE',  ( 0.4621254960020631519, -1.116205757145168231, 1.679226196708947016 ) ) ;
#130964=CARTESIAN_POINT ( 'NONE',  ( 1.512731952202387653, -2.162554957723664462, 0.7796286979407650586 ) ) ;
#130966=CARTESIAN_POINT ( 'NONE',  ( 1.898125948304218547, -0.7631055018291610370, 2.129926759817270199 ) ) ;
#130967=CARTESIAN_POINT ( 'NONE',  ( 3.985071343692931034, -0.2060594512321256011, -2.095964026187596918 ) ) ;
#130969=CARTESIAN_POINT ( 'NONE',  ( 2.055556868256277259, 1.765410544359298894, -0.1243799924028898551 ) ) ;
#130976=CARTESIAN_POINT ( 'NONE',  ( -0.004779673669230537214, -2.156333359934967220, -0.5329991086745686779 ) ) ;
#130977=CARTESIAN_POINT ( 'NONE',  ( 3.996163734398257894, -0.6867376513691285655, -2.081127982183433645 ) ) ;
#130980=CARTESIAN_POINT ( 'NONE',  ( 6.586587867412674768, -1.305319418013479948, 1.671791285998667442 ) ) ;
#130984=CARTESIAN_POINT ( 'NONE',  ( 5.924112389714110805, -2.104401743431310923, 0.2612745606217213856 ) ) ;
#130990=CARTESIAN_POINT ( 'NONE',  ( 6.603072989126265391, -0.3962418105841297167, 1.804722624154910360 ) ) ;
#130994=CARTESIAN_POINT ( 'NONE',  ( 2.120290817172516551, 0.0009401564262049438847, 1.740626721131139698 ) ) ;
#130997=CARTESIAN_POINT ( 'NONE',  ( 0.5726126529861443881, 1.355618539282506640, -1.418395753018865113 ) ) ;
#131000=CARTESIAN_POINT ( 'NONE',  ( 6.086834708314957432, -0.3123483334277510348, -2.138898144987111838 ) ) ;
#131003=CARTESIAN_POINT ( 'NONE',  ( 5.629794960336353071, -1.368038101806166029, -1.673757646710342550 ) ) ;
#131007=CARTESIAN_POINT ( 'NONE',  ( 5.606699263565281477, 1.494642942781895023, -1.285547057225975509 ) ) ;
#131008=CARTESIAN_POINT ( 'NONE',  ( 5.114428339645875177, 0.5428861372157275378, -1.646692512460482982 ) ) ;
#131010=CARTESIAN_POINT ( 'NONE',  ( 2.261505105119133052, 2.148611799745976381, -0.4309092228176118478 ) ) ;
#131011=CARTESIAN_POINT ( 'NONE',  ( 3.171242727813221585, -2.131442559959194849, -0.8847066026466602340 ) ) ;
#131012=CARTESIAN_POINT ( 'NONE',  ( 4.288392841435205938, -2.037809284099707074, -0.3060936983758227870 ) ) ;
#131013=CARTESIAN_POINT ( 'NONE',  ( 1.025216207372595223, -1.231406509999972254, -1.501593997598904995 ) ) ;
#131017=CARTESIAN_POINT ( 'NONE',  ( 4.359710196644346780, -1.641147893522959089, -1.343014508298406628 ) ) ;
#131019=CARTESIAN_POINT ( 'NONE',  ( 2.742814741689561853, 2.006446121045248887, -0.2004354718553730264 ) ) ;
#131021=CARTESIAN_POINT ( 'NONE',  ( 5.016741729952475914, 1.524926965779101140, -1.595359541877178877 ) ) ;
#131023=B_SPLINE_CURVE_WITH_KNOTS ( 'NONE', 3,
 ( #188007, #40721, #7109, #59082, #75339, #106827, #156605, #172857, #90540, #58019, #141456, #39633, #124183, #190146, #173939, #207463, #125242, #191202, #100632, #166709, #87320, #153388, #192267, #160862, #80678, #27649, #92682, #29800, #12456, #130567, #43928, #42867, #26579, #111104, #113246, #179251, #158727, #30874, #127379, #60150, #62290, #112181, #10324, #146769, #212786, #126307, #128450, #177110, #11388, #46059, #28726, #64423, #76398, #14582, #142507, #208515, #93748, #95885, #94812, #108975, #161939, #194417, #210664, #78531, #110043, #77466, #193351, #178185, #176055, #96953, #195495, #144649, #174994, #13532, #159786, #143585, #163001, #209578, #44995, #145721, #61223, #79602, #211720, #63356, #129515, #47131, #69726, #183492, #32987, #67581, #149948, #50307, #81737, #165118, #132654, #35101, #99064, #1517, #102249, #182416, #166181, #117501, #133726, #196557, #48200, #100119, #147818, #17769, #444, #199732, #83858, #164069, #115371, #3647, #51378, #101172, #31931, #167261, #168323, #16710, #18846, #84931, #151020, #82795, #148869, #118566, #36172, #114312, #19918, #98013, #213837, #65455, #34046, #2587, #134780, #68657, #200789, #180311, #52440, #131605, #49250, #181363, #184551, #198658, #86003, #66512, #197606, #152077, #116425, #15648, #72935, #135830, #87066, #203986, #172600, #55633, #136899, #154209, #171514, #23108, #137965, #139039, #173685, #202928, #106573, #24179, #104395, #121789, #54570, #90282, #187756, #88139, #39385, #156351, #205064, #7935, #74024, #105481, #89223, #155276, #6856, #9013, #120718, #201855, #119636, #56706, #206140, #57771, #185620, #123932, #5779, #153138, #71858, #4712, #122873, #186691, #189900, #140114, #188834, #53499, #40470, #41542, #170442, #107656, #25261, #91362, #37252, #157422, #103322, #169384, #38319, #20969, #70786, #22030, #62050, #126054, #160607, #28472, #143331, #174750, #43679, #92437, #26323, #45813, #208268, #109798, #158476, #79358, #210408, #94564, #162759, #75089, #193097, #10076, #110852, #93497, #12209, #44746, #42614, #59901, #96710, #141201, #129273, #78280, #112994, #207212, #128205, #195246, #194166, #111933, #175805, #27397, #211471, #46882, #58836, #179007, #124991, #76152, #142256, #60971, #127127, #30621, #209324, #159537, #190950, #11135, #192016, #95640, #77212, #177935, #176859, #161691, #144408, #29548, #13285, #145476, #63105, #108724, #14333, #180063, #82541, #195, #184299, #134535, #66264, #67331, #17521, #149690, #165936, #52187, #81490, #199477, #51121, #197359, #132412, #147567, #117244, #198414, #181116, #50058, #183244, #163820, #116179, #118313, #213588, #64181, #1273, #182164, #102001, #15399, #80423, #212541, #148629, #84683, #150770, #130322, #2332, #33795, #65213, #68408, #167011, #35924, #97762, #99873, #83609, #49002, #133475, #34848, #146522, #196312, #200541, #47956, #114071, #131364, #100923, #18603, #31686, #115120, #32735, #98815, #164867, #16461, #172597, #23104, #105478, #187753, #58832, #6853, #56703, #39382, #92431, #9009, #107651, #175800, #88136, #206137, #171511, #123928, #106569, #173681, #57767, #72932, #109792, #157418, #25257, #137962, #91357, #59896, #122870, #124987, #174745, #71854, #189896, #203983, #155272, #154206, #90279, #188831, #41538, #75084, #26319, #74020, #140111, #158471, #10071, #141197, #5775 ),
 .UNSPECIFIED., .F., .F.,
 ( 4, 1, 1, 1, 1, 1, 1, 1, 1, 1, 1, 1, 1, 1, 1, 1, 1, 1, 1, 1, 1, 1, 1, 1, 1, 1, 1, 1, 1, 1, 1, 1, 1, 1, 1, 1, 1, 1, 1, 1, 1, 1, 1, 1, 1, 1, 1, 1, 1, 1, 1, 1, 1, 1, 1, 1, 1, 1, 1, 1, 1, 1, 1, 1, 1, 1, 1, 1, 1, 1, 1, 1, 1, 1, 1, 1, 1, 1, 1, 1, 1, 1, 1, 1, 1, 1, 1, 1, 1, 1, 1, 1, 1, 1, 1, 1, 1, 1, 1, 1, 1, 1, 1, 1, 1, 1, 1, 1, 1, 1, 1, 1, 1, 1, 1, 1, 1, 1, 1, 1, 1, 1, 1, 1, 1, 1, 1, 1, 1, 1, 1, 1, 1, 1, 1, 1, 1, 1, 1, 1, 1, 1, 1, 1, 1, 1, 1, 1, 1, 1, 1, 1, 1, 1, 1, 1, 1, 1, 1, 1, 1, 1, 1, 1, 1, 1, 1, 1, 1, 1, 1, 1, 1, 1, 1, 1, 1, 1, 1, 1, 1, 1, 1, 1, 1, 1, 1, 1, 1, 1, 1, 1, 1, 1, 1, 1, 1, 1, 1, 1, 1, 1, 1, 1, 1, 1, 1, 1, 1, 1, 1, 1, 1, 1, 1, 1, 1, 1, 1, 1, 1, 1, 1, 1, 1, 1, 1, 1, 1, 1, 1, 1, 1, 1, 1, 1, 1, 1, 1, 1, 1, 1, 1, 1, 1, 1, 1, 1, 1, 1, 1, 1, 1, 1, 1, 1, 1, 1, 1, 1, 1, 1, 1, 1, 1, 1, 1, 1, 1, 1, 1, 1, 1, 1, 1, 1, 1, 1, 1, 1, 1, 1, 1, 1, 1, 1, 1, 1, 1, 1, 1, 1, 1, 1, 1, 1, 1, 1, 1, 1, 1, 1, 1, 1, 1, 1, 1, 1, 1, 1, 1, 1, 1, 1, 1, 1, 1, 1, 1, 1, 1, 1, 1, 1, 1, 1, 1, 1, 1, 1, 1, 1, 1, 1, 1, 1, 1, 1, 1, 1, 1, 1, 1, 1, 1, 1, 1, 1, 1, 1, 1, 1, 1, 1, 1, 1, 1, 1, 1, 1, 1, 1, 1, 1, 1, 1, 1, 1, 1, 1, 1, 1, 1, 1, 1, 1, 1, 1, 1, 1, 1, 1, 1, 1, 4 ),
 ( 0.000000000000000000, 0.002599909708945224215, 0.005208776875251038344, 0.007813105021672143990, 0.01041684075506122895, 0.01302033053878596733, 0.01562516449037322508, 0.01822901888718816976, 0.02083333248856494152, 0.02343767784666880849, 0.02604151204071371642, 0.02864616705684025488, 0.03124974664057501156, 0.03385445107693609706, 0.03645811663825353210, 0.03906264587105176544, 0.04166673705245293319, 0.04427082116499847508, 0.04687535697974040683, 0.04947901875943551409, 0.05208372524935509645, 0.05468730636643894666, 0.05729195276349181160, 0.05989578571700067411, 0.06250012971910297310, 0.06510448174046053194, 0.06770830932160050442, 0.07031296016926287529, 0.07291653972921435800, 0.07552124384959360559, 0.07812490789241745281, 0.08072943556986492131, 0.08333352577934262373, 0.08593760861062926804, 0.08854214333088818167, 0.09114580385899402615, 0.09375050919907033931, 0.09635408915385039463, 0.09895873428887830281, 0.1015625661591952889, 0.1041669088510773916, 0.1067712598504420435, 0.1093750861808121810, 0.1119797359579501050, 0.1145833143474069837, 0.1171880172914337714, 0.1197916802446672702, 0.1223962066585842084, 0.1250002958591681090, 0.1276043774339237491, 0.1302089111537957367, 0.1328125705047451810, 0.1354172747579587832, 0.1380208536162275679, 0.1406254975582941213, 0.1432293284131295197, 0.1458336698625422867, 0.1484380199076493767, 0.1510418450546419100, 0.1536464938294531402, 0.1562500711155297428, 0.1588547729514310503, 0.1614584348822658832, 0.1640629601007041471, 0.1666670483599762276, 0.1692711287458052438, 0.1718756615333107141, 0.1744793197742946778, 0.1770840230088624179, 0.1796876008377196188, 0.1822922436549848091, 0.1848960735616705098, 0.1875004138364584350, 0.1901047629951247708, 0.1927085870260826783, 0.1953132348667029061, 0.1979168111164897881, 0.2005215119124719170, 0.2031251728880697216, 0.2057296969790492203, 0.2083337843645647058, 0.2109378636290424602, 0.2135423955521746908, 0.2161460527503557827, 0.2187507550344668650, 0.2213543319009846355, 0.2239589736615800464, 0.2265628026874214052, 0.2291671418554001027, 0.2317714901954165685, 0.2343753131776551424, 0.2369799601521939414, 0.2395835354327550959, 0.2421882352569974250, 0.2447918953444941648, 0.2473964183760076208, 0.2500005049552969649, 0.2526045831659717300, 0.2552091142926994904, 0.2578127705152143956, 0.2604174719170327390, 0.2630210478882585856, 0.2656256886602897938, 0.2682295168725681855, 0.2708338550015275126, 0.2734382025906618163, 0.2760420245914711468, 0.2786466707680146371, 0.2812502451463897990, 0.2838549440670474211, 0.2864586033335557724, 0.2890631253735708728, 0.2916672112141422968, 0.2942712884385379479, 0.2968758188368077477, 0.2994794741507696423, 0.3020841747384366283, 0.3046877498813952978, 0.3072923897329448151, 0.3098962171989202430, 0.3125005543566263810, 0.3151049012626256918, 0.3177087223492732204, 0.3203133677958864278, 0.3229169413390938770, 0.3255216394243000688, 0.3281252979369121969, 0.3307298190533745630, 0.3333339042227165261, 0.3359379805283350118, 0.3385425102660742369, 0.3411461647385755636, 0.3437508645802123675, 0.3463544389619092612, 0.3489590779610384774, 0.3515629047479519320, 0.3541672410021501904, 0.3567715872927431642, 0.3593754075324762653, 0.3619800523172059803, 0.3645836250922447341, 0.3671883224101137877, 0.3697919802359038166, 0.3723965004967392245, 0.3750005850623230885, 0.3776046605166471504, 0.3802091896617659783, 0.3828128433598806946, 0.3854175425235913388, 0.3880211162110140388, 0.3906257544257662473, 0.3932295806008425099, 0.3958339160192597128, 0.3984382617621595180, 0.4010420812222079689, 0.4036467254130849946, 0.4062502974869375283, 0.4088549941055670267, 0.4114586513115932598, 0.4140631707847102772, 0.4166672548139925825, 0.4192713294844879757, 0.4218758581048823730, 0.4244795110956688933, 0.4270842096495421902, 0.4296877827096635682, 0.4322924202080664635, 0.4348962458385162155, 0.4375005804888632555, 0.4401049257517701263, 0.4427087444993486054, 0.4453133881643903114, 0.4479169596040251111, 0.4505216555914985932, 0.4531253122448062887, 0.4557298309980991058, 0.4583339145585244578, 0.4609379885126426157, 0.4635425166761967808, 0.4661461690266998081, 0.4687508670388120247, 0.4713544395385928509, 0.4739590763886608604, 0.4765629015416836811, 0.4791672354916582388, 0.4817715803422617515, 0.4843753984445725025, 0.4869800416517858221, 0.4895836125241597725, 0.4921883079485492862, 0.4947919641161733773, 0.4973964822175238609, 0.5000005653765271507, 0.5026046386817077938, 0.5052091664562964324, 0.5078128182335502894, 0.5104175157719683664, 0.5130210877783591972, 0.5156257240480961457, 0.5182295487908826770, 0.5208338821081714975, 0.5234382266141532902, 0.5260420441383883983, 0.5286466869557716608, 0.5312502573278325979, 0.5338549522572011430, 0.5364586080061681805, 0.5390631255234488162, 0.5416672083484578293, 0.5442712810721315186, 0.5468758085256230084, 0.5494794597966533578, 0.5520841569294364648, 0.5546877285093810839, 0.5572923642667827471, 0.5598961886665174692, 0.5625005214187991376, 0.5651048656478350196, 0.5677086826611791315, 0.5703133251567252815, 0.5729168950954143247, 0.5755215895978186280, 0.5781252449951498340, 0.5807297619962258350, 0.5833338445546641937, 0.5859379167642547737, 0.5885424439645127181, 0.5911460947963396162, 0.5937507915915425372, 0.5963543628119793993, 0.5989589981250363904, 0.6015628222488997867, 0.6041671545038470592, 0.6067714985236103420, 0.6093753150932430529, 0.6119799573349418154, 0.6145835269071964202, 0.6171882210506893784, 0.6197918761634028106, 0.6223963927161352272, 0.6250004750754242222, 0.6276045468383509851, 0.6302090738532378777, 0.6328127243128783830, 0.6354174208385534595, 0.6380209917664191321, 0.6406256267031188445, 0.6432294506182901772, 0.6458337824435727015, 0.6484381263217364744, 0.6510419425148348260, 0.6536465845706755928, 0.6562501538434313275, 0.6588548476960643940, 0.6614585025911776661, 0.6640630187634258830, 0.6666671009909873602, 0.6692711723746683772, 0.6718756992720475996, 0.6744793494265174383, 0.6770840457507175669, 0.6796876164529486175, 0.6822922510812780006, 0.6848960748549377531, 0.6875004063182246217, 0.6901047501224634173, 0.6927085660062048955, 0.6953132079441787239, 0.6979167769843723779, 0.7005214706141982273, 0.7031251253587310623, 0.7057296412183544643, 0.7083337233816132672, 0.7109377944534676086, 0.7135423213012055399, 0.7161459712175226588, 0.7187506674083037339, 0.7213542379518396164, 0.7239588723397878400, 0.7265626960391206035, 0.7291670272080824633, 0.7317713710060759214, 0.7343751866476402324, 0.7369798285357428425, 0.7395833974103146469, 0.7421880908853900616, 0.7447917455463664016, 0.7473962611612280371, 0.7500003433276148934, 0.7526044141550642941, 0.7552089410210337528, 0.7578125907662203176, 0.7604172868916432293, 0.7630208573434285046, 0.7656254915589897347, 0.7682293152511859846, 0.7708336461934980344, 0.7734379900529331220, 0.7760418055195050790, 0.7786464474257392965, 0.7812500162016354777, 0.7838547095900232353, 0.7864583642344741277, 0.7890628796724428184, 0.7916669619093961163, 0.7942710325598689725, 0.7968755595119511037, 0.7994792091530360523, 0.8020839052811703507, 0.8046874757081575735, 0.8072921098193328593, 0.8098959335715922858, 0.8125002643549369408, 0.8151046083435100620, 0.8177084237022821389, 0.8203130656946604482, 0.8229166344388356702, 0.8255213278086077633, 0.8281249825035741363, 0.8307294978325265866, 0.8333335802074958165, 0.8359376507484286289, 0.8385421778545157911, 0.8411458274585372763, 0.8437505236574627254, 0.8463540941266142204, 0.8489587282014147140, 0.8515625520809478877, 0.8541668827730166669, 0.8567712269584367712, 0.8593750422766117669, 0.8619796844231587540, 0.8645832532025788941, 0.8671879466218186394, 0.8697916014343529678, 0.8723961167221769841, 0.8750001993026245151, 0.8776042698014647758, 0.8802087971294628721, 0.8828124467634709260, 0.8854171431012803906, 0.8880207136795719158, 0.8906253477860208712, 0.8932291718600525732, 0.8958335025285494302, 0.8984378469785403443, 0.9010416623233333810, 0.9036463046920883979, 0.9062498735737328781, 0.9088545671105374701, 0.9114582221077071056, 0.9140627374223044832, 0.9166668202757080053, 0.9192708907999164181, 0.9218754184177497812, 0.9244790681488107564, 0.9270837646936044285, 0.9296873354480212903, 0.9322919696541906998, 0.9348957939899811276, 0.9375001247025137596, 0.9401044694846933947, 0.9427082849236875228, 0.9453129275835465695, 0.9479164966330613229, 0.9505211903504858784, 0.9531248456066239161, 0.9557293610412391782, 0.9583334441921064206, 0.9609375147049603605, 0.9635420428945489224, 0.9661456931510739032, 0.9687503890924937799, 0.9713539588735070618, 0.9739585961357111188, 0.9765624261165479769, 0.9791667493207181217, 0.9817710620974646751, 0.9843748983037424738, 0.9869797303524157073, 0.9895832060093603388, 0.9921869237806116848, 0.9947912468131487884, 0.9974000922265050528, 0.9999999999999998890 ),
 .UNSPECIFIED. ) ;
#131030=CARTESIAN_POINT ( 'NONE',  ( 4.539950165727339559, 0.8829098278404916567, -1.862335138179547211 ) ) ;
#131034=CARTESIAN_POINT ( 'NONE',  ( 3.563153132451855054, -1.649810593967064865, 1.164694042050371303 ) ) ;
#131039=CARTESIAN_POINT ( 'NONE',  ( 3.080987681966301572, -0.1499786273361273514, -2.055480798767507444 ) ) ;
#131042=CARTESIAN_POINT ( 'NONE',  ( -0.1411974294642124317, 6.947781193150396994, -2.495311724135263809 ) ) ;
#131044=CARTESIAN_POINT ( 'NONE',  ( 1.271164299617353333, 1.095269041189731452, 1.479763895647051353 ) ) ;
#131045=CARTESIAN_POINT ( 'NONE',  ( 0.1359762249627448627, -2.107041879058098033, 0.9415998322012062438 ) ) ;
#131047=CARTESIAN_POINT ( 'NONE',  ( 3.145949958485740883, 0.7812230816454240889, -2.015650884352723882 ) ) ;
#131050=CARTESIAN_POINT ( 'NONE',  ( 1.938685741270998797, -1.555697844595272716, 1.282991390469834458 ) ) ;
#131052=CARTESIAN_POINT ( 'NONE',  ( 2.601245504928787700, 1.085180258111384077, -2.026094289238103752 ) ) ;
#131055=CARTESIAN_POINT ( 'NONE',  ( 4.680523324745738734, -1.912062325676016306, -0.4798145647967356764 ) ) ;
#131056=CARTESIAN_POINT ( 'NONE',  ( 4.592982591267942283, 1.756852934926198317, 0.9896879400849432074 ) ) ;
#131060=CARTESIAN_POINT ( 'NONE',  ( 5.725249284967181218, -0.05305106314347144553, 2.105570132020935237 ) ) ;
#131061=CARTESIAN_POINT ( 'NONE',  ( 6.057099581687969803, 1.694805161836069107, -1.188877858866774107 ) ) ;
#131064=CARTESIAN_POINT ( 'NONE',  ( 6.639320575229244348, 1.270172395628932360, 2.119701008677194132 ) ) ;
#131065=CARTESIAN_POINT ( 'NONE',  ( 5.818619510638624703, -0.7308962487734929070, -1.883076464014792117 ) ) ;
#131067=CARTESIAN_POINT ( 'NONE',  ( 2.913035970020665388, 1.671030660360285802, -1.591803581779531074 ) ) ;
#131068=CARTESIAN_POINT ( 'NONE',  ( 1.745062578162811073, -0.2986309630071918853, -2.040702096407704058 ) ) ;
#131076=CARTESIAN_POINT ( 'NONE',  ( 4.615793470729397718, 0.4799340867196815741, -2.117318520224883205 ) ) ;
#131079=CARTESIAN_POINT ( 'NONE',  ( 3.421284184235491743, -1.099380227797893905, -1.476844927387373163 ) ) ;
#131081=CARTESIAN_POINT ( 'NONE',  ( 5.407841436338867602, -0.9846607899807978681, -1.957994596084790206 ) ) ;
#131083=CARTESIAN_POINT ( 'NONE',  ( 6.139586942761116717, -1.633760600410700592, -1.565427815648293031 ) ) ;
#131088=CARTESIAN_POINT ( 'NONE',  ( 6.919227944281516329, -0.1317407762830881124, 1.740281130587753688 ) ) ;
#131090=CARTESIAN_POINT ( 'NONE',  ( 4.442045433088864570, -1.240138855636420567, -1.585653348822992026 ) ) ;
#131092=CARTESIAN_POINT ( 'NONE',  ( 2.696425475562960195, -2.100245048574858497, -0.1560501473716560672 ) ) ;
#131093=CARTESIAN_POINT ( 'NONE',  ( 1.845192132668025176, 0.3254238344292461060, -1.887580106770263999 ) ) ;
#131095=CARTESIAN_POINT ( 'NONE',  ( 2.840245056987787287, -1.014795158497614036, 1.687856822838776916 ) ) ;
#131096=CARTESIAN_POINT ( 'NONE',  ( 0.6197280442463182215, -0.9970892369244135356, -1.582582228963416160 ) ) ;
#131097=CARTESIAN_POINT ( 'NONE',  ( 0.9241798626423223251, 0.9638202082158978667, 1.708698881219716137 ) ) ;
#131098=CARTESIAN_POINT ( 'NONE',  ( 0.6680393924826667496, 1.910109291395128972, -0.09634788558426229943 ) ) ;
#131104=CARTESIAN_POINT ( 'NONE',  ( 6.737176827083626307, -0.09545985418329960837, -2.068160202195384656 ) ) ;
#131107=CARTESIAN_POINT ( 'NONE',  ( 1.135311898753359472, -0.04898221611688948623, -2.069941200615910581 ) ) ;
#131112=CARTESIAN_POINT ( 'NONE',  ( 5.233110275169113201, 1.959380141031796585, 0.8112103084707968925 ) ) ;
#131117=CARTESIAN_POINT ( 'NONE',  ( 6.197705743426439540, -1.420020466879829302, -1.353909852041992767 ) ) ;
#131119=CARTESIAN_POINT ( 'NONE',  ( 4.780624950969222020, -1.977747464269607347, 0.3905396900540994420 ) ) ;
#131121=CARTESIAN_POINT ( 'NONE',  ( 3.397576204589338733, -1.886455135561039942, 0.3326623127566808447 ) ) ;
#131123=CARTESIAN_POINT ( 'NONE',  ( 1.909981697816802049, -1.036543071415759298, -1.930953618257096993 ) ) ;
#131124=CARTESIAN_POINT ( 'NONE',  ( 3.462029368274913477, 0.8381641302350505418, 1.672297462726477946 ) ) ;
#131126=CARTESIAN_POINT ( 'NONE',  ( 4.693612458567416823, 1.876924737948972188, -0.7285200738881071336 ) ) ;
#131129=CARTESIAN_POINT ( 'NONE',  ( 5.448860601978118723, -1.914358274237770496, -0.9046119500179942152 ) ) ;
#131131=CARTESIAN_POINT ( 'NONE',  ( 1.874669627338154454, -0.1056657526060876956, -2.088216114563210102 ) ) ;
#131133=CARTESIAN_POINT ( 'NONE',  ( 0.4458014021226979207, 1.719615392401403708, 0.1342584403209358679 ) ) ;
#131143=CARTESIAN_POINT ( 'NONE',  ( 1.242487904981701252, 1.745646600027310980, 0.4836494453460266074 ) ) ;
#131147=CARTESIAN_POINT ( 'NONE',  ( 6.539320575229256249, 4.699150603835311912, 2.459441311396874941 ) ) ;
#131151=CARTESIAN_POINT ( 'NONE',  ( 2.681907113330802339, -1.068898278170841598, -1.523273593526828673 ) ) ;
#131153=CARTESIAN_POINT ( 'NONE',  ( 0.2806859451011362583, 1.592165405827509650, -1.064819009530016958 ) ) ;
#131154=CARTESIAN_POINT ( 'NONE',  ( 6.651400849050447484, -1.547811450530303778, -1.146644766597894938 ) ) ;
#131155=CARTESIAN_POINT ( 'NONE',  ( 5.934052368846653991, 1.230181698326970663, 1.665117723180092213 ) ) ;
#131160=CARTESIAN_POINT ( 'NONE',  ( 4.592606226310515183, 1.930599660924517957, 0.3882996684868595394 ) ) ;
#131161=CARTESIAN_POINT ( 'NONE',  ( 1.752743329737327826, 2.097873456429504735, 0.3079802404963858931 ) ) ;
#131166=CARTESIAN_POINT ( 'NONE',  ( 6.404242042726283834, 1.626525233829802408, -1.468802942141099299 ) ) ;
#131168=CARTESIAN_POINT ( 'NONE',  ( 4.225552302291880835, -1.843726210754624173, 0.5582998813679838079 ) ) ;
#131171=CARTESIAN_POINT ( 'NONE',  ( 0.6982365061397632910, -0.7907169553198112322, 2.060542492664858560 ) ) ;
#131175=( LENGTH_UNIT ( ) NAMED_UNIT ( * ) SI_UNIT ( .MILLI., .METRE. ) );
#131177=CARTESIAN_POINT ( 'NONE',  ( 6.420757345757475143, -1.395243968761919362, 1.390232514205336001 ) ) ;
#131178=CARTESIAN_POINT ( 'NONE',  ( 1.065847985493496797, -1.230715344637549391, 1.502334450403658206 ) ) ;
#131179=CARTESIAN_POINT ( 'NONE',  ( 6.380222486609858912, -0.2913964880489598452, 2.279815279960105467 ) ) ;
#131181=CARTESIAN_POINT ( 'NONE',  ( 4.908966729185230804, -1.496192014157717631, 1.106395937811145203 ) ) ;
#131188=CARTESIAN_POINT ( 'NONE',  ( 1.452940684028160234, -1.882004992133184285, -1.122693704575933316 ) ) ;
#131193=CARTESIAN_POINT ( 'NONE',  ( 1.488595654847742145, -0.2661386877833261111, -1.806066791206423439 ) ) ;
#131196=CARTESIAN_POINT ( 'NONE',  ( 6.509000000000013664, 7.052434016701248254, 2.698154332336550887 ) ) ;
#131198=CARTESIAN_POINT ( 'NONE',  ( 6.516225534515442952, -0.8655890497146904172, -1.607451055071248636 ) ) ;
#131199=CARTESIAN_POINT ( 'NONE',  ( 4.680490258543752446, 1.210089798712219000, -1.543956201849092436 ) ) ;
#131202=CARTESIAN_POINT ( 'NONE',  ( 4.195009555701286530, 1.760677850468267414, 1.304791629949946019 ) ) ;
#131204=CARTESIAN_POINT ( 'NONE',  ( 6.609000000000038177, 2.443064466336189788, 2.382833824652215160 ) ) ;
#131205=CARTESIAN_POINT ( 'NONE',  ( 2.448173108494243078, -0.8891298726186761536, 1.869765896676472083 ) ) ;
#131209=CARTESIAN_POINT ( 'NONE',  ( 3.375889859521400194, -0.4501408176796182770, -2.254053602989118499 ) ) ;
#131213=CARTESIAN_POINT ( 'NONE',  ( 6.720655732516652492, 7.053303974100803231, 2.424416723604695179 ) ) ;
#131215=CARTESIAN_POINT ( 'NONE',  ( 3.380740619721524620, 1.755215216048062521, -0.8311813869739079763 ) ) ;
#131218=CARTESIAN_POINT ( 'NONE',  ( 3.673993457511487204, 1.897360377298975553, -0.2389773157873422427 ) ) ;
#131220=CARTESIAN_POINT ( 'NONE',  ( 5.262619041473771020, -1.246969283750315460, 1.191858809209481285 ) ) ;
#131221=CARTESIAN_POINT ( 'NONE',  ( 3.907435596788138010, -1.928258004016227378, 0.5899861904685861358 ) ) ;
#131222=CARTESIAN_POINT ( 'NONE',  ( 4.764420831138592938, 2.145307606383870969, -0.8259888504972175971 ) ) ;
#131224=CARTESIAN_POINT ( 'NONE',  ( 0.2587985324217950689, 0.8487602207661277820, 2.037339956011212649 ) ) ;
#131226=CARTESIAN_POINT ( 'NONE',  ( 5.923074920120706466, -0.04171666621876138348, 1.769427632397130079 ) ) ;
#131228=CARTESIAN_POINT ( 'NONE',  ( 1.992491592054939531, -0.6139151001693385901, -2.208460184710277385 ) ) ;
#131229=CARTESIAN_POINT ( 'NONE',  ( 0.7787878715554141795, 1.165832476461704292, 1.292284986363402055 ) ) ;
#131234=CARTESIAN_POINT ( 'NONE',  ( 1.820994678651502330, -1.536134449795123480, 1.534618252339227329 ) ) ;
#131235=CARTESIAN_POINT ( 'NONE',  ( 1.885954221117658092, -2.015980662343511032, 0.05432778586660082232 ) ) ;
#131238=CARTESIAN_POINT ( 'NONE',  ( 5.285741052758629266, 1.295255816434317753, 1.426247342039884014 ) ) ;
#131241=CARTESIAN_POINT ( 'NONE',  ( 2.426306324659221136, -2.196553987802750907, 0.3307981192552343352 ) ) ;
#131248=CARTESIAN_POINT ( 'NONE',  ( 5.108843383178156117, -0.2480618215125965365, 1.722539690991312877 ) ) ;
#131249=CARTESIAN_POINT ( 'NONE',  ( 3.965250677406896962, 1.681448970545707855, 1.010551734412237668 ) ) ;
#131253=CARTESIAN_POINT ( 'NONE',  ( 4.622535034725678393, 1.396675434457357756, -1.779734664907887343 ) ) ;
#131254=CARTESIAN_POINT ( 'NONE',  ( 1.012259994385706019, 2.060384570222949741, -0.09942193159017187476 ) ) ;
#131257=CARTESIAN_POINT ( 'NONE',  ( 2.395744609331447172, 1.748901261223069437, 1.435362524944477025 ) ) ;
#131260=CARTESIAN_POINT ( 'NONE',  ( 2.389737607000471442, -0.8038258883538218491, 1.689183408448757362 ) ) ;
#131261=CARTESIAN_POINT ( 'NONE',  ( 1.845948222207854483, 0.2957656664513158007, -1.708526460754287157 ) ) ;
#131262=CARTESIAN_POINT ( 'NONE',  ( 5.196902890030515643, 1.791362914573800369, 1.262263373074036688 ) ) ;
#131263=CARTESIAN_POINT ( 'NONE',  ( 0.1830476545506658226, -2.141193618969746471, -0.5335393285625378290 ) ) ;
#131264=CARTESIAN_POINT ( 'NONE',  ( 3.696290335837215668, -2.159122111672501454, -0.1082323872379290647 ) ) ;
#131265=CARTESIAN_POINT ( 'NONE',  ( 4.136618238866495822, -1.688923885309162376, 0.9583718017313649362 ) ) ;
#131268=CARTESIAN_POINT ( 'NONE',  ( 0.5312500000000220934, -0.7852924748305555314, -1.895863743164076576 ) ) ;
#131270=CARTESIAN_POINT ( 'NONE',  ( -0.1048463755018592264, -0.8645036352170620830, -1.819965476435807306 ) ) ;
#131272=CARTESIAN_POINT ( 'NONE',  ( 5.203750078570229753, 1.864167652161516031, 0.7691231355932278690 ) ) ;
#131276=CARTESIAN_POINT ( 'NONE',  ( 2.262075381241589245, 0.7800679334904643270, 1.650788133108482825 ) ) ;
#131285=CARTESIAN_POINT ( 'NONE',  ( 6.586581121665559202, -1.240835222743674526, 1.594039115436784337 ) ) ;
#131286=CARTESIAN_POINT ( 'NONE',  ( 0.9266185682500321930, -0.9568284065921551784, -1.892426592148554132 ) ) ;
#131290=CARTESIAN_POINT ( 'NONE',  ( 6.209851105358469958, -2.045643633555578766, 0.2495701479476707119 ) ) ;
#131291=CARTESIAN_POINT ( 'NONE',  ( 5.115861365725079324, 0.1511377038382749338, 2.010826595755777824 ) ) ;
#131298=CARTESIAN_POINT ( 'NONE',  ( 5.501327308730313170, 1.985796898448642933, 0.3474119236192701465 ) ) ;
#131299=CARTESIAN_POINT ( 'NONE',  ( 4.523293815724619193, -1.134750198001058585, -1.449786353205910538 ) ) ;
#131300=CARTESIAN_POINT ( 'NONE',  ( -0.02319159430949797526, 7.629137130509074716, -2.410989586153565067 ) ) ;
#131301=CARTESIAN_POINT ( 'NONE',  ( 3.141587237543626454, -2.035091569058588679, 1.088060180353218165 ) ) ;
#131303=CARTESIAN_POINT ( 'NONE',  ( 6.468072252983536607, 1.105043713804385153, 1.857642994352682653 ) ) ;
#131305=CARTESIAN_POINT ( 'NONE',  ( 1.645936167706591569, 0.6108386606893880799, 1.843543891229272313 ) ) ;
#131312=CARTESIAN_POINT ( 'NONE',  ( 3.221420234344949840, -1.803205065257794004, 0.4975683872451354683 ) ) ;
#131313=CARTESIAN_POINT ( 'NONE',  ( 1.670022949053862948, 1.907054940702714863, -0.1439945843566131367 ) ) ;
#131316=CARTESIAN_POINT ( 'NONE',  ( 2.491098823239074278, -0.3784457004711218042, -2.174036671264235387 ) ) ;
#131317=CARTESIAN_POINT ( 'NONE',  ( 6.883263157960366918, 3.696842586722656865, 2.460469087180997327 ) ) ;
#131321=CARTESIAN_POINT ( 'NONE',  ( 1.106637804720354668, 1.495658270405418877, -1.284366697391533529 ) ) ;
#131322=CARTESIAN_POINT ( 'NONE',  ( 0.8510977523443744586, 0.6731378975963157041, 2.207243034677327298 ) ) ;
#131323=CARTESIAN_POINT ( 'NONE',  ( 1.135121963537696566, -0.04462593873827064989, -1.961518378280776354 ) ) ;
#131324=CARTESIAN_POINT ( 'NONE',  ( 5.295784840496287060, -1.454754056633072778, -1.462402424637335052 ) ) ;
#131331=CARTESIAN_POINT ( 'NONE',  ( 0.9894204570943666566, 0.1578702891864954827, 2.165348367497366144 ) ) ;
#131332=CARTESIAN_POINT ( 'NONE',  ( 6.005383971424570255, -1.826508537601937432, 0.2321369796495567073 ) ) ;
#131335=CARTESIAN_POINT ( 'NONE',  ( 1.282252794574537447, -1.823689378192733912, -0.4153219600965887826 ) ) ;
#131336=CARTESIAN_POINT ( 'NONE',  ( 6.028642311625867833, 2.081422104948245533, 0.5829617784755269927 ) ) ;
#131340=CARTESIAN_POINT ( 'NONE',  ( 1.840342752298686380, 1.099902316243700939, -1.564109231055022864 ) ) ;
#131341=CARTESIAN_POINT ( 'NONE',  ( 2.535733614153494742, 0.8364609567749015095, -1.559706200981937352 ) ) ;
#131342=CARTESIAN_POINT ( 'NONE',  ( 0.4516295384478058450, -1.352486712789633172, -1.352142238705160704 ) ) ;
#131344=CARTESIAN_POINT ( 'NONE',  ( 5.589432567506730010, -0.4607417488133085381, 1.859251224981002482 ) ) ;
#131345=CARTESIAN_POINT ( 'NONE',  ( 6.268014395358870061, -1.954855384380562722, 0.2394079155795188485 ) ) ;
#131347=CARTESIAN_POINT ( 'NONE',  ( 1.248456593208754795, 1.040400552670465162, -1.847740296886036582 ) ) ;
#131348=CARTESIAN_POINT ( 'NONE',  ( 4.891396039733495016, 1.386484060982313249, 1.255958711209571810 ) ) ;
#131349=CARTESIAN_POINT ( 'NONE',  ( 0.7678472254676466102, 0.8974085622692473674, 1.589837017038860045 ) ) ;
#131351=CARTESIAN_POINT ( 'NONE',  ( 5.092482806099829062, -2.189899077852827780, -0.2726905915074183673 ) ) ;
#131355=CARTESIAN_POINT ( 'NONE',  ( 1.645062733043511027, -0.3006328960593112054, -2.040525779345269797 ) ) ;
#131362=CARTESIAN_POINT ( 'NONE',  ( 4.686024408448190570, -1.271122505372159539, -1.634150330299996012 ) ) ;
#131364=CARTESIAN_POINT ( 'NONE',  ( 1.089409339093825979, 1.906878951332368732, -1.017924135055588541 ) ) ;
#131366=CARTESIAN_POINT ( 'NONE',  ( 2.332681060731033540, 1.317659697769531624, -1.530744237074317171 ) ) ;
#131367=CARTESIAN_POINT ( 'NONE',  ( 6.720655732516647163, -0.004400176169771369272, 2.173773060281408931 ) ) ;
#131372=CARTESIAN_POINT ( 'NONE',  ( 0.07540816263147330500, 1.497505997221737273, 1.350731191893522976 ) ) ;
#131373=CARTESIAN_POINT ( 'NONE',  ( 4.845371438081495619, 0.6875289519675978900, -2.081009137124201658 ) ) ;
#131375=CARTESIAN_POINT ( 'NONE',  ( 3.603681638446740720, 1.388520161702249567, 1.315275747533505069 ) ) ;
#131377=B_SPLINE_CURVE_WITH_KNOTS ( 'NONE', 3,
 ( #120288, #170017, #21605, #87712, #153783, #5353, #24831, #207846, #23765, #73589, #76779 ),
 .UNSPECIFIED., .F., .F.,
 ( 4, 1, 1, 1, 1, 1, 1, 1, 4 ),
 ( 0.000000000000000000, 0.2256926809922864541, 0.3979886288388991278, 0.5260859906349554249, 0.6192013483571605637, 0.6864504996671639825, 0.7364865548622955282, 0.7772638159577213157, 1.000000000000000000 ),
 .UNSPECIFIED. ) ;
#131380=CARTESIAN_POINT ( 'NONE',  ( 2.091422941747251851, -0.4390073250180903663, 1.967893905867940996 ) ) ;
#131382=CARTESIAN_POINT ( 'NONE',  ( 0.9785521075769167965, -2.238008663356937156, -0.4956820494700850399 ) ) ;
#131384=CARTESIAN_POINT ( 'NONE',  ( 4.119902764342167956, -0.8871895459346083035, -1.478924549062347049 ) ) ;
#131385=CARTESIAN_POINT ( 'NONE',  ( -0.1394461523061195918, 6.947787103499363681, -2.875373568546248482 ) ) ;
#131389=CARTESIAN_POINT ( 'NONE',  ( 0.1755611466353786954, 2.859968053823423784, -2.732108412375580109 ) ) ;
#131392=CARTESIAN_POINT ( 'NONE',  ( 4.934136933359813071, -0.9735637292621384109, -1.527415209752202019 ) ) ;
#131396=CARTESIAN_POINT ( 'NONE',  ( 6.358062532015329005, 0.6862230018901045447, -1.676680497432983641 ) ) ;
#131399=CARTESIAN_POINT ( 'NONE',  ( 2.959115643078192637, 0.3208686883675835877, -2.167707805308824121 ) ) ;
#131400=CARTESIAN_POINT ( 'NONE',  ( 6.795359140062033454, -1.661660808857531313, 0.8381669064597346841 ) ) ;
#131402=CARTESIAN_POINT ( 'NONE',  ( 3.392102565403580350, -0.7792391910043224845, -1.750150251150209391 ) ) ;
#131407=CARTESIAN_POINT ( 'NONE',  ( 5.788306078712673219, -0.7643476728274435361, -1.974717070840046107 ) ) ;
#131408=CARTESIAN_POINT ( 'NONE',  ( 1.182749364907993206, -2.109161078630458430, -0.4729781282231394490 ) ) ;
#131411=CARTESIAN_POINT ( 'NONE',  ( 0.9381830591699467092, 1.797733097909786304, 0.3167546781352030272 ) ) ;
#131413=CARTESIAN_POINT ( 'NONE',  ( 3.082817581614716307, -0.1327354176642106531, -1.820802398864965088 ) ) ;
#131416=CARTESIAN_POINT ( 'NONE',  ( 3.226963424687212090, -1.818787540941589009, -0.7562359814760648558 ) ) ;
#131418=CARTESIAN_POINT ( 'NONE',  ( 4.440924170176640651, -1.503556815104054811, -1.229221392163130755 ) ) ;
#131421=CARTESIAN_POINT ( 'NONE',  ( 5.344028447597857223, -1.346983732444573256, -1.637812552581649594 ) ) ;
#131423=CARTESIAN_POINT ( 'NONE',  ( 2.490748672031910083, -1.830495558572857728, -0.5533032672612181457 ) ) ;
#131425=CARTESIAN_POINT ( 'NONE',  ( 0.2331563151865486128, 1.372759770070256291, -2.202161770551560149 ) ) ;
#131428=CARTESIAN_POINT ( 'NONE',  ( 4.231111847260408787, 1.841413651135707985, 0.8138496092669408322 ) ) ;
#131430=CARTESIAN_POINT ( 'NONE',  ( 4.916531288042031989, 1.256637652550334883, -1.324621001416517840 ) ) ;
#131431=CARTESIAN_POINT ( 'NONE',  ( 1.205626512970816355, -1.630946839658468983, -1.275175305487465049 ) ) ;
#131435=CARTESIAN_POINT ( 'NONE',  ( 5.594569530875262764, -0.4557361262383100020, -1.814172972432124720 ) ) ;
#131444=CARTESIAN_POINT ( 'NONE',  ( 1.270471156847551075, -0.9273748054965322840, -1.850965650132020635 ) ) ;
#131447=CARTESIAN_POINT ( 'NONE',  ( 1.792722901331974761, 1.566437577840825712, -1.424566180320179010 ) ) ;
#131450=CARTESIAN_POINT ( 'NONE',  ( 6.262565978045822490, -0.7396069823457154246, -1.933831554736538338 ) ) ;
#131455=CARTESIAN_POINT ( 'NONE',  ( 2.590095216689162427, -2.286210222917249180, -0.1672752534159216153 ) ) ;
#131457=CARTESIAN_POINT ( 'NONE',  ( 2.408343312057196872, -1.907530749141531423, -0.1368029246449145864 ) ) ;
#131460=CARTESIAN_POINT ( 'NONE',  ( 0.7736903856863480700, 0.3886292558455446411, -1.975178614941161870 ) ) ;
#131461=CARTESIAN_POINT ( 'NONE',  ( 1.305434336737832490, -1.543085766649286317, -1.211208057394968618 ) ) ;
#131465=CARTESIAN_POINT ( 'NONE',  ( 4.277343952648727132, 1.365583793738689655, 1.583094835029410063 ) ) ;
#131466=CARTESIAN_POINT ( 'NONE',  ( 2.676313443976061190, -1.692906749566702507, -0.5160995803213176414 ) ) ;
#131469=CARTESIAN_POINT ( 'NONE',  ( 5.876963737413220201, 2.120050906709324501, -0.8721662429640556491 ) ) ;
#131470=CARTESIAN_POINT ( 'NONE',  ( 4.628681372238307112, -1.589566819310319845, 0.7089629299102307991 ) ) ;
#131473=CARTESIAN_POINT ( 'NONE',  ( 4.534371549175888028, 1.681635666518576988, -0.4216726850935527127 ) ) ;
#131474=CARTESIAN_POINT ( 'NONE',  ( 4.527882006162959883, 2.107076143796441592, -0.5232759588417631447 ) ) ;
#131476=CARTESIAN_POINT ( 'NONE',  ( 6.069546051295945155, 1.394081536189460069, 1.457239770841619597 ) ) ;
#131477=CARTESIAN_POINT ( 'NONE',  ( 0.4999999999999185651, 1.979557137443526406E-12, -2.052068128417952941 ) ) ;
#131479=CARTESIAN_POINT ( 'NONE',  ( 2.151277967514260592, -1.545957563563664650, -1.149148694925563596 ) ) ;
#131481=CARTESIAN_POINT ( 'NONE',  ( 5.273765199871699672, 0.4330091245797212385, -2.178642023334904199 ) ) ;
#131483=CARTESIAN_POINT ( 'NONE',  ( 6.883263157960391787, -0.001104538646235289417, 1.946037152736757925 ) ) ;
#131486=CARTESIAN_POINT ( 'NONE',  ( 1.981385142061100835, -2.032350350298214980, -0.8968915317347254668 ) ) ;
#131494=CARTESIAN_POINT ( 'NONE',  ( 4.738769042418014443, -1.999979230503599048, -0.5042011814720639418 ) ) ;
#131498=CARTESIAN_POINT ( 'NONE',  ( 5.975831987570860981, 1.113884111790110820, 1.502598383168303409 ) ) ;
#131499=CARTESIAN_POINT ( 'NONE',  ( 4.939963660092479891, -1.468890173064988147, -0.9213945099728354515 ) ) ;
#131500=CARTESIAN_POINT ( 'NONE',  ( 4.106796630993492236, -0.2923914088966376723, 1.715523938624329281 ) ) ;
#131502=CARTESIAN_POINT ( 'NONE',  ( 2.384684040179287479, -0.3955501765894597344, -2.257852644028814915 ) ) ;
#131504=CARTESIAN_POINT ( 'NONE',  ( 5.601146835291897830, -0.5070800215070477845, 2.028203315493964709 ) ) ;
#131505=CARTESIAN_POINT ( 'NONE',  ( 0.9195641160042143936, 1.098457714822091091, -1.477412082521646575 ) ) ;
#131508=CARTESIAN_POINT ( 'NONE',  ( 3.235000160576475992, 2.016597019841442240, -0.002811030766311505089 ) ) ;
#131509=CARTESIAN_POINT ( 'NONE',  ( 0.9377431681640016059, 0.8850447378907432272, -2.004962588275795543 ) ) ;
#131512=CARTESIAN_POINT ( 'NONE',  ( 1.768117254402020277, -2.054967671486531255, 0.2513356459030794410 ) ) ;
#131515=CARTESIAN_POINT ( 'NONE',  ( 3.369896858953734142, 0.5134250039646214292, -2.057278921464212207 ) ) ;
#131517=CARTESIAN_POINT ( 'NONE',  ( 6.445924739416000193, 0.6936395621829589686, -1.688995215704327313 ) ) ;
#131524=CARTESIAN_POINT ( 'NONE',  ( 3.217061457047249551, 1.589534765328611154, -1.246005657720136606 ) ) ;
#131525=CARTESIAN_POINT ( 'NONE',  ( 0.5519644926167607268, 0.6605455615449079554, -1.999741160550670527 ) ) ;
#131528=CARTESIAN_POINT ( 'NONE',  ( 4.891365455385704664, -1.702569429429393599, 0.7516348641289184451 ) ) ;
#131534=CARTESIAN_POINT ( 'NONE',  ( 0.2862814217290919894, -1.017545141758866789, 1.907252267444502269 ) ) ;
#131538=CARTESIAN_POINT ( 'NONE',  ( 2.266548906626513649, -1.733607756391885912, 0.03760194650299571173 ) ) ;
#131539=CARTESIAN_POINT ( 'NONE',  ( 1.218268023815568535, -0.04584277261814385940, 1.739893813429808311 ) ) ;
#131540=CARTESIAN_POINT ( 'NONE',  ( 6.358097629954328589, 2.302029506726857466, -0.1628147022267756039 ) ) ;
#131543=CARTESIAN_POINT ( 'NONE',  ( 2.864585088123726919, -1.423607738919046906, 1.490243374215278971 ) ) ;
#131546=CARTESIAN_POINT ( 'NONE',  ( 1.335314297916901927, -1.281167425915705316, 1.556668322744148014 ) ) ;
#131547=CARTESIAN_POINT ( 'NONE',  ( 6.925078400183553029, 2.941156041390875941, 2.696161060448130975 ) ) ;
#131549=CARTESIAN_POINT ( 'NONE',  ( 6.455916552660014851, 1.865467424361374249, -0.1398750677365916961 ) ) ;
#131550=CARTESIAN_POINT ( 'NONE',  ( 4.218947473185084007, 1.474887410857337100, -1.217315437338606365 ) ) ;
#131552=CARTESIAN_POINT ( 'NONE',  ( 5.707716145626243964, -0.5396369327701348029, 2.139774205771049154 ) ) ;
#131557=CARTESIAN_POINT ( 'NONE',  ( 0.6100282365348074221, -0.7248652973187595938, 1.885305865817282323 ) ) ;
#131560=CARTESIAN_POINT ( 'NONE',  ( 4.911288641948820199, 2.004953420984519674, 1.142316731622401882 ) ) ;
#131561=CARTESIAN_POINT ( 'NONE',  ( 4.756279191188107269, -1.961398630904508833, -0.05015466537350299348 ) ) ;
#131562=CARTESIAN_POINT ( 'NONE',  ( 1.692165188054130187, 0.9715730843921737137, -1.704227633833883759 ) ) ;
#131566=CARTESIAN_POINT ( 'NONE',  ( 0.5853561509586381328, 1.734793994416533369, 1.213709793590052932 ) ) ;
#131569=CARTESIAN_POINT ( 'NONE',  ( 0.6558947131179297951, -1.335331635844772880, 1.267786537210900510 ) ) ;
#131571=CARTESIAN_POINT ( 'NONE',  ( 4.469693783504245843, -0.3772167039018388124, 2.137918043537301305 ) ) ;
#131573=CARTESIAN_POINT ( 'NONE',  ( 2.039458538997685366, 0.004855507148140979744, 2.120778211687989856 ) ) ;
#131578=CARTESIAN_POINT ( 'NONE',  ( 2.477870184918748997, 1.265364588504451548, 1.626488340418334566 ) ) ;
#131582=CARTESIAN_POINT ( 'NONE',  ( 0.07755575628183573877, 1.325091491099144259, -2.441202027401535357 ) ) ;
#131584=CARTESIAN_POINT ( 'NONE',  ( 5.197880135092803222, 1.287283252470315720, 1.414272151883423589 ) ) ;
#131585=CARTESIAN_POINT ( 'NONE',  ( 0.08304785351339466493, -2.141800023564765620, -0.5316218738360134477 ) ) ;
#131586=CARTESIAN_POINT ( 'NONE',  ( 1.511376755312091591, 1.995097771225157635, 1.066857341152693373 ) ) ;
#131588=CARTESIAN_POINT ( 'NONE',  ( 1.107327745774109529, 1.372724574380719043, 1.182278994020573792 ) ) ;
#131590=CARTESIAN_POINT ( 'NONE',  ( 2.131924177892559058, 1.915402082336896461, 0.04262488632780260522 ) ) ;
#131591=CARTESIAN_POINT ( 'NONE',  ( 3.490741092712910998, 2.019281663078629219, 0.4563312328872348722 ) ) ;
#131593=CARTESIAN_POINT ( 'NONE',  ( 1.393369717069929514, 1.491581312685308580, 1.289216981855696664 ) ) ;
#131594=CARTESIAN_POINT ( 'NONE',  ( 5.777940811437299651, 1.149350900142607879, 1.545952477797669200 ) ) ;
#131595=CARTESIAN_POINT ( 'NONE',  ( 1.225685606067970612, -0.05223309053147862785, 2.307267396272806970 ) ) ;
#131598=CARTESIAN_POINT ( 'NONE',  ( 5.582507124453381486, 1.231422846540839666, -1.654610746699414214 ) ) ;
#131601=CARTESIAN_POINT ( 'NONE',  ( 6.282269041519704444, -1.129704631681987204, 1.777121156631493726 ) ) ;
#131605=CARTESIAN_POINT ( 'NONE',  ( 4.499409293453607184, 1.733128992574247684, 1.291583502853070886 ) ) ;
#131606=CARTESIAN_POINT ( 'NONE',  ( 5.092447094119275874, -1.120170962321866082, 1.680348583886650315 ) ) ;
#131615=CARTESIAN_POINT ( 'NONE',  ( 3.626185617424378282, 2.007256095728218614, 0.1928357053486499662 ) ) ;
#131620=CARTESIAN_POINT ( 'NONE',  ( 5.032170685167933755, 1.114402916724830161, -1.852182961850391774 ) ) ;
#131625=CARTESIAN_POINT ( 'NONE',  ( 5.853138716089107518, 0.1455171034051294665, -2.011206573937059261 ) ) ;
#131627=CARTESIAN_POINT ( 'NONE',  ( 0.3985097114710112742, 1.437023721582047830, -0.9536953323180746844 ) ) ;
#131632=CARTESIAN_POINT ( 'NONE',  ( 6.714126539417144102, -0.8821443205445091973, -1.649434700640100226 ) ) ;
#131633=CARTESIAN_POINT ( 'NONE',  ( 0.7682272020711936600, 2.010684543107125410, -0.1010625827991030873 ) ) ;
#131634=CARTESIAN_POINT ( 'NONE',  ( 3.206306947805489305, -2.204311952916749640, 0.1065802224688369715 ) ) ;
#131638=CARTESIAN_POINT ( 'NONE',  ( 1.963691422110905638, -1.704870618661393999, -1.260721693921822428 ) ) ;
#131639=CARTESIAN_POINT ( 'NONE',  ( 2.021111450618333194, -1.799914642762674433, 0.9091633978678403949 ) ) ;
#131640=CARTESIAN_POINT ( 'NONE',  ( 2.496125854487367235, -0.9279945471987390837, 1.555666070890851627 ) ) ;
#131643=STYLED_ITEM ( 'NONE', ( #112015 ), #161027 ) ;
#131646=CARTESIAN_POINT ( 'NONE',  ( 0.4092221944725178417, -1.818073194988058194, 0.6039046695034550050 ) ) ;
#131653=CARTESIAN_POINT ( 'NONE',  ( 4.680646922328831394, -2.095996545452833981, -0.5284188670612933736 ) ) ;
#131656=CARTESIAN_POINT ( 'NONE',  ( 2.338272602237463360, -1.224740070204191511, -1.730971256048131401 ) ) ;
#131658=CARTESIAN_POINT ( 'NONE',  ( 2.987526725409937800, 1.391544230491305933, 1.396620715705886084 ) ) ;
#131659=CARTESIAN_POINT ( 'NONE',  ( 5.853752780977106163, -1.389761788226477002, -1.313969904969368496 ) ) ;
#131662=CARTESIAN_POINT ( 'NONE',  ( 6.268014395358870061, -1.954855384380562722, 0.2394079155795188485 ) ) ;
#131663=CARTESIAN_POINT ( 'NONE',  ( 1.605311038211139740, -1.927294583035423114, 0.2376585312828301821 ) ) ;
#131668=CARTESIAN_POINT ( 'NONE',  ( 2.097712127064654819, -2.090152927352141532, 0.05235412406051109108 ) ) ;
#131673=CARTESIAN_POINT ( 'NONE',  ( 5.830699381415811899, 1.280921311228696347, -1.420062396151056117 ) ) ;
#131675=CARTESIAN_POINT ( 'NONE',  ( 4.213639274598267370, -0.3785452818781535611, 2.174016619501429215 ) ) ;
#131676=CARTESIAN_POINT ( 'NONE',  ( 2.485638465518677176, 2.017858404210779888, -0.8937526715337427152 ) ) ;
#131678=CARTESIAN_POINT ( 'NONE',  ( 0.9262460828363194842, -0.8603794558708977025, -1.707882697979688391 ) ) ;
#131681=CARTESIAN_POINT ( 'NONE',  ( 3.807136610393092813, -1.694265131726957252, 1.189645435975445809 ) ) ;
#131683=CARTESIAN_POINT ( 'NONE',  ( 1.956163130892615731, 2.155914767609674598, -0.1587918856347721730 ) ) ;
#131684=CARTESIAN_POINT ( 'NONE',  ( 3.562233144267571650, -1.470601008620987749, 1.625073949779440419 ) ) ;
#131690=CARTESIAN_POINT ( 'NONE',  ( 0.2115648487451895210, 1.930418618556551946, 0.5826528611774861588 ) ) ;
#131692=CARTESIAN_POINT ( 'NONE',  ( 5.102424979711988051, 2.064335680360945169, 0.1577259720206558580 ) ) ;
#131693=CARTESIAN_POINT ( 'NONE',  ( 5.360994948850416719, -0.05292929278505505153, -2.116735950649220932 ) ) ;
#131696=CARTESIAN_POINT ( 'NONE',  ( 3.748844217038479698, -0.3797678475170936929, -1.932296744971262692 ) ) ;
#131697=CARTESIAN_POINT ( 'NONE',  ( 5.613300874620239078, -2.237517390240588711, 0.4973276143641935931 ) ) ;
#131698=CARTESIAN_POINT ( 'NONE',  ( 3.211362085483655981, -0.3553965070040401852, 1.790585553824732612 ) ) ;
#131706=CARTESIAN_POINT ( 'NONE',  ( 3.797138801009732667, -0.2017130330635922841, -2.003102573442970158 ) ) ;
#131707=CARTESIAN_POINT ( 'NONE',  ( 6.416599408848439268, -1.497502150434773194, -1.744030381972218047 ) ) ;
#131708=CARTESIAN_POINT ( 'NONE',  ( 4.821123798404616245, -1.750560105953799184, -0.8856655065374097191 ) ) ;
#131713=CARTESIAN_POINT ( 'NONE',  ( 0.5036076356924833464, -2.080315145378656805, 0.2087293992604210557 ) ) ;
#131714=CARTESIAN_POINT ( 'NONE',  ( 5.453870971094811004, 1.767685242813926250, -0.08968725887432274502 ) ) ;
#131716=CARTESIAN_POINT ( 'NONE',  ( 1.851786237446376049, 2.185420115623282200, -0.1633297828415938846 ) ) ;
#131717=CARTESIAN_POINT ( 'NONE',  ( 1.346757998634398712, 0.5060278187854657661, -1.665264516905233361 ) ) ;
#131719=FACE_OUTER_BOUND ( 'NONE', #55199, .T. ) ;
#131720=CARTESIAN_POINT ( 'NONE',  ( 2.086159243269372521, -1.691233086580298695, -0.3380474007560717031 ) ) ;
#131721=CARTESIAN_POINT ( 'NONE',  ( 1.171705676731093604, 1.309414992938146893, 1.757219779060022580 ) ) ;
#131722=CARTESIAN_POINT ( 'NONE',  ( 3.774219598512587037, 1.225428716765289749, 1.835190637982798023 ) ) ;
#131723=CARTESIAN_POINT ( 'NONE',  ( 1.165147980530324201, 1.645521545068162617, -1.416405498411864583 ) ) ;
#131725=CARTESIAN_POINT ( 'NONE',  ( 2.044302899665669138, 0.9103292306275132528, 1.911821358334654608 ) ) ;
#131726=CARTESIAN_POINT ( 'NONE',  ( 6.827182134110222123, 7.629137130509067610, 2.789055895399249252 ) ) ;
#131728=CARTESIAN_POINT ( 'NONE',  ( 2.736170862265740578, 2.275407485025813692, 0.2777600125268233633 ) ) ;
#131730=CARTESIAN_POINT ( 'NONE',  ( 0.07755575628183573877, 5.720052600789671260, -2.782970829007725744 ) ) ;
#131732=CARTESIAN_POINT ( 'NONE',  ( 4.442156590966897411, -1.366343709131916828, -1.751266766990001944 ) ) ;
#131741=CARTESIAN_POINT ( 'NONE',  ( 3.516250148862578584, -1.862017090670412767, 0.7743150488077471527 ) ) ;
#131743=CARTESIAN_POINT ( 'NONE',  ( 0.6376417299419987472, 1.925892387546113582, -0.7388170802648945656 ) ) ;
#131744=CARTESIAN_POINT ( 'NONE',  ( 6.983263157960366563, -0.003091553303710344557, 1.945923119799706669 ) ) ;
#131748=CARTESIAN_POINT ( 'NONE',  ( 4.119203469048302146, -2.097337170177868693, 0.6352863671069891582 ) ) ;
#131749=CARTESIAN_POINT ( 'NONE',  ( 1.828750219146151323, 0.7691198443132395424, -1.864169014999479623 ) ) ;
#131750=CARTESIAN_POINT ( 'NONE',  ( 0.8547319020580852467, 0.3593373433725781108, -1.805665335529122784 ) ) ;
#131753=CARTESIAN_POINT ( 'NONE',  ( 4.770415466175468744, -1.191763575130764696, 1.382976834283907053 ) ) ;
#131754=CARTESIAN_POINT ( 'NONE',  ( 6.082657761774013849, -0.6767167302549759178, 1.899617564980569995 ) ) ;
#131756=CARTESIAN_POINT ( 'NONE',  ( 4.100629699907013759, -0.7064081464536530186, -2.149486123859779330 ) ) ;
#131758=CARTESIAN_POINT ( 'NONE',  ( 0.6277293814327978838, -1.999128025905463568, 0.6627883249872651428 ) ) ;
#131760=CARTESIAN_POINT ( 'NONE',  ( 4.703616579153604427, -1.598285800263723910, -1.315984976451072930 ) ) ;
#131770=CARTESIAN_POINT ( 'NONE',  ( 0.2992908618118708675, -0.2657624787030036240, -2.103842954668332599 ) ) ;
#131771=CARTESIAN_POINT ( 'NONE',  ( 1.652877544743835969, 2.198119390704804665, 0.3199964322739051736 ) ) ;
#131776=CARTESIAN_POINT ( 'NONE',  ( 3.156644782993088150, -0.5669402238272451822, -1.878178299617596192 ) ) ;
#131782=CARTESIAN_POINT ( 'NONE',  ( 1.810938747355747447, -0.5704394276861005642, -2.042344090522000055 ) ) ;
#131784=CARTESIAN_POINT ( 'NONE',  ( 4.053139552913617827, 1.658577106941661272, -1.047563642765911185 ) ) ;
#131785=CARTESIAN_POINT ( 'NONE',  ( 2.835029207381420502, 0.2633842809251253358, 2.145520918749081574 ) ) ;
#131786=CARTESIAN_POINT ( 'NONE',  ( 3.052128622409277181, -1.392423357299840792, 1.204796875372941667 ) ) ;
#131790=CARTESIAN_POINT ( 'NONE',  ( 4.945099085969404840, 0.5415675326034079529, -1.653987846916603610 ) ) ;
#131794=CARTESIAN_POINT ( 'NONE',  ( 2.044033295145482043, 0.8276103948961744949, -1.997198329219296742 ) ) ;
#131795=CARTESIAN_POINT ( 'NONE',  ( 4.464220131058834085, 1.617570847575640736, 1.203168917025834839 ) ) ;
#131797=CARTESIAN_POINT ( 'NONE',  ( 1.165152350680317195, -1.954565670758709128, -0.9236901323337529668 ) ) ;
#131798=CARTESIAN_POINT ( 'NONE',  ( 2.600799297785437947, 1.585616864491301348, -1.171192495528531330 ) ) ;
#131800=CARTESIAN_POINT ( 'NONE',  ( 3.104954810669264376, -0.3761875069782861236, 1.905116956637223913 ) ) ;
#131806=ADVANCED_FACE ( 'NONE', ( #96345 ), #46516, .T. ) ;
#131810=CARTESIAN_POINT ( 'NONE',  ( 1.220068447022312652, -2.152735442661047216, 0.4846846590640523367 ) ) ;
#131812=CARTESIAN_POINT ( 'NONE',  ( 5.787936641206399280, -1.241742415844361291, -1.518776266119965745 ) ) ;
#131814=CARTESIAN_POINT ( 'NONE',  ( 3.345011933649364444, -1.869310496227539531, -0.9943253416123465360 ) ) ;
#131816=CARTESIAN_POINT ( 'NONE',  ( 0.07459516483346911864, 0.7642615113957001993, -1.841455071455591064 ) ) ;
#131817=CARTESIAN_POINT ( 'NONE',  ( 4.277188459880359339, 1.204364621523913437, 1.392669941884729035 ) ) ;
#131821=CARTESIAN_POINT ( 'NONE',  ( 5.326475955075804514, -0.9554483686352827077, -1.893264085526874974 ) ) ;
#131825=CARTESIAN_POINT ( 'NONE',  ( 5.307911771147946212, -2.051258671218537444, 0.1976249854395220606 ) ) ;
#131827=CARTESIAN_POINT ( 'NONE',  ( 0.7306206827372868640, -1.750454575335522067, -0.6323700682324316924 ) ) ;
#131828=CARTESIAN_POINT ( 'NONE',  ( 3.104851637799400876, -0.3563606998662186554, 1.806257425991746546 ) ) ;
#131834=CARTESIAN_POINT ( 'NONE',  ( 3.897267319706390065, 1.864829029706360330, -1.179861312946443697 ) ) ;
#131835=CARTESIAN_POINT ( 'NONE',  ( 4.446707141204663039, 0.5976617499744775186, 2.181999625662895959 ) ) ;
#131837=CARTESIAN_POINT ( 'NONE',  ( 4.992358684838777982, -0.9999893916136384231, 1.510367140083505699 ) ) ;
#131838=CARTESIAN_POINT ( 'NONE',  ( 5.383970194100923479, -1.915903400165029469, 0.006849619181082886032 ) ) ;
#131840=CARTESIAN_POINT ( 'NONE',  ( 5.682452175617663137, -1.825344843996518529, -0.4084625512627630406 ) ) ;
#131841=CARTESIAN_POINT ( 'NONE',  ( 6.478945253086064504, 1.736940705955980269, 0.6686975948369151546 ) ) ;
#131842=CARTESIAN_POINT ( 'NONE',  ( 6.455894400631252417, 1.764744506579400962, -0.1349141608881914423 ) ) ;
#131845=CARTESIAN_POINT ( 'NONE',  ( 2.789785578339375238, 1.489779160094312660, 1.488918557309417467 ) ) ;
#131851=CARTESIAN_POINT ( 'NONE',  ( 1.810812951734928511, -0.5429070200502202903, -1.945354291398709412 ) ) ;
#131855=CARTESIAN_POINT ( 'NONE',  ( 3.532649767544591590, 2.108058052951222283, 0.4773693597190583060 ) ) ;
#131856=CARTESIAN_POINT ( 'NONE',  ( 6.609999999999999432, 2.404169510734831761, 2.660384318335922149 ) ) ;
#131861=CARTESIAN_POINT ( 'NONE',  ( 6.925078400183548588, 0.0006614011395407459748, 1.855452278108092656 ) ) ;
#131864=CARTESIAN_POINT ( 'NONE',  ( 1.136565065649897344, 0.4323997850379875385, 2.148315308122191514 ) ) ;
#131866=CARTESIAN_POINT ( 'NONE',  ( 1.921153072736818013, 2.111338651666348376, 0.8135812809707074766 ) ) ;
#131873=CARTESIAN_POINT ( 'NONE',  ( 2.917004591651660927, -0.1773711190117404635, 1.760840049638369154 ) ) ;
#131875=CARTESIAN_POINT ( 'NONE',  ( 6.545939543708723107, 0.8506627741289953804, -2.036432556493542823 ) ) ;
#131879=CARTESIAN_POINT ( 'NONE',  ( 5.677361293727043901, 1.528752376640944100, 1.314985542479940817 ) ) ;
#131881=CARTESIAN_POINT ( 'NONE',  ( 2.799504582125960095, -0.5885537693137884441, 1.775713401224961574 ) ) ;
#131882=CARTESIAN_POINT ( 'NONE',  ( 3.625891163443736076, 2.020865133175090644, -0.4488579359705275329 ) ) ;
#131885=CARTESIAN_POINT ( 'NONE',  ( 1.916128293556786044, -1.911906470838855343, 0.05044092668918254141 ) ) ;
#131890=CARTESIAN_POINT ( 'NONE',  ( 1.230557176020011134, 1.282188879665364656, -1.419081615486268433 ) ) ;
#131891=CARTESIAN_POINT ( 'NONE',  ( 2.840232074097197579, -1.010955899468408248, 1.681206195012739046 ) ) ;
#131896=CARTESIAN_POINT ( 'NONE',  ( 6.221945801152132027, -1.093087313283289230, -1.640361058829779228 ) ) ;
#131898=CARTESIAN_POINT ( 'NONE',  ( 2.109637220322407192, 1.559014694980038085, 1.273805747723085746 ) ) ;
#131901=CARTESIAN_POINT ( 'NONE',  ( 2.566138216211190759, -1.085845923642224209, 1.817437617555809792 ) ) ;
#131903=CARTESIAN_POINT ( 'NONE',  ( 4.299325596424930396, -1.802881993240162961, 1.017688063649782482 ) ) ;
#131905=CARTESIAN_POINT ( 'NONE',  ( 5.630836714711354496, -1.890471120482087652, 0.8929869209393003215 ) ) ;
#131907=CARTESIAN_POINT ( 'NONE',  ( 4.682524874021861017, -1.770931954651306262, -0.4427778663074270482 ) ) ;
#131911=CARTESIAN_POINT ( 'NONE',  ( 5.227635310461984375, -2.096914331502324647, 0.6878394029543041244 ) ) ;
#131914=CARTESIAN_POINT ( 'NONE',  ( 4.336511155197938727, 1.173803677898217712, -1.509565991254034678 ) ) ;
#131922=CARTESIAN_POINT ( 'NONE',  ( 0.1691535571452691677, 1.059206136818511501, 1.505872603892892458 ) ) ;
#131927=CARTESIAN_POINT ( 'NONE',  ( 4.464026755505964950, 0.8799173153972823513, 1.650629236088823282 ) ) ;
#131932=CARTESIAN_POINT ( 'NONE',  ( 1.639439270303972851, 1.821716124042528584, -0.7488776562727271768 ) ) ;
#131933=CARTESIAN_POINT ( 'NONE',  ( 2.372672929649359386, -0.3474902101525711440, -1.986097784353996643 ) ) ;
#131937=CARTESIAN_POINT ( 'NONE',  ( 2.045129345224237394, -1.761195505111545989, -1.303888621850733509 ) ) ;
#131947=CARTESIAN_POINT ( 'NONE',  ( 4.968220237687512864, -1.735557695065930606, -0.6152675618510683453 ) ) ;
#131948=CARTESIAN_POINT ( 'NONE',  ( 1.313140557769366890, 1.644527964066449632, -1.160800818697106163 ) ) ;
#131949=CARTESIAN_POINT ( 'NONE',  ( 3.181363629901075463, -1.130666556857576444, -2.000962643106804606 ) ) ;
#131951=CARTESIAN_POINT ( 'NONE',  ( 1.252544054828262476, -0.4453625992760417707, -1.806759803163625167 ) ) ;
#131954=CARTESIAN_POINT ( 'NONE',  ( 5.853752780977106163, -1.389761788226477002, -1.313969904969368496 ) ) ;
#131957=CARTESIAN_POINT ( 'NONE',  ( 3.614856758894122724, -0.1514882961727741506, 2.085299387778175806 ) ) ;
#131958=CARTESIAN_POINT ( 'NONE',  ( 2.781945002432617997, -0.9632652739061451364, 1.603442845774772474 ) ) ;
#131961=CARTESIAN_POINT ( 'NONE',  ( 6.339398910184078417, 0.6979989802004606947, -1.704029730133400866 ) ) ;
#131964=CARTESIAN_POINT ( 'NONE',  ( 4.547283022377748729, -1.335744037758682667, -1.091317429222604884 ) ) ;
#131966=CARTESIAN_POINT ( 'NONE',  ( 0.3340423123194468658, 0.5469568729883391711, -1.645723886551814452 ) ) ;
#131970=AXIS2_PLACEMENT_3D ( 'NONE', #197681, #181434, #33063 ) ;
#131972=CARTESIAN_POINT ( 'NONE',  ( 4.241221290925122567, -0.2070989531138747453, -2.161143177887809852 ) ) ;
#131973=CARTESIAN_POINT ( 'NONE',  ( 3.017977635683791071, -0.9002817137206723386, -1.588204215665294461 ) ) ;
#131974=CARTESIAN_POINT ( 'NONE',  ( 0.8484012048698870156, -1.946262134508335739, -0.2457884297097159831 ) ) ;
#131975=CARTESIAN_POINT ( 'NONE',  ( 5.594942764039734229, 1.868482245966827326, 0.9958698414167986845 ) ) ;
#131978=CARTESIAN_POINT ( 'NONE',  ( 6.356980026238091774, 0.3966049396831958229, -2.257653707126358267 ) ) ;
#131982=CARTESIAN_POINT ( 'NONE',  ( 1.313308151137903224, 1.731519532738003297, -1.223779428986125462 ) ) ;
#131987=CARTESIAN_POINT ( 'NONE',  ( 6.473493066963706966, -0.2743099562094972743, 2.153646047958713172 ) ) ;
#131988=CARTESIAN_POINT ( 'NONE',  ( 6.883263157960358924, 7.052235917045241997, 2.651962373728885325 ) ) ;
#131990=CARTESIAN_POINT ( 'NONE',  ( 2.631719755377628811, -0.2151721393647449687, 2.210840341435269973 ) ) ;
#131992=CARTESIAN_POINT ( 'NONE',  ( 6.082657761774013849, -0.6767167302549759178, 1.899617564980569995 ) ) ;
#131994=CARTESIAN_POINT ( 'NONE',  ( 4.381722380181817478, -1.975297276180818296, 0.5937428812356324581 ) ) ;
#131996=CARTESIAN_POINT ( 'NONE',  ( -0.2409995289980246258, 2.020898751655671788, -2.415740196953279462 ) ) ;
#132000=CARTESIAN_POINT ( 'NONE',  ( 4.440845869443198701, -1.426288408191313639, -1.164454570719307469 ) ) ;
#132002=DIRECTION ( 'NONE',  ( 0.000000000000000000, 0.000000000000000000, 1.000000000000000000 ) ) ;
#132003=CARTESIAN_POINT ( 'NONE',  ( 1.324769809204975557, -0.04781147349866912699, 1.724288685672677568 ) ) ;
#132005=CARTESIAN_POINT ( 'NONE',  ( 2.057686432631794293, -1.410295276735703540, 1.815187820423395992 ) ) ;
#132007=CARTESIAN_POINT ( 'NONE',  ( 0.7732102150014728004, -2.130643883221981838, -0.7610950190743612787 ) ) ;
#132008=CARTESIAN_POINT ( 'NONE',  ( 3.791714260247856849, 1.525338472785308097, 1.452445685796518227 ) ) ;
#132010=CARTESIAN_POINT ( 'NONE',  ( 3.022431051408695613, 1.665045927894950095, 0.5999815234925524043 ) ) ;
#132017=CARTESIAN_POINT ( 'NONE',  ( 4.939773707303276140, -2.109081064246129067, 0.6975513078685476875 ) ) ;
#132018=CARTESIAN_POINT ( 'NONE',  ( 3.205210054081304438, -0.4271916898582402422, 2.149238826137919389 ) ) ;
#132023=CARTESIAN_POINT ( 'NONE',  ( 6.890000000000007674, 6.036127733823692054, 2.594896729422516923 ) ) ;
#132025=CARTESIAN_POINT ( 'NONE',  ( 6.187751663909415001, 2.028806014889028120, -0.6170373231123224000 ) ) ;
#132031=CARTESIAN_POINT ( 'NONE',  ( 5.935073298327618652, -1.338256116417003927, -1.264887592264056559 ) ) ;
#132034=CARTESIAN_POINT ( 'NONE',  ( 1.592878374036447164, -0.5866614404700842833, 1.638733785964431755 ) ) ;
#132036=CARTESIAN_POINT ( 'NONE',  ( 0.3265133270617843753, -1.284392789319420913, 1.483054880892265892 ) ) ;
#132038=CARTESIAN_POINT ( 'NONE',  ( 4.750933126423753095, -1.738186171353903742, 1.284983810367075208 ) ) ;
#132042=CARTESIAN_POINT ( 'NONE',  ( 4.452137864729129646, 2.161286467946467837, -0.05003489268536746859 ) ) ;
#132046=CARTESIAN_POINT ( 'NONE',  ( 5.536387714897482049, 1.941722972556509053, 0.3397322875919612795 ) ) ;
#132047=CARTESIAN_POINT ( 'NONE',  ( 5.307816166741994302, -1.486200299559970128, 0.8926388968444918248 ) ) ;
#132049=CARTESIAN_POINT ( 'NONE',  ( 2.033021410476544943, -1.955939774129427988, 0.9887309579383956049 ) ) ;
#132050=CARTESIAN_POINT ( 'NONE',  ( 2.854834436329793057, 0.7764391075696615019, 2.173172238055173455 ) ) ;
#132051=CARTESIAN_POINT ( 'NONE',  ( 4.235659074092642307, -1.418359850100110009, -1.495269491646352256 ) ) ;
#132052=CARTESIAN_POINT ( 'NONE',  ( 0.4627034902389154936, 0.1913720229725413835, -1.932491135362510715 ) ) ;
#132057=CARTESIAN_POINT ( 'NONE',  ( 3.551138032611600437, 0.3147205237276836653, 2.097014573754731881 ) ) ;
#132059=CARTESIAN_POINT ( 'NONE',  ( 1.670546294658280084, 1.392546765991018454, 1.458555661489918442 ) ) ;
#132061=CARTESIAN_POINT ( 'NONE',  ( 4.665167916288286420, -1.969490514480085164, -0.9956290437203789701 ) ) ;
#132070=CARTESIAN_POINT ( 'NONE',  ( 4.504794318429003575, 1.594258339665870938, -1.305997064384886830 ) ) ;
#132073=CARTESIAN_POINT ( 'NONE',  ( 3.123699121837515413, -0.3918110498563053268, 1.981120561552232262 ) ) ;
#132077=CARTESIAN_POINT ( 'NONE',  ( 3.467699783257427004, 2.010999201309400686, -0.4499753609362132090 ) ) ;
#132081=CARTESIAN_POINT ( 'NONE',  ( -0.1408020194050354501, 2.869306972054268989, -2.588546047063750688 ) ) ;
#132082=CARTESIAN_POINT ( 'NONE',  ( 1.007454599746326895, -0.8259622865525710900, -1.645551850779983116 ) ) ;
#132083=CARTESIAN_POINT ( 'NONE',  ( 6.358075476802443227, 2.201304964888863402, -0.1578768562689457922 ) ) ;
#132085=CARTESIAN_POINT ( 'NONE',  ( 1.159701560084012595, 0.4228694819443152286, -2.119656415666733906 ) ) ;
#132087=CARTESIAN_POINT ( 'NONE',  ( 1.551970632248239612, 1.040795554343958429, 1.727062486439542965 ) ) ;
#132090=CARTESIAN_POINT ( 'NONE',  ( 0.1978467685152424937, -1.870139902624564865, -0.05068021481659244765 ) ) ;
#132092=CARTESIAN_POINT ( 'NONE',  ( 4.487161871577921346, 1.761403164857084702, -0.8856326919300193667 ) ) ;
#132093=CARTESIAN_POINT ( 'NONE',  ( 4.926970384345759513, -1.727065721694167832, 1.040790168839386798 ) ) ;
#132096=CARTESIAN_POINT ( 'NONE',  ( 6.727182134110234024, -0.002100931800118072384, 2.089081857379895268 ) ) ;
#132098=CARTESIAN_POINT ( 'NONE',  ( 5.248515149483167441, -2.054309126314420642, -0.2569322651706855143 ) ) ;
#132102=CARTESIAN_POINT ( 'NONE',  ( 5.168225562285083896, 2.017301038980311656, -0.1031631561184200713 ) ) ;
#132104=CARTESIAN_POINT ( 'NONE',  ( 3.352467919438668620, 2.307868970251240714, 0.0003179301051748489328 ) ) ;
#132106=CARTESIAN_POINT ( 'NONE',  ( 1.288015978462764277, -1.305315335096700613, -1.597021576285734268 ) ) ;
#132113=CARTESIAN_POINT ( 'NONE',  ( 4.158752335142390955, -0.6773029245935069387, -2.062915381819859562 ) ) ;
#132115=CARTESIAN_POINT ( 'NONE',  ( 3.140019216317342376, 0.4501627324021878485, 1.785233193441162491 ) ) ;
#132117=CARTESIAN_POINT ( 'NONE',  ( 4.511385190476093321, -2.149204750630455241, 0.4279282578087198474 ) ) ;
#132119=CARTESIAN_POINT ( 'NONE',  ( 5.295900185863533061, -0.8195587353489269811, 2.109036902066116603 ) ) ;
#132125=CARTESIAN_POINT ( 'NONE',  ( 6.397684210179588327, -0.5939413028648796722, 1.667199339893215448 ) ) ;
#132127=CARTESIAN_POINT ( 'NONE',  ( 4.143230477514478594, 0.1011454402246019235, 2.010680395766785811 ) ) ;
#132129=CARTESIAN_POINT ( 'NONE',  ( 2.854625263381281641, 0.7083305855763160075, 1.983406512126543841 ) ) ;
#132130=CARTESIAN_POINT ( 'NONE',  ( 2.583477129321013255, -0.5985834622587657972, 1.819768813671450935 ) ) ;
#132133=CARTESIAN_POINT ( 'NONE',  ( 3.051173608728700248, 1.690664904776484789, -1.010063219348409813 ) ) ;
#132134=CARTESIAN_POINT ( 'NONE',  ( 1.041631754505952134, 0.7616270086890539748, -1.708776438048253077 ) ) ;
#132135=CARTESIAN_POINT ( 'NONE',  ( 1.258172656280614365, -1.962046632281065461, -0.003472340283867945618 ) ) ;
#132136=CARTESIAN_POINT ( 'NONE',  ( 0.2988868148526523938, -0.2362956723594503705, -1.897694653714178781 ) ) ;
#132140=CARTESIAN_POINT ( 'NONE',  ( 6.438356904408193415, 1.850619875698428674, 0.2722718653145329015 ) ) ;
#132144=CARTESIAN_POINT ( 'NONE',  ( 6.209843387784003355, 0.6066176463192971546, -1.979359621541395553 ) ) ;
#132146=CARTESIAN_POINT ( 'NONE',  ( 1.398975865466948632, 0.4019745351953528112, 2.030794141931663521 ) ) ;
#132151=CARTESIAN_POINT ( 'NONE',  ( 5.602226918196428151, -0.9533447246646039597, 1.894147766696724799 ) ) ;
#132156=CARTESIAN_POINT ( 'NONE',  ( 6.338335788673861160, -1.050647824335379399, 1.656640365463659670 ) ) ;
#132158=CARTESIAN_POINT ( 'NONE',  ( 2.882185300971401798, -0.2004049647258976941, 2.006138917898095730 ) ) ;
#132159=CARTESIAN_POINT ( 'NONE',  ( 3.133901338358492161, 1.915903397621956383, -0.005105665024216290114 ) ) ;
#132161=CARTESIAN_POINT ( 'NONE',  ( 1.769323484426460480, 2.095969018468134770, -0.6401429536977767398 ) ) ;
#132162=CARTESIAN_POINT ( 'NONE',  ( 0.2331713839410966271, 5.723577825403736163, -2.547423061495857954 ) ) ;
#132163=CARTESIAN_POINT ( 'NONE',  ( 3.198369223161025676, -0.5396142385952484855, -1.791042426047453784 ) ) ;
#132167=CARTESIAN_POINT ( 'NONE',  ( 5.835599761872579450, 0.6139674163637841575, -2.026275392342128612 ) ) ;
#132169=CARTESIAN_POINT ( 'NONE',  ( 6.689897370947560873, -1.349224794794257720, -1.570457413003906177 ) ) ;
#132170=CARTESIAN_POINT ( 'NONE',  ( 1.769195444908505888, 1.999712852614519143, -0.6101556835421716452 ) ) ;
#132172=CARTESIAN_POINT ( 'NONE',  ( 0.6742806677700216023, -1.621663110835226629, -0.5878086553270861492 ) ) ;
#132181=CARTESIAN_POINT ( 'NONE',  ( 1.418313031307829153, -0.6519236697288594007, -1.690267533947023892 ) ) ;
#132186=CARTESIAN_POINT ( 'NONE',  ( 6.539320575229256249, 6.039323383297771741, 2.391644441267444687 ) ) ;
#132189=CARTESIAN_POINT ( 'NONE',  ( 2.769781630715903997, -1.841240947949342788, 0.2698520108674675733 ) ) ;
#132190=CARTESIAN_POINT ( 'NONE',  ( 0.7553224350208649351, 1.845776580612036533, -0.5121453728616427448 ) ) ;
#132191=CARTESIAN_POINT ( 'NONE',  ( 6.774445256934315651, -1.184694399318196201, 1.519801669933226407 ) ) ;
#132198=CARTESIAN_POINT ( 'NONE',  ( 4.645333151331359822, 1.761124666023382579, -0.8816396696852289994 ) ) ;
#132199=CARTESIAN_POINT ( 'NONE',  ( 1.963691422110905638, -1.704870618661393999, -1.260721693921822428 ) ) ;
#132202=CARTESIAN_POINT ( 'NONE',  ( 5.718738293430368991, -0.05686238728638653983, 2.190873718245327506 ) ) ;
#132204=CARTESIAN_POINT ( 'NONE',  ( 4.594702886556338406, -0.4214696541114425488, -1.879573207023744974 ) ) ;
#132206=CARTESIAN_POINT ( 'NONE',  ( 0.3053143536290472970, -0.4923201697357786899, 1.757875871163571802 ) ) ;
#132207=CARTESIAN_POINT ( 'NONE',  ( 1.278255639411193245, 1.316999024263129092, 1.770685722221450709 ) ) ;
#132211=CARTESIAN_POINT ( 'NONE',  ( 6.578958714233388072, 1.836342173298356917, 0.7121609383471518839 ) ) ;
#132212=CARTESIAN_POINT ( 'NONE',  ( 1.944774020950320592, -1.561091384877069554, -1.155077030050962295 ) ) ;
#132213=CARTESIAN_POINT ( 'NONE',  ( 6.538407551539116902, 2.202477839928073333, -0.6571292610791487077 ) ) ;
#132215=CARTESIAN_POINT ( 'NONE',  ( 4.012436097835626825, 0.6663421089948203813, 1.737758261286206807 ) ) ;
#132220=CARTESIAN_POINT ( 'NONE',  ( -0.005964567173097347699, -2.191213315851054944, -0.04726126812268362232 ) ) ;
#132226=CARTESIAN_POINT ( 'NONE',  ( 1.611646134362737959, -1.812087876328593916, 0.2219229778191167957 ) ) ;
#132228=CARTESIAN_POINT ( 'NONE',  ( 3.533592999799278989, -1.415137147236225079, 1.001973916141611687 ) ) ;
#132230=CARTESIAN_POINT ( 'NONE',  ( 6.508999999999979025, 4.693190036150777011, 2.662629399390674667 ) ) ;
#132232=CARTESIAN_POINT ( 'NONE',  ( 0.2582596107527914131, 0.7359740259155130859, 1.780569212123730871 ) ) ;
#132233=CARTESIAN_POINT ( 'NONE',  ( 4.627759936859944467, 1.903863570041373077, -0.4726564843360381851 ) ) ;
#132237=CARTESIAN_POINT ( 'NONE',  ( 4.494861206476631565, -2.057060146276223023, -0.5143016718046622415 ) ) ;
#132240=CARTESIAN_POINT ( 'NONE',  ( 2.483334644719075168, -0.004358110040847408898, 2.070434559716929357 ) ) ;
#132244=CARTESIAN_POINT ( 'NONE',  ( 2.637635294750583004, 0.7773225462509441019, 2.163377341885423188 ) ) ;
#132252=CARTESIAN_POINT ( 'NONE',  ( 4.095896644567202038, 1.253117935160457552, 1.444681106026260320 ) ) ;
#132254=CARTESIAN_POINT ( 'NONE',  ( 4.893404818765360709, 1.279633041931761639, 1.156618277182480892 ) ) ;
#132255=CARTESIAN_POINT ( 'NONE',  ( 3.696500153570709379, 1.422608671726926177, -1.429447704489300364 ) ) ;
#132256=CARTESIAN_POINT ( 'NONE',  ( 5.116020035227313301, 0.1674390183682184785, 2.292669612833755810 ) ) ;
#132258=CARTESIAN_POINT ( 'NONE',  ( 0.8564375766340023288, 2.204168734417511821, -0.1118928034387969561 ) ) ;
#132260=CARTESIAN_POINT ( 'NONE',  ( 5.413276439055476175, -0.2588944790761596448, 1.750576072867173316 ) ) ;
#132262=CARTESIAN_POINT ( 'NONE',  ( 1.869451396563295065, 2.192715141705191773, -0.6681815460085840375 ) ) ;
#132263=CARTESIAN_POINT ( 'NONE',  ( 6.210883717528068892, -0.2205035313364057392, 1.827825250963102111 ) ) ;
#132269=CARTESIAN_POINT ( 'NONE',  ( 6.549288556030710140, 1.803345607721940524, -1.016871928424132099 ) ) ;
#132270=CARTESIAN_POINT ( 'NONE',  ( 2.518767860054324625, 0.2516336668320385828, 2.000731427934741902 ) ) ;
#132273=CARTESIAN_POINT ( 'NONE',  ( 5.426370213035293766, 1.145732239094964466, -1.548636736622555299 ) ) ;
#132275=CARTESIAN_POINT ( 'NONE',  ( 2.496574912728947382, -1.137965521849234607, 1.907653428263719864 ) ) ;
#132283=CARTESIAN_POINT ( 'NONE',  ( 5.425286103790146974, -1.110369212591550747, -1.340227399214832360 ) ) ;
#132284=CARTESIAN_POINT ( 'NONE',  ( 3.016010921186715432, 1.952665002612500533, -0.1895750030070641190 ) ) ;
#132288=CARTESIAN_POINT ( 'NONE',  ( 4.921284695982240720, -0.1178685990214298068, 2.259476483347002240 ) ) ;
#132289=CARTESIAN_POINT ( 'NONE',  ( 0.8364713509731898089, -1.147405136530167624, 1.713900253247694350 ) ) ;
#132292=CARTESIAN_POINT ( 'NONE',  ( 1.850798253084064537, 0.7104643512030085484, 2.148151574381700790 ) ) ;
#132295=CARTESIAN_POINT ( 'NONE',  ( 2.618241971997347317, 1.224968108320439342, -1.413705424714882586 ) ) ;
#132296=CARTESIAN_POINT ( 'NONE',  ( 1.652526702274889514, 0.8913305402388423948, 1.487382274443969754 ) ) ;
#132297=CARTESIAN_POINT ( 'NONE',  ( 5.583573808894983337, -0.9862700065477579825, 1.957137920222583372 ) ) ;
#132298=CARTESIAN_POINT ( 'NONE',  ( 6.370204010553460527, 1.178711257604664109, 1.983722394024198143 ) ) ;
#132299=CARTESIAN_POINT ( 'NONE',  ( 1.252885565054340011, -1.625093837591420787, 1.267311679704327121 ) ) ;
#132300=CARTESIAN_POINT ( 'NONE',  ( 4.540924088961058480, -1.502189473471927439, -1.230693300551897185 ) ) ;
#132302=CARTESIAN_POINT ( 'NONE',  ( 5.483624757375023862, 1.255567903217995829, 1.386730702750748945 ) ) ;
#132303=CARTESIAN_POINT ( 'NONE',  ( 1.625000000000001554, -2.052068128417951165, 9.007296548519099900E-14 ) ) ;
#132305=CARTESIAN_POINT ( 'NONE',  ( 6.327499943094792023, -1.427716970705223520, 1.423745300580002482 ) ) ;
#132309=CARTESIAN_POINT ( 'NONE',  ( 4.342422763466713853, 0.4390309838058319425, -1.967887491402267486 ) ) ;
#132315=CARTESIAN_POINT ( 'NONE',  ( 2.121465551170404140, -1.771062468586531047, 0.4427346646293239818 ) ) ;
#132316=CARTESIAN_POINT ( 'NONE',  ( 6.670655732516626912, 7.629137130509076492, 2.426260288887295502 ) ) ;
#132318=ORIENTED_EDGE ( 'NONE', *, *, #32535, .F. ) ;
#132322=CARTESIAN_POINT ( 'NONE',  ( -0.1930879795662324705, -0.4444491470046680326, -1.977061965688177825 ) ) ;
#132323=CARTESIAN_POINT ( 'NONE',  ( 0.04773460823432121303, -1.936894771697717621, 0.8635138731061947626 ) ) ;
#132328=CARTESIAN_POINT ( 'NONE',  ( 6.034070662188514511, 1.017841854155163706, -1.791927558475673754 ) ) ;
#132329=CARTESIAN_POINT ( 'NONE',  ( 5.291638762709002464, 1.525045427759319727, -1.319226660814104335 ) ) ;
#132331=EDGE_LOOP ( 'NONE', ( #104070, #184082, #37687, #56079 ) ) ;
#132335=CARTESIAN_POINT ( 'NONE',  ( 0.2331563151865738703, 7.629137130509052511, -2.545728013813946866 ) ) ;
#132338=CARTESIAN_POINT ( 'NONE',  ( 5.606796008369615336, 0.8196459417171353401, -1.842166028910074527 ) ) ;
#132339=CARTESIAN_POINT ( 'NONE',  ( 4.277188459880359339, 1.204364621523913437, 1.392669941884729035 ) ) ;
#132341=CARTESIAN_POINT ( 'NONE',  ( 3.370030522709596355, 2.251568201494443588, -0.5052104078027676026 ) ) ;
#132343=CARTESIAN_POINT ( 'NONE',  ( 4.341216920475977403, -1.883070171734081200, 1.061215411333437109 ) ) ;
#132344=CARTESIAN_POINT ( 'NONE',  ( 3.380092458137720968, -2.014432998692190058, -0.09411721906785883163 ) ) ;
#132346=CARTESIAN_POINT ( 'NONE',  ( 0.9076408456279178028, -0.8746481411591797706, -1.734042483418346547 ) ) ;
#132351=CARTESIAN_POINT ( 'NONE',  ( 3.045614982896325262, 0.6747646648952825288, -1.744891315567910439 ) ) ;
#132354=CARTESIAN_POINT ( 'NONE',  ( 1.089939655121434203, 1.141396045679959004, 1.534244836814010693 ) ) ;
#132357=CARTESIAN_POINT ( 'NONE',  ( 3.053566222061272040, -1.804402116661915967, -1.270350324234905903 ) ) ;
#132364=CARTESIAN_POINT ( 'NONE',  ( 0.9835902346791641770, 1.320712255264442803, 1.463733941802777716 ) ) ;
#132365=CARTESIAN_POINT ( 'NONE',  ( 6.621674845842873580, -2.240319515690874397, 0.5532079777821105049 ) ) ;
#132366=CARTESIAN_POINT ( 'NONE',  ( 1.521847698614446687, 1.933392594956625521, -0.3320675068423510345 ) ) ;
#132367=CARTESIAN_POINT ( 'NONE',  ( 5.383662037909134668, -1.960299721042932930, 0.6417261926762083402 ) ) ;
#132374=CARTESIAN_POINT ( 'NONE',  ( 0.7784788067067629491, -1.160020112895485456, -1.834993543685500939 ) ) ;
#132376=CARTESIAN_POINT ( 'NONE',  ( 5.899929530298204661, -0.6689130865737795695, -1.715630562827724637 ) ) ;
#132377=ADVANCED_FACE ( 'NONE', ( #24381 ), #13978, .T. ) ;
#132380=CARTESIAN_POINT ( 'NONE',  ( 1.352582913587907942, -1.478046865151939393, 1.146363905606573086 ) ) ;
#132381=CARTESIAN_POINT ( 'NONE',  ( 5.905597126736788383, -0.5315564325061740147, 2.095088507090197893 ) ) ;
#132387=CARTESIAN_POINT ( 'NONE',  ( 0.9789966485893276671, -1.729064073676725544, -0.8170501332188941923 ) ) ;
#132388=CARTESIAN_POINT ( 'NONE',  ( 2.570886989259568267, 0.08925172825972882418, -1.767725737713058631 ) ) ;
#132389=CARTESIAN_POINT ( 'NONE',  ( 1.260255548581414642, 1.910129771108992625, 0.09294656408432439010 ) ) ;
#132391=CARTESIAN_POINT ( 'NONE',  ( 4.939036846723444008, -1.620647644904899654, -1.020970555301304206 ) ) ;
#132392=CARTESIAN_POINT ( 'NONE',  ( 6.021921669442146907, 1.940670798679052123, -0.3350140356708011802 ) ) ;
#132394=CARTESIAN_POINT ( 'NONE',  ( 1.476976393720278002, -1.495863523836362896, 1.503369785937097136 ) ) ;
#132396=CARTESIAN_POINT ( 'NONE',  ( 4.047608660086319254, 0.6306619223146043840, -1.761260876548931709 ) ) ;
#132397=CARTESIAN_POINT ( 'NONE',  ( 0.2053145577999641036, -0.4904175937916722128, 1.758528939493007481 ) ) ;
#132399=CARTESIAN_POINT ( 'NONE',  ( 4.881566871873391555, 2.059980941486462047, -0.7921658822237286346 ) ) ;
#132402=CARTESIAN_POINT ( 'NONE',  ( 1.662626038903247228, -0.7403543059694576156, -1.925410787417888958 ) ) ;
#132408=CARTESIAN_POINT ( 'NONE',  ( 6.486579876843340919, -1.171037552013409089, 1.512559164390047561 ) ) ;
#132410=CARTESIAN_POINT ( 'NONE',  ( 4.457524453155742528, 1.660904245173303373, 1.235824716467534889 ) ) ;
#132412=CARTESIAN_POINT ( 'NONE',  ( 1.774925396934714295, -2.051924176137665423, -0.6798970441593693570 ) ) ;
#132414=CARTESIAN_POINT ( 'NONE',  ( 1.611979286579327431, -0.6784349324776539625, 1.902464779174169562 ) ) ;
#132421=CARTESIAN_POINT ( 'NONE',  ( 0.1808755166769344669, 1.673851406602990366, -1.124249698880399162 ) ) ;
#132423=CARTESIAN_POINT ( 'NONE',  ( 5.214472588068230330, 2.024700573814151028, 0.8392323156421463981 ) ) ;
#132425=CARTESIAN_POINT ( 'NONE',  ( 3.832203377193269755, -0.9874410831685247469, -1.637625244210038300 ) ) ;
#132429=CARTESIAN_POINT ( 'NONE',  ( 2.513296185832504470, -1.880429104915388727, 0.7283969491318904588 ) ) ;
#132431=CARTESIAN_POINT ( 'NONE',  ( 0.5040057298127769148, -2.280580521882575429, 0.2324455964911649464 ) ) ;
#132433=CARTESIAN_POINT ( 'NONE',  ( 4.418794198169028853, 1.577559062085803765, 0.6976772398503274797 ) ) ;
#132437=CARTESIAN_POINT ( 'NONE',  ( 0.7484013653801385724, -1.946605496936428370, -0.2438083268051088881 ) ) ;
#132440=CARTESIAN_POINT ( 'NONE',  ( 0.1753634416057740786, 1.334841368177059895, -2.397339160348281428 ) ) ;
#132441=EDGE_LOOP ( 'NONE', ( #105017, #198037, #56991, #94624 ) ) ;
#132446=CARTESIAN_POINT ( 'NONE',  ( 5.145072886348948771, 0.1388508722429954989, 1.806219837558323826 ) ) ;
#132451=CARTESIAN_POINT ( 'NONE',  ( 5.971335983229998590, -1.557292021941504734, -0.9250951156042800383 ) ) ;
#132455=CARTESIAN_POINT ( 'NONE',  ( 6.408657378324259746, 0.5850815967071677504, 1.766781856238110127 ) ) ;
#132457=CARTESIAN_POINT ( 'NONE',  ( 3.286649939900693429, 1.508079230315559016, -1.181058552281685659 ) ) ;
#132461=CARTESIAN_POINT ( 'NONE',  ( 5.770749444886737578, -0.3132382886438951908, -2.093953712743265694 ) ) ;
#132462=CARTESIAN_POINT ( 'NONE',  ( 0.2159880523044250267, -2.119658899406823505, 0.4233941889316418239 ) ) ;
#132465=CARTESIAN_POINT ( 'NONE',  ( 1.395219695971817941, 1.379742824092672349, 1.195523663710513995 ) ) ;
#132467=CARTESIAN_POINT ( 'NONE',  ( 3.750846114953470867, -1.492790808496821775, 1.050590184284278861 ) ) ;
#132469=CARTESIAN_POINT ( 'NONE',  ( 2.513799616133075343, -0.5961229146635020903, 1.817204401178821760 ) ) ;
#132471=CARTESIAN_POINT ( 'NONE',  ( 3.174220446822792141, -0.9683065041741106826, -1.714983525329449421 ) ) ;
#132472=CARTESIAN_POINT ( 'NONE',  ( 4.792492878049551486, 1.612589784423448025, -1.081918670939057137 ) ) ;
#132475=CARTESIAN_POINT ( 'NONE',  ( 5.660427296577901224, 2.118236611397010805, 0.1021076702828054988 ) ) ;
#132477=CARTESIAN_POINT ( 'NONE',  ( 2.736851483355093873, 1.801321139115559244, 0.6423184003811268639 ) ) ;
#132484=CARTESIAN_POINT ( 'NONE',  ( 4.582524934692378871, -1.771534430979417429, -0.4408631061849078714 ) ) ;
#132485=CARTESIAN_POINT ( 'NONE',  ( 0.8013346216862862192, -1.776568573310655985, 1.062853015585236482 ) ) ;
#132489=CARTESIAN_POINT ( 'NONE',  ( 5.401189721097995111, 1.529905263132097071, 1.076157610686766075 ) ) ;
#132501=CARTESIAN_POINT ( 'NONE',  ( 6.719587830005472995, 0.3798626643731088937, -2.137457590422507714 ) ) ;
#132502=CARTESIAN_POINT ( 'NONE',  ( 2.689187139871064502, 1.790190400678292715, 1.130151903539077463 ) ) ;
#132505=CARTESIAN_POINT ( 'NONE',  ( 6.614133338355735248, 2.065126723422955557, -0.1462301744803648496 ) ) ;
#132510=CARTESIAN_POINT ( 'NONE',  ( 2.326505592738498329, 2.223965110380062615, 0.5549310701656160472 ) ) ;
#132511=CARTESIAN_POINT ( 'NONE',  ( 0.01192831195480706721, -0.7772932952810689411, -1.650495136788888040 ) ) ;
#132512=CARTESIAN_POINT ( 'NONE',  ( 0.2333690889706726279, 7.629137130509075604, -2.653349640194931247 ) ) ;
#132513=CARTESIAN_POINT ( 'NONE',  ( 2.496234081663367022, -0.9796988711565941532, 1.642222327643327873 ) ) ;
#132517=CARTESIAN_POINT ( 'NONE',  ( 0.1760394598168211200, 1.990691791301450575, -0.2996127288820998325 ) ) ;
#132518=CARTESIAN_POINT ( 'NONE',  ( 0.8484012048698870156, -1.946262134508335739, -0.2457884297097159831 ) ) ;
#132522=CARTESIAN_POINT ( 'NONE',  ( 3.521503319566265944, -1.245636697800769355, -1.678868242315070258 ) ) ;
#132523=CARTESIAN_POINT ( 'NONE',  ( 2.887294646099856532, 1.250245360129684791, 1.252957939402859600 ) ) ;
#132526=CARTESIAN_POINT ( 'NONE',  ( 5.437530556340149701, 0.9332327497303912756, -2.093863557220442484 ) ) ;
#132527=CARTESIAN_POINT ( 'NONE',  ( 3.696946667989671642, -0.5033324012985186391, 1.665945954428204923 ) ) ;
#132531=CARTESIAN_POINT ( 'NONE',  ( 2.899396954618923772, 0.2085115220819243054, 1.721149687620449953 ) ) ;
#132532=CARTESIAN_POINT ( 'NONE',  ( 3.297511149327167601, -1.916070068265750992, 1.021083071776592410 ) ) ;
#132534=CARTESIAN_POINT ( 'NONE',  ( 5.823453932400854960, -1.463924103857511039, -1.387103351090559711 ) ) ;
#132535=CARTESIAN_POINT ( 'NONE',  ( 0.6875000000000004441, -1.451031289061094132, 1.451031289061148755 ) ) ;
#132537=CARTESIAN_POINT ( 'NONE',  ( 2.186434445367648749, -1.888794084208703206, -0.3779312967549207092 ) ) ;
#132539=CARTESIAN_POINT ( 'NONE',  ( 5.625276811391259457, 1.958927336128764241, 1.047432077188856780 ) ) ;
#132541=CARTESIAN_POINT ( 'NONE',  ( 6.883263157960391787, 1.249388486322531078, 2.158948101847418144 ) ) ;
#132545=CARTESIAN_POINT ( 'NONE',  ( 1.629831963231648029, -0.2677717415913836718, 2.205032603725831652 ) ) ;
#132550=CARTESIAN_POINT ( 'NONE',  ( 4.545415624535277921, 1.843838458276589209, -0.9247144854665176883 ) ) ;
#132554=CARTESIAN_POINT ( 'NONE',  ( 5.852782322939767745, -1.474943281369223369, 1.150351685248012457 ) ) ;
#132555=CARTESIAN_POINT ( 'NONE',  ( 4.764171500175623741, 1.615563337074712225, -0.6307657835151522230 ) ) ;
#132556=CARTESIAN_POINT ( 'NONE',  ( 3.983749006537410153, -1.722186279587777369, -0.2504274415035238621 ) ) ;
#132558=CARTESIAN_POINT ( 'NONE',  ( 2.085838899777220590, -0.9763249575661275825, 2.074189754910108263 ) ) ;
#132560=CARTESIAN_POINT ( 'NONE',  ( 6.269093502906415871, 2.000459608610676288, -0.6076830679577133187 ) ) ;
#132561=CARTESIAN_POINT ( 'NONE',  ( 1.517261703430743625, -1.021610662766696764, -1.531488883528262512 ) ) ;
#132562=CARTESIAN_POINT ( 'NONE',  ( 1.723279953462612202, 1.994870059565261755, 0.2930690452552578429 ) ) ;
#132568=CARTESIAN_POINT ( 'NONE',  ( 3.264422710156249963, 2.120667954687505574, -0.001943060928578931989 ) ) ;
#132570=CARTESIAN_POINT ( 'NONE',  ( 5.566980414702134894, -1.652319403193935887, -0.7768266693391965294 ) ) ;
#132576=CARTESIAN_POINT ( 'NONE',  ( 3.621357264417348620, 1.734514936435461507, 1.034602781942542515 ) ) ;
#132577=CARTESIAN_POINT ( 'NONE',  ( 6.633804142636003931, -1.436369002829580133, -1.675418478561958802 ) ) ;
#132580=CARTESIAN_POINT ( 'NONE',  ( 4.662867571641106323, 1.440366211568647303, -1.178370841985799888 ) ) ;
#132585=CARTESIAN_POINT ( 'NONE',  ( 6.473517581629535833, 1.972881934646727231, -0.5958391983454867091 ) ) ;
#132590=CARTESIAN_POINT ( 'NONE',  ( 1.211752002169782738, -1.362220228754877027, -1.072495211514002289 ) ) ;
#132591=CARTESIAN_POINT ( 'NONE',  ( 0.7436347644121766853, 0.5012835123295921180, 1.666554394910790382 ) ) ;
#132592=CARTESIAN_POINT ( 'NONE',  ( 6.533790081910475500, -1.501629927769430273, -1.752384480091616847 ) ) ;
#132595=CARTESIAN_POINT ( 'NONE',  ( 2.161468745749118625, 0.3553341821136410950, -2.029755476197503850 ) ) ;
#132596=CARTESIAN_POINT ( 'NONE',  ( 1.686874821769188237, -1.117660090026689979, -1.677749154088927552 ) ) ;
#132599=CARTESIAN_POINT ( 'NONE',  ( 0.1980364362535640133, -1.970970528886636153, -0.05095907160383715551 ) ) ;
#132600=CARTESIAN_POINT ( 'NONE',  ( 4.939673314881130040, -1.814047719456039154, 0.6055163330952323397 ) ) ;
#132602=CARTESIAN_POINT ( 'NONE',  ( 5.654950187766193181, -1.741821662664808867, 1.355018943897445149 ) ) ;
#132606=CARTESIAN_POINT ( 'NONE',  ( 6.604144390287855160, -0.9070803646254663732, 1.914764756563241965 ) ) ;
#132608=CARTESIAN_POINT ( 'NONE',  ( 3.487651025411703021, 2.087124329425969371, -0.9845696281253720761 ) ) ;
#132609=CARTESIAN_POINT ( 'NONE',  ( 4.580490334204036174, 1.208584658811951762, -1.545285769342201965 ) ) ;
#132610=CARTESIAN_POINT ( 'NONE',  ( 1.393326438508041942, -1.775833184744341375, 0.8338576968042878956 ) ) ;
#132614=CARTESIAN_POINT ( 'NONE',  ( -0.06503379110851194300, -1.696408147887063178, 1.266814603907985504 ) ) ;
#132616=CARTESIAN_POINT ( 'NONE',  ( 1.288719586054212884, 1.393062650230517674, 1.203921758438614376 ) ) ;
#132617=CARTESIAN_POINT ( 'NONE',  ( 4.293918747171243666, -1.492831977124044363, -1.576629974643141363 ) ) ;
#132619=CARTESIAN_POINT ( 'NONE',  ( 1.336355901170083849, -1.182550835430173919, -1.760063440837428272 ) ) ;
#132625=CARTESIAN_POINT ( 'NONE',  ( 2.284514177335088991, -2.020382039854185408, -0.4051362335234820478 ) ) ;
#132626=CIRCLE ( 'NONE', #39204, 0.04999999999999883010 ) ;
#132632=CARTESIAN_POINT ( 'NONE',  ( 4.441997247558228779, -1.179148908705367482, -1.505365500079666852 ) ) ;
#132634=CARTESIAN_POINT ( 'NONE',  ( 1.564152511173346749, 2.229009205740081434, -0.3863987453041685116 ) ) ;
#132636=CARTESIAN_POINT ( 'NONE',  ( 0.9491188979427627181, -1.637284982186116400, 0.7756696494297130595 ) ) ;
#132637=CARTESIAN_POINT ( 'NONE',  ( 2.342874207364954220, -1.669023557642179467, -0.9401844802782586275 ) ) ;
#132638=CARTESIAN_POINT ( 'NONE',  ( 2.752462066230080495, -2.064650614848703825, -0.1547973748374023295 ) ) ;
#132640=CARTESIAN_POINT ( 'NONE',  ( 0.9363264705049412218, 1.941902958617349961, 0.3393069938249710371 ) ) ;
#132641=CARTESIAN_POINT ( 'NONE',  ( 5.549420396211061757, -1.520166291496179323, -1.183330462961203589 ) ) ;
#132642=CARTESIAN_POINT ( 'NONE',  ( 1.506910664365119334, -0.8341063803433286239, -2.151852887045426765 ) ) ;
#132645=CARTESIAN_POINT ( 'NONE',  ( 5.301261097381549270, -1.770826635688247386, 1.057502194177829979 ) ) ;
#132651=CARTESIAN_POINT ( 'NONE',  ( 5.104563850188495344, -0.7068653695375884949, -1.983929190867816494 ) ) ;
#132654=CARTESIAN_POINT ( 'NONE',  ( 5.290363030411685763, -2.144575937485785566, -0.2703735795691122323 ) ) ;
#132655=CARTESIAN_POINT ( 'NONE',  ( 5.777991907792089599, 1.989422559269612201, -0.3473161181037613954 ) ) ;
#132663=CARTESIAN_POINT ( 'NONE',  ( 3.204314817619222211, 1.275555974797081049, -1.561881975048397209 ) ) ;
#132668=CARTESIAN_POINT ( 'NONE',  ( 5.313408243115379292, -0.3210861823062813314, 2.137610926513198617 ) ) ;
#132673=CARTESIAN_POINT ( 'NONE',  ( 5.835564593388589572, 0.5826401998472263699, -1.930423629703325927 ) ) ;
#132675=CARTESIAN_POINT ( 'NONE',  ( 0.9434950454815290710, 0.7028112840000885209, -1.575391610592514757 ) ) ;
#132680=CARTESIAN_POINT ( 'NONE',  ( 6.538356921592370696, 1.850225872366149105, 0.2742375073267953045 ) ) ;
#132681=CARTESIAN_POINT ( 'NONE',  ( 0.9615884438243198495, -1.588399402277500760, -1.236662224066273019 ) ) ;
#132686=CARTESIAN_POINT ( 'NONE',  ( 2.561320117580662803, -1.761587792986643475, 1.180070990429403555 ) ) ;
#132687=CARTESIAN_POINT ( 'NONE',  ( 1.739861462675455828, 2.010826045486389102, -0.1511602461454417123 ) ) ;
#132688=CARTESIAN_POINT ( 'NONE',  ( 2.443383269832733795, -1.689004019812107460, 0.6554920229192174874 ) ) ;
#132690=CARTESIAN_POINT ( 'NONE',  ( 6.543834100630380846, 0.8322713294773576020, -1.995267709627518427 ) ) ;
#132694=CARTESIAN_POINT ( 'NONE',  ( 0.3564614995229599681, -1.804831555932787657, -0.6427613734035338977 ) ) ;
#132702=CARTESIAN_POINT ( 'NONE',  ( 4.487301133948972343, 1.932317252032596411, -0.9692046190768678349 ) ) ;
#132705=CARTESIAN_POINT ( 'NONE',  ( 2.303126745213024851, -0.3670769733005624369, -2.088442229865586697 ) ) ;
#132707=CARTESIAN_POINT ( 'NONE',  ( 3.268780567936521830, -1.820120084945201500, -0.7576984602858954920 ) ) ;
#132708=CARTESIAN_POINT ( 'NONE',  ( 5.572493885891085519, 0.7809320506734825917, 1.745880147543739325 ) ) ;
#132711=CARTESIAN_POINT ( 'NONE',  ( 6.320757381585181633, -1.393903556229304730, 1.391728847557841542 ) ) ;
#132712=CARTESIAN_POINT ( 'NONE',  ( 1.253738886202176106, 0.7867099759248905588, 1.775636482627058088 ) ) ;
#132720=CARTESIAN_POINT ( 'NONE',  ( 6.147114339676178041, 0.1922309238813116328, 1.902605946959089689 ) ) ;
#132722=CARTESIAN_POINT ( 'NONE',  ( 4.635508124736155366, -2.018492079602551392, 0.8926152185086615454 ) ) ;
#132723=CARTESIAN_POINT ( 'NONE',  ( 2.186817281270125424, -2.164169025584137263, -0.4306803264119417607 ) ) ;
#132725=CARTESIAN_POINT ( 'NONE',  ( 1.102048709075389654, -0.8591247869965330519, 1.708478583560539166 ) ) ;
#132729=CARTESIAN_POINT ( 'NONE',  ( 3.666520218671379006, -0.8364210039109070127, -1.894060025281426585 ) ) ;
#132733=CARTESIAN_POINT ( 'NONE',  ( 1.973706723050288936, 2.068691090354588091, -0.6273066937243013674 ) ) ;
#132734=CARTESIAN_POINT ( 'NONE',  ( 3.632539538618652752, 0.3231117836275976818, 2.167502126216628522 ) ) ;
#132741=CARTESIAN_POINT ( 'NONE',  ( 5.731065183167076249, 1.732634240323025043, 0.07581458514279926231 ) ) ;
#132744=CARTESIAN_POINT ( 'NONE',  ( 4.082924941702062327, 1.964217522864346810, 0.6541895251909736198 ) ) ;
#132745=CARTESIAN_POINT ( 'NONE',  ( 5.202788454032899246, 1.956619031766251737, 0.8093448757829673212 ) ) ;
#132748=CARTESIAN_POINT ( 'NONE',  ( 3.063290813078624719, 1.661244007368352982, 1.057527034793050547 ) ) ;
#132749=CARTESIAN_POINT ( 'NONE',  ( 5.419995920891611085, 1.369053228189264670, -1.838397148955115412 ) ) ;
#132750=CARTESIAN_POINT ( 'NONE',  ( 2.455445036260803349, 0.4872311372507812655, -1.759406031448563557 ) ) ;
#132756=CARTESIAN_POINT ( 'NONE',  ( 3.621343358005862267, 1.728792273982106220, 1.031380397273339078 ) ) ;
#132757=CARTESIAN_POINT ( 'NONE',  ( 3.942202469084721272, -0.9707516781715104237, 1.704694321266352786 ) ) ;
#132760=CARTESIAN_POINT ( 'NONE',  ( 0.07556134207193675179, -0.004209888911949499594, -2.244269416743961187 ) ) ;
#132761=CARTESIAN_POINT ( 'NONE',  ( 0.1344724916707736029, 0.3614680779570299540, 2.059103226732065028 ) ) ;
#132762=CARTESIAN_POINT ( 'NONE',  ( 5.717594842608604289, -1.725906139129701478, 0.3911541089357990497 ) ) ;
#132764=CARTESIAN_POINT ( 'NONE',  ( 2.027518650255655253, -1.432890729411402830, -1.658174735819065049 ) ) ;
#132765=CARTESIAN_POINT ( 'NONE',  ( 0.5908509756735094154, -0.6286620326499070543, 1.623129586062905805 ) ) ;
#132767=CARTESIAN_POINT ( 'NONE',  ( 0.2333690889706682703, 0.003390530909083006028, -2.053566628440507635 ) ) ;
#132768=CARTESIAN_POINT ( 'NONE',  ( 0.8907089605301542479, 1.523294409195220966, -0.8092020298176191284 ) ) ;
#132769=CARTESIAN_POINT ( 'NONE',  ( 0.5975257653535933633, 1.179397575757964001, -1.972621981072789410 ) ) ;
#132770=CARTESIAN_POINT ( 'NONE',  ( 0.9783777488623355278, -2.139296967303818686, -0.4750931833387496694 ) ) ;
#132771=CARTESIAN_POINT ( 'NONE',  ( 3.457846583235091753, 0.5364296187198510646, -2.140574738106671759 ) ) ;
#132773=CARTESIAN_POINT ( 'NONE',  ( 1.464000922811282468, -0.5298712919106687291, 2.105275420227727956 ) ) ;
#132775=CARTESIAN_POINT ( 'NONE',  ( 1.780608593570524034, -0.5699985197749558585, -2.039088110117696750 ) ) ;
#132777=CARTESIAN_POINT ( 'NONE',  ( 5.702155557734973179, -1.926566265495327723, 0.0002483051060025303638 ) ) ;
#132779=CARTESIAN_POINT ( 'NONE',  ( 2.595625714788946770, -0.7159257691751429453, 2.177794363412302481 ) ) ;
#132783=CARTESIAN_POINT ( 'NONE',  ( 5.004621511133813705, -2.204373672735039147, -0.2730638322096557435 ) ) ;
#132791=CARTESIAN_POINT ( 'NONE',  ( 2.637342451166882373, 0.6819965276749391236, 1.897697610567940174 ) ) ;
#132793=CARTESIAN_POINT ( 'NONE',  ( 1.129816159781659390, 1.988900438959967376, -0.5462022044933153575 ) ) ;
#132799=CARTESIAN_POINT ( 'NONE',  ( 3.662233025353780480, -1.472007171213615351, 1.623636439255560227 ) ) ;
#132800=CARTESIAN_POINT ( 'NONE',  ( 0.9674229098759130618, -1.967888300253183953, -0.4390273639364171698 ) ) ;
#132801=CARTESIAN_POINT ( 'NONE',  ( 0.9250624443557056154, -1.167992581197497604, -1.423340509374780405 ) ) ;
#132802=CARTESIAN_POINT ( 'NONE',  ( 5.091491514903929705, -0.8269519956315901643, 2.138199492833972482 ) ) ;
#132803=CARTESIAN_POINT ( 'NONE',  ( 4.488128036367874607, -0.4058819498431766037, -1.795677737744493019 ) ) ;
#132806=CARTESIAN_POINT ( 'NONE',  ( 5.543921259432438298, 0.7380120197021734496, -1.669944898041133552 ) ) ;
#132807=CARTESIAN_POINT ( 'NONE',  ( 6.399064592084179992, -0.9530083391863402031, -1.777013033299412292 ) ) ;
#132809=CARTESIAN_POINT ( 'NONE',  ( 5.014671263542332724, 1.563880152264264245, -1.635232377595864595 ) ) ;
#132811=CARTESIAN_POINT ( 'NONE',  ( 6.616252143301227129, -0.9890948110137095517, -1.859226117534703571 ) ) ;
#132813=CARTESIAN_POINT ( 'NONE',  ( 4.615722581382986967, 0.4567890626981512270, -2.019179087418949692 ) ) ;
#132819=CARTESIAN_POINT ( 'NONE',  ( 2.578635874325632127, -1.843646926959886523, -0.5589146710999506329 ) ) ;
#132824=CARTESIAN_POINT ( 'NONE',  ( 1.037531286769650452, -0.04638328994046451298, 2.120250110247793085 ) ) ;
#132825=CARTESIAN_POINT ( 'NONE',  ( 1.389269710167878369, -2.111442789942123088, -0.6905784607170639688 ) ) ;
#132826=CARTESIAN_POINT ( 'NONE',  ( 3.311648941680225722, -0.4124737740866398217, 2.064988983437756165 ) ) ;
#132829=CARTESIAN_POINT ( 'NONE',  ( 3.543363863352413823, 1.774678991803163575, -0.8365776047038612218 ) ) ;
#132835=CARTESIAN_POINT ( 'NONE',  ( 2.162495577681341707, 2.120227376586072854, 0.04728746717985036346 ) ) ;
#132837=CARTESIAN_POINT ( 'NONE',  ( 4.668382477721988444, -0.8370036265390871089, -1.774476930476886594 ) ) ;
#132838=CARTESIAN_POINT ( 'NONE',  ( 2.729541802387557059, -2.017400560480298033, 0.7770373237434913261 ) ) ;
#132839=CARTESIAN_POINT ( 'NONE',  ( 3.315785976855676775, 1.165629053876730659, -1.425327459889616399 ) ) ;
#132842=CARTESIAN_POINT ( 'NONE',  ( 4.329842768969596634, 1.707365525456190358, 0.3361313568818121156 ) ) ;
#132846=CARTESIAN_POINT ( 'NONE',  ( 1.727627455807039691, -2.035446057602477321, 0.7283451284763039490 ) ) ;
#132847=CARTESIAN_POINT ( 'NONE',  ( 3.989611116449209405, 1.913510565032714883, 0.6351021849077125303 ) ) ;
#132849=CARTESIAN_POINT ( 'NONE',  ( 1.657319961134783748, -1.854130675604428902, -1.111159678259740602 ) ) ;
#132850=CARTESIAN_POINT ( 'NONE',  ( 2.957844615808038480, 1.962099266425470390, -0.1918489139557562340 ) ) ;
#132851=CARTESIAN_POINT ( 'NONE',  ( 6.509000000000014552, 2.959959533984284352, 2.552917358632576850 ) ) ;
#132852=CARTESIAN_POINT ( 'NONE',  ( 3.315898775378321339, 1.229719374647167296, -1.503149361444736876 ) ) ;
#132861=CARTESIAN_POINT ( 'NONE',  ( 0.6927435329204565395, -2.190372518412486702, -0.2681103625320201411 ) ) ;
#132863=CARTESIAN_POINT ( 'NONE',  ( 5.014483083204026137, 0.7471541359172824137, 1.814103259000845458 ) ) ;
#132864=CARTESIAN_POINT ( 'NONE',  ( 2.496720397819631732, -1.994071314890283553, 0.2986276487200872354 ) ) ;
#132866=CARTESIAN_POINT ( 'NONE',  ( 3.046228577489984879, 0.9562745863303960814, 1.889201325992972080 ) ) ;
#132870=CARTESIAN_POINT ( 'NONE',  ( 3.925598083870453614, 0.9833751987384667936, -1.556331266066004027 ) ) ;
#132875=CARTESIAN_POINT ( 'NONE',  ( 5.695592476053609410, 1.958610405324921588, -0.8133567297157192622 ) ) ;
#132876=EDGE_CURVE ( 'NONE', #190431, #137219, #149742, .T. ) ;
#132879=CARTESIAN_POINT ( 'NONE',  ( 5.343066995996487378, -1.769704953023493399, 1.055641863377870138 ) ) ;
#132881=CARTESIAN_POINT ( 'NONE',  ( 0.4845113730182957767, 1.779151863920569232, 0.5459849130424464514 ) ) ;
#132882=CARTESIAN_POINT ( 'NONE',  ( 1.962219809069129184, -1.683971100191889336, -0.7449956418128443891 ) ) ;
#132886=CARTESIAN_POINT ( 'NONE',  ( 1.700138637298425737, -0.7412910010123253679, 2.078789392164873906 ) ) ;
#132887=CARTESIAN_POINT ( 'NONE',  ( 5.360715614582075794, -1.643942929158914268, 1.554587190974612732 ) ) ;
#132889=CARTESIAN_POINT ( 'NONE',  ( 4.904484127313208042, -1.798792703336571375, -0.2141664767603863595 ) ) ;
#132890=CARTESIAN_POINT ( 'NONE',  ( 4.979654327277899917, -0.6834858053395581612, 1.789849564252174119 ) ) ;
#132892=CARTESIAN_POINT ( 'NONE',  ( 4.838664814796108438, 0.3202261158844340594, 1.842872994462002367 ) ) ;
#132893=CARTESIAN_POINT ( 'NONE',  ( 5.213276571848306951, -1.572085989900060765, -0.9957144527335654027 ) ) ;
#132895=CARTESIAN_POINT ( 'NONE',  ( 6.368005316177769437, 0.9137572655052300652, 1.515547905889617519 ) ) ;
#132896=CARTESIAN_POINT ( 'NONE',  ( 0.6730650033222317363, 1.776164188848127878, -0.9548607967814757291 ) ) ;
#132898=CARTESIAN_POINT ( 'NONE',  ( 2.332770561069871462, 2.043027141408111813, 0.5109185277013729154 ) ) ;
#132903=CARTESIAN_POINT ( 'NONE',  ( 1.547134890100225535, 0.2020692043026971751, 2.009678023649637879 ) ) ;
#132905=CARTESIAN_POINT ( 'NONE',  ( 6.720655732516650716, 1.307757891114844417, 1.844004982043083940 ) ) ;
#132908=CARTESIAN_POINT ( 'NONE',  ( 1.950665695202157046, 0.6760947502928333908, 2.053231632317173538 ) ) ;
#132909=CARTESIAN_POINT ( 'NONE',  ( 6.610000000000002096, 6.034162285353575683, 2.874900418788868262 ) ) ;
#132916=CARTESIAN_POINT ( 'NONE',  ( 0.8553300576445364012, 0.4222666777726029608, -2.150330908352434012 ) ) ;
#132918=CARTESIAN_POINT ( 'NONE',  ( 1.868429791336771340, 1.163878172895687069, 1.940057763798187951 ) ) ;
#132925=CARTESIAN_POINT ( 'NONE',  ( 3.479546766767865673, 1.120508650343427171, 1.369845563140754230 ) ) ;
#132927=CARTESIAN_POINT ( 'NONE',  ( 0.08314155087942810829, -0.1569203414564980525, -2.071771216027401774 ) ) ;
#132931=CARTESIAN_POINT ( 'NONE',  ( 5.694935465533643715, 1.779635825068434984, 0.9480254120717497290 ) ) ;
#132933=CARTESIAN_POINT ( 'NONE',  ( 2.623731232481395725, -1.075365945362505293, -1.530472918023266571 ) ) ;
#132934=CARTESIAN_POINT ( 'NONE',  ( 2.483334644719074724, -0.004358110040847408898, 2.070434559716929357 ) ) ;
#132937=CARTESIAN_POINT ( 'NONE',  ( 2.285291272251275707, 0.09004542135446562401, -1.910373438827176251 ) ) ;
#132943=CARTESIAN_POINT ( 'NONE',  ( 0.2461629937395051482, 0.9812432698282258503, -1.641294572782559635 ) ) ;
#132946=CARTESIAN_POINT ( 'NONE',  ( 2.453501617077270769, 1.514643136537169310, 1.246875331876770243 ) ) ;
#132949=CARTESIAN_POINT ( 'NONE',  ( 5.660427296577901224, 2.118236611397011249, 0.1021076702828054988 ) ) ;
#132953=CARTESIAN_POINT ( 'NONE',  ( 0.1923495491853322581, -0.4021996241703913455, -1.833441224692602844 ) ) ;
#132955=CARTESIAN_POINT ( 'NONE',  ( 2.355728993131640525, -1.494696414742059387, -1.348868867694212881 ) ) ;
#132957=CARTESIAN_POINT ( 'NONE',  ( 1.054496592829538004, -1.339774933521440392, 1.639435421165438500 ) ) ;
#132959=CARTESIAN_POINT ( 'NONE',  ( 2.453653613718423276, 1.598880132357576755, 1.315258840600006085 ) ) ;
#132963=CARTESIAN_POINT ( 'NONE',  ( 6.070280604649140876, -1.984772539198733865, -0.6570628365835521345 ) ) ;
#132965=CARTESIAN_POINT ( 'NONE',  ( 3.821172736587064023, -0.1348131347885111742, 1.820669774636254346 ) ) ;
#132966=CARTESIAN_POINT ( 'NONE',  ( 2.402729293200474459, -0.3110027565414590356, -1.784399550462684392 ) ) ;
#132971=CARTESIAN_POINT ( 'NONE',  ( 5.385833121705805304, 1.478444731487274622, 1.638484004604986000 ) ) ;
#132974=CARTESIAN_POINT ( 'NONE',  ( 3.721269560815092525, 1.641568950759502377, 0.9805937191851579193 ) ) ;
#132982=CARTESIAN_POINT ( 'NONE',  ( 0.4855842612344652975, -1.827229208960782447, -0.2260576252584786672 ) ) ;
#132985=CARTESIAN_POINT ( 'NONE',  ( 4.622238261848357510, 1.152259890254858421, -1.473394524551619789 ) ) ;
#132991=CARTESIAN_POINT ( 'NONE',  ( 1.744903480705553012, -0.2836847097360816194, -1.948756091721944861 ) ) ;
#132992=CARTESIAN_POINT ( 'NONE',  ( 2.653922917551009952, 1.081085551080329443, 1.701936510390424928 ) ) ;
#132996=CARTESIAN_POINT ( 'NONE',  ( 2.853686581259745836, 2.180823047698337902, -0.2155538573413370296 ) ) ;
#132997=CARTESIAN_POINT ( 'NONE',  ( 6.604126001430527637, -1.825160783932573860, 0.05055279568313279792 ) ) ;
#133008=CARTESIAN_POINT ( 'NONE',  ( 3.913478945735289205, -0.9499487412085620974, -1.577145280185827447 ) ) ;
#133009=CARTESIAN_POINT ( 'NONE',  ( 1.225244855396601551, 1.776329837998322780, 0.9471711224926461226 ) ) ;
#133010=CARTESIAN_POINT ( 'NONE',  ( 3.023178501820302344, 2.287506772329782390, -0.2231754551033394429 ) ) ;
#133012=CARTESIAN_POINT ( 'NONE',  ( 0.6900174830311635032, 0.9632304765912635958, -1.592144255797292463 ) ) ;
#133016=CARTESIAN_POINT ( 'NONE',  ( 4.851772015791367743, -1.356534033432246211, -1.348250844427544282 ) ) ;
#133019=CARTESIAN_POINT ( 'NONE',  ( 3.948837864290375421, -1.739349124335771712, -1.159800787976144720 ) ) ;
#133020=CARTESIAN_POINT ( 'NONE',  ( 2.166681600665042229, -1.709288833360942617, -0.7604731621856930524 ) ) ;
#133023=CARTESIAN_POINT ( 'NONE',  ( 5.882333747326812023, -0.2767177626767613474, -1.820229446528654371 ) ) ;
#133026=CARTESIAN_POINT ( 'NONE',  ( 3.773808747373870620, 0.9599976342714054978, 1.432812656881277791 ) ) ;
#133028=CARTESIAN_POINT ( 'NONE',  ( 6.656857027519620829, -1.708965229049699053, 1.396003577074665714 ) ) ;
#133030=CARTESIAN_POINT ( 'NONE',  ( 4.416952212917071741, -1.612892420192946652, 1.453532087098859504 ) ) ;
#133031=CARTESIAN_POINT ( 'NONE',  ( 3.246530741642670304, 0.4443377543969920795, 1.770662692542070538 ) ) ;
#133032=CARTESIAN_POINT ( 'NONE',  ( 0.7956631384608278124, -1.383255022760669251, -1.391342014947574146 ) ) ;
#133033=CARTESIAN_POINT ( 'NONE',  ( 5.243409334377605369, 0.4101777817676309223, -2.077071965933465769 ) ) ;
#133036=CARTESIAN_POINT ( 'NONE',  ( 6.233931918547526152, 2.266764885754421144, 0.3408509611897111991 ) ) ;
#133039=CARTESIAN_POINT ( 'NONE',  ( 1.541811043186253061, -1.995513645039903361, 0.7175487213698438227 ) ) ;
#133043=CARTESIAN_POINT ( 'NONE',  ( 6.596539238361469160, 2.146192635953731553, 0.3271905807876190897 ) ) ;
#133044=CARTESIAN_POINT ( 'NONE',  ( 6.983263157960365675, 7.629137130509066722, 2.553810918356711479 ) ) ;
#133046=CARTESIAN_POINT ( 'NONE',  ( 1.981385142061100835, -2.032350350298214980, -0.8968915317347254668 ) ) ;
#133048=CARTESIAN_POINT ( 'NONE',  ( -0.05159450770049476415, -2.057278634402651907, -1.025749021234131364 ) ) ;
#133050=CARTESIAN_POINT ( 'NONE',  ( 4.996965725392733759, 0.3474287616172208604, 2.032942699294958633 ) ) ;
#133056=CARTESIAN_POINT ( 'NONE',  ( 0.1331565106231328843, 0.003911343561965873426, -1.946049565259087455 ) ) ;
#133057=CARTESIAN_POINT ( 'NONE',  ( 0.6563342376118604937, -1.512884991606887386, 1.443139479479842668 ) ) ;
#133058=CARTESIAN_POINT ( 'NONE',  ( 5.168592345394213972, 1.356298078840772803, 1.492257005506092193 ) ) ;
#133059=CARTESIAN_POINT ( 'NONE',  ( 4.493604616018744835, -1.840970053361364656, -0.04044509776383875543 ) ) ;
#133064=CARTESIAN_POINT ( 'NONE',  ( 2.256509660847346943, -1.335373073873729943, 1.091610183656815503 ) ) ;
#133065=CARTESIAN_POINT ( 'NONE',  ( 0.05782782957228919940, 1.164991625563294386, 1.645756161228327130 ) ) ;
#133066=CARTESIAN_POINT ( 'NONE',  ( 1.600609022366938916, -0.2761435782051116505, 2.281986030651184993 ) ) ;
#133068=CARTESIAN_POINT ( 'NONE',  ( 1.019259390987249603, 2.090591978351970859, 0.8652678750288608223 ) ) ;
#133069=CARTESIAN_POINT ( 'NONE',  ( 3.738982163358902877, 0.3088429966837880070, 2.083174605729753992 ) ) ;
#133073=CARTESIAN_POINT ( 'NONE',  ( 5.687500000000004441, -1.451031289060884077, 1.451031289061342378 ) ) ;
#133078=CARTESIAN_POINT ( 'NONE',  ( 5.027667009318355973, -0.3252736580323810633, 2.197331836796195592 ) ) ;
#133079=CARTESIAN_POINT ( 'NONE',  ( 3.662233025353780480, -1.472007171213615351, 1.623636439255560227 ) ) ;
#133083=CARTESIAN_POINT ( 'NONE',  ( 6.889999999999970370, 3.679256271150095792, 2.793895465809397294 ) ) ;
#133085=CARTESIAN_POINT ( 'NONE',  ( 5.256147377898004791, 0.8573370980917979223, -1.939729252509444279 ) ) ;
#133089=CARTESIAN_POINT ( 'NONE',  ( 6.789893189004300389, -0.9291300992274166282, 1.949920244826188309 ) ) ;
#133091=CARTESIAN_POINT ( 'NONE',  ( 6.022987620897008121, -1.731432113864934674, 0.6267441317700100933 ) ) ;
#133094=CARTESIAN_POINT ( 'NONE',  ( 0.7490575545651646516, 1.738588327661923394, -0.08332016361957059192 ) ) ;
#133099=CARTESIAN_POINT ( 'NONE',  ( 5.243122039519461097, -1.856066598825537373, 1.107904190987746063 ) ) ;
#133103=CARTESIAN_POINT ( 'NONE',  ( 4.434552454296070145, 2.119417814153037316, 0.4246342833542292028 ) ) ;
#133106=CARTESIAN_POINT ( 'NONE',  ( 6.344996225704436554, -1.666636976361988154, 1.052594414163325220 ) ) ;
#133107=CARTESIAN_POINT ( 'NONE',  ( 5.044171318280882055, 1.617313383883935529, -0.6254187727454744161 ) ) ;
#133110=CARTESIAN_POINT ( 'NONE',  ( 1.540847765565691585, -1.849059859674206496, 1.176127931831471907 ) ) ;
#133111=CARTESIAN_POINT ( 'NONE',  ( 2.046342449252246620, 0.8823731130137985046, -2.132409122670553270 ) ) ;
#133112=CARTESIAN_POINT ( 'NONE',  ( 4.850885224688990860, -1.657504552092460504, 1.224352689660711535 ) ) ;
#133113=CARTESIAN_POINT ( 'NONE',  ( 0.4802856102240244951, -0.2370191179813440352, -1.927374317010506877 ) ) ;
#133117=CARTESIAN_POINT ( 'NONE',  ( 3.252298345715322281, 0.9499829135306799843, -1.895951488860507128 ) ) ;
#133118=CARTESIAN_POINT ( 'NONE',  ( 1.424454163599726320, -1.462446849824734274, -1.388484543128357229 ) ) ;
#133120=CARTESIAN_POINT ( 'NONE',  ( 4.524592175135637717, 1.360519573838222085, -1.737388959189074100 ) ) ;
#133122=CARTESIAN_POINT ( 'NONE',  ( 1.568971434307638857, 1.638126988201485279, 0.8830449202173286105 ) ) ;
#133124=CARTESIAN_POINT ( 'NONE',  ( 0.1399997263886038068, 6.947785072119228467, -2.594798351071639253 ) ) ;
#133130=CARTESIAN_POINT ( 'NONE',  ( 3.678635468349491511, -1.985665955521208614, -0.5514216839303841544 ) ) ;
#133133=CARTESIAN_POINT ( 'NONE',  ( 3.440107494509841768, -1.204893485711604484, -1.620726792054197452 ) ) ;
#133136=CARTESIAN_POINT ( 'NONE',  ( 1.938423425814293388, 2.038317423364948588, 0.3033609537064930750 ) ) ;
#133140=CARTESIAN_POINT ( 'NONE',  ( -0.2409995289980246258, 1.355929887833319469, -2.254219809973062816 ) ) ;
#133141=CARTESIAN_POINT ( 'NONE',  ( 1.288719586054212884, 1.393062650230517674, 1.203921758438614376 ) ) ;
#133142=CARTESIAN_POINT ( 'NONE',  ( 6.129534211984397629, -2.079372889712034489, 0.7396383780838566846 ) ) ;
#133144=CARTESIAN_POINT ( 'NONE',  ( 2.003414267471514965, 1.795956895356983551, 1.202623776965026536 ) ) ;
#133146=CARTESIAN_POINT ( 'NONE',  ( 2.325407997918966796, -1.497503195670712328, -1.350734289967000512 ) ) ;
#133149=CARTESIAN_POINT ( 'NONE',  ( 4.100430126988792168, -0.6171887515804741486, -1.872443122656509029 ) ) ;
#133151=CARTESIAN_POINT ( 'NONE',  ( 3.309780021317248355, -1.205041885261768808, -1.616693488061982098 ) ) ;
#133155=CARTESIAN_POINT ( 'NONE',  ( 6.445935634123193481, 0.8078061350838610100, -1.945192272397469280 ) ) ;
#133157=CARTESIAN_POINT ( 'NONE',  ( 5.723117673755029777, -1.870111591731966616, -0.8886290660751752224 ) ) ;
#133161=CARTESIAN_POINT ( 'NONE',  ( 5.344012529290226965, -1.284645313656457288, -1.558556736529070674 ) ) ;
#133164=CARTESIAN_POINT ( 'NONE',  ( 0.4091259740910870302, -1.658837074242287102, 1.225595967756993865 ) ) ;
#133170=CARTESIAN_POINT ( 'NONE',  ( 6.727182134110199385, 3.711531441867378600, 2.225637065106730095 ) ) ;
#133172=CARTESIAN_POINT ( 'NONE',  ( 2.717415358725610908, -1.887964963866497259, -1.072103292869843960 ) ) ;
#133176=CARTESIAN_POINT ( 'NONE',  ( 2.700538275128167687, 1.556679782967337999, 0.9830204120172959525 ) ) ;
#133178=CARTESIAN_POINT ( 'NONE',  ( 4.019203527901527018, -2.096847714747759106, 0.6372333828079318474 ) ) ;
#133180=CARTESIAN_POINT ( 'NONE',  ( 4.311571290614625518, -0.3905533787264577894, 2.228413237907675537 ) ) ;
#133185=CARTESIAN_POINT ( 'NONE',  ( 6.555894367415777246, 1.764769525206461687, -0.1329060007094622631 ) ) ;
#133186=CARTESIAN_POINT ( 'NONE',  ( 3.826817946245956392, 1.422007987377239546, -1.425180056034919041 ) ) ;
#133188=CARTESIAN_POINT ( 'NONE',  ( 2.626118769021787536, -1.211593817910999293, -1.722331309457482362 ) ) ;
#133189=CARTESIAN_POINT ( 'NONE',  ( 1.528765853866232538, -1.617345627753681514, 1.026210199876474105 ) ) ;
#133191=CARTESIAN_POINT ( 'NONE',  ( 1.574589453129974004, 1.325232347829819135, -1.457171473731319278 ) ) ;
#133192=CARTESIAN_POINT ( 'NONE',  ( 1.076777757339364205, -0.04213119042271313425, -1.870346338061685154 ) ) ;
#133193=CARTESIAN_POINT ( 'NONE',  ( 0.5198770262540284293, 1.941052373433370448, -0.2841105942011297736 ) ) ;
#133194=CARTESIAN_POINT ( 'NONE',  ( 0.4219365929402639215, -1.902980170924161385, 0.1897552588234762416 ) ) ;
#133199=CARTESIAN_POINT ( 'NONE',  ( 5.840666405660361882, 0.3664468388623157158, 1.834233659845654119 ) ) ;
#133202=CARTESIAN_POINT ( 'NONE',  ( 6.244996659533327943, -0.2978818936431072983, -2.048576297084458098 ) ) ;
#133211=CARTESIAN_POINT ( 'NONE',  ( 6.426224708462171087, 1.007414738832881351, 1.683299376423300853 ) ) ;
#133213=CARTESIAN_POINT ( 'NONE',  ( 3.268907511149142575, -2.013924394373915128, 0.09611935726179518524 ) ) ;
#133214=CARTESIAN_POINT ( 'NONE',  ( 4.135878506090823414, 1.915180532728939289, -0.05283342432932899152 ) ) ;
#133216=CARTESIAN_POINT ( 'NONE',  ( 1.751786407749492014, 2.185395279939935431, -0.1653414253460702699 ) ) ;
#133217=CARTESIAN_POINT ( 'NONE',  ( 0.1333692844072559280, 6.947498546895843674, -2.648624074793118233 ) ) ;
#133218=CARTESIAN_POINT ( 'NONE',  ( 2.987410616422137899, 1.320145714686842497, 1.325460448179466066 ) ) ;
#133222=CARTESIAN_POINT ( 'NONE',  ( 4.077823013788191453, -0.8085361882982607939, 1.956954002425244088 ) ) ;
#133225=CARTESIAN_POINT ( 'NONE',  ( 5.916483165358986440, 0.8355632440216669288, 1.894440869009452300 ) ) ;
#133226=CARTESIAN_POINT ( 'NONE',  ( 2.401997865216979111, -0.8028288615537516604, -1.930668023334235484 ) ) ;
#133227=CARTESIAN_POINT ( 'NONE',  ( 6.620655732516668834, 7.629137130509086262, 2.873739711112702544 ) ) ;
#133228=CARTESIAN_POINT ( 'NONE',  ( 0.6919144707170435948, -1.710882258413017221, -0.2179282654613586834 ) ) ;
#133238=CARTESIAN_POINT ( 'NONE',  ( 0.5217373455332212639, -1.802923944912222520, 0.1758665181858156124 ) ) ;
#133248=CARTESIAN_POINT ( 'NONE',  ( 2.523689441098162511, 1.825779920793478839, -0.3596660026494375995 ) ) ;
#133249=CARTESIAN_POINT ( 'NONE',  ( 0.5795164177304649167, -0.6885740665637375413, 1.787764417203549172 ) ) ;
#133250=CARTESIAN_POINT ( 'NONE',  ( 0.7332529803791461021, 1.960763319057107879, 0.8078710241638600298 ) ) ;
#133253=CARTESIAN_POINT ( 'NONE',  ( -0.1399997263889611598, 2.874570648431204578, -2.488748559936367233 ) ) ;
#133257=CARTESIAN_POINT ( 'NONE',  ( 4.627768981117735159, 1.911305289405954344, -0.4745475857620209958 ) ) ;
#133258=CARTESIAN_POINT ( 'NONE',  ( 1.137531110418067204, -0.04838959064331486287, 2.120096749846810624 ) ) ;
#133262=CARTESIAN_POINT ( 'NONE',  ( 5.595707529797693702, -2.191629465999441084, -0.002916574791289594515 ) ) ;
#133264=CARTESIAN_POINT ( 'NONE',  ( 4.506809989931632288, 1.489605450875215453, -1.221516061710873347 ) ) ;
#133266=CARTESIAN_POINT ( 'NONE',  ( 0.1295496576057716120, -1.118478952742516297, -1.443350188048427629 ) ) ;
#133267=CARTESIAN_POINT ( 'NONE',  ( 0.9091299924109221831, 1.668792687453458878, -1.444214864661397035 ) ) ;
#133270=ORIENTED_EDGE ( 'NONE', *, *, #148486, .T. ) ;
#133273=CARTESIAN_POINT ( 'NONE',  ( 5.717622241336643540, 0.3879015478767386949, -1.930678852912662391 ) ) ;
#133274=CARTESIAN_POINT ( 'NONE',  ( 1.452572125225624955, -1.666495805118956897, -0.9969474394922008820 ) ) ;
#133275=CARTESIAN_POINT ( 'NONE',  ( 6.731773689652298387, -2.096994807688298934, -0.9412720059410217832 ) ) ;
#133277=CARTESIAN_POINT ( 'NONE',  ( 4.434314628233038569, -1.074157013132440275, 1.519412852752539678 ) ) ;
#133283=CARTESIAN_POINT ( 'NONE',  ( -0.07626876867936756288, -1.353788312843669406, -1.724171373301164767 ) ) ;
#133287=CARTESIAN_POINT ( 'NONE',  ( 1.805030607383810715, 1.517133602069477893, 1.015288170653723343 ) ) ;
#133290=CARTESIAN_POINT ( 'NONE',  ( 3.990606130280470509, -1.729166733334456030, 0.1323968765898491939 ) ) ;
#133294=CARTESIAN_POINT ( 'NONE',  ( 0.4164666496747080338, 1.329428171303851824, -1.394508830869565230 ) ) ;
#133295=CARTESIAN_POINT ( 'NONE',  ( 4.803538753074391821, -1.513872852549098091, -1.247617340562396926 ) ) ;
#133298=CARTESIAN_POINT ( 'NONE',  ( 4.547591073264711348, -1.938359017324686961, 0.8602097090630378418 ) ) ;
#133303=CARTESIAN_POINT ( 'NONE',  ( 3.080986915251407776, 1.947773190787219555, 0.7018234266842755531 ) ) ;
#133307=CARTESIAN_POINT ( 'NONE',  ( 2.831036414133382806, 0.8244386821347724492, -2.145926533794308533 ) ) ;
#133313=CARTESIAN_POINT ( 'NONE',  ( 6.609000000000015085, -6.653734696159079563E-05, 2.100160721423646404 ) ) ;
#133318=CARTESIAN_POINT ( 'NONE',  ( 3.867365959033176814, -1.592763314076732106, -1.058159689705892692 ) ) ;
#133320=CARTESIAN_POINT ( 'NONE',  ( 5.139545982361763521, -1.221863454424999329, -1.217595815693907957 ) ) ;
#133321=CARTESIAN_POINT ( 'NONE',  ( 3.204314817619222211, 1.275555974797081049, -1.561881975048397209 ) ) ;
#133322=CARTESIAN_POINT ( 'NONE',  ( 5.326872488440856479, 0.9340183262317149904, -2.100526973934746522 ) ) ;
#133324=CARTESIAN_POINT ( 'NONE',  ( 0.6982365061397632910, -0.7907169553198112322, 2.060542492664858560 ) ) ;
#133326=CARTESIAN_POINT ( 'NONE',  ( 5.571497546025357295, 1.705283197966761310, -0.4730582879079441305 ) ) ;
#133328=CARTESIAN_POINT ( 'NONE',  ( 1.746416057278064482, 0.7220573502318957670, 2.175635376676859689 ) ) ;
#133329=CARTESIAN_POINT ( 'NONE',  ( 6.720655732516648939, 0.005566325962592238129, 1.826293863978686538 ) ) ;
#133335=CARTESIAN_POINT ( 'NONE',  ( 6.478973898625433492, 1.930320082341809629, 0.7489585856828018251 ) ) ;
#133336=CARTESIAN_POINT ( 'NONE',  ( 0.7082206942033396624, 1.197301205363930254, -1.622488844446705381 ) ) ;
#133338=CARTESIAN_POINT ( 'NONE',  ( 5.109954983015153829, -1.917020813385891254, 0.1909056391717136592 ) ) ;
#133340=CARTESIAN_POINT ( 'NONE',  ( 2.285647630545981190, 0.1040316455800850692, -2.219075330209609120 ) ) ;
#133346=CARTESIAN_POINT ( 'NONE',  ( 4.669343813871559945, 1.007284801977660349, 1.419122490755047705 ) ) ;
#133347=CARTESIAN_POINT ( 'NONE',  ( 2.383191274269541360, -0.003000794896521400724, 1.962046632024143866 ) ) ;
#133353=CARTESIAN_POINT ( 'NONE',  ( 1.522013433763437895, 2.032506561856410876, -0.3506121680386958261 ) ) ;
#133356=CARTESIAN_POINT ( 'NONE',  ( 1.200488511320395579, -2.262689073810118412, 0.002107776778791786276 ) ) ;
#133359=CARTESIAN_POINT ( 'NONE',  ( 2.126040175964475143, 1.080828230516362121, -1.526477596812993553 ) ) ;
#133360=CARTESIAN_POINT ( 'NONE',  ( 0.9494047574800461575, -1.567277312892487284, -0.7424874142042283687 ) ) ;
#133361=CARTESIAN_POINT ( 'NONE',  ( 5.530878137806295669, -1.981686641427220286, 0.9361944923952856268 ) ) ;
#133362=CARTESIAN_POINT ( 'NONE',  ( 5.614422408412740317, -1.031215703586242149, -2.064428503307714546 ) ) ;
#133363=CARTESIAN_POINT ( 'NONE',  ( 1.112264416572866566, -0.9257652390157306010, -1.841317064699917516 ) ) ;
#133364=CARTESIAN_POINT ( 'NONE',  ( 3.679572934066538181, -0.9564393601015194202, 1.690012426612282681 ) ) ;
#133367=CARTESIAN_POINT ( 'NONE',  ( 5.940666398231567058, 0.3644617591120716260, 1.834516074763043347 ) ) ;
#133368=CARTESIAN_POINT ( 'NONE',  ( 1.562500000000001554, -1.451031289061184282, -1.451031289061057050 ) ) ;
#133370=CARTESIAN_POINT ( 'NONE',  ( 6.204453847213379447, -1.458334814074750740, -1.392330997281837623 ) ) ;
#133373=CARTESIAN_POINT ( 'NONE',  ( 4.360000113718985659, -0.002809843368253156070, -2.016597020062675050 ) ) ;
#133377=CARTESIAN_POINT ( 'NONE',  ( 2.015964598666186269, -0.8597642540715648707, -1.610575774528985704 ) ) ;
#133380=CARTESIAN_POINT ( 'NONE',  ( -0.1296875068447882473, 5.724785194352729256, -2.420566058096422779 ) ) ;
#133386=CARTESIAN_POINT ( 'NONE',  ( 6.428379779529339366, -0.9538188281377130151, -1.780268319267635846 ) ) ;
#133387=CARTESIAN_POINT ( 'NONE',  ( 6.428415558115947448, -1.044286553621230240, -1.960546399981792476 ) ) ;
#133390=CARTESIAN_POINT ( 'NONE',  ( 5.436423068491611055, 2.030003055342466389, 0.3545201283375771228 ) ) ;
#133391=CARTESIAN_POINT ( 'NONE',  ( 4.834611377684539413, 0.6298767044488964295, -1.915599524792414465 ) ) ;
#133396=CARTESIAN_POINT ( 'NONE',  ( -0.2108831679770961642, 2.882544375557041239, -2.385815782126239792 ) ) ;
#133397=ADVANCED_FACE ( 'NONE', ( #83640 ), #15433, .T. ) ;
#133402=CARTESIAN_POINT ( 'NONE',  ( 5.307970166423544356, -1.730600239375930549, 1.034008556546859969 ) ) ;
#133403=CARTESIAN_POINT ( 'NONE',  ( 4.699059028873219468, -0.4882365319774860102, 1.775153104902137624 ) ) ;
#133405=CARTESIAN_POINT ( 'NONE',  ( 2.877863741784414842, 2.191074257732894548, -0.7245186886237849899 ) ) ;
#133407=CARTESIAN_POINT ( 'NONE',  ( 5.378265110509337532, -1.205767192478784500, 1.793856531414832256 ) ) ;
#133409=CARTESIAN_POINT ( 'NONE',  ( 0.1869208759678643028, 1.439853572182720587, 1.303434232916983015 ) ) ;
#133411=CARTESIAN_POINT ( 'NONE',  ( 3.937115517079175842, 1.273119805769900026, 1.913412639830965434 ) ) ;
#133414=CARTESIAN_POINT ( 'NONE',  ( 3.906994808788874174, 1.604092888448312326, 0.9621832354540849064 ) ) ;
#133416=CARTESIAN_POINT ( 'NONE',  ( 1.652457426684301955, 1.892030339952909035, 0.2773405859870237133 ) ) ;
#133419=CARTESIAN_POINT ( 'NONE',  ( 2.772332522587173997, 1.181257105606844160, 1.863944272329665086 ) ) ;
#133425=CARTESIAN_POINT ( 'NONE',  ( 0.3859243437699639845, -0.9334011365476569955, 1.736406649063494623 ) ) ;
#133426=CARTESIAN_POINT ( 'NONE',  ( 6.568959576340373197, -2.106780069790818555, -0.9421804820441375128 ) ) ;
#133427=CARTESIAN_POINT ( 'NONE',  ( 1.803102349535959714, -1.659081995624330563, 1.046767247423967095 ) ) ;
#133428=CARTESIAN_POINT ( 'NONE',  ( 4.733292769410803125, 0.005207392524877744490, -2.062741129207305235 ) ) ;
#133431=ORIENTED_EDGE ( 'NONE', *, *, #6489, .T. ) ;
#133434=DIRECTION ( 'NONE',  ( 1.039099362110107450E-15, 1.000000000000000000, -4.583713267641621330E-32 ) ) ;
#133436=CARTESIAN_POINT ( 'NONE',  ( 6.707499178395360140, -1.739742505839674047, -1.298780901186733505 ) ) ;
#133441=CARTESIAN_POINT ( 'NONE',  ( 1.000990332655056436, 1.525750722454706443, 1.081861512215509524 ) ) ;
#133447=CARTESIAN_POINT ( 'NONE',  ( 1.506358462150747091, -1.903157483220425883, -0.1863595701613318112 ) ) ;
#133448=CARTESIAN_POINT ( 'NONE',  ( 2.641160111863867233, -1.309778345111691999, -1.190485388269453049 ) ) ;
#133450=CARTESIAN_POINT ( 'NONE',  ( 0.5395309102857149819, -1.815710607404594557, 0.6001554849531522962 ) ) ;
#133452=CARTESIAN_POINT ( 'NONE',  ( 4.183139505431884508, 1.540756628010631735, 1.138051695910688998 ) ) ;
#133454=CARTESIAN_POINT ( 'NONE',  ( 5.072688767047404568, 1.359683132420253182, -1.425145238552152582 ) ) ;
#133455=CARTESIAN_POINT ( 'NONE',  ( 0.8793290508635929204, -1.919567575575848339, -0.9014759086384205311 ) ) ;
#133458=CARTESIAN_POINT ( 'NONE',  ( 4.153091690245942047, -1.555063956268587066, -1.039456662654779207 ) ) ;
#133459=CARTESIAN_POINT ( 'NONE',  ( 0.1174333910212103232, -1.791171220025630895, 0.3524246893974944395 ) ) ;
#133461=CARTESIAN_POINT ( 'NONE',  ( 3.950008152305323428, 0.7444041667201054535, -2.077678867657362538 ) ) ;
#133464=CARTESIAN_POINT ( 'NONE',  ( 0.8013246507756426329, -1.769997244335961284, 1.058882903378530749 ) ) ;
#133471=CARTESIAN_POINT ( 'NONE',  ( 0.1753634416057497925, 6.947017063990798214, -2.739087685391654148 ) ) ;
#133472=ORIENTED_EDGE ( 'NONE', *, *, #79797, .F. ) ;
#133473=CARTESIAN_POINT ( 'NONE',  ( 4.035645461687249913, 1.950487776689105557, -0.6946759356915442885 ) ) ;
#133475=CARTESIAN_POINT ( 'NONE',  ( 1.212450271513715094, -0.9707322288472040039, -1.931405299116680796 ) ) ;
#133477=CARTESIAN_POINT ( 'NONE',  ( 1.541671952839033688, -1.900923180158103021, 0.6826752959473363358 ) ) ;
#133482=CARTESIAN_POINT ( 'NONE',  ( 6.292342264464226176, -1.899326897351862664, 0.6766127494588560776 ) ) ;
#133483=CARTESIAN_POINT ( 'NONE',  ( -0.08279552664090458758, -1.841734517378278424, 0.8216794407479923734 ) ) ;
#133484=CARTESIAN_POINT ( 'NONE',  ( 6.639320575229256782, 0.5729255850590134758, 2.155858052613166986 ) ) ;
#133485=CARTESIAN_POINT ( 'NONE',  ( 4.564136437409766600, -1.431273618155091576, 1.659743667367798103 ) ) ;
#133487=CARTESIAN_POINT ( 'NONE',  ( 3.884940529579200774, -1.786240503712609895, -0.6835825222790415934 ) ) ;
#133491=CARTESIAN_POINT ( 'NONE',  ( 2.144157856786413241, 0.8647422840215597262, 1.821734841475818101 ) ) ;
#133493=CARTESIAN_POINT ( 'NONE',  ( 0.3458147113889240565, 0.7113776200376471515, -2.179290858394256070 ) ) ;
#133495=CARTESIAN_POINT ( 'NONE',  ( 4.084733067335220902, -0.1695706708978762522, -1.716391344981627709 ) ) ;
#133499=CARTESIAN_POINT ( 'NONE',  ( 1.433958818539453395, 1.165882187713672247, 1.577721859592796205 ) ) ;
#133502=CARTESIAN_POINT ( 'NONE',  ( 0.07536363704233049743, 2.002983476668462881, -2.558365315478607904 ) ) ;
#133506=CARTESIAN_POINT ( 'NONE',  ( 4.248556108744420357, 1.777317977963272178, 0.3491261437693141123 ) ) ;
#133510=CARTESIAN_POINT ( 'NONE',  ( 5.004484103855499910, -1.798449698946352537, -0.2161431223286890690 ) ) ;
#133514=CARTESIAN_POINT ( 'NONE',  ( 6.549252741683062595, 1.618575325784047392, -0.9183544947665848168 ) ) ;
#133516=CARTESIAN_POINT ( 'NONE',  ( 4.165583994951371771, 1.254247372560507223, 1.447964403467276506 ) ) ;
#133523=CARTESIAN_POINT ( 'NONE',  ( 1.094844843509492183, -0.5259716649698794599, -2.096624219460433647 ) ) ;
#133526=CARTESIAN_POINT ( 'NONE',  ( 0.7096328715897933792, -1.817275359149352676, 0.1739118742359047065 ) ) ;
#133528=CARTESIAN_POINT ( 'NONE',  ( 3.416849837094409370, 1.649954109374281996, 0.7815844185870901573 ) ) ;
#133531=CARTESIAN_POINT ( 'NONE',  ( 1.722773492080275748, 1.414811824084385661, -1.286832238068566392 ) ) ;
#133533=CARTESIAN_POINT ( 'NONE',  ( 2.682036910502568539, -1.131707915740775672, -1.611748346588251168 ) ) ;
#133534=CARTESIAN_POINT ( 'NONE',  ( 4.968278857500742163, -1.829972417919925265, -0.6506317318197059052 ) ) ;
#133537=CARTESIAN_POINT ( 'NONE',  ( 4.078469121099765005, 1.002472831208834680, 1.868716877859360137 ) ) ;
#133539=CARTESIAN_POINT ( 'NONE',  ( 3.035702773332124238, -1.842316306609870891, 0.5122265333450183311 ) ) ;
#133541=CARTESIAN_POINT ( 'NONE',  ( 0.2331563151865730654, 0.7315591717663977311, -2.029986209603263259 ) ) ;
#133542=ORIENTED_EDGE ( 'NONE', *, *, #38690, .T. ) ;
#133546=CARTESIAN_POINT ( 'NONE',  ( 4.986841741376339066, -0.2268417095559888130, -1.811474396668552700 ) ) ;
#133551=CARTESIAN_POINT ( 'NONE',  ( 5.840666405660361882, 0.3664468388623157158, 1.834233659845653897 ) ) ;
#133561=CARTESIAN_POINT ( 'NONE',  ( 6.737192315218426764, -0.09781360997717462868, -2.168977284074862677 ) ) ;
#133562=CARTESIAN_POINT ( 'NONE',  ( 0.7380959315415897004, 2.114583753240849795, -0.1084930780173159887 ) ) ;
#133566=CARTESIAN_POINT ( 'NONE',  ( 6.543811353064236336, 1.423268159695538326, 1.503672778047180358 ) ) ;
#133567=CARTESIAN_POINT ( 'NONE',  ( 1.153568636672014369, 0.7464410156945017194, 1.683350060182234209 ) ) ;
#133572=CARTESIAN_POINT ( 'NONE',  ( 1.992491592054939531, -0.6139151001693385901, -2.208460184710277385 ) ) ;
#133575=EDGE_CURVE ( 'NONE', #78277, #63091, #45662, .T. ) ;
#133580=CARTESIAN_POINT ( 'NONE',  ( 0.7561087546162044148, 0.8121304633340595824, -1.842289638184602341 ) ) ;
#133581=CARTESIAN_POINT ( 'NONE',  ( 1.569116724355507975, 1.727593668635756918, 0.9295332132536607839 ) ) ;
#133586=CARTESIAN_POINT ( 'NONE',  ( 3.943374907373353278, 0.7044166278388838132, -1.968527102906494575 ) ) ;
#133587=CARTESIAN_POINT ( 'NONE',  ( 1.920411955722916453, 1.650032497218676397, 0.6405850872945593188 ) ) ;
#133590=CARTESIAN_POINT ( 'NONE',  ( 5.209026396049201146, -0.3404489335739938061, 2.266724491853837620 ) ) ;
#133591=CARTESIAN_POINT ( 'NONE',  ( 3.732115773437282513, 0.2573812008909857618, 1.721053547986243215 ) ) ;
#133593=CARTESIAN_POINT ( 'NONE',  ( 2.829097238278361459, -1.198370081129100262, 1.253277946039689450 ) ) ;
#133594=CARTESIAN_POINT ( 'NONE',  ( 3.244746832269917558, -2.138594630188391132, -0.3739374351436116073 ) ) ;
#133596=CARTESIAN_POINT ( 'NONE',  ( 6.016814611094169152, 0.2024578496369993375, 2.006372135924570088 ) ) ;
#133597=CARTESIAN_POINT ( 'NONE',  ( 0.01034996896555614825, -0.2601230917365888740, -1.999999999999999556 ) ) ;
#133600=CARTESIAN_POINT ( 'NONE',  ( 2.080962409574789174, -0.09239518442967499523, -1.924287757472051164 ) ) ;
#133602=CARTESIAN_POINT ( 'NONE',  ( 5.185853984360066171, 2.140751028750527141, -0.5928278168529849124 ) ) ;
#133604=CARTESIAN_POINT ( 'NONE',  ( -0.2106854629475244378, 6.948332279000682732, -2.592197477433130448 ) ) ;
#133613=CARTESIAN_POINT ( 'NONE',  ( 6.696538538688765918, -0.5935452916538739299, -2.183133895321730744 ) ) ;
#133617=CARTESIAN_POINT ( 'NONE',  ( -0.1399997263889594112, -0.002789056014654289761, -2.000146600338557956 ) ) ;
#133618=CARTESIAN_POINT ( 'NONE',  ( 3.982923569253065121, 1.957725435881779941, 0.6497275974019289801 ) ) ;
#133622=CARTESIAN_POINT ( 'NONE',  ( 5.395714598229544023, -0.6742385858747660388, 1.744967798948720228 ) ) ;
#133623=CARTESIAN_POINT ( 'NONE',  ( 5.203642376314169482, 1.605325691485876671, 0.6564576239363513199 ) ) ;
#133624=CARTESIAN_POINT ( 'NONE',  ( 4.634162599488286460, 0.3036646131651790093, 1.713576892981442557 ) ) ;
#133626=CARTESIAN_POINT ( 'NONE',  ( 1.347684858569838440, 0.6597076516901092536, -2.195415608770342253 ) ) ;
#133628=CARTESIAN_POINT ( 'NONE',  ( 5.794497793856321799, 1.708647746284063684, -1.204582154990775811 ) ) ;
#133629=CARTESIAN_POINT ( 'NONE',  ( 0.1461044202776436429, -1.480667811789614596, 1.094048858351577724 ) ) ;
#133632=CARTESIAN_POINT ( 'NONE',  ( 1.652970434142877920, 1.038994816082598804, 1.728001345923817267 ) ) ;
#133633=CARTESIAN_POINT ( 'NONE',  ( 0.6213436022244858137, -2.079703760468250451, 0.6910661131078954522 ) ) ;
#133638=CARTESIAN_POINT ( 'NONE',  ( 3.598385148150527346, -1.043669326629501848, 1.845773325594574077 ) ) ;
#133640=CARTESIAN_POINT ( 'NONE',  ( 5.426323838365306074, 1.084245000580752238, -1.468710674947353967 ) ) ;
#133648=CARTESIAN_POINT ( 'NONE',  ( 2.900653795123844692, -1.990604234199357281, -0.3410580241900613707 ) ) ;
#133649=CARTESIAN_POINT ( 'NONE',  ( 6.528370574810466564, 1.275976099532463381, -1.800301716031265764 ) ) ;
#133651=CARTESIAN_POINT ( 'NONE',  ( 3.713571355222999415, 0.4562380391235145161, -1.803994140785330602 ) ) ;
#133659=CARTESIAN_POINT ( 'NONE',  ( 1.739138385086140159, -1.644397438216003593, -0.5498640316261136363 ) ) ;
#133660=CARTESIAN_POINT ( 'NONE',  ( 0.9721243863554385189, -0.03892262269361351779, -1.740072766964487316 ) ) ;
#133661=CARTESIAN_POINT ( 'NONE',  ( 0.07775346131144458828, -0.005211914751935413023, -2.288974916015192651 ) ) ;
#133664=CARTESIAN_POINT ( 'NONE',  ( 0.9485937975238111219, 0.5957422345228384764, 1.972812641012058776 ) ) ;
#133666=CARTESIAN_POINT ( 'NONE',  ( 6.573571087534610058, 1.710132712828818402, -1.535791079811721360 ) ) ;
#133669=CARTESIAN_POINT ( 'NONE',  ( 0.3562423511419475775, 0.7522458758148011793, 1.822497947957350428 ) ) ;
#133670=CARTESIAN_POINT ( 'NONE',  ( 4.341997288149157086, -1.180789491531178292, -1.504210074635865757 ) ) ;
#133672=CARTESIAN_POINT ( 'NONE',  ( 6.182275136424624229, -1.184133725572718676, 1.862117674348878760 ) ) ;
#133676=CARTESIAN_POINT ( 'NONE',  ( -0.005205762187880831615, -1.959593580757122089, -0.4885912094437401820 ) ) ;
#133678=CARTESIAN_POINT ( 'NONE',  ( 3.206425952641503319, -2.304998342715250281, 0.1115464655990650450 ) ) ;
#133679=CARTESIAN_POINT ( 'NONE',  ( 5.178158156489047315, -1.047961880893449882, -1.658324637040713867 ) ) ;
#133680=CARTESIAN_POINT ( 'NONE',  ( 0.8308171121041010299, -1.845250773774274267, -0.6662997747023179373 ) ) ;
#133684=CARTESIAN_POINT ( 'NONE',  ( -0.2408018239684434625, -0.007136184528846663787, -2.100252307185761058 ) ) ;
#133688=CARTESIAN_POINT ( 'NONE',  ( 4.610331778354775700, 2.170709972759849116, -0.04705437256473897489 ) ) ;
#133691=CARTESIAN_POINT ( 'NONE',  ( 1.512141599020993432, -0.7094941370262074498, 1.998545949238240027 ) ) ;
#133696=CARTESIAN_POINT ( 'NONE',  ( 1.932957488262206480, 0.1987776095667900533, 2.051143708757536821 ) ) ;
#133698=CARTESIAN_POINT ( 'NONE',  ( 6.609000000000038177, 0.002801690667396730672, 2.000160786441218530 ) ) ;
#133703=CARTESIAN_POINT ( 'NONE',  ( 4.143145976665215002, 0.09703654569752531711, 1.909951782607082427 ) ) ;
#133705=CARTESIAN_POINT ( 'NONE',  ( 1.300488321244117618, -2.262578820359177012, 9.798025588786393801E-05 ) ) ;
#133707=CARTESIAN_POINT ( 'NONE',  ( 1.705023097204850346, 1.575028893885391579, -0.8949447657340557916 ) ) ;
#133708=CARTESIAN_POINT ( 'NONE',  ( 0.4795166263942132745, -0.6867406401212177158, 1.788596380544268616 ) ) ;
#133709=CARTESIAN_POINT ( 'NONE',  ( 2.049362625460974030, 1.802418521853879962, -1.018503948505583789 ) ) ;
#133712=CARTESIAN_POINT ( 'NONE',  ( 0.1804621682222322943, -1.911711055282316662, -0.4813082943134691094 ) ) ;
#133713=CARTESIAN_POINT ( 'NONE',  ( 5.461526653864938297, 0.3736970969714300539, -1.889748759083320406 ) ) ;
#133714=CARTESIAN_POINT ( 'NONE',  ( 6.428370569364434850, 1.274405893209800356, -1.801548588985131039 ) ) ;
#133718=CARTESIAN_POINT ( 'NONE',  ( 4.791499389596598490, -1.887151845835168817, 0.8330235203531827226 ) ) ;
#133722=CARTESIAN_POINT ( 'NONE',  ( 5.280345248378272238, -1.172444710293341963, 1.749198092158671614 ) ) ;
#133724=CARTESIAN_POINT ( 'NONE',  ( 1.065148145857688577, 1.644283457976392748, -1.417989991454001730 ) ) ;
#133726=CARTESIAN_POINT ( 'NONE',  ( 5.149776166300943814, 0.6834882490109328579, -2.050742609271530181 ) ) ;
#133727=CARTESIAN_POINT ( 'NONE',  ( 4.881513094923572105, 0.1956549798781386795, -2.010156034525738988 ) ) ;
#133734=CARTESIAN_POINT ( 'NONE',  ( 3.063685658700274761, 1.282989771343697294, 1.555699169480361022 ) ) ;
#133738=CARTESIAN_POINT ( 'NONE',  ( 5.260679775997886054, -1.568431141927080219, 1.487858469166832176 ) ) ;
#133743=CARTESIAN_POINT ( 'NONE',  ( 5.097279880301520905, -0.2930512725940071506, 1.994873791649566463 ) ) ;
#133745=CARTESIAN_POINT ( 'NONE',  ( 1.031410063161166013, -1.091267733730487466, -1.335775140220570201 ) ) ;
#133750=CARTESIAN_POINT ( 'NONE',  ( 5.958239543830243790, 0.7576973323653664050, 1.710380810381225913 ) ) ;
#133751=CARTESIAN_POINT ( 'NONE',  ( 5.853776559028295523, -1.461190594579380608, -1.385140169207878413 ) ) ;
#133755=CARTESIAN_POINT ( 'NONE',  ( 2.614065066921432479, -0.6628553294307990562, 2.014303955012682223 ) ) ;
#133756=CARTESIAN_POINT ( 'NONE',  ( 1.230092461119953517, 2.014234866427236259, 0.09611455020034495589 ) ) ;
#133757=CARTESIAN_POINT ( 'NONE',  ( 0.9667389835759466754, -1.427192611269219924, 1.115597691851821116 ) ) ;
#133759=CARTESIAN_POINT ( 'NONE',  ( 6.526263005029545816, 1.249015235541932167, -1.764162671312206498 ) ) ;
#133763=CARTESIAN_POINT ( 'NONE',  ( -0.06540554862877968889, -1.536972603800386361, 1.143280314369120587 ) ) ;
#133771=CARTESIAN_POINT ( 'NONE',  ( 4.258765444007106105, -1.603684720688375975, 1.449730421305382544 ) ) ;
#133774=CARTESIAN_POINT ( 'NONE',  ( 1.951583061186522583, -1.892041120407188304, 0.9578705467366486204 ) ) ;
#133775=CARTESIAN_POINT ( 'NONE',  ( 6.528339890195162809, 1.048227956652090009, -1.494441373796271399 ) ) ;
#133777=CARTESIAN_POINT ( 'NONE',  ( 2.741432468550320412, -1.458365196291089072, -1.326584384502631719 ) ) ;
#133778=CARTESIAN_POINT ( 'NONE',  ( 5.027564050633359649, -0.2746679736120913318, 1.892429487827557599 ) ) ;
#133781=CARTESIAN_POINT ( 'NONE',  ( 5.934039001034627780, 1.171926208273272207, 1.582800714458313385 ) ) ;
#133782=CARTESIAN_POINT ( 'NONE',  ( 1.517416608934060385, -1.078585517578967368, -1.614684294522166663 ) ) ;
#133790=CARTESIAN_POINT ( 'NONE',  ( 6.287759715630294011, 1.828497742151834027, -0.5598019499635784602 ) ) ;
#133792=CARTESIAN_POINT ( 'NONE',  ( 3.299657469156279888, 1.739734091921738557, 1.357710657151039779 ) ) ;
#133793=CARTESIAN_POINT ( 'NONE',  ( 1.782535857997105566, -1.180187651135233384, 1.864495428577646274 ) ) ;
#133794=CARTESIAN_POINT ( 'NONE',  ( 0.2582720099171370021, 1.907150531373353664, 0.1405958444523764117 ) ) ;
#133797=CARTESIAN_POINT ( 'NONE',  ( 3.156751980976373329, -0.5984545454679365273, -1.982000093670479135 ) ) ;
#133801=CARTESIAN_POINT ( 'NONE',  ( 1.710078970767275885, -2.145365142986368934, 0.2646356489638818088 ) ) ;
#133802=CARTESIAN_POINT ( 'NONE',  ( 3.737968522918270864, 2.181131050170285857, 0.2133239450496857148 ) ) ;
#133807=CARTESIAN_POINT ( 'NONE',  ( 5.572856105055380205, -0.7716597722284452843, 1.553080519226685885 ) ) ;
#133809=CARTESIAN_POINT ( 'NONE',  ( 3.977443466873982203, -0.1572589350618114057, 2.064370724987254047 ) ) ;
#133810=CARTESIAN_POINT ( 'NONE',  ( 4.552435263133931542, -1.381712717965150938, 1.604331009294196031 ) ) ;
#133813=CARTESIAN_POINT ( 'NONE',  ( 2.746873616242023086, -0.3318220265390697254, -1.941108330032844664 ) ) ;
#133814=CARTESIAN_POINT ( 'NONE',  ( 0.7031954830387620037, 1.685401770928725007, -0.9037484838233383888 ) ) ;
#133815=CARTESIAN_POINT ( 'NONE',  ( 4.611445210273608986, -2.248620548832699573, 0.4443846451570551692 ) ) ;
#133816=CARTESIAN_POINT ( 'NONE',  ( 3.088313589057069208, -1.798746773638896457, -0.3115406389907551810 ) ) ;
#133823=CARTESIAN_POINT ( 'NONE',  ( 3.515888537569244132, -0.5802020150980004010, 1.927815774739343180 ) ) ;
#133824=CARTESIAN_POINT ( 'NONE',  ( 4.627759936859944467, 1.903863570041373077, -0.4726564843360381851 ) ) ;
#133828=CARTESIAN_POINT ( 'NONE',  ( 0.07556134207194721564, 2.859159929750184848, -2.732257853551669946 ) ) ;
#133830=CARTESIAN_POINT ( 'NONE',  ( 0.6442209307526406414, 0.6107738465899931191, 1.999526160293135568 ) ) ;
#133831=CARTESIAN_POINT ( 'NONE',  ( 5.207753166488873653, -1.761066459785052274, 0.1758167199723305041 ) ) ;
#133833=CARTESIAN_POINT ( 'NONE',  ( 2.273600812266802773, 1.349468827467028120, 1.726581335083368085 ) ) ;
#133834=CARTESIAN_POINT ( 'NONE',  ( 6.333937804992649134, 1.722499169431927601, 0.2476611369811829999 ) ) ;
#133837=CARTESIAN_POINT ( 'NONE',  ( 0.9610595616070281011, 0.3405255003954327786, -1.690740162648683320 ) ) ;
#133838=CARTESIAN_POINT ( 'NONE',  ( 0.7557052203445973060, -2.281327611594321958, -0.2792575881873406440 ) ) ;
#133839=CARTESIAN_POINT ( 'NONE',  ( 0.9080814035550346386, -0.9900877184637231210, -1.955254813705724404 ) ) ;
#133840=CARTESIAN_POINT ( 'NONE',  ( 6.731818218530718489, -1.587343137472529309, -0.6980196547925822115 ) ) ;
#133841=CARTESIAN_POINT ( 'NONE',  ( 2.561379550486083012, -1.920685204893451292, -1.086737900330703166 ) ) ;
#133842=CARTESIAN_POINT ( 'NONE',  ( 6.760228240101231023, -2.170840268647770799, 0.04637219581851703687 ) ) ;
#133844=CARTESIAN_POINT ( 'NONE',  ( 2.237658791021436056, 0.5595254372263277487, -2.042044324946710621 ) ) ;
#133845=CARTESIAN_POINT ( 'NONE',  ( 6.827182134110192813, 7.051736335826703339, 2.787205296604370108 ) ) ;
#133846=CARTESIAN_POINT ( 'NONE',  ( 5.122061974917812677, -1.030465543002171858, -1.627433240741954723 ) ) ;
#133848=CARTESIAN_POINT ( 'NONE',  ( 2.015536172832455897, -2.222481616396556170, 0.5612588729206613447 ) ) ;
#133853=CARTESIAN_POINT ( 'NONE',  ( 4.371885135981863790, 0.4866971690204218159, -2.167184880714991824 ) ) ;
#133863=CARTESIAN_POINT ( 'NONE',  ( 2.514296259408643319, -1.880434619097739013, 0.7283795345095490648 ) ) ;
#133865=CARTESIAN_POINT ( 'NONE',  ( 0.9013244701963195604, -1.770926582075180944, 1.057100273733258433 ) ) ;
#133870=CARTESIAN_POINT ( 'NONE',  ( 4.382901342696458258, 1.958101449220098988, -0.9841704303943515919 ) ) ;
#133871=CARTESIAN_POINT ( 'NONE',  ( 1.424454163599726320, -1.462446849824734274, -1.388484543128357229 ) ) ;
#133872=CARTESIAN_POINT ( 'NONE',  ( 1.505144418776669601, -1.827259764946763454, 0.2261131901925839127 ) ) ;
#133873=CARTESIAN_POINT ( 'NONE',  ( 4.792671637142519536, 1.906707348304257366, -1.272296631038958070 ) ) ;
#133874=CARTESIAN_POINT ( 'NONE',  ( 3.081803158279991628, -1.813988701161291628, -0.3140598505507880556 ) ) ;
#133876=CARTESIAN_POINT ( 'NONE',  ( 3.873894609034499670, 1.013791609252197690, 1.518000939925366000 ) ) ;
#133877=CARTESIAN_POINT ( 'NONE',  ( 5.485000066852382616, -2.016597020608828839, 0.002808655738886777897 ) ) ;
#133879=CARTESIAN_POINT ( 'NONE',  ( 4.452213415057678425, 2.262087339288323840, -0.05152095106783493444 ) ) ;
#133881=CARTESIAN_POINT ( 'NONE',  ( 6.827182134110199030, -0.004087946457608306570, 2.088967824442849341 ) ) ;
#133882=CARTESIAN_POINT ( 'NONE',  ( 3.982925052038261526, 1.964963782255540359, 0.6523228965355857278 ) ) ;
#133887=CARTESIAN_POINT ( 'NONE',  ( 1.893070592381540740, 1.676246824859698892, -0.9494106994061870530 ) ) ;
#133890=CARTESIAN_POINT ( 'NONE',  ( 6.350452388456855779, -1.959648489363738699, -0.1964464578135850514 ) ) ;
#133894=CARTESIAN_POINT ( 'NONE',  ( 0.7914572142167939361, -0.05789999323873443182, -2.119991495365561640 ) ) ;
#133895=CARTESIAN_POINT ( 'NONE',  ( 2.022025532713614737, -0.4812968563913700981, 2.168513943247989850 ) ) ;
#133896=CARTESIAN_POINT ( 'NONE',  ( 3.135867587238525100, -1.413284743790550468, -1.561492743641406999 ) ) ;
#133899=CARTESIAN_POINT ( 'NONE',  ( 6.912964126797830566, -1.438640208141970245, 1.180240733875538517 ) ) ;
#133906=CARTESIAN_POINT ( 'NONE',  ( 1.564851893998190135, 0.6701894319398638000, 2.011955567234039677 ) ) ;
#133909=CARTESIAN_POINT ( 'NONE',  ( 4.316819842036943911, -1.455217238560998272, 1.315978175897666080 ) ) ;
#133910=CARTESIAN_POINT ( 'NONE',  ( 3.045950098598048328, 0.7793912989166664751, -2.016482303682599841 ) ) ;
#133911=CARTESIAN_POINT ( 'NONE',  ( 1.487592393518050837, -1.832424703912252317, -0.1798031890194173865 ) ) ;
#133914=CARTESIAN_POINT ( 'NONE',  ( 4.698987106650459822, -0.4602053158732459237, 1.678299975232977026 ) ) ;
#133915=CARTESIAN_POINT ( 'NONE',  ( 6.639320575229280763, 7.629137130509070275, 2.496737603865983424 ) ) ;
#133919=CARTESIAN_POINT ( 'NONE',  ( 1.833122199354455972, 0.2117775504973731793, 2.151289291301178075 ) ) ;
#133920=CARTESIAN_POINT ( 'NONE',  ( 3.761092154037175117, -2.013677596940225190, -0.1017350580494805479 ) ) ;
#133922=CARTESIAN_POINT ( 'NONE',  ( 1.059701713109785670, 0.4209238396889224965, -2.120155868012041811 ) ) ;
#133923=CARTESIAN_POINT ( 'NONE',  ( 3.414874914781691473, 1.781649806626634858, 0.8443359948157087569 ) ) ;
#133925=CARTESIAN_POINT ( 'NONE',  ( 3.017060306806388148, -1.870969668351904147, 0.5203628790987256947 ) ) ;
#133935=CARTESIAN_POINT ( 'NONE',  ( 0.4818276840582723652, 2.058231501447154610, -0.7964225590989246761 ) ) ;
#133937=CARTESIAN_POINT ( 'NONE',  ( 4.979329090789969214, -0.1002203015587413149, 1.959344625532564610 ) ) ;
#133938=CARTESIAN_POINT ( 'NONE',  ( 1.793592486599729252, 1.492254607734722072, -1.356300734917381678 ) ) ;
#133940=CARTESIAN_POINT ( 'NONE',  ( 3.661412522060889074, 1.992289893316813609, -0.7171584230975246443 ) ) ;
#133944=CARTESIAN_POINT ( 'NONE',  ( 3.468544592087896561, 0.04396668885017079864, -1.840778273432375212 ) ) ;
#133948=CARTESIAN_POINT ( 'NONE',  ( 4.869442314738527067, -1.792836814666173062, -1.132239877606910472 ) ) ;
#133951=CARTESIAN_POINT ( 'NONE',  ( 5.132131416026131987, 1.062877790662479116, -1.765404227961290484 ) ) ;
#133953=CARTESIAN_POINT ( 'NONE',  ( 1.117373073715557164, 0.3680575366376471758, -1.824110739772739631 ) ) ;
#133954=CARTESIAN_POINT ( 'NONE',  ( 2.348939331405873077, 0.4892633877765646400, -1.774999737812533063 ) ) ;
#133958=CARTESIAN_POINT ( 'NONE',  ( 1.717678464306471309, -0.2677704892378242607, 2.190511422692428045 ) ) ;
#133959=CARTESIAN_POINT ( 'NONE',  ( 4.552213317786341307, 2.262020173471789963, -0.04951151886351152359 ) ) ;
#133961=CARTESIAN_POINT ( 'NONE',  ( 4.183730900115702589, 1.755568954123175596, -0.4464138967742969366 ) ) ;
#133962=CARTESIAN_POINT ( 'NONE',  ( 4.891753643660703865, -1.905893201010636195, 0.1940691045876908327 ) ) ;
#133965=CARTESIAN_POINT ( 'NONE',  ( 4.170748999387418721, -1.839122178589139178, -0.7105754535856413368 ) ) ;
#133966=CARTESIAN_POINT ( 'NONE',  ( 4.891396039733495016, 1.386484060982313249, 1.255958711209571810 ) ) ;
#133967=CARTESIAN_POINT ( 'NONE',  ( 4.685918305224146430, -1.144368955370359098, -1.467557204495354872 ) ) ;
#133969=CARTESIAN_POINT ( 'NONE',  ( 0.6379081216283178923, 2.014007883293071899, -0.1037844182863178755 ) ) ;
#133972=CARTESIAN_POINT ( 'NONE',  ( 2.156984414944181694, -1.627247350590403707, 1.336999143475733121 ) ) ;
#133976=CARTESIAN_POINT ( 'NONE',  ( 3.023802379225454473, -0.4096935937694180518, 2.080477853870852378 ) ) ;
#133977=DIRECTION ( 'NONE',  ( 1.040834085586084257E-15, 1.000000000000000000, -4.622230424712076367E-32 ) ) ;
#133978=CARTESIAN_POINT ( 'NONE',  ( 2.004171506046021012, -0.8596719693435939114, 1.827822491074476918 ) ) ;
#133980=CARTESIAN_POINT ( 'NONE',  ( 6.720655732516647163, 0.5950723047917580999, 1.879543361893110109 ) ) ;
#133983=CARTESIAN_POINT ( 'NONE',  ( 2.407699484934812784, -0.4761397456576694776, 2.108333575599189214 ) ) ;
#133984=CARTESIAN_POINT ( 'NONE',  ( 6.610000000000014531, 2.942932264094192174, 2.732153830519419291 ) ) ;
#133992=CARTESIAN_POINT ( 'NONE',  ( 1.294752383181968503, 1.788903229852260246, -1.265732775075766092 ) ) ;
#133994=CARTESIAN_POINT ( 'NONE',  ( 1.639924147338491123, -1.639646335682118927, -1.559238602228057990 ) ) ;
#133997=CARTESIAN_POINT ( 'NONE',  ( 4.417204035549080920, -1.841734835922325120, 0.8216704330437707426 ) ) ;
#134002=CARTESIAN_POINT ( 'NONE',  ( 4.230855031843249847, 0.08773280417345018234, 1.722775095924995004 ) ) ;
#134005=CARTESIAN_POINT ( 'NONE',  ( 3.004884002558502853, 1.492965937746863148, 0.9499605963744962578 ) ) ;
#134006=CARTESIAN_POINT ( 'NONE',  ( 5.087059579022827904, -0.2656672225294122169, -2.190654145894948890 ) ) ;
#134009=CARTESIAN_POINT ( 'NONE',  ( 4.816029892389546596, 1.034148959857810190, -1.730877356967218894 ) ) ;
#134011=CARTESIAN_POINT ( 'NONE',  ( 2.711613914024712191, -1.850561042518297672, 0.2725550856255419818 ) ) ;
#134013=CARTESIAN_POINT ( 'NONE',  ( 1.810667312839256304, -0.5133170510521027907, -1.842115474350584980 ) ) ;
#134018=CARTESIAN_POINT ( 'NONE',  ( 0.7031954830387620037, 1.685401770928725007, -0.9037484838233383888 ) ) ;
#134020=CARTESIAN_POINT ( 'NONE',  ( 1.592165322863370980, 0.9698756732311950568, -1.705302290208744687 ) ) ;
#134023=CARTESIAN_POINT ( 'NONE',  ( 5.396778611113259849, -2.069399493756381769, -0.4625044129713885011 ) ) ;
#134026=CARTESIAN_POINT ( 'NONE',  ( 6.116478573505100158, 1.325718183447884169, -1.459148498715772790 ) ) ;
#134028=CARTESIAN_POINT ( 'NONE',  ( 1.968995789680173303, -1.553632997376572566, 1.280276984777522165 ) ) ;
#134031=CARTESIAN_POINT ( 'NONE',  ( 1.001738948178192645, -2.064706785862341132, 0.4679990497924620407 ) ) ;
#134033=CARTESIAN_POINT ( 'NONE',  ( 2.102089431743926706, 0.7944251937819692966, -1.912079865474418439 ) ) ;
#134037=CARTESIAN_POINT ( 'NONE',  ( 4.980460981504991835, -0.2552229379441274815, -2.074931007936396288 ) ) ;
#134039=CARTESIAN_POINT ( 'NONE',  ( 2.573050890253928635, 0.09191801231544714790, -1.823395950357763695 ) ) ;
#134040=CARTESIAN_POINT ( 'NONE',  ( 2.596125760314275777, -0.9296622322433767405, 1.554548433350180225 ) ) ;
#134044=CARTESIAN_POINT ( 'NONE',  ( 5.544034191846948900, 0.8990280053539388971, -2.015528879820461583 ) ) ;
#134047=CARTESIAN_POINT ( 'NONE',  ( 3.440010667329951310, -1.141173813254949820, -1.534285795567114974 ) ) ;
#134048=AXIS2_PLACEMENT_3D ( 'NONE', #102753, #120138, #116923 ) ;
#134056=CARTESIAN_POINT ( 'NONE',  ( 0.6613494997313728030, 0.9071737413179328247, 1.602200521169500957 ) ) ;
#134059=CARTESIAN_POINT ( 'NONE',  ( 3.497188413392815498, 1.472618687456558551, 1.153256759092120554 ) ) ;
#134064=CARTESIAN_POINT ( 'NONE',  ( 0.5320047819624426078, 1.129344350875445935, 1.613283618269464981 ) ) ;
#134065=CARTESIAN_POINT ( 'NONE',  ( 1.792592436991577109, 1.492242793082170449, -1.356315429364700176 ) ) ;
#134069=CARTESIAN_POINT ( 'NONE',  ( 2.326364362698669641, 2.126017103801054464, 0.5310240739047759062 ) ) ;
#134070=CARTESIAN_POINT ( 'NONE',  ( 6.445924739416000193, 0.6936395621829589686, -1.688995215704327535 ) ) ;
#134077=CARTESIAN_POINT ( 'NONE',  ( 4.071694929070113211, -1.056692140236010102, 1.507659738195665788 ) ) ;
#134078=CARTESIAN_POINT ( 'NONE',  ( 0.4518146667342719525, -1.425121331298753402, -1.422066715514385349 ) ) ;
#134079=CARTESIAN_POINT ( 'NONE',  ( 2.583761237542493205, 1.502156065388253081, -1.739619357585840520 ) ) ;
#134081=CARTESIAN_POINT ( 'NONE',  ( 1.340418531419234505, -1.814007083311576451, -0.4145509422008378242 ) ) ;
#134084=CARTESIAN_POINT ( 'NONE',  ( 4.500206361630255003, -0.8965733778899236395, 1.689174240301967389 ) ) ;
#134089=CARTESIAN_POINT ( 'NONE',  ( 3.491813360781896858, -2.088456202509383797, -0.1002299605681444133 ) ) ;
#134090=CARTESIAN_POINT ( 'NONE',  ( 2.026040307571222332, 1.079255042350239391, -1.527726335390042767 ) ) ;
#134093=CARTESIAN_POINT ( 'NONE',  ( 3.544249451937312667, -1.420498570261208959, 1.005328601869423633 ) ) ;
#134096=CARTESIAN_POINT ( 'NONE',  ( 4.019902842142981214, -0.8889698729942583366, -1.477996400630256613 ) ) ;
#134098=CARTESIAN_POINT ( 'NONE',  ( 6.393228082638676923, 1.922373441260841087, -1.083778638264052852 ) ) ;
#134101=CARTESIAN_POINT ( 'NONE',  ( 3.098652014986380543, 2.154143853245940043, 0.2703130112568508103 ) ) ;
#134102=CARTESIAN_POINT ( 'NONE',  ( 1.980809073483770000, -0.08854697198140694392, -1.823669195971427071 ) ) ;
#134104=CARTESIAN_POINT ( 'NONE',  ( 5.577400755804389654, 1.605162776699980753, 1.380938528300587276 ) ) ;
#134106=CARTESIAN_POINT ( 'NONE',  ( 5.741781754149911876, 2.289535525127144311, 0.1160191304092756254 ) ) ;
#134109=CARTESIAN_POINT ( 'NONE',  ( 1.348456458401224412, 1.042098076042829780, -1.846665823592225975 ) ) ;
#134114=CARTESIAN_POINT ( 'NONE',  ( 6.069212964912024333, 1.910890531626436184, 1.030632506159581352 ) ) ;
#134117=CARTESIAN_POINT ( 'NONE',  ( 1.049838644336478000, -2.005893928647552116, 0.9545428114200222858 ) ) ;
#134119=CARTESIAN_POINT ( 'NONE',  ( -0.06910031042392690559, -1.782763753708914267, -1.450585907311294775 ) ) ;
#134121=CARTESIAN_POINT ( 'NONE',  ( 4.575086232891404592, 1.883663672660494504, 0.8406736911329756312 ) ) ;
#134127=CARTESIAN_POINT ( 'NONE',  ( 0.6914939563917784637, -0.7507456521842426067, 1.951374281879012962 ) ) ;
#134128=CARTESIAN_POINT ( 'NONE',  ( 5.098279808040273586, -0.2930726886911338425, 1.994869512123042199 ) ) ;
#134129=CARTESIAN_POINT ( 'NONE',  ( 3.895923546780861724, -0.5813109859279729230, -1.747131793041277970 ) ) ;
#134132=CARTESIAN_POINT ( 'NONE',  ( 0.7622199101927947806, -1.253934870956091352, 1.184532473512718509 ) ) ;
#134133=CARTESIAN_POINT ( 'NONE',  ( -0.06521966986864842497, -1.616690375843790273, 1.205047459138554045 ) ) ;
#134134=CARTESIAN_POINT ( 'NONE',  ( 0.3703313985920617668, -0.2899475993979240274, -2.280306813078219363 ) ) ;
#134136=CARTESIAN_POINT ( 'NONE',  ( 1.493865258296807275, 1.713033017868152763, 1.477889207592040455 ) ) ;
#134137=CARTESIAN_POINT ( 'NONE',  ( 3.000711368280566393, -0.6119465431162304236, -2.015196771704963030 ) ) ;
#134141=CARTESIAN_POINT ( 'NONE',  ( 6.218749999999983125, -0.7852924748301916003, 1.895863743164212467 ) ) ;
#134145=CARTESIAN_POINT ( 'NONE',  ( 4.570683916498400556, 0.8515115505445168820, 2.051917206062872978 ) ) ;
#134146=CARTESIAN_POINT ( 'NONE',  ( 4.013774469618203611, -1.125877316280783358, -1.879984707117538845 ) ) ;
#134150=CARTESIAN_POINT ( 'NONE',  ( 6.610000000000002096, 6.034162285353575683, 2.874900418788868262 ) ) ;
#134153=CARTESIAN_POINT ( 'NONE',  ( 5.045234882716379765, 0.1584239314957915090, 2.114765283346302205 ) ) ;
#134157=CARTESIAN_POINT ( 'NONE',  ( 6.227428301493934448, -2.037140905555033576, 0.7235935974677574212 ) ) ;
#134159=CARTESIAN_POINT ( 'NONE',  ( 4.792441439910442469, 1.527937338083688923, -1.027124420945782157 ) ) ;
#134161=CARTESIAN_POINT ( 'NONE',  ( 0.7315135518511396429, 1.714293348657709881, 0.2994600772705089953 ) ) ;
#134165=CARTESIAN_POINT ( 'NONE',  ( 4.997027575558514734, 1.799266821141291661, -1.197868618907194316 ) ) ;
#134170=CARTESIAN_POINT ( 'NONE',  ( 4.206063578812153203, -2.156103337031569200, 0.1562769059922017589 ) ) ;
#134172=CARTESIAN_POINT ( 'NONE',  ( 6.116478573505100158, 1.325718183447884169, -1.459148498715772790 ) ) ;
#134173=CARTESIAN_POINT ( 'NONE',  ( 5.466046595369183692, 1.418568314722228996, 0.9965602304959333413 ) ) ;
#134174=CARTESIAN_POINT ( 'NONE',  ( 2.314256413632868714, 1.428969747754246233, -1.661726224907192684 ) ) ;
#134175=CARTESIAN_POINT ( 'NONE',  ( 2.099037836983450589, -0.6160640708386398989, -2.223778577795953115 ) ) ;
#134176=CARTESIAN_POINT ( 'NONE',  ( 4.587218493272061437, 1.842632243969796413, -0.9228815313185294578 ) ) ;
#134177=CARTESIAN_POINT ( 'NONE',  ( 0.3748122768056568743, 1.812325467826606085, -0.6980362920307162655 ) ) ;
#134181=CARTESIAN_POINT ( 'NONE',  ( 1.231092510272915552, 2.014232830173094513, 0.09613330637052441840 ) ) ;
#134183=CARTESIAN_POINT ( 'NONE',  ( 3.944505925199864649, 2.195883038551619038, 0.2190369969904403802 ) ) ;
#134185=CARTESIAN_POINT ( 'NONE',  ( 1.393147051786493673, -1.685373162331062602, 0.7893452609444310264 ) ) ;
#134186=CARTESIAN_POINT ( 'NONE',  ( -0.1288028175207089898, 5.718623287604398087, -2.868046808693432315 ) ) ;
#134190=CARTESIAN_POINT ( 'NONE',  ( 6.825078400183544503, 6.034152930826206962, 2.739236550662868197 ) ) ;
#134193=CARTESIAN_POINT ( 'NONE',  ( 3.871991401782824749, 1.143396993664235417, 1.714400680826788426 ) ) ;
#134196=CARTESIAN_POINT ( 'NONE',  ( 2.701824437540679469, 1.429832853698081108, 1.426684077065028422 ) ) ;
#134199=CARTESIAN_POINT ( 'NONE',  ( 1.815377929200719720, -0.2531822047686766441, 2.045215655110666830 ) ) ;
#134204=CARTESIAN_POINT ( 'NONE',  ( -0.2411972340275865823, -0.002466136893032512371, -1.900252416837118208 ) ) ;
#134205=CARTESIAN_POINT ( 'NONE',  ( 0.7261896124251127072, 0.1329856088156805560, 1.836402230816103209 ) ) ;
#134206=CARTESIAN_POINT ( 'NONE',  ( 5.215527394842717435, -0.3265260713646127022, 2.182469266582609091 ) ) ;
#134208=CARTESIAN_POINT ( 'NONE',  ( 1.265152180075890254, -1.953616520262021039, -0.9254636565915741464 ) ) ;
#134210=CARTESIAN_POINT ( 'NONE',  ( 1.833220611596135363, -1.622487599052296670, -1.197302888167578683 ) ) ;
#134211=CARTESIAN_POINT ( 'NONE',  ( 2.038793776981039141, 2.199649879376049721, -0.6664975855598854748 ) ) ;
#134214=CARTESIAN_POINT ( 'NONE',  ( 0.1802491246630563426, -1.813337052076903877, -0.4591185353455888296 ) ) ;
#134216=CARTESIAN_POINT ( 'NONE',  ( 2.113927203836548419, -0.8795192785214582809, -1.650985937663045577 ) ) ;
#134217=CARTESIAN_POINT ( 'NONE',  ( 3.907435596788138010, -1.928258004016227378, 0.5899861904685861358 ) ) ;
#134221=CARTESIAN_POINT ( 'NONE',  ( 4.653012138262506703, -1.691843218806210247, 1.254050867608807129 ) ) ;
#134224=CARTESIAN_POINT ( 'NONE',  ( 6.539320575229278454, 3.689604457162498630, 2.617406275049142916 ) ) ;
#134225=CARTESIAN_POINT ( 'NONE',  ( 5.695571270406009745, 1.864622851205568699, -0.7768453975713036641 ) ) ;
#134228=CARTESIAN_POINT ( 'NONE',  ( 0.6903719162679988752, 1.063636609032023950, -1.767059929103020677 ) ) ;
#134237=CARTESIAN_POINT ( 'NONE',  ( 2.611994278460927799, 0.5808993838645438723, -2.091943403374715515 ) ) ;
#134240=CARTESIAN_POINT ( 'NONE',  ( 2.471991059931688106, -1.762569054296094340, -0.5325411743367302053 ) ) ;
#134242=CARTESIAN_POINT ( 'NONE',  ( 3.948915171154475878, -1.822730400009948237, -1.216494452853926322 ) ) ;
#134244=CARTESIAN_POINT ( 'NONE',  ( 5.260715670973223901, -1.642634774727338653, 1.556112085687613611 ) ) ;
#134251=CARTESIAN_POINT ( 'NONE',  ( 6.503183016764070068, 1.472852356768614479, 0.9808112332466749628 ) ) ;
#134252=CARTESIAN_POINT ( 'NONE',  ( 3.932292794061467589, -1.036904606752734326, -1.725386108540658103 ) ) ;
#134254=CARTESIAN_POINT ( 'NONE',  ( 2.942513229011092690, 2.089901898437613870, 0.2590637233205703716 ) ) ;
#134255=CARTESIAN_POINT ( 'NONE',  ( 0.6674275129862971001, 1.287417287929611076, 1.418633514309353583 ) ) ;
#134259=CARTESIAN_POINT ( 'NONE',  ( 2.576555279139204568, 1.288776560207754551, -1.489423508990360023 ) ) ;
#134261=CARTESIAN_POINT ( 'NONE',  ( 0.6605093422152423788, -0.6574743052488278838, -1.848563176889833626 ) ) ;
#134262=CARTESIAN_POINT ( 'NONE',  ( 0.5977379272000953314, 1.286164058678052946, 1.415416067018962165 ) ) ;
#134266=CARTESIAN_POINT ( 'NONE',  ( 5.559403950928493821, 0.3636877230743483236, -1.834782481876767291 ) ) ;
#134268=CARTESIAN_POINT ( 'NONE',  ( 5.840704046183605946, -2.018525344099521668, -0.4591754850708437696 ) ) ;
#134271=CARTESIAN_POINT ( 'NONE',  ( 0.2388460773940295212, -2.007853281042128568, -0.5044432775610437902 ) ) ;
#134281=CARTESIAN_POINT ( 'NONE',  ( 4.738696794244872557, -1.902450960283699199, -0.4786090228221794307 ) ) ;
#134283=CARTESIAN_POINT ( 'NONE',  ( 2.706407486732204326, -1.492025830231600070, -1.356093404896424826 ) ) ;
#134284=CARTESIAN_POINT ( 'NONE',  ( 2.870226655882984090, -1.888176233477338872, -0.3226071530259622677 ) ) ;
#134286=CARTESIAN_POINT ( 'NONE',  ( -0.07626876867936756288, -1.353788312843669406, -1.724171373301164767 ) ) ;
#134287=CARTESIAN_POINT ( 'NONE',  ( 0.1331715793776418189, 2.029267568408019695, -2.369146612602909041 ) ) ;
#134288=CARTESIAN_POINT ( 'NONE',  ( 3.778450875046265534, -1.801938340082277712, -0.5016190811713144848 ) ) ;
#134292=CARTESIAN_POINT ( 'NONE',  ( 4.429392955138825805, -1.637772332673973485, -1.341807030983455773 ) ) ;
#134293=CARTESIAN_POINT ( 'NONE',  ( 6.092251258522619395, 1.023830597077223903, -1.799436568697235783 ) ) ;
#134294=CARTESIAN_POINT ( 'NONE',  ( 1.962552558803489555, -1.912825090402545225, -0.8444004386199343015 ) ) ;
#134295=CARTESIAN_POINT ( 'NONE',  ( 6.620655732516642189, 2.417337544263608251, 2.554705107920357321 ) ) ;
#134296=CARTESIAN_POINT ( 'NONE',  ( 0.6215558277854142943, -0.9165932506310509043, -1.460862699585960822 ) ) ;
#134301=( NAMED_UNIT ( * ) PLANE_ANGLE_UNIT ( ) SI_UNIT ( $, .RADIAN. ) );
#134305=CARTESIAN_POINT ( 'NONE',  ( 0.3811517019768875802, 0.1791931900220759266, -1.802556192996515705 ) ) ;
#134315=CARTESIAN_POINT ( 'NONE',  ( 0.7201576878450620667, 1.887430420354209160, 0.3262839321072578125 ) ) ;
#134316=CARTESIAN_POINT ( 'NONE',  ( 0.01256502854718108061, -2.120115106878577294, -0.04748564598491820943 ) ) ;
#134324=CARTESIAN_POINT ( 'NONE',  ( 3.784006971647640327, -1.169605039944806357, -1.584395421511639812 ) ) ;
#134325=CARTESIAN_POINT ( 'NONE',  ( 1.260569961473339440, 2.118219532560499996, 0.1004958096475216667 ) ) ;
#134329=CARTESIAN_POINT ( 'NONE',  ( 5.859372887940716090, 2.159598860408561194, -0.3713886045505072064 ) ) ;
#134331=CARTESIAN_POINT ( 'NONE',  ( 3.733351708207183428, -1.780342035418970736, 0.7362343730293962052 ) ) ;
#134334=CARTESIAN_POINT ( 'NONE',  ( 1.489210700298746692, -0.3264265768355456565, -2.182489157894373033 ) ) ;
#134339=CARTESIAN_POINT ( 'NONE',  ( 5.700047960291365179, 0.8015925475840814940, -1.799137058317602067 ) ) ;
#134340=CARTESIAN_POINT ( 'NONE',  ( -0.07675543424010172755, -1.195724141806488561, -1.531021551883532172 ) ) ;
#134341=CARTESIAN_POINT ( 'NONE',  ( 6.151801744867631427, -0.3282927394851458125, -2.274731023314037870 ) ) ;
#134343=CARTESIAN_POINT ( 'NONE',  ( 4.188223417972539053, 0.9984873940180930552, -1.570204455898941420 ) ) ;
#134349=CARTESIAN_POINT ( 'NONE',  ( 6.720655732516625847, 7.629137130509076492, 2.426260288887295058 ) ) ;
#134350=CARTESIAN_POINT ( 'NONE',  ( 6.620655732516666170, 0.0004550665020433551948, 2.073887158236031425 ) ) ;
#134352=ORIENTED_EDGE ( 'NONE', *, *, #39650, .F. ) ;
#134355=CARTESIAN_POINT ( 'NONE',  ( 0.2229205655521030172, -0.09321834626660817358, 1.823428419517532983 ) ) ;
#134357=CARTESIAN_POINT ( 'NONE',  ( 3.129275142338799665, 0.4248101585269374869, 1.681139380183617194 ) ) ;
#134361=CARTESIAN_POINT ( 'NONE',  ( 6.709597972018079837, -0.3944863986210072060, 1.789098616620278470 ) ) ;
#134362=CARTESIAN_POINT ( 'NONE',  ( 3.889464431383614862, -1.814284039448841979, 0.7467176931179178023 ) ) ;
#134363=MECHANICAL_DESIGN_GEOMETRIC_PRESENTATION_REPRESENTATION('',(#213917),#113682);
#134367=CARTESIAN_POINT ( 'NONE',  ( 5.057343377742961721, -1.818460011135439869, 1.090507627184752693 ) ) ;
#134371=CARTESIAN_POINT ( 'NONE',  ( 2.993098612437725681, 0.2488643248897918769, 2.055149816265568585 ) ) ;
#134374=CARTESIAN_POINT ( 'NONE',  ( 4.547657996348432263, -2.031006315926532135, 0.8999586162586125093 ) ) ;
#134376=CARTESIAN_POINT ( 'NONE',  ( 2.866213343745026343, -0.1723225051825111875, -2.292302961975992037 ) ) ;
#134384=CARTESIAN_POINT ( 'NONE',  ( 3.937688585161042809, -1.828529804631402023, 0.5600222464785462595 ) ) ;
#134386=CARTESIAN_POINT ( 'NONE',  ( 4.805503449324158183, -0.4579143662744952770, 1.662777411968613839 ) ) ;
#134387=CARTESIAN_POINT ( 'NONE',  ( 2.958220528980559205, -1.197304571117228100, 1.622486353517027968 ) ) ;
#134388=CARTESIAN_POINT ( 'NONE',  ( 4.237165586469007650, 2.298153656159235503, -0.05646909981197979073 ) ) ;
#134390=CARTESIAN_POINT ( 'NONE',  ( 6.463511354401173747, 0.3618736704080193212, -2.074577690073164060 ) ) ;
#134392=CARTESIAN_POINT ( 'NONE',  ( 5.870295291196549137, -1.121585077578592049, 1.368893044642209178 ) ) ;
#134394=CARTESIAN_POINT ( 'NONE',  ( 1.658568045375780731, -1.618562549950094187, 1.623430423404078837 ) ) ;
#134395=CARTESIAN_POINT ( 'NONE',  ( 0.1283017097272065865, -1.593451896579937355, 0.7002181395190426594 ) ) ;
#134402=CARTESIAN_POINT ( 'NONE',  ( 6.637176860265922684, -0.09746846054551477900, -2.068182370504913159 ) ) ;
#134403=CARTESIAN_POINT ( 'NONE',  ( 1.481658059775035952, -0.6748446255696785023, 1.900416712880992343 ) ) ;
#134405=CARTESIAN_POINT ( 'NONE',  ( 5.619733630554700099, -1.879067156935828820, 0.4242066570522682878 ) ) ;
#134407=CARTESIAN_POINT ( 'NONE',  ( 2.074768627854159053, 0.9548037322763336388, 2.005906060693471993 ) ) ;
#134415=CARTESIAN_POINT ( 'NONE',  ( 4.018918099032080526, -1.663992213871115178, 0.5101021115980988174 ) ) ;
#134416=CARTESIAN_POINT ( 'NONE',  ( 2.646866301197240645, -0.3325320220872363675, -1.933311746529025266 ) ) ;
#134422=CARTESIAN_POINT ( 'NONE',  ( 1.117717378214663881, 0.4042816502292169711, -2.022510655824232728 ) ) ;
#134425=CARTESIAN_POINT ( 'NONE',  ( 1.429016818436980474, 2.180957219565873295, 0.6017249355739097139 ) ) ;
#134426=ORIENTED_EDGE ( 'NONE', *, *, #90488, .F. ) ;
#134428=CARTESIAN_POINT ( 'NONE',  ( 2.846779338809723559, -1.557328454271855955, 1.035869100625155470 ) ) ;
#134429=CARTESIAN_POINT ( 'NONE',  ( 1.371252568922965098, -0.2536805693413109464, -1.715349781374966742 ) ) ;
#134430=CARTESIAN_POINT ( 'NONE',  ( 5.442994344319362021, -1.727133847215430729, -1.348975639928217118 ) ) ;
#134431=CARTESIAN_POINT ( 'NONE',  ( 5.350698970897345141, 0.6634653876971875475, 2.210164229930264845 ) ) ;
#134433=CARTESIAN_POINT ( 'NONE',  ( 1.428666007085793277, 1.985871523383303749, 0.5506756191897729247 ) ) ;
#134434=CARTESIAN_POINT ( 'NONE',  ( 3.732312008210575627, 0.2860496425412931143, 1.920654750396868726 ) ) ;
#134436=CARTESIAN_POINT ( 'NONE',  ( 5.676977070516882051, -0.04517083460114229565, -1.870152005306220611 ) ) ;
#134438=CARTESIAN_POINT ( 'NONE',  ( 6.766953912288387940, -2.015720078709513086, 0.04667315333419658208 ) ) ;
#134441=CARTESIAN_POINT ( 'NONE',  ( 4.658827374183164949, 1.163267680695536876, 1.646840100852072997 ) ) ;
#134445=CARTESIAN_POINT ( 'NONE',  ( 1.752308680507021155, 0.5713779359179693706, 1.734036872924920702 ) ) ;
#134454=CARTESIAN_POINT ( 'NONE',  ( 6.111974619354628935, -0.6785462737385530296, 1.902425049502977528 ) ) ;
#134455=CARTESIAN_POINT ( 'NONE',  ( 0.3992906662320141464, -0.2637550127744873185, -2.103967267096308991 ) ) ;
#134459=CARTESIAN_POINT ( 'NONE',  ( 4.838775396685393915, 0.3501730741383273782, 2.030750449888196751 ) ) ;
#134460=CARTESIAN_POINT ( 'NONE',  ( 5.643203987388664800, 0.8197706014990979728, 1.842448445624145226 ) ) ;
#134469=CARTESIAN_POINT ( 'NONE',  ( 4.657577273293715514, -0.4389639308803178208, -1.967586094827819654 ) ) ;
#134470=CARTESIAN_POINT ( 'NONE',  ( 4.312339554033173705, 1.684294245562456993, 0.7440144950455057637 ) ) ;
#134472=CARTESIAN_POINT ( 'NONE',  ( 2.192384427926857615, -0.9847255960707482769, 2.087179981119008598 ) ) ;
#134475=CARTESIAN_POINT ( 'NONE',  ( 5.026735257907362531, 2.066873009482797841, 0.6328083787210944111 ) ) ;
#134476=CARTESIAN_POINT ( 'NONE',  ( 3.344935638061694139, -1.780668040901035143, -0.9463001528628791625 ) ) ;
#134478=CARTESIAN_POINT ( 'NONE',  ( 0.1517630622446651534, 0.7442075171455504456, 1.793999140845178530 ) ) ;
#134481=CARTESIAN_POINT ( 'NONE',  ( 3.256579335763456040, -1.417408692332474462, 1.220890361658559575 ) ) ;
#134483=CARTESIAN_POINT ( 'NONE',  ( 6.533470331352867255, -0.1283082721124771952, 1.781802213622991404 ) ) ;
#134486=CARTESIAN_POINT ( 'NONE',  ( 2.315298440750997777, 1.971968782506158924, 0.9909306302095726160 ) ) ;
#134487=CARTESIAN_POINT ( 'NONE',  ( 6.720655732516647163, -0.004400176169771369272, 2.173773060281408931 ) ) ;
#134492=CARTESIAN_POINT ( 'NONE',  ( 0.2628735715076990220, -1.758816568047173234, -0.8906303152973747972 ) ) ;
#134493=CARTESIAN_POINT ( 'NONE',  ( 0.4996044509122186672, 1.916167126895538031, -1.285522792546058390 ) ) ;
#134494=CARTESIAN_POINT ( 'NONE',  ( 1.539427311113782837, 1.813978416018032558, -0.7477436361984082236 ) ) ;
#134496=CARTESIAN_POINT ( 'NONE',  ( 4.610253265130005218, 2.062215687086375038, -0.04552280787792003375 ) ) ;
#134503=CARTESIAN_POINT ( 'NONE',  ( 6.285609470618021888, -2.046568710056245965, 0.7253697862827021003 ) ) ;
#134504=CARTESIAN_POINT ( 'NONE',  ( 6.163598723784101452, 0.9525508894225950263, 1.575581956637741587 ) ) ;
#134507=CARTESIAN_POINT ( 'NONE',  ( 1.018573325691285003, 1.726041315240328444, 0.7214104187760681519 ) ) ;
#134512=CARTESIAN_POINT ( 'NONE',  ( 0.6274217273865911881, -0.2802014979648696502, 1.891502685196180034 ) ) ;
#134513=CARTESIAN_POINT ( 'NONE',  ( 2.729092984789914578, -1.652188407247729529, 0.6350153418272014294 ) ) ;
#134514=CARTESIAN_POINT ( 'NONE',  ( 0.5219363917940004205, -1.903054291476031112, 0.1877445768119419822 ) ) ;
#134516=CARTESIAN_POINT ( 'NONE',  ( 4.798395639560619763, 1.317935440718048135, -1.390428439694970431 ) ) ;
#134518=CARTESIAN_POINT ( 'NONE',  ( 4.914487397858644080, 0.7518983826605809551, 1.820584232156793769 ) ) ;
#134519=CARTESIAN_POINT ( 'NONE',  ( 0.4574861729177078229, -1.815669959853306370, 1.095388807130371900 ) ) ;
#134521=CARTESIAN_POINT ( 'NONE',  ( 3.537841792810627606, 0.8420186812403904764, -1.670516725672297031 ) ) ;
#134522=CARTESIAN_POINT ( 'NONE',  ( 0.3283667639546791195, 1.746078182827022429, 0.5332771064449209897 ) ) ;
#134524=CARTESIAN_POINT ( 'NONE',  ( 3.739080281021701868, 0.3231575147602770426, 2.182976880621155136 ) ) ;
#134526=CARTESIAN_POINT ( 'NONE',  ( 0.9770945003616584579, 1.905102050789074353, 0.7911672170514363334 ) ) ;
#134533=CARTESIAN_POINT ( 'NONE',  ( 3.455589482447298355, 1.630370400113918095, 1.275915752658786095 ) ) ;
#134535=CARTESIAN_POINT ( 'NONE',  ( 1.968271169257681752, 1.109365460190291586, 1.855047589327807778 ) ) ;
#134537=CARTESIAN_POINT ( 'NONE',  ( 0.6979228276546626253, 1.358177971483988555, 1.494960626620364552 ) ) ;
#134543=CARTESIAN_POINT ( 'NONE',  ( 6.450546045330814771, 1.388275245401158431, 1.462219883709668045 ) ) ;
#134544=CARTESIAN_POINT ( 'NONE',  ( 6.262892222096183126, -0.1014175117164286682, -1.913191589401983528 ) ) ;
#134545=CARTESIAN_POINT ( 'NONE',  ( 6.539320575229294441, 2.949125184229839380, 2.655650464557571144 ) ) ;
#134546=CARTESIAN_POINT ( 'NONE',  ( 4.722331747100577459, 2.097238624054961864, 0.6360808509995665716 ) ) ;
#134548=CARTESIAN_POINT ( 'NONE',  ( 3.058751851047710080, 0.4689117840017149041, 1.853869267190631831 ) ) ;
#134553=CARTESIAN_POINT ( 'NONE',  ( 1.388296234047466049, -0.7283980888908546669, -1.880428666220852696 ) ) ;
#134556=CARTESIAN_POINT ( 'NONE',  ( 0.01182134700736507844, -2.246462713633586183, 0.4557613021327082681 ) ) ;
#134558=CARTESIAN_POINT ( 'NONE',  ( 4.278129899785966472, -0.9921777787025712891, 1.410595609005516504 ) ) ;
#134559=CARTESIAN_POINT ( 'NONE',  ( 0.1394461523056798324, 0.009327122704651937685, -1.719853553173174232 ) ) ;
#134563=CARTESIAN_POINT ( 'NONE',  ( 1.557006721180295150, 1.605793932651664813, -1.126831546849601740 ) ) ;
#134566=CARTESIAN_POINT ( 'NONE',  ( 0.1751657365761495888, 6.947016338497860488, -2.639079955608885975 ) ) ;
#134571=CARTESIAN_POINT ( 'NONE',  ( 4.371601898205011771, 0.3924986647133471007, -1.768265068870542800 ) ) ;
#134575=CARTESIAN_POINT ( 'NONE',  ( 5.145072886348948771, 0.1388508722429954989, 1.806219837558323826 ) ) ;
#134577=CIRCLE ( 'NONE', #110479, 0.04999999999999969746 ) ;
#134580=CARTESIAN_POINT ( 'NONE',  ( 5.740631066870683696, -1.815735608131360479, -0.4073663091734185948 ) ) ;
#134582=CARTESIAN_POINT ( 'NONE',  ( 4.200734335399162411, 1.752999579934441998, 0.7727710859696481638 ) ) ;
#134589=CARTESIAN_POINT ( 'NONE',  ( 1.147603855448702248, -1.704515299458901012, -1.329379018566230641 ) ) ;
#134592=CARTESIAN_POINT ( 'NONE',  ( 0.8151338971811080691, -0.2727355552937099636, 1.804975678908596226 ) ) ;
#134594=CARTESIAN_POINT ( 'NONE',  ( 4.067279105520240634, 0.2236234833344897255, -1.811772463268163547 ) ) ;
#134596=CARTESIAN_POINT ( 'NONE',  ( 2.232540727315056373, 1.246330492051262784, -1.450604739030990187 ) ) ;
#134597=CARTESIAN_POINT ( 'NONE',  ( 2.453506318599480096, 1.520516184767862100, 1.251830903418025054 ) ) ;
#134598=CARTESIAN_POINT ( 'NONE',  ( 4.054194213510796452, -1.436945492307143635, 1.306602268835421077 ) ) ;
#134602=CARTESIAN_POINT ( 'NONE',  ( 4.201511661969238531, 1.892856375164463367, -0.9562558712687405649 ) ) ;
#134609=CARTESIAN_POINT ( 'NONE',  ( 4.160648861918358143, -1.351394993475165673, 1.227733137840483879 ) ) ;
#134616=CARTESIAN_POINT ( 'NONE',  ( 4.698043743269282757, -1.870269067358639958, -0.04562963166049315705 ) ) ;
#134618=CARTESIAN_POINT ( 'NONE',  ( 3.826716429392281071, 1.829700617163315002, 0.6032043533580729866 ) ) ;
#134625=CARTESIAN_POINT ( 'NONE',  ( 1.546650761107182914, -1.494491507556227505, 1.499968751290579494 ) ) ;
#134628=CARTESIAN_POINT ( 'NONE',  ( 6.772334134356085222, -0.9704686269969391432, -1.828672837219179392 ) ) ;
#134629=CARTESIAN_POINT ( 'NONE',  ( 1.522747961674526085, -1.733470594775164075, 0.6210259959333885860 ) ) ;
#134634=CARTESIAN_POINT ( 'NONE',  ( 1.658568045375780731, -1.618562549950094187, 1.623430423404078837 ) ) ;
#134635=CARTESIAN_POINT ( 'NONE',  ( 5.613211309847925712, -1.894178568204254676, 0.4274185452872342195 ) ) ;
#134638=CARTESIAN_POINT ( 'NONE',  ( 1.090090997392887173, 1.202455520763350272, 1.614487003566661638 ) ) ;
#134643=CARTESIAN_POINT ( 'NONE',  ( 4.365234240191905535, 2.027873629061471838, -0.5078740465511691893 ) ) ;
#134644=CARTESIAN_POINT ( 'NONE',  ( 1.797346856567107798, -0.6001438452145327895, 1.665118380002019283 ) ) ;
#134647=CARTESIAN_POINT ( 'NONE',  ( 5.138769532551322072, -1.968056315684912683, 1.175056510511104158 ) ) ;
#134648=CARTESIAN_POINT ( 'NONE',  ( 3.890341755399207013, 1.468866505370895137, -0.9330376088199500151 ) ) ;
#134652=CARTESIAN_POINT ( 'NONE',  ( 3.338897068646465627, -1.034916488738941709, 1.390885369450091336 ) ) ;
#134654=CARTESIAN_POINT ( 'NONE',  ( 3.596278845262687263, 0.9791764565295042466, -1.937929667198809769 ) ) ;
#134656=CARTESIAN_POINT ( 'NONE',  ( 4.997279897388729353, -0.2910847460899004258, 1.995267753224789997 ) ) ;
#134657=CARTESIAN_POINT ( 'NONE',  ( 0.03128095451081137207, -0.7860540964617872550, -1.895863743164089676 ) ) ;
#134659=CARTESIAN_POINT ( 'NONE',  ( 2.608320942171663326, -0.7355144804263250569, -1.780640224430999563 ) ) ;
#134661=CARTESIAN_POINT ( 'NONE',  ( 6.170221320256972675, 2.215557125880045053, -0.1624646739342323065 ) ) ;
#134663=CARTESIAN_POINT ( 'NONE',  ( 6.883263157960399781, 2.970623603138924818, 2.399364662246627589 ) ) ;
#134669=CARTESIAN_POINT ( 'NONE',  ( 0.3994919479695389075, -0.2781545790336605317, -2.203771652037065376 ) ) ;
#134670=CARTESIAN_POINT ( 'NONE',  ( 6.074655751228532630, 1.318658252384183438, -1.452748870126779890 ) ) ;
#134673=CARTESIAN_POINT ( 'NONE',  ( 6.784454189598811524, -2.216766238704069636, -0.4514476129710183194 ) ) ;
#134676=CARTESIAN_POINT ( 'NONE',  ( 3.877431937021211361, -0.1548021625025173265, 2.056941320008953245 ) ) ;
#134680=CARTESIAN_POINT ( 'NONE',  ( 5.887941446147332947, -0.8415115861447747259, 1.670666529855535654 ) ) ;
#134681=CARTESIAN_POINT ( 'NONE',  ( 5.150864522821732017, 0.8611363216781149355, 1.505151585408972981 ) ) ;
#134682=CARTESIAN_POINT ( 'NONE',  ( 3.649730646487856056, 0.6304092353721781894, 1.622436561192377891 ) ) ;
#134684=CARTESIAN_POINT ( 'NONE',  ( 1.874976642369927005, -0.1173453557595251634, -2.289501271392534676 ) ) ;
#134686=CARTESIAN_POINT ( 'NONE',  ( 5.636299653793654940, 0.4088526781071535887, 2.050197504659311942 ) ) ;
#134687=CARTESIAN_POINT ( 'NONE',  ( 0.4097734724025984820, 1.271762808003698009, -1.331557029818277060 ) ) ;
#134689=CARTESIAN_POINT ( 'NONE',  ( 1.758435621656749603, 1.928751379572872571, -0.5880216644931559600 ) ) ;
#134690=CARTESIAN_POINT ( 'NONE',  ( 0.6389542677898361056, -1.877638805159736579, 1.129783718924075364 ) ) ;
#134694=CARTESIAN_POINT ( 'NONE',  ( 2.280079029133400326, 2.079044457705871096, -0.4163345062310334632 ) ) ;
#134696=CARTESIAN_POINT ( 'NONE',  ( 5.109893933574640279, -1.816543354971979163, 0.1824992186492402357 ) ) ;
#134702=CARTESIAN_POINT ( 'NONE',  ( 2.777608160125254688, 0.2920557517631214295, -1.998411540393054020 ) ) ;
#134703=CARTESIAN_POINT ( 'NONE',  ( 6.299877592275240801, -0.7493655176046759570, 2.075778730795534877 ) ) ;
#134705=CARTESIAN_POINT ( 'NONE',  ( 4.451900780290086956, -0.7152352812324501707, 1.718214207458491849 ) ) ;
#134713=CARTESIAN_POINT ( 'NONE',  ( 1.475528429365607019, 1.526226248090801318, 0.8227105958887138693 ) ) ;
#134714=CARTESIAN_POINT ( 'NONE',  ( 1.517106797927396444, -0.9646358079543941866, -1.448293472534349702 ) ) ;
#134716=CARTESIAN_POINT ( 'NONE',  ( 5.356226580172758212, 2.305273348739949935, -0.1085102657557151934 ) ) ;
#134719=CARTESIAN_POINT ( 'NONE',  ( 1.194684731684968693, -0.4980721920408748282, -1.999570191575838818 ) ) ;
#134721=CARTESIAN_POINT ( 'NONE',  ( 6.872461156203343080, -0.5239007177601956444, 2.246970456009795836 ) ) ;
#134724=CARTESIAN_POINT ( 'NONE',  ( 6.754772315933175619, -1.444328698515121800, 1.188528157999017454 ) ) ;
#134725=CARTESIAN_POINT ( 'NONE',  ( 4.605663860560767375, 1.420894170025093439, 1.280184534114735095 ) ) ;
#134727=CARTESIAN_POINT ( 'NONE',  ( 6.129534211984397629, -2.079372889712034489, 0.7396383780838566846 ) ) ;
#134732=CARTESIAN_POINT ( 'NONE',  ( 0.4518267731568551548, -1.429874679360541023, -1.426642250087527541 ) ) ;
#134734=CARTESIAN_POINT ( 'NONE',  ( 3.891899753260852801, 1.669126095664546838, 1.593640439619238514 ) ) ;
#134735=CARTESIAN_POINT ( 'NONE',  ( 4.369553226407375313, -0.3375162941181614751, 1.932460123137308861 ) ) ;
#134737=CARTESIAN_POINT ( 'NONE',  ( 0.4968289091572677396, 0.3296062100675010154, 1.933703066120408209 ) ) ;
#134741=CARTESIAN_POINT ( 'NONE',  ( 6.456263137377813877, -1.236968576560824040, 1.593241027169020052 ) ) ;
#134743=CARTESIAN_POINT ( 'NONE',  ( 2.676840970354518845, 1.421027823260514911, -1.641450307487320792 ) ) ;
#134745=CARTESIAN_POINT ( 'NONE',  ( 1.072698285844303934, 0.8645715524648779349, 1.936551149067309741 ) ) ;
#134750=CARTESIAN_POINT ( 'NONE',  ( 2.583338899891209017, 1.885494326376845775, -0.8321024974875782521 ) ) ;
#134758=CARTESIAN_POINT ( 'NONE',  ( 4.793567869993575314, 1.782951692925707654, -0.6917526515820491273 ) ) ;
#134760=CARTESIAN_POINT ( 'NONE',  ( 1.089599759544016999, 1.994953948513054742, -1.067007742874733545 ) ) ;
#134762=CARTESIAN_POINT ( 'NONE',  ( 1.581973821214562204, 0.9331543445117953528, 1.552620351220496353 ) ) ;
#134763=CARTESIAN_POINT ( 'NONE',  ( 0.8135319083415553099, -1.217954555017298324, -1.478650609923468195 ) ) ;
#134764=CARTESIAN_POINT ( 'NONE',  ( 1.645070734656968625, -0.3017366986639741788, -2.048123538821471801 ) ) ;
#134766=CARTESIAN_POINT ( 'NONE',  ( 6.819227946136852125, -0.1326586024288610444, 1.840611662119538749 ) ) ;
#134767=CARTESIAN_POINT ( 'NONE',  ( 5.971306315489836258, 0.1393824199819072851, -1.921517340817725961 ) ) ;
#134768=CARTESIAN_POINT ( 'NONE',  ( 6.375609195709820654, 2.113139023092651225, -0.6363509056886568205 ) ) ;
#134771=CARTESIAN_POINT ( 'NONE',  ( 3.912594259961211574, 0.7396031425229695477, 1.925699983396757409 ) ) ;
#134776=CARTESIAN_POINT ( 'NONE',  ( 4.911209521004105127, 1.831006069304096373, 1.040297942642433249 ) ) ;
#134778=CARTESIAN_POINT ( 'NONE',  ( 6.830528382861658088, -1.277203763263988101, 1.630111558092485868 ) ) ;
#134780=CARTESIAN_POINT ( 'NONE',  ( 4.587301040747738590, 1.933109172225885963, -0.9673573668882374799 ) ) ;
#134781=CARTESIAN_POINT ( 'NONE',  ( 5.795571226005820087, 1.865288689459403848, -0.7749498061812712946 ) ) ;
#134789=CARTESIAN_POINT ( 'NONE',  ( 3.960172920142067898, -1.157100329752266621, 1.651342637023434090 ) ) ;
#134797=CARTESIAN_POINT ( 'NONE',  ( 4.112907772398490813, 0.1017678201147946826, 2.013986186455194449 ) ) ;
#134799=CARTESIAN_POINT ( 'NONE',  ( 0.2930059409478984467, 1.274291793118907723, 1.162708412170476713 ) ) ;
#134805=CARTESIAN_POINT ( 'NONE',  ( 5.061713478001653499, 1.850364105758989020, -0.2730526881008291662 ) ) ;
#134806=CARTESIAN_POINT ( 'NONE',  ( 6.029547050951932441, -0.2422988993314358630, 1.998484822443524322 ) ) ;
#134811=CARTESIAN_POINT ( 'NONE',  ( 0.1754079408978586052, 1.496066871905444851, 1.352139405095334590 ) ) ;
#134812=CARTESIAN_POINT ( 'NONE',  ( 1.388595261843462714, -1.720809334905664567, -0.5665428721913360333 ) ) ;
#134818=CARTESIAN_POINT ( 'NONE',  ( 0.1279635871501626776, 1.910768599467532081, 0.1380287717926073077 ) ) ;
#134820=FACE_OUTER_BOUND ( 'NONE', #136573, .T. ) ;
#134825=CARTESIAN_POINT ( 'NONE',  ( 4.276362541559985075, -1.246951984143488623, 1.765614359104182629 ) ) ;
#134828=CARTESIAN_POINT ( 'NONE',  ( 1.072698285844303934, 0.8645715524648778239, 1.936551149067309519 ) ) ;
#134831=CARTESIAN_POINT ( 'NONE',  ( 2.249238725404782091, -1.581088017263340806, -1.177247449022495118 ) ) ;
#134832=CARTESIAN_POINT ( 'NONE',  ( 4.728717205193702533, 1.314622909153417174, -1.389140896021365368 ) ) ;
#134835=CARTESIAN_POINT ( 'NONE',  ( 6.619592842669682398, 0.3380432134332654881, -1.940159576567195288 ) ) ;
#134836=CARTESIAN_POINT ( 'NONE',  ( 1.868985280173897756, 1.858391233338702042, -0.5634987755925959796 ) ) ;
#134843=CARTESIAN_POINT ( 'NONE',  ( 4.740819843082155316, 1.831016553098392619, 0.5515768964349797576 ) ) ;
#134845=CARTESIAN_POINT ( 'NONE',  ( 3.616033620774202983, -2.174319932014677548, 0.3768175846284789743 ) ) ;
#134846=CARTESIAN_POINT ( 'NONE',  ( 1.764966765715753949, -1.560254191817540992, 1.560848541443552895 ) ) ;
#134848=CARTESIAN_POINT ( 'NONE',  ( 0.4692111731946085884, -1.615589042895089200, -1.022764193708516789 ) ) ;
#134849=CARTESIAN_POINT ( 'NONE',  ( 0.07680821025391955381, 1.395885924038504644, -2.068540888291516833 ) ) ;
#134852=CARTESIAN_POINT ( 'NONE',  ( 3.297389726143422184, -1.827171938055579314, 0.9735347560282038293 ) ) ;
#134856=CARTESIAN_POINT ( 'NONE',  ( 0.5499753625364013354, 0.6768306982547143136, -2.053065283773393368 ) ) ;
#134857=CARTESIAN_POINT ( 'NONE',  ( 3.263397454411249399, 2.137687552337414587, -0.4822058812353549606 ) ) ;
#134865=CARTESIAN_POINT ( 'NONE',  ( 6.381516696256908538, -0.4728550111133908995, -1.668365442416564814 ) ) ;
#134867=CARTESIAN_POINT ( 'NONE',  ( 3.995033623311712301, 0.2988084191791628985, 2.048438004591215389 ) ) ;
#134868=CARTESIAN_POINT ( 'NONE',  ( 4.411780756640943046, -1.303739072956756617, -1.668109288273095014 ) ) ;
#134871=CARTESIAN_POINT ( 'NONE',  ( 2.465619613223976270, -0.4363654233677862759, 1.920310867443141278 ) ) ;
#134872=CARTESIAN_POINT ( 'NONE',  ( 1.300873410958070409, -0.2835801433653042380, -1.891145142470892715 ) ) ;
#134873=CARTESIAN_POINT ( 'NONE',  ( 5.226663038502143088, 0.1645964690673335229, 2.286419844370500165 ) ) ;
#134874=CARTESIAN_POINT ( 'NONE',  ( 3.316849939159485228, 1.650902842016691130, 0.7798126646740562995 ) ) ;
#134878=CARTESIAN_POINT ( 'NONE',  ( 4.166274970888473206, 2.012660793657996106, -0.05373556394885727755 ) ) ;
#134879=CARTESIAN_POINT ( 'NONE',  ( 3.836726278109466204, -1.889416792123297162, -0.5274722977551549175 ) ) ;
#134882=CARTESIAN_POINT ( 'NONE',  ( 0.1753634416057497647, 0.2329791690731698173, -2.177930625204091086 ) ) ;
#134883=CARTESIAN_POINT ( 'NONE',  ( -0.1234093946873336678, -0.1598125250084568849, -2.056614676860648583 ) ) ;
#134884=CARTESIAN_POINT ( 'NONE',  ( 5.471497560916138703, 1.704843785431299219, -0.4750155384096472755 ) ) ;
#134886=CARTESIAN_POINT ( 'NONE',  ( 1.623246906879351581, -2.062630869249089116, 0.7406334225198917265 ) ) ;
#134887=CARTESIAN_POINT ( 'NONE',  ( 6.263578219495629540, 0.9010232283708031753, 1.488777805958479528 ) ) ;
#134889=CARTESIAN_POINT ( 'NONE',  ( 0.1335669894368343991, 6.947499997881672940, -2.748639729795236963 ) ) ;
#134890=CARTESIAN_POINT ( 'NONE',  ( 0.4512176508754310866, 0.5462255407458499468, -1.636193974722987221 ) ) ;
#134891=CARTESIAN_POINT ( 'NONE',  ( 0.5800033175489105464, 1.582751930679682228, -1.666757776657208145 ) ) ;
#134892=CARTESIAN_POINT ( 'NONE',  ( 0.5038066827526345159, -2.180447833630628107, 0.2205874978757973448 ) ) ;
#134893=CARTESIAN_POINT ( 'NONE',  ( 6.309869086801066729, -1.462580435118435496, 0.9307709330467325293 ) ) ;
#134894=CARTESIAN_POINT ( 'NONE',  ( 2.473496279428960776, 0.1070396533628548558, -2.204406164007084445 ) ) ;
#134895=CARTESIAN_POINT ( 'NONE',  ( 6.514155524301521005, 2.165825943586483504, -0.1531846826740568268 ) ) ;
#134897=CARTESIAN_POINT ( 'NONE',  ( 1.253280101782401124, 0.1498745247594003016, -2.112069961602327517 ) ) ;
#134898=CARTESIAN_POINT ( 'NONE',  ( 6.827182134110223899, 2.937564492898884438, 2.740749177975018380 ) ) ;
#134899=CARTESIAN_POINT ( 'NONE',  ( 4.981433139801599630, 1.797578344525651906, -0.6930591852608753989 ) ) ;
#134901=CARTESIAN_POINT ( 'NONE',  ( 1.224644656679523713, 2.210950556192964989, 0.6053773189644614527 ) ) ;
#134906=CARTESIAN_POINT ( 'NONE',  ( 5.391355351084783365, -0.05288786341082692827, -2.220837934544753089 ) ) ;
#134912=CARTESIAN_POINT ( 'NONE',  ( 1.934220422044398813, -1.621183349045727473, -1.198859219795316955 ) ) ;
#134914=CARTESIAN_POINT ( 'NONE',  ( 1.217717225187223473, 0.4062273103370617755, -2.022011198395957887 ) ) ;
#134919=CARTESIAN_POINT ( 'NONE',  ( 3.837968455498752096, 2.180838135830205804, 0.2153102754597763235 ) ) ;
#134921=CARTESIAN_POINT ( 'NONE',  ( 0.8092204703840089053, 1.198858234535697065, -1.621184076614573533 ) ) ;
#134922=CARTESIAN_POINT ( 'NONE',  ( 0.8723036553972834950, -0.04505207493780280514, -1.840872848514919502 ) ) ;
#134923=CARTESIAN_POINT ( 'NONE',  ( 5.566080547264319556, -1.456586111465259403, 1.770153815000871989 ) ) ;
#134924=CARTESIAN_POINT ( 'NONE',  ( 3.257574473681293270, 0.8286728953739975756, 1.644182576024610265 ) ) ;
#134927=EDGE_CURVE ( 'NONE', #165662, #194636, #42354, .T. ) ;
#134928=CARTESIAN_POINT ( 'NONE',  ( 4.577060434696750946, -0.0006114206978560799951, -1.825762228460731551 ) ) ;
#134929=CARTESIAN_POINT ( 'NONE',  ( 4.641250102003463773, 0.7743139518727223392, 1.862017545363145565 ) ) ;
#134931=CARTESIAN_POINT ( 'NONE',  ( 4.487383681424582882, 2.022794180288649990, -1.013680454646571638 ) ) ;
#134933=CARTESIAN_POINT ( 'NONE',  ( 6.106491565043327796, -0.7546634490227432934, -1.966289716088761796 ) ) ;
#134934=CARTESIAN_POINT ( 'NONE',  ( 3.104029480343179603, 0.7476448069429382226, -1.930825944200013966 ) ) ;
#134939=CARTESIAN_POINT ( 'NONE',  ( 1.980962579895541920, -0.09440724433935901438, -1.924309447538669060 ) ) ;
#134941=CARTESIAN_POINT ( 'NONE',  ( 0.3265233526151562482, -1.289390354768883862, 1.488895225407897538 ) ) ;
#134946=CARTESIAN_POINT ( 'NONE',  ( 1.213460986420217047, 1.812193587075833667, -1.284517086575332367 ) ) ;
#134947=CARTESIAN_POINT ( 'NONE',  ( 3.751088088702017487, -1.722778774704723181, 1.210957861328536112 ) ) ;
#134950=CARTESIAN_POINT ( 'NONE',  ( 1.082201983675265655, 1.112762242526295298, -1.491567265455741476 ) ) ;
#134955=CARTESIAN_POINT ( 'NONE',  ( 1.160570123509139906, 2.118417766304943495, 0.09849428607798524360 ) ) ;
#134958=CARTESIAN_POINT ( 'NONE',  ( 4.615648854252428102, 0.4318217149890530848, -1.913582009320368371 ) ) ;
#134959=CARTESIAN_POINT ( 'NONE',  ( 3.520547545725543515, 1.372905562624787024, -1.669742455111824286 ) ) ;
#134960=CARTESIAN_POINT ( 'NONE',  ( 2.085277916773973228, -0.7859315772556186852, 1.665205719185464561 ) ) ;
#134963=CARTESIAN_POINT ( 'NONE',  ( 5.191228607790203675, -0.6215644750859107281, 1.625735776773645780 ) ) ;
#134967=CARTESIAN_POINT ( 'NONE',  ( 1.587033755777764510, -0.3173376132806354222, -2.138153673666403964 ) ) ;
#134969=CARTESIAN_POINT ( 'NONE',  ( 3.444685325028495004, 1.276847194542466646, 1.560261755768836744 ) ) ;
#134971=CARTESIAN_POINT ( 'NONE',  ( 1.534274790466340299, 1.065227450066742687, -1.880959520452238465 ) ) ;
#134972=CARTESIAN_POINT ( 'NONE',  ( 3.116049734078304212, -0.9705229388551097625, -1.715950581178276479 ) ) ;
#134973=CARTESIAN_POINT ( 'NONE',  ( 6.609000000000012420, 4.697979799133416456, 2.462673521647487540 ) ) ;
#134974=CARTESIAN_POINT ( 'NONE',  ( 3.755361975916061024, 1.927010760186953497, -0.2409419434407939486 ) ) ;
#134983=CARTESIAN_POINT ( 'NONE',  ( 6.686558038528344738, -2.261219263861591333, -0.4595595737692282912 ) ) ;
#134986=CARTESIAN_POINT ( 'NONE',  ( 4.258614474744500278, -0.6113484564182982695, -1.864166799412938502 ) ) ;
#134988=CARTESIAN_POINT ( 'NONE',  ( 2.145157927413956944, 0.8647252629472859109, 1.821741647932619390 ) ) ;
#134990=CARTESIAN_POINT ( 'NONE',  ( 3.204427616716760685, 1.339657272674670718, -1.639694800048612899 ) ) ;
#134992=CARTESIAN_POINT ( 'NONE',  ( 0.07459516483345349225, 1.413926688351078154, -2.016100038618890089 ) ) ;
#134994=CARTESIAN_POINT ( 'NONE',  ( 3.415785861374909249, 1.167101634185686576, -1.423959568491977912 ) ) ;
#134998=CARTESIAN_POINT ( 'NONE',  ( 5.168275554957600271, 2.118074532352266282, -0.1063875075708180934 ) ) ;
#135000=CARTESIAN_POINT ( 'NONE',  ( 5.448532837019475217, 0.5942636223626071024, 1.973259177745954718 ) ) ;
#135001=CARTESIAN_POINT ( 'NONE',  ( 0.4142149233586078227, 0.7067589711089922178, 1.721844540100337717 ) ) ;
#135002=CARTESIAN_POINT ( 'NONE',  ( 2.964219115174483665, -1.702287218311925310, -0.7022057971969236645 ) ) ;
#135007=CARTESIAN_POINT ( 'NONE',  ( 2.139570144280181108, -1.970530345926827742, 0.9937953903183869286 ) ) ;
#135008=CARTESIAN_POINT ( 'NONE',  ( 5.202513629402051976, -0.7552652112401860851, -2.132769717564055867 ) ) ;
#135010=CARTESIAN_POINT ( 'NONE',  ( 4.570457401048643398, 0.6997940171077315918, 1.671178544893426654 ) ) ;
#135011=CARTESIAN_POINT ( 'NONE',  ( 4.241352010100610137, 0.4139369872660918492, -1.870304626840668893 ) ) ;
#135014=CARTESIAN_POINT ( 'NONE',  ( 3.450034532000289200, 1.971640592831106709, 0.001386944525654659321 ) ) ;
#135015=CARTESIAN_POINT ( 'NONE',  ( 4.698043743269282757, -1.870269067358639958, -0.04562963166049315705 ) ) ;
#135016=CARTESIAN_POINT ( 'NONE',  ( 5.125394178454842020, 0.1826033194989445385, -1.852086804783218188 ) ) ;
#135018=CARTESIAN_POINT ( 'NONE',  ( 0.3742329010679063539, -2.001858617179689492, -0.2420261300371470137 ) ) ;
#135020=CARTESIAN_POINT ( 'NONE',  ( 1.664816323125760889, -1.488367931135538891, 1.490329786196037398 ) ) ;
#135024=CARTESIAN_POINT ( 'NONE',  ( 3.586284538990120119, 1.181046903802231984, 1.761068336431830472 ) ) ;
#135026=CARTESIAN_POINT ( 'NONE',  ( 1.863541707127059688, -1.624685865379692506, -1.199789887509305597 ) ) ;
#135032=CARTESIAN_POINT ( 'NONE',  ( 2.653791512158054200, 0.5793167894731532375, -2.082426382048585101 ) ) ;
#135033=CARTESIAN_POINT ( 'NONE',  ( 6.890000000000010338, 4.693995042360769254, 2.562605081426703180 ) ) ;
#135041=CARTESIAN_POINT ( 'NONE',  ( 0.7322823680011962821, 2.160084099745246178, 0.3691886501416344335 ) ) ;
#135043=CARTESIAN_POINT ( 'NONE',  ( 1.569569324160888124, 0.1651462269399027738, -2.256556122256009100 ) ) ;
#135050=CARTESIAN_POINT ( 'NONE',  ( 4.002375702155434922, -0.5437682074083802775, -1.636994321040524447 ) ) ;
#135052=CARTESIAN_POINT ( 'NONE',  ( 1.528175773270981308, 1.703719318302211683, 0.4785495757857262666 ) ) ;
#135054=CARTESIAN_POINT ( 'NONE',  ( 2.930340344496225935, -0.9942814366015439997, -1.750357268347104256 ) ) ;
#135056=CARTESIAN_POINT ( 'NONE',  ( 5.297975422827020608, -0.7987165953184969247, 2.057335881587420534 ) ) ;
#135058=CARTESIAN_POINT ( 'NONE',  ( 4.060810560252373413, 0.5428485958907465214, 1.945370397410832730 ) ) ;
#135060=CARTESIAN_POINT ( 'NONE',  ( 4.095327490859664188, -0.3419149367107060522, 1.987051255384481463 ) ) ;
#135062=CARTESIAN_POINT ( 'NONE',  ( 3.063207453921251489, 0.2760179531714930246, -1.850060308400132358 ) ) ;
#135065=CARTESIAN_POINT ( 'NONE',  ( 1.529408426332915960, -0.2309274165002393187, 1.898302859121250297 ) ) ;
#135070=CARTESIAN_POINT ( 'NONE',  ( -0.1757481403069499348, -0.8193859263425256056, -1.726394157293545062 ) ) ;
#135072=CARTESIAN_POINT ( 'NONE',  ( 1.715213470010600538, -1.680963409367957295, -1.011360081469035999 ) ) ;
#135075=CARTESIAN_POINT ( 'NONE',  ( 5.220985865760717992, 1.604251394084664550, -1.386888226476624242 ) ) ;
#135078=CARTESIAN_POINT ( 'NONE',  ( 5.923112194766430250, -0.05102361969991364710, 1.970867320657720301 ) ) ;
#135080=CARTESIAN_POINT ( 'NONE',  ( 1.002198536899261860, -0.9015652438304004868, 1.800089726458251826 ) ) ;
#135082=CARTESIAN_POINT ( 'NONE',  ( 1.195080948601736859, 1.869106744463861158, 0.9945057017613133654 ) ) ;
#135084=CARTESIAN_POINT ( 'NONE',  ( 2.928250347896840022, 1.105370970781336837, 1.750397071514836478 ) ) ;
#135088=CARTESIAN_POINT ( 'NONE',  ( 4.488279598995706721, -0.4578276946864130448, -2.039718000080573912 ) ) ;
#135090=CARTESIAN_POINT ( 'NONE',  ( 2.713660727937649231, -1.805999004224107418, 0.2657717501357085843 ) ) ;
#135091=CARTESIAN_POINT ( 'NONE',  ( 1.365539917532717196, 0.5261944252722695614, -1.733370571883424693 ) ) ;
#135096=CARTESIAN_POINT ( 'NONE',  ( 5.649526978565787338, -1.736373965863503122, -1.361823127433124725 ) ) ;
#135099=CARTESIAN_POINT ( 'NONE',  ( 4.107995242876061326, -0.7289348763114507079, 1.768098669557085056 ) ) ;
#135102=CARTESIAN_POINT ( 'NONE',  ( 6.144996677366851401, -0.2998803957653916052, -2.048400609436632269 ) ) ;
#135110=CARTESIAN_POINT ( 'NONE',  ( 3.251090012001829788, -1.527204365403836306, -1.079795099579644591 ) ) ;
#135116=CARTESIAN_POINT ( 'NONE',  ( 6.825056245572477032, -1.890314563506745316, -0.8446596084958692963 ) ) ;
#135117=CARTESIAN_POINT ( 'NONE',  ( 1.036732716359071604, -1.587823911754655315, 1.242746109592095527 ) ) ;
#135121=CARTESIAN_POINT ( 'NONE',  ( 0.9377431681640016059, 0.8850447378907433382, -2.004962588275795543 ) ) ;
#135122=CARTESIAN_POINT ( 'NONE',  ( 6.287720257080702702, 1.262826302610157381, 1.318732360701305062 ) ) ;
#135129=CARTESIAN_POINT ( 'NONE',  ( 4.247483403459266782, 1.840758003770435414, -0.04960325993209198370 ) ) ;
#135130=CARTESIAN_POINT ( 'NONE',  ( 0.1178376421791422907, -0.5346926475991298222, 1.940734443874014836 ) ) ;
#135131=CARTESIAN_POINT ( 'NONE',  ( 2.355183240404590705, -0.9839461204387394133, 2.077256468512170162 ) ) ;
#135133=CARTESIAN_POINT ( 'NONE',  ( 0.6372766190945264864, 1.739209566756502845, -0.6625725129940361890 ) ) ;
#135137=CARTESIAN_POINT ( 'NONE',  ( 4.289254230599209627, -0.005406649120142519548, -1.912571728590661380 ) ) ;
#135141=CARTESIAN_POINT ( 'NONE',  ( 3.368770691598612643, 0.04892471221396628434, -2.090337739860036681 ) ) ;
#135142=CARTESIAN_POINT ( 'NONE',  ( 1.779943879855113709, -1.003247456797161652, 1.578688272967261996 ) ) ;
#135145=CARTESIAN_POINT ( 'NONE',  ( 3.667295640872432649, 0.9703414817801876424, 1.444613691174992720 ) ) ;
#135149=CARTESIAN_POINT ( 'NONE',  ( 3.791373243616827704, 1.250846937323921715, 1.187934608979845708 ) ) ;
#135151=CARTESIAN_POINT ( 'NONE',  ( 3.544632465004614374, -1.790652189326558563, 1.263247045326252094 ) ) ;
#135152=CARTESIAN_POINT ( 'NONE',  ( 6.217417563691929772, -0.2743312036321900460, 2.189694890431858276 ) ) ;
#135154=CARTESIAN_POINT ( 'NONE',  ( 4.030270078087188068, 1.201442806954319487, 1.808153907555063000 ) ) ;
#135155=CARTESIAN_POINT ( 'NONE',  ( 1.892912435568369744, 1.589020553905008626, -0.8988452475950716725 ) ) ;
#135156=CARTESIAN_POINT ( 'NONE',  ( 4.927025384238821637, -1.814351377589568548, 1.091279385997992568 ) ) ;
#135158=CARTESIAN_POINT ( 'NONE',  ( 5.003627799853592073, -2.281530862488420297, 0.2229171871234881530 ) ) ;
#135160=CARTESIAN_POINT ( 'NONE',  ( 6.720655732516649827, 2.453385726714229609, 2.309856631140958960 ) ) ;
#135164=CARTESIAN_POINT ( 'NONE',  ( 1.102369588802411426, -0.9501182663193027400, 1.895776817140030213 ) ) ;
#135170=CARTESIAN_POINT ( 'NONE',  ( 6.883263157960364254, 2.038911835798001171, 2.358809022084580764 ) ) ;
#135173=CARTESIAN_POINT ( 'NONE',  ( 6.188124994278807023, 1.678003296889327034, 1.117835524071027598 ) ) ;
#135175=CARTESIAN_POINT ( 'NONE',  ( 4.873915701820059176, -2.023805994998853830, 0.3972042427494940076 ) ) ;
#135181=CARTESIAN_POINT ( 'NONE',  ( 0.3926704732973253509, 1.736993494895492152, -1.163127744158433119 ) ) ;
#135182=CARTESIAN_POINT ( 'NONE',  ( 4.570935502227962743, -0.9480417383296577682, 1.779625852769652905 ) ) ;
#135183=CARTESIAN_POINT ( 'NONE',  ( 4.704558828624370470, 1.604442792107749760, 0.9031527321438773681 ) ) ;
#135186=CARTESIAN_POINT ( 'NONE',  ( 0.2875850076352819973, -0.8198804995633873771, 1.517450437728053325 ) ) ;
#135187=CARTESIAN_POINT ( 'NONE',  ( 0.2863426850727782136, -0.6839425765656822476, -1.897108587135355684 ) ) ;
#135188=CARTESIAN_POINT ( 'NONE',  ( 0.9679111143040418641, -2.244285626452859450, -0.4966636800145701747 ) ) ;
#135190=CARTESIAN_POINT ( 'NONE',  ( 0.8962371694669484246, -0.8134219682564158838, 2.111273946446708738 ) ) ;
#135191=CARTESIAN_POINT ( 'NONE',  ( 3.158910222468692908, -1.594458197781272846, 1.376041720736504992 ) ) ;
#135195=FILL_AREA_STYLE ('',( #69075 ) ) ;
#135200=CARTESIAN_POINT ( 'NONE',  ( 4.764059104694277735, 0.6956466834483631123, -2.109775416031458128 ) ) ;
#135201=CARTESIAN_POINT ( 'NONE',  ( 1.957222284144799929, 0.3726435881295562247, -2.159377063894574622 ) ) ;
#135204=CARTESIAN_POINT ( 'NONE',  ( 5.055110333045015558, 1.632132345252810035, -1.088295032039228172 ) ) ;
#135207=CARTESIAN_POINT ( 'NONE',  ( 6.889999999999970370, 7.053389210336755255, 2.318152334880723142 ) ) ;
#135210=CARTESIAN_POINT ( 'NONE',  ( 4.254221937059123881, 0.9039275175388861161, -1.918405034562712830 ) ) ;
#135216=CARTESIAN_POINT ( 'NONE',  ( 5.020983453748395497, -1.746657797055195305, 0.5827527221545365510 ) ) ;
#135221=CARTESIAN_POINT ( 'NONE',  ( 0.8018505195637380956, 1.319035621562004934, -1.135522575981460003 ) ) ;
#135225=CARTESIAN_POINT ( 'NONE',  ( 5.225516498768126183, -2.053876642077703707, 0.6744380372525200507 ) ) ;
#135228=CARTESIAN_POINT ( 'NONE',  ( 5.014612968065254250, 1.493337269798940881, -1.563205770552501761 ) ) ;
#135230=CARTESIAN_POINT ( 'NONE',  ( 5.395764264914824970, -0.7120431519804657494, 1.838431125455505688 ) ) ;
#135231=CARTESIAN_POINT ( 'NONE',  ( 4.235468066436924417, -1.617573843961607416, -0.6246848730444684028 ) ) ;
#135232=CARTESIAN_POINT ( 'NONE',  ( 1.347511689332027807, 0.6317163119916607839, -2.098556723903362009 ) ) ;
#135233=CARTESIAN_POINT ( 'NONE',  ( 2.257223126251302947, -1.783628160338263768, 1.464130300071916135 ) ) ;
#135234=CARTESIAN_POINT ( 'NONE',  ( 4.411438286107774331, -0.3560947707623678959, 2.029623144953551339 ) ) ;
#135235=CARTESIAN_POINT ( 'NONE',  ( 6.356980358691139088, 0.3275572002108660952, -1.914087848568704731 ) ) ;
#135239=CARTESIAN_POINT ( 'NONE',  ( 1.037732671793228700, -1.587836052788630603, 1.242728777923551409 ) ) ;
#135241=CARTESIAN_POINT ( 'NONE',  ( 3.276612781706738087, -1.315965827422488132, 1.771305981150771647 ) ) ;
#135243=CARTESIAN_POINT ( 'NONE',  ( 0.4614603993745093891, -0.5041695895235782654, 1.791261842318598863 ) ) ;
#135249=CARTESIAN_POINT ( 'NONE',  ( 6.825078400183511640, 3.690008145721306310, 2.558400262806997283 ) ) ;
#135250=CARTESIAN_POINT ( 'NONE',  ( 6.316338248019476964, 1.719745045379994064, 0.6579504788090040357 ) ) ;
#135252=CARTESIAN_POINT ( 'NONE',  ( 3.116143102785688068, -1.014332071340098285, -1.793896330205650980 ) ) ;
#135255=CARTESIAN_POINT ( 'NONE',  ( 1.998700280430569576, -1.981126291604264233, -0.3917822458236255301 ) ) ;
#135258=CARTESIAN_POINT ( 'NONE',  ( 2.272404554480491168, -1.268947053487592846, 1.623793324639089874 ) ) ;
#135264=CARTESIAN_POINT ( 'NONE',  ( 6.059228469117068805, -1.890744221452178353, -1.137928576693452820 ) ) ;
#135265=CARTESIAN_POINT ( 'NONE',  ( 1.634274655659254005, 1.066924998833935989, -1.879885089102695250 ) ) ;
#135267=CARTESIAN_POINT ( 'NONE',  ( 0.4797043241997685503, -0.7212876333932433104, 1.883314553594167107 ) ) ;
#135271=CARTESIAN_POINT ( 'NONE',  ( 1.692057038649401601, -1.861345348035767344, -0.1864469194169729449 ) ) ;
#135272=CARTESIAN_POINT ( 'NONE',  ( 3.925017756809038527, -1.752140073516525565, 0.9981236898717813499 ) ) ;
#135277=CARTESIAN_POINT ( 'NONE',  ( 5.215496775961459441, -0.3099510095366068696, 2.083004237123146307 ) ) ;
#135281=CARTESIAN_POINT ( 'NONE',  ( 5.484630696634174463, -1.278254659592213516, 1.563874148425943078 ) ) ;
#135283=CARTESIAN_POINT ( 'NONE',  ( 0.7782751772977951621, -1.100228457372550261, -1.744432094316533677 ) ) ;
#135291=CARTESIAN_POINT ( 'NONE',  ( 3.473242058572806990, 1.961495611989271248, 0.9311941066344242568 ) ) ;
#135293=CARTESIAN_POINT ( 'NONE',  ( 1.346931166825489967, 0.5339940059071214273, -1.762130705996706181 ) ) ;
#135296=CARTESIAN_POINT ( 'NONE',  ( 4.704715985517350596, 1.906866092115505840, 1.080010033982371498 ) ) ;
#135297=CARTESIAN_POINT ( 'NONE',  ( 6.983263157960370116, 1.251666756963093041, 2.167287073222202931 ) ) ;
#135298=CARTESIAN_POINT ( 'NONE',  ( 4.786124093267453361, -1.070777880904892232, 1.993102913963458400 ) ) ;
#135306=CARTESIAN_POINT ( 'NONE',  ( 5.764868906847371299, -1.600580677892119441, -0.7553990054774415430 ) ) ;
#135309=CARTESIAN_POINT ( 'NONE',  ( 2.239418434904976607, -1.881632620311970649, 0.9459126739295388164 ) ) ;
#135312=CARTESIAN_POINT ( 'NONE',  ( 1.767950473188628857, -1.955055593144053194, 0.2378005183036585035 ) ) ;
#135313=CARTESIAN_POINT ( 'NONE',  ( 1.059204734455133412, 0.3686402435371800013, -1.833797362824276078 ) ) ;
#135314=CARTESIAN_POINT ( 'NONE',  ( 1.433958818539453395, 1.165882187713672247, 1.577721859592796205 ) ) ;
#135315=CARTESIAN_POINT ( 'NONE',  ( 5.467019156909919353, -1.422831870918849217, 1.121200454338074692 ) ) ;
#135319=CARTESIAN_POINT ( 'NONE',  ( 6.104356062600288624, -0.6750377415852754082, -1.744797942764392706 ) ) ;
#135321=CARTESIAN_POINT ( 'NONE',  ( 5.629760504653214426, 1.996728726787128538, -0.5467053113129491937 ) ) ;
#135332=CARTESIAN_POINT ( 'NONE',  ( 4.984793487045196869, 1.876812866478014596, 0.5713181500588762063 ) ) ;
#135334=CARTESIAN_POINT ( 'NONE',  ( 3.216172551982798833, -1.646586737935524125, -1.163091166099708529 ) ) ;
#135335=CARTESIAN_POINT ( 'NONE',  ( 2.325271742496349159, -1.422496398144998508, -1.283381434195222326 ) ) ;
#135337=CARTESIAN_POINT ( 'NONE',  ( 0.5038066827526346270, -2.180447833630628107, 0.2205874978757973448 ) ) ;
#135338=CARTESIAN_POINT ( 'NONE',  ( 0.2333690889706925564, 0.2409277441041447754, -2.087868073146467829 ) ) ;
#135339=CARTESIAN_POINT ( 'NONE',  ( 2.776451973220807279, -1.788819259240326698, -0.5467896145717602296 ) ) ;
#135341=CARTESIAN_POINT ( 'NONE',  ( 3.955341514648374357, -1.749461739742008470, 0.9961098753780948112 ) ) ;
#135344=CARTESIAN_POINT ( 'NONE',  ( 4.517270869736185190, -1.935087425045402654, 0.8595401143802297028 ) ) ;
#135346=CARTESIAN_POINT ( 'NONE',  ( 5.512195382060368409, 2.068158883198469855, -0.09793725168850964113 ) ) ;
#135347=CARTESIAN_POINT ( 'NONE',  ( 1.382492367555522295, -0.3100735531622924035, -2.067509394536557021 ) ) ;
#135348=CARTESIAN_POINT ( 'NONE',  ( 6.620655732516647518, 3.684600858287550906, 2.687722323901103660 ) ) ;
#135349=CARTESIAN_POINT ( 'NONE',  ( 6.528339890195161921, 1.048227956652090231, -1.494441373796271622 ) ) ;
#135350=ORIENTED_EDGE ( 'NONE', *, *, #175445, .F. ) ;
#135356=CARTESIAN_POINT ( 'NONE',  ( 0.6975727754284127835, 1.215713746931287753, 1.343078931132860587 ) ) ;
#135365=CARTESIAN_POINT ( 'NONE',  ( 5.958611281643053204, -1.915606116362132072, -0.6298603123368745615 ) ) ;
#135366=CARTESIAN_POINT ( 'NONE',  ( 0.5398874254142792539, -2.012210497580559476, 0.6691108114003360141 ) ) ;
#135368=FACE_OUTER_BOUND ( 'NONE', #178712, .T. ) ;
#135372=CARTESIAN_POINT ( 'NONE',  ( 3.362113288959746704, -1.967404159762261795, 0.09189030742163574461 ) ) ;
#135373=CARTESIAN_POINT ( 'NONE',  ( 4.692982559244565088, 1.755779632255444422, 0.9913831279167032440 ) ) ;
#135376=CARTESIAN_POINT ( 'NONE',  ( 4.330150130892728377, 2.148942519667027984, 0.4286813238914553570 ) ) ;
#135378=CARTESIAN_POINT ( 'NONE',  ( 4.805647293689061961, -0.5139743781695116365, 1.856484447351488765 ) ) ;
#135380=CARTESIAN_POINT ( 'NONE',  ( -0.1294898018151837138, 2.036186877494918335, -2.343407025977122693 ) ) ;
#135383=CARTESIAN_POINT ( 'NONE',  ( 5.576995328841173105, 1.818227641914264225, 0.7572995901278417596 ) ) ;
#135384=CARTESIAN_POINT ( 'NONE',  ( 0.6088030852571654217, -0.2837962540496056785, 1.921085339388538982 ) ) ;
#135385=CARTESIAN_POINT ( 'NONE',  ( 4.565094110769337910, -1.615551665759178412, 1.200850101804177283 ) ) ;
#135386=CARTESIAN_POINT ( 'NONE',  ( 5.975955848901470802, 2.022625890308630048, 1.091648031176053468 ) ) ;
#135388=CARTESIAN_POINT ( 'NONE',  ( 4.293699386915854177, -1.280875055806574236, -1.350249269484518955 ) ) ;
#135393=CARTESIAN_POINT ( 'NONE',  ( 0.6268464039562298140, 0.1668571106153530770, 2.185281662807083691 ) ) ;
#135397=CARTESIAN_POINT ( 'NONE',  ( 0.7502976729042536430, 0.5272139720400963459, 1.747899773703022408 ) ) ;
#135399=CARTESIAN_POINT ( 'NONE',  ( 2.619397310362530096, 0.2141275842034353338, 1.720801833696316008 ) ) ;
#135403=CARTESIAN_POINT ( 'NONE',  ( 5.057177669875371429, -1.544152220135000420, -0.9737345633797565014 ) ) ;
#135404=CARTESIAN_POINT ( 'NONE',  ( 3.291801117278610800, -1.314073873198824627, -1.456807609480186061 ) ) ;
#135409=CARTESIAN_POINT ( 'NONE',  ( 4.705793326368500118, 1.571798730262342181, 1.423547657546264000 ) ) ;
#135413=CARTESIAN_POINT ( 'NONE',  ( 2.747004861044194612, -0.3495022371792326221, -2.040372298647576965 ) ) ;
#135416=CARTESIAN_POINT ( 'NONE',  ( 4.582826572872266802, -1.451171176318547529, 1.681852496032259614 ) ) ;
#135418=CARTESIAN_POINT ( 'NONE',  ( 3.463815647965732936, -2.215898795117266840, -0.6112515151598179042 ) ) ;
#135424=CARTESIAN_POINT ( 'NONE',  ( 3.058751851047710080, 0.4689117840017149041, 1.853869267190631831 ) ) ;
#135426=CARTESIAN_POINT ( 'NONE',  ( 4.348488605181799471, 0.4613061074445113374, 1.661866727659202736 ) ) ;
#135427=CARTESIAN_POINT ( 'NONE',  ( 3.731657894805060938, 0.6748485617756972976, -1.900415309456899182 ) ) ;
#135428=CARTESIAN_POINT ( 'NONE',  ( 3.991116696687820209, -2.292486273863734603, 0.1698809440028921647 ) ) ;
#135430=CARTESIAN_POINT ( 'NONE',  ( 6.111965604441711442, -2.090389680133018846, 0.2559737671669787273 ) ) ;
#135433=CARTESIAN_POINT ( 'NONE',  ( 4.745210919507984570, -1.367539302148174318, -1.123239564495488674 ) ) ;
#135435=CARTESIAN_POINT ( 'NONE',  ( 0.5863596474044476814, -2.275655805637688989, -0.2749888630660061728 ) ) ;
#135436=CARTESIAN_POINT ( 'NONE',  ( 0.3920123891120600446, 1.449622948667350641, -0.9626461102210502885 ) ) ;
#135439=CARTESIAN_POINT ( 'NONE',  ( 6.456982561897790518, 0.3786298020890948024, -2.158335565738931816 ) ) ;
#135443=CARTESIAN_POINT ( 'NONE',  ( 0.2917819264270337110, -1.984717812412156501, 0.8806528889930710369 ) ) ;
#135444=CARTESIAN_POINT ( 'NONE',  ( 0.9894706735516716201, -0.4852629857438545691, 1.957171443305204761 ) ) ;
#135446=CARTESIAN_POINT ( 'NONE',  ( 5.883413297016587329, 1.779079706761811153, -0.7395700111451685155 ) ) ;
#135448=CARTESIAN_POINT ( 'NONE',  ( 1.055278351191447639, 0.4402236684300055991, 2.177206957374391738 ) ) ;
#135457=CARTESIAN_POINT ( 'NONE',  ( 3.895860127252141591, -0.5505607855701463160, -1.651121638195630181 ) ) ;
#135458=CARTESIAN_POINT ( 'NONE',  ( 1.961309178647975715, 1.629323162926434199, 1.092499269706406650 ) ) ;
#135463=CARTESIAN_POINT ( 'NONE',  ( 6.338335788673861160, -1.050647824335379399, 1.656640365463659670 ) ) ;
#135466=CARTESIAN_POINT ( 'NONE',  ( 1.393865445735403830, 1.714438158727617179, 1.476448846179352348 ) ) ;
#135471=CARTESIAN_POINT ( 'NONE',  ( 1.616246341788161622, 1.260175398906153266, -1.382505567627971388 ) ) ;
#135472=CARTESIAN_POINT ( 'NONE',  ( 0.7735316488602840268, 1.530413877909537979, -0.8155550471512038602 ) ) ;
#135473=CARTESIAN_POINT ( 'NONE',  ( 3.948915171154475878, -1.822730400009948237, -1.216494452853926322 ) ) ;
#135474=CARTESIAN_POINT ( 'NONE',  ( 5.069473898719869531, 0.2322026582469650102, -2.295885384840197663 ) ) ;
#135475=CARTESIAN_POINT ( 'NONE',  ( 1.200152769736504421, -2.061077815970461025, -0.0008511993763692102862 ) ) ;
#135476=CARTESIAN_POINT ( 'NONE',  ( 3.609261671491706736, -1.913043583297647565, 0.3329670706836064809 ) ) ;
#135478=CARTESIAN_POINT ( 'NONE',  ( 5.571519856497625156, 1.802974293077023393, -0.4980454429602265698 ) ) ;
#135480=CARTESIAN_POINT ( 'NONE',  ( 0.2097273702015931829, -1.334265282896981208, -1.107180986369905362 ) ) ;
#135483=CARTESIAN_POINT ( 'NONE',  ( 4.641250102003463773, 0.7743139518727223392, 1.862017545363145565 ) ) ;
#135486=CARTESIAN_POINT ( 'NONE',  ( 1.681982107312831154, -0.9779208310041755947, 1.541497997293653555 ) ) ;
#135495=CARTESIAN_POINT ( 'NONE',  ( 5.848308768596990781, 0.9934667122631580805, -1.758341319078795761 ) ) ;
#135496=CARTESIAN_POINT ( 'NONE',  ( 6.375645204974608404, 0.3829637424261604361, -2.187886986038441339 ) ) ;
#135500=CARTESIAN_POINT ( 'NONE',  ( 5.717669251203768788, -2.011168408518650974, 0.4492202366306179417 ) ) ;
#135501=CARTESIAN_POINT ( 'NONE',  ( 4.658827374183164949, 1.163267680695537099, 1.646840100852072997 ) ) ;
#135509=CARTESIAN_POINT ( 'NONE',  ( 5.536482449520531368, 1.943773098233076757, -0.5350085594507182352 ) ) ;
#135510=CARTESIAN_POINT ( 'NONE',  ( 3.784953330938052751, 1.334695924059103644, 1.268461399425282687 ) ) ;
#135512=CARTESIAN_POINT ( 'NONE',  ( -0.02338929933909470252, 2.896474228846234844, -2.200133910884606081 ) ) ;
#135513=CARTESIAN_POINT ( 'NONE',  ( 1.665117554179825321, -1.629454703905337087, 1.634364892973801719 ) ) ;
#135515=CARTESIAN_POINT ( 'NONE',  ( 4.534552404040613105, 2.118918870418550870, 0.4265773709258223190 ) ) ;
#135517=CARTESIAN_POINT ( 'NONE',  ( 0.01113493735188827126, -1.904398801838134148, 0.3797647843634504583 ) ) ;
#135518=CARTESIAN_POINT ( 'NONE',  ( 2.694546298722868549, 1.457235452327232395, -1.394086077981852911 ) ) ;
#135520=CARTESIAN_POINT ( 'NONE',  ( 3.849189735728062001, -1.136876111170448178, 1.997481460179703960 ) ) ;
#135522=CARTESIAN_POINT ( 'NONE',  ( 3.080767038946086611, -0.1360980058115155988, -1.865751385159146070 ) ) ;
#135523=CARTESIAN_POINT ( 'NONE',  ( 6.385619905723967094, 1.359199996644964381, 1.428251207276862500 ) ) ;
#135526=CARTESIAN_POINT ( 'NONE',  ( 1.471597369358583318, 0.1596246592955492538, -2.201166978212334424 ) ) ;
#135532=CARTESIAN_POINT ( 'NONE',  ( 0.8253839628637716919, -1.873344321310044469, 0.6141440057798281948 ) ) ;
#135533=CARTESIAN_POINT ( 'NONE',  ( 0.3941752559601471306, 1.712991706939146486, 1.546321376980333007 ) ) ;
#135534=CARTESIAN_POINT ( 'NONE',  ( 0.4319881149899909567, 1.126445828788334991, 1.606065282034954578 ) ) ;
#135535=CARTESIAN_POINT ( 'NONE',  ( 4.381722380181817478, -1.975297276180818296, 0.5937428812356324581 ) ) ;
#135538=ORIENTED_EDGE ( 'NONE', *, *, #185885, .F. ) ;
#135543=CARTESIAN_POINT ( 'NONE',  ( 6.672352044927558623, -1.017530931492259816, -1.917974758356699505 ) ) ;
#135545=CARTESIAN_POINT ( 'NONE',  ( 5.249485218566787736, 1.838879873951341004, -0.09611505855997715120 ) ) ;
#135554=CARTESIAN_POINT ( 'NONE',  ( 0.8383554657987003500, 1.138622818284718008, -1.536203910471350298 ) ) ;
#135555=CARTESIAN_POINT ( 'NONE',  ( 1.867668082833298993, 0.9064309091474114233, 1.519949287764200685 ) ) ;
#135556=CARTESIAN_POINT ( 'NONE',  ( 5.901044691261273734, -0.2977458250903759485, -1.990848032377992016 ) ) ;
#135558=CARTESIAN_POINT ( 'NONE',  ( 4.481992950489037675, -1.915292616430896544, -0.04288535553729002497 ) ) ;
#135560=CARTESIAN_POINT ( 'NONE',  ( 5.142998410927586583, -0.2390059684120172390, -1.954905448695958059 ) ) ;
#135561=CARTESIAN_POINT ( 'NONE',  ( -0.1753031400193918732, -0.9122597987226389593, -1.912455998546586544 ) ) ;
#135563=CARTESIAN_POINT ( 'NONE',  ( 3.783945140921864070, -0.9226758061156097313, 1.627204332209288395 ) ) ;
#135564=CARTESIAN_POINT ( 'NONE',  ( 5.742733201377892449, 0.3429454505429993527, 1.690258806964558547 ) ) ;
#135566=CARTESIAN_POINT ( 'NONE',  ( 3.756632125300945368, 0.7937082651479386852, 2.059386989456575279 ) ) ;
#135569=CARTESIAN_POINT ( 'NONE',  ( 0.9595213787957155294, 1.685235279958563037, 1.189114231603551675 ) ) ;
#135578=CARTESIAN_POINT ( 'NONE',  ( 3.473154722801426786, 1.870513717286937494, 0.8877811045280564750 ) ) ;
#135582=CARTESIAN_POINT ( 'NONE',  ( 0.7858139957730024827, 1.945786914974199089, -0.5409757216557200543 ) ) ;
#135585=CARTESIAN_POINT ( 'NONE',  ( 0.07479286986305369589, 0.004866263145587855152, -1.855573292446037970 ) ) ;
#135587=CARTESIAN_POINT ( 'NONE',  ( 6.186875009713125984, -1.117664052418202658, -1.677746505241828334 ) ) ;
#135588=CARTESIAN_POINT ( 'NONE',  ( 5.999236059146234368, -0.2270968913323672123, 1.902120139356741069 ) ) ;
#135589=CARTESIAN_POINT ( 'NONE',  ( 6.539320575229239374, 3.684509595994990061, 2.717302710099603225 ) ) ;
#135590=CARTESIAN_POINT ( 'NONE',  ( 3.896163805485418852, -0.6886730243073329039, -2.080591098665984795 ) ) ;
#135592=CARTESIAN_POINT ( 'NONE',  ( 3.199369407753744454, 1.726971514772487559, -0.8218122705464236954 ) ) ;
#135596=CARTESIAN_POINT ( 'NONE',  ( 1.194935658704935566, 1.779638138761422628, 0.9480210990304924756 ) ) ;
#135598=CARTESIAN_POINT ( 'NONE',  ( 5.952700804540857149, -1.878875186057769486, -1.127905468421293689 ) ) ;
#135600=CARTESIAN_POINT ( 'NONE',  ( 2.572937677043420912, 0.08726698667262809683, -1.722694834735357894 ) ) ;
#135602=CARTESIAN_POINT ( 'NONE',  ( 0.1399997263885795762, 1.361443548867202979, -2.255028951473649901 ) ) ;
#135607=CARTESIAN_POINT ( 'NONE',  ( 1.697631272820496307, -1.418720726069604865, -1.355276769646639901 ) ) ;
#135610=CARTESIAN_POINT ( 'NONE',  ( 0.07536363704230969462, 1.333366039338843789, -2.397125032416930424 ) ) ;
#135614=CARTESIAN_POINT ( 'NONE',  ( 3.422321195131371674, -0.7368491698513750521, -1.655029553552778809 ) ) ;
#135618=CARTESIAN_POINT ( 'NONE',  ( 5.250580378299275708, 1.785639943600283219, 0.3038008075236381389 ) ) ;
#135622=CARTESIAN_POINT ( 'NONE',  ( 4.598021663640887269, 0.7965279161250311546, -1.682138884369558607 ) ) ;
#135624=CARTESIAN_POINT ( 'NONE',  ( 2.952642602588346321, -1.771063984568725935, -0.7304820402930515266 ) ) ;
#135631=CARTESIAN_POINT ( 'NONE',  ( 0.7257156204387126275, -2.052300050329861847, 0.6792298617422781737 ) ) ;
#135633=CARTESIAN_POINT ( 'NONE',  ( 2.009825619773229377, -0.9864030779522957593, -1.843301731911746399 ) ) ;
#135635=CARTESIAN_POINT ( 'NONE',  ( 0.6217474354073999621, -0.9722136304874777757, -1.544982199245432897 ) ) ;
#135637=CARTESIAN_POINT ( 'NONE',  ( 2.678497062878131274, -1.746332412481563345, -0.5319975912557314279 ) ) ;
#135639=CARTESIAN_POINT ( 'NONE',  ( 2.162237915172473546, 1.912057200688283665, 0.04323261116381121871 ) ) ;
#135640=CARTESIAN_POINT ( 'NONE',  ( 2.769919614283973264, -1.948520106842245525, 0.2860871629452500509 ) ) ;
#135641=CARTESIAN_POINT ( 'NONE',  ( 3.263160552478797882, 1.894124000634039851, -0.4281397233536556879 ) ) ;
#135644=CARTESIAN_POINT ( 'NONE',  ( 4.482752736079084421, -1.382999391253452615, 1.607682512923855445 ) ) ;
#135652=CARTESIAN_POINT ( 'NONE',  ( 4.283705427790140519, 1.194290084605063251, 1.380960126487425166 ) ) ;
#135658=CARTESIAN_POINT ( 'NONE',  ( 4.434354141042872399, 1.834536173243521917, 0.3649259964926266364 ) ) ;
#135661=CARTESIAN_POINT ( 'NONE',  ( 1.840333348128117885, 1.905464876828693921, 0.2831333259317326823 ) ) ;
#135669=CARTESIAN_POINT ( 'NONE',  ( 1.054496592829538004, -1.339774933521440392, 1.639435421165438500 ) ) ;
#135672=CARTESIAN_POINT ( 'NONE',  ( 6.209843387784004243, 0.6066176463192971546, -1.979359621541395331 ) ) ;
#135673=CARTESIAN_POINT ( 'NONE',  ( 0.8371598888798935656, 0.7463826720714299423, -1.683355135116317847 ) ) ;
#135675=CARTESIAN_POINT ( 'NONE',  ( 6.604150285194997139, -0.1511744057106997885, 2.264526297252217990 ) ) ;
#135679=CARTESIAN_POINT ( 'NONE',  ( 1.430038810223871026, 1.126473215625309887, -1.996311628086711254 ) ) ;
#135682=CARTESIAN_POINT ( 'NONE',  ( 6.439402819763696328, 0.7408549094962694204, -1.795268486070795477 ) ) ;
#135686=CARTESIAN_POINT ( 'NONE',  ( 0.5803383592409648850, 0.9960403410373251942, 1.749501224816521816 ) ) ;
#135691=CARTESIAN_POINT ( 'NONE',  ( 3.328152359787967640, 2.039751367458849884, 0.4576943786474896858 ) ) ;
#135692=CARTESIAN_POINT ( 'NONE',  ( 0.9711603072033472284, 1.707112214499702407, -0.4667758381974375648 ) ) ;
#135695=CARTESIAN_POINT ( 'NONE',  ( 4.207168913946373934, -0.3938425722496830539, 2.258028373892074558 ) ) ;
#135696=CARTESIAN_POINT ( 'NONE',  ( 3.099246252510225119, -1.738326302361908882, 0.08608614090572026811 ) ) ;
#135699=CARTESIAN_POINT ( 'NONE',  ( 3.602662725270942445, 0.7809228151291653930, -1.548105009325143833 ) ) ;
#135700=CARTESIAN_POINT ( 'NONE',  ( 3.402935010178400166, 0.5245792999575286109, 2.106750930608875194 ) ) ;
#135702=CARTESIAN_POINT ( 'NONE',  ( 5.050017674172561755, 0.9981218692422781924, 1.752141108012375437 ) ) ;
#135703=CARTESIAN_POINT ( 'NONE',  ( 3.062500000000001776, -1.451031289061242013, -1.451031289060994656 ) ) ;
#135705=CARTESIAN_POINT ( 'NONE',  ( 1.606340841434449329, -0.6908775452558654218, -1.798418176235560662 ) ) ;
#135707=CARTESIAN_POINT ( 'NONE',  ( 5.027667009318355973, -0.3252736580323810633, 2.197331836796195592 ) ) ;
#135709=CARTESIAN_POINT ( 'NONE',  ( -0.1110810684432986112, 0.7552414886912374170, -1.881935688996359213 ) ) ;
#135714=CARTESIAN_POINT ( 'NONE',  ( 0.2939904269894151323, 2.070328538627811632, -0.8053792395062376874 ) ) ;
#135715=CARTESIAN_POINT ( 'NONE',  ( 5.916451087343006954, 0.7937011933104149985, 1.794315766958521241 ) ) ;
#135718=CARTESIAN_POINT ( 'NONE',  ( 0.2984011986874868794, -2.161112683670802337, -0.05330630956579958390 ) ) ;
#135723=CARTESIAN_POINT ( 'NONE',  ( 3.209489602684848286, -1.684771875651757123, -1.189772946182314106 ) ) ;
#135726=EDGE_CURVE ( 'NONE', #21539, #21772, #10080, .T. ) ;
#135728=CARTESIAN_POINT ( 'NONE',  ( 6.239502018287079288, -1.354773164471131164, -1.289998633004642237 ) ) ;
#135729=CARTESIAN_POINT ( 'NONE',  ( 4.465268017702548775, -1.683484418668965921, -0.4155383358091616075 ) ) ;
#135730=CARTESIAN_POINT ( 'NONE',  ( 3.526658842500699720, -1.606625690567566656, 0.6697392890405767796 ) ) ;
#135731=CARTESIAN_POINT ( 'NONE',  ( 1.400361390298704656, -0.8304178796270310636, -2.136844513788013433 ) ) ;
#135733=CARTESIAN_POINT ( 'NONE',  ( 5.319903205935248458, 1.244510898466891780, -1.679860476595731233 ) ) ;
#135734=CARTESIAN_POINT ( 'NONE',  ( 0.4449246239494052402, 0.5802587426733482046, -1.747387232072565189 ) ) ;
#135737=CARTESIAN_POINT ( 'NONE',  ( 1.635388916632842360, 0.6352005984417673501, 1.913803229121699534 ) ) ;
#135738=CARTESIAN_POINT ( 'NONE',  ( 0.3752731597879420677, 2.043270790221253908, -0.7926104125151807178 ) ) ;
#135742=CARTESIAN_POINT ( 'NONE',  ( 2.930460433956377564, -1.047063434655249647, -1.843881786051679850 ) ) ;
#135744=CARTESIAN_POINT ( 'NONE',  ( 5.742758765878789085, 0.3605303665093100851, 1.789564367143759327 ) ) ;
#135750=CARTESIAN_POINT ( 'NONE',  ( 1.599874016572962798, 1.395964939349272349, 1.459955266877453806 ) ) ;
#135751=CARTESIAN_POINT ( 'NONE',  ( 0.4992256481273240065, 1.750750569696429171, -1.170121261866068130 ) ) ;
#135754=CARTESIAN_POINT ( 'NONE',  ( 4.276097919418925031, -0.9535845961709583651, -1.597878833905818086 ) ) ;
#135760=CARTESIAN_POINT ( 'NONE',  ( 5.496661139185262002, -0.4475443406098400523, -1.769863040007889410 ) ) ;
#135764=CARTESIAN_POINT ( 'NONE',  ( 1.580929310206186100, 1.169321551402967119, -1.280364243709716243 ) ) ;
#135765=CARTESIAN_POINT ( 'NONE',  ( 0.5326489567317398421, -1.227437504408007474, -1.234024486680666000 ) ) ;
#135766=CARTESIAN_POINT ( 'NONE',  ( 5.830798129077900072, 2.222503408945066816, 0.6210771851366378993 ) ) ;
#135769=CARTESIAN_POINT ( 'NONE',  ( 1.423197193765327384, -0.05341811584172677374, 2.060271317188705709 ) ) ;
#135771=CARTESIAN_POINT ( 'NONE',  ( 6.538407551539116902, 2.202477839928073333, -0.6571292610791487077 ) ) ;
#135774=CARTESIAN_POINT ( 'NONE',  ( 0.4265601315296633778, 1.885908329847274745, 0.5744540738892388587 ) ) ;
#135775=CARTESIAN_POINT ( 'NONE',  ( 3.709155072767254868, 1.612916391665040416, -1.027221078234448859 ) ) ;
#135777=CARTESIAN_POINT ( 'NONE',  ( 5.408869034151480903, 1.673104959687292448, -1.439203791633147267 ) ) ;
#135782=CARTESIAN_POINT ( 'NONE',  ( 5.373730994130427874, 0.4134100146411868737, -2.079626175754036410 ) ) ;
#135783=CARTESIAN_POINT ( 'NONE',  ( 3.768876097860610397, -1.551941239651495108, 1.707908033328522146 ) ) ;
#135784=CARTESIAN_POINT ( 'NONE',  ( 4.264078424595136418, -1.956757550135434620, 0.1421211968542570592 ) ) ;
#135785=CARTESIAN_POINT ( 'NONE',  ( 0.6901946996495964548, 1.013433542811643440, -1.679602092450118489 ) ) ;
#135789=CARTESIAN_POINT ( 'NONE',  ( 6.280482454654814362, -0.5424645211669875122, -1.942098458069536848 ) ) ;
#135792=CARTESIAN_POINT ( 'NONE',  ( 2.852568495416502703, -2.164958695077593642, -0.1640175257638913364 ) ) ;
#135794=CARTESIAN_POINT ( 'NONE',  ( 1.090261293813089560, 1.267680250814690934, 1.699812782343253170 ) ) ;
#135799=CARTESIAN_POINT ( 'NONE',  ( 1.669287087933446490, 0.1544451976582127406, -2.055073672515697059 ) ) ;
#135805=CARTESIAN_POINT ( 'NONE',  ( 4.846305138012901637, 0.9798207982155520135, -1.642033262021398654 ) ) ;
#135810=CARTESIAN_POINT ( 'NONE',  ( -0.1056357528139931640, -1.757099710744941312, -0.4406103525058014392 ) ) ;
#135812=CARTESIAN_POINT ( 'NONE',  ( 0.5322733027907312620, 0.5591794568308214863, 1.832249074504808783 ) ) ;
#135813=CARTESIAN_POINT ( 'NONE',  ( 2.137250951388528275, -0.09934309608320915363, -2.068088366144354318 ) ) ;
#135815=CARTESIAN_POINT ( 'NONE',  ( 0.5144491564793505223, 1.361202580669124584, -1.426332009298651116 ) ) ;
#135816=CARTESIAN_POINT ( 'NONE',  ( 3.316849939159485228, 1.650902842016691130, 0.7798126646740562995 ) ) ;
#135817=CARTESIAN_POINT ( 'NONE',  ( 6.410767893487317792, 1.638320036227768783, -1.478771730184471389 ) ) ;
#135820=CARTESIAN_POINT ( 'NONE',  ( 4.141125080024585792, -0.1993089607698217136, -2.053009638179447371 ) ) ;
#135826=CARTESIAN_POINT ( 'NONE',  ( 5.561587576256037835, 0.4139992630615954572, -2.064685544603379608 ) ) ;
#135828=CARTESIAN_POINT ( 'NONE',  ( 6.549288556030710140, 1.803345607721940524, -1.016871928424132099 ) ) ;
#135830=CARTESIAN_POINT ( 'NONE',  ( 4.288457955665158750, -2.137403104576699242, -0.3218062170811594735 ) ) ;
#135831=CARTESIAN_POINT ( 'NONE',  ( 4.020179312760450152, -2.014129041962478883, 0.1506293649766801690 ) ) ;
#135832=CARTESIAN_POINT ( 'NONE',  ( 6.620655732516651071, -0.002413161512292844035, 2.173887093218453082 ) ) ;
#135837=CARTESIAN_POINT ( 'NONE',  ( 1.991423064788412800, -0.4370762659771566527, 1.968445590580846893 ) ) ;
#135845=CARTESIAN_POINT ( 'NONE',  ( 4.640250013031629095, 0.7743308749140092040, 1.862011755488258480 ) ) ;
#135847=CARTESIAN_POINT ( 'NONE',  ( 0.7676545703292583234, 0.8460830606174443158, 1.503042688352700829 ) ) ;
#135853=CARTESIAN_POINT ( 'NONE',  ( 5.430866635118035468, 0.1366067128489474591, 1.865587184704711632 ) ) ;
#135854=CARTESIAN_POINT ( 'NONE',  ( 6.222908185483853494, 1.488938611106488841, -1.355157726057078404 ) ) ;
#135859=CARTESIAN_POINT ( 'NONE',  ( 0.7379079170338508353, 2.013986002441462198, -0.1017714793793283723 ) ) ;
#135860=CARTESIAN_POINT ( 'NONE',  ( 1.511653934090980034, -0.6084181080006717535, 1.706514628581125681 ) ) ;
#135868=CARTESIAN_POINT ( 'NONE',  ( 0.1631139290103194861, 1.786460926609586330, -0.6921882798058466291 ) ) ;
#135875=CARTESIAN_POINT ( 'NONE',  ( 3.995124980148881288, 1.827535992889782523, -1.154293374375232828 ) ) ;
#135878=CARTESIAN_POINT ( 'NONE',  ( 0.6508261300204335464, 2.090236094481153550, 0.3566229023672163878 ) ) ;
#135879=CARTESIAN_POINT ( 'NONE',  ( 6.792070425361753649, -0.7769146798779454910, 1.650438213995283565 ) ) ;
#135881=CARTESIAN_POINT ( 'NONE',  ( 2.020718154849282744, 1.838011538856450855, 0.7131330410372925810 ) ) ;
#135882=CARTESIAN_POINT ( 'NONE',  ( 4.183787391381143195, 1.853651273288700718, -0.4697857328580385960 ) ) ;
#135885=CARTESIAN_POINT ( 'NONE',  ( 6.144967554776202157, -0.2872888210109864060, -1.948340736549762697 ) ) ;
#135886=CARTESIAN_POINT ( 'NONE',  ( 0.6209105903263291149, -1.844282116485985501, 0.6082893332694323529 ) ) ;
#135893=CARTESIAN_POINT ( 'NONE',  ( 5.461546741811521777, -1.510119879425949385, -1.173092037529008369 ) ) ;
#135894=ORIENTED_EDGE ( 'NONE', *, *, #117909, .F. ) ;
#135895=CARTESIAN_POINT ( 'NONE',  ( 1.307976841356368602, -0.5351398426680589182, 2.140771676462468687 ) ) ;
#135897=CARTESIAN_POINT ( 'NONE',  ( 0.3637282827039616251, 0.5997036651611362679, -1.815894722023647656 ) ) ;
#135898=CARTESIAN_POINT ( 'NONE',  ( -0.02319159430949970999, 2.891346550825595774, -2.299931007135449512 ) ) ;
#135899=( BOUNDED_CURVE ( )  B_SPLINE_CURVE ( 3, ( #26364, #55670, #121826, #158518 ),
 .UNSPECIFIED., .F., .T. ) 
 B_SPLINE_CURVE_WITH_KNOTS ( ( 4, 4 ),
 ( 0.000000000000000000, 0.4999999999999988898 ),
 .UNSPECIFIED. ) 
 CURVE ( )  GEOMETRIC_REPRESENTATION_ITEM ( )  RATIONAL_B_SPLINE_CURVE ( ( 1.000000000000000444, 0.3333333333333349802, 0.3333333333333334814, 0.9999999999999990008 ) ) 
 REPRESENTATION_ITEM ( '' )  );
#135902=CARTESIAN_POINT ( 'NONE',  ( 2.822784111170244525, -1.429543836668966561, 1.497820115680066122 ) ) ;
#135906=CARTESIAN_POINT ( 'NONE',  ( 0.08116279290028630133, -0.1557560750096824431, -2.127278773206460638 ) ) ;
#135911=CARTESIAN_POINT ( 'NONE',  ( 5.801316117833412278, 1.158123311926442911, -1.290955512118051818 ) ) ;
#135913=CARTESIAN_POINT ( 'NONE',  ( 3.133707330959301096, 1.967300496787489639, -0.6450458050009516553 ) ) ;
#135914=CARTESIAN_POINT ( 'NONE',  ( 4.780926590999498238, 1.759528625808198354, -1.177310133890494548 ) ) ;
#135917=CARTESIAN_POINT ( 'NONE',  ( 2.782036810173736718, -1.130008284276774022, -1.612816519099938173 ) ) ;
#135918=CARTESIAN_POINT ( 'NONE',  ( 0.6680393924826667496, 1.910109291395128972, -0.09634788558426229943 ) ) ;
#135919=CARTESIAN_POINT ( 'NONE',  ( 5.156304180611417820, -1.663069175626085139, 1.577778581399520652 ) ) ;
#135920=CARTESIAN_POINT ( 'NONE',  ( 3.387140609607977026, 1.650079954178599539, -0.7815607168924765258 ) ) ;
#135926=CARTESIAN_POINT ( 'NONE',  ( 4.447525235540350508, -1.838889683631849348, 0.8198632543043646859 ) ) ;
#135927=CARTESIAN_POINT ( 'NONE',  ( 2.782025223480470544, -1.125517505138178942, -1.606590762409945583 ) ) ;
#135930=CARTESIAN_POINT ( 'NONE',  ( 0.1751657365761704888, 2.870293503558702497, -2.532510806204853804 ) ) ;
#135931=CARTESIAN_POINT ( 'NONE',  ( 6.703094305332148117, -0.4564761572844484028, 2.047479069123214757 ) ) ;
#135932=CARTESIAN_POINT ( 'NONE',  ( 5.647242114940491220, -1.397150190615953358, -1.086277386216354168 ) ) ;
#135934=CARTESIAN_POINT ( 'NONE',  ( 2.431793384409334902, 1.031818167245980744, -1.933333044699904857 ) ) ;
#135935=CARTESIAN_POINT ( 'NONE',  ( 0.3623613221122607420, 0.1732436440316066917, -1.731762550003753898 ) ) ;
#135937=CARTESIAN_POINT ( 'NONE',  ( 0.2333690889706820926, 2.873202992247088083, -2.541887414127189881 ) ) ;
#135938=CARTESIAN_POINT ( 'NONE',  ( 0.06452196833307657919, -1.538014849765593439, -0.7809378474108348289 ) ) ;
#135939=CARTESIAN_POINT ( 'NONE',  ( 0.4217922253725381321, 0.8825364984147118230, 2.122365683989856588 ) ) ;
#135940=CARTESIAN_POINT ( 'NONE',  ( 0.5916818631664167993, -0.7834642122952638621, 2.046923429677327100 ) ) ;
#135942=CARTESIAN_POINT ( 'NONE',  ( 6.766931417284230754, -1.733354565069046505, 0.04740994324908299334 ) ) ;
#135943=CARTESIAN_POINT ( 'NONE',  ( 2.772332522587173997, 1.181257105606844160, 1.863944272329665086 ) ) ;
#135945=CARTESIAN_POINT ( 'NONE',  ( 0.3917816989358015034, -1.985425474602352525, 0.8787674391965931697 ) ) ;
#135947=CARTESIAN_POINT ( 'NONE',  ( 0.6204977360529799757, 2.087120111646578291, 0.3555802741468729877 ) ) ;
#135949=CARTESIAN_POINT ( 'NONE',  ( 6.620655732516624425, 7.629137130509072051, 2.773739711112707784 ) ) ;
#135950=CARTESIAN_POINT ( 'NONE',  ( 5.297847195631281814, -0.6933188941696236673, 1.797466220796402725 ) ) ;
#135952=CARTESIAN_POINT ( 'NONE',  ( 1.101600182630409819, -0.5506920761103645257, 2.225148091679912454 ) ) ;
#135956=CARTESIAN_POINT ( 'NONE',  ( 3.246955274364712540, 2.167573551356954731, 0.4849624922091085866 ) ) ;
#135962=CARTESIAN_POINT ( 'NONE',  ( 1.547500230860882287, -1.423960469535384465, 1.427938386157491246 ) ) ;
#135964=CARTESIAN_POINT ( 'NONE',  ( 1.147418581349904265, 1.820775857560010369, -0.9689367605143526241 ) ) ;
#135966=CARTESIAN_POINT ( 'NONE',  ( 0.06366010765614799061, -1.203631707120488947, 1.393476991864414760 ) ) ;
#135969=CARTESIAN_POINT ( 'NONE',  ( 2.284116761108864413, -1.734514481284253007, -0.3503773294724100706 ) ) ;
#135970=CARTESIAN_POINT ( 'NONE',  ( 1.811172873341511336, 1.158687402475454098, -1.650082692374904125 ) ) ;
#135971=CARTESIAN_POINT ( 'NONE',  ( 0.08126746489400815676, -0.8690269180096841239, 1.623235155968821841 ) ) ;
#135972=CARTESIAN_POINT ( 'NONE',  ( 5.653944246587851552, 0.9260977375703757231, 2.097164529332084637 ) ) ;
#135973=CARTESIAN_POINT ( 'NONE',  ( 2.941158370608713213, 0.6622022323767087215, -1.718108305994885177 ) ) ;
#135974=EDGE_CURVE ( 'NONE', #193311, #99811, #205785, .T. ) ;
#135976=CARTESIAN_POINT ( 'NONE',  ( 3.768406797884563897, -1.226484811506942441, 1.352366043108324201 ) ) ;
#135977=CARTESIAN_POINT ( 'NONE',  ( 5.186172726741035355, 1.650080556555008293, 1.158690440749516881 ) ) ;
#135979=CARTESIAN_POINT ( 'NONE',  ( 3.467884472470097457, 2.207893551020873257, -0.4935151710872084929 ) ) ;
#135981=CARTESIAN_POINT ( 'NONE',  ( 6.036178822307518566, 1.040974378708346526, -1.830621892639591630 ) ) ;
#135983=CARTESIAN_POINT ( 'NONE',  ( 3.824723168590526523, -1.392635068473629500, 1.532133406949770960 ) ) ;
#135986=CARTESIAN_POINT ( 'NONE',  ( 5.444028431581452665, -1.345373016635186714, -1.639009079359869725 ) ) ;
#135989=CARTESIAN_POINT ( 'NONE',  ( 2.631371740967450634, -1.797512724518410598, 0.6935160474876176373 ) ) ;
#135992=CARTESIAN_POINT ( 'NONE',  ( 6.649268376821393822, 1.715264285883275397, -0.9675598167100638580 ) ) ;
#135997=CARTESIAN_POINT ( 'NONE',  ( 0.6686063958157261178, 2.218491797483721051, -0.1167170572400257761 ) ) ;
#135999=CARTESIAN_POINT ( 'NONE',  ( 3.223755556863156180, -2.030008631501342808, 0.5602397303039460263 ) ) ;
#136002=CARTESIAN_POINT ( 'NONE',  ( 0.9943274703284404881, 1.832596168249778446, 0.3232805840463324198 ) ) ;
#136007=CARTESIAN_POINT ( 'NONE',  ( 1.213308285724056690, 1.730450836393576886, -1.225479750871574458 ) ) ;
#136010=CARTESIAN_POINT ( 'NONE',  ( 4.176187491914356897, -1.006606191838583131, -1.683785057063936552 ) ) ;
#136011=CARTESIAN_POINT ( 'NONE',  ( 2.448304249002517974, 2.161202317112873139, 0.05382173394478938222 ) ) ;
#136012=CARTESIAN_POINT ( 'NONE',  ( 1.610644152589552958, -0.2245515952020246953, 1.827417025815617935 ) ) ;
#136015=CARTESIAN_POINT ( 'NONE',  ( 4.663825473582838832, -1.133750416550326046, 1.320446528551111776 ) ) ;
#136019=CARTESIAN_POINT ( 'NONE',  ( 1.376082401959723089, 1.288024388040419632, 1.735935173841046675 ) ) ;
#136020=CARTESIAN_POINT ( 'NONE',  ( 3.198592129611950607, -1.351947076146834403, -1.495823048609262518 ) ) ;
#136022=CARTESIAN_POINT ( 'NONE',  ( 0.9190830904215805397, 1.997680973563022544, 0.8264451868333838602 ) ) ;
#136024=CARTESIAN_POINT ( 'NONE',  ( 3.713711766734467012, -1.942503170530969436, 0.3358077238896309824 ) ) ;
#136025=CARTESIAN_POINT ( 'NONE',  ( 6.509000000000048303, 0.5949247728001515467, 1.954148248227548290 ) ) ;
#136026=CARTESIAN_POINT ( 'NONE',  ( 2.841277192181762334, 0.6965426786647112012, -1.813031058463436818 ) ) ;
#136031=CARTESIAN_POINT ( 'NONE',  ( -0.1108833634136975610, 0.7331455517814323697, -1.980187714524218823 ) ) ;
#136037=CARTESIAN_POINT ( 'NONE',  ( 6.563506341781633502, 0.4036857245812221495, -2.271876217655709240 ) ) ;
#136040=CARTESIAN_POINT ( 'NONE',  ( 4.557442073745519018, 1.573120015848201492, 1.171846803954358363 ) ) ;
#136042=CARTESIAN_POINT ( 'NONE',  ( 1.371720446232262081, -0.2986288616722633793, -1.994071132515719880 ) ) ;
#136044=CARTESIAN_POINT ( 'NONE',  ( 2.958335891534333850, -1.257395014299323988, 1.703445231074371291 ) ) ;
#136048=CARTESIAN_POINT ( 'NONE',  ( 3.679498877186979211, -0.9061679144062879665, 1.602619060095414216 ) ) ;
#136052=CARTESIAN_POINT ( 'NONE',  ( 3.621431001533811589, 1.820626359085864454, 1.087046460333654485 ) ) ;
#136055=CARTESIAN_POINT ( 'NONE',  ( 5.044241359090890775, 2.054987069614383266, 0.1556004420267612098 ) ) ;
#136057=CARTESIAN_POINT ( 'NONE',  ( 2.102840161960460197, -0.4018910908503615653, 1.796694178532439956 ) ) ;
#136063=CARTESIAN_POINT ( 'NONE',  ( 2.438337523484556790, 1.039148161723329578, -1.946916322307743474 ) ) ;
#136064=CARTESIAN_POINT ( 'NONE',  ( 3.532755146446086680, 2.206387722723508915, 0.4996636332569806549 ) ) ;
#136066=CARTESIAN_POINT ( 'NONE',  ( 5.097853226644959435, 1.222535334948423813, 1.337041937662573288 ) ) ;
#136067=CARTESIAN_POINT ( 'NONE',  ( 4.452287505575288407, -1.246817998045848697, 1.454578644467845017 ) ) ;
#136069=CARTESIAN_POINT ( 'NONE',  ( 3.871915168923282913, 1.094167467933440108, 1.639771958457488132 ) ) ;
#136070=CARTESIAN_POINT ( 'NONE',  ( 4.645289301550183936, -1.446173438076237217, -1.186536486241091204 ) ) ;
#136071=CARTESIAN_POINT ( 'NONE',  ( 3.704037377190313673, -0.6708616879335957961, 2.208036538417802230 ) ) ;
#136072=CARTESIAN_POINT ( 'NONE',  ( 4.808966763405270406, -1.495079835775798838, 1.108065441546413288 ) ) ;
#136076=CARTESIAN_POINT ( 'NONE',  ( 1.805437418371407254, 1.751699828856004837, 1.168899091633753384 ) ) ;
#136080=CARTESIAN_POINT ( 'NONE',  ( 3.094099843433151253, 1.348383549611749332, 1.636666742212993686 ) ) ;
#136082=CARTESIAN_POINT ( 'NONE',  ( 0.4221360882172753293, -2.009675015244154483, 0.2020994116621494530 ) ) ;
#136087=CARTESIAN_POINT ( 'NONE',  ( 2.091316376603330252, 1.881825464268515269, -1.063406855978922039 ) ) ;
#136094=CARTESIAN_POINT ( 'NONE',  ( 6.403528931544730796, -1.954801056786956259, 0.4946215565981848528 ) ) ;
#136096=CARTESIAN_POINT ( 'NONE',  ( 6.515180868147061766, -2.027822497041928518, 0.5085933055150316795 ) ) ;
#136098=CARTESIAN_POINT ( 'NONE',  ( 1.815646767810099149, -0.2761031220132881270, 2.245556248662975207 ) ) ;
#136106=CARTESIAN_POINT ( 'NONE',  ( 3.615580125028591052, -1.699004861347377604, 0.2966152939984505466 ) ) ;
#136108=CARTESIAN_POINT ( 'NONE',  ( 2.161070758698178107, 0.3078950573750063313, -1.742579939182072657 ) ) ;
#136109=CARTESIAN_POINT ( 'NONE',  ( 3.106110754726201240, -0.8138748988139458129, 1.841402425526596387 ) ) ;
#136110=CARTESIAN_POINT ( 'NONE',  ( 4.840968367003476658, 0.3731960759543617723, 2.174832070070693568 ) ) ;
#136113=CARTESIAN_POINT ( 'NONE',  ( 3.937764026144819685, -1.931520177269234306, 0.5904599756008358513 ) ) ;
#136115=CARTESIAN_POINT ( 'NONE',  ( 5.619825546450978315, -0.5151785252428126016, 2.056841324599982368 ) ) ;
#136116=CARTESIAN_POINT ( 'NONE',  ( 4.200796113533305842, 1.844717850457804120, 0.8146114232021259838 ) ) ;
#136117=CARTESIAN_POINT ( 'NONE',  ( 4.218897050542698146, 1.396175630728054173, -1.154312599804697914 ) ) ;
#136121=CARTESIAN_POINT ( 'NONE',  ( 1.305301652190330675, -0.4579020413679709689, 1.813615928118620380 ) ) ;
#136124=CARTESIAN_POINT ( 'NONE',  ( 6.147087800311862971, 0.1847020338378597137, 1.802040927518679281 ) ) ;
#136129=CARTESIAN_POINT ( 'NONE',  ( 0.7207899753199145110, 1.446443371814851941, -1.251069288267861346 ) ) ;
#136131=CARTESIAN_POINT ( 'NONE',  ( 1.469116868872882620, 1.728625619535430369, 0.9278086228877155950 ) ) ;
#136134=CARTESIAN_POINT ( 'NONE',  ( 4.535463010148616192, -0.1012041512906610846, 2.118281909017679432 ) ) ;
#136137=CARTESIAN_POINT ( 'NONE',  ( 5.764905551123544747, -1.781034818069273884, -0.8454043039353341671 ) ) ;
#136139=CARTESIAN_POINT ( 'NONE',  ( 1.142838885277572825, 1.941394601512283602, 0.5327644489504842484 ) ) ;
#136141=CARTESIAN_POINT ( 'NONE',  ( 0.9489988177146626569, -1.915858558953801749, -0.9014485902382618487 ) ) ;
#136143=CARTESIAN_POINT ( 'NONE',  ( 2.664580169416390643, -0.7900844611210651180, -1.913877855911281234 ) ) ;
#136148=CARTESIAN_POINT ( 'NONE',  ( 4.787105812777236125, 1.548788850919210702, 1.404477511574409920 ) ) ;
#136150=CARTESIAN_POINT ( 'NONE',  ( 3.346530664597209714, 0.4423686283943834563, 1.771051422834311051 ) ) ;
#136151=CARTESIAN_POINT ( 'NONE',  ( 1.717148478332259254, 1.506203170942743030, 1.006022724715895045 ) ) ;
#136153=CARTESIAN_POINT ( 'NONE',  ( 6.639307388351803674, -1.973492857608965423, 0.9879489342229507143 ) ) ;
#136156=CARTESIAN_POINT ( 'NONE',  ( 4.823365732668142947, -0.1123398232194070118, 2.204042774474362254 ) ) ;
#136159=CARTESIAN_POINT ( 'NONE',  ( 3.791585636498477463, 1.799617611794877670, -0.6470144256675299799 ) ) ;
#136162=CARTESIAN_POINT ( 'NONE',  ( 6.303194806757332458, -1.751150776259063457, 1.104182018118210262 ) ) ;
#136164=CARTESIAN_POINT ( 'NONE',  ( 5.917560222199001352, -1.216239291071326001, -1.822900893127032962 ) ) ;
#136168=CARTESIAN_POINT ( 'NONE',  ( 3.866346082213562685, -1.258301477641217803, 1.384200088751494251 ) ) ;
#136169=CARTESIAN_POINT ( 'NONE',  ( -0.02319159430947541692, 2.051704324979522820, -2.228571760951563618 ) ) ;
#136175=CARTESIAN_POINT ( 'NONE',  ( 6.807487347360918761, -1.659057770219806160, -1.238116672595261480 ) ) ;
#136176=CARTESIAN_POINT ( 'NONE',  ( 0.8609541034889023337, -0.05231784723681161264, -2.015913592316537883 ) ) ;
#136177=CIRCLE ( 'NONE', #4710, 0.1399999999999995137 ) ;
#136181=CARTESIAN_POINT ( 'NONE',  ( 1.183813618819636870, -0.9825931803647185436, 1.958887836816553429 ) ) ;
#136182=CARTESIAN_POINT ( 'NONE',  ( 5.830640656690653678, 1.760721658632548037, 0.4824517239352192344 ) ) ;
#136191=CARTESIAN_POINT ( 'NONE',  ( 3.298233973420101606, 1.449563003725433896, -1.135193286699177628 ) ) ;
#136192=CARTESIAN_POINT ( 'NONE',  ( 0.6979027206182022436, 1.353502529517286446, 1.490303647139071153 ) ) ;
#136193=CARTESIAN_POINT ( 'NONE',  ( 2.144337281971959719, -0.1124944508365255252, -2.295720847718041746 ) ) ;
#136195=CARTESIAN_POINT ( 'NONE',  ( 1.498636204049142773, 0.3563576638296832577, 1.826325547775342173 ) ) ;
#136199=CARTESIAN_POINT ( 'NONE',  ( 3.972844611716894736, -1.413603510852480927, 1.288168406687495215 ) ) ;
#136203=CARTESIAN_POINT ( 'NONE',  ( 4.124618644571789616, 0.1043759322204278750, 2.088280726629719197 ) ) ;
#136204=CARTESIAN_POINT ( 'NONE',  ( 2.395189659270926086, 1.444574673180216706, 1.188490415850687265 ) ) ;
#136207=CARTESIAN_POINT ( 'NONE',  ( 3.034399582073334489, -1.533639759443014894, 0.8228653360542650397 ) ) ;
#136211=CARTESIAN_POINT ( 'NONE',  ( 3.527714679269139619, -1.028799902082434992, -1.384306889003545926 ) ) ;
#136212=CARTESIAN_POINT ( 'NONE',  ( 3.491892070630482348, -2.189115664112693871, -0.1057334378413293807 ) ) ;
#136214=CARTESIAN_POINT ( 'NONE',  ( 3.344746749068757019, -2.138148195731132351, -0.3758941404270431108 ) ) ;
#136215=CARTESIAN_POINT ( 'NONE',  ( 2.455445036260803349, 0.4872311372507812655, -1.759406031448563557 ) ) ;
#136216=CARTESIAN_POINT ( 'NONE',  ( 0.5144084716053355377, 0.7454083195421266073, 1.814826383214888983 ) ) ;
#136217=CARTESIAN_POINT ( 'NONE',  ( 4.663340677796647071, 1.974402194736598837, -0.7651654921337573967 ) ) ;
#136219=CARTESIAN_POINT ( 'NONE',  ( 4.458679977242249848, -2.047270833213535202, -1.031427349252316272 ) ) ;
#136221=CARTESIAN_POINT ( 'NONE',  ( 6.620655732516642189, 0.6076529131340856482, 1.780684370158796881 ) ) ;
#136223=CARTESIAN_POINT ( 'NONE',  ( 0.08289510313583270396, -1.381697626658566547, 1.608636130391014163 ) ) ;
#136230=CARTESIAN_POINT ( 'NONE',  ( 5.414685466650038137, -1.281359335986744341, -1.556910257834144051 ) ) ;
#136232=CARTESIAN_POINT ( 'NONE',  ( 4.786014635464308498, -1.264713950826271027, -1.629283840103493253 ) ) ;
#136234=CARTESIAN_POINT ( 'NONE',  ( -0.1409997244346087863, -0.002808977843308038246, -2.000147647483837776 ) ) ;
#136239=CARTESIAN_POINT ( 'NONE',  ( 0.1331565106231328566, 1.371277436080810208, -2.201942895618694607 ) ) ;
#136240=CARTESIAN_POINT ( 'NONE',  ( 0.7618063994256699667, 1.031939465966443814, 1.818122583218291677 ) ) ;
#136241=CARTESIAN_POINT ( 'NONE',  ( 4.500625067706437221, -1.976956227568788638, 0.3961002554062897918 ) ) ;
#136242=CARTESIAN_POINT ( 'NONE',  ( 3.632213977189250098, 0.2737156317273430894, 1.820677940640710979 ) ) ;
#136245=CARTESIAN_POINT ( 'NONE',  ( 0.2524154375680361939, -1.389930774942317759, 1.021034751394875428 ) ) ;
#136247=CARTESIAN_POINT ( 'NONE',  ( 0.7042444638330731532, 2.126757524241583486, 0.8727403922216511178 ) ) ;
#136249=CARTESIAN_POINT ( 'NONE',  ( 6.702048742255109381, -2.262191126150433274, 0.04724482429044154358 ) ) ;
#136250=CARTESIAN_POINT ( 'NONE',  ( 2.631583836753316863, -1.964825297316885155, 0.7587525405363388931 ) ) ;
#136259=CARTESIAN_POINT ( 'NONE',  ( 5.062811918942510481, 0.6453760322048059939, 2.125560002649288460 ) ) ;
#136260=CARTESIAN_POINT ( 'NONE',  ( 2.502122453320880346, -0.8398649383675670377, -2.024319193490734303 ) ) ;
#136263=CARTESIAN_POINT ( 'NONE',  ( 5.125427350195786325, 0.1941421753944693185, -1.952251141935714696 ) ) ;
#136266=CARTESIAN_POINT ( 'NONE',  ( 6.889999999999996128, 2.105039946316529242, 2.031469082812328519 ) ) ;
#136268=CARTESIAN_POINT ( 'NONE',  ( 4.412424163657523657, -2.120181911468725033, -0.04909571644767100895 ) ) ;
#136272=CARTESIAN_POINT ( 'NONE',  ( 6.368072262247213899, 1.106822706796772193, 1.856716078747308263 ) ) ;
#136274=CARTESIAN_POINT ( 'NONE',  ( 4.704558828624370470, 1.604442792107749760, 0.9031527321438773681 ) ) ;
#136277=CARTESIAN_POINT ( 'NONE',  ( 1.329236136963531489, 0.8583591509643221373, -1.513936452999464555 ) ) ;
#136280=DIRECTION ( 'NONE',  ( 2.949029909160572061E-17, 1.000000000000000000, -8.673600428462391266E-15 ) ) ;
#136281=CARTESIAN_POINT ( 'NONE',  ( 5.700121470611750674, -2.161883445634639411, -0.004416275431240455560 ) ) ;
#136285=CARTESIAN_POINT ( 'NONE',  ( 4.100566281481184738, -0.6756360485904688851, -2.053482476349233643 ) ) ;
#136287=CARTESIAN_POINT ( 'NONE',  ( 4.991463202408453093, 1.458887350482462875, 1.326006969317705009 ) ) ;
#136288=CARTESIAN_POINT ( 'NONE',  ( 3.989331682606485519, 1.645927443309925353, 0.5452122354672321869 ) ) ;
#136289=CARTESIAN_POINT ( 'NONE',  ( 0.8377433530848135135, 0.8832496248250313320, -2.005872107257236969 ) ) ;
#136290=CARTESIAN_POINT ( 'NONE',  ( 2.415413485888187495, 2.061215426621319402, 1.037632957015870661 ) ) ;
#136291=CARTESIAN_POINT ( 'NONE',  ( 3.848945901207713849, -1.686846252213095365, 1.183521113291643223 ) ) ;
#136292=CARTESIAN_POINT ( 'NONE',  ( 0.5681770160902823719, -1.828317568802136250, -0.6549081214334094847 ) ) ;
#136298=CARTESIAN_POINT ( 'NONE',  ( 3.768774344222697970, -1.483932802477351487, 1.633493490917396151 ) ) ;
#136301=CARTESIAN_POINT ( 'NONE',  ( 0.3384086464433467278, -1.803039684303367141, -0.4601552930486965121 ) ) ;
#136302=CARTESIAN_POINT ( 'NONE',  ( -0.1288028175206907822, -0.008968661790493319408, -2.273875003271645934 ) ) ;
#136306=CARTESIAN_POINT ( 'NONE',  ( 6.925078400183575233, 2.022016365062285104, 2.447829694591229899 ) ) ;
#136309=CARTESIAN_POINT ( 'NONE',  ( 3.239188564323669528, -1.818332144261879613, 0.9699876223461401104 ) ) ;
#136316=CARTESIAN_POINT ( 'NONE',  ( 2.202092877552201067, -2.060466153685360791, 0.04932271190436626068 ) ) ;
#136321=EDGE_CURVE ( 'NONE', #12895, #30003, #65222, .T. ) ;
#136322=CARTESIAN_POINT ( 'NONE',  ( 5.953802724510455668, 0.6443607167232848765, -2.110727517106169682 ) ) ;
#136323=CARTESIAN_POINT ( 'NONE',  ( 0.9839146201040609441, 1.450980403326153301, 1.602422216231303320 ) ) ;
#136325=CARTESIAN_POINT ( 'NONE',  ( 1.059780186608853203, 1.205045252304644210, 1.616690996016925563 ) ) ;
#136326=CARTESIAN_POINT ( 'NONE',  ( 2.337686028923485537, -1.414513361329417851, 1.811461888080208027 ) ) ;
#136328=CARTESIAN_POINT ( 'NONE',  ( 6.252599623108594074, 1.892168639490459325, 0.2757424028280440753 ) ) ;
#136331=CARTESIAN_POINT ( 'NONE',  ( 2.342468781959532453, 0.4075140148256419792, 1.825566309089213579 ) ) ;
#136332=CARTESIAN_POINT ( 'NONE',  ( 3.450407915430803385, -1.350735839785843773, 1.497501794165828626 ) ) ;
#136336=CARTESIAN_POINT ( 'NONE',  ( 4.635441201516187881, -1.925843587088198916, 0.8528682856967207959 ) ) ;
#136341=CARTESIAN_POINT ( 'NONE',  ( 5.080334495226257907, 0.9990293545295618749, 1.755361416599170443 ) ) ;
#136343=CARTESIAN_POINT ( 'NONE',  ( 0.3212321915853528220, -1.840712657873358138, -0.9308276203483353273 ) ) ;
#136345=CARTESIAN_POINT ( 'NONE',  ( 6.046190728430958394, 2.158797838069245412, 0.1127497994189360364 ) ) ;
#136353=CARTESIAN_POINT ( 'NONE',  ( 3.051421578680337809, 1.863438581370242986, -1.114033871086346217 ) ) ;
#136356=CARTESIAN_POINT ( 'NONE',  ( 1.839159199666509981, 0.7036077657225293658, -1.701706503975081830 ) ) ;
#136358=CARTESIAN_POINT ( 'NONE',  ( 3.474349307649237328, -2.112600797985896950, -0.5827812199917583591 ) ) ;
#136359=CARTESIAN_POINT ( 'NONE',  ( 6.883263157960330503, 7.629137130509037412, 2.753810918356710769 ) ) ;
#136360=CARTESIAN_POINT ( 'NONE',  ( 4.434621138646507532, 2.218105251380130483, 0.4453182654360221537 ) ) ;
#136367=CARTESIAN_POINT ( 'NONE',  ( 5.501144674179510474, 1.447219185280288700, 1.018257267444661496 ) ) ;
#136368=B_SPLINE_CURVE_WITH_KNOTS ( 'NONE', 3,
 ( #88798, #188405, #103978, #184134, #35758, #40043, #101832, #102900, #5357, #167901, #85575 ),
 .UNSPECIFIED., .F., .F.,
 ( 4, 1, 1, 1, 1, 1, 1, 1, 4 ),
 ( 0.000000000000000000, 0.2254101072112788262, 0.3970395454107691902, 0.5239558410346354389, 0.6152342776129972046, 0.6800502191696807808, 0.7279184599320936977, 0.7685697607527866015, 1.000000000000000000 ),
 .UNSPECIFIED. ) ;
#136370=CARTESIAN_POINT ( 'NONE',  ( 1.518734001684220347, 1.414770742371696644, -1.560122519311944345 ) ) ;
#136373=CARTESIAN_POINT ( 'NONE',  ( 2.260148812482842828, -1.969196485324760326, 0.04527702327579082725 ) ) ;
#136374=CARTESIAN_POINT ( 'NONE',  ( 6.727182134110200273, -0.004969159814478123736, 2.189081792362323586 ) ) ;
#136376=CARTESIAN_POINT ( 'NONE',  ( 6.363521484574993003, -1.460773276151544176, -1.071267404939825640 ) ) ;
#136381=CARTESIAN_POINT ( 'NONE',  ( 5.418772907935071714, 1.728844841293469159, 0.7149302089985640762 ) ) ;
#136383=CARTESIAN_POINT ( 'NONE',  ( 5.453992358814952368, -0.7503507308065425763, 1.929658000011783336 ) ) ;
#136387=CARTESIAN_POINT ( 'NONE',  ( 0.1333692844072559280, 0.001398348041498076455, -2.053671342968105051 ) ) ;
#136394=CARTESIAN_POINT ( 'NONE',  ( 5.178158156489047315, -1.047961880893449882, -1.658324637040713867 ) ) ;
#136396=CARTESIAN_POINT ( 'NONE',  ( 3.409529676982744562, 0.4871283372531940992, 1.956261718130556160 ) ) ;
#136397=CARTESIAN_POINT ( 'NONE',  ( 2.149496333622540334, 1.877876629180765589, -0.3779552698702989266 ) ) ;
#136400=CARTESIAN_POINT ( 'NONE',  ( 0.7322823680011962821, 2.160084099745246178, 0.3691886501416344335 ) ) ;
#136401=CARTESIAN_POINT ( 'NONE',  ( 0.2333690889706926119, 0.7157316027301027228, -2.136973218959358434 ) ) ;
#136402=CARTESIAN_POINT ( 'NONE',  ( 2.319419987651088810, -1.815478447740950685, 0.4500915571382518854 ) ) ;
#136404=CARTESIAN_POINT ( 'NONE',  ( 4.394793396725252599, -1.953840400094335905, -0.4849018877997012256 ) ) ;
#136407=CARTESIAN_POINT ( 'NONE',  ( 4.482099252480286289, -2.116778089722763045, -0.05043497882678028149 ) ) ;
#136409=CARTESIAN_POINT ( 'NONE',  ( 6.443811375169310907, 1.424792453395683500, 1.502365266013883538 ) ) ;
#136410=CARTESIAN_POINT ( 'NONE',  ( 0.6618065864371965867, 1.033746398093362773, 1.817239694416083795 ) ) ;
#136412=CARTESIAN_POINT ( 'NONE',  ( 6.821331453475777629, -0.1281762050449504198, 1.796388512460028286 ) ) ;
#136413=VERTEX_POINT ( 'NONE', #99420 ) ;
#136421=CARTESIAN_POINT ( 'NONE',  ( 0.4690326002820300877, -1.529415377529659503, -0.9703845247886667691 ) ) ;
#136429=CARTESIAN_POINT ( 'NONE',  ( 6.028922772295511656, -1.701938481575874684, 1.081082441910637071 ) ) ;
#136430=CARTESIAN_POINT ( 'NONE',  ( -0.04015575566676531788, -1.641981170221143094, -1.341450104213978589 ) ) ;
#136437=CARTESIAN_POINT ( 'NONE',  ( 2.992966325197043531, 0.2361965902525232364, 1.955129705961492270 ) ) ;
#136438=CARTESIAN_POINT ( 'NONE',  ( 4.394157760337158436, -0.8647400765994193161, -1.821735888681835558 ) ) ;
#136440=SURFACE_STYLE_FILL_AREA ( #37854 ) ;
#136442=CARTESIAN_POINT ( 'NONE',  ( 5.279302027902110339, 1.469929824498400039, 1.625505876179579534 ) ) ;
#136444=CARTESIAN_POINT ( 'NONE',  ( 3.539987092570716865, 0.8674169631235107980, -1.720131978839019693 ) ) ;
#136446=CARTESIAN_POINT ( 'NONE',  ( -0.02988540731101250320, 5.726092063503692486, -2.320384613474982594 ) ) ;
#136447=CARTESIAN_POINT ( 'NONE',  ( 0.1331565106231328843, 0.003911343561965873426, -1.946049565259087455 ) ) ;
#136451=CARTESIAN_POINT ( 'NONE',  ( 5.506690373602650901, 0.5681407172444596920, 1.885743917740757114 ) ) ;
#136452=CARTESIAN_POINT ( 'NONE',  ( 0.09902944379243035222, -0.5168498253214492966, 1.871975360678623579 ) ) ;
#136453=CARTESIAN_POINT ( 'NONE',  ( 4.213543065054736303, 1.618255708775760970, 1.197237177376732964 ) ) ;
#136454=CARTESIAN_POINT ( 'NONE',  ( 5.431170548343748905, 1.126412363255802518, 2.003379520639406497 ) ) ;
#136456=CARTESIAN_POINT ( 'NONE',  ( 3.836619860451701669, -1.792334419201064399, -0.5002748670543122333 ) ) ;
#136462=CARTESIAN_POINT ( 'NONE',  ( 0.1346727191937693857, 0.3808678606769915209, 2.158067550307264604 ) ) ;
#136467=CARTESIAN_POINT ( 'NONE',  ( 0.8381832108898427114, 1.798179982845280467, 0.3147962740308178353 ) ) ;
#136469=CARTESIAN_POINT ( 'NONE',  ( 2.795252500310735133, 1.254151915811404061, -1.197898925204267995 ) ) ;
#136472=CARTESIAN_POINT ( 'NONE',  ( 5.848246728868278232, 1.823843535133644389, 0.08496628090458313576 ) ) ;
#136473=CARTESIAN_POINT ( 'NONE',  ( 3.766413727395605093, -0.7909564911158167844, -1.795405819223389488 ) ) ;
#136477=CARTESIAN_POINT ( 'NONE',  ( 3.897227946829431300, -0.2092540311423168320, -2.110150122182581356 ) ) ;
#136480=CARTESIAN_POINT ( 'NONE',  ( 2.219664259111033378, 0.3580842396277704176, -2.038906786875307020 ) ) ;
#136484=CARTESIAN_POINT ( 'NONE',  ( 4.125785508553894587, -0.3794599818576475658, 2.188496638732019495 ) ) ;
#136486=CARTESIAN_POINT ( 'NONE',  ( 1.372188323541504218, -0.3435771540031757332, -2.272792483656468576 ) ) ;
#136494=CARTESIAN_POINT ( 'NONE',  ( 2.707167837304753633, 1.638089068140319071, -0.9866689735503200165 ) ) ;
#136496=CARTESIAN_POINT ( 'NONE',  ( 3.908989539853875428, 1.479446464633243474, 0.8863536201247077528 ) ) ;
#136497=CARTESIAN_POINT ( 'NONE',  ( 2.009000277268524481, 0.004839059525654776373, 2.016708403978189956 ) ) ;
#136498=CARTESIAN_POINT ( 'NONE',  ( 3.709890859234076466, 2.183183022688690578, 0.7197655052363950423 ) ) ;
#136500=CARTESIAN_POINT ( 'NONE',  ( -0.02244404828157658613, -0.004869073801674199918, -2.189079685368473527 ) ) ;
#136502=CARTESIAN_POINT ( 'NONE',  ( 5.290226454957744018, -1.756441682966399132, -0.2160651130965525468 ) ) ;
#136505=CARTESIAN_POINT ( 'NONE',  ( 1.078551950277906402, -2.237456700407819632, -0.4976139165283523513 ) ) ;
#136506=CARTESIAN_POINT ( 'NONE',  ( 0.1986093482617317107, -0.4694325260376422948, 1.675759954737522150 ) ) ;
#136508=CARTESIAN_POINT ( 'NONE',  ( 5.208995777154565410, -0.3238732214236837992, 2.167259527466679270 ) ) ;
#136513=CARTESIAN_POINT ( 'NONE',  ( 6.760220206081136496, -2.069995208266177666, 0.04663682477341199450 ) ) ;
#136514=CARTESIAN_POINT ( 'NONE',  ( 1.393767942625488532, -2.000731169080074423, 0.2516357431460446992 ) ) ;
#136516=CARTESIAN_POINT ( 'NONE',  ( 4.354074215503287881, 1.926045596674738514, -0.04874250487575670227 ) ) ;
#136519=CARTESIAN_POINT ( 'NONE',  ( 1.424421946217780732, -2.203867130488819548, 0.2783968414596868501 ) ) ;
#136526=CARTESIAN_POINT ( 'NONE',  ( 4.686888010602763721, 1.293897920562389947, 1.164242640570410714 ) ) ;
#136527=CARTESIAN_POINT ( 'NONE',  ( 1.873419974815058842, -0.2433403713097622156, 1.946663811685337420 ) ) ;
#136532=CARTESIAN_POINT ( 'NONE',  ( 6.496542546517183325, 1.940334402339534581, 0.2891159199209930031 ) ) ;
#136537=CARTESIAN_POINT ( 'NONE',  ( 0.8489190418228099722, 0.6593363751366092540, 2.164330503585075505 ) ) ;
#136541=CARTESIAN_POINT ( 'NONE',  ( 1.334983872447586872, -1.693447605269988276, 0.7947349781701130711 ) ) ;
#136542=CARTESIAN_POINT ( 'NONE',  ( -0.05262932013434371004, -1.547529252455181581, -0.7825623337873451879 ) ) ;
#136543=CARTESIAN_POINT ( 'NONE',  ( 4.159861740090546434, 1.033864333764370702, 1.932389678422803181 ) ) ;
#136544=CARTESIAN_POINT ( 'NONE',  ( 5.878008146920711496, 1.368277704907730374, 1.858044196986943675 ) ) ;
#136545=CARTESIAN_POINT ( 'NONE',  ( 1.305620473665240366, -0.5016907458927004626, 1.998752541464960952 ) ) ;
#136546=CARTESIAN_POINT ( 'NONE',  ( 3.785046133934614865, 1.407330997726879973, 1.338362524258763786 ) ) ;
#136549=CARTESIAN_POINT ( 'NONE',  ( 5.430866635118035468, 0.1366067128489474591, 1.865587184704711632 ) ) ;
#136551=CARTESIAN_POINT ( 'NONE',  ( 4.465470312728934132, -1.956561007648183192, -0.4872041746135646889 ) ) ;
#136555=CARTESIAN_POINT ( 'NONE',  ( 1.137010146156680834, -1.651496384925277283, 0.7785749969668461778 ) ) ;
#136561=CARTESIAN_POINT ( 'NONE',  ( 6.491097285755237145, 1.794469726164525492, -1.013322515520258538 ) ) ;
#136565=CARTESIAN_POINT ( 'NONE',  ( 6.129558478109055741, -0.2449627755865962375, 2.004677898944156489 ) ) ;
#136566=CARTESIAN_POINT ( 'NONE',  ( 6.076846083367460238, -1.572777764080468321, 1.568860064416939037 ) ) ;
#136570=CARTESIAN_POINT ( 'NONE',  ( 5.489158015974754612, 1.818697853212094095, -0.9693054586683967910 ) ) ;
#136571=CARTESIAN_POINT ( 'NONE',  ( 4.483046177357690176, -2.016033783801042034, -0.04667830911464498911 ) ) ;
#136573=EDGE_LOOP ( 'NONE', ( #186907, #198342 ) ) ;
#136580=CARTESIAN_POINT ( 'NONE',  ( 4.393907559866160994, 0.09612058942952760032, 2.013924333851605297 ) ) ;
#136581=CARTESIAN_POINT ( 'NONE',  ( 4.083814069670049562, -1.821384084514931612, -0.2681248149544179227 ) ) ;
#136583=CARTESIAN_POINT ( 'NONE',  ( 2.280263026629821166, 1.421315682977505546, 1.817977143087915026 ) ) ;
#136585=CARTESIAN_POINT ( 'NONE',  ( 4.464260128311710041, 1.014592192358022338, 1.908665273222116543 ) ) ;
#136587=CARTESIAN_POINT ( 'NONE',  ( -0.09434409087969403140, -0.8304652339055562660, -1.753633067539569490 ) ) ;
#136591=CARTESIAN_POINT ( 'NONE',  ( 2.694054421766533203, -1.865511834602461949, -0.1395888279770511053 ) ) ;
#136592=CARTESIAN_POINT ( 'NONE',  ( 6.754760782388981255, -1.524083220479439005, 1.250168222439652421 ) ) ;
#136595=CARTESIAN_POINT ( 'NONE',  ( 1.682535984017709874, -1.178549783888741320, 1.865657194899547733 ) ) ;
#136601=CARTESIAN_POINT ( 'NONE',  ( 5.664905584638975533, -1.781982755157806908, -0.8436340872482649411 ) ) ;
#136602=CARTESIAN_POINT ( 'NONE',  ( 6.375599228498684212, 2.210405824868751701, -0.6629917143727501738 ) ) ;
#136603=CARTESIAN_POINT ( 'NONE',  ( 0.7132427667453158371, -1.655377960257615966, -1.052639099659122390 ) ) ;
#136604=CARTESIAN_POINT ( 'NONE',  ( 4.012594160722949610, 0.7376926799337081286, 1.926325278971857236 ) ) ;
#136612=CARTESIAN_POINT ( 'NONE',  ( 6.004372733575126020, 2.168386774327632160, 0.1126981005201161401 ) ) ;
#136614=CARTESIAN_POINT ( 'NONE',  ( 5.495603940606402560, -1.841430844871448258, 0.006098274996368944698 ) ) ;
#136617=CARTESIAN_POINT ( 'NONE',  ( 0.6494046996203367561, 0.5928216254872006319, -1.774177939146783345 ) ) ;
#136621=CARTESIAN_POINT ( 'NONE',  ( 1.436035868020806738, -1.063167577064242142, -1.589284522738307448 ) ) ;
#136622=CARTESIAN_POINT ( 'NONE',  ( 2.465387952175815744, 1.736178859682969700, -0.3425752158293988159 ) ) ;
#136623=CARTESIAN_POINT ( 'NONE',  ( 6.217445370822936468, 1.674971474680493788, 1.116412877057591624 ) ) ;
#136625=CARTESIAN_POINT ( 'NONE',  ( 4.376519623831674366, -0.4236097701148673900, -1.868001571610947043 ) ) ;
#136627=CARTESIAN_POINT ( 'NONE',  ( 5.002387483831562953, 1.964158282178072312, 0.1467643733194800570 ) ) ;
#136628=CARTESIAN_POINT ( 'NONE',  ( 0.1234922912959918878, 1.848187084301698757, 1.039613981531524400 ) ) ;
#136630=CARTESIAN_POINT ( 'NONE',  ( 3.713615009860570915, -1.843089489661839053, 0.3189824552965599969 ) ) ;
#136631=CARTESIAN_POINT ( 'NONE',  ( 6.375633740537438143, 1.648238817998586958, -0.5085109915310691564 ) ) ;
#136633=CARTESIAN_POINT ( 'NONE',  ( 3.721466898765386500, -0.1629207441977159332, 2.200919931280575170 ) ) ;
#136637=CARTESIAN_POINT ( 'NONE',  ( 0.6255240776356413290, 0.2040786869749251498, -2.052575575099666150 ) ) ;
#136645=CARTESIAN_POINT ( 'NONE',  ( 2.805202726412972858, -1.722705984639979704, 1.148039668612794051 ) ) ;
#136650=CARTESIAN_POINT ( 'NONE',  ( 1.225266875139136458, 1.782313340379863442, 0.9499306202595361182 ) ) ;
#136655=CARTESIAN_POINT ( 'NONE',  ( 0.1749903794560748460, 0.004523422195302355051, -1.955468523092759314 ) ) ;
#136657=CARTESIAN_POINT ( 'NONE',  ( 6.643907658006512840, -0.09612306880287316280, -2.013924184692199137 ) ) ;
#136658=CARTESIAN_POINT ( 'NONE',  ( 6.298046708350548251, -0.9096110389208410529, -1.686033347247811731 ) ) ;
#136660=CARTESIAN_POINT ( 'NONE',  ( 3.421585747727782678, -1.306972202059282218, -1.759028276249123168 ) ) ;
#136662=CARTESIAN_POINT ( 'NONE',  ( 2.548957913124219044, 0.2380835140640500114, 1.897471792728817386 ) ) ;
#136666=CARTESIAN_POINT ( 'NONE',  ( 1.335564786618839817, 0.5826355126458090394, -1.930425043884366865 ) ) ;
#136668=CARTESIAN_POINT ( 'NONE',  ( 6.233935805145816467, 2.167428969419796125, 0.3234103439683775894 ) ) ;
#136670=CARTESIAN_POINT ( 'NONE',  ( 2.977275877015468364, 1.638319938685417476, -0.5394319952881917457 ) ) ;
#136672=CARTESIAN_POINT ( 'NONE',  ( 0.1394461523057084484, 7.629137130509043629, -2.319723760180956607 ) ) ;
#136676=CARTESIAN_POINT ( 'NONE',  ( 1.258172656280614365, -1.962046632281065461, -0.003472340283867945618 ) ) ;
#136679=CARTESIAN_POINT ( 'NONE',  ( 0.1399997263886020860, 0.7221123407896400392, -2.083281383436136558 ) ) ;
#136681=CARTESIAN_POINT ( 'NONE',  ( 4.020002786455856736, -1.806352922022226304, 0.1370799816429474904 ) ) ;
#136686=CARTESIAN_POINT ( 'NONE',  ( 5.320911890206324379, 1.367686037040320768, -1.187891890861958899 ) ) ;
#136690=CARTESIAN_POINT ( 'NONE',  ( 5.090230039108806892, 0.9569469540476289726, -1.596034515973473455 ) ) ;
#136692=CARTESIAN_POINT ( 'NONE',  ( 2.724132717865447084, 1.901453608201342238, 0.2316716071539808575 ) ) ;
#136701=CARTESIAN_POINT ( 'NONE',  ( 1.271554197678253839, 1.246673013970694077, 1.678101005879296004 ) ) ;
#136703=CARTESIAN_POINT ( 'NONE',  ( 6.036148348713140876, 0.9492135318787934262, -1.676240969703364891 ) ) ;
#136705=CARTESIAN_POINT ( 'NONE',  ( 2.168725436055967570, -1.667931858681595880, -0.7425449061374130855 ) ) ;
#136707=CARTESIAN_POINT ( 'NONE',  ( 2.267699027020404490, 0.5063876334258295975, -1.844086191983687062 ) ) ;
#136708=CARTESIAN_POINT ( 'NONE',  ( 1.539439451811152493, 1.821048954109681706, -0.7507764504887379786 ) ) ;
#136709=CARTESIAN_POINT ( 'NONE',  ( 3.790518096397344383, 1.638939831120878932, -1.041601972383674468 ) ) ;
#136714=CARTESIAN_POINT ( 'NONE',  ( 3.920270587443940080, -2.114697630030224929, 0.1593259359235904837 ) ) ;
#136721=CARTESIAN_POINT ( 'NONE',  ( 3.967279163243800255, 0.2216459979678051528, -1.812115712870238537 ) ) ;
#136722=CARTESIAN_POINT ( 'NONE',  ( 6.157435431667657610, 1.928259211291092123, -0.5899821858514133766 ) ) ;
#136727=CARTESIAN_POINT ( 'NONE',  ( 4.451927283622527654, 1.870250842541102410, -0.04591718433973044494 ) ) ;
#136729=CARTESIAN_POINT ( 'NONE',  ( 2.297378195909089982, 1.489297080225897574, 1.222053532002062903 ) ) ;
#136730=CARTESIAN_POINT ( 'NONE',  ( 6.877797714452785094, -1.903667959252927533, 0.4735691183095217527 ) ) ;
#136736=CARTESIAN_POINT ( 'NONE',  ( 1.142374532877686644, 0.8619398222155623124, 1.934021905983105416 ) ) ;
#136738=CARTESIAN_POINT ( 'NONE',  ( 5.120015143727554729, 2.048507142264085701, -0.2983452141967629645 ) ) ;
#136739=CARTESIAN_POINT ( 'NONE',  ( 0.6965153189463432204, 1.505040478001760107, 1.060415605250275339 ) ) ;
#136741=CARTESIAN_POINT ( 'NONE',  ( 5.924520554715382303, -1.662438412150448963, -1.587772413480701639 ) ) ;
#136745=CARTESIAN_POINT ( 'NONE',  ( 0.9555020568867471642, 0.4423240407584581035, -2.249030425913514541 ) ) ;
#136748=CARTESIAN_POINT ( 'NONE',  ( 6.193304230345664685, -0.6518728838521523627, 1.829399646200319252 ) ) ;
#136752=CARTESIAN_POINT ( 'NONE',  ( -0.05247892273943338681, -1.838936383286099652, 0.8197664084235550819 ) ) ;
#136753=CARTESIAN_POINT ( 'NONE',  ( 0.1333692844072559280, 0.001398348041498076455, -2.053671342968105051 ) ) ;
#136756=CARTESIAN_POINT ( 'NONE',  ( 2.660199397079235695, -1.441175001385604393, 1.514759066650630093 ) ) ;
#136757=CARTESIAN_POINT ( 'NONE',  ( 1.146904862891504173, -1.391901254704702273, -1.093021760518765539 ) ) ;
#136761=CARTESIAN_POINT ( 'NONE',  ( 4.013863964491473979, -1.177108192605724746, -1.966824220290509961 ) ) ;
#136762=CARTESIAN_POINT ( 'NONE',  ( 3.028976774107559944, -1.169381637243168903, -1.289075744332576878 ) ) ;
#136765=CARTESIAN_POINT ( 'NONE',  ( 3.655360161107966022, -0.3364991752431121808, -1.700650080047048318 ) ) ;
#136766=CARTESIAN_POINT ( 'NONE',  ( 4.053319971960964274, 1.836175303466779374, -1.158372938815607656 ) ) ;
#136768=CARTESIAN_POINT ( 'NONE',  ( 4.364470425680367249, -1.957169923074707274, -0.4852690807995581057 ) ) ;
#136769=CARTESIAN_POINT ( 'NONE',  ( 1.593750000000000666, -1.895863743164122983, -0.7852924748298991675 ) ) ;
#136771=CARTESIAN_POINT ( 'NONE',  ( 0.9910896068104644296, 1.700257414060426964, -0.9055851426933002601 ) ) ;
#136773=CARTESIAN_POINT ( 'NONE',  ( 4.693709758858874537, 2.072258576215581183, -0.8006532145865407069 ) ) ;
#136780=CARTESIAN_POINT ( 'NONE',  ( 0.1885310067011408963, 1.284270987554763765, 1.812239126532013689 ) ) ;
#136781=CARTESIAN_POINT ( 'NONE',  ( 5.441838459065293065, 1.316327937319297758, 1.454900926449454124 ) ) ;
#136784=CARTESIAN_POINT ( 'NONE',  ( 6.327429347084096101, -2.133486974870369313, 0.7532543551938327697 ) ) ;
#136787=CARTESIAN_POINT ( 'NONE',  ( 3.508308746731583216, 2.062851380131548229, 0.002797760368935045105 ) ) ;
#136793=CARTESIAN_POINT ( 'NONE',  ( 4.639837347815604751, 0.8015432297804045980, -1.690266223530467293 ) ) ;
#136795=CARTESIAN_POINT ( 'NONE',  ( 3.832397100292153524, 0.5799717274662331556, -1.634443932507266384 ) ) ;
#136796=CARTESIAN_POINT ( 'NONE',  ( 3.860698480431251411, 0.2083224649859614919, -1.727840645513075923 ) ) ;
#136797=CARTESIAN_POINT ( 'NONE',  ( 0.9961154782066735658, -2.292545471836278992, 0.006648471028786878678 ) ) ;
#136799=CARTESIAN_POINT ( 'NONE',  ( 4.405862271158119903, -0.8954353465763136288, -1.889446048457727789 ) ) ;
#136800=CARTESIAN_POINT ( 'NONE',  ( 0.005434845660363255178, -0.7843016415976924449, -1.664241202765592176 ) ) ;
#136802=CARTESIAN_POINT ( 'NONE',  ( 1.178361531996233280, 1.528742360773158282, 1.314995429398260196 ) ) ;
#136803=CARTESIAN_POINT ( 'NONE',  ( 0.5861907285475282947, -2.175377356269320828, -0.2643977408666315365 ) ) ;
#136807=CARTESIAN_POINT ( 'NONE',  ( 2.842561206135377994, 1.176089095116246153, -1.764248410475676820 ) ) ;
#136809=CARTESIAN_POINT ( 'NONE',  ( 5.531824841778981927, -1.161409778037244100, -1.408645805323349487 ) ) ;
#136815=CARTESIAN_POINT ( 'NONE',  ( 2.109634291106620818, 1.563931847922779728, 1.278184196155268904 ) ) ;
#136816=CARTESIAN_POINT ( 'NONE',  ( 0.4289210115673793844, 2.015304021226202558, 0.6111801191295732627 ) ) ;
#136818=CARTESIAN_POINT ( 'NONE',  ( 3.819077715518546690, -1.639399709636097713, -0.8806717989592935947 ) ) ;
#136824=CARTESIAN_POINT ( 'NONE',  ( 5.162654993523497993, -1.319871331358621669, 1.261628347558927166 ) ) ;
#136829=CARTESIAN_POINT ( 'NONE',  ( 0.8426186123336505407, -0.9696909581486823360, 1.437080622210512360 ) ) ;
#136830=CARTESIAN_POINT ( 'NONE',  ( 0.6029369919973374126, -1.732405018438128552, 0.1659646143751663805 ) ) ;
#136831=CARTESIAN_POINT ( 'NONE',  ( 5.865930957382810895, 2.274600175340906638, -0.3886535673101945143 ) ) ;
#136833=CARTESIAN_POINT ( 'NONE',  ( 1.300152579660202923, -2.060967562519558705, -0.002860995899278336550 ) ) ;
#136836=CARTESIAN_POINT ( 'NONE',  ( 0.2103132415818432799, -1.556605082263945228, -1.280954711483893727 ) ) ;
#136839=CARTESIAN_POINT ( 'NONE',  ( 5.401189721097995111, 1.529905263132097071, 1.076157610686766075 ) ) ;
#136840=( GEOMETRIC_REPRESENTATION_CONTEXT ( 3 ) GLOBAL_UNCERTAINTY_ASSIGNED_CONTEXT ( ( #99477 ) ) GLOBAL_UNIT_ASSIGNED_CONTEXT ( ( #108248, #159061, #158015 ) ) REPRESENTATION_CONTEXT ( 'NONE', 'WORKASPACE' ) );
#136841=CARTESIAN_POINT ( 'NONE',  ( 3.884940529579200774, -1.786240503712609895, -0.6835825222790415934 ) ) ;
#136843=CARTESIAN_POINT ( 'NONE',  ( 4.565167970240332274, -1.970479184476851886, -0.9938812724585781577 ) ) ;
#136849=CARTESIAN_POINT ( 'NONE',  ( 6.129554906816851556, -0.2598956320666659381, 2.104415924757463419 ) ) ;
#136851=CARTESIAN_POINT ( 'NONE',  ( 3.399772400530599370, 1.817812331725022101, 1.421335012277170629 ) ) ;
#136852=CARTESIAN_POINT ( 'NONE',  ( 3.771884902471400292, -1.933230903833718539, 0.3329965046865584477 ) ) ;
#136854=CARTESIAN_POINT ( 'NONE',  ( 0.8659734994756922433, -1.952832785578303199, 0.1866259229855102009 ) ) ;
#136858=CARTESIAN_POINT ( 'NONE',  ( 6.122279814772176643, 1.995267444086584296, 0.2910868170948808786 ) ) ;
#136861=CARTESIAN_POINT ( 'NONE',  ( 2.729531698892784242, 0.1106738598409856555, -2.168390435917330716 ) ) ;
#136863=CARTESIAN_POINT ( 'NONE',  ( 1.230900525853476868, 1.420129835883350955, -1.575055732827963295 ) ) ;
#136869=CARTESIAN_POINT ( 'NONE',  ( 0.5794586325245559832, 1.923780613697351427, -0.7393501692522960189 ) ) ;
#136871=CARTESIAN_POINT ( 'NONE',  ( 6.827182134110161726, 7.629137130509051623, 2.510944104600740356 ) ) ;
#136875=CARTESIAN_POINT ( 'NONE',  ( 4.020093958671668410, -1.906945023982812515, 0.1437811316862200317 ) ) ;
#136876=CARTESIAN_POINT ( 'NONE',  ( 5.471497560916138703, 1.704843785431299219, -0.4750155384096472755 ) ) ;
#136879=CARTESIAN_POINT ( 'NONE',  ( 0.07017708175168728413, 0.6932349927748741036, 1.673895389460538397 ) ) ;
#136881=CARTESIAN_POINT ( 'NONE',  ( 1.288148359701014600, -0.6930021182445024186, -1.786147582385696486 ) ) ;
#136882=CARTESIAN_POINT ( 'NONE',  ( 1.522023487246677798, 2.040062638832959241, -0.3519594530456415793 ) ) ;
#136884=CARTESIAN_POINT ( 'NONE',  ( 0.6023365795125863453, -0.6618663087945526602, -1.857178468014776263 ) ) ;
#136885=CARTESIAN_POINT ( 'NONE',  ( 3.334410585898534674, 1.781380905032422746, 0.3990451814587444024 ) ) ;
#136886=CARTESIAN_POINT ( 'NONE',  ( 0.2941754776928190429, 1.714430973684363257, 1.544913290951188012 ) ) ;
#136890=CARTESIAN_POINT ( 'NONE',  ( 4.088373676034792403, 1.106037789618707912, -1.740905279395239758 ) ) ;
#136895=CARTESIAN_POINT ( 'NONE',  ( 5.702208657235168232, -2.106147099624333219, -0.003344702849475410765 ) ) ;
#136897=CARTESIAN_POINT ( 'NONE',  ( 6.637176860265922684, -0.09746846054551477900, -2.068182370504913159 ) ) ;
#136899=CARTESIAN_POINT ( 'NONE',  ( 4.200566210393744448, -0.6737006675727378324, -2.054019326127386691 ) ) ;
#136900=CARTESIAN_POINT ( 'NONE',  ( 4.090493647085408746, -1.161108546167070488, 1.652349136562575760 ) ) ;
#136907=CARTESIAN_POINT ( 'NONE',  ( 2.817592499383800853, -1.357869084745389809, -1.490969456672403881 ) ) ;
#136912=CARTESIAN_POINT ( 'NONE',  ( 5.343983030329363615, -1.218012673290536974, -1.474316871017399944 ) ) ;
#136915=CARTESIAN_POINT ( 'NONE',  ( 4.728138764314923748, 2.011206665557175199, 0.1455158850461671372 ) ) ;
#136918=CARTESIAN_POINT ( 'NONE',  ( 6.686556848510641693, -1.692700875910668312, -0.3300756604382968362 ) ) ;
#136923=CARTESIAN_POINT ( 'NONE',  ( 5.219927230130699591, -0.9996001844756461363, -1.580852690948472361 ) ) ;
#136924=CARTESIAN_POINT ( 'NONE',  ( 6.521754290436940771, -0.4404898795188401106, 1.971875975034496742 ) ) ;
#136926=CARTESIAN_POINT ( 'NONE',  ( 1.956005403265232978, -0.7013823251572397499, 1.947930506816720087 ) ) ;
#136928=ORIENTED_EDGE ( 'NONE', *, *, #166608, .T. ) ;
#136930=CARTESIAN_POINT ( 'NONE',  ( 0.8257962581623284892, 0.8146080751335778025, -1.844719337431327544 ) ) ;
#136932=CARTESIAN_POINT ( 'NONE',  ( 1.669862777068024995, 1.806593842016694484, -0.1355503349984941153 ) ) ;
#136939=CARTESIAN_POINT ( 'NONE',  ( 6.556256410252866651, -1.173993033552203968, 1.514159254448317782 ) ) ;
#136947=CARTESIAN_POINT ( 'NONE',  ( 3.116266767097406909, -1.064116542966097922, -1.881565754655416756 ) ) ;
#136951=CARTESIAN_POINT ( 'NONE',  ( 1.178162429063234207, 2.088287186665960693, -0.3679680078583212333 ) ) ;
#136952=CARTESIAN_POINT ( 'NONE',  ( 6.071303273277399271, 0.1315155018670917386, -1.820917815106848359 ) ) ;
#136953=CARTESIAN_POINT ( 'NONE',  ( 1.844934828179781050, -1.667470251784016089, 1.051280099994149841 ) ) ;
#136954=CARTESIAN_POINT ( 'NONE',  ( 4.535362393419643645, -0.08824616237496611670, 1.910463848342447202 ) ) ;
#136955=FACE_OUTER_BOUND ( 'NONE', #104462, .T. ) ;
#136956=CARTESIAN_POINT ( 'NONE',  ( 4.633233401965040521, 0.002145104102065781716, -1.969739563307022712 ) ) ;
#136957=CARTESIAN_POINT ( 'NONE',  ( 0.9549039013059671399, 0.3793949951976150481, -1.904366508208689357 ) ) ;
#136963=CARTESIAN_POINT ( 'NONE',  ( 5.215449470722859360, 1.565665547294055715, 1.097690013397538022 ) ) ;
#136965=CARTESIAN_POINT ( 'NONE',  ( 0.9739772326014316528, 2.126351460888118883, -0.5901193814053447007 ) ) ;
#136967=CARTESIAN_POINT ( 'NONE',  ( 6.340495571224031401, 1.157139813629002756, -1.647119299906736556 ) ) ;
#136971=CARTESIAN_POINT ( 'NONE',  ( 3.104029480343179603, 0.7476448069429382226, -1.930825944200013966 ) ) ;
#136976=CARTESIAN_POINT ( 'NONE',  ( 1.147603855448702248, -1.704515299458901012, -1.329379018566230641 ) ) ;
#136981=CARTESIAN_POINT ( 'NONE',  ( 6.925078400183531713, 7.629137130509038300, 2.555651831298339616 ) ) ;
#136983=CARTESIAN_POINT ( 'NONE',  ( 5.625553438129872852, 0.3468616029342861951, 1.698903693450015684 ) ) ;
#136985=CARTESIAN_POINT ( 'NONE',  ( 3.748938768049938197, -0.3990674421511587466, -2.031259957477090428 ) ) ;
#136986=CARTESIAN_POINT ( 'NONE',  ( 4.095393968650405725, -0.3601260033815486539, 2.086223071001345630 ) ) ;
#136989=CARTESIAN_POINT ( 'NONE',  ( 2.606253914610905387, 1.968914028630329272, 0.05319026939461755227 ) ) ;
#136990=CARTESIAN_POINT ( 'NONE',  ( 0.8262462788446511830, -0.8622288892402606431, -1.707089296137359158 ) ) ;
#136991=CARTESIAN_POINT ( 'NONE',  ( 4.365347222306335873, 2.224029864950861857, -0.5546456485611241938 ) ) ;
#136992=CARTESIAN_POINT ( 'NONE',  ( 2.103868193876055503, -1.825329726703457833, 0.04394198290156441783 ) ) ;
#136996=CARTESIAN_POINT ( 'NONE',  ( 2.390887483786011014, -1.927808053674067823, -0.5802275739894193762 ) ) ;
#136997=CARTESIAN_POINT ( 'NONE',  ( 3.608209768781400761, 1.961936380018937331, 0.004537341891153179319 ) ) ;
#137000=CARTESIAN_POINT ( 'NONE',  ( 0.07536363704237906969, 4.084105538841027894, -2.698926661290324880 ) ) ;
#137001=CARTESIAN_POINT ( 'NONE',  ( 6.456985077987440924, 0.3587005216530990692, -2.059463350302393359 ) ) ;
#137002=CARTESIAN_POINT ( 'NONE',  ( 5.084699950150380232, -0.2187599903600515594, -1.756180685135479091 ) ) ;
#137005=CARTESIAN_POINT ( 'NONE',  ( 1.324469081069843623, 2.112754910877081560, 0.5817525768514880680 ) ) ;
#137006=CARTESIAN_POINT ( 'NONE',  ( -0.1123202547218312558, -0.3730905450354308206, -1.705658634530213602 ) ) ;
#137009=CARTESIAN_POINT ( 'NONE',  ( 0.3163000706473735879, -1.844146670390820475, 1.371622413452098233 ) ) ;
#137010=CARTESIAN_POINT ( 'NONE',  ( 0.01162390915069450026, -2.148011843722149372, 0.4338911918742721641 ) ) ;
#137011=CARTESIAN_POINT ( 'NONE',  ( 6.415404398373737216, 0.5482957075174756945, 1.644958459601528755 ) ) ;
#137012=CARTESIAN_POINT ( 'NONE',  ( 3.176612885197922953, -1.314426786483071208, 1.772596291930063739 ) ) ;
#137013=CARTESIAN_POINT ( 'NONE',  ( 0.2687526973377635797, -0.9260139170579514412, -1.961338766822422919 ) ) ;
#137015=CARTESIAN_POINT ( 'NONE',  ( 1.270887751945870336, -0.3167050496251391234, -2.093436144997854687 ) ) ;
#137016=CARTESIAN_POINT ( 'NONE',  ( 3.687500000000002665, -1.451031289060967788, 1.451031289061265550 ) ) ;
#137017=CARTESIAN_POINT ( 'NONE',  ( 6.727182134110222478, 7.629137130509071163, 2.789055895399249252 ) ) ;
#137018=CARTESIAN_POINT ( 'NONE',  ( 5.807627864512785898, -0.4676060548664852101, 1.868651349408587681 ) ) ;
#137020=CARTESIAN_POINT ( 'NONE',  ( 1.558568218312964326, -1.617219677351620089, 1.624929221499067600 ) ) ;
#137024=CARTESIAN_POINT ( 'NONE',  ( 3.440272213978716742, -1.324219266349660806, -1.783276862766651760 ) ) ;
#137027=EDGE_CURVE ( 'NONE', #82118, #185927, #147213, .T. ) ;
#137031=CARTESIAN_POINT ( 'NONE',  ( 1.442029965644067158, -1.730867108953790590, -1.034163949609874233 ) ) ;
#137033=CARTESIAN_POINT ( 'NONE',  ( 6.812941044521420686, -1.596950470092706853, 1.305146078352089845 ) ) ;
#137036=CARTESIAN_POINT ( 'NONE',  ( 0.04610459085982108324, -1.479553692838073475, 1.095721268101347734 ) ) ;
#137038=CARTESIAN_POINT ( 'NONE',  ( 1.791920237496129609, -1.760627435414298558, -0.1794978127376868071 ) ) ;
#137039=CARTESIAN_POINT ( 'NONE',  ( 0.0006249722829775038483, -1.976948959267275541, 0.3961041280396286890 ) ) ;
#137040=CARTESIAN_POINT ( 'NONE',  ( 6.462468575563847573, -1.595429648854440385, -0.6960047898553810564 ) ) ;
#137041=CARTESIAN_POINT ( 'NONE',  ( 4.124787647867947271, 0.1125639427311639490, 2.289740828591101174 ) ) ;
#137042=CARTESIAN_POINT ( 'NONE',  ( 3.908013947242465314, 1.300727540704300633, -1.303293010247716488 ) ) ;
#137046=CARTESIAN_POINT ( 'NONE',  ( 3.944226942909400346, 1.816763600636053688, 0.1792749827478901103 ) ) ;
#137047=CARTESIAN_POINT ( 'NONE',  ( 4.817029820108094995, 1.034167108704350024, -1.730865207599366240 ) ) ;
#137049=CARTESIAN_POINT ( 'NONE',  ( 2.923041840916926315, 2.129999922893408559, 0.7632657742467786610 ) ) ;
#137051=CARTESIAN_POINT ( 'NONE',  ( 0.1882882188262140766, -0.9905318517600868455, 1.858590670187587612 ) ) ;
#137053=CARTESIAN_POINT ( 'NONE',  ( 3.402844027952243167, 0.5003511028610057032, 2.008882729757965890 ) ) ;
#137056=CARTESIAN_POINT ( 'NONE',  ( 5.672555391165950311, 0.8593836824349295744, 1.938725756316476589 ) ) ;
#137059=CARTESIAN_POINT ( 'NONE',  ( 1.523919215901398783, -1.069746099203742418, -1.602010878309991559 ) ) ;
#137061=CARTESIAN_POINT ( 'NONE',  ( 6.631706394207740551, 1.885626601332585306, -0.5685293109318545479 ) ) ;
#137066=CARTESIAN_POINT ( 'NONE',  ( 0.8619570425896695420, -1.755772037458620316, -1.360811342731186979 ) ) ;
#137067=CARTESIAN_POINT ( 'NONE',  ( 3.083145409929681335, -0.1532580487927890645, -2.100430568508942830 ) ) ;
#137070=CARTESIAN_POINT ( 'NONE',  ( 0.5372768211588532239, 1.738583335619352077, -0.6644854061606010331 ) ) ;
#137075=CARTESIAN_POINT ( 'NONE',  ( 1.090261293813089560, 1.267680250814690934, 1.699812782343253170 ) ) ;
#137078=CARTESIAN_POINT ( 'NONE',  ( 3.543363863352413823, 1.774678991803163575, -0.8365776047038612218 ) ) ;
#137079=CARTESIAN_POINT ( 'NONE',  ( 2.483474991488154870, 1.976725341044349271, -0.8753317036461552014 ) ) ;
#137080=CARTESIAN_POINT ( 'NONE',  ( 1.206327419354651820, 1.623952629372883427, 0.8676893986077349741 ) ) ;
#137083=CARTESIAN_POINT ( 'NONE',  ( 3.802475355173411842, 1.493833042257145305, 0.8925963562203437229 ) ) ;
#137087=CARTESIAN_POINT ( 'NONE',  ( 0.7784641540938314064, -1.199969256800371697, 1.797863220954009966 ) ) ;
#137089=CARTESIAN_POINT ( 'NONE',  ( 3.848982377512807140, -0.9961485462514390044, 1.752762419822328832 ) ) ;
#137091=CARTESIAN_POINT ( 'NONE',  ( 0.5323697292517782786, 1.110078392871534314, -1.854780036684190669 ) ) ;
#137093=CARTESIAN_POINT ( 'NONE',  ( 3.696128747971284323, -1.969148060776576337, -0.09815990810512796594 ) ) ;
#137095=CARTESIAN_POINT ( 'NONE',  ( 6.509000000000035868, 7.629137130509092479, 2.600000000000000977 ) ) ;
#137096=CARTESIAN_POINT ( 'NONE',  ( 2.788543057918268619, 1.664307371569521132, -1.000645113138714848 ) ) ;
#137105=CARTESIAN_POINT ( 'NONE',  ( 6.493248230727125758, 2.012220109224418518, -1.129477038640940734 ) ) ;
#137107=CARTESIAN_POINT ( 'NONE',  ( 4.575024454672827368, 1.791946274209740952, 0.7988320279663924106 ) ) ;
#137109=CARTESIAN_POINT ( 'NONE',  ( 1.529922885524273912, -1.701946718671920600, 1.081067414773040802 ) ) ;
#137111=CARTESIAN_POINT ( 'NONE',  ( 2.132168502032088409, 2.116975549207784635, 0.04667972686168975205 ) ) ;
#137115=CARTESIAN_POINT ( 'NONE',  ( 3.169683937527142170, -1.096016708463069422, 1.479218548343118389 ) ) ;
#137119=CARTESIAN_POINT ( 'NONE',  ( 4.060867369437678676, 0.5686956411946364476, 2.042824496258560441 ) ) ;
#137122=CARTESIAN_POINT ( 'NONE',  ( 4.358703909566331802, -1.529595902882211256, 1.381216288725060082 ) ) ;
#137124=CARTESIAN_POINT ( 'NONE',  ( 2.384105128782065819, -0.3166398734758494315, -1.813660976904336808 ) ) ;
#137130=CARTESIAN_POINT ( 'NONE',  ( 1.787996309160574837, 1.523479866092191548, 1.596893430481533649 ) ) ;
#137131=CARTESIAN_POINT ( 'NONE',  ( 3.321791363677785380, -2.181432725256218674, 0.5997193178089550436 ) ) ;
#137133=CARTESIAN_POINT ( 'NONE',  ( 3.058660868685322498, 0.4446918012569016643, 1.755998500949424113 ) ) ;
#137135=CARTESIAN_POINT ( 'NONE',  ( 3.924928585964591932, -1.664043332733669667, 0.9490909334420574162 ) ) ;
#137136=CARTESIAN_POINT ( 'NONE',  ( 5.406714943436663035, 0.5975561702324573288, 1.982271326387271770 ) ) ;
#137139=CARTESIAN_POINT ( 'NONE',  ( 4.311372413323046437, -0.3381597629931332172, 1.942102657548309796 ) ) ;
#137140=CARTESIAN_POINT ( 'NONE',  ( 1.500868375504460728, 1.576442195784112155, -1.106916717273882300 ) ) ;
#137141=CARTESIAN_POINT ( 'NONE',  ( 4.750782166719051069, -1.502237938222051650, 1.114538048626475986 ) ) ;
#137142=CARTESIAN_POINT ( 'NONE',  ( 3.123938245303990335, -2.224009237659807958, 0.6155878327348850432 ) ) ;
#137143=CARTESIAN_POINT ( 'NONE',  ( 4.299146511743386689, -1.619905129461503224, 0.9160139579608633786 ) ) ;
#137147=CARTESIAN_POINT ( 'NONE',  ( 2.086679739605776351, -2.065639965682735557, -0.4097663305358787977 ) ) ;
#137152=CARTESIAN_POINT ( 'NONE',  ( 3.217144136595586179, 1.669276650691432495, -1.307696563879121365 ) ) ;
#137154=CARTESIAN_POINT ( 'NONE',  ( 1.230729765704338563, 1.353420925896263061, -1.499466043412321703 ) ) ;
#137161=CARTESIAN_POINT ( 'NONE',  ( 1.774925396934714295, -2.051924176137665423, -0.6798970441593693570 ) ) ;
#137162=CARTESIAN_POINT ( 'NONE',  ( 6.610000000000018083, 6.039292104641935666, 2.314898989754467618 ) ) ;
#137164=CARTESIAN_POINT ( 'NONE',  ( 6.925078400183546812, 2.074047572655359328, 2.163550030515603684 ) ) ;
#137167=CARTESIAN_POINT ( 'NONE',  ( 6.262907710099243630, -0.1037740067610822270, -2.014008436551452785 ) ) ;
#137169=CARTESIAN_POINT ( 'NONE',  ( 6.444877668667830406, -1.679477184941297496, -1.245029935506683838 ) ) ;
#137171=CARTESIAN_POINT ( 'NONE',  ( 0.6555950923613624859, -1.913042455388717311, -1.207739878423098823 ) ) ;
#137178=CARTESIAN_POINT ( 'NONE',  ( 2.631144668424452604, -1.609571295485120457, 0.6205441041484575093 ) ) ;
#137180=CARTESIAN_POINT ( 'NONE',  ( 2.530210103492841256, 1.715365446638704494, 0.4347029418121580169 ) ) ;
#137182=CARTESIAN_POINT ( 'NONE',  ( 2.613933768341146102, -0.6292564844058865514, 1.912298747220711359 ) ) ;
#137184=CARTESIAN_POINT ( 'NONE',  ( 5.561621765989873900, 0.4355406452380207738, -2.163202247768724718 ) ) ;
#137186=CARTESIAN_POINT ( 'NONE',  ( 4.552993113364055766, 0.3493383367317858257, 1.989188622967730025 ) ) ;
#137188=CARTESIAN_POINT ( 'NONE',  ( 4.494861206476631565, -2.057060146276223023, -0.5143016718046622415 ) ) ;
#137189=CARTESIAN_POINT ( 'NONE',  ( 4.341422844945469706, 0.4390097190783425196, -1.967893369681630533 ) ) ;
#137190=CARTESIAN_POINT ( 'NONE',  ( 4.377109366116209266, -1.621248278760094363, -0.8084319655582442588 ) ) ;
#137194=CARTESIAN_POINT ( 'NONE',  ( 1.147088892781012781, -1.472398045354219587, -1.153743250124287689 ) ) ;
#137196=CARTESIAN_POINT ( 'NONE',  ( 5.672461423068217989, 0.7400952288921599509, 1.653588109013460095 ) ) ;
#137202=CARTESIAN_POINT ( 'NONE',  ( 0.6856317642073318508, 1.842354612247762091, -0.5124485439033445999 ) ) ;
#137204=CARTESIAN_POINT ( 'NONE',  ( 1.328483007144948935, -1.247240240105648601, 1.514344512384787622 ) ) ;
#137208=CARTESIAN_POINT ( 'NONE',  ( 3.621431001533811589, 1.820626359085864454, 1.087046460333654485 ) ) ;
#137209=CARTESIAN_POINT ( 'NONE',  ( -0.1294898018152226826, 6.948707995275583471, -2.521562306467279857 ) ) ;
#137211=CARTESIAN_POINT ( 'NONE',  ( 5.800065155369113157, -1.971530342684927772, -0.002616305567698303924 ) ) ;
#137213=CARTESIAN_POINT ( 'NONE',  ( 1.248292583380994136, 0.9887404755159521219, -1.753579541237253903 ) ) ;
#137216=CARTESIAN_POINT ( 'NONE',  ( 1.177538910780148385, 1.606043500598727247, 1.379722209976147251 ) ) ;
#137218=CARTESIAN_POINT ( 'NONE',  ( 2.436061438456170958, 1.271862942251865691, 1.633573898902056731 ) ) ;
#137219=VERTEX_POINT ( 'NONE', #82641 ) ;
#137223=CARTESIAN_POINT ( 'NONE',  ( 4.347661206880347073, 2.090185315053775472, -0.05106478779118817091 ) ) ;
#137225=CARTESIAN_POINT ( 'NONE',  ( 2.959763373685083909, 1.816946311034864703, -0.1772020141349931188 ) ) ;
#137226=CARTESIAN_POINT ( 'NONE',  ( 1.418313031307829153, -0.6519236697288594007, -1.690267533947023892 ) ) ;
#137228=CARTESIAN_POINT ( 'NONE',  ( 6.129534211984397629, -2.079372889712034489, 0.7396383780838566846 ) ) ;
#137229=CARTESIAN_POINT ( 'NONE',  ( 4.155453238874762256, -1.833011353516471154, -1.228491751752130323 ) ) ;
#137232=CARTESIAN_POINT ( 'NONE',  ( 3.404848115249804685, -0.3755933644018424888, -1.874856250562627391 ) ) ;
#137235=CARTESIAN_POINT ( 'NONE',  ( 6.584440175795505112, 1.195396180001909059, -1.690200020538407566 ) ) ;
#137237=CARTESIAN_POINT ( 'NONE',  ( 5.601184584505256581, -0.5335315006234629953, 2.125516261704554211 ) ) ;
#137242=CARTESIAN_POINT ( 'NONE',  ( 3.057714436724996876, 1.861869414292870006, -0.1796979844640861634 ) ) ;
#137249=CARTESIAN_POINT ( 'NONE',  ( 6.789897376884641567, -1.347643488625469121, -1.571692526165118009 ) ) ;
#137250=CARTESIAN_POINT ( 'NONE',  ( 1.265250157614560278, 1.862010354082012098, -0.7743342583275418800 ) ) ;
#137254=CARTESIAN_POINT ( 'NONE',  ( 1.658417429842372393, -1.548019161032044844, 1.551412955586493947 ) ) ;
#137255=CARTESIAN_POINT ( 'NONE',  ( 6.727182134110222478, 0.005875948494733079785, 1.810970247402940547 ) ) ;
#137262=CARTESIAN_POINT ( 'NONE',  ( 3.473999211503727036, -1.775402473473717935, -0.4878004006634574230 ) ) ;
#137263=CARTESIAN_POINT ( 'NONE',  ( 1.119790083981372142, -0.4868965817936173335, 1.953217858147300090 ) ) ;
#137264=CARTESIAN_POINT ( 'NONE',  ( 1.581885565347431966, 1.542867095709683056, -1.703685752350136751 ) ) ;
#137266=CARTESIAN_POINT ( 'NONE',  ( 6.086763564210844635, 1.889667650816441391, 0.5265613530214608984 ) ) ;
#137269=CARTESIAN_POINT ( 'NONE',  ( 3.937688585161042809, -1.828529804631402023, 0.5600222464785462595 ) ) ;
#137273=CARTESIAN_POINT ( 'NONE',  ( 2.278955919255227336, 1.910372346673551602, -0.8499720230255493059 ) ) ;
#137274=CARTESIAN_POINT ( 'NONE',  ( 0.8834254411415434216, 1.253375741028007084, 1.388844808110502038 ) ) ;
#137275=CARTESIAN_POINT ( 'NONE',  ( 1.651720012567552853, -0.2930234437087535504, -1.994564656426714988 ) ) ;
#137278=CARTESIAN_POINT ( 'NONE',  ( 2.717972786412402364, 1.639536828598524121, 0.5844088115515410076 ) ) ;
#137282=CARTESIAN_POINT ( 'NONE',  ( 4.424228590228207914, 1.058368455644955963, -1.361911123238012111 ) ) ;
#137283=CARTESIAN_POINT ( 'NONE',  ( 3.456733517523991051, -1.933646301634945885, -1.031433503814835007 ) ) ;
#137284=CARTESIAN_POINT ( 'NONE',  ( 6.182275136424624229, -1.184133725572718676, 1.862117674348878760 ) ) ;
#137287=CARTESIAN_POINT ( 'NONE',  ( 3.538082186586584577, 1.373364251514897383, 1.681533162179976060 ) ) ;
#137288=CARTESIAN_POINT ( 'NONE',  ( 2.402731849113007190, 1.466575434288765800, -1.087121784572639527 ) ) ;
#137289=CARTESIAN_POINT ( 'NONE',  ( 0.4968289091572677396, 0.3296062100675010154, 1.933703066120408431 ) ) ;
#137290=CARTESIAN_POINT ( 'NONE',  ( 4.962167979565689002, -1.173633690672538865, 1.762117774576977602 ) ) ;
#137293=CARTESIAN_POINT ( 'NONE',  ( 4.827800031893906052, 1.179792396777184615, -1.965320743881134646 ) ) ;
#137298=CARTESIAN_POINT ( 'NONE',  ( 0.4344390223590781641, -1.137927343861804053, -1.789123301873453364 ) ) ;
#137304=CARTESIAN_POINT ( 'NONE',  ( 4.869767617671093340, -0.2496050341583149201, -2.000857388266870984 ) ) ;
#137306=CARTESIAN_POINT ( 'NONE',  ( 3.520431386055590917, 0.9232258726861832798, 1.844449542969233358 ) ) ;
#137308=CARTESIAN_POINT ( 'NONE',  ( -0.2409995289980246813, 5.721856934700204178, -2.594540323675114113 ) ) ;
#137311=CARTESIAN_POINT ( 'NONE',  ( 6.123007039855313138, -2.064672272812938747, 0.7349105657750015785 ) ) ;
#137312=CARTESIAN_POINT ( 'NONE',  ( 4.289685514112329123, 1.556909497225898109, -1.281360267751927129 ) ) ;
#137313=CARTESIAN_POINT ( 'NONE',  ( 3.192734241421916419, 1.453351889590439816, 1.130385295574042104 ) ) ;
#137316=CARTESIAN_POINT ( 'NONE',  ( 0.9380131109506375520, 1.698111720264935620, 0.3011209518388803241 ) ) ;
#137318=CARTESIAN_POINT ( 'NONE',  ( 0.5460333347737976739, -1.659586600764794584, 1.590741637488497062 ) ) ;
#137320=CARTESIAN_POINT ( 'NONE',  ( 6.579017896966585788, -0.1030185651522512180, -2.260299859776133236 ) ) ;
#137321=CARTESIAN_POINT ( 'NONE',  ( 3.352270206574393008, 2.106257355090755290, -0.0002192025019883553090 ) ) ;
#137325=CARTESIAN_POINT ( 'NONE',  ( 5.625000000000003553, -2.052068128417940951, 3.204627906038193246E-13 ) ) ;
#137331=CARTESIAN_POINT ( 'NONE',  ( 3.428187820690358656, -2.188011084934568196, 0.3830038565930964367 ) ) ;
#137332=CARTESIAN_POINT ( 'NONE',  ( 2.748186945943337012, 0.7392028471469231921, 2.063141171074922120 ) ) ;
#137335=CARTESIAN_POINT ( 'NONE',  ( 5.266048140081638351, -1.952571265509401854, 0.1905133553196102503 ) ) ;
#137337=CARTESIAN_POINT ( 'NONE',  ( 6.610000000000042952, 1.321253023796984172, 1.840686448008920229 ) ) ;
#137339=CARTESIAN_POINT ( 'NONE',  ( 4.394861267144759331, -2.057662932662501110, -0.5123870273424437904 ) ) ;
#137343=CARTESIAN_POINT ( 'NONE',  ( 5.155217493315787713, -1.824165352752779246, -1.159627250419709155 ) ) ;
#137345=CARTESIAN_POINT ( 'NONE',  ( 5.073706409418358376, -1.018251046719556685, 1.533866337327425056 ) ) ;
#137348=CARTESIAN_POINT ( 'NONE',  ( 6.333937804992649134, 1.722499169431927601, 0.2476611369811829999 ) ) ;
#137353=CARTESIAN_POINT ( 'NONE',  ( 4.645497774645744649, -1.668943667408796294, -1.373881373981879594 ) ) ;
#137354=EDGE_CURVE ( 'NONE', #106915, #185927, #120842, .T. ) ;
#137357=CARTESIAN_POINT ( 'NONE',  ( 3.836934241894359054, 0.3148432204054998351, 2.138525872868973998 ) ) ;
#137358=CARTESIAN_POINT ( 'NONE',  ( 4.604731966549804767, 1.525920046185350376, -1.248162976031294003 ) ) ;
#137359=CARTESIAN_POINT ( 'NONE',  ( 3.795997188448175130, -1.602592684597732298, 0.6622489764130984335 ) ) ;
#137360=CARTESIAN_POINT ( 'NONE',  ( 1.083813775577105565, -0.9808430935620198188, 1.959877696171570927 ) ) ;
#137361=CARTESIAN_POINT ( 'NONE',  ( 2.538448204128932240, 1.088115672400795431, -2.034946615453626872 ) ) ;
#137362=CARTESIAN_POINT ( 'NONE',  ( 3.971991334398959239, 1.141669855754149365, 1.715422085859653833 ) ) ;
#137363=CARTESIAN_POINT ( 'NONE',  ( 6.110880135979408045, -0.2334805506369178330, 1.927903797987507106 ) ) ;
#137369=CARTESIAN_POINT ( 'NONE',  ( 3.118423654462946892, -1.086285162511631652, -1.920806481261853493 ) ) ;
#137372=CARTESIAN_POINT ( 'NONE',  ( 1.129495572712395646, 1.795378659943444033, -0.4894723102292392047 ) ) ;
#137374=CARTESIAN_POINT ( 'NONE',  ( -0.02919842301645457147, -0.002306431287177941429, -2.073770398395402115 ) ) ;
#137377=CARTESIAN_POINT ( 'NONE',  ( 6.925078400183553029, 2.042159606913606762, 2.349846261904017464 ) ) ;
#137378=CARTESIAN_POINT ( 'NONE',  ( 6.421814705521882161, 1.055779539018763646, -1.508159643570324393 ) ) ;
#137380=CARTESIAN_POINT ( 'NONE',  ( 3.713790661510278923, -2.030684131657393365, 0.3505542424454102246 ) ) ;
#137386=CARTESIAN_POINT ( 'NONE',  ( 2.166935907724653720, -1.883791910722651952, -0.8362540481525667646 ) ) ;
#137391=CARTESIAN_POINT ( 'NONE',  ( 5.391335350415090488, 1.947751002805158560, -1.037606470750504828 ) ) ;
#137392=CARTESIAN_POINT ( 'NONE',  ( 0.3862812426984676972, -1.019270635400490121, 1.906220128828392646 ) ) ;
#137394=CARTESIAN_POINT ( 'NONE',  ( 0.6379081216283178923, 2.014007883293071899, -0.1037844182863178755 ) ) ;
#137398=CARTESIAN_POINT ( 'NONE',  ( 2.166681600665042229, -1.709288833360942617, -0.7604731621856930524 ) ) ;
#137400=CARTESIAN_POINT ( 'NONE',  ( 3.292204118033771110, -0.8216723425069611952, -1.841733987974409237 ) ) ;
#137403=CARTESIAN_POINT ( 'NONE',  ( 4.916683514525310272, 1.453009998446822992, -1.524801812277425839 ) ) ;
#137408=CARTESIAN_POINT ( 'NONE',  ( 4.412371012857700947, -2.019438640443659505, -0.04532404540058888875 ) ) ;
#137410=CARTESIAN_POINT ( 'NONE',  ( 6.215292634054179643, -1.767141628190834757, -1.063693359622622125 ) ) ;
#137413=CARTESIAN_POINT ( 'NONE',  ( 5.940740243836844847, 0.4152237956781511530, 2.121177236311201586 ) ) ;
#137419=CARTESIAN_POINT ( 'NONE',  ( 3.561125603554469610, 1.713606050895712718, -1.333181090037469652 ) ) ;
#137422=CARTESIAN_POINT ( 'NONE',  ( 2.050122339901743196, -1.422379512129726908, 1.169167124061460949 ) ) ;
#137424=CARTESIAN_POINT ( 'NONE',  ( 3.702820756938397295, 1.880440254450808757, 1.125299312022425280 ) ) ;
#137425=CARTESIAN_POINT ( 'NONE',  ( 6.883263157960365142, -0.007059606330772279746, 2.153658854459541416 ) ) ;
#137426=CARTESIAN_POINT ( 'NONE',  ( 4.100629699907013759, -0.7064081464536530186, -2.149486123859779330 ) ) ;
#137428=B_SPLINE_CURVE_WITH_KNOTS ( 'NONE', 3,
 ( #213096, #14891, #99377, #98308, #67898, #83103, #117824, #165430, #183814, #113559, #182741 ),
 .UNSPECIFIED., .F., .F.,
 ( 4, 1, 1, 1, 1, 1, 1, 1, 4 ),
 ( 0.000000000000000000, 0.2255619619413396781, 0.3975297875667437308, 0.5250373104567740423, 0.6172314665434700531, 0.6832587661106447330, 0.7322037845459880012, 0.7729093456892226488, 1.000000000000000000 ),
 .UNSPECIFIED. ) ;
#137434=CARTESIAN_POINT ( 'NONE',  ( 5.465970981792784400, 0.8728298736929670509, 1.539401198699318352 ) ) ;
#137436=CARTESIAN_POINT ( 'NONE',  ( 3.387361027847039185, 0.04724124570358113201, -2.012690625139363032 ) ) ;
#137438=CARTESIAN_POINT ( 'NONE',  ( 2.274573006691050558, -1.296483931956838198, 1.659472957066634669 ) ) ;
#137441=CARTESIAN_POINT ( 'NONE',  ( 0.6780957659633795043, -1.050550344063156061, -1.665771736420356808 ) ) ;
#137444=CARTESIAN_POINT ( 'NONE',  ( 5.590068458682615038, 1.086043493620889144, 1.449778898616445488 ) ) ;
#137449=CARTESIAN_POINT ( 'NONE',  ( 4.645289301550183936, -1.446173438076237217, -1.186536486241091204 ) ) ;
#137452=CARTESIAN_POINT ( 'NONE',  ( 5.383670357325340383, -1.967593191946028996, 0.6441560278484457225 ) ) ;
#137463=CARTESIAN_POINT ( 'NONE',  ( 5.055110333045015558, 1.632132345252810035, -1.088295032039228172 ) ) ;
#137466=CARTESIAN_POINT ( 'NONE',  ( 2.143907462275076892, -0.09611812122205246056, -2.013924455302518624 ) ) ;
#137468=CARTESIAN_POINT ( 'NONE',  ( 0.08191350661116909848, -1.027414926483052326, 1.935800647029708665 ) ) ;
#137470=CARTESIAN_POINT ( 'NONE',  ( 2.530351333283612281, 1.813318468827030072, 0.4585936022679508728 ) ) ;
#137472=CARTESIAN_POINT ( 'NONE',  ( 4.517842040498582179, -0.5326873650394120530, 1.941415848259191446 ) ) ;
#137475=CARTESIAN_POINT ( 'NONE',  ( 4.095393968650405725, -0.3601260033815486539, 2.086223071001345630 ) ) ;
#137477=CARTESIAN_POINT ( 'NONE',  ( 6.197728532230423859, -1.496850047335227085, -1.430563974149069661 ) ) ;
#137478=CARTESIAN_POINT ( 'NONE',  ( 1.101248736683122953, -0.5045743719560727980, 2.028828713580214771 ) ) ;
#137479=CARTESIAN_POINT ( 'NONE',  ( 6.720655732516644498, 4.691561721546229968, 2.636312907496433322 ) ) ;
#137480=CARTESIAN_POINT ( 'NONE',  ( 6.264658373536385660, -1.288822541704701452, 1.293195164663100583 ) ) ;
#137488=CARTESIAN_POINT ( 'NONE',  ( 0.5745104438982637785, -1.313040981126518902, 1.248171054211825171 ) ) ;
#137495=CARTESIAN_POINT ( 'NONE',  ( 5.624625116526842383, 0.3961212581503182339, 1.976953148079656719 ) ) ;
#137498=CARTESIAN_POINT ( 'NONE',  ( -0.1394461523061195918, 6.947787103499363681, -2.875373568546248482 ) ) ;
#137501=CARTESIAN_POINT ( 'NONE',  ( 3.994935505748583360, 0.2844874371618256736, 1.948636269439333546 ) ) ;
#137502=CARTESIAN_POINT ( 'NONE',  ( 4.359000025081374297, -0.002827702239943663542, -2.016598147179492262 ) ) ;
#137505=CARTESIAN_POINT ( 'NONE',  ( 5.103566685217446164, -2.181124530238859993, 0.2125310249164805709 ) ) ;
#137507=CARTESIAN_POINT ( 'NONE',  ( 3.329043352767379282, 0.04595412404927168293, 1.925998307505512486 ) ) ;
#137510=CARTESIAN_POINT ( 'NONE',  ( 0.4170028235400899397, 1.518763190251697370, -1.601383572969114599 ) ) ;
#137515=CARTESIAN_POINT ( 'NONE',  ( 5.524252356588593926, 0.9672068372908498857, 1.715464803677963834 ) ) ;
#137517=CARTESIAN_POINT ( 'NONE',  ( -0.006442494416806704600, -1.941642170872309281, -0.04679624317607820189 ) ) ;
#137518=CARTESIAN_POINT ( 'NONE',  ( 3.492840887459470522, -1.940756296261561209, -0.5346130827820451126 ) ) ;
#137519=CARTESIAN_POINT ( 'NONE',  ( 5.466298696655274902, 1.874607906009964964, 1.329618201824170898 ) ) ;
#137521=CARTESIAN_POINT ( 'NONE',  ( 2.957670719111748614, -0.5886736602933821949, 1.765425544305933014 ) ) ;
#137528=CARTESIAN_POINT ( 'NONE',  ( 6.216366674833015971, 1.951045902775162322, 0.7519257042096252341 ) ) ;
#137532=CARTESIAN_POINT ( 'NONE',  ( 0.6272434487209905818, -1.734552980249819631, 0.5698080454362154379 ) ) ;
#137534=CARTESIAN_POINT ( 'NONE',  ( 2.250263858207638634, 1.700335624809163004, -0.3396627995243851061 ) ) ;
#137536=CARTESIAN_POINT ( 'NONE',  ( 6.609000000000052388, 1.285212548570794588, 2.017169166534539038 ) ) ;
#137540=CARTESIAN_POINT ( 'NONE',  ( 0.6903901511902330590, 1.067356595782501749, -1.773781848916009096 ) ) ;
#137541=CARTESIAN_POINT ( 'NONE',  ( 5.654876981934024549, -1.436564326775534806, 1.126588154728463742 ) ) ;
#137542=CARTESIAN_POINT ( 'NONE',  ( 3.555471618195928496, 1.543666060651678551, 1.210462546525910010 ) ) ;
#137546=CARTESIAN_POINT ( 'NONE',  ( 3.598385148150527346, -1.043669326629501848, 1.845773325594574077 ) ) ;
#137550=CARTESIAN_POINT ( 'NONE',  ( 1.586871713678970730, 1.994102569620255228, 0.5559867524188369936 ) ) ;
#137553=CARTESIAN_POINT ( 'NONE',  ( 4.354274701107041956, 0.9498992632326860308, -2.008065553403962422 ) ) ;
#137555=CARTESIAN_POINT ( 'NONE',  ( 1.301886090224623205, 1.538925899722990431, -1.707713671238730635 ) ) ;
#137557=CARTESIAN_POINT ( 'NONE',  ( 0.5495624486224826022, 1.449728300881658383, 1.321815246172884040 ) ) ;
#137564=CARTESIAN_POINT ( 'NONE',  ( 2.601700882821424976, 1.355260107747566334, 1.349524769375435973 ) ) ;
#137566=CARTESIAN_POINT ( 'NONE',  ( 4.190264469598516506, -1.706116514292443931, -0.2520994348873573654 ) ) ;
#137567=CARTESIAN_POINT ( 'NONE',  ( 2.114470590943520634, 1.957170936680457052, 0.4852650170619755565 ) ) ;
#137568=CARTESIAN_POINT ( 'NONE',  ( 4.465672607755381662, -2.229637596627360718, -0.5588700134179708234 ) ) ;
#137569=CARTESIAN_POINT ( 'NONE',  ( 3.479979345725477291, 1.432071248269211505, 1.751504329374527158 ) ) ;
#137570=CARTESIAN_POINT ( 'NONE',  ( 6.235009869002534622, 0.2045095422857303724, 2.096118580758222549 ) ) ;
#137572=CARTESIAN_POINT ( 'NONE',  ( 4.253014324580971284, -1.470476824294727702, -0.9843664617138027095 ) ) ;
#137574=CARTESIAN_POINT ( 'NONE',  ( 1.113678556162515543, -2.235424308229993162, 0.5066684154252357741 ) ) ;
#137575=CARTESIAN_POINT ( 'NONE',  ( 6.140549721451361798, -1.552764191669778304, 0.9890077265983505672 ) ) ;
#137577=CARTESIAN_POINT ( 'NONE',  ( 5.982419568921025999, -0.3181065885738461607, -2.168126298386578110 ) ) ;
#137581=CARTESIAN_POINT ( 'NONE',  ( 5.353992430378140099, -0.7485205528568983357, 1.930488744064068785 ) ) ;
#137582=CARTESIAN_POINT ( 'NONE',  ( 0.9367328597341374463, -1.586666764284098807, 1.244388658875786424 ) ) ;
#137585=CARTESIAN_POINT ( 'NONE',  ( 4.635331898966036590, -1.760702172612697458, 0.7822757977788937778 ) ) ;
#137587=CARTESIAN_POINT ( 'NONE',  ( 0.9498388403609931974, -2.005144016916958982, 0.9564107486674018332 ) ) ;
#137594=CARTESIAN_POINT ( 'NONE',  ( 4.440767568709752311, -1.349020001278607550, -1.099687749275481741 ) ) ;
#137596=CARTESIAN_POINT ( 'NONE',  ( 2.471086628630547288, 1.751123931924388089, 0.8847596551376719631 ) ) ;
#137602=CARTESIAN_POINT ( 'NONE',  ( 0.1333542156527478262, 0.001576319744088505292, -2.046049510433409768 ) ) ;
#137605=CARTESIAN_POINT ( 'NONE',  ( 4.874232570624013050, -2.001857581374043349, -0.2420344392276354561 ) ) ;
#137606=CARTESIAN_POINT ( 'NONE',  ( 0.7258825447220511595, -2.147484179761431022, 0.7124928158122600941 ) ) ;
#137608=EDGE_LOOP ( 'NONE', ( #25716, #84523, #192060, #198418 ) ) ;
#137610=CARTESIAN_POINT ( 'NONE',  ( 1.528351178377739927, 1.801267752838480840, 0.5040548479407629401 ) ) ;
#137611=CARTESIAN_POINT ( 'NONE',  ( 0.3692042219665427893, -0.2092721526018372635, -1.721406745681583583 ) ) ;
#137613=CARTESIAN_POINT ( 'NONE',  ( 3.720431430916489646, 2.081484170424623859, 0.6860852429351402826 ) ) ;
#137614=CARTESIAN_POINT ( 'NONE',  ( 5.754963864978503985, -1.823789643192383014, 1.413694633616706886 ) ) ;
#137615=CARTESIAN_POINT ( 'NONE',  ( 6.784453644556415419, -2.020073987206136401, -0.4066529033334795873 ) ) ;
#137616=CARTESIAN_POINT ( 'NONE',  ( 2.185399619353834311, -0.8303394849570409075, 1.755606585091240568 ) ) ;
#137621=CARTESIAN_POINT ( 'NONE',  ( 2.953750172290268150, -1.864168560446223033, -0.7691209412190866956 ) ) ;
#137625=CARTESIAN_POINT ( 'NONE',  ( 0.9788029507734037349, -0.04229004422508231970, -1.825371421953936757 ) ) ;
#137631=CARTESIAN_POINT ( 'NONE',  ( 0.3038912542124502236, -0.5749842496362895794, 2.083749421223294540 ) ) ;
#137635=CARTESIAN_POINT ( 'NONE',  ( 5.549475203002828927, -1.825015992387307273, 0.8654263401719575199 ) ) ;
#137636=CARTESIAN_POINT ( 'NONE',  ( 5.461676247742112800, -1.750072316323016963, -1.367929348606132800 ) ) ;
#137640=CARTESIAN_POINT ( 'NONE',  ( 5.559468503951485729, 0.4043298029084033685, -2.020654889403751486 ) ) ;
#137641=CARTESIAN_POINT ( 'NONE',  ( 3.867814693791224112, -0.2004342644464084944, -2.006446243107910199 ) ) ;
#137648=CARTESIAN_POINT ( 'NONE',  ( 4.306017418194902469, -1.755500069608874281, 0.9912479507018998603 ) ) ;
#137649=CARTESIAN_POINT ( 'NONE',  ( 3.573999110145977820, -1.774750109099573869, -0.4897004633943187191 ) ) ;
#137651=CARTESIAN_POINT ( 'NONE',  ( 1.981525833354264243, -0.1160811445666837666, -2.304894087891403487 ) ) ;
#137653=CARTESIAN_POINT ( 'NONE',  ( 3.163507678178357541, 0.3205598832158839673, -2.137589075770351066 ) ) ;
#137659=CARTESIAN_POINT ( 'NONE',  ( 2.711613914024712191, -1.850561042518297672, 0.2725550856255419818 ) ) ;
#137660=CARTESIAN_POINT ( 'NONE',  ( 6.508667090220362716, 1.461156067397894054, -1.323708773930740268 ) ) ;
#137663=CARTESIAN_POINT ( 'NONE',  ( 1.787996309160574837, 1.523479866092191548, 1.596893430481533649 ) ) ;
#137669=CARTESIAN_POINT ( 'NONE',  ( 6.016478623866945874, 1.324313071814016141, -1.460584582105582285 ) ) ;
#137670=CARTESIAN_POINT ( 'NONE',  ( 5.690114378391165850, -1.042650834883801947, 2.058788517775663962 ) ) ;
#137671=CARTESIAN_POINT ( 'NONE',  ( 0.2034672893990868703, -1.513989045467616146, -1.247398002513319781 ) ) ;
#137672=CARTESIAN_POINT ( 'NONE',  ( 4.698127260392297444, 0.8867148737545665904, -1.862399597460895784 ) ) ;
#137680=CARTESIAN_POINT ( 'NONE',  ( 6.514155524301521005, 2.165825943586483504, -0.1531846826740568268 ) ) ;
#137682=CARTESIAN_POINT ( 'NONE',  ( 5.548353751603532835, -1.447698842669535413, 1.137588655622793876 ) ) ;
#137683=CARTESIAN_POINT ( 'NONE',  ( 6.620655732516623537, 7.629137130509068498, 2.426260288887295058 ) ) ;
#137684=CARTESIAN_POINT ( 'NONE',  ( 6.093348126157794198, -0.7399906200981146709, 2.062998119606203939 ) ) ;
#137689=CARTESIAN_POINT ( 'NONE',  ( -0.02298948590537253783, -1.708053232816408196, -0.8599758793098393195 ) ) ;
#137690=CARTESIAN_POINT ( 'NONE',  ( 1.832500204630353124, 0.1694391671427826207, 1.761704050274701894 ) ) ;
#137692=CARTESIAN_POINT ( 'NONE',  ( 6.393232662110455600, -0.1012007143085277561, -2.010677637860050382 ) ) ;
#137694=CARTESIAN_POINT ( 'NONE',  ( 4.341351955572036125, 0.4158663518127497793, -1.869753321735210916 ) ) ;
#137696=CARTESIAN_POINT ( 'NONE',  ( 5.389095231685527843, 0.1428881311146198430, 1.964408359074652388 ) ) ;
#137697=CARTESIAN_POINT ( 'NONE',  ( 6.533471379370169529, -0.1492333671020330821, 1.986230151431379598 ) ) ;
#137699=CARTESIAN_POINT ( 'NONE',  ( 2.904993682805886213, 1.579364189935757778, 1.002181356900035070 ) ) ;
#137700=CARTESIAN_POINT ( 'NONE',  ( 6.024008130617486856, -0.9641997184709062418, -1.430004917837023104 ) ) ;
#137702=CARTESIAN_POINT ( 'NONE',  ( 2.455956380646412196, 0.5873987694336445520, -2.127207350628975924 ) ) ;
#137705=CARTESIAN_POINT ( 'NONE',  ( 0.4146024514614836676, 0.7878568475925759040, 1.906473239439598677 ) ) ;
#137714=CARTESIAN_POINT ( 'NONE',  ( 2.875506610227479332, -0.2054619808779626633, 2.060159609288146232 ) ) ;
#137718=CARTESIAN_POINT ( 'NONE',  ( 0.5045642862554244878, -2.004696059604444081, -0.2448167134727705085 ) ) ;
#137723=CARTESIAN_POINT ( 'NONE',  ( 0.07459516483346911864, 0.007201286963446140027, -1.755573347271717211 ) ) ;
#137725=CARTESIAN_POINT ( 'NONE',  ( 6.784528966312857179, -1.956291195211720346, 0.4871289682274528299 ) ) ;
#137726=CARTESIAN_POINT ( 'NONE',  ( 6.456256392861089211, -1.172487466661990663, 1.515489988593403226 ) ) ;
#137728=CARTESIAN_POINT ( 'NONE',  ( 3.878626735558046157, -0.2160506499642600997, -2.180900317982924275 ) ) ;
#137730=CARTESIAN_POINT ( 'NONE',  ( 2.654443970922310214, 1.898414275235399407, 0.2300336082040748686 ) ) ;
#137735=CARTESIAN_POINT ( 'NONE',  ( 1.124625310196948558, 0.3961260723950796314, 1.976952190469769111 ) ) ;
#137737=CARTESIAN_POINT ( 'NONE',  ( 6.462441986028243157, -2.002789442531027309, -0.8901952361822995652 ) ) ;
#137739=CARTESIAN_POINT ( 'NONE',  ( 3.539825753290166688, 0.7759033148657649148, -1.540472896381483769 ) ) ;
#137741=CARTESIAN_POINT ( 'NONE',  ( 0.1399997263885795484, 5.723012109828673921, -2.593777676649943409 ) ) ;
#137745=CARTESIAN_POINT ( 'NONE',  ( 0.6780837441340243910, -1.046368970337024473, -1.659334490400856454 ) ) ;
#137752=CARTESIAN_POINT ( 'NONE',  ( 3.791515551631476910, 1.704436734775734985, -0.6137984976519753610 ) ) ;
#137756=CARTESIAN_POINT ( 'NONE',  ( 4.916585655956178691, -0.6154711373431708266, -1.703840371469134807 ) ) ;
#137760=CARTESIAN_POINT ( 'NONE',  ( 5.055058894927250357, 1.547480351173950552, -1.033501273311630886 ) ) ;
#137762=CARTESIAN_POINT ( 'NONE',  ( 2.917496427270527715, -1.288711974188415654, -1.417462588220135933 ) ) ;
#137771=CARTESIAN_POINT ( 'NONE',  ( 0.8496949173334772398, 2.088161746953997255, -0.1042977956757246832 ) ) ;
#137773=CARTESIAN_POINT ( 'NONE',  ( 0.1119280604304096899, -0.7754228321929098611, -1.651232954423286436 ) ) ;
#137775=CARTESIAN_POINT ( 'NONE',  ( 2.819161699164650869, -0.1809198688003388622, 1.816599095187728219 ) ) ;
#137777=CARTESIAN_POINT ( 'NONE',  ( 1.652457426684301955, 1.892030339952909035, 0.2773405859870237133 ) ) ;
#137778=CARTESIAN_POINT ( 'NONE',  ( 1.855843448759408210, -0.6666243292093411155, 1.853429361541816700 ) ) ;
#137779=CARTESIAN_POINT ( 'NONE',  ( 3.386211154777326815, -0.3816624740031882568, -1.904027918096486527 ) ) ;
#137784=CARTESIAN_POINT ( 'NONE',  ( 4.465154236216789307, -1.701427117168831549, 1.265499569954648962 ) ) ;
#137793=CARTESIAN_POINT ( 'NONE',  ( 4.389149243953620605, 1.629682310347341456, -0.8231139397327084106 ) ) ;
#137798=CARTESIAN_POINT ( 'NONE',  ( 4.153091690245942047, -1.555063956268587066, -1.039456662654779207 ) ) ;
#137800=CARTESIAN_POINT ( 'NONE',  ( 2.578635874325632127, -1.843646926959886523, -0.5589146710999506329 ) ) ;
#137807=CARTESIAN_POINT ( 'NONE',  ( 0.7029266809492543677, 1.957958796488759035, 0.8061104088524527755 ) ) ;
#137811=CARTESIAN_POINT ( 'NONE',  ( 5.453992358814952368, -0.7503507308065425763, 1.929658000011783336 ) ) ;
#137812=CARTESIAN_POINT ( 'NONE',  ( 0.1691535571452691677, 1.059206136818511501, 1.505872603892892458 ) ) ;
#137814=CARTESIAN_POINT ( 'NONE',  ( 5.274211419651455124, 2.028235465341983623, -1.081840468886515305 ) ) ;
#137818=CARTESIAN_POINT ( 'NONE',  ( 1.254322107098894801, 0.9329652568456588968, 2.093986936342966398 ) ) ;
#137821=CARTESIAN_POINT ( 'NONE',  ( 4.505766059781188382, -0.8317635995198893184, -1.754939027834252485 ) ) ;
#137825=CARTESIAN_POINT ( 'NONE',  ( 5.906500813101932756, -1.903809282439900219, -0.1807861040028224398 ) ) ;
#137826=CARTESIAN_POINT ( 'NONE',  ( 5.155482549980198392, 1.942097955248718533, -0.5424665614216088727 ) ) ;
#137830=CARTESIAN_POINT ( 'NONE',  ( 2.923863239626739663, 1.160869195616637706, -1.738502609096896467 ) ) ;
#137831=CARTESIAN_POINT ( 'NONE',  ( 1.199668116878411128, -1.770032029468296964, -0.005122706785119778526 ) ) ;
#137834=CARTESIAN_POINT ( 'NONE',  ( 3.644716121489647076, -1.874467426877159504, 1.319156965210349197 ) ) ;
#137835=CARTESIAN_POINT ( 'NONE',  ( 1.851089384485626210, 1.735827849189163663, -0.1260499613615853887 ) ) ;
#137838=CARTESIAN_POINT ( 'NONE',  ( 2.389626358114539162, -0.004507738041977306029, 1.734034291262590788 ) ) ;
#137839=CARTESIAN_POINT ( 'NONE',  ( 2.190095119440739424, -1.416971674389384761, -1.645159614449900776 ) ) ;
#137841=CARTESIAN_POINT ( 'NONE',  ( 5.032435514249763209, 0.5899841883351600869, 1.928258608204669766 ) ) ;
#137842=CARTESIAN_POINT ( 'NONE',  ( 1.968750000000001332, 0.7852924748298835134, -1.895863743164130755 ) ) ;
#137846=CARTESIAN_POINT ( 'NONE',  ( 1.131717742382963632, -1.219707097817297692, -1.491085513105432581 ) ) ;
#137848=CARTESIAN_POINT ( 'NONE',  ( 4.553117645631366450, 0.3812515705259692522, 2.188315991368384505 ) ) ;
#137850=CARTESIAN_POINT ( 'NONE',  ( -0.1110810684433168327, 2.049790377237853178, -2.213868588080004418 ) ) ;
#137855=CARTESIAN_POINT ( 'NONE',  ( 0.6104036325267605534, -0.7939654203579590286, 2.074740863049700845 ) ) ;
#137856=CARTESIAN_POINT ( 'NONE',  ( 6.162552467866693640, -0.7048080804108979303, -1.831077584432870609 ) ) ;
#137860=CARTESIAN_POINT ( 'NONE',  ( 6.503223684228603751, 1.875565888388399660, 1.264963274899598256 ) ) ;
#137863=CARTESIAN_POINT ( 'NONE',  ( 3.279784535431028658, -1.988673744353728123, 0.5473864365612387539 ) ) ;
#137867=CARTESIAN_POINT ( 'NONE',  ( 4.868341698904518289, -1.223052743625025141, 1.415352931214426846 ) ) ;
#137868=CARTESIAN_POINT ( 'NONE',  ( 3.357800782942537143, 0.03855433513636970927, -1.733892557700001502 ) ) ;
#137869=CARTESIAN_POINT ( 'NONE',  ( 3.350842269037973331, 0.4194941847268919832, -1.688999647770361490 ) ) ;
#137870=CARTESIAN_POINT ( 'NONE',  ( 0.8027370721926800901, 1.731296644042874755, -1.502618532894074876 ) ) ;
#137872=CARTESIAN_POINT ( 'NONE',  ( 4.827721544939969966, 1.073412050285113661, -1.793994897088858176 ) ) ;
#137873=CARTESIAN_POINT ( 'NONE',  ( 0.3043191165176573620, 1.600368420507289668, 0.9101283655772866021 ) ) ;
#137876=CARTESIAN_POINT ( 'NONE',  ( 0.5807041986926939625, -0.7231374404764076003, 1.882475062126743204 ) ) ;
#137877=CARTESIAN_POINT ( 'NONE',  ( 0.9848172835694012361, -1.340914915981223476, 1.642866500755429948 ) ) ;
#137882=CARTESIAN_POINT ( 'NONE',  ( 2.772263606761758759, 2.110060413066455975, -0.2101530891244970389 ) ) ;
#137884=CARTESIAN_POINT ( 'NONE',  ( 4.477060521952030747, -0.002618581577289170060, -1.825872481161804561 ) ) ;
#137891=CARTESIAN_POINT ( 'NONE',  ( 2.654562054903885304, 2.005031730908119147, 0.2428967267811207309 ) ) ;
#137892=CARTESIAN_POINT ( 'NONE',  ( 6.036183878773405453, 1.092744051193066834, -1.917163762461614240 ) ) ;
#137894=CARTESIAN_POINT ( 'NONE',  ( 4.381604285809827637, -1.781765127997904763, 0.5371461504297748712 ) ) ;
#137899=CARTESIAN_POINT ( 'NONE',  ( 5.584540971669589737, -1.782103179330214449, -0.3958202769075992444 ) ) ;
#137903=CARTESIAN_POINT ( 'NONE',  ( 0.3679294144470013905, -0.4713284034136792644, 1.668465712161566916 ) ) ;
#137904=CARTESIAN_POINT ( 'NONE',  ( 0.6381061630796550643, -1.494939029692418320, 0.8907679528266756463 ) ) ;
#137905=CARTESIAN_POINT ( 'NONE',  ( 5.479250216003205054, -0.05159697844352681417, -2.307286710698839727 ) ) ;
#137907=CARTESIAN_POINT ( 'NONE',  ( 1.616555492630408875, 1.386288697630438715, -1.524948804171057493 ) ) ;
#137908=CARTESIAN_POINT ( 'NONE',  ( 6.362725135800558540, -0.7832434641057796076, 2.160938040253687742 ) ) ;
#137911=CARTESIAN_POINT ( 'NONE',  ( 6.121928861531041655, -1.040746078065577063, -1.554202398018275755 ) ) ;
#137912=CARTESIAN_POINT ( 'NONE',  ( 3.041163856788456687, 0.05134138945498378792, 1.911883771832747048 ) ) ;
#137914=CARTESIAN_POINT ( 'NONE',  ( 5.356176587289051660, 2.204499490778097481, -0.1052899746726426722 ) ) ;
#137919=CARTESIAN_POINT ( 'NONE',  ( 5.690118541956746157, 1.263103799472656164, 1.703077153987264669 ) ) ;
#137920=CARTESIAN_POINT ( 'NONE',  ( 2.766999470516241288, -1.591810197153446182, 1.670866638877396060 ) ) ;
#137921=CARTESIAN_POINT ( 'NONE',  ( 3.508209890309890167, 1.962046631884439174, 0.002529298861464468473 ) ) ;
#137922=CARTESIAN_POINT ( 'NONE',  ( 0.9362904128984714802, -1.094497954693674391, 1.627855050370475620 ) ) ;
#137926=CARTESIAN_POINT ( 'NONE',  ( 5.682827415814322158, 1.645762192317705486, -1.164983060713747909 ) ) ;
#137929=CARTESIAN_POINT ( 'NONE',  ( 3.344746749068757019, -2.138148195731132351, -0.3758941404270431108 ) ) ;
#137931=CARTESIAN_POINT ( 'NONE',  ( 1.037531286769650452, -0.04638328994046451298, 2.120250110247793085 ) ) ;
#137937=CARTESIAN_POINT ( 'NONE',  ( 1.335309304440901235, -1.864295028495915441, 0.8784465167368092908 ) ) ;
#137943=CARTESIAN_POINT ( 'NONE',  ( 3.141163725242692273, 0.04933110545866059571, 1.911816780882446221 ) ) ;
#137944=CARTESIAN_POINT ( 'NONE',  ( 5.787929806067755756, -0.7924508370336593721, 1.582612139130882278 ) ) ;
#137947=CARTESIAN_POINT ( 'NONE',  ( 0.4920785707626255112, -1.005892833030905598, 1.506422592618541278 ) ) ;
#137949=CARTESIAN_POINT ( 'NONE',  ( 0.5146670378583360073, 0.1438656263933698054, 1.910404373559170477 ) ) ;
#137951=CARTESIAN_POINT ( 'NONE',  ( 1.908725956546155178, 0.6474277305483535638, 1.966616875269424192 ) ) ;
#137953=CARTESIAN_POINT ( 'NONE',  ( 6.543822781336226413, 0.7137633992815132222, -1.729328153040734506 ) ) ;
#137954=CARTESIAN_POINT ( 'NONE',  ( 2.807047293222181494, 1.542382716246639474, 0.9765254425028799812 ) ) ;
#137955=CARTESIAN_POINT ( 'NONE',  ( -0.02224634325198419221, -0.007204097619508199532, -2.289079630542793620 ) ) ;
#137958=CARTESIAN_POINT ( 'NONE',  ( 3.754389245258652252, -2.060177385294372776, -0.1042076536686628307 ) ) ;
#137962=CARTESIAN_POINT ( 'NONE',  ( 0.5269342146079664113, 2.068330297753611546, 0.6279826202375409228 ) ) ;
#137963=CARTESIAN_POINT ( 'NONE',  ( 0.1511277727459575393, -0.4806850054440474085, -2.125521221522770787 ) ) ;
#137965=CARTESIAN_POINT ( 'NONE',  ( 4.130267194010744269, 1.160198474277823300, -1.823679694223250491 ) ) ;
#137966=CARTESIAN_POINT ( 'NONE',  ( 3.914717006531149401, -0.6357662484684013515, -1.917053231858157236 ) ) ;
#137973=CARTESIAN_POINT ( 'NONE',  ( 2.202361591730035428, 1.313542931311746598, -1.530159205979222170 ) ) ;
#137978=CARTESIAN_POINT ( 'NONE',  ( 5.326388512780113160, -0.8654452107222168067, -1.705464787417856787 ) ) ;
#137983=CARTESIAN_POINT ( 'NONE',  ( 3.972279928656559100, -1.994873972748755442, -0.2930500606010341125 ) ) ;
#137986=CARTESIAN_POINT ( 'NONE',  ( 6.387718858896353602, 1.193691027695796825, 1.245227284122518485 ) ) ;
#137990=CARTESIAN_POINT ( 'NONE',  ( 5.553920895479774522, 1.868435625992425742, -0.09091641586010666687 ) ) ;
#137991=CARTESIAN_POINT ( 'NONE',  ( 5.941657920834610529, -1.894198565178412119, 0.6822040374353780523 ) ) ;
#137992=CARTESIAN_POINT ( 'NONE',  ( -0.1290005225502675879, -0.006633637972621592160, -2.173875058097324064 ) ) ;
#137993=CARTESIAN_POINT ( 'NONE',  ( 2.026315959858393967, 1.060668813445601044, 1.777738962378045295 ) ) ;
#137997=CARTESIAN_POINT ( 'NONE',  ( 1.124625310196948558, 0.3961260723950796314, 1.976952190469769111 ) ) ;
#137998=CARTESIAN_POINT ( 'NONE',  ( 1.230386416485089729, 1.215489027575139769, -1.343484786563201805 ) ) ;
#138004=CARTESIAN_POINT ( 'NONE',  ( 6.134394303309665730, 0.6061128391178214336, 1.817247008912269646 ) ) ;
#138013=CARTESIAN_POINT ( 'NONE',  ( 3.344745324850742385, 0.5235245934552492653, 2.097234944377385002 ) ) ;
#138016=CARTESIAN_POINT ( 'NONE',  ( 0.3871773095200456982, -1.998849835692744659, -0.7086421328065874992 ) ) ;
#138017=CARTESIAN_POINT ( 'NONE',  ( 6.247073575888860475, -1.540555741078741825, 0.9791950884799265342 ) ) ;
#138018=CARTESIAN_POINT ( 'NONE',  ( 2.565645918639497314, 1.934049084626581205, -0.3809019065194594877 ) ) ;
#138019=CARTESIAN_POINT ( 'NONE',  ( 4.834190613173367623, -1.027981871586785889, -1.612434056610718480 ) ) ;
#138021=DIRECTION ( 'NONE',  ( 1.014813233446432150E-15, 1.000000000000000000, -4.583713267641621330E-32 ) ) ;
#138022=CARTESIAN_POINT ( 'NONE',  ( 4.439879492920996817, 1.284938098365424164, 1.492779756951348125 ) ) ;
#138023=CARTESIAN_POINT ( 'NONE',  ( 0.6033350840282033500, -1.932664299774440098, 0.1897328419256556487 ) ) ;
#138030=CARTESIAN_POINT ( 'NONE',  ( 5.496708366351358066, -1.866603419165157041, -0.4147590543357379533 ) ) ;
#138032=CARTESIAN_POINT ( 'NONE',  ( 1.026743138268666922, 1.313310656681260680, -1.773271738842125300 ) ) ;
#138035=CARTESIAN_POINT ( 'NONE',  ( 5.813144886445268611, 1.644464822582414332, -1.160890557811714352 ) ) ;
#138036=CARTESIAN_POINT ( 'NONE',  ( -0.02319159430949970999, 0.003959926571647092407, -1.810968101872318714 ) ) ;
#138039=CARTESIAN_POINT ( 'NONE',  ( 3.314952806421948672, -1.569539724514938950, 1.350292352848787569 ) ) ;
#138043=CARTESIAN_POINT ( 'NONE',  ( 0.1456854043008250221, -1.672057201651616642, -1.369741535119282982 ) ) ;
#138048=CARTESIAN_POINT ( 'NONE',  ( 6.925078400183550364, 2.474256779287649088, 2.140290375984225335 ) ) ;
#138051=CARTESIAN_POINT ( 'NONE',  ( 5.309090426574582189, 1.026673973311197585, -1.397408945856312590 ) ) ;
#138053=CARTESIAN_POINT ( 'NONE',  ( 2.342711862795249012, -2.029470198211943632, -0.4080651701656515251 ) ) ;
#138054=CARTESIAN_POINT ( 'NONE',  ( 4.025106843427800563, -1.841118617500647314, 1.045351873429276601 ) ) ;
#138057=CARTESIAN_POINT ( 'NONE',  ( 2.289847402107755947, -1.282740503449712577, -1.494545344566786449 ) ) ;
#138059=CARTESIAN_POINT ( 'NONE',  ( 1.318461241437279607, -0.6911404020932455650, -1.783297644634279200 ) ) ;
#138060=CARTESIAN_POINT ( 'NONE',  ( 4.822401350889861327, 2.192639013963990635, 0.6684651760814497301 ) ) ;
#138061=CARTESIAN_POINT ( 'NONE',  ( 1.646812808029130215, -1.543121136568927243, 0.9753659028155501343 ) ) ;
#138065=CARTESIAN_POINT ( 'NONE',  ( 3.392840988816598902, -1.941408766427907384, -0.5327130583171105771 ) ) ;
#138066=CARTESIAN_POINT ( 'NONE',  ( 3.098438489093110704, 1.946378968836332213, 0.2448508753878294586 ) ) ;
#138070=CARTESIAN_POINT ( 'NONE',  ( 5.701146808890831252, -0.5089937999912234057, 2.027600676370949095 ) ) ;
#138071=CARTESIAN_POINT ( 'NONE',  ( 4.276060399186999206, -1.018433877553532207, 1.447237009025013732 ) ) ;
#138073=CARTESIAN_POINT ( 'NONE',  ( 0.9025786099917804117, 1.657183926254527595, -1.434042119274607563 ) ) ;
#138074=CARTESIAN_POINT ( 'NONE',  ( 0.06344835015564037617, -1.139564578658038618, 1.315610641012928239 ) ) ;
#138076=CARTESIAN_POINT ( 'NONE',  ( 0.1331715793776574175, 0.2412765091673596263, -1.987739918565622821 ) ) ;
#138077=CARTESIAN_POINT ( 'NONE',  ( 0.2284049197783468987, -2.054502581980635956, -1.030649272238814085 ) ) ;
#138079=CARTESIAN_POINT ( 'NONE',  ( 5.483642203991152542, 1.602890455293109584, 0.6615300989148454880 ) ) ;
#138080=CARTESIAN_POINT ( 'NONE',  ( 2.174722684859807575, -1.356406721008751814, 1.740749382485320407 ) ) ;
#138081=CARTESIAN_POINT ( 'NONE',  ( 0.4972420419220639487, 0.3698279840313797862, 2.139175918340649574 ) ) ;
#138083=CARTESIAN_POINT ( 'NONE',  ( 1.358780451569325365, -2.012465911620679115, -0.6584304486853159721 ) ) ;
#138084=CARTESIAN_POINT ( 'NONE',  ( 3.218750000000001776, -0.7852924748298164559, 1.895863743164153847 ) ) ;
#138085=CARTESIAN_POINT ( 'NONE',  ( 6.827182134110235445, 0.5726250382554041174, 2.141766166723162002 ) ) ;
#138086=CARTESIAN_POINT ( 'NONE',  ( 4.524389607583827910, 1.185449959155547850, -1.518358881950541139 ) ) ;
#138087=CARTESIAN_POINT ( 'NONE',  ( 1.313460851834074905, 1.813262283420258525, -1.282816764689881373 ) ) ;
#138090=CARTESIAN_POINT ( 'NONE',  ( 1.892491709730130145, -0.6158747592755541289, -2.208019654398277520 ) ) ;
#138094=CARTESIAN_POINT ( 'NONE',  ( 3.598459204466686323, -1.093923138158871433, 1.933176262723006467 ) ) ;
#138096=COLOUR_RGB ( '', 0.31764706, 0.68627451, 0.89019608) ;
#138103=CARTESIAN_POINT ( 'NONE',  ( 1.406875202279284753, -1.122500148236497575, -1.674886495921081631 ) ) ;
#138105=CARTESIAN_POINT ( 'NONE',  ( 6.408646180098039657, 0.6432782940990633413, 1.959889192978042205 ) ) ;
#138107=CARTESIAN_POINT ( 'NONE',  ( 0.1691535571452691677, 1.059206136818511501, 1.505872603892892458 ) ) ;
#138110=CARTESIAN_POINT ( 'NONE',  ( 1.686396851806533315, -0.2532433360125495025, -1.751381468886082038 ) ) ;
#138111=CARTESIAN_POINT ( 'NONE',  ( 6.451818256879360725, -1.589883334587833152, -0.6930036952102114345 ) ) ;
#138112=CARTESIAN_POINT ( 'NONE',  ( 6.620655732516682157, 0.01042156863441953685, 1.726407961933309476 ) ) ;
#138113=CARTESIAN_POINT ( 'NONE',  ( 4.704755546018094314, 1.993839351151542427, 1.131020188671335136 ) ) ;
#138114=CARTESIAN_POINT ( 'NONE',  ( 3.222423357234117436, 0.04607595322191247733, 1.840729346561786661 ) ) ;
#138118=CARTESIAN_POINT ( 'NONE',  ( 4.506759567000420574, 1.410888988908312047, -1.158519065656477220 ) ) ;
#138119=CARTESIAN_POINT ( 'NONE',  ( 3.287732575140737801, 1.587837554856496691, -1.242726844152845178 ) ) ;
#138121=CARTESIAN_POINT ( 'NONE',  ( 3.713984175222109663, -2.229511888261398678, 0.3841874803040145059 ) ) ;
#138123=CARTESIAN_POINT ( 'NONE',  ( 5.631892205062830392, -1.333580992396019571, -1.629923671128389762 ) ) ;
#138125=CARTESIAN_POINT ( 'NONE',  ( 3.736834853878097107, -1.994506513866915576, -0.5549897870569252545 ) ) ;
#138128=CARTESIAN_POINT ( 'NONE',  ( 5.338584462458719315, 1.262900380722062454, -1.703257760751579530 ) ) ;
#138130=CARTESIAN_POINT ( 'NONE',  ( 0.6977243349758615043, -0.6943943954660827256, 1.797178231592330588 ) ) ;
#138132=CARTESIAN_POINT ( 'NONE',  ( 0.4495734683114894215, 1.456899865409568617, 1.325532655419828787 ) ) ;
#138137=CARTESIAN_POINT ( 'NONE',  ( 1.072868727471010253, 0.9067168766181363804, 2.028134479351159314 ) ) ;
#138138=CARTESIAN_POINT ( 'NONE',  ( 2.731583703245387351, -1.965451047913500116, 0.7568412939000405126 ) ) ;
#138141=CARTESIAN_POINT ( 'NONE',  ( 0.5548465212725885998, 1.550470960922016861, -1.029025501433494583 ) ) ;
#138147=CARTESIAN_POINT ( 'NONE',  ( 1.301209403646291118, -0.3165094942152619772, -2.096747597609450953 ) ) ;
#138150=CARTESIAN_POINT ( 'NONE',  ( 3.736726379466179804, -1.890069333072645241, -0.5255722985574098338 ) ) ;
#138151=CARTESIAN_POINT ( 'NONE',  ( 2.307699607974790901, -0.4742087202370263155, 2.108885336910087283 ) ) ;
#138152=CARTESIAN_POINT ( 'NONE',  ( 1.874305484616908934, -0.09156810461483089192, -1.839108553062768214 ) ) ;
#138156=CARTESIAN_POINT ( 'NONE',  ( 3.187183321348503018, -0.7043554338151243321, 1.591608241653941214 ) ) ;
#138159=CARTESIAN_POINT ( 'NONE',  ( 0.5148121308554790554, 1.489681748880047563, -1.566682057046255849 ) ) ;
#138160=CARTESIAN_POINT ( 'NONE',  ( 3.866564406427867251, -0.5879305547937460075, 1.928456347981069019 ) ) ;
#138162=CARTESIAN_POINT ( 'NONE',  ( 0.4444780689869810564, 2.156031605563761833, 0.1575401717312311101 ) ) ;
#138163=CARTESIAN_POINT ( 'NONE',  ( 1.991034414115494089, 1.716142376821601534, -0.9701854037313780710 ) ) ;
#138165=CARTESIAN_POINT ( 'NONE',  ( 6.509000000000034980, 7.629137130509102249, 2.499999999999994227 ) ) ;
#138166=CARTESIAN_POINT ( 'NONE',  ( 2.419391519165543070, -1.120004824200554916, -1.586377984052749879 ) ) ;
#138174=CARTESIAN_POINT ( 'NONE',  ( 6.387736634265912983, 1.584785628913528699, 1.677562689604541468 ) ) ;
#138175=CARTESIAN_POINT ( 'NONE',  ( 6.830524215763060347, -1.208013408316032322, 1.546442907991877558 ) ) ;
#138176=CARTESIAN_POINT ( 'NONE',  ( 3.731260466781026963, 0.05263058604075031982, -1.961233346245725429 ) ) ;
#138178=CARTESIAN_POINT ( 'NONE',  ( 1.600232647554021392, -0.2440283035436350279, 2.001511509883910911 ) ) ;
#138180=CARTESIAN_POINT ( 'NONE',  ( 1.868513053102664356, -2.077584836267523105, -0.4075993926472165074 ) ) ;
#138184=CARTESIAN_POINT ( 'NONE',  ( 3.152128525617302834, -1.393660036906883226, 1.203213496783587910 ) ) ;
#138189=CARTESIAN_POINT ( 'NONE',  ( 4.289387122732970958, -0.003046686910593982868, -2.120778211268215419 ) ) ;
#138190=CARTESIAN_POINT ( 'NONE',  ( 0.04061758243546764735, -1.421021341975825969, -1.170429047309962112 ) ) ;
#138194=CARTESIAN_POINT ( 'NONE',  ( 4.886040457987857799, -0.9749269275126177803, 1.815604017143893634 ) ) ;
#138197=CARTESIAN_POINT ( 'NONE',  ( 1.487592393518050837, -1.832424703912252317, -0.1798031890194173865 ) ) ;
#138201=CARTESIAN_POINT ( 'NONE',  ( 1.014635385311330795, -0.9952708415592588231, -1.969785480804244315 ) ) ;
#138202=CARTESIAN_POINT ( 'NONE',  ( 4.270984383450874944, -2.108973115933824527, -0.8193970387949424117 ) ) ;
#138204=CARTESIAN_POINT ( 'NONE',  ( 4.113381391103660967, 1.458659968308340993, 1.074121561303176264 ) ) ;
#138205=CARTESIAN_POINT ( 'NONE',  ( 4.012823373000539817, 0.09967532595039167720, 1.913279002700827514 ) ) ;
#138206=CARTESIAN_POINT ( 'NONE',  ( 5.037584538744971141, 1.933038169019934527, -0.7419538039311265321 ) ) ;
#138208=CARTESIAN_POINT ( 'NONE',  ( 2.289859582131337223, -0.8446868967569521880, 1.781483357239101117 ) ) ;
#138209=CARTESIAN_POINT ( 'NONE',  ( 1.096560174117457764, -0.4650716533593258761, -1.869300808490617305 ) ) ;
#138210=CARTESIAN_POINT ( 'NONE',  ( 4.065207594588423845, 0.2294239933214488880, -1.856472568989680161 ) ) ;
#138212=CARTESIAN_POINT ( 'NONE',  ( 3.721538942197761379, -0.1710094959430948913, 2.301408321908961607 ) ) ;
#138213=CARTESIAN_POINT ( 'NONE',  ( 3.877287848637627210, -0.1385928533646582361, 1.855967808809717789 ) ) ;
#138216=CARTESIAN_POINT ( 'NONE',  ( 1.787856894401329333, 1.453325235529376869, 1.524497383921459726 ) ) ;
#138221=CARTESIAN_POINT ( 'NONE',  ( 2.883181758455736432, -1.960942133159260692, -0.8077274430827171559 ) ) ;
#138223=CARTESIAN_POINT ( 'NONE',  ( 0.9319058833903216543, -1.969584188619889487, 0.4467263836498857055 ) ) ;
#138228=CARTESIAN_POINT ( 'NONE',  ( 0.8960494714182369869, -0.7788709108395329705, 2.016556642405589184 ) ) ;
#138229=CARTESIAN_POINT ( 'NONE',  ( 6.610000000000030518, 2.992693383986976041, 2.174209315121559349 ) ) ;
#138233=CARTESIAN_POINT ( 'NONE',  ( 5.577361344084559747, 1.530155114678043660, 1.313547687611632764 ) ) ;
#138235=CARTESIAN_POINT ( 'NONE',  ( -0.1290005225502675879, -0.006633637972621592160, -2.173875058097324064 ) ) ;
#138237=CARTESIAN_POINT ( 'NONE',  ( 0.4974159974337259427, 1.879172763871908902, -1.259763710243780865 ) ) ;
#138242=CARTESIAN_POINT ( 'NONE',  ( 1.229944743773615956, 1.913488753162166045, 0.09234796458578581335 ) ) ;
#138246=CARTESIAN_POINT ( 'NONE',  ( 3.404663882806455266, 1.358838683821527393, -1.062305643495575103 ) ) ;
#138248=CARTESIAN_POINT ( 'NONE',  ( 1.704008468626088790, -0.6311095051503686770, -1.653581786927365904 ) ) ;
#138249=CARTESIAN_POINT ( 'NONE',  ( 3.088541981101311507, -1.197259257089001716, 1.618239360019198880 ) ) ;
#138251=CARTESIAN_POINT ( 'NONE',  ( 5.649526978565787338, -1.736373965863503122, -1.361823127433124725 ) ) ;
#138253=CARTESIAN_POINT ( 'NONE',  ( 4.342060261306793123, -1.245981751006501437, -1.589553384294100091 ) ) ;
#138255=CARTESIAN_POINT ( 'NONE',  ( 4.037823014030429647, -2.028772383530423884, 0.6168223452112443494 ) ) ;
#138256=CARTESIAN_POINT ( 'NONE',  ( 3.831657784458125882, 0.6766976527424087839, -1.899625577706779422 ) ) ;
#138260=CARTESIAN_POINT ( 'NONE',  ( 1.428351348257720588, 1.801920623737063520, 0.5021531274154652502 ) ) ;
#138262=CARTESIAN_POINT ( 'NONE',  ( 6.182253972182746971, 0.9374619682817868505, 1.549891177688822452 ) ) ;
#138271=CARTESIAN_POINT ( 'NONE',  ( 4.342108446431157454, -1.306982937058022820, -1.669832246961988176 ) ) ;
#138274=CARTESIAN_POINT ( 'NONE',  ( 4.991463202408453093, 1.458887350482462875, 1.326006969317705009 ) ) ;
#138276=CARTESIAN_POINT ( 'NONE',  ( 1.318609283782465003, -0.7284450440303428254, -1.876953636963938354 ) ) ;
#138278=CARTESIAN_POINT ( 'NONE',  ( -0.05292715583045219663, -1.893440308637056146, -0.9475653277955156106 ) ) ;
#138280=CARTESIAN_POINT ( 'NONE',  ( 1.469279758060073160, 1.824989553406907383, 0.9776941847434923449 ) ) ;
#138284=CARTESIAN_POINT ( 'NONE',  ( 4.312501488504257630, 1.911392599577836693, 0.8473735431044140398 ) ) ;
#138287=CARTESIAN_POINT ( 'NONE',  ( 3.381694320706640333, 1.157239582903809128, 1.411935816614327655 ) ) ;
#138288=CARTESIAN_POINT ( 'NONE',  ( 1.945701609745503324, -1.183853311710543199, -1.371160031100856935 ) ) ;
#138290=CARTESIAN_POINT ( 'NONE',  ( 6.498651167236064730, -0.5841124237929047336, -2.128106146270396071 ) ) ;
#138292=CARTESIAN_POINT ( 'NONE',  ( 4.225739626866775289, -2.112672615930260900, 0.6375689414055001336 ) ) ;
#138294=CARTESIAN_POINT ( 'NONE',  ( 2.385291144485178982, 0.09204604084523880514, -1.910175020619097275 ) ) ;
#138297=CARTESIAN_POINT ( 'NONE',  ( 6.426242046702522082, 1.060841730010402495, 1.777776562702712226 ) ) ;
#138299=CARTESIAN_POINT ( 'NONE',  ( 5.442994344319362021, -1.727133847215430729, -1.348975639928217118 ) ) ;
#138305=CARTESIAN_POINT ( 'NONE',  ( 3.655401173194738007, 0.4573680094964554521, -1.813624142381641491 ) ) ;
#138310=CARTESIAN_POINT ( 'NONE',  ( 6.614133338355735248, 2.065126723422955557, -0.1462301744803648496 ) ) ;
#138311=CARTESIAN_POINT ( 'NONE',  ( 1.651970485933237143, 1.039013645561959853, 1.727991324714774013 ) ) ;
#138314=CARTESIAN_POINT ( 'NONE',  ( 1.306853331985533107, 1.934050699793531836, 1.030479497498619557 ) ) ;
#138315=CARTESIAN_POINT ( 'NONE',  ( 5.443921307256319508, 0.7362202147598859714, -1.670853202368663082 ) ) ;
#138323=CARTESIAN_POINT ( 'NONE',  ( 2.929072846782492245, -1.238530643895646488, -1.362589426554157157 ) ) ;
#138324=CARTESIAN_POINT ( 'NONE',  ( 0.1002437576986033446, -0.9471954198254585178, 1.776316830230479260 ) ) ;
#138325=CARTESIAN_POINT ( 'NONE',  ( 1.458857794315861156, 1.741214688395021470, 1.500301734068248294 ) ) ;
#138327=CARTESIAN_POINT ( 'NONE',  ( 6.877797714452785982, -1.903667959252927533, 0.4735691183095217527 ) ) ;
#138330=CARTESIAN_POINT ( 'NONE',  ( 3.164218664783400747, 1.912571728330178855, -0.004505864839042527346 ) ) ;
#138334=CARTESIAN_POINT ( 'NONE',  ( 2.191069407410517478, 1.617985365078830950, 1.324160459713573879 ) ) ;
#138335=CARTESIAN_POINT ( 'NONE',  ( 1.358040219746913024, 0.7549631825471068147, 1.711723683848711985 ) ) ;
#138336=CARTESIAN_POINT ( 'NONE',  ( 2.266953675890924558, -2.015725231744563306, 0.04666741021024794350 ) ) ;
#138339=CARTESIAN_POINT ( 'NONE',  ( 3.157457554155696844, 0.7852445609939761040, 1.553317506218002464 ) ) ;
#138344=CARTESIAN_POINT ( 'NONE',  ( 3.228823373612188519, 0.04322303627742052345, 1.724510841617853840 ) ) ;
#138345=CARTESIAN_POINT ( 'NONE',  ( 2.964592600559623037, -2.025863808726846127, -0.8364240203130177687 ) ) ;
#138346=CARTESIAN_POINT ( 'NONE',  ( 5.654950187766193181, -1.741821662664808867, 1.355018943897445149 ) ) ;
#138348=CARTESIAN_POINT ( 'NONE',  ( 3.327178260015594802, -2.004142704238300876, -0.8352945444606455494 ) ) ;
#138349=CARTESIAN_POINT ( 'NONE',  ( 2.473051018021198200, 0.08991741065280876855, -1.823594477012622228 ) ) ;
#138351=CARTESIAN_POINT ( 'NONE',  ( 4.821547164884887771, -1.499609098395672246, -1.495007082409164356 ) ) ;
#138352=CARTESIAN_POINT ( 'NONE',  ( 6.639320575229248789, 2.444019389566108647, 2.379739370560208567 ) ) ;
#138354=ORIENTED_EDGE ( 'NONE', *, *, #147573, .T. ) ;
#138355=CARTESIAN_POINT ( 'NONE',  ( 4.529038776287770851, -2.096192991274762996, 0.9282860960324219590 ) ) ;
#138359=CARTESIAN_POINT ( 'NONE',  ( 0.1004478525090373164, -0.9956121213324088393, 1.872212410442177344 ) ) ;
#138366=CARTESIAN_POINT ( 'NONE',  ( 5.291638762709002464, 1.525045427759319727, -1.319226660814104335 ) ) ;
#138368=CARTESIAN_POINT ( 'NONE',  ( 3.098538415137185531, 2.046439989356943823, 0.2571918767454490773 ) ) ;
#138370=CARTESIAN_POINT ( 'NONE',  ( -0.2409995289980003397, 4.087843961663322645, -2.555282842491034323 ) ) ;
#138374=CARTESIAN_POINT ( 'NONE',  ( 6.667925998804712151, -1.351855065013835455, 1.725503752137508284 ) ) ;
#138375=CARTESIAN_POINT ( 'NONE',  ( 3.516250148862578584, -1.862017090670412767, 0.7743150488077471527 ) ) ;
#138376=CARTESIAN_POINT ( 'NONE',  ( 3.087279721815265443, -0.7436087841871074078, 1.684586988852328160 ) ) ;
#138380=CARTESIAN_POINT ( 'NONE',  ( 0.6742806677700216023, -1.621663110835226629, -0.5878086553270861492 ) ) ;
#138382=CARTESIAN_POINT ( 'NONE',  ( 0.4757056697715462690, -2.282288811291408148, -0.2737132658124728501 ) ) ;
#138384=CARTESIAN_POINT ( 'NONE',  ( 0.5622849326936694148, 2.237558834470813274, -0.3334926475991057959 ) ) ;
#138385=CARTESIAN_POINT ( 'NONE',  ( 3.563196004013529983, -1.857486927118640718, -0.9925908497740908443 ) ) ;
#138394=CARTESIAN_POINT ( 'NONE',  ( 3.674281580191523400, 2.204306621758029383, -0.2748671541705596799 ) ) ;
#138395=CARTESIAN_POINT ( 'NONE',  ( 2.431793384409334902, 1.031818167245980744, -1.933333044699905079 ) ) ;
#138398=CARTESIAN_POINT ( 'NONE',  ( 5.037533845850875380, 1.831247050742194515, -0.7043679133837479345 ) ) ;
#138403=CARTESIAN_POINT ( 'NONE',  ( 4.219064148821600746, 1.637239594409030330, -1.347683705884415106 ) ) ;
#138406=CARTESIAN_POINT ( 'NONE',  ( 5.577088068215094729, -0.04877400797019536272, -2.161318155665878038 ) ) ;
#138408=CARTESIAN_POINT ( 'NONE',  ( 5.144037045698616417, 0.5398437887287730330, 1.760322748975438500 ) ) ;
#138411=CARTESIAN_POINT ( 'NONE',  ( 0.3095773630682343569, 1.202386210327820004, -1.258585571321766627 ) ) ;
#138412=CARTESIAN_POINT ( 'NONE',  ( 6.727182134110202050, 7.629137130509070275, 2.410944104600750038 ) ) ;
#138416=CARTESIAN_POINT ( 'NONE',  ( 4.170900312159072421, -2.016029151617684256, -0.7805680927704603533 ) ) ;
#138419=CARTESIAN_POINT ( 'NONE',  ( 3.045950098598048328, 0.7793912989166664751, -2.016482303682599841 ) ) ;
#138420=CARTESIAN_POINT ( 'NONE',  ( 4.657473197611246896, 0.4347632249906174806, -1.922659379041303129 ) ) ;
#138421=CARTESIAN_POINT ( 'NONE',  ( 3.426783358884141428, 0.7772304037446680081, 1.549921577765429825 ) ) ;
#138423=CARTESIAN_POINT ( 'NONE',  ( 0.4334776158547505864, -1.553986563932317377, -1.545601477622601472 ) ) ;
#138424=CARTESIAN_POINT ( 'NONE',  ( 1.642099192286674336, -1.672607260348612845, -1.589979871525433408 ) ) ;
#138425=CARTESIAN_POINT ( 'NONE',  ( 3.251298195952691206, -1.682652751511631850, -1.189445392860078110 ) ) ;
#138426=CARTESIAN_POINT ( 'NONE',  ( 6.075724011240296818, -1.035248994944122369, 1.642949693582099302 ) ) ;
#138429=ADVANCED_FACE ( 'NONE', ( #118672 ), #184655, .T. ) ;
#138434=CARTESIAN_POINT ( 'NONE',  ( 3.294164632606086940, -0.8960083017303889230, 2.016869484631748310 ) ) ;
#138436=EDGE_LOOP ( 'NONE', ( #169192, #61891 ) ) ;
#138437=CARTESIAN_POINT ( 'NONE',  ( 0.3560157238547481118, -1.860367465765656814, -0.05377290132800408712 ) ) ;
#138438=CARTESIAN_POINT ( 'NONE',  ( -0.02900071798685525254, 1.326456003635017922, -2.425894103910302135 ) ) ;
#138442=CARTESIAN_POINT ( 'NONE',  ( 6.620655732516647518, 0.007553340620044743381, 1.826407896915738238 ) ) ;
#138443=CARTESIAN_POINT ( 'NONE',  ( 6.263598714517844002, 0.9507720431706817577, 1.576509192756641475 ) ) ;
#138445=CARTESIAN_POINT ( 'NONE',  ( 1.973578683463860672, 1.972434364383905292, -0.5973212362519930707 ) ) ;
#138449=CARTESIAN_POINT ( 'NONE',  ( 1.323197370116558469, -0.05141181009169673577, 2.060424651611890479 ) ) ;
#138450=CARTESIAN_POINT ( 'NONE',  ( 4.845164456061270997, 0.5726227986864868003, -1.750029900461601340 ) ) ;
#138456=CARTESIAN_POINT ( 'NONE',  ( 4.864015066594513215, 2.183220759563545776, -0.3215228633955333759 ) ) ;
#138457=CARTESIAN_POINT ( 'NONE',  ( 6.784454189598811524, -2.216766238704069636, -0.4514476129710183194 ) ) ;
#138459=CARTESIAN_POINT ( 'NONE',  ( 0.2285749388857594433, 1.317234250586714284, -1.386657971642536014 ) ) ;
#138460=CARTESIAN_POINT ( 'NONE',  ( 1.130092623156966347, 2.014433208573155110, 0.09411304420373775570 ) ) ;
#138462=CARTESIAN_POINT ( 'NONE',  ( 6.807498166657679484, -0.4075194142965676836, 1.832415718333743282 ) ) ;
#138463=CARTESIAN_POINT ( 'NONE',  ( 6.410809557875646547, -0.5148348048229570706, -1.841598127471068658 ) ) ;
#138465=CARTESIAN_POINT ( 'NONE',  ( 1.569004590881704075, 0.1408476687595125731, -1.865417194689425795 ) ) ;
#138466=CARTESIAN_POINT ( 'NONE',  ( 2.255092540634635156, 0.09411513195021348199, -2.014433103604281960 ) ) ;
#138470=CARTESIAN_POINT ( 'NONE',  ( 5.127606433170654121, -2.000101594804974514, 0.6598296307055817600 ) ) ;
#138475=CARTESIAN_POINT ( 'NONE',  ( 4.183856667257361828, 1.958065582907195568, -0.4948979464895820191 ) ) ;
#138477=CARTESIAN_POINT ( 'NONE',  ( 5.916483495826922123, 0.8326555988564422472, 1.887315221659194631 ) ) ;
#138479=CARTESIAN_POINT ( 'NONE',  ( 4.587301040747738590, 1.933109172225886185, -0.9673573668882375909 ) ) ;
#138485=CARTESIAN_POINT ( 'NONE',  ( 1.768284035615394600, -2.154879749829127444, 0.2648707735025003229 ) ) ;
#138488=CARTESIAN_POINT ( 'NONE',  ( 1.804012939494209267, 1.363607186100148638, -1.237405090928713092 ) ) ;
#138491=CARTESIAN_POINT ( 'NONE',  ( 3.052458795248469414, -1.657928338269051505, 1.433322580492613296 ) ) ;
#138492=CARTESIAN_POINT ( 'NONE',  ( 6.983263157960349687, 0.5706719223780298833, 2.105707282093812083 ) ) ;
#138493=CARTESIAN_POINT ( 'NONE',  ( 3.749113412367131914, -1.851274732041636950, 1.300436299091920045 ) ) ;
#138499=CARTESIAN_POINT ( 'NONE',  ( 5.800005483916761406, -1.769921774263127912, 0.001416880316495658159 ) ) ;
#138501=CARTESIAN_POINT ( 'NONE',  ( 2.415183150638998466, 1.880743233677120818, 0.9477269459148714992 ) ) ;
#138504=CARTESIAN_POINT ( 'NONE',  ( 1.363649640492822668, -0.4818474322187695780, 1.909556114072549882 ) ) ;
#138506=CARTESIAN_POINT ( 'NONE',  ( 0.1858947801188018389, -1.204007190563995078, -1.549573762531175625 ) ) ;
#138507=CARTESIAN_POINT ( 'NONE',  ( 5.800986464141828058, -0.2745434460682676936, -1.790553645544520345 ) ) ;
#138511=CARTESIAN_POINT ( 'NONE',  ( 4.926551758443063811, 1.790249073151507275, 0.5424879929923772659 ) ) ;
#138514=CARTESIAN_POINT ( 'NONE',  ( 5.049704560591026237, 1.530381825397047812, 1.394388655583590042 ) ) ;
#138524=CARTESIAN_POINT ( 'NONE',  ( 4.721123852359588646, -1.751549048416237486, -0.8839179009662299080 ) ) ;
#138526=CARTESIAN_POINT ( 'NONE',  ( 2.565779641467882399, 1.620934753846922982, -1.198676126143098486 ) ) ;
#138528=CARTESIAN_POINT ( 'NONE',  ( 0.5389544483674936215, -1.876709678404146153, 1.131566444868239874 ) ) ;
#138530=CARTESIAN_POINT ( 'NONE',  ( 1.844777716111935861, -1.582881869529973562, 0.9963996312925410548 ) ) ;
#138532=CARTESIAN_POINT ( 'NONE',  ( 3.779544948098710666, 0.2423517821111692006, -1.998478243804775900 ) ) ;
#138535=CARTESIAN_POINT ( 'NONE',  ( 3.128620947210249970, 0.5168888077675163339, 2.053037424179054327 ) ) ;
#138536=CARTESIAN_POINT ( 'NONE',  ( 4.562978833902987752, 1.602482145440896399, -1.310924660355553106 ) ) ;
#138538=CARTESIAN_POINT ( 'NONE',  ( 1.312182373965790072, 1.401635355298202379, -1.551525349546636123 ) ) ;
#138539=CARTESIAN_POINT ( 'NONE',  ( 6.620655732516618208, 1.260995252412312251, 2.189931766300906801 ) ) ;
#138540=CARTESIAN_POINT ( 'NONE',  ( 6.422862827026682098, 1.704596635199370880, 0.6539724957527744964 ) ) ;
#138549=CARTESIAN_POINT ( 'NONE',  ( 5.901015568784107934, -0.2851453878830525479, -1.890788771128081969 ) ) ;
#138559=CARTESIAN_POINT ( 'NONE',  ( 6.239861269555550649, 2.010826412442122013, -0.1511553674920090573 ) ) ;
#138565=CARTESIAN_POINT ( 'NONE',  ( 3.239063133055252841, -0.1400698962470778297, -1.964493882382233991 ) ) ;
#138566=CARTESIAN_POINT ( 'NONE',  ( 4.816029892389546596, 1.034148959857810190, -1.730877356967218894 ) ) ;
#138569=CARTESIAN_POINT ( 'NONE',  ( 4.523480939507462217, -1.347072049868164978, -1.728447516733351952 ) ) ;
#138570=CARTESIAN_POINT ( 'NONE',  ( 2.872000511136533873, 1.029149822700244465, 1.628267440728261573 ) ) ;
#138572=CARTESIAN_POINT ( 'NONE',  ( -0.02968770228137588424, 4.095675376368371090, -2.381331788581673159 ) ) ;
#138573=CARTESIAN_POINT ( 'NONE',  ( 0.03028722099337673168, -1.361824662662258767, -1.737358624739212321 ) ) ;
#138581=CARTESIAN_POINT ( 'NONE',  ( 0.8021671156859496721, 1.469769370800941166, -1.269469122775281456 ) ) ;
#138582=CARTESIAN_POINT ( 'NONE',  ( 2.526041439118778431, -1.990860190764773829, 0.2976642988744558904 ) ) ;
#138583=CARTESIAN_POINT ( 'NONE',  ( 5.132278277959533064, 0.2326997901972542582, -2.286600633956968220 ) ) ;
#138585=CARTESIAN_POINT ( 'NONE',  ( 3.291705155655884951, -1.246473628130102762, -1.382024748694546501 ) ) ;
#138588=CARTESIAN_POINT ( 'NONE',  ( 6.222915752822945734, 1.412394824171304908, -1.289504995239741714 ) ) ;
#138591=CARTESIAN_POINT ( 'NONE',  ( 5.513254163946260000, -2.039523011555996579, 0.4591751592910776614 ) ) ;
#138596=CARTESIAN_POINT ( 'NONE',  ( 0.9436603434208358232, 0.7422609627109194586, -1.668170528445270140 ) ) ;
#138599=CARTESIAN_POINT ( 'NONE',  ( 2.162404540820038967, 1.068076967457934012, 1.366050734290222834 ) ) ;
#138603=CARTESIAN_POINT ( 'NONE',  ( 0.4267348894952603944, -1.354911996285239617, 1.565345633960464111 ) ) ;
#138604=CARTESIAN_POINT ( 'NONE',  ( 5.092344371507952161, -1.812320225013038133, -0.2200062734805732223 ) ) ;
#138605=CARTESIAN_POINT ( 'NONE',  ( 3.151168776707893748, 1.684956273983062580, -1.004420888743910334 ) ) ;
#138609=CARTESIAN_POINT ( 'NONE',  ( 4.213620120093874988, 1.703795446819071691, 1.262174061880352083 ) ) ;
#138612=CARTESIAN_POINT ( 'NONE',  ( 2.149362472714404504, 1.803301116200561882, -1.016697834320609894 ) ) ;
#138615=CARTESIAN_POINT ( 'NONE',  ( 4.143395664610330265, 0.1093779850947790705, 2.218736840405158173 ) ) ;
#138617=CARTESIAN_POINT ( 'NONE',  ( 1.899501351379283554, -1.088314401552924249, -2.024763765589305820 ) ) ;
#138619=CARTESIAN_POINT ( 'NONE',  ( 6.192244813941197634, 1.021713635409545073, -1.791695130993501417 ) ) ;
#138622=CARTESIAN_POINT ( 'NONE',  ( 6.269096963164666469, 1.759884223096353173, -0.5412972069449849544 ) ) ;
#138626=CARTESIAN_POINT ( 'NONE',  ( 3.269685606991072468, 0.4601866041431811327, -1.856093204100267124 ) ) ;
#138627=CARTESIAN_POINT ( 'NONE',  ( -0.1106727585415837045, 2.018984206239351042, -2.418200238751634146 ) ) ;
#138628=CARTESIAN_POINT ( 'NONE',  ( 3.627714610788032701, -1.027129601966117134, -1.385419451709940519 ) ) ;
#138629=CARTESIAN_POINT ( 'NONE',  ( 2.694546298722868549, 1.457235452327232395, -1.394086077981852911 ) ) ;
#138631=CARTESIAN_POINT ( 'NONE',  ( 3.551692777231782561, -1.542557649656286944, 1.704429084079077006 ) ) ;
#138632=CARTESIAN_POINT ( 'NONE',  ( 3.603020308667020277, 1.786206176199186535, -1.388445577547703369 ) ) ;
#138633=CARTESIAN_POINT ( 'NONE',  ( 0.06543086261080394150, -1.973449318085427340, -0.9880335165917543128 ) ) ;
#138636=CARTESIAN_POINT ( 'NONE',  ( 4.692510491889085422, -0.3870912556891945577, -1.726709192852653230 ) ) ;
#138638=CARTESIAN_POINT ( 'NONE',  ( 1.025772235718758196, -1.457823864038493733, -1.768965695191491827 ) ) ;
#138639=CARTESIAN_POINT ( 'NONE',  ( 5.419803763747102821, 1.093575605593154920, -1.481025086994464113 ) ) ;
#138641=CARTESIAN_POINT ( 'NONE',  ( 5.507841377412062478, -0.9828142975771281264, -1.958786091674463714 ) ) ;
#138646=CARTESIAN_POINT ( 'NONE',  ( 6.232888004217203459, -1.964670499678453197, -0.6532144590316590893 ) ) ;
#138647=CARTESIAN_POINT ( 'NONE',  ( 0.4269707148552639997, -1.727061408318403712, 1.040797348915108111 ) ) ;
#138649=CARTESIAN_POINT ( 'NONE',  ( 4.072816532378962684, -1.798017144868354178, -0.6922151418781684606 ) ) ;
#138652=CARTESIAN_POINT ( 'NONE',  ( 0.6861347341944658007, 2.138861475627896080, -0.5996866306409093239 ) ) ;
#138662=CARTESIAN_POINT ( 'NONE',  ( 0.9593383959572501229, 1.601786533887459507, 1.132500672181527168 ) ) ;
#138665=CARTESIAN_POINT ( 'NONE',  ( 6.654749070045313353, -0.5220710138904552933, -1.891073168474053823 ) ) ;
#138670=CARTESIAN_POINT ( 'NONE',  ( 0.1107634673921135821, -0.9696846621911526798, -2.041722876818732324 ) ) ;
#138674=CARTESIAN_POINT ( 'NONE',  ( 1.211929638205839765, -0.8359089839212189288, -1.673436591668895579 ) ) ;
#138675=CARTESIAN_POINT ( 'NONE',  ( -0.1347034368660744441, -0.1421164721313403212, -1.704521202080215847 ) ) ;
#138678=CARTESIAN_POINT ( 'NONE',  ( 4.423480980095358284, -1.348712413769267426, -1.727291790683552541 ) ) ;
#138679=CARTESIAN_POINT ( 'NONE',  ( 4.559805550777903171, 0.5102292677348593264, -2.250327227043275702 ) ) ;
#138680=CARTESIAN_POINT ( 'NONE',  ( 6.538362368396775537, 2.037695317216736246, 0.3068575337649599444 ) ) ;
#138681=CARTESIAN_POINT ( 'NONE',  ( 1.921723552510564259, 1.118073055411296313, -1.587613466820477992 ) ) ;
#138687=CARTESIAN_POINT ( 'NONE',  ( 3.270157880292836605, 1.821742160604752137, -0.8647241845514613834 ) ) ;
#138691=CARTESIAN_POINT ( 'NONE',  ( 1.013953575274041619, -0.8186894766500467657, -1.631917417583013341 ) ) ;
#138695=EDGE_LOOP ( 'NONE', ( #31744, #178847, #100176, #29057 ) ) ;
#138696=CARTESIAN_POINT ( 'NONE',  ( 5.559468503951485729, 0.4043298029084033685, -2.020654889403751486 ) ) ;
#138701=CARTESIAN_POINT ( 'NONE',  ( 5.936196224836090884, -1.123750473735840361, -1.677956830082157236 ) ) ;
#138702=CARTESIAN_POINT ( 'NONE',  ( 5.619863295618399590, -0.5416267994347803150, 2.154155341088887177 ) ) ;
#138707=CARTESIAN_POINT ( 'NONE',  ( 4.346593572148568896, 0.5479209435249388083, 1.986652789453833057 ) ) ;
#138708=CARTESIAN_POINT ( 'NONE',  ( 3.621720349255663773, 0.2986264320336135536, 1.994071497604548382 ) ) ;
#138715=CARTESIAN_POINT ( 'NONE',  ( 3.778672575519220977, -1.986742196792599335, 0.3418835855632795795 ) ) ;
#138716=CARTESIAN_POINT ( 'NONE',  ( 3.837712106225504183, 1.832433245109680531, 0.1787696065849928018 ) ) ;
#138718=CARTESIAN_POINT ( 'NONE',  ( 1.840857126529979126, 2.283052885565831858, 0.3356036407394235033 ) ) ;
#138720=CARTESIAN_POINT ( 'NONE',  ( 3.304151629394710632, -2.159270932758147854, 0.1024373671053082913 ) ) ;
#138724=CARTESIAN_POINT ( 'NONE',  ( 3.567963868821962592, 1.814363981409074844, -1.410851157308941506 ) ) ;
#138726=CARTESIAN_POINT ( 'NONE',  ( 2.078771448894382701, -0.08914341469279044028, -1.868647664167771616 ) ) ;
#138727=CARTESIAN_POINT ( 'NONE',  ( 6.368046306259418365, 1.013251383440600284, 1.691012432383535602 ) ) ;
#138731=CARTESIAN_POINT ( 'NONE',  ( 1.805583701156989518, 1.836052299496168771, 1.224139149458243425 ) ) ;
#138736=CARTESIAN_POINT ( 'NONE',  ( 6.297732458894883756, -0.6644727202288897017, 1.856229495857963263 ) ) ;
#138737=CARTESIAN_POINT ( 'NONE',  ( 6.182281242350501138, -1.240197753460486663, 1.945954285860839850 ) ) ;
#138738=CARTESIAN_POINT ( 'NONE',  ( 0.2913577194270203785, -1.795273245208812485, 0.7915465721433642132 ) ) ;
#138739=CARTESIAN_POINT ( 'NONE',  ( 2.536046341495324707, 1.265347977242038402, 1.628790341535201636 ) ) ;
#138746=CARTESIAN_POINT ( 'NONE',  ( 5.107971825378077924, 0.6857059611327814830, -2.060108355502160649 ) ) ;
#138747=CARTESIAN_POINT ( 'NONE',  ( 6.539320575229249144, 0.007148032025052972194, 1.896977914940492393 ) ) ;
#138748=CARTESIAN_POINT ( 'NONE',  ( 4.634224865634020141, 0.3196297827482602050, 1.813140464320086132 ) ) ;
#138752=CARTESIAN_POINT ( 'NONE',  ( 0.4041009963523278237, -0.6015683965250936405, 2.180870993196832419 ) ) ;
#138756=CARTESIAN_POINT ( 'NONE',  ( 0.2055213853429035953, 1.417038256915002181, 1.284265443176696442 ) ) ;
#138758=CARTESIAN_POINT ( 'NONE',  ( 2.008344819247428248, 1.313797796480600244, -1.186068062872788209 ) ) ;
#138760=CARTESIAN_POINT ( 'NONE',  ( 0.1000639402851908749, -0.9014739813196898099, 1.686438745833309438 ) ) ;
#138762=CARTESIAN_POINT ( 'NONE',  ( 3.603066768525709396, -0.1374138116273740384, 1.910719597520103896 ) ) ;
#138764=CARTESIAN_POINT ( 'NONE',  ( 4.316829372628319561, -1.460888098903726728, 1.321172513512254065 ) ) ;
#138765=CARTESIAN_POINT ( 'NONE',  ( -0.03470293633787284449, -1.699275230904277789, 1.268407768021381221 ) ) ;
#138767=CARTESIAN_POINT ( 'NONE',  ( 2.641296366799699147, -1.384790685969448099, -1.257831364775918503 ) ) ;
#138768=CARTESIAN_POINT ( 'NONE',  ( 6.322847717702526182, 1.612277268089978621, 0.6135241758537502976 ) ) ;
#138770=CARTESIAN_POINT ( 'NONE',  ( 2.825073394047578734, 2.078234123670623212, 0.7428476018367863309 ) ) ;
#138773=CARTESIAN_POINT ( 'NONE',  ( 6.877413162628407406, -0.1429737755889188000, 1.930079329684093237 ) ) ;
#138776=CARTESIAN_POINT ( 'NONE',  ( 0.1747926744264660381, 0.006858446013176254172, -1.855468577918440776 ) ) ;
#138780=CARTESIAN_POINT ( 'NONE',  ( 3.332542965736586371, -1.235447621225284509, 1.661183390374972424 ) ) ;
#138784=CARTESIAN_POINT ( 'NONE',  ( 0.3990893844944528590, -0.2493554465154389221, -2.004162882155545056 ) ) ;
#138787=CARTESIAN_POINT ( 'NONE',  ( 0.1749903794560384862, 2.035240947854660920, -2.372290655319588382 ) ) ;
#138789=CARTESIAN_POINT ( 'NONE',  ( 5.729842239849809893, -1.821464125411855983, -0.8645900286049985617 ) ) ;
#138790=CARTESIAN_POINT ( 'NONE',  ( 5.419116407314492179, -1.729028094342921706, 0.8252531017051125684 ) ) ;
#138791=CARTESIAN_POINT ( 'NONE',  ( 6.539320575229280230, 7.629137130509070275, 2.703262396134015866 ) ) ;
#138792=CARTESIAN_POINT ( 'NONE',  ( 3.702820756938397295, 1.880440254450808757, 1.125299312022425280 ) ) ;
#138794=CARTESIAN_POINT ( 'NONE',  ( 2.461071540317420148, -1.587761714688112002, 1.065645112462119570 ) ) ;
#138798=CARTESIAN_POINT ( 'NONE',  ( 1.441030037510174777, -1.730879250949714843, -1.034145807338890277 ) ) ;
#138800=CARTESIAN_POINT ( 'NONE',  ( -0.1288028175206907822, -0.008968661790493319408, -2.273875003271645934 ) ) ;
#138802=CARTESIAN_POINT ( 'NONE',  ( 3.135487559415173653, -1.157359333423061409, -1.278988843622446137 ) ) ;
#138804=CARTESIAN_POINT ( 'NONE',  ( 6.328397690248316110, -1.000878058022572903, -1.869571840794107986 ) ) ;
#138809=CARTESIAN_POINT ( 'NONE',  ( 0.5901948623465642640, 1.011764341257429978, -1.680720577067334354 ) ) ;
#138815=CARTESIAN_POINT ( 'NONE',  ( 3.088311256162243446, -1.077087438943722164, 1.456314016777765286 ) ) ;
#138819=CARTESIAN_POINT ( 'NONE',  ( 3.598146505595464006, -0.8898571075792599538, 1.577739831003275084 ) ) ;
#138824=CARTESIAN_POINT ( 'NONE',  ( 5.248444859377932481, -1.846993913715170077, -0.2278608691909170259 ) ) ;
#138827=CARTESIAN_POINT ( 'NONE',  ( 2.196773704658647297, 1.712196953037805613, 0.8591283806286521552 ) ) ;
#138838=CARTESIAN_POINT ( 'NONE',  ( 1.746151220907150359, 0.6571888886500141247, 1.984721739902342019 ) ) ;
#138839=CARTESIAN_POINT ( 'NONE',  ( 6.721714886968523928, -1.868385559882647318, 0.4688378381374983528 ) ) ;
#138841=CARTESIAN_POINT ( 'NONE',  ( 2.063248287022978467, 0.3151258922809499485, -1.798016661460503984 ) ) ;
#138842=CARTESIAN_POINT ( 'NONE',  ( 3.123846942790895920, -2.126788776302591888, 0.5888931905130635469 ) ) ;
#138844=CARTESIAN_POINT ( 'NONE',  ( 1.160255710619631397, 1.910328232974867868, 0.09094507755665059978 ) ) ;
#138845=CARTESIAN_POINT ( 'NONE',  ( 1.697640821309716497, -1.424308401971938975, -1.360563176039381261 ) ) ;
#138846=CARTESIAN_POINT ( 'NONE',  ( 4.229980187955574067, 1.905242447948073403, 0.3755566216582290617 ) ) ;
#138850=CARTESIAN_POINT ( 'NONE',  ( 6.719592977537645062, 0.3186052404706584129, -1.833303987817246794 ) ) ;
#138855=CARTESIAN_POINT ( 'NONE',  ( 2.788834510562918645, 1.878274557074947948, -1.128960604485473862 ) ) ;
#138861=CARTESIAN_POINT ( 'NONE',  ( 3.633261591126951018, -1.686358373764598406, 0.7000054678709469735 ) ) ;
#138865=DIRECTION ( 'NONE',  ( 1.040834085586084257E-15, 1.000000000000000000, -4.622230424712076367E-32 ) ) ;
#138866=CARTESIAN_POINT ( 'NONE',  ( 4.100366707588389836, -0.5864361863821172527, -1.776433678864146382 ) ) ;
#138868=CARTESIAN_POINT ( 'NONE',  ( 2.455585946167909928, 0.5135756288857267204, -1.856723504524477875 ) ) ;
#138869=CARTESIAN_POINT ( 'NONE',  ( 6.368018226480639754, -1.947316962026977682, 0.2367824842242904348 ) ) ;
#138875=CARTESIAN_POINT ( 'NONE',  ( 0.5798918133415768006, -0.7576680531077238934, 1.977200763303339714 ) ) ;
#138878=CARTESIAN_POINT ( 'NONE',  ( 4.926661076633905623, -1.356332079400805135, 1.564123780295342492 ) ) ;
#138879=CARTESIAN_POINT ( 'NONE',  ( 0.3976880421775743635, -0.6195963491163231085, -1.733980255833282191 ) ) ;
#138882=CARTESIAN_POINT ( 'NONE',  ( 5.098365541279441082, -0.3395090112114571013, 2.273368781073564993 ) ) ;
#138886=CARTESIAN_POINT ( 'NONE',  ( 0.4458144982435990888, 0.7132466706018144587, -2.178543642160748917 ) ) ;
#138889=CARTESIAN_POINT ( 'NONE',  ( 5.103436805131417842, -1.932407887632971555, 0.1922973783335303055 ) ) ;
#138890=EDGE_LOOP ( 'NONE', ( #60711, #159566, #68857, #146826 ) ) ;
#138894=CARTESIAN_POINT ( 'NONE',  ( -0.2106854629475244378, -0.004120941679102134263, -1.996958217618934661 ) ) ;
#138895=CARTESIAN_POINT ( 'NONE',  ( 6.069546051295944267, 1.394081536189459847, 1.457239770841619375 ) ) ;
#138899=CARTESIAN_POINT ( 'NONE',  ( 3.082061393860520138, -2.059794914563463308, -0.3567947225071969042 ) ) ;
#138900=CARTESIAN_POINT ( 'NONE',  ( 1.375481398426938284, 1.050436561215197351, 1.424246879149461797 ) ) ;
#138903=CARTESIAN_POINT ( 'NONE',  ( 4.119262515598776098, -2.194098707595509623, 0.6636001952689452033 ) ) ;
#138905=CARTESIAN_POINT ( 'NONE',  ( 2.273056812072488775, 1.069988629298643579, 1.372433606717870846 ) ) ;
#138908=CARTESIAN_POINT ( 'NONE',  ( 2.020412548985677681, 1.729603159991144556, -0.1218859752038989053 ) ) ;
#138910=CARTESIAN_POINT ( 'NONE',  ( 1.293147247811817779, -1.684623093139308025, 0.7912131235938785201 ) ) ;
#138911=CARTESIAN_POINT ( 'NONE',  ( 2.383468162319524630, -0.001743713053406481962, 2.171350059665664300 ) ) ;
#138913=CARTESIAN_POINT ( 'NONE',  ( 3.591030000661588062, 1.731995077137841843, 1.032480907900306111 ) ) ;
#138914=CARTESIAN_POINT ( 'NONE',  ( 1.781250000000001332, 0.7852924748300815772, 1.895863743164048154 ) ) ;
#138917=CARTESIAN_POINT ( 'NONE',  ( 0.5340448022827409824, 0.9932739084477918423, -1.650449964952714454 ) ) ;
#138919=CARTESIAN_POINT ( 'NONE',  ( 4.535507215201760367, -0.1075840215562298280, 2.218897223943790742 ) ) ;
#138926=CARTESIAN_POINT ( 'NONE',  ( 1.032228388637240313, -2.166051452891520679, 0.4916964420428306948 ) ) ;
#138927=CARTESIAN_POINT ( 'NONE',  ( 6.215287892896892430, -1.681934637451238279, -1.009743211781432670 ) ) ;
#138929=CARTESIAN_POINT ( 'NONE',  ( 5.466221857368295467, 1.108383815247836690, 1.972225493889906867 ) ) ;
#138931=CARTESIAN_POINT ( 'NONE',  ( 3.719230382982277927, -1.817711772858042751, -0.9750064267827946995 ) ) ;
#138935=CARTESIAN_POINT ( 'NONE',  ( 4.323419078940895943, -1.790677508454678657, 0.5408235849187342792 ) ) ;
#138936=CARTESIAN_POINT ( 'NONE',  ( 3.674194220352343443, 1.259077133501560697, 1.192749331401379731 ) ) ;
#138937=CARTESIAN_POINT ( 'NONE',  ( 3.579424886596099586, -0.8542006638617373193, 1.516299650553302181 ) ) ;
#138939=CARTESIAN_POINT ( 'NONE',  ( 0.3106431952284515741, 1.574884954006963600, -1.665989127006389126 ) ) ;
#138941=CARTESIAN_POINT ( 'NONE',  ( 4.915614241032515430, -1.119620181645267776, -1.765504464341709934 ) ) ;
#138942=CARTESIAN_POINT ( 'NONE',  ( 5.824156380204161820, 1.872177270857039000, 0.5156464658115608168 ) ) ;
#138945=CARTESIAN_POINT ( 'NONE',  ( 0.5982800022500452952, -0.2930678230431381648, 1.994870242743536304 ) ) ;
#138946=CARTESIAN_POINT ( 'NONE',  ( 0.3871773095200456982, -1.998849835692744659, -0.7086421328065874992 ) ) ;
#138952=CARTESIAN_POINT ( 'NONE',  ( 4.723181480036696023, -0.08661695748878039947, 1.823760500460340550 ) ) ;
#138959=CARTESIAN_POINT ( 'NONE',  ( 2.232681213900446160, 1.316219961256912763, -1.532148775131780383 ) ) ;
#138960=CARTESIAN_POINT ( 'NONE',  ( 6.159228477734898455, -1.889628185881117695, -1.139594184263223120 ) ) ;
#138962=CARTESIAN_POINT ( 'NONE',  ( 3.115880741807099508, 1.852434257297396858, -0.1774315261868253668 ) ) ;
#138969=CARTESIAN_POINT ( 'NONE',  ( 5.391160240453525709, 1.608232483172780558, -0.8641324296934371763 ) ) ;
#138973=CARTESIAN_POINT ( 'NONE',  ( 0.8953158854557360380, 0.1194439997053517860, 1.729786500971510765 ) ) ;
#138974=CARTESIAN_POINT ( 'NONE',  ( 0.005214030526056419486, -0.7400075616556491820, -1.574097848898856622 ) ) ;
#138975=CARTESIAN_POINT ( 'NONE',  ( 5.901056178406707708, 1.890114102979102650, -1.323741089068092958 ) ) ;
#138977=CARTESIAN_POINT ( 'NONE',  ( 0.5267265402719328860, 1.971218143044730420, 0.6008300406652696823 ) ) ;
#138979=CARTESIAN_POINT ( 'NONE',  ( 5.747524558462486333, -2.240600987983232262, -0.5116226552598357458 ) ) ;
#138984=CARTESIAN_POINT ( 'NONE',  ( 6.051601594667258333, 0.5412791183288803154, -1.790613848972313571 ) ) ;
#138985=CARTESIAN_POINT ( 'NONE',  ( 3.252119977711815491, 0.8557668478980616777, -1.710280963351323846 ) ) ;
#138987=CARTESIAN_POINT ( 'NONE',  ( 4.811249113497881424, 1.919052844561389692, 1.089612025192594258 ) ) ;
#138988=CARTESIAN_POINT ( 'NONE',  ( 4.786377933101198856, -0.7163331637287263520, -1.992584184115009149 ) ) ;
#138990=CARTESIAN_POINT ( 'NONE',  ( 6.883263157960393563, 4.695771316066229772, 2.508818740863460572 ) ) ;
#138991=CARTESIAN_POINT ( 'NONE',  ( -0.2108831679770960255, -0.001785917861228669690, -1.896958272444612792 ) ) ;
#138994=CARTESIAN_POINT ( 'NONE',  ( 5.426475896148662770, -0.9536019125786737716, -1.894055658958586852 ) ) ;
#138995=CARTESIAN_POINT ( 'NONE',  ( 2.591229953566904776, -0.3941274307956154077, -2.273529888306951019 ) ) ;
#138996=CARTESIAN_POINT ( 'NONE',  ( 4.193769882565239193, -1.351282707657221582, -1.422545440481419510 ) ) ;
#138997=CARTESIAN_POINT ( 'NONE',  ( 6.297729475711208558, -1.489980986158835119, -1.426453875638087343 ) ) ;
#139001=CARTESIAN_POINT ( 'NONE',  ( 5.717982508692024624, 0.9896897593998502662, -1.756851901128737348 ) ) ;
#139005=CARTESIAN_POINT ( 'NONE',  ( 2.905323041198346612, -1.807408099546173208, 1.202558989554833646 ) ) ;
#139007=CARTESIAN_POINT ( 'NONE',  ( 1.143014088299774578, 2.045220145331683614, 0.5602274146137007360 ) ) ;
#139011=CARTESIAN_POINT ( 'NONE',  ( 0.8079727292511580394, -2.051105382888893658, 0.1991618667988598601 ) ) ;
#139014=CARTESIAN_POINT ( 'NONE',  ( 6.727182134110231360, 6.039168392632435989, 2.405853653942995773 ) ) ;
#139017=ORIENTED_EDGE ( 'NONE', *, *, #25165, .F. ) ;
#139018=CARTESIAN_POINT ( 'NONE',  ( 3.826736342760712173, 1.350229473097919630, -1.354399478966497483 ) ) ;
#139019=CARTESIAN_POINT ( 'NONE',  ( 5.137463350450376609, -1.253266684191740810, -1.249936613051380485 ) ) ;
#139022=CARTESIAN_POINT ( 'NONE',  ( 0.01741795466771427214, -0.4834593703179098645, 1.745828368453090418 ) ) ;
#139024=CARTESIAN_POINT ( 'NONE',  ( 6.327746003090493510, 0.7280626223893000848, -1.772066133663487530 ) ) ;
#139025=CARTESIAN_POINT ( 'NONE',  ( 1.188034388246852480, -1.312013912954514971, -1.601590607232979524 ) ) ;
#139028=CARTESIAN_POINT ( 'NONE',  ( 5.840666405660361882, 0.3664468388623157158, 1.834233659845653897 ) ) ;
#139029=CARTESIAN_POINT ( 'NONE',  ( 2.314841291766779108, 1.630546960418734148, 0.8213866120303781049 ) ) ;
#139030=CARTESIAN_POINT ( 'NONE',  ( 5.162800556355915838, -1.600310254184673431, 1.519886962452212664 ) ) ;
#139033=CARTESIAN_POINT ( 'NONE',  ( 3.842276591979614242, -1.019319043456867524, 1.793165911747495844 ) ) ;
#139037=CARTESIAN_POINT ( 'NONE',  ( 6.215297738502283842, -1.773692237561547147, -1.067698627785176768 ) ) ;
#139039=CARTESIAN_POINT ( 'NONE',  ( 4.112696061561730509, 1.531809107248631507, -1.525399859652858847 ) ) ;
#139040=CARTESIAN_POINT ( 'NONE',  ( 4.617835026475571425, -0.5366920026289195844, 1.946999912814169287 ) ) ;
#139041=CARTESIAN_POINT ( 'NONE',  ( 1.662477996687723669, -0.7030478115006146833, -1.831755296705489977 ) ) ;
#139047=CARTESIAN_POINT ( 'NONE',  ( 2.413296319342159713, -1.879803466158457059, 0.7303082167480907660 ) ) ;
#139050=CARTESIAN_POINT ( 'NONE',  ( 6.187759705938407073, 1.828009178079874841, -0.5617473972939349691 ) ) ;
#139054=CARTESIAN_POINT ( 'NONE',  ( 4.060172857048785389, -1.158672032380179573, 1.650094836768666084 ) ) ;
#139057=CARTESIAN_POINT ( 'NONE',  ( 6.809587843971872445, -0.3681478646948634914, 1.690922663601742038 ) ) ;
#139061=CARTESIAN_POINT ( 'NONE',  ( 4.516781199771729760, 1.709404882366181377, 0.7599583452636837766 ) ) ;
#139064=CARTESIAN_POINT ( 'NONE',  ( 2.553653463975919635, 1.597511423921485818, 1.316731848974454833 ) ) ;
#139070=CARTESIAN_POINT ( 'NONE',  ( 0.2808753465170962249, 1.674874268995883320, -1.122520385770639839 ) ) ;
#139071=CARTESIAN_POINT ( 'NONE',  ( -0.1935108285373255133, -0.3924519521045151671, -1.774502223569380144 ) ) ;
#139078=CARTESIAN_POINT ( 'NONE',  ( 6.362892188913578551, -0.09940890854263698118, -1.913169475778592865 ) ) ;
#139083=CARTESIAN_POINT ( 'NONE',  ( 3.485389320157119553, 1.955090977548096687, -0.9225387301767663528 ) ) ;
#139086=CARTESIAN_POINT ( 'NONE',  ( 1.336355901170083849, -1.182550835430173919, -1.760063440837428272 ) ) ;
#139087=CARTESIAN_POINT ( 'NONE',  ( 5.860330175037710809, 0.7421476303169189936, 1.668095884353037128 ) ) ;
#139089=CARTESIAN_POINT ( 'NONE',  ( 1.669145487688096896, 0.1492116152736686074, -1.965789094590511654 ) ) ;
#139090=CARTESIAN_POINT ( 'NONE',  ( 3.340010735810138520, -1.142844047782382466, -1.533173144288489276 ) ) ;
#139092=CARTESIAN_POINT ( 'NONE',  ( 5.283641479639247684, -1.870778298764510961, 0.6161543930274359093 ) ) ;
#139093=CARTESIAN_POINT ( 'NONE',  ( -0.02948999725180690215, 0.001137248348246927814, -1.926291057026579656 ) ) ;
#139098=CARTESIAN_POINT ( 'NONE',  ( 4.758414378865199801, 1.907420806491459064, 0.1369992607160031295 ) ) ;
#139100=CARTESIAN_POINT ( 'NONE',  ( 1.290363523627102049, -0.9912053058820712304, 1.971723787660728977 ) ) ;
#139103=CARTESIAN_POINT ( 'NONE',  ( 5.988937038716908745, -1.912324646158647168, -0.6291777902352905238 ) ) ;
#139106=CARTESIAN_POINT ( 'NONE',  ( 1.873570696236816158, -0.2555354716398828274, 2.054483085851127377 ) ) ;
#139109=CARTESIAN_POINT ( 'NONE',  ( 0.2687375195599971400, -1.410744835756465365, 1.637978619736128127 ) ) ;
#139115=CARTESIAN_POINT ( 'NONE',  ( 6.825078400183573812, 7.629137130509070275, 2.455651831298297338 ) ) ;
#139117=CARTESIAN_POINT ( 'NONE',  ( 4.570818470097482766, -0.8114142876072638622, 1.532583664885181607 ) ) ;
#139120=CARTESIAN_POINT ( 'NONE',  ( 2.254815949590884827, -0.5480598642870064818, -1.996355599893632649 ) ) ;
#139121=CARTESIAN_POINT ( 'NONE',  ( 3.409862312649377003, -1.263030510572001885, -1.699084664797428479 ) ) ;
#139124=CARTESIAN_POINT ( 'NONE',  ( 1.990998161727207449, 0.1877779126488627881, 1.960439330322023999 ) ) ;
#139126=CARTESIAN_POINT ( 'NONE',  ( 6.411931881972196610E-05, -0.8997486769052507327, 1.687471195204979457 ) ) ;
#139127=CARTESIAN_POINT ( 'NONE',  ( 4.048992419199006321, -1.904907007256863904, -1.274792539085588539 ) ) ;
#139128=CARTESIAN_POINT ( 'NONE',  ( 1.260069262837599791, 0.7379878962356714034, 1.670071910705408946 ) ) ;
#139132=CARTESIAN_POINT ( 'NONE',  ( 2.636979257498579088, 1.897111442976556317, 0.6741904779793208569 ) ) ;
#139133=CARTESIAN_POINT ( 'NONE',  ( 3.344534541303633368, -1.931932779036081183, -0.3399374921491463142 ) ) ;
#139137=CARTESIAN_POINT ( 'NONE',  ( 6.439408583351804438, 0.8014019654560710082, -1.931139719275380084 ) ) ;
#139138=CARTESIAN_POINT ( 'NONE',  ( 4.205725695155067889, -1.765064932122958785, 0.1306522685067777467 ) ) ;
#139140=CARTESIAN_POINT ( 'NONE',  ( 0.8322822162843239724, 2.159637434087835928, 0.3711470721824081109 ) ) ;
#139141=CARTESIAN_POINT ( 'NONE',  ( 5.771390581163715616, 1.041905927170128754, 1.393825671036960534 ) ) ;
#139142=CIRCLE ( 'NONE', #7703, 0.04999999999999929501 ) ;
#139144=CARTESIAN_POINT ( 'NONE',  ( 0.1331715793776418189, 2.029267568408019695, -2.369146612602909041 ) ) ;
#139145=CARTESIAN_POINT ( 'NONE',  ( 6.434253291069976122, -1.843495385113643525, -1.373021106398547131 ) ) ;
#139147=CARTESIAN_POINT ( 'NONE',  ( 5.466046595369183692, 1.418568314722228996, 0.9965602304959333413 ) ) ;
#139148=CARTESIAN_POINT ( 'NONE',  ( 1.489210700298746692, -0.3264265768355456010, -2.182489157894373033 ) ) ;
#139149=CARTESIAN_POINT ( 'NONE',  ( 5.459503713743925069, 1.771904602436706222, 1.254488129281390751 ) ) ;
#139151=CARTESIAN_POINT ( 'NONE',  ( 0.8138397394129359697, -1.348031465540124207, -1.632742428372506049 ) ) ;
#139152=CARTESIAN_POINT ( 'NONE',  ( 4.468750000000002665, 0.7852924748297492874, -1.895863743164178494 ) ) ;
#139153=CARTESIAN_POINT ( 'NONE',  ( 6.827182134110223011, 1.235230467647760788, 2.302354205009625954 ) ) ;
#139154=CARTESIAN_POINT ( 'NONE',  ( 4.436495903120683870, 1.889097993355067562, 0.3764034397915373975 ) ) ;
#139155=CARTESIAN_POINT ( 'NONE',  ( 1.506789913206330489, -2.211016841974380309, -0.2134033219785695379 ) ) ;
#139160=CARTESIAN_POINT ( 'NONE',  ( 4.002737143027909283, -2.197200394838841664, -0.3254818186308478523 ) ) ;
#139166=CARTESIAN_POINT ( 'NONE',  ( 2.004529941291322448, -1.955172360644286789, 0.4926429297785542283 ) ) ;
#139168=CARTESIAN_POINT ( 'NONE',  ( 6.795384964414455276, -1.844194740592384196, 0.9240657454356243639 ) ) ;
#139171=CARTESIAN_POINT ( 'NONE',  ( 6.198757988109700356, 1.452298656357524864, 0.9588401209737663633 ) ) ;
#139174=CARTESIAN_POINT ( 'NONE',  ( 1.528175773270981308, 1.703719318302211683, 0.4785495757857262666 ) ) ;
#139175=CARTESIAN_POINT ( 'NONE',  ( 0.4225002777262388265, -1.427939226333583500, -1.423959630194884696 ) ) ;
#139176=CARTESIAN_POINT ( 'NONE',  ( 6.198757988109700356, 1.452298656357524864, 0.9588401209737663633 ) ) ;
#139177=CARTESIAN_POINT ( 'NONE',  ( 4.230218865515364968, 2.248128804489764043, 0.4474220685124987162 ) ) ;
#139178=CARTESIAN_POINT ( 'NONE',  ( 2.132514540308296791, -1.644867172388216003, 0.8273176719292076875 ) ) ;
#139181=CARTESIAN_POINT ( 'NONE',  ( 3.381694320706640333, 1.157239582903809128, 1.411935816614327655 ) ) ;
#139182=CARTESIAN_POINT ( 'NONE',  ( 3.850232551101365086, 0.2440307281281335616, -2.001511205109906655 ) ) ;
#139184=CARTESIAN_POINT ( 'NONE',  ( 3.801889278938491934, -0.6593813483589389124, 2.164292034026161549 ) ) ;
#139186=CARTESIAN_POINT ( 'NONE',  ( 5.174884205284945082, -1.981925234046210571, -0.7124256662833851061 ) ) ;
#139188=CARTESIAN_POINT ( 'NONE',  ( 2.611853368047814872, 0.5545374748289233491, -1.994631108499920646 ) ) ;
#139191=CARTESIAN_POINT ( 'NONE',  ( 5.496778590849229040, -2.068848325035842706, -0.4644329061709790429 ) ) ;
#139193=CARTESIAN_POINT ( 'NONE',  ( 1.066875820281657949, -1.741210523058086324, -0.8246449397346886645 ) ) ;
#139201=CARTESIAN_POINT ( 'NONE',  ( 0.7564555125054818197, 0.8934716743186126298, -2.033981271184843731 ) ) ;
#139202=CARTESIAN_POINT ( 'NONE',  ( 1.940588816512535120, 2.082954711654343427, 0.3096100588686269695 ) ) ;
#139205=CARTESIAN_POINT ( 'NONE',  ( 6.174622966819019787, 1.250768081284852951, -1.378062710742117059 ) ) ;
#139209=CARTESIAN_POINT ( 'NONE',  ( 0.3344391967911933272, -1.139684030083350841, -1.788147294700337397 ) ) ;
#139212=CARTESIAN_POINT ( 'NONE',  ( 3.174217076811707727, -0.9646401420641316227, -1.708233030250068785 ) ) ;
#139213=CARTESIAN_POINT ( 'NONE',  ( 2.501032641837992454, 1.736685530831501456, -1.287010829427559289 ) ) ;
#139214=CARTESIAN_POINT ( 'NONE',  ( 1.012948470060770934, -1.796336717620912626, 0.4034172393945419377 ) ) ;
#139218=CARTESIAN_POINT ( 'NONE',  ( 3.081702191724482454, -1.714667182045168214, -0.2967042344550906985 ) ) ;
#139221=CARTESIAN_POINT ( 'NONE',  ( 1.235488887756378551, -1.954010380348418119, 0.9248176494114216384 ) ) ;
#139222=CARTESIAN_POINT ( 'NONE',  ( 2.214220036344019871, -1.617569417291262690, -1.203170845901546215 ) ) ;
#139224=CARTESIAN_POINT ( 'NONE',  ( 0.6378455412261313517, -1.529572671500577297, -1.527792216034072670 ) ) ;
#139226=CARTESIAN_POINT ( 'NONE',  ( 2.307442625383813617, -0.4335913300187159702, 1.923040929009907973 ) ) ;
#139232=CARTESIAN_POINT ( 'NONE',  ( -0.2108831679770926115, 5.723481173670196043, -2.491210874135452613 ) ) ;
#139235=CARTESIAN_POINT ( 'NONE',  ( 2.684245096118286877, 1.082265567382127758, 1.705031398228576078 ) ) ;
#139238=CARTESIAN_POINT ( 'NONE',  ( 5.737451576302465384, -2.089288847444936259, 0.9800045452074584995 ) ) ;
#139239=CARTESIAN_POINT ( 'NONE',  ( 6.654749070045313353, -0.5220710138904552933, -1.891073168474053823 ) ) ;
#139240=CARTESIAN_POINT ( 'NONE',  ( 4.188298518248589453, 1.053080760608171129, -1.654974388233184657 ) ) ;
#139243=CARTESIAN_POINT ( 'NONE',  ( 0.1060925565549031974, -0.09613213100253051313, 2.014232862735332308 ) ) ;
#139245=CARTESIAN_POINT ( 'NONE',  ( 1.973964399615803389, -0.9004667817871301327, 1.916432390954267984 ) ) ;
#139249=CARTESIAN_POINT ( 'NONE',  ( 2.413779523973126118, 1.202770565240804279, -1.394052804434331216 ) ) ;
#139253=CARTESIAN_POINT ( 'NONE',  ( 3.726904977748810133, 1.497142547446396410, -1.502090761940577002 ) ) ;
#139254=CARTESIAN_POINT ( 'NONE',  ( 0.09336763325077861164, -1.840659761701424646, -0.04852334659839750014 ) ) ;
#139259=CARTESIAN_POINT ( 'NONE',  ( 4.604794268142059721, 1.595455460008918580, -1.304385708662815002 ) ) ;
#139262=CARTESIAN_POINT ( 'NONE',  ( 1.522747961674526085, -1.733470594775164075, 0.6210259959333885860 ) ) ;
#139267=CARTESIAN_POINT ( 'NONE',  ( 0.6278963055918493907, -2.094311335337955882, 0.6960538111202837497 ) ) ;
#139268=CARTESIAN_POINT ( 'NONE',  ( 3.251526197659323270, -1.847530484110882387, -1.305540666510462078 ) ) ;
#139270=CARTESIAN_POINT ( 'NONE',  ( 3.287185820011778947, 0.03942761580559561718, -1.811315726287704431 ) ) ;
#139271=CARTESIAN_POINT ( 'NONE',  ( 3.731564767512856040, 0.6402975007456043199, -1.805710188498848456 ) ) ;
#139272=CARTESIAN_POINT ( 'NONE',  ( 5.477033855465498924, 1.911541192706748715, 0.7957256658025002594 ) ) ;
#139274=CARTESIAN_POINT ( 'NONE',  ( 2.360178788647437464, 0.8414710005770206225, 1.782988266942896693 ) ) ;
#139275=CARTESIAN_POINT ( 'NONE',  ( 0.7449895426413064570, -1.653788825565579046, 0.9876836116205435223 ) ) ;
#139276=CARTESIAN_POINT ( 'NONE',  ( 3.485083742438867649, 1.691615344724434200, -0.7988839237506044633 ) ) ;
#139277=CARTESIAN_POINT ( 'NONE',  ( 1.946342613620454243, 0.8805590942474375016, -2.133279852835685109 ) ) ;
#139278=CARTESIAN_POINT ( 'NONE',  ( 3.648742529127374734, -0.3609857515115758586, -1.825517407628447053 ) ) ;
#139285=CARTESIAN_POINT ( 'NONE',  ( 0.4871192430246041316, -0.2598372338927424918, -2.089908867234680834 ) ) ;
#139289=CARTESIAN_POINT ( 'NONE',  ( 1.705496241919310707, 1.842552997918958768, -1.049655202612943095 ) ) ;
#139291=CARTESIAN_POINT ( 'NONE',  ( 0.3869806665078223129, -1.903265420633104332, -0.6765555904410057719 ) ) ;
#139296=CARTESIAN_POINT ( 'NONE',  ( 1.493687833870473325, 1.635750924671933282, 1.413141523588061776 ) ) ;
#139302=CARTESIAN_POINT ( 'NONE',  ( 5.876185452347599814, -2.007255679753978228, -0.1928398672442974138 ) ) ;
#139304=CARTESIAN_POINT ( 'NONE',  ( 0.1874131419884322858, 1.628132678060219884, 1.467219630700428157 ) ) ;
#139306=CARTESIAN_POINT ( 'NONE',  ( 6.825078400183575589, -0.005632053428735600553, 2.144262460745151255 ) ) ;
#139310=CARTESIAN_POINT ( 'NONE',  ( 0.8783700953360704666, -0.4667435877003899836, -1.857722024819864037 ) ) ;
#139315=CARTESIAN_POINT ( 'NONE',  ( 2.965164839364425653, 0.2526306750327989015, -1.706137528056344888 ) ) ;
#139317=CARTESIAN_POINT ( 'NONE',  ( 1.493014682725684938, 1.335586794047480153, 1.161194053514543745 ) ) ;
#139318=CARTESIAN_POINT ( 'NONE',  ( 1.664698924820615433, 0.6334283372178346472, 1.910891431425953302 ) ) ;
#139320=CARTESIAN_POINT ( 'NONE',  ( 3.733602637680955461, -2.039903990487580643, 0.8422819887162477093 ) ) ;
#139324=CARTESIAN_POINT ( 'NONE',  ( 3.897227946829431300, -0.2092540311423168320, -2.110150122182581356 ) ) ;
#139325=CARTESIAN_POINT ( 'NONE',  ( 4.394157760337158436, -0.8647400765994192051, -1.821735888681835336 ) ) ;
#139326=CARTESIAN_POINT ( 'NONE',  ( 4.464998409566146798, -1.450835031669978292, 1.084616504919968305 ) ) ;
#139331=CARTESIAN_POINT ( 'NONE',  ( 1.111929834214450796, -0.8377583890188080584, -1.672643128629976772 ) ) ;
#139342=CARTESIAN_POINT ( 'NONE',  ( 4.676102344489991403, 2.097148071331572439, -0.3138259731317455392 ) ) ;
#139343=CARTESIAN_POINT ( 'NONE',  ( -0.1294898018152201291, 4.092224548688067287, -2.481517387982924649 ) ) ;
#139345=CARTESIAN_POINT ( 'NONE',  ( 5.817641553194794035, -1.923906765362886961, 0.4292884390787749527 ) ) ;
#139347=CARTESIAN_POINT ( 'NONE',  ( 0.9143154035033382865, -2.013376230895477903, 0.004183558276700528357 ) ) ;
#139349=CARTESIAN_POINT ( 'NONE',  ( 6.503150284217945831, -0.1439854277452867481, 2.084527530714448407 ) ) ;
#139351=CARTESIAN_POINT ( 'NONE',  ( 1.047426762419433777, 1.826728496382063582, -0.9743617655595809834 ) ) ;
#139355=CARTESIAN_POINT ( 'NONE',  ( 3.046908718545093819, -1.709425224762064266, -1.203301715110078662 ) ) ;
#139358=CARTESIAN_POINT ( 'NONE',  ( 2.221465439867484903, -1.771451409125622600, 0.4407646962370226351 ) ) ;
#139359=CARTESIAN_POINT ( 'NONE',  ( 1.664434086620687703, 0.5685959063129341073, 1.719966406682835958 ) ) ;
#139360=VERTEX_POINT ( 'NONE', #305 ) ;
#139361=CARTESIAN_POINT ( 'NONE',  ( 5.022202109028018668, -1.178465353167540197, -1.865713892744431446 ) ) ;
#139363=CARTESIAN_POINT ( 'NONE',  ( 3.874219531129017291, 1.223701582695544632, 1.836212042189053761 ) ) ;
#139365=CARTESIAN_POINT ( 'NONE',  ( 2.895058368816882499, -0.1428820475998151818, -1.907012587803847303 ) ) ;
#139367=CARTESIAN_POINT ( 'NONE',  ( 5.371561628297467195, -0.3073141173523045167, 2.047320497149993646 ) ) ;
#139370=CARTESIAN_POINT ( 'NONE',  ( 5.548420995840112724, -1.728225626343689925, 1.347513067664840358 ) ) ;
#139379=CARTESIAN_POINT ( 'NONE',  ( 6.350451050988413115, -2.059726887988411637, -0.2088473404622398499 ) ) ;
#139380=CARTESIAN_POINT ( 'NONE',  ( 4.934167778409569216, 0.9889366926784399769, -1.653171546959011140 ) ) ;
#139382=CARTESIAN_POINT ( 'NONE',  ( 1.282827611874960416, 1.646826022920354848, -1.163289555428485667 ) ) ;
#139386=CARTESIAN_POINT ( 'NONE',  ( 1.834175572193702530, 2.167931929539984814, 0.3193665180123914094 ) ) ;
#139387=CARTESIAN_POINT ( 'NONE',  ( 5.268108045213575785, 0.9031548532531764595, 1.586571422427636824 ) ) ;
#139394=CARTESIAN_POINT ( 'NONE',  ( 2.384105128782065819, -0.3166398734758494315, -1.813660976904336808 ) ) ;
#139395=CARTESIAN_POINT ( 'NONE',  ( 6.152595719530761009, 1.991896818749523845, 0.2912318779872117847 ) ) ;
#139396=CARTESIAN_POINT ( 'NONE',  ( 1.863111423135884293, -0.7740270289045609875, 2.164224664766948525 ) ) ;
#139397=CARTESIAN_POINT ( 'NONE',  ( 6.297705697576845729, -1.418553083497756884, -1.355282376159852475 ) ) ;
#139400=CARTESIAN_POINT ( 'NONE',  ( 3.410326831400651404, -1.910418641682644969, -0.08914582809275289899 ) ) ;
#139404=CARTESIAN_POINT ( 'NONE',  ( 2.648082478619179003, 0.7070732986501033768, 1.967675578925948354 ) ) ;
#139405=CARTESIAN_POINT ( 'NONE',  ( 1.709613803025863188, -1.856884215550944850, 0.2259493607114013147 ) ) ;
#139406=CARTESIAN_POINT ( 'NONE',  ( 2.056017322730230301, 1.755501262438976751, -0.9912458455646618871 ) ) ;
#139410=CARTESIAN_POINT ( 'NONE',  ( 2.594910355399903334, -0.5442454861351472273, 1.653239653166445278 ) ) ;
#139415=CARTESIAN_POINT ( 'NONE',  ( 3.351896425306086336, 1.725068445106912707, -0.001234800371389954687 ) ) ;
#139416=CARTESIAN_POINT ( 'NONE',  ( 2.489988787850425656, -2.185901284972164405, -0.1580625509675498419 ) ) ;
#139417=CARTESIAN_POINT ( 'NONE',  ( 5.760442859251142522, 0.8911043219209063837, 2.019162844794204048 ) ) ;
#139419=CARTESIAN_POINT ( 'NONE',  ( 2.131898410887596906, 2.078612851201648404, -0.6269345663092191767 ) ) ;
#139420=CARTESIAN_POINT ( 'NONE',  ( 1.488595654847742145, -0.2661386877833261111, -1.806066791206423439 ) ) ;
#139421=SURFACE_STYLE_FILL_AREA ( #94678 ) ;
#139422=CARTESIAN_POINT ( 'NONE',  ( 4.012992375354424546, 0.1078809898697324771, 2.114737393012538824 ) ) ;
#139425=CARTESIAN_POINT ( 'NONE',  ( 4.687240393977892161, 1.697883010200517129, 1.540384229137826466 ) ) ;
#139429=CARTESIAN_POINT ( 'NONE',  ( 0.3465379015402513252, 1.086389676674501148, -1.820904993421072371 ) ) ;
#139436=CARTESIAN_POINT ( 'NONE',  ( 5.608046130584797950, -0.04667949407829303371, 2.016033753796213635 ) ) ;
#139438=CARTESIAN_POINT ( 'NONE',  ( 2.922777048086916629, -1.425580663919909563, 1.490811266603887963 ) ) ;
#139440=CARTESIAN_POINT ( 'NONE',  ( 6.883263157960369583, 7.629137130509070275, 2.546189081643289942 ) ) ;
#139444=CARTESIAN_POINT ( 'NONE',  ( 5.718738293430368991, -0.05686238728638653983, 2.190873718245327506 ) ) ;
#139445=CARTESIAN_POINT ( 'NONE',  ( 3.586564705785996843, -0.5826563296015655480, 1.930417576838711957 ) ) ;
#139446=CARTESIAN_POINT ( 'NONE',  ( 3.403688466941825475, -0.7492148395099357261, -1.682118234477212537 ) ) ;
#139449=CARTESIAN_POINT ( 'NONE',  ( 6.036143291503483610, 0.8974207610169572247, -1.589712159477923992 ) ) ;
#139451=CARTESIAN_POINT ( 'NONE',  ( 0.1242335807666505171, 0.4018034787525020524, 2.263199520926823638 ) ) ;
#139453=CARTESIAN_POINT ( 'NONE',  ( 0.1755611466353265426, -0.002217706044388422469, -2.244164702216360219 ) ) ;
#139454=CARTESIAN_POINT ( 'NONE',  ( 2.403073576612833939, 1.690916729301103594, -1.255302274246564043 ) ) ;
#139465=CARTESIAN_POINT ( 'NONE',  ( 2.144932638433934002, 2.058100890041581810, 0.5106320605416380110 ) ) ;
#139466=CARTESIAN_POINT ( 'NONE',  ( 4.307018013452124983, -0.4884699388765164074, -2.166881332863872522 ) ) ;
#139467=CARTESIAN_POINT ( 'NONE',  ( 2.730644157659181559, 0.2691629481662433099, 2.174792594416566249 ) ) ;
#139469=CARTESIAN_POINT ( 'NONE',  ( 0.3115100037339203487, 1.922317768103290803, 1.083863418116323807 ) ) ;
#139471=CARTESIAN_POINT ( 'NONE',  ( 4.967221142815226642, 1.706001049663580460, 0.9686458024478412643 ) ) ;
#139478=CARTESIAN_POINT ( 'NONE',  ( 3.199588043238619228, 1.915454767000431602, -0.9102714984489732597 ) ) ;
#139480=CARTESIAN_POINT ( 'NONE',  ( 5.647404790089923132, -1.701416311724871067, -1.333359258283283166 ) ) ;
#139482=CARTESIAN_POINT ( 'NONE',  ( 3.456447201099471123, -1.625387274077850996, -0.8650149607793490292 ) ) ;
#139486=CARTESIAN_POINT ( 'NONE',  ( 6.667905886031927132, -1.063982290101581185, 1.377602455597818132 ) ) ;
#139487=CARTESIAN_POINT ( 'NONE',  ( 6.727182134110193168, 4.701113012587437190, 2.373661997258198486 ) ) ;
#139490=CARTESIAN_POINT ( 'NONE',  ( 4.276362541559985075, -1.246951984143488623, 1.765614359104182629 ) ) ;
#139492=CARTESIAN_POINT ( 'NONE',  ( 6.749375321999433908, -1.976647572034227140, -0.3960365597561604778 ) ) ;
#139494=CARTESIAN_POINT ( 'NONE',  ( 3.977527890101069996, 2.036293384626610248, -0.7259696361804208742 ) ) ;
#139495=CARTESIAN_POINT ( 'NONE',  ( 5.044191579798307679, 1.965876612296811654, 0.1480472272742116568 ) ) ;
#139496=CARTESIAN_POINT ( 'NONE',  ( 4.270605845326081784, -1.729236537505800086, 0.1267691526786636214 ) ) ;
#139497=CARTESIAN_POINT ( 'NONE',  ( 1.154151856878969928, 0.8927059368322427524, 2.001694687108931170 ) ) ;
#139498=CARTESIAN_POINT ( 'NONE',  ( 0.7632353006940760798, -1.668858575275869116, 1.593938313602519363 ) ) ;
#139499=CARTESIAN_POINT ( 'NONE',  ( 3.620434630758031069, 1.310268768930487937, -1.590567769477232662 ) ) ;
#139500=CARTESIAN_POINT ( 'NONE',  ( 5.565949569975685129, -1.228723311412585950, 1.503964349303931192 ) ) ;
#139507=CARTESIAN_POINT ( 'NONE',  ( 2.151677955860908487, -1.772288797910109404, -1.314638326115322053 ) ) ;
#139510=CARTESIAN_POINT ( 'NONE',  ( 0.5318007479364270651, 1.064995724915913433, 1.525891442952797439 ) ) ;
#139511=CARTESIAN_POINT ( 'NONE',  ( -0.02880301295722554472, 4.079423595021631321, -2.828475351696632778 ) ) ;
#139516=CARTESIAN_POINT ( 'NONE',  ( 6.210883717528068892, -0.2205035313364057392, 1.827825250963102333 ) ) ;
#139518=CARTESIAN_POINT ( 'NONE',  ( 2.325137485922982084, -0.001238304602014379070, 2.061077815622249343 ) ) ;
#139524=CARTESIAN_POINT ( 'NONE',  ( 0.9716393833266089297, 1.986344416073432484, -0.5490401152750885583 ) ) ;
#139526=CARTESIAN_POINT ( 'NONE',  ( 5.144037045698616417, 0.5398437887287730330, 1.760322748975438500 ) ) ;
#139532=CARTESIAN_POINT ( 'NONE',  ( 4.389439674793148782, 1.972019932058775016, -0.9908447712502415072 ) ) ;
#139533=CARTESIAN_POINT ( 'NONE',  ( 0.2632415847364302786, -1.930764589519979424, -0.9721467891136772455 ) ) ;
#139535=CARTESIAN_POINT ( 'NONE',  ( -0.01753026575586694516, -1.247696154478775021, 1.449428981083925150 ) ) ;
#139536=CARTESIAN_POINT ( 'NONE',  ( 0.6203277878081385754, 1.987498645412737908, 0.3399528957561820386 ) ) ;
#139541=CARTESIAN_POINT ( 'NONE',  ( 0.4966798268824790252, 1.557709316500059726, -1.035497600327957235 ) ) ;
#139543=CARTESIAN_POINT ( 'NONE',  ( 1.991423064788412800, -0.4370762659771566527, 1.968445590580846893 ) ) ;
#139547=CARTESIAN_POINT ( 'NONE',  ( 4.108114811375044084, -2.100464006233178083, 0.1544923775467464122 ) ) ;
#139552=CARTESIAN_POINT ( 'NONE',  ( 4.588152005245718534, 1.166368207181975869, 1.648760302449885584 ) ) ;
#139554=CARTESIAN_POINT ( 'NONE',  ( 6.180145878880094479, -1.142753862412404509, -1.717008129757614077 ) ) ;
#139556=CARTESIAN_POINT ( 'NONE',  ( 4.956408742875526130, 0.8222144862577386304, 1.999314050312686053 ) ) ;
#139562=CARTESIAN_POINT ( 'NONE',  ( 2.084662720398474001, 1.251192046665784208, -1.774223565721672724 ) ) ;
#139565=CARTESIAN_POINT ( 'NONE',  ( 2.120424178990498731, 0.001545453418709194504, 1.841430844159386293 ) ) ;
#139567=CARTESIAN_POINT ( 'NONE',  ( 3.790727848299980440, 1.850687065220711469, -1.173560875862532660 ) ) ;
#139568=CARTESIAN_POINT ( 'NONE',  ( 6.983263157960404754, 0.5601148359399975574, 2.204851038219941106 ) ) ;
#139569=CARTESIAN_POINT ( 'NONE',  ( 3.854571047428239527, 0.8115417623771915556, 2.112135835510853710 ) ) ;
#139575=CARTESIAN_POINT ( 'NONE',  ( 5.448444396454582339, 0.5145788473605721336, 1.693291817928108234 ) ) ;
#139576=CARTESIAN_POINT ( 'NONE',  ( 3.334638158648925099, 1.275257586908218110, -1.557663628481553264 ) ) ;
#139578=CARTESIAN_POINT ( 'NONE',  ( 1.764816150188710298, -1.489710805432680418, 1.488830988054674620 ) ) ;
#139581=CARTESIAN_POINT ( 'NONE',  ( 0.5726248362980547180, 1.360856580973464069, -1.424029402571887148 ) ) ;
#139584=CARTESIAN_POINT ( 'NONE',  ( 5.326340473083292615, -0.8217345736999382977, -1.614601580891014354 ) ) ;
#139588=CARTESIAN_POINT ( 'NONE',  ( 5.225416543158964977, -1.776039340814106637, 0.5876355328483380269 ) ) ;
#139591=CARTESIAN_POINT ( 'NONE',  ( 4.135645376760338721, 1.951069878921590561, -0.6927527371542246959 ) ) ;
#139603=CARTESIAN_POINT ( 'NONE',  ( 4.158614545834369736, -0.6132839004606009947, -1.863630207987923004 ) ) ;
#139605=CARTESIAN_POINT ( 'NONE',  ( 2.319685276966905629, -1.560262528187049025, 1.276846253076675541 ) ) ;
#139610=CARTESIAN_POINT ( 'NONE',  ( 2.512791842090915218, 1.668957736969980621, 0.8448945032545759348 ) ) ;
#139612=CARTESIAN_POINT ( 'NONE',  ( 4.236591777569945982, 1.235091891264840314, -1.589779643154372701 ) ) ;
#139615=CARTESIAN_POINT ( 'NONE',  ( 3.058335788041772307, -1.258934183635691095, 1.702155058717010672 ) ) ;
#139616=CARTESIAN_POINT ( 'NONE',  ( 4.826661161267837841, -1.354893614093263254, 1.565527137264411728 ) ) ;
#139618=CARTESIAN_POINT ( 'NONE',  ( 0.9430502156211654219, -1.650385480578796749, -1.283440319295367615 ) ) ;
#139619=CARTESIAN_POINT ( 'NONE',  ( 6.620655732516651071, 1.241313378043694238, 2.288056600130850882 ) ) ;
#139620=CARTESIAN_POINT ( 'NONE',  ( 0.1820471141361617307, -1.670984272841398832, -0.4269972090983116253 ) ) ;
#139628=CARTESIAN_POINT ( 'NONE',  ( 5.988906256519173077, -1.817303134770717588, -0.5954205699960082310 ) ) ;
#139637=CARTESIAN_POINT ( 'NONE',  ( 5.870720304489429608, -0.2986452421533461465, -1.994069804803912049 ) ) ;
#139640=CARTESIAN_POINT ( 'NONE',  ( -0.1399997263889820043, 5.722209607272843002, -2.594334538518060729 ) ) ;
#139644=CARTESIAN_POINT ( 'NONE',  ( 2.131642331222316500, 1.886095724437972798, -0.5669754052412961931 ) ) ;
#139646=CARTESIAN_POINT ( 'NONE',  ( 3.989861366179075386, -2.010826228832915508, 0.1511578083489423796 ) ) ;
#139648=CARTESIAN_POINT ( 'NONE',  ( 6.727182134110167411, 4.690976314540481695, 2.651619508270358416 ) ) ;
#139649=CARTESIAN_POINT ( 'NONE',  ( 4.804715953495782621, 1.905792977913090214, 1.081705336968781239 ) ) ;
#139651=CARTESIAN_POINT ( 'NONE',  ( 3.311465173828963326, -0.3771673786017637475, 1.888946036755128288 ) ) ;
#139654=CARTESIAN_POINT ( 'NONE',  ( -0.1296875068448159474, 0.7431874094961619104, -1.910093690679348200 ) ) ;
#139655=CARTESIAN_POINT ( 'NONE',  ( -0.01666059994226073634, -0.1612322585618740090, -2.171656592459797253 ) ) ;
#139661=CARTESIAN_POINT ( 'NONE',  ( 6.497600353373155002, -1.840680978339729545, 0.05264081064878384231 ) ) ;
#139662=CARTESIAN_POINT ( 'NONE',  ( 3.264317399697822530, 2.013265973121576291, -0.002229150246490021157 ) ) ;
#139663=CARTESIAN_POINT ( 'NONE',  ( 5.413504136812340661, 0.6594720349357428013, 2.201770641885878899 ) ) ;
#139665=CARTESIAN_POINT ( 'NONE',  ( 3.572968443166994579, 1.680613686130405515, 0.7995154651666557255 ) ) ;
#139667=DIRECTION ( 'NONE',  ( -0.9999980456341538426, 0.000000000000000000, -0.001977050295949953074 ) ) ;
#139671=CARTESIAN_POINT ( 'NONE',  ( 5.952696063536119908, -1.793662432779649540, -1.073965677532197072 ) ) ;
#139676=CARTESIAN_POINT ( 'NONE',  ( 5.988827324695590981, -0.2600698726980456010, -1.705031240916178525 ) ) ;
#139679=CARTESIAN_POINT ( 'NONE',  ( 1.881130407182354469, -0.4634198587198985475, -1.670964061236743348 ) ) ;
#139684=CARTESIAN_POINT ( 'NONE',  ( 0.7079804021624566124, 0.6528548590773940452, -1.964656565413371414 ) ) ;
#139686=CARTESIAN_POINT ( 'NONE',  ( 5.356004772612798170, 1.823420152956479523, -0.09349780940721279243 ) ) ;
#139687=CARTESIAN_POINT ( 'NONE',  ( 2.149198318390078910, 1.709348667602617500, -0.9624241554767108964 ) ) ;
#139690=CARTESIAN_POINT ( 'NONE',  ( 3.405043383231837417, -0.4154483767263848493, -2.079220720149973278 ) ) ;
#139693=CARTESIAN_POINT ( 'NONE',  ( 1.604436975501881468, 2.067711310959176707, 0.1055696395834623824 ) ) ;
#139696=CARTESIAN_POINT ( 'NONE',  ( 3.264521566599550173, 2.221473416772083098, -0.001674386450213962828 ) ) ;
#139698=CARTESIAN_POINT ( 'NONE',  ( 1.758794133653733827, 2.198278648980501515, -0.6719540409268388581 ) ) ;
#139700=CARTESIAN_POINT ( 'NONE',  ( 0.3386216902839487841, -1.901412053528793722, -0.4823507731460881520 ) ) ;
#139704=CARTESIAN_POINT ( 'NONE',  ( 6.444863656277017405, -1.483217659742748218, -1.090817886357238198 ) ) ;
#139706=CARTESIAN_POINT ( 'NONE',  ( -0.1104750535120268828, 4.084583917300320444, -2.658209514912849514 ) ) ;
#139707=CARTESIAN_POINT ( 'NONE',  ( 3.311258828109595154, -0.3375135790737812114, 1.691226829923969666 ) ) ;
#139708=CARTESIAN_POINT ( 'NONE',  ( 2.132046339962359038, 2.016188815772378629, 0.04465230659478347519 ) ) ;
#139709=CARTESIAN_POINT ( 'NONE',  ( 2.584987504963653038, -0.7174396784795608051, 2.183947998982360250 ) ) ;
#139710=CARTESIAN_POINT ( 'NONE',  ( 3.128476345081227628, 1.259638568860393493, -1.879123747193896632 ) ) ;
#139711=CARTESIAN_POINT ( 'NONE',  ( 5.514326386059018148, -0.9456761151771397866, -1.881892731060728519 ) ) ;
#139714=CARTESIAN_POINT ( 'NONE',  ( 5.114393831954183511, 1.220379059178023695, -1.281870188591783588 ) ) ;
#139716=CARTESIAN_POINT ( 'NONE',  ( 0.4809653258567511691, -0.2865729554843428062, -2.274222260372929405 ) ) ;
#139717=CARTESIAN_POINT ( 'NONE',  ( 5.736236344406846932, 0.3633543575551900773, 1.804753862313414281 ) ) ;
#139721=CARTESIAN_POINT ( 'NONE',  ( 6.246043798300164873, 0.6838514278588082584, 2.082077653496945402 ) ) ;
#139724=CARTESIAN_POINT ( 'NONE',  ( 5.951642636407409093, 1.565221049572671719, 1.355249363302114318 ) ) ;
#139725=CARTESIAN_POINT ( 'NONE',  ( -0.1179535434602772825, -2.016182236903838465, -0.04464881524945257807 ) ) ;
#139728=CARTESIAN_POINT ( 'NONE',  ( 3.967344596728016093, 0.2348649212099394590, -1.912067515532820838 ) ) ;
#139731=CARTESIAN_POINT ( 'NONE',  ( 1.441950287000768771, -2.089521377041357653, 0.7543469697938051111 ) ) ;
#139741=CARTESIAN_POINT ( 'NONE',  ( 1.082386330805637398, 1.171445227557347923, -1.573568114121715933 ) ) ;
#139745=CARTESIAN_POINT ( 'NONE',  ( 6.461383593301071926, 1.630371061775518271, 1.090930979547571456 ) ) ;
#139748=CARTESIAN_POINT ( 'NONE',  ( 6.737200384369169903, -1.933438233944267060, 0.9670071574134844195 ) ) ;
#139752=CARTESIAN_POINT ( 'NONE',  ( 0.8779421195594695471, -1.044212112285093585, 1.551753832453220294 ) ) ;
#139753=CARTESIAN_POINT ( 'NONE',  ( 0.7560338623246564138, 1.671613681001963281, -0.4610611789691662632 ) ) ;
#139756=CARTESIAN_POINT ( 'NONE',  ( 4.511385190476093321, -2.149204750630455241, 0.4279282578087198474 ) ) ;
#139757=CARTESIAN_POINT ( 'NONE',  ( 4.155530545730415248, -1.916392541607782496, -1.285185436265631642 ) ) ;
#139758=CARTESIAN_POINT ( 'NONE',  ( 6.889916301919797981, -0.8861221739737500380, 1.859037482098152338 ) ) ;
#139759=CARTESIAN_POINT ( 'NONE',  ( 2.853385946047338084, 1.932536089888321040, -0.1910151464093560736 ) ) ;
#139761=CARTESIAN_POINT ( 'NONE',  ( 5.150683391976684788, 2.089615912265533559, 0.3601871064465370087 ) ) ;
#139763=CARTESIAN_POINT ( 'NONE',  ( 3.217422812353257555, 1.967887761762876941, 0.4390297752325384995 ) ) ;
#139767=CARTESIAN_POINT ( 'NONE',  ( 1.260069262837599791, 0.7379878962356714034, 1.670071910705408946 ) ) ;
#139772=CARTESIAN_POINT ( 'NONE',  ( 5.032131441678504125, 1.061211460345131252, -1.766520746938464947 ) ) ;
#139776=CARTESIAN_POINT ( 'NONE',  ( 5.092447094119275874, -1.120170962321866082, 1.680348583886650315 ) ) ;
#139777=CARTESIAN_POINT ( 'NONE',  ( 5.584718243131947091, -1.410645330893144589, 1.715908544892131626 ) ) ;
#139782=CARTESIAN_POINT ( 'NONE',  ( 4.030192151223922714, 1.103973922444676070, -1.740068238149700353 ) ) ;
#139783=CARTESIAN_POINT ( 'NONE',  ( 4.078750125433938223, -0.7691220382576718917, 1.864168106189521890 ) ) ;
#139790=CARTESIAN_POINT ( 'NONE',  ( 3.602888598310006074, 0.9090057795711030675, -1.799647124144133858 ) ) ;
#139791=CARTESIAN_POINT ( 'NONE',  ( 4.048646477676579813, -1.531818510360350327, -1.021117339664041834 ) ) ;
#139793=CARTESIAN_POINT ( 'NONE',  ( 1.542099375240197245, -1.674077152000338797, -1.588604925253054745 ) ) ;
#139795=CARTESIAN_POINT ( 'NONE',  ( 4.235729478701364847, -1.487246874726022128, -1.568870776130903089 ) ) ;
#139798=CARTESIAN_POINT ( 'NONE',  ( 3.111036021816812713, 0.8295677418227834776, -2.143598788741421401 ) ) ;
#139800=CARTESIAN_POINT ( 'NONE',  ( 1.990876257202532695, 1.628914321797021669, -0.9196232060951770038 ) ) ;
#139801=CARTESIAN_POINT ( 'NONE',  ( 0.2628735715076990220, -1.758816568047173234, -0.8906303152973747972 ) ) ;
#139806=CARTESIAN_POINT ( 'NONE',  ( 1.331021600797330118, 2.127646391749141941, 0.5858054460900484761 ) ) ;
#139811=CARTESIAN_POINT ( 'NONE',  ( 6.666873957964818409, -1.802346848367493592, -0.7993007979140465125 ) ) ;
#139812=CARTESIAN_POINT ( 'NONE',  ( 5.813149116883928436, 2.032396105517704221, 1.093072976444838362 ) ) ;
#139813=CARTESIAN_POINT ( 'NONE',  ( 6.883263157960402445, 0.001763689368145578400, 1.846037217754380011 ) ) ;
#139814=CARTESIAN_POINT ( 'NONE',  ( 3.344635507851092981, -2.031254381041375456, -0.3572892473815546532 ) ) ;
#139820=CARTESIAN_POINT ( 'NONE',  ( 5.881339278728036746, -0.05926448915108929044, 2.170540009233146606 ) ) ;
#139823=CARTESIAN_POINT ( 'NONE',  ( 4.792441439910442469, 1.527937338083688923, -1.027124420945781935 ) ) ;
#139826=CARTESIAN_POINT ( 'NONE',  ( 6.620655732516649294, -0.002413161512292843602, 2.173887093218459743 ) ) ;
#139827=CARTESIAN_POINT ( 'NONE',  ( 0.2802489257003986101, -1.812731005579379051, -0.4610361243657657981 ) ) ;
#139828=CARTESIAN_POINT ( 'NONE',  ( 6.719576162335838099, -2.196678875378419882, 0.5415391501680610897 ) ) ;
#139835=CARTESIAN_POINT ( 'NONE',  ( 2.447821898584545242, 1.769419436591600725, 0.04612135499031978086 ) ) ;
#139836=CARTESIAN_POINT ( 'NONE',  ( 6.252595736715376162, 1.991502868314236174, 0.2931975281106109499 ) ) ;
#139838=CARTESIAN_POINT ( 'NONE',  ( 3.743669890235715947, 1.900728030520698830, -0.2378226680747745625 ) ) ;
#139839=CARTESIAN_POINT ( 'NONE',  ( 4.422284282497963126, 0.9263432559908044706, 1.738082477136545956 ) ) ;
#139840=CARTESIAN_POINT ( 'NONE',  ( 6.275650217586050239, 0.3411474428106214263, -1.990588700022011714 ) ) ;
#139842=CARTESIAN_POINT ( 'NONE',  ( 2.571000202304725590, 0.09389976206976291540, -1.868427151830873267 ) ) ;
#139843=CARTESIAN_POINT ( 'NONE',  ( 5.988827324695590981, -0.2600698726980456010, -1.705031240916178525 ) ) ;
#139845=CARTESIAN_POINT ( 'NONE',  ( 2.245003380770736801, 0.4850519687749441644, 2.152760086278446394 ) ) ;
#139848=CARTESIAN_POINT ( 'NONE',  ( 6.127397123722368555, 0.1457569626216181913, -1.956525209266091192 ) ) ;
#139855=CARTESIAN_POINT ( 'NONE',  ( 2.506376218629560171, 2.069854378281150709, 0.05321039126485183068 ) ) ;
#139859=CARTESIAN_POINT ( 'NONE',  ( -0.07552420640595960966, -0.8660980012666683603, -1.823048286210580793 ) ) ;
#139863=CARTESIAN_POINT ( 'NONE',  ( 0.07479286986305544449, 2.046156589154801253, -2.272744413733415403 ) ) ;
#139865=CARTESIAN_POINT ( 'NONE',  ( 5.483749906247235906, 1.861732415968733401, 0.7741956105717237024 ) ) ;
#139866=CARTESIAN_POINT ( 'NONE',  ( 5.225768846659354594, 0.7701814094057590765, -1.754262016157917881 ) ) ;
#139867=CARTESIAN_POINT ( 'NONE',  ( 6.539320575229278454, 3.689604457162498630, 2.617406275049142916 ) ) ;
#139868=CARTESIAN_POINT ( 'NONE',  ( 2.507599501126521524, -2.167277876680247850, 0.3246147914140809498 ) ) ;
#139870=CARTESIAN_POINT ( 'NONE',  ( 1.986440140746603911, -1.173720106059353396, 1.509789020923378189 ) ) ;
#139873=CARTESIAN_POINT ( 'NONE',  ( 6.187133403942106646, 1.760427041935657799, 1.175965560660442444 ) ) ;
#139875=CARTESIAN_POINT ( 'NONE',  ( 6.409741707328596938, -1.031184584194230647, -1.933826218581576439 ) ) ;
#139877=CARTESIAN_POINT ( 'NONE',  ( 3.029983902540707152, 0.9595516922606081023, -1.432977992855663185 ) ) ;
#139879=CARTESIAN_POINT ( 'NONE',  ( 5.924112389714111693, -2.104401743431310923, 0.2612745606217213856 ) ) ;
#139882=CARTESIAN_POINT ( 'NONE',  ( 0.1331565106231328843, 0.003911343561965873426, -1.946049565259087455 ) ) ;
#139886=CARTESIAN_POINT ( 'NONE',  ( 0.1399997263886003374, 0.002789056014650820314, -1.999853399661279063 ) ) ;
#139890=CARTESIAN_POINT ( 'NONE',  ( 2.508236654460756387, -1.806733793710820324, -0.1315605372460958433 ) ) ;
#139894=CARTESIAN_POINT ( 'NONE',  ( 3.721195823539941827, 1.555462818066039254, 0.9281401003491447366 ) ) ;
#139898=CARTESIAN_POINT ( 'NONE',  ( 4.791365544089026152, -1.701862485369805000, 0.7535167838805619800 ) ) ;
#139900=CARTESIAN_POINT ( 'NONE',  ( 3.005391328865916645, -1.845313015785840172, 0.5138285116655214591 ) ) ;
#139901=CARTESIAN_POINT ( 'NONE',  ( 1.131563826228650038, -1.154680578942975044, -1.414029504508321100 ) ) ;
#139912=CARTESIAN_POINT ( 'NONE',  ( 0.1632417891470130944, -1.931755829615459996, -0.9703963252955111196 ) ) ;
#139913=CARTESIAN_POINT ( 'NONE',  ( 1.482492212676550070, -0.3080716119066116421, -2.067685480015791111 ) ) ;
#139914=CARTESIAN_POINT ( 'NONE',  ( 6.651400849050447484, -1.547811450530303778, -1.146644766597894938 ) ) ;
#139917=CARTESIAN_POINT ( 'NONE',  ( 2.485134345765506847, 1.670108983700506977, -0.7376146046164518966 ) ) ;
#139918=CARTESIAN_POINT ( 'NONE',  ( 2.965657822035951963, 0.3232568108629539361, -2.182957019552448141 ) ) ;
#139920=CARTESIAN_POINT ( 'NONE',  ( 1.248149539447914735, 0.9399939672071171426, -1.665319807275446706 ) ) ;
#139924=CARTESIAN_POINT ( 'NONE',  ( 1.680066331807037905, -1.091455746017004014, -1.639250758224161775 ) ) ;
#139925=CARTESIAN_POINT ( 'NONE',  ( 2.946749062660087848, -1.589232290113586910, -1.115973732403415131 ) ) ;
#139929=CARTESIAN_POINT ( 'NONE',  ( 6.403157621081472683, -1.572583794901558862, 0.9946829920960180704 ) ) ;
#139934=CARTESIAN_POINT ( 'NONE',  ( 2.191216702865448784, 1.696344223602393786, 1.387594652289561248 ) ) ;
#139938=CARTESIAN_POINT ( 'NONE',  ( 3.053144290054691901, -1.492835736363471888, -1.050712463094093385 ) ) ;
#139945=CARTESIAN_POINT ( 'NONE',  ( 2.350114058346234547, 1.926077408352431464, 0.04734757869597795016 ) ) ;
#139946=CARTESIAN_POINT ( 'NONE',  ( 6.280128941539553367, -1.086961472313338284, -1.632890767417946032 ) ) ;
#139954=CARTESIAN_POINT ( 'NONE',  ( 5.647352632913819726, 1.828451368696734747, -0.9708816006866529680 ) ) ;
#139955=CARTESIAN_POINT ( 'NONE',  ( -0.1237769027084348328, -0.1346504581853508187, -1.811164470923332104 ) ) ;
#139959=CARTESIAN_POINT ( 'NONE',  ( 5.590575961319281362, -0.5612465257360791382, 2.229044676911738687 ) ) ;
#139963=CARTESIAN_POINT ( 'NONE',  ( -0.02880301295727759683, -0.006976478922920535501, -2.273770288744044521 ) ) ;
#139966=CARTESIAN_POINT ( 'NONE',  ( 4.839755972451986743, 1.936857930295164065, 0.1413805851513943446 ) ) ;
#139971=CARTESIAN_POINT ( 'NONE',  ( 6.416268857797894576, -1.911816439625917852, 0.05404522429636184067 ) ) ;
#139972=CARTESIAN_POINT ( 'NONE',  ( 0.3458015845922198239, 1.719860733928044949, 0.1322621976239789499 ) ) ;
#139973=CARTESIAN_POINT ( 'NONE',  ( 5.454314652423888354, -1.275559214091715354, 1.561879324423600890 ) ) ;
#139977=CARTESIAN_POINT ( 'NONE',  ( 2.466838723508807174, 0.1015857406408589014, -2.088290385120465498 ) ) ;
#139978=CARTESIAN_POINT ( 'NONE',  ( 1.006321374186702311, 1.343689884961623227, -1.152001066587736267 ) ) ;
#139981=CARTESIAN_POINT ( 'NONE',  ( 4.189605479905995189, -0.8790709274306067744, 2.117190895528203498 ) ) ;
#139982=CARTESIAN_POINT ( 'NONE',  ( 2.483973769465233961, -0.2969572910719043279, -1.714626640263767543 ) ) ;
#139984=CARTESIAN_POINT ( 'NONE',  ( 2.953504815971871977, -1.868289524550557523, 1.003269902519101864 ) ) ;
#139986=CARTESIAN_POINT ( 'NONE',  ( 1.721629994271107744, -1.484111423267266527, -0.8961763045370867431 ) ) ;
#139988=CARTESIAN_POINT ( 'NONE',  ( 1.117373073715557164, 0.3680575366376471758, -1.824110739772739631 ) ) ;
#139989=CARTESIAN_POINT ( 'NONE',  ( 2.664704904736223234, -0.8290184881076659851, -2.006861667775594160 ) ) ;
#139991=CARTESIAN_POINT ( 'NONE',  ( 3.450407915430803385, -1.350735839785843773, 1.497501794165828626 ) ) ;
#139992=CARTESIAN_POINT ( 'NONE',  ( 2.312500000000001776, 1.451031289061216478, 1.451031289061020857 ) ) ;
#139994=CARTESIAN_POINT ( 'NONE',  ( 1.325083149161108365, -0.05013198271685941065, 1.925904219417676089 ) ) ;
#139996=CARTESIAN_POINT ( 'NONE',  ( 4.816739660502834752, -0.7493216981008001820, -2.091313736985983773 ) ) ;
#139998=CARTESIAN_POINT ( 'NONE',  ( -0.2108831679771203116, 0.7314853703891763814, -1.979988191570913880 ) ) ;
#140002=CARTESIAN_POINT ( 'NONE',  ( 6.170221320256972675, 2.215557125880045053, -0.1624646739342323065 ) ) ;
#140003=CARTESIAN_POINT ( 'NONE',  ( 4.615648854252428102, 0.4318217149890530848, -1.913582009320368371 ) ) ;
#140006=CARTESIAN_POINT ( 'NONE',  ( 5.729810862507367375, -1.428767958649424408, -1.754208347296302373 ) ) ;
#140008=CARTESIAN_POINT ( 'NONE',  ( 2.822777196768213592, -1.424206252425799679, 1.492280444834346520 ) ) ;
#140012=CARTESIAN_POINT ( 'NONE',  ( 4.604681543780857034, 1.447206075137374759, -1.185162884121161442 ) ) ;
#140013=CARTESIAN_POINT ( 'NONE',  ( 3.656634503061773067, 0.9670403524725273980, 1.439223064172075350 ) ) ;
#140014=CARTESIAN_POINT ( 'NONE',  ( 1.751089554790756342, 1.735802523247106377, -0.1280615824842730732 ) ) ;
#140015=CARTESIAN_POINT ( 'NONE',  ( 1.136728594277321980, 0.4534141614637792195, 2.246936901365268913 ) ) ;
#140016=CARTESIAN_POINT ( 'NONE',  ( 0.6048602812970468312, -0.7454967350204610987, -2.077179305122120123 ) ) ;
#140017=CARTESIAN_POINT ( 'NONE',  ( 4.300388110500093397, 1.614917507917512207, -1.327843252744983049 ) ) ;
#140018=CARTESIAN_POINT ( 'NONE',  ( 5.402268692527759875, 1.469326413266746956, -1.269838510729433212 ) ) ;
#140020=CARTESIAN_POINT ( 'NONE',  ( 0.2818752512256904597, 1.674885806461807958, -1.122501178855893400 ) ) ;
#140021=CARTESIAN_POINT ( 'NONE',  ( -0.1225938595818750754, -1.897163925677572305, -0.9476133185889324961 ) ) ;
#140023=CARTESIAN_POINT ( 'NONE',  ( 6.451795992440088057, -1.844709169062180409, -0.8146298745319994206 ) ) ;
#140027=CARTESIAN_POINT ( 'NONE',  ( 4.143042835627613663, -1.587387879459275286, 0.9017181768668989239 ) ) ;
#140028=CARTESIAN_POINT ( 'NONE',  ( 2.696532018272995490, -2.200798769047443759, -0.1632673417703081331 ) ) ;
#140034=CARTESIAN_POINT ( 'NONE',  ( 2.689718276569666333, 1.916506935140523726, -0.6377304922457660563 ) ) ;
#140035=ADVANCED_FACE ( 'NONE', ( #203853 ), #144367, .T. ) ;
#140037=CARTESIAN_POINT ( 'NONE',  ( 2.904952611580268851, -1.549997479519327648, 1.029535618745812675 ) ) ;
#140043=CARTESIAN_POINT ( 'NONE',  ( 5.039593146249602640, -1.293522693445446015, -1.288650932716684849 ) ) ;
#140047=CARTESIAN_POINT ( 'NONE',  ( 0.4031117941524774984, 0.2875473383168804520, 1.709643368666772467 ) ) ;
#140048=CARTESIAN_POINT ( 'NONE',  ( 6.685540632719009224, -0.7820230359689305244, 1.665195522482863399 ) ) ;
#140049=CARTESIAN_POINT ( 'NONE',  ( 3.914918041407587257, 1.633027907263858491, -1.630791690553441420 ) ) ;
#140051=CARTESIAN_POINT ( 'NONE',  ( 0.6849272659917711170, -0.2494827685093256309, -2.045528899044207982 ) ) ;
#140055=CARTESIAN_POINT ( 'NONE',  ( 6.274848118712046841, -2.282167594539401101, 0.2721878479114477334 ) ) ;
#140059=CARTESIAN_POINT ( 'NONE',  ( 5.418772907935071714, 1.728844841293469159, 0.7149302089985640762 ) ) ;
#140061=CARTESIAN_POINT ( 'NONE',  ( 3.146637304467227558, 1.866760668956708447, 0.4145885930168375921 ) ) ;
#140063=CARTESIAN_POINT ( 'NONE',  ( 5.233140740401229785, 0.1595256157847015632, 2.201181388321731269 ) ) ;
#140064=CARTESIAN_POINT ( 'NONE',  ( 4.505136581001433882, -0.1005046246093168893, 2.115047560132724325 ) ) ;
#140066=CARTESIAN_POINT ( 'NONE',  ( 6.983263157960366563, 2.056882910316945701, 2.252511522010155698 ) ) ;
#140069=CARTESIAN_POINT ( 'NONE',  ( 1.888135564707097425, 1.592107727680527329, 1.670599446388189913 ) ) ;
#140070=CARTESIAN_POINT ( 'NONE',  ( 3.877359892829432386, -0.1466975079335990917, 1.956454564409334296 ) ) ;
#140072=CARTESIAN_POINT ( 'NONE',  ( 6.280145880020024052, -1.141028152120068917, -1.718028578259041872 ) ) ;
#140076=CARTESIAN_POINT ( 'NONE',  ( 5.296111364736042937, -0.9110065213352031011, -1.799124599017036585 ) ) ;
#140081=CARTESIAN_POINT ( 'NONE',  ( 1.587047119190465594, 2.091647000433814352, 0.5815059253076891865 ) ) ;
#140086=CARTESIAN_POINT ( 'NONE',  ( 1.106794710556399997, 1.562239816646590285, -1.344093658231941824 ) ) ;
#140087=CARTESIAN_POINT ( 'NONE',  ( -0.02244404828160086532, 2.859736408857795009, -2.677210243787793598 ) ) ;
#140092=CARTESIAN_POINT ( 'NONE',  ( 3.861887077619485797, 0.6414691495152945455, -1.801623935260010079 ) ) ;
#140093=CARTESIAN_POINT ( 'NONE',  ( 5.330810035471644781, 0.1327828994084866154, 1.764904742964703122 ) ) ;
#140097=CARTESIAN_POINT ( 'NONE',  ( -0.04785004733596533166, -1.249461711056678803, 1.452303129844798590 ) ) ;
#140099=CARTESIAN_POINT ( 'NONE',  ( 0.3267351109269465148, -1.353470794461093973, 1.566751113397255812 ) ) ;
#140101=CARTESIAN_POINT ( 'NONE',  ( 5.664887262500884368, -1.691755685069219695, -0.7986314380193232365 ) ) ;
#140102=CARTESIAN_POINT ( 'NONE',  ( 3.246530741642670304, 0.4443377543969920795, 1.770662692542070538 ) ) ;
#140103=CARTESIAN_POINT ( 'NONE',  ( 5.971336403843030105, 0.1662174427981797931, -2.200672837095698497 ) ) ;
#140106=CARTESIAN_POINT ( 'NONE',  ( 3.314939881033797331, -1.563807569242671613, 1.345168064507019423 ) ) ;
#140111=CARTESIAN_POINT ( 'NONE',  ( 0.2280961430754513408, -1.329988288769240024, -1.704746276402234528 ) ) ;
#140112=CARTESIAN_POINT ( 'NONE',  ( 5.740704066448026666, -2.019076491677873619, -0.4572469816465085657 ) ) ;
#140114=CARTESIAN_POINT ( 'NONE',  ( 3.479894426560462328, 1.368377867093536482, 1.673357603396708360 ) ) ;
#140116=CARTESIAN_POINT ( 'NONE',  ( 4.494788958170754078, -1.959534436568559190, -0.4887017053271830447 ) ) ;
#140117=CARTESIAN_POINT ( 'NONE',  ( 1.855835942623608181, -0.6640040153468586004, 1.846199708051485811 ) ) ;
#140118=CARTESIAN_POINT ( 'NONE',  ( 6.620655732516668834, 7.629137130509086262, 2.873739711112702544 ) ) ;
#140125=CARTESIAN_POINT ( 'NONE',  ( 1.938685741270998797, -1.555697844595272716, 1.282991390469834458 ) ) ;
#140129=CARTESIAN_POINT ( 'NONE',  ( 6.047114369478562956, 0.1942372860762129894, 1.902532258075719351 ) ) ;
#140133=CARTESIAN_POINT ( 'NONE',  ( 3.638296137631126914, 0.7283958097016438593, 1.880429543521966007 ) ) ;
#140136=CARTESIAN_POINT ( 'NONE',  ( 5.913083851878619512, 1.523424462977729599, 0.8087443918367646090 ) ) ;
#140140=CARTESIAN_POINT ( 'NONE',  ( 4.815616550699190590, -1.834762568278673900, 0.3632225495420540184 ) ) ;
#140143=CARTESIAN_POINT ( 'NONE',  ( 1.973570569994816060, -0.2575147360633044391, 2.054139978358980656 ) ) ;
#140147=CARTESIAN_POINT ( 'NONE',  ( -0.1058464554703278104, -0.8645191204341062807, -1.819937883007181512 ) ) ;
#140148=CARTESIAN_POINT ( 'NONE',  ( 0.8085208021518180965, -0.4412475195509023562, -1.756857618417038358 ) ) ;
#140154=CLOSED_SHELL ( 'NONE', ( #114959, #7847, #54872, #178428, #138429, #113040, #36985, #8539 ) ) ;
#140155=CARTESIAN_POINT ( 'NONE',  ( 6.116788041597909675, 0.1929307199614685164, 1.905880049602140636 ) ) ;
#140163=CARTESIAN_POINT ( 'NONE',  ( 3.432649856329002880, 2.108609624295390006, 0.4754391814798044069 ) ) ;
#140168=CARTESIAN_POINT ( 'NONE',  ( 5.332948099851452461, 0.1360325894329272867, 1.820554394434070744 ) ) ;
#140170=CARTESIAN_POINT ( 'NONE',  ( 0.9132762689940625567, -0.2936195204277583515, 1.949272377766637643 ) ) ;
#140171=CARTESIAN_POINT ( 'NONE',  ( 3.673993457511487204, 1.897360377298975553, -0.2389773157873422427 ) ) ;
#140174=CARTESIAN_POINT ( 'NONE',  ( 5.195741393986025969, -1.391442517743620710, -1.394189886649561227 ) ) ;
#140176=CARTESIAN_POINT ( 'NONE',  ( 0.3396542298245264213, 1.936664667523413152, 0.1439508268369827926 ) ) ;
#140180=CARTESIAN_POINT ( 'NONE',  ( 6.047156637250688860, 0.2094617991648151656, 2.110256208591613003 ) ) ;
#140183=CARTESIAN_POINT ( 'NONE',  ( 3.686107007616833631, 1.064666855108999721, 1.588282736317746302 ) ) ;
#140185=CARTESIAN_POINT ( 'NONE',  ( 0.5697015142280477118, 0.2141057807664331902, -2.196374807094509496 ) ) ;
#140187=CARTESIAN_POINT ( 'NONE',  ( 6.633470333208185465, -0.1360683555875797923, 1.981904614263108266 ) ) ;
#140189=CARTESIAN_POINT ( 'NONE',  ( 6.721331454403435934, -0.1262074967819451221, 1.796610827203233063 ) ) ;
#140190=CARTESIAN_POINT ( 'NONE',  ( 5.612517632836664383, 1.944729323200470095, 0.5331731267440716904 ) ) ;
#140191=CARTESIAN_POINT ( 'NONE',  ( 1.768117254402020277, -2.054967671486531255, 0.2513356459030794410 ) ) ;
#140202=CARTESIAN_POINT ( 'NONE',  ( 6.825078400183544503, 2.075476428726834577, 2.163873318353096931 ) ) ;
#140205=CARTESIAN_POINT ( 'NONE',  ( 4.711369565069784215, 1.661324788532690500, 0.4972849887868810437 ) ) ;
#140208=CARTESIAN_POINT ( 'NONE',  ( 2.061466481998303735, 1.718891244229248105, 1.153550331455879707 ) ) ;
#140209=CARTESIAN_POINT ( 'NONE',  ( 3.673546786387419605, 1.535089753090538078, 1.458380203637131833 ) ) ;
#140213=CARTESIAN_POINT ( 'NONE',  ( 1.270285106180467416, -0.8805531663822261379, -1.761673308874162069 ) ) ;
#140217=CARTESIAN_POINT ( 'NONE',  ( 3.398623556838876514, 1.807253594820698250, -1.409964679536945598 ) ) ;
#140218=CARTESIAN_POINT ( 'NONE',  ( 1.681982107312831154, -0.9779208310041755947, 1.541497997293653555 ) ) ;
#140222=CARTESIAN_POINT ( 'NONE',  ( 2.549090200060105893, 0.2507624435445845457, 1.997490752340509879 ) ) ;
#140223=CARTESIAN_POINT ( 'NONE',  ( 3.151168776707893748, 1.684956273983062580, -1.004420888743910334 ) ) ;
#140227=CARTESIAN_POINT ( 'NONE',  ( 6.544877668737552945, -1.678188448499055685, -1.246566921223101865 ) ) ;
#140228=CARTESIAN_POINT ( 'NONE',  ( 4.979261681649114202, 1.650653357529890730, -0.6390028274257038010 ) ) ;
#140230=CARTESIAN_POINT ( 'NONE',  ( 1.025618320672251560, -1.392776288830662512, -1.691927514038966907 ) ) ;
#140231=CARTESIAN_POINT ( 'NONE',  ( 5.999919492459485859, -0.6329648550039753685, -1.621342527780894827 ) ) ;
#140233=CARTESIAN_POINT ( 'NONE',  ( 0.1333692844072559280, 0.001398348041498076455, -2.053671342968105051 ) ) ;
#140234=CARTESIAN_POINT ( 'NONE',  ( 6.539654151966706408, -1.780142272834178918, 1.453760081647121671 ) ) ;
#140236=CARTESIAN_POINT ( 'NONE',  ( 5.887993837006205489, -0.03927123031851989521, 1.733586367271770179 ) ) ;
#140237=CARTESIAN_POINT ( 'NONE',  ( 5.336453890206420247, -1.210535830701382709, 1.802210774359000567 ) ) ;
#140239=CARTESIAN_POINT ( 'NONE',  ( 0.04044418650436896329, 0.8167838292495681607, 1.953657075893009853 ) ) ;
#140240=CARTESIAN_POINT ( 'NONE',  ( 2.843750000000001332, 1.895863743164146298, 0.7852924748298368840 ) ) ;
#140243=CARTESIAN_POINT ( 'NONE',  ( 3.997031241255116552, 1.627850364849007248, -1.029807644849835890 ) ) ;
#140245=CARTESIAN_POINT ( 'NONE',  ( 1.752877424878969803, 2.197725149470313166, 0.3219655503990859757 ) ) ;
#140250=CARTESIAN_POINT ( 'NONE',  ( 2.912952216767932256, -0.6468334258018549887, -2.125021405654815787 ) ) ;
#140257=CARTESIAN_POINT ( 'NONE',  ( 0.9850002542920628379, -2.016597020373378513, 0.002813405579435435122 ) ) ;
#140259=CARTESIAN_POINT ( 'NONE',  ( 6.637180544258393766, -0.09741176211745629365, -2.060485520500746848 ) ) ;
#140262=CARTESIAN_POINT ( 'NONE',  ( 6.146048976554097543, 0.5551056870855082259, 1.649627438850902017 ) ) ;
#140265=CARTESIAN_POINT ( 'NONE',  ( 0.9656335942268097217, 0.8653965441102560163, 1.543625204253181948 ) ) ;
#140266=CARTESIAN_POINT ( 'NONE',  ( 6.539718741795587320, -1.333554142906383744, 1.108523769342983689 ) ) ;
#140267=CARTESIAN_POINT ( 'NONE',  ( -0.1296875068448159751, 0.001480089298542403009, -1.826395826379861864 ) ) ;
#140268=CARTESIAN_POINT ( 'NONE',  ( 3.896227223837216869, -0.7194467914123764407, -2.176594258899899437 ) ) ;
#140270=CARTESIAN_POINT ( 'NONE',  ( 2.659893383946440260, -1.269561761542839617, 1.333649727802692198 ) ) ;
#140274=CARTESIAN_POINT ( 'NONE',  ( 3.135583521505393545, -1.224952879796761041, -1.353777129306121818 ) ) ;
#140275=CARTESIAN_POINT ( 'NONE',  ( 3.938125092175647879, -1.678004675797317713, -1.117833462672225497 ) ) ;
#140277=CARTESIAN_POINT ( 'NONE',  ( 3.133911187764222728, -1.518274094020392706, -1.677614996870570918 ) ) ;
#140279=CARTESIAN_POINT ( 'NONE',  ( 5.702208657235168232, -2.106147099624333219, -0.003344702849475410765 ) ) ;
#140281=CARTESIAN_POINT ( 'NONE',  ( 2.664580169416390643, -0.7900844611210651180, -1.913877855911281234 ) ) ;
#140284=CARTESIAN_POINT ( 'NONE',  ( 5.725269513181780567, 1.870077439114096629, 0.9995941271150191598 ) ) ;
#140287=CARTESIAN_POINT ( 'NONE',  ( 0.9262474005801927257, 1.148234195015400694, -1.546785173711192840 ) ) ;
#140295=CARTESIAN_POINT ( 'NONE',  ( 0.1764466950717893667, 2.196028898142581731, -0.3343166089466164115 ) ) ;
#140296=CARTESIAN_POINT ( 'NONE',  ( 1.799976324648028481, -0.7102278526811952597, 1.982709249334560164 ) ) ;
#140299=CARTESIAN_POINT ( 'NONE',  ( 5.875803118876519626, -1.815897848738392106, 0.4062362408630160737 ) ) ;
#140307=CARTESIAN_POINT ( 'NONE',  ( 3.139059813392345077, -0.1416510307416830594, -1.956792864499560691 ) ) ;
#140308=CARTESIAN_POINT ( 'NONE',  ( 2.395597313961893349, 1.670541196947441520, 1.371929806955954012 ) ) ;
#140312=CARTESIAN_POINT ( 'NONE',  ( 3.767295573485733851, 0.9686143178696275946, 1.445635114442943348 ) ) ;
#140316=CARTESIAN_POINT ( 'NONE',  ( 1.968124833515383809, 1.674630251985644414, 1.122327857054454814 ) ) ;
#140318=CARTESIAN_POINT ( 'NONE',  ( 0.08116279290028630133, -0.1557560750096824431, -2.127278773206460638 ) ) ;
#140319=CARTESIAN_POINT ( 'NONE',  ( 2.043765361886350274, 0.7562441204337754241, -1.820841827831324533 ) ) ;
#140326=CARTESIAN_POINT ( 'NONE',  ( 2.086587641237521495, -1.240871089896943280, 1.593450946908819832 ) ) ;
#140328=CARTESIAN_POINT ( 'NONE',  ( 5.561655955723623812, 0.4570820274143985729, -2.261718950934066275 ) ) ;
#140330=CARTESIAN_POINT ( 'NONE',  ( 2.535929169054650156, 1.202975682259961765, 1.549578550289295586 ) ) ;
#140332=CARTESIAN_POINT ( 'NONE',  ( 1.002577532868035526, -1.966644254196001196, 0.4445047019146358691 ) ) ;
#140334=CARTESIAN_POINT ( 'NONE',  ( 2.114611820864919611, 2.055121497718506163, 0.5091636546959156240 ) ) ;
#140338=CARTESIAN_POINT ( 'NONE',  ( 2.079791654855645877, -1.805462111169679584, -0.3597937517794968509 ) ) ;
#140342=CARTESIAN_POINT ( 'NONE',  ( 3.058948843759463188, 0.5191580478346514704, 2.055925682384197373 ) ) ;
#140343=CARTESIAN_POINT ( 'NONE',  ( 6.632770897174698810, -1.733374817101345000, 0.8757406700844807546 ) ) ;
#140347=CARTESIAN_POINT ( 'NONE',  ( 4.376282966308748357, -1.189761084491423926, 1.682430632154131578 ) ) ;
#140349=CARTESIAN_POINT ( 'NONE',  ( 0.9250624443557056154, -1.167992581197497604, -1.423340509374780405 ) ) ;
#140353=CARTESIAN_POINT ( 'NONE',  ( 1.594636444620714633, -2.196503929104542951, -0.2137616909994101977 ) ) ;
#140354=CARTESIAN_POINT ( 'NONE',  ( 3.427297576727184047, 0.05164501975941707818, 2.261966552586023749 ) ) ;
#140356=CARTESIAN_POINT ( 'NONE',  ( 3.990334445075129466, -1.038098595406260705, 1.484453480236499923 ) ) ;
#140357=CARTESIAN_POINT ( 'NONE',  ( 2.694441388940031601, 1.384233754937878258, -1.324569364742228972 ) ) ;
#140358=CARTESIAN_POINT ( 'NONE',  ( 3.754400092289136737, -2.067862582909282487, -0.1045053291982081939 ) ) ;
#140360=CARTESIAN_POINT ( 'NONE',  ( 2.448066223300342514, 1.970991375097268961, 0.05018580263361701460 ) ) ;
#140361=CARTESIAN_POINT ( 'NONE',  ( 1.008667890995796457, 1.460797969510800876, -1.255919511179462322 ) ) ;
#140362=CARTESIAN_POINT ( 'NONE',  ( 4.276139911362797363, -1.077190196239918851, 1.529178877381555335 ) ) ;
#140363=CARTESIAN_POINT ( 'NONE',  ( 2.702171824926146826, -0.7227257407616082263, 2.191671519121952461 ) ) ;
#140364=CARTESIAN_POINT ( 'NONE',  ( 3.842128478764065047, -0.9187925100661897826, 1.618370328034287597 ) ) ;
#140370=CARTESIAN_POINT ( 'NONE',  ( 0.1882882188262140766, -0.9905318517600868455, 1.858590670187587612 ) ) ;
#140375=CARTESIAN_POINT ( 'NONE',  ( 1.617596980227502756, 1.765956010477184535, 1.173731981927571555 ) ) ;
#140376=CARTESIAN_POINT ( 'NONE',  ( 0.2990895800742687793, -0.2513629124439535345, -2.004038569727568664 ) ) ;
#140380=CARTESIAN_POINT ( 'NONE',  ( 1.528841242883504981, 2.082761121880230881, 0.5781018612496248155 ) ) ;
#140383=CARTESIAN_POINT ( 'NONE',  ( 6.925078400183553029, 7.052683076116534444, 2.553806833665558162 ) ) ;
#140386=CARTESIAN_POINT ( 'NONE',  ( 5.401577436481666439, -1.966305606708594667, 0.4464985920552416720 ) ) ;
#140391=CARTESIAN_POINT ( 'NONE',  ( 0.6028508490328026159, -0.7652319425662640340, -2.129318446015377120 ) ) ;
#140395=CARTESIAN_POINT ( 'NONE',  ( 0.03459428079104728826, -1.538086888106354522, 1.141608027856432450 ) ) ;
#140399=CARTESIAN_POINT ( 'NONE',  ( 2.349869733406087402, 1.724505987646451688, 0.04327962033413671611 ) ) ;
#140402=CARTESIAN_POINT ( 'NONE',  ( 1.440303513825416992, 0.3384911870211620988, 1.736878781881325384 ) ) ;
#140403=CARTESIAN_POINT ( 'NONE',  ( 1.998691314347844417, -1.974684511280549559, -0.3905480285893418446 ) ) ;
#140406=CARTESIAN_POINT ( 'NONE',  ( 4.594872931952145301, -0.4798491958124780910, -2.153818993410236970 ) ) ;
#140410=CARTESIAN_POINT ( 'NONE',  ( 4.670628115925999246, 0.8122961462209904449, 1.958930372594757330 ) ) ;
#140411=CARTESIAN_POINT ( 'NONE',  ( 2.882435586221145041, -0.5880402899147362250, -1.928746874286999757 ) ) ;
#140412=CARTESIAN_POINT ( 'NONE',  ( 3.146531925530637430, 1.768428357263505557, 0.3923012617871086682 ) ) ;
#140416=CARTESIAN_POINT ( 'NONE',  ( 1.656895194024514906, -1.602792776363659133, -0.9643473572949824435 ) ) ;
#140418=CARTESIAN_POINT ( 'NONE',  ( 6.498675964634617941, -0.4922777150685350156, -1.758009983081544991 ) ) ;
#140421=CARTESIAN_POINT ( 'NONE',  ( 2.061615604755413500, 1.182011660234401962, 1.507458768284040129 ) ) ;
#140428=CARTESIAN_POINT ( 'NONE',  ( 4.786342355033275986, -0.6839347017603314427, -1.897111394664739326 ) ) ;
#140433=CARTESIAN_POINT ( 'NONE',  ( 4.394861267144759331, -2.057662932662501110, -0.5123870273424437904 ) ) ;
#140434=CARTESIAN_POINT ( 'NONE',  ( -0.02968770228137587730, 6.948707269782667062, -2.421356871654921417 ) ) ;
#140436=CARTESIAN_POINT ( 'NONE',  ( 3.936761750732898690, 0.2861355568666827387, 1.950351509585077858 ) ) ;
#140438=CARTESIAN_POINT ( 'NONE',  ( -0.1052096654315381741, -1.953846233167291002, -0.4849948655165080558 ) ) ;
#140440=CARTESIAN_POINT ( 'NONE',  ( 6.333232048763643540, -1.701881231816049000, -1.259509043995930222 ) ) ;
#140443=CARTESIAN_POINT ( 'NONE',  ( 1.293514844328220281, -1.872496763586928514, 0.8835221827151735763 ) ) ;
#140448=CARTESIAN_POINT ( 'NONE',  ( 3.345728622622257564, 2.090823719190892049, -0.0003901280219448939298 ) ) ;
#140451=CARTESIAN_POINT ( 'NONE',  ( 1.729251940891060713, -1.720190037149814444, 0.6116943438041824166 ) ) ;
#140452=CARTESIAN_POINT ( 'NONE',  ( 0.2229362713279548491, 1.575107908988721883, 0.8944890650159162959 ) ) ;
#140454=CARTESIAN_POINT ( 'NONE',  ( 6.006501602161061548, -0.7906231143557164165, -2.060575041408031272 ) ) ;
#140456=CARTESIAN_POINT ( 'NONE',  ( 4.717920652503574175, -2.164970738276258189, 0.4266498443898231185 ) ) ;
#140458=CARTESIAN_POINT ( 'NONE',  ( 2.736851483355093873, 1.801321139115559244, 0.6423184003811268639 ) ) ;
#140460=CARTESIAN_POINT ( 'NONE',  ( 5.318829906782316819, -1.502041817331278173, 1.425132596443792643 ) ) ;
#140463=CARTESIAN_POINT ( 'NONE',  ( 5.513277522340928272, -2.138352208816508782, 0.4792397250529822905 ) ) ;
#140465=FILL_AREA_STYLE_COLOUR ( '', #100960 ) ;
#140473=CARTESIAN_POINT ( 'NONE',  ( 6.368043163206878354, -2.055323469740528264, 0.2474699835256082281 ) ) ;
#140474=CARTESIAN_POINT ( 'NONE',  ( 4.441968003317652958, 0.8225352836801721468, -1.742211325687251788 ) ) ;
#140475=CARTESIAN_POINT ( 'NONE',  ( 0.5269705342763851830, -1.727990693721896287, 1.039014695730144933 ) ) ;
#140479=CARTESIAN_POINT ( 'NONE',  ( 0.5861907285475282947, -2.175377356269320828, -0.2643977408666315365 ) ) ;
#140480=CARTESIAN_POINT ( 'NONE',  ( 5.672426548614881270, -1.154804106291613675, 1.414059844683832612 ) ) ;
#140487=CARTESIAN_POINT ( 'NONE',  ( 2.999365392321148516, -1.839032331094083927, 0.09308366406014097205 ) ) ;
#140488=CARTESIAN_POINT ( 'NONE',  ( 6.099863781956886832, 1.391357071557168146, 1.455236689230124947 ) ) ;
#140489=CARTESIAN_POINT ( 'NONE',  ( 0.9842439076201170423, 2.124318566921878482, 0.8778218499742740377 ) ) ;
#140490=CARTESIAN_POINT ( 'NONE',  ( 6.772321408939014020, -0.9219223515295159599, -1.731591420108986812 ) ) ;
#140495=CARTESIAN_POINT ( 'NONE',  ( 0.7837444799244470683, -1.966470238067185905, 0.6478734989143407619 ) ) ;
#140497=CARTESIAN_POINT ( 'NONE',  ( 2.472313036883976078, -2.001511166234470007, -0.6043430715973686640 ) ) ;
#140498=CARTESIAN_POINT ( 'NONE',  ( 1.164687902950040321, -1.689591380799923215, -0.8031939614948147010 ) ) ;
#140499=CARTESIAN_POINT ( 'NONE',  ( 1.774767310740913207, -2.001205085354029301, 0.2439901982170673833 ) ) ;
#140502=CARTESIAN_POINT ( 'NONE',  ( 1.839017211142121244, 0.6657927772366920571, -1.608260388387482420 ) ) ;
#140506=CARTESIAN_POINT ( 'NONE',  ( 3.035487670047633202, -1.158914029964135395, -1.277714875195012700 ) ) ;
#140507=CARTESIAN_POINT ( 'NONE',  ( 2.771223791512751333, 2.080116120148074010, -0.6901165687889164735 ) ) ;
#140508=CARTESIAN_POINT ( 'NONE',  ( 4.758537496233657293, 0.8426522330295079799, 2.039869969286691731 ) ) ;
#140510=CARTESIAN_POINT ( 'NONE',  ( 2.202231255880624516, 0.8340544509695562159, -2.004656366586863303 ) ) ;
#140511=CARTESIAN_POINT ( 'NONE',  ( 1.260069262837599791, 0.7379878962356714034, 1.670071910705408946 ) ) ;
#140512=CARTESIAN_POINT ( 'NONE',  ( 3.889952640533121286, -2.111394073168832097, 0.1598612332101984890 ) ) ;
#140515=CARTESIAN_POINT ( 'NONE',  ( 3.122906911094673887, 0.05843746759831092152, 2.291794357358638123 ) ) ;
#140519=CARTESIAN_POINT ( 'NONE',  ( -0.04015575566676531788, -1.641981170221142872, -1.341450104213978589 ) ) ;
#140527=CARTESIAN_POINT ( 'NONE',  ( 4.693982515131527755, 1.755768268644173791, 0.9914009648221073778 ) ) ;
#140529=CARTESIAN_POINT ( 'NONE',  ( 3.291897078901334428, -1.381674118267547602, -1.531590470265832726 ) ) ;
#140534=CARTESIAN_POINT ( 'NONE',  ( 6.597619724345276104, -2.191060131252516641, 0.04951108399064289151 ) ) ;
#140535=CARTESIAN_POINT ( 'NONE',  ( 4.061172775696818782, -1.158689426361030561, 1.650081270007992318 ) ) ;
#140536=CARTESIAN_POINT ( 'NONE',  ( 3.245484093776138668, 1.841430844176932480, -0.003062914905635482320 ) ) ;
#140538=CARTESIAN_POINT ( 'NONE',  ( 6.545924712158827319, 0.6954503440314525609, -1.688125835592364066 ) ) ;
#140540=CARTESIAN_POINT ( 'NONE',  ( 0.07143917554365029898, -1.076037094620578616, 2.031297111741585226 ) ) ;
#140542=CARTESIAN_POINT ( 'NONE',  ( 0.4392367245290337840, 0.3885019757292383913, 2.228643277672849976 ) ) ;
#140543=CARTESIAN_POINT ( 'NONE',  ( 2.332770561069871462, 2.043027141408111813, 0.5109185277013729154 ) ) ;
#140554=CARTESIAN_POINT ( 'NONE',  ( 4.271885190509593144, 0.4847678284230126922, -2.167736239397171083 ) ) ;
#140555=CARTESIAN_POINT ( 'NONE',  ( 0.9904705247469265394, -0.5356807779838267392, -2.124848333686576662 ) ) ;
#140556=CARTESIAN_POINT ( 'NONE',  ( 0.3642759247451561322, 2.182245240920151375, -0.3280614795862640820 ) ) ;
#140558=CARTESIAN_POINT ( 'NONE',  ( 4.861744986159981075, -0.5251177144562025889, 1.890194517805739771 ) ) ;
#140566=CARTESIAN_POINT ( 'NONE',  ( 4.008146050417991546, -0.8085630067716749192, 1.960596031080278356 ) ) ;
#140568=CARTESIAN_POINT ( 'NONE',  ( 5.875883356151954118, 1.283970044810868849, 1.738936680771227206 ) ) ;
#140569=CARTESIAN_POINT ( 'NONE',  ( 4.423293856316495187, -1.136390847421838490, -1.448631019334602144 ) ) ;
#140572=CARTESIAN_POINT ( 'NONE',  ( 0.1513755341013711675, 0.6631104863988640519, 1.609371435944781936 ) ) ;
#140573=CARTESIAN_POINT ( 'NONE',  ( 6.827182134110195477, 0.006757161851597691914, 1.710856279483467413 ) ) ;
#140578=CARTESIAN_POINT ( 'NONE',  ( 3.784175263432405956, -1.067420458145739826, 1.879713924940962677 ) ) ;
#140580=CARTESIAN_POINT ( 'NONE',  ( 5.835314490094169138, -1.281163661392352493, 1.556671411349755285 ) ) ;
#140582=CARTESIAN_POINT ( 'NONE',  ( 3.309602206082487008, -0.4233974974612622066, 2.119663826602156131 ) ) ;
#140584=CARTESIAN_POINT ( 'NONE',  ( 3.936761750732898690, 0.2861355568666827387, 1.950351509585077858 ) ) ;
#140585=CARTESIAN_POINT ( 'NONE',  ( 1.483892314354786857, 2.131289638308156320, -0.8850757863276045301 ) ) ;
#140586=CARTESIAN_POINT ( 'NONE',  ( 4.165347332011271497, 0.2559277237221342371, -2.044777286818760142 ) ) ;
#140587=CARTESIAN_POINT ( 'NONE',  ( 6.146037779257278011, 0.6132840560482490933, 1.842739892034722882 ) ) ;
#140596=CARTESIAN_POINT ( 'NONE',  ( 2.802037382575186975, -0.6933082239683820980, 2.095089865402133267 ) ) ;
#140599=CARTESIAN_POINT ( 'NONE',  ( 6.051606296966551390, 1.483190043545830505, 1.284043323103729595 ) ) ;
#140600=CARTESIAN_POINT ( 'NONE',  ( -0.1290005225502432740, 4.081813041011835175, -2.728655865233818201 ) ) ;
#140604=CARTESIAN_POINT ( 'NONE',  ( 5.296754776809613041, 1.507285696749562476, 1.057021923447129197 ) ) ;
#140606=CARTESIAN_POINT ( 'NONE',  ( 1.868112839806375325, 1.058416689118582665, 1.768180007894581740 ) ) ;
#140612=CARTESIAN_POINT ( 'NONE',  ( 1.112264416572866566, -0.9257652390157306010, -1.841317064699917516 ) ) ;
#140614=CARTESIAN_POINT ( 'NONE',  ( 4.810013364240863787, 1.265987717737980134, -1.337210144835267345 ) ) ;
#140617=CARTESIAN_POINT ( 'NONE',  ( 6.610000000000026965, 7.052677709320480659, 2.598153670447616470 ) ) ;
#140619=CARTESIAN_POINT ( 'NONE',  ( 4.424592250794217030, 1.359014646446855767, -1.738718759629574118 ) ) ;
#140620=CARTESIAN_POINT ( 'NONE',  ( 0.4566077865506940059, 0.8268718848777978359, 1.997384878126715613 ) ) ;
#140622=CARTESIAN_POINT ( 'NONE',  ( -0.1054227091227821350, -1.855472971956134920, -0.4628026090111520552 ) ) ;
#140623=CARTESIAN_POINT ( 'NONE',  ( -0.1882626618336727398, -1.244567986390752390, -1.587255334073833790 ) ) ;
#140625=CARTESIAN_POINT ( 'NONE',  ( 0.07536363704235826688, -0.001874865094115066300, -2.144269471569634877 ) ) ;
#140626=CARTESIAN_POINT ( 'NONE',  ( 5.356085673312771966, 0.7711821229579116643, -1.750063228584404440 ) ) ;
#140628=CARTESIAN_POINT ( 'NONE',  ( 1.182252951876180180, -1.824241171369020531, -0.4133900166373091767 ) ) ;
#140629=CARTESIAN_POINT ( 'NONE',  ( 2.641814858895009444, 2.006371511526034546, -0.2024640970367599380 ) ) ;
#140631=CARTESIAN_POINT ( 'NONE',  ( 3.475310780013381340, 0.05149396089606420035, -2.105609240523627967 ) ) ;
#140636=CARTESIAN_POINT ( 'NONE',  ( 4.500263427444707531, -0.9482861330638262531, 1.783302102689677371 ) ) ;
#140640=CARTESIAN_POINT ( 'NONE',  ( 4.710339443014814442, -0.9195336665917231977, -1.956380038831563972 ) ) ;
#140645=CARTESIAN_POINT ( 'NONE',  ( 1.926474581872784420, 1.115185415580312700, 1.862746952601635808 ) ) ;
#140648=CARTESIAN_POINT ( 'NONE',  ( 0.5207438388301621757, -1.748553680932497745, 0.5769860859521497298 ) ) ;
#140651=CARTESIAN_POINT ( 'NONE',  ( 3.421585747727782678, -1.306972202059282218, -1.759028276249123168 ) ) ;
#140652=CARTESIAN_POINT ( 'NONE',  ( 6.983263157960330147, 7.052490050591996962, 2.551961896892048109 ) ) ;
#140653=CARTESIAN_POINT ( 'NONE',  ( 3.432755235230527280, 2.206939294067700619, 0.4977334550177249795 ) ) ;
#140659=CARTESIAN_POINT ( 'NONE',  ( 4.586996685387556560, 1.581260375356493331, -0.7947977318805318214 ) ) ;
#140661=CARTESIAN_POINT ( 'NONE',  ( 0.6574224672675427206, -1.779203033188281990, -1.126420244723020270 ) ) ;
#140664=CARTESIAN_POINT ( 'NONE',  ( 1.328490337915340991, -1.252144239891037403, 1.520259730874585768 ) ) ;
#140667=CARTESIAN_POINT ( 'NONE',  ( 5.238451434589118882, 1.072694688086765158, -1.459716015685054602 ) ) ;
#140672=CARTESIAN_POINT ( 'NONE',  ( 4.592568387165754551, -0.4099775813008778025, -1.825014511474598589 ) ) ;
#140674=CARTESIAN_POINT ( 'NONE',  ( 4.768459183169745152, -0.8803848081004579385, -1.873848736155204087 ) ) ;
#140685=CARTESIAN_POINT ( 'NONE',  ( 4.510177812457000002, 1.961482754637720927, -0.04604004567236585910 ) ) ;
#140686=CARTESIAN_POINT ( 'NONE',  ( 1.563827143785265328, 1.649830188709809686, -1.158509706484150970 ) ) ;
#140690=CARTESIAN_POINT ( 'NONE',  ( 1.563515255687727645, 1.843751956470768283, -0.3144994141817195055 ) ) ;
#140692=CARTESIAN_POINT ( 'NONE',  ( 2.531496316177814787, -0.1932786158439051827, 2.003878288502713101 ) ) ;
#140694=CARTESIAN_POINT ( 'NONE',  ( 3.568056664072499995, -1.041641863948725932, 1.843179926220348541 ) ) ;
#140697=CARTESIAN_POINT ( 'NONE',  ( 5.055165704564410944, 1.723227314588217318, -1.147259442322377865 ) ) ;
#140699=CARTESIAN_POINT ( 'NONE',  ( 0.5211768519108473940, -1.983982463993728906, 0.6597393503331959730 ) ) ;
#140700=CARTESIAN_POINT ( 'NONE',  ( 6.620655732516652847, 0.5779860733656561056, 2.127054332187257923 ) ) ;
#140701=CARTESIAN_POINT ( 'NONE',  ( 4.893472065931465664, 1.353474861756031267, 1.225258530246610134 ) ) ;
#140708=CARTESIAN_POINT ( 'NONE',  ( 5.742805640131908973, 1.844151595126357179, 0.5056804652876015771 ) ) ;
#140718=CARTESIAN_POINT ( 'NONE',  ( 5.448842280278080707, -1.824126957265741256, -0.8596167168879662590 ) ) ;
#140721=CARTESIAN_POINT ( 'NONE',  ( 0.1394461523057084484, 7.629137130509043629, -2.319723760180956607 ) ) ;
#140725=CARTESIAN_POINT ( 'NONE',  ( 2.078894642590666031, 1.835759051837970945, 0.7136754054878727827 ) ) ;
#140726=CARTESIAN_POINT ( 'NONE',  ( 3.831657784458125438, 0.6766976527424087839, -1.899625577706779422 ) ) ;
#140728=CARTESIAN_POINT ( 'NONE',  ( 6.727182134110237577, 2.938513203633616566, 2.740843696613648017 ) ) ;
#140730=CARTESIAN_POINT ( 'NONE',  ( 4.136819237485493517, -1.907179771870757268, 1.079280405373375773 ) ) ;
#140732=CARTESIAN_POINT ( 'NONE',  ( 2.309485145960771035, -0.4240201670873133266, 1.878992650109307716 ) ) ;
#140735=CARTESIAN_POINT ( 'NONE',  ( 0.2333540202161792088, 2.022347194651296753, -2.461825824937914575 ) ) ;
#140742=CARTESIAN_POINT ( 'NONE',  ( 5.653808312887880660, 0.7519890275384639722, 1.680886247995525773 ) ) ;
#140743=CARTESIAN_POINT ( 'NONE',  ( 2.367839801511921305, 0.5346396131555611886, -1.940748983941695371 ) ) ;
#140744=CARTESIAN_POINT ( 'NONE',  ( 5.888098204360154853, -0.06530352750959941832, 2.297622472229691404 ) ) ;
#140745=CARTESIAN_POINT ( 'NONE',  ( 3.010441868158566958, 0.6223964701937385602, 1.753942229013090159 ) ) ;
#140751=CARTESIAN_POINT ( 'NONE',  ( 5.812080397998875547, 1.403551008015807788, -1.549792465900756477 ) ) ;
#140756=CARTESIAN_POINT ( 'NONE',  ( 5.777914075412113881, 1.032862044635925569, 1.381300780159310460 ) ) ;
#140758=CARTESIAN_POINT ( 'NONE',  ( 1.564674090997038025, -0.9275931817575002736, 1.464960531123546961 ) ) ;
#140761=CARTESIAN_POINT ( 'NONE',  ( 6.315302488195832176, -1.857785929941946135, -1.123309179604212504 ) ) ;
#140762=CARTESIAN_POINT ( 'NONE',  ( 4.670415550810885996, -1.190324863180821646, 1.384379922071424351 ) ) ;
#140763=CARTESIAN_POINT ( 'NONE',  ( 1.727322521004183598, 0.1496332796787832875, -1.956138870750294023 ) ) ;
#140767=CARTESIAN_POINT ( 'NONE',  ( 3.703867829435038228, 1.536975034498413439, 1.461131120854219700 ) ) ;
#140771=CARTESIAN_POINT ( 'NONE',  ( 1.973570569994816060, -0.2575147360633044391, 2.054139978358980656 ) ) ;
#140774=CARTESIAN_POINT ( 'NONE',  ( 3.879691667246706110, 0.2712996660018602846, -2.204593333604548455 ) ) ;
#140776=CARTESIAN_POINT ( 'NONE',  ( 1.231506118810040018, 2.296321937838792238, 0.1066795702680169711 ) ) ;
#140778=CARTESIAN_POINT ( 'NONE',  ( 6.174688434915334589, 1.389358497796209013, -1.524562697504736164 ) ) ;
#140782=CARTESIAN_POINT ( 'NONE',  ( 6.339398910184078417, 0.6979989802004606947, -1.704029730133400866 ) ) ;
#140784=CARTESIAN_POINT ( 'NONE',  ( -0.1104750535120251481, 6.947232870375212421, -2.698533382536407732 ) ) ;
#140785=CARTESIAN_POINT ( 'NONE',  ( 3.504663807952506538, 1.359994529648723249, -1.060664293495124477 ) ) ;
#140786=CARTESIAN_POINT ( 'NONE',  ( 1.780482797753998092, -0.5424726148271253878, -1.942096288550937411 ) ) ;
#140787=CARTESIAN_POINT ( 'NONE',  ( 3.077065830326791929, -0.9295426453954873658, 2.102514275539566935 ) ) ;
#140788=CARTESIAN_POINT ( 'NONE',  ( 3.585499571845919942, 2.047054288528706412, -0.9635960562263863327 ) ) ;
#140789=CARTESIAN_POINT ( 'NONE',  ( 5.795568699328918605, 1.593732954614892616, 1.376895199011922477 ) ) ;
#140791=CARTESIAN_POINT ( 'NONE',  ( 3.374023350818358580, -1.056766630983814625, 1.419390967538982418 ) ) ;
#140795=CARTESIAN_POINT ( 'NONE',  ( 0.1469514510107531868, -1.837142584329341410, 1.370738489780512825 ) ) ;
#140797=CARTESIAN_POINT ( 'NONE',  ( 5.595603887632320195, -1.841320590885606068, 0.004091980732826016286 ) ) ;
#140800=CARTESIAN_POINT ( 'NONE',  ( 5.367185978643659539, 2.112682091867735146, -0.5819856738719306755 ) ) ;
#140803=CARTESIAN_POINT ( 'NONE',  ( 5.934052368846653991, 1.230181698326970885, 1.665117723180092213 ) ) ;
#140806=CARTESIAN_POINT ( 'NONE',  ( 4.670489471188726149, -1.257041717089462773, 1.459967279689990960 ) ) ;
#140809=CARTESIAN_POINT ( 'NONE',  ( 6.451439665316073935, -1.893653415279672902, 0.9546920624979161607 ) ) ;
#140818=CARTESIAN_POINT ( 'NONE',  ( 1.539427311113782837, 1.813978416018032558, -0.7477436361984082236 ) ) ;
#140822=CARTESIAN_POINT ( 'NONE',  ( 5.687936657224680559, -1.243353266631580523, -1.517579924814119074 ) ) ;
#140826=CARTESIAN_POINT ( 'NONE',  ( 0.5853300251711880398, -0.2802842603415867107, -2.245014038439311577 ) ) ;
#140827=CARTESIAN_POINT ( 'NONE',  ( -0.2106725631050281045, 2.870437361830021405, -2.492085498774513574 ) ) ;
#140830=CARTESIAN_POINT ( 'NONE',  ( 0.4560483712790652233, 0.7097975879313439540, 1.730851494400275747 ) ) ;
#140831=CARTESIAN_POINT ( 'NONE',  ( 5.817694146727262705, -1.364776552785733399, 1.069276891063369650 ) ) ;
#140833=CARTESIAN_POINT ( 'NONE',  ( 3.175498511859841333, 1.392037702009111033, 1.692654053968026151 ) ) ;
#140834=CARTESIAN_POINT ( 'NONE',  ( 4.524672722398297431, 1.423327999681742062, -1.816260527432728811 ) ) ;
#140835=CARTESIAN_POINT ( 'NONE',  ( 0.6376604129620618844, -1.456937097490097255, -1.457867103223365213 ) ) ;
#140836=CARTESIAN_POINT ( 'NONE',  ( 2.097507970028670510, -1.941522886764552203, 0.04780177728339052301 ) ) ;
#140840=CARTESIAN_POINT ( 'NONE',  ( 4.676102344489991403, 2.097148071331572439, -0.3138259731317455392 ) ) ;
#140842=CARTESIAN_POINT ( 'NONE',  ( 3.393204081532863459, -0.8197727808607684352, -1.842447475547980495 ) ) ;
#140846=CARTESIAN_POINT ( 'NONE',  ( 0.9436603434208358232, 0.7422609627109194586, -1.668170528445270140 ) ) ;
#140851=CARTESIAN_POINT ( 'NONE',  ( 5.752824481226431530, -1.626044790292068498, 1.266090340377580947 ) ) ;
#140856=CARTESIAN_POINT ( 'NONE',  ( 4.635418745873795210, -0.09682320349532060055, 2.017468490573450346 ) ) ;
#140857=CARTESIAN_POINT ( 'NONE',  ( 5.338630837375411886, 1.324400161455315805, -1.783172940106398485 ) ) ;
#140861=CARTESIAN_POINT ( 'NONE',  ( 3.678635468349491511, -1.985665955521208614, -0.5514216839303841544 ) ) ;
#140862=CARTESIAN_POINT ( 'NONE',  ( 4.113907844847329187, 0.1017495355152969322, 2.013985960686740295 ) ) ;
#140870=CARTESIAN_POINT ( 'NONE',  ( 4.464220131058834085, 1.617570847575640736, 1.203168917025834839 ) ) ;
#140871=CARTESIAN_POINT ( 'NONE',  ( 2.290725937607818175, 1.422998120520948984, 1.168276728405498455 ) ) ;
#140873=CARTESIAN_POINT ( 'NONE',  ( 1.489377799468382113, -0.3424701664414407931, -2.282033458877083199 ) ) ;
#140875=CARTESIAN_POINT ( 'NONE',  ( 3.321700061091820366, -2.084211496276411779, 0.5730272365244913901 ) ) ;
#140879=CARTESIAN_POINT ( 'NONE',  ( 1.867826558377215118, 0.9591755677602131769, 1.605880698980370225 ) ) ;
#140880=CARTESIAN_POINT ( 'NONE',  ( 5.911001178172424986, 1.738356976118849984, 0.9299647631116741975 ) ) ;
#140885=CARTESIAN_POINT ( 'NONE',  ( 0.3818278861203865393, 2.057605126571937060, -0.7983354260262252033 ) ) ;
#140891=CARTESIAN_POINT ( 'NONE',  ( 6.121945800013044447, -1.094813031782817303, -1.639340605029938835 ) ) ;
#140893=CARTESIAN_POINT ( 'NONE',  ( 5.848310222665911162, 2.304730150483401463, 0.1192407711079427196 ) ) ;
#140894=CARTESIAN_POINT ( 'NONE',  ( 5.881279174647062291, -0.04503291608629880066, 1.860690090596372137 ) ) ;
#140895=CARTESIAN_POINT ( 'NONE',  ( 3.239185349552040183, -0.1472093337855179818, -2.057344904835652688 ) ) ;
#140902=CARTESIAN_POINT ( 'NONE',  ( 5.055217142685058285, 1.807878865648751221, -1.202052933306910765 ) ) ;
#140904=CARTESIAN_POINT ( 'NONE',  ( 4.001369526190221571, -1.836035423186295201, 0.1395379388276704880 ) ) ;
#140909=CARTESIAN_POINT ( 'NONE',  ( 0.8258823708265795593, -2.148021843699068789, 0.7105549608077809109 ) ) ;
#140914=CARTESIAN_POINT ( 'NONE',  ( 0.4340482808194640607, -1.023182136338888659, -1.615339470012015166 ) ) ;
#140915=CARTESIAN_POINT ( 'NONE',  ( 1.199668116878411128, -1.770032029468296964, -0.005122706785119778526 ) ) ;
#140916=CARTESIAN_POINT ( 'NONE',  ( 5.795569859559966730, 1.859138327062941132, -0.7725605513991992135 ) ) ;
#140918=CARTESIAN_POINT ( 'NONE',  ( 3.698352234880129874, -2.103465879664846216, -0.1051872838587295522 ) ) ;
#140920=CARTESIAN_POINT ( 'NONE',  ( 3.040549542926245241, -1.448533627684518654, 1.253585735969472648 ) ) ;
#140922=CARTESIAN_POINT ( 'NONE',  ( 4.246515029176777034, -1.947796394531702280, -0.2911330189915450339 ) ) ;
#140923=CARTESIAN_POINT ( 'NONE',  ( 4.974870412032891487, -1.460018184141493647, 1.395898791055903976 ) ) ;
#140924=CARTESIAN_POINT ( 'NONE',  ( 2.342468781959532453, 0.4075140148256419792, 1.825566309089213579 ) ) ;
#140925=CARTESIAN_POINT ( 'NONE',  ( 5.391107817497476695, 1.518517088589757424, -0.8181074574388611520 ) ) ;
#140927=CARTESIAN_POINT ( 'NONE',  ( 2.561379550486083012, -1.920685204893451292, -1.086737900330703166 ) ) ;
#140930=CARTESIAN_POINT ( 'NONE',  ( 6.303176765056641706, -1.658072099422291057, 1.048360225930293321 ) ) ;
#140938=CARTESIAN_POINT ( 'NONE',  ( 2.453653613718423276, 1.598880132357576755, 1.315258840600006085 ) ) ;
#140942=CARTESIAN_POINT ( 'NONE',  ( -0.04036499569192492781, -1.562578347245877630, -1.279382211958324689 ) ) ;
#140948=CARTESIAN_POINT ( 'NONE',  ( 5.132185397524263060, 0.2004025303571632666, -2.006139158026089220 ) ) ;
#140949=CARTESIAN_POINT ( 'NONE',  ( 5.313669575012682778, -1.220653882476211427, -1.476441452469556159 ) ) ;
#140950=CARTESIAN_POINT ( 'NONE',  ( 6.639320575229294086, 0.002105643433562148347, 2.003388605011639179 ) ) ;
#140951=CARTESIAN_POINT ( 'NONE',  ( 2.279091853667324141, 2.002311374866962979, -0.8913168663882904408 ) ) ;
#140956=CARTESIAN_POINT ( 'NONE',  ( 2.197387184563174944, 1.746976956643018219, -0.7784620831182070821 ) ) ;
#140959=CARTESIAN_POINT ( 'NONE',  ( 0.2281389574181335589, 2.011207032379238591, 0.1455110067964115739 ) ) ;
#140962=CARTESIAN_POINT ( 'NONE',  ( 2.929326106026585830, -1.406127681732218360, -1.547418247020322601 ) ) ;
#140964=CARTESIAN_POINT ( 'NONE',  ( 2.414726000362901637, 1.539333419754819854, 0.7781589270328890251 ) ) ;
#140966=CARTESIAN_POINT ( 'NONE',  ( 6.258074605086497932, 0.8102346573028992305, -1.959903593942226907 ) ) ;
#140969=CARTESIAN_POINT ( 'NONE',  ( 0.6429252097494702056, -0.2364460082661112295, -1.947484529462916836 ) ) ;
#140976=CARTESIAN_POINT ( 'NONE',  ( 2.613665174717228368, -0.5667244042059360609, 1.720617414772870335 ) ) ;
#140980=CARTESIAN_POINT ( 'NONE',  ( 4.072783076529101542, -1.339505953097392066, 1.219664821550008549 ) ) ;
#140984=CARTESIAN_POINT ( 'NONE',  ( 4.088223475482699598, 0.9968510564385362205, -1.571365414726686227 ) ) ;
#140987=CARTESIAN_POINT ( 'NONE',  ( 1.229944743773615956, 1.913488753162166045, 0.09234796458578581335 ) ) ;
#140988=CARTESIAN_POINT ( 'NONE',  ( 0.7623938366894518204, -1.325735992016435105, 1.255310662410371370 ) ) ;
#140997=CARTESIAN_POINT ( 'NONE',  ( 5.401205523299864808, -1.691175329543142647, 1.008977833701154125 ) ) ;
#140999=CARTESIAN_POINT ( 'NONE',  ( 0.1280963075596490419, -1.331634228802502928, -1.703589906866372017 ) ) ;
#141000=CARTESIAN_POINT ( 'NONE',  ( 0.8672654471616656480, 2.014311826519481929, -0.5594637955527237416 ) ) ;
#141001=CARTESIAN_POINT ( 'NONE',  ( 6.422877973628248860, 1.797746274024723201, 0.6925914001822802701 ) ) ;
#141004=CARTESIAN_POINT ( 'NONE',  ( 1.852308540880560850, 0.5694407911355814367, 1.734573797025913189 ) ) ;
#141005=CARTESIAN_POINT ( 'NONE',  ( 3.194164748978207680, -0.8942147705085048415, 2.017778291555922809 ) ) ;
#141007=CARTESIAN_POINT ( 'NONE',  ( 1.107505169401588274, 1.450017293480215352, 1.247013401884336403 ) ) ;
#141008=CARTESIAN_POINT ( 'NONE',  ( 1.996483073472170133, 1.947676829468534265, 0.2919340086137369727 ) ) ;
#141009=CARTESIAN_POINT ( 'NONE',  ( 2.489705217443307195, -1.937006489018164190, -0.1406711297040150188 ) ) ;
#141013=CARTESIAN_POINT ( 'NONE',  ( 6.631710597105570315, 1.780986809720253694, -0.5397248755362458184 ) ) ;
#141018=CARTESIAN_POINT ( 'NONE',  ( 2.630644284709309666, 0.2711686948545319886, 2.174668582101045633 ) ) ;
#141022=CARTESIAN_POINT ( 'NONE',  ( 2.754317325142870754, 0.6151756178996542479, 1.719052816137212503 ) ) ;
#141028=CARTESIAN_POINT ( 'NONE',  ( -0.02968770228140016343, 0.2527710104786498047, -1.861515397111657144 ) ) ;
#141030=CARTESIAN_POINT ( 'NONE',  ( 0.9789820196765993687, -0.04640813864221354085, -1.926104504880983725 ) ) ;
#141031=CARTESIAN_POINT ( 'NONE',  ( 5.453941704850034711, -0.7095916301838971485, 1.829088932523432964 ) ) ;
#141039=CARTESIAN_POINT ( 'NONE',  ( 5.067269747081383890, 1.798595138155817841, 1.025117745595036878 ) ) ;
#141042=CARTESIAN_POINT ( 'NONE',  ( 4.817139702178411476, 1.183121084409150425, -1.970709701559998805 ) ) ;
#141046=CARTESIAN_POINT ( 'NONE',  ( 0.8852319118969053102, 2.019148884293726631, -1.085135299617467020 ) ) ;
#141050=CARTESIAN_POINT ( 'NONE',  ( 4.382716955277085269, 1.733964400234957459, -0.8745241987923138005 ) ) ;
#141054=CARTESIAN_POINT ( 'NONE',  ( 6.381121926128928479, -1.751337275642101510, -0.7685668267764720341 ) ) ;
#141055=CARTESIAN_POINT ( 'NONE',  ( 6.827182134110228340, 0.006757161851634120239, 1.710856279483467191 ) ) ;
#141056=CARTESIAN_POINT ( 'NONE',  ( 5.278529876733943915, -0.4946281652532490969, -1.954780475499573900 ) ) ;
#141060=CARTESIAN_POINT ( 'NONE',  ( 1.148509085094330029, -1.646982989033857869, 1.287593708729701802 ) ) ;
#141061=CARTESIAN_POINT ( 'NONE',  ( 6.661408102931688724, 0.2994711133218473931, -1.744046391327475964 ) ) ;
#141062=CARTESIAN_POINT ( 'NONE',  ( 5.766250055133458119, 1.862018000461727052, -0.7743128548072516493 ) ) ;
#141064=CARTESIAN_POINT ( 'NONE',  ( 3.099882009726143917, -2.289598904869084350, 0.1129434519280565069 ) ) ;
#141065=CARTESIAN_POINT ( 'NONE',  ( 1.939017046771335240, 0.6676067653633214194, -1.607389671016548949 ) ) ;
#141067=CARTESIAN_POINT ( 'NONE',  ( 1.950155486560195772, 1.191851295230661467, 1.259505011191792923 ) ) ;
#141069=CARTESIAN_POINT ( 'NONE',  ( 1.890827768869116632, 0.1781016032055370568, 1.852494144255438346 ) ) ;
#141070=CARTESIAN_POINT ( 'NONE',  ( 2.137404458564879484, -0.1051889750803415707, -2.168730265314787076 ) ) ;
#141071=CARTESIAN_POINT ( 'NONE',  ( 3.362517798112668821, -1.944730434982215650, -0.5331690889110105580 ) ) ;
#141072=CARTESIAN_POINT ( 'NONE',  ( 4.000000000000002665, -2.278188019141646974E-13, -2.052068128417946280 ) ) ;
#141074=CARTESIAN_POINT ( 'NONE',  ( 0.7977241263109683400, -0.6962278615636787737, 1.796346399320443821 ) ) ;
#141076=CARTESIAN_POINT ( 'NONE',  ( 3.586370468055916305, 1.236567345028506182, 1.845233891176313756 ) ) ;
#141078=CARTESIAN_POINT ( 'NONE',  ( -0.2108831679770926115, 5.723481173670196043, -2.491210874135452613 ) ) ;
#141082=CARTESIAN_POINT ( 'NONE',  ( 6.275645185405086757, 0.3810096023663198661, -2.188332947720336819 ) ) ;
#141083=CARTESIAN_POINT ( 'NONE',  ( 4.721123852359588646, -1.751549048416237486, -0.8839179009662299080 ) ) ;
#141087=CARTESIAN_POINT ( 'NONE',  ( 5.290393965937395748, -2.244422280358076005, -0.2844362755431028567 ) ) ;
#141089=CARTESIAN_POINT ( 'NONE',  ( 2.611848684353266226, 0.5523815846302374544, -1.987258587729407999 ) ) ;
#141094=CARTESIAN_POINT ( 'NONE',  ( 4.991395955090764502, 1.385047395102714685, 1.257364466828891914 ) ) ;
#141095=CARTESIAN_POINT ( 'NONE',  ( 3.111645937125429029, 0.04567828748044086562, 1.733733899787115229 ) ) ;
#141096=CARTESIAN_POINT ( 'NONE',  ( 2.454330514505886018, -1.515118085899306521, -0.8562798468515414596 ) ) ;
#141097=CARTESIAN_POINT ( 'NONE',  ( 0.8203738007961014489, 1.359819376615223785, -1.845384199244608947 ) ) ;
#141098=CARTESIAN_POINT ( 'NONE',  ( 0.6752036787147744912, -2.078553970830565145, -0.7415856106591719454 ) ) ;
#141099=CARTESIAN_POINT ( 'NONE',  ( 4.862875367868015886, 0.2033134212856284595, -2.080814050062954390 ) ) ;
#141100=CARTESIAN_POINT ( 'NONE',  ( 5.859312505936116189, 1.912822604199882148, -0.3342364482464658115 ) ) ;
#141101=EDGE_CURVE ( 'NONE', #2638, #59934, #74845, .T. ) ;
#141105=CARTESIAN_POINT ( 'NONE',  ( 0.6158615555539399544, 0.1511424999406512648, 2.010826230049263863 ) ) ;
#141112=CARTESIAN_POINT ( 'NONE',  ( 3.984828715814022981, -0.1808549858164226476, -1.816707794649790708 ) ) ;
#141113=CARTESIAN_POINT ( 'NONE',  ( 1.641937377912294771, -1.598774535768614280, -1.521335986861327427 ) ) ;
#141118=CARTESIAN_POINT ( 'NONE',  ( 0.7033857886646873725, 1.779361102145039286, -0.9557781530431900263 ) ) ;
#141122=CARTESIAN_POINT ( 'NONE',  ( 2.483057756668010541, -0.005615179255674587061, 1.861131632832468963 ) ) ;
#141126=ORIENTED_EDGE ( 'NONE', *, *, #49103, .T. ) ;
#141129=CARTESIAN_POINT ( 'NONE',  ( 3.545350327189537687, -1.383302465072188792, -1.191577590537174158 ) ) ;
#141135=CARTESIAN_POINT ( 'NONE',  ( 0.4558326304775248139, 1.278721518017480685, 1.171137906463788347 ) ) ;
#141136=CARTESIAN_POINT ( 'NONE',  ( 5.384640740818634974, 1.621930891500168670, -0.8712783443201177480 ) ) ;
#141137=CARTESIAN_POINT ( 'NONE',  ( 4.969473931871945638, 0.2302171888925855225, -2.296178194122914018 ) ) ;
#141139=CARTESIAN_POINT ( 'NONE',  ( 6.573507624224045109, 2.070638407997299257, -0.6205318887850322929 ) ) ;
#141141=CARTESIAN_POINT ( 'NONE',  ( 5.325646502758397460, -1.669998024346308618, 1.579374382026963675 ) ) ;
#141143=CARTESIAN_POINT ( 'NONE',  ( 5.682452175617663137, -1.825344843996518529, -0.4084625512627630406 ) ) ;
#141147=CARTESIAN_POINT ( 'NONE',  ( 2.302860652515530848, -0.3306829512400177862, -1.883434002855538081 ) ) ;
#141150=CARTESIAN_POINT ( 'NONE',  ( 4.248781725523794073, 0.5872999373685274804, 2.127227798101683387 ) ) ;
#141151=CARTESIAN_POINT ( 'NONE',  ( 4.628176351164477786, 2.111873176223429738, 0.1524955421974716341 ) ) ;
#141153=CARTESIAN_POINT ( 'NONE',  ( 6.883263157960364254, 6.036844454314826081, 2.541088405340941492 ) ) ;
#141154=CARTESIAN_POINT ( 'NONE',  ( -0.2110808730066960626, 4.094899759311981136, -2.352064028521171135 ) ) ;
#141158=CARTESIAN_POINT ( 'NONE',  ( 2.538448204128932240, 1.088115672400795431, -2.034946615453626872 ) ) ;
#141159=CARTESIAN_POINT ( 'NONE',  ( 3.121486724888074882, 0.2905151309811822569, -1.940125473959073421 ) ) ;
#141160=CARTESIAN_POINT ( 'NONE',  ( 6.737180511075488987, -0.09540316190201691970, -2.060463472160603882 ) ) ;
#141164=CARTESIAN_POINT ( 'NONE',  ( 4.874232570624013050, -2.001857581374043349, -0.2420344392276354561 ) ) ;
#141168=CARTESIAN_POINT ( 'NONE',  ( 1.481551236908748237, -0.05589941666775917473, 2.170521761658677828 ) ) ;
#141172=CARTESIAN_POINT ( 'NONE',  ( 0.9661734561289528900, 1.013198095218909245, 1.794397040888571437 ) ) ;
#141178=CARTESIAN_POINT ( 'NONE',  ( 3.088426618631805010, -1.137173348016347063, 1.537276688398481861 ) ) ;
#141180=CARTESIAN_POINT ( 'NONE',  ( 4.821055670345097077, -0.08498437303107277130, 1.767940285534306488 ) ) ;
#141184=CARTESIAN_POINT ( 'NONE',  ( -0.08300117844089061059, -1.750507139949438296, 0.7787328797612643738 ) ) ;
#141186=CARTESIAN_POINT ( 'NONE',  ( 0.8364851226981102617, -1.151554295457988930, 1.720357586142134076 ) ) ;
#141188=CARTESIAN_POINT ( 'NONE',  ( 6.192256348250350761, -1.861847689568534081, -0.1814220289034565448 ) ) ;
#141189=CARTESIAN_POINT ( 'NONE',  ( 1.980809073483770000, -0.08854697198140694392, -1.823669195971427071 ) ) ;
#141190=CARTESIAN_POINT ( 'NONE',  ( 5.408869034151480903, 1.673104959687292448, -1.439203791633147267 ) ) ;
#141193=CARTESIAN_POINT ( 'NONE',  ( 3.191897189531978096, -1.383228714077057830, -1.530316362279722231 ) ) ;
#141197=CARTESIAN_POINT ( 'NONE',  ( 0.1811626231076196580, -0.1537715369321658587, -2.127283700313627346 ) ) ;
#141199=CARTESIAN_POINT ( 'NONE',  ( 5.318829906782316819, -1.502041817331278173, 1.425132596443792643 ) ) ;
#141201=CARTESIAN_POINT ( 'NONE',  ( 2.706508253401081809, -0.8245430293080566742, -1.998349536214229616 ) ) ;
#141203=CARTESIAN_POINT ( 'NONE',  ( 3.229170203573806130, 1.826861024573895653, 0.8614713780644381869 ) ) ;
#141204=CARTESIAN_POINT ( 'NONE',  ( 1.803102349535959714, -1.659081995624330563, 1.046767247423967095 ) ) ;
#141210=CARTESIAN_POINT ( 'NONE',  ( 0.8312679839070147292, -1.592664559859976237, -1.236796411087807801 ) ) ;
#141212=CARTESIAN_POINT ( 'NONE',  ( 6.585463931165095985, -0.9389328202267492873, 1.978239266594773671 ) ) ;
#141215=CARTESIAN_POINT ( 'NONE',  ( 6.082274476537278041, 0.9889857280602430967, 1.636697341158253272 ) ) ;
#141219=CARTESIAN_POINT ( 'NONE',  ( 2.829704019156009220, 0.7231233381281775285, -1.882481713119791067 ) ) ;
#141223=CARTESIAN_POINT ( 'NONE',  ( 6.176716277887216222, -1.639393978788429740, -0.5360894954027517478 ) ) ;
#141227=CARTESIAN_POINT ( 'NONE',  ( 4.657402308249613654, 0.4116239899518738810, -1.824517662812553009 ) ) ;
#141229=CARTESIAN_POINT ( 'NONE',  ( 1.428671948192638208, -1.316369429293560156, 1.597808059233512656 ) ) ;
#141233=CARTESIAN_POINT ( 'NONE',  ( 0.07017708175168728413, 0.6932349927748741036, 1.673895389460538397 ) ) ;
#141239=CARTESIAN_POINT ( 'NONE',  ( 1.627322669196319849, 0.1476378700930695564, -1.956383933670035713 ) ) ;
#141241=CARTESIAN_POINT ( 'NONE',  ( 4.886306726311728355, -0.6496138446146214607, -1.802220356481977204 ) ) ;
#141248=CARTESIAN_POINT ( 'NONE',  ( 3.397504326804317909, 1.702965868850464082, 1.331369057855802174 ) ) ;
#141251=CARTESIAN_POINT ( 'NONE',  ( 0.1762450972803020210, 2.096614079038420897, -0.3174041833761130360 ) ) ;
#141253=CARTESIAN_POINT ( 'NONE',  ( 4.594645031659345236, -0.4005623417570289280, -1.780931357837008733 ) ) ;
#141255=CARTESIAN_POINT ( 'NONE',  ( 1.089067603693228525, 1.740485041285372958, -0.9256802945506740210 ) ) ;
#141256=CARTESIAN_POINT ( 'NONE',  ( 3.884940529579200774, -1.786240503712609895, -0.6835825222790415934 ) ) ;
#141259=CARTESIAN_POINT ( 'NONE',  ( 4.773860271397749599, -1.931934984910467890, 0.3821518213343431669 ) ) ;
#141261=CARTESIAN_POINT ( 'NONE',  ( 6.462452672982783142, -1.777441430900746688, -0.7828909329169189135 ) ) ;
#141265=CARTESIAN_POINT ( 'NONE',  ( 6.293239850429793947, -0.1054838202379469042, -2.118119863012501991 ) ) ;
#141267=CARTESIAN_POINT ( 'NONE',  ( 3.809155001108742056, 1.613891119516493999, -1.025466636117925212 ) ) ;
#141271=CARTESIAN_POINT ( 'NONE',  ( 5.918613486546395741, -0.7266362437793117968, -1.877539736040201079 ) ) ;
#141273=CARTESIAN_POINT ( 'NONE',  ( 6.252569598636129378, 0.5776572744066664766, 1.731972519516040032 ) ) ;
#141274=CARTESIAN_POINT ( 'NONE',  ( 5.735564631760892595, 0.5807582108038509272, -1.931123567068816493 ) ) ;
#141276=CARTESIAN_POINT ( 'NONE',  ( 1.750525128138082254, -2.060206210462053988, -0.2049951091474821463 ) ) ;
#141285=PLANE ( 'NONE',  #213721 ) ;
#141287=CARTESIAN_POINT ( 'NONE',  ( 6.925078400183550364, 4.696033252921790968, 2.518291795588607052 ) ) ;
#141290=CARTESIAN_POINT ( 'NONE',  ( 4.869590383887318019, -0.2189826452120811340, -1.720196969245034513 ) ) ;
#141293=CARTESIAN_POINT ( 'NONE',  ( 2.219664259111033378, 0.3580842396277704176, -2.038906786875307020 ) ) ;
#141294=CARTESIAN_POINT ( 'NONE',  ( 3.146228450019908252, 0.9544266383219732752, 1.889993806685738464 ) ) ;
#141297=CARTESIAN_POINT ( 'NONE',  ( 1.797640638355556320, -1.422838571669628127, -1.361938172677351400 ) ) ;
#141300=CARTESIAN_POINT ( 'NONE',  ( 0.1582721923853447621, 1.907395734848855051, 0.1385995803297388196 ) ) ;
#141301=CARTESIAN_POINT ( 'NONE',  ( 3.838036126445078633, 2.281091060459582209, 0.2259633074802695485 ) ) ;
#141302=CARTESIAN_POINT ( 'NONE',  ( 1.664397423953474009, -1.292156093668932693, 1.290017532847971271 ) ) ;
#141306=CARTESIAN_POINT ( 'NONE',  ( 2.513933912945048199, -0.6273889547634775576, 1.913045067402745936 ) ) ;
#141307=CARTESIAN_POINT ( 'NONE',  ( 1.832786370036399326, -1.861117592713131819, -0.6203919267877275878 ) ) ;
#141310=CARTESIAN_POINT ( 'NONE',  ( 0.07516593201275456604, 0.0004601587237917924593, -2.044269526395313452 ) ) ;
#141311=CARTESIAN_POINT ( 'NONE',  ( 4.892568727727841349, 1.738426232616798295, -1.160983500135639890 ) ) ;
#141312=CARTESIAN_POINT ( 'NONE',  ( 3.203702280051218931, -1.767899805609447261, 0.08541964596707474211 ) ) ;
#141314=CARTESIAN_POINT ( 'NONE',  ( 0.3928598746986839974, 1.819701785225702473, -1.220828600141062203 ) ) ;
#141315=CARTESIAN_POINT ( 'NONE',  ( 5.454937174282652457, 0.3337844340769695606, -1.707832357695503234 ) ) ;
#141318=CARTESIAN_POINT ( 'NONE',  ( 5.977181698541591537, -2.287177818765488091, -0.2295778655121790968 ) ) ;
#141320=CARTESIAN_POINT ( 'NONE',  ( 5.676976676600826721, -0.7816020568793962120, -1.547713907698013092 ) ) ;
#141321=CARTESIAN_POINT ( 'NONE',  ( 6.021977204206338641, 2.140098014189107278, -0.3652067468529682226 ) ) ;
#141323=CARTESIAN_POINT ( 'NONE',  ( 0.2338150414605598693, 0.6575980258751003005, -2.012739700429423628 ) ) ;
#141324=CARTESIAN_POINT ( 'NONE',  ( 3.281250000000002665, 0.7852924748301588487, 1.895863743164012849 ) ) ;
#141325=CARTESIAN_POINT ( 'NONE',  ( 6.827182134110231004, 7.052068023338082803, 2.687205202894725975 ) ) ;
#141326=CARTESIAN_POINT ( 'NONE',  ( 4.137660063496669594, -1.327783069688622586, -1.395926297547624984 ) ) ;
#141328=CARTESIAN_POINT ( 'NONE',  ( 1.471644961476214597, -1.907451222982279093, -1.138109381883713578 ) ) ;
#141334=CARTESIAN_POINT ( 'NONE',  ( 2.631719755377628811, -0.2151721393647449687, 2.210840341435269973 ) ) ;
#141339=CARTESIAN_POINT ( 'NONE',  ( 0.5982800022500452952, -0.2930678230431381648, 1.994870242743536304 ) ) ;
#141341=CARTESIAN_POINT ( 'NONE',  ( 6.848098694195379643, -0.8844518680410964340, 1.861345814548149624 ) ) ;
#141345=CARTESIAN_POINT ( 'NONE',  ( 1.264531387369687065, -1.596916444607907382, -0.7631234423778727738 ) ) ;
#141346=CARTESIAN_POINT ( 'NONE',  ( 0.7037502660087076034, 1.864169469917423161, 0.7691187473759173443 ) ) ;
#141347=CARTESIAN_POINT ( 'NONE',  ( 5.249435226766168583, 1.738107782858036687, -0.09287461536438243459 ) ) ;
#141348=CARTESIAN_POINT ( 'NONE',  ( 3.685359659257981146, 1.661040094275951340, 1.580089079255690088 ) ) ;
#141350=CARTESIAN_POINT ( 'NONE',  ( 1.816098422328410900, 1.717562825535594140, 0.6636192267199735317 ) ) ;
#141354=CARTESIAN_POINT ( 'NONE',  ( 3.241029684393876842, -1.610631872634618933, 0.8593927405577477252 ) ) ;
#141355=CARTESIAN_POINT ( 'NONE',  ( 4.324842380567116784, 0.8596320953860696612, -1.824118450417112847 ) ) ;
#141357=CARTESIAN_POINT ( 'NONE',  ( 2.589068414660402606, -0.3862909535316555454, -2.229145898733439157 ) ) ;
#141359=CARTESIAN_POINT ( 'NONE',  ( 5.403390757083595730, 1.719820611593615656, 1.215146281773227921 ) ) ;
#141360=B_SPLINE_CURVE_WITH_KNOTS ( 'NONE', 3,
 ( #54302, #169106, #3384, #38051, #20703, #72665, #150750, #6586, #84661, #2311 ),
 .UNSPECIFIED., .F., .F.,
 ( 4, 1, 1, 1, 1, 1, 1, 4 ),
 ( 0.000000000000000000, 0.09489293188423997272, 0.1878783894049059211, 0.2584743716234961797, 0.3617987437640678983, 0.5212292184658617877, 0.7337638816394396191, 1.000000000000000000 ),
 .UNSPECIFIED. ) ;
#141362=CARTESIAN_POINT ( 'NONE',  ( 2.383334800519558705, -0.002349189141126820958, 2.070544812199434315 ) ) ;
#141365=CARTESIAN_POINT ( 'NONE',  ( 5.162787349232583090, 0.6159572760087470567, 2.029033592890214788 ) ) ;
#141367=CARTESIAN_POINT ( 'NONE',  ( 1.488762753728092969, -0.2822029396061729867, -1.905608977972670370 ) ) ;
#141372=CIRCLE ( 'NONE', #207028, 0.04999999999999883010 ) ;
#141374=CARTESIAN_POINT ( 'NONE',  ( -0.1047794747230318818, -2.156939676625940994, -0.5310815526072456549 ) ) ;
#141375=CARTESIAN_POINT ( 'NONE',  ( 2.239418434904976607, -1.881632620311970649, 0.9459126739295388164 ) ) ;
#141378=CARTESIAN_POINT ( 'NONE',  ( 6.789920448004552078, -1.215336557376142101, -1.409407482083424590 ) ) ;
#141385=CARTESIAN_POINT ( 'NONE',  ( 0.3695850531008069706, -1.794773754367712693, -1.129184308951653781 ) ) ;
#141388=CARTESIAN_POINT ( 'NONE',  ( 3.332423539472821439, -1.170687260143790320, 1.574129132985650825 ) ) ;
#141389=CARTESIAN_POINT ( 'NONE',  ( 0.5499753625364013354, 0.6768306982547143136, -2.053065283773393368 ) ) ;
#141393=CARTESIAN_POINT ( 'NONE',  ( 2.483973769465233961, -0.2969572910719043279, -1.714626640263767543 ) ) ;
#141396=CARTESIAN_POINT ( 'NONE',  ( 1.862657450031137474, -0.6818942500997280387, 1.897406292459068222 ) ) ;
#141397=CARTESIAN_POINT ( 'NONE',  ( 6.825078400183550720, 7.629137130509051623, 2.844348168701658075 ) ) ;
#141399=CARTESIAN_POINT ( 'NONE',  ( 2.641432621735483544, -1.459803026827242611, -1.325177341282377741 ) ) ;
#141401=CARTESIAN_POINT ( 'NONE',  ( 5.343983030329363615, -1.218012673290536974, -1.474316871017400166 ) ) ;
#141403=ADVANCED_FACE ( 'NONE', ( #155893 ), #108319, .F. ) ;
#141407=CARTESIAN_POINT ( 'NONE',  ( 2.754561962923445684, 2.004688795240500365, 0.2448751400806712664 ) ) ;
#141410=CARTESIAN_POINT ( 'NONE',  ( 5.192513718098597408, -2.289403112372697890, -0.2887273360754892826 ) ) ;
#141411=CARTESIAN_POINT ( 'NONE',  ( 6.602011099637477010, 0.7519813002578833450, -1.812223124677159181 ) ) ;
#141412=CARTESIAN_POINT ( 'NONE',  ( 3.397265449134680981, -1.732261247800225279, 0.9206733083975682241 ) ) ;
#141414=CARTESIAN_POINT ( 'NONE',  ( 0.3697678102792775756, -0.2496098759999023087, -2.000856779379902139 ) ) ;
#141416=CARTESIAN_POINT ( 'NONE',  ( 2.905574018005254722, -2.039320757748352086, 0.5691538075108558692 ) ) ;
#141419=CARTESIAN_POINT ( 'NONE',  ( 1.939159035295745737, 0.7054217538491478479, -1.700835786604155242 ) ) ;
#141421=CARTESIAN_POINT ( 'NONE',  ( 3.098842478760281516, 1.825076540557273974, 0.8578426345753201732 ) ) ;
#141424=CARTESIAN_POINT ( 'NONE',  ( 2.619513681940002670, 1.793805257907291395, 1.130712135851599465 ) ) ;
#141428=CARTESIAN_POINT ( 'NONE',  ( 4.446593522994434444, 0.5459629501111874506, 1.987092823586662504 ) ) ;
#141430=CARTESIAN_POINT ( 'NONE',  ( 1.786409390178132162, 1.601450680722369846, -0.9084932335857234253 ) ) ;
#141436=CARTESIAN_POINT ( 'NONE',  ( 0.8036966383840878914, 1.806304194667744500, 1.267646993260997723 ) ) ;
#141437=CARTESIAN_POINT ( 'NONE',  ( 3.181238891614282416, -0.1630793868099291999, -2.256562113509274159 ) ) ;
#141439=CARTESIAN_POINT ( 'NONE',  ( 3.445387325821075652, -1.671857736322950094, 0.6981543005735133534 ) ) ;
#141440=CARTESIAN_POINT ( 'NONE',  ( 3.292102688380782460, -0.7811219226253396375, -1.749442990535796438 ) ) ;
#141441=CARTESIAN_POINT ( 'NONE',  ( 4.352052382902608763, -0.7952921280917917279, 1.911720769834825973 ) ) ;
#141443=CARTESIAN_POINT ( 'NONE',  ( 2.993000350225515138, 1.691612214138412007, -1.012252976823005968 ) ) ;
#141444=CARTESIAN_POINT ( 'NONE',  ( 1.395397119253296569, 1.457039974399224391, 1.260252556074402897 ) ) ;
#141445=CARTESIAN_POINT ( 'NONE',  ( 4.030043484472041193, 1.001115284758803625, -1.580040089582811280 ) ) ;
#141446=CARTESIAN_POINT ( 'NONE',  ( 2.051827946393524726, -1.855052535695273841, -1.372493790568436012 ) ) ;
#141448=CARTESIAN_POINT ( 'NONE',  ( 3.719077791506773423, -1.640430839875358204, -0.8789487387581331745 ) ) ;
#141453=CARTESIAN_POINT ( 'NONE',  ( 0.8738170914556376845, 2.029154634757854847, -0.5636997952245518251 ) ) ;
#141456=CARTESIAN_POINT ( 'NONE',  ( 6.766866382711775429, -1.973269837180600561, -0.8828958408187634888 ) ) ;
#141457=CARTESIAN_POINT ( 'NONE',  ( 2.180079139336263516, 2.078761533942363737, -0.4183221158333137457 ) ) ;
#141458=CARTESIAN_POINT ( 'NONE',  ( 6.375650237155517708, 0.3431015828706286408, -1.990142738341105000 ) ) ;
#141462=CARTESIAN_POINT ( 'NONE',  ( 0.9487563388480976245, 0.6265645459165304354, 2.068816658077163861 ) ) ;
#141466=CARTESIAN_POINT ( 'NONE',  ( 4.469935555517978720, -0.9463019959239076240, 1.780667052345537238 ) ) ;
#141470=CARTESIAN_POINT ( 'NONE',  ( 0.7610528644104715967, -1.636749228899089470, 1.562301092707372607 ) ) ;
#141474=CARTESIAN_POINT ( 'NONE',  ( 6.275017575846199236, 1.753023089329442064, -0.9963169848806670004 ) ) ;
#141478=CARTESIAN_POINT ( 'NONE',  ( 2.912419603134624779, 1.249142870932816507, -1.189721958963300130 ) ) ;
#141482=CARTESIAN_POINT ( 'NONE',  ( 0.8250501123308005003, -1.682963436248402056, 0.5476568922856797084 ) ) ;
#141484=CARTESIAN_POINT ( 'NONE',  ( 2.315091943819780340, 1.615584347832084600, -1.200805960377361981 ) ) ;
#141486=CARTESIAN_POINT ( 'NONE',  ( 4.173040645679537697, -2.057929556117383374, -0.7971749352265260491 ) ) ;
#141490=CARTESIAN_POINT ( 'NONE',  ( 4.020270485675044192, -2.114722421624544157, 0.1573160286183969692 ) ) ;
#141491=CARTESIAN_POINT ( 'NONE',  ( 2.495720449669074803, -1.994069261235394741, 0.2986488809556055446 ) ) ;
#141492=CARTESIAN_POINT ( 'NONE',  ( 3.128980605277735361, 1.639808012139221116, 0.7702280095687010775 ) ) ;
#141496=CARTESIAN_POINT ( 'NONE',  ( 0.4615142869485132637, 1.850934062480696252, -0.2700578556205368574 ) ) ;
#141499=CARTESIAN_POINT ( 'NONE',  ( 5.988856447087389512, -0.2726756491404982441, -1.805090154579996442 ) ) ;
#141501=CARTESIAN_POINT ( 'NONE',  ( 2.659291035590090058, 1.817528298045675061, -0.6055613653334031010 ) ) ;
#141508=CARTESIAN_POINT ( 'NONE',  ( 3.023802379225454473, -0.4096935937694180518, 2.080477853870852378 ) ) ;
#141512=CARTESIAN_POINT ( 'NONE',  ( 4.569576162043214929, 1.912950159424832375, -0.4759120794774750474 ) ) ;
#141513=CARTESIAN_POINT ( 'NONE',  ( -0.1579526903544171412, -1.242116785587377592, -1.585096312452577205 ) ) ;
#141514=EDGE_LOOP ( 'NONE', ( #198758, #26358, #161854, #186471 ) ) ;
#141515=CARTESIAN_POINT ( 'NONE',  ( 0.1756132116073009508, 1.572246328413629435, 1.418195661691145304 ) ) ;
#141517=CARTESIAN_POINT ( 'NONE',  ( 1.451716722110554025, 1.566445173006292935, 1.353826630019476562 ) ) ;
#141518=CARTESIAN_POINT ( 'NONE',  ( 2.202979905913711178, -0.4252542987780962291, 1.894666818490578164 ) ) ;
#141519=VERTEX_POINT ( 'NONE', #199011 ) ;
#141522=CARTESIAN_POINT ( 'NONE',  ( 3.275413508211636238, 1.326730841477074208, 1.615706224610208519 ) ) ;
#141525=CARTESIAN_POINT ( 'NONE',  ( 0.7327119416217167114, 1.673282569690562882, 0.6944263290599298477 ) ) ;
#141527=CARTESIAN_POINT ( 'NONE',  ( 5.408869034151480903, 1.673104959687292448, -1.439203791633147267 ) ) ;
#141529=CARTESIAN_POINT ( 'NONE',  ( 3.716033540554028125, -2.174548934981130444, 0.3748234698989146296 ) ) ;
#141531=CARTESIAN_POINT ( 'NONE',  ( 2.561071438676546741, -1.588783617390630898, 1.063917234122884858 ) ) ;
#141533=CARTESIAN_POINT ( 'NONE',  ( 5.353992430378140099, -0.7485205528568984468, 1.930488744064068785 ) ) ;
#141535=CARTESIAN_POINT ( 'NONE',  ( 3.309602206082487008, -0.4233974974612622066, 2.119663826602156131 ) ) ;
#141536=CARTESIAN_POINT ( 'NONE',  ( 4.370767597569780172, -0.0006098066561242150270, -2.191739723162715592 ) ) ;
#141546=CARTESIAN_POINT ( 'NONE',  ( 6.051642586050198780, 1.563818258945088191, 1.356687170345116211 ) ) ;
#141547=CARTESIAN_POINT ( 'NONE',  ( 4.020081831311307141, -0.9914672019816127557, -1.651657144357060014 ) ) ;
#141548=CARTESIAN_POINT ( 'NONE',  ( 6.485961931490698440, -2.116758087377061504, 0.05204923864161013075 ) ) ;
#141551=CARTESIAN_POINT ( 'NONE',  ( 5.453942691717160507, -0.7125396638749655898, 1.836196350841996949 ) ) ;
#141552=CARTESIAN_POINT ( 'NONE',  ( 6.667932745306283771, -1.416340830354723135, 1.803254352984103859 ) ) ;
#141553=CARTESIAN_POINT ( 'NONE',  ( 4.740742070742828496, 0.3150700179065483719, 1.798135100120237473 ) ) ;
#141560=CARTESIAN_POINT ( 'NONE',  ( 2.524749765808989466, -1.717266272480859834, 0.6646640004178904215 ) ) ;
#141561=CARTESIAN_POINT ( 'NONE',  ( 6.187749739576326569, 1.925281575520617849, -0.5883678985393098193 ) ) ;
#141562=CARTESIAN_POINT ( 'NONE',  ( 1.019433853822170777, 2.295598214472119203, -0.1149376033552674814 ) ) ;
#141563=CARTESIAN_POINT ( 'NONE',  ( 6.491066726104213203, 0.1889763263339637456, 1.952597990788194959 ) ) ;
#141567=CARTESIAN_POINT ( 'NONE',  ( 0.2915762745691782287, -1.893489616766583339, 0.8377075429084477332 ) ) ;
#141569=CARTESIAN_POINT ( 'NONE',  ( 2.401997865216979111, -0.8028288615537516604, -1.930668023334235484 ) ) ;
#141570=CARTESIAN_POINT ( 'NONE',  ( 1.727212824277712944, -1.762453432929488528, 0.6273722324065673650 ) ) ;
#141571=CARTESIAN_POINT ( 'NONE',  ( 1.827499746633702182, -1.427720486614523221, 1.423741782973136694 ) ) ;
#141574=CARTESIAN_POINT ( 'NONE',  ( 1.874151978141885833, -0.08570891532005876778, -1.738468184182701881 ) ) ;
#141578=CARTESIAN_POINT ( 'NONE',  ( 2.525662786804376836, -0.9926222177696201188, -1.410421675411769993 ) ) ;
#141579=CARTESIAN_POINT ( 'NONE',  ( 2.331793494658142230, 1.030094174309360344, -1.934364310732391345 ) ) ;
#141580=CARTESIAN_POINT ( 'NONE',  ( 5.725267921653402148, -0.05769419298589681389, 2.206291853148376170 ) ) ;
#141583=CARTESIAN_POINT ( 'NONE',  ( 2.483468006519026439, -0.003752633953101049049, 2.171239807183155790 ) ) ;
#141584=CARTESIAN_POINT ( 'NONE',  ( 0.8733498553583609603, 1.760202786292342170, -0.4843115980177821744 ) ) ;
#141585=CARTESIAN_POINT ( 'NONE',  ( 3.784452290478927505, -0.6679156082517538895, -2.009268603764336358 ) ) ;
#141588=CARTESIAN_POINT ( 'NONE',  ( 3.702894494004336678, 1.966553232070525237, 1.177740060511106135 ) ) ;
#141592=CARTESIAN_POINT ( 'NONE',  ( 5.461676247742112800, -1.750072316323016963, -1.367929348606132800 ) ) ;
#141598=CARTESIAN_POINT ( 'NONE',  ( 4.061172775696818782, -1.158689426361030561, 1.650081270007992318 ) ) ;
#141600=CARTESIAN_POINT ( 'NONE',  ( 2.782143433959896051, -1.183836405090990640, -1.688839807681275174 ) ) ;
#141605=CARTESIAN_POINT ( 'NONE',  ( 6.685463922536254877, -0.9407050535897142352, 1.977304495687677521 ) ) ;
#141606=CARTESIAN_POINT ( 'NONE',  ( 3.182267690267494231, 1.591318367894577701, 1.238320962759748234 ) ) ;
#141607=CARTESIAN_POINT ( 'NONE',  ( 2.243484787601189634, 1.840893492186860492, 0.04347913094143729396 ) ) ;
#141610=CARTESIAN_POINT ( 'NONE',  ( 6.616225513087798049, -0.8637638766970030524, -1.608286988965562214 ) ) ;
#141612=CARTESIAN_POINT ( 'NONE',  ( 5.735331106285326719, -2.048134886816056266, 0.9616036564972543221 ) ) ;
#141613=CARTESIAN_POINT ( 'NONE',  ( 2.209725257209711469, -0.4604840958662699268, 2.054942820982478935 ) ) ;
#141623=CARTESIAN_POINT ( 'NONE',  ( 3.779691724966814270, 0.2693221142107836696, -2.204936161957889329 ) ) ;
#141624=CARTESIAN_POINT ( 'NONE',  ( 0.1533209562146371774, -1.769702838771534559, 1.318327933512997152 ) ) ;
#141628=CARTESIAN_POINT ( 'NONE',  ( 4.791432466842788784, -1.794507165602466037, 0.7932701521168731285 ) ) ;
#141631=( BOUNDED_SURFACE ( )  B_SPLINE_SURFACE ( 3, 3, ( 
 ( #198177, #49810, #115937, #2089, #135348, #185120, #134295, #68163, #83360, #166766, #50879 ),
 ( #133227, #3158, #199232, #168886, #117002, #20490, #119138, #18361, #200302, #51954, #184063 ),
 ( #201362, #167826, #19425, #85504, #151591, #69230, #36745, #8515, #104980, #74596, #155849 ),
 ( #25825, #188332, #123442, #189404, #124498, #71363, #39972, #169949, #157995, #89805, #122375 ),
 ( #107155, #171020, #22617, #137479, #88726, #103903, #187268, #38894, #203493, #106079, #121292 ),
 ( #154784, #75660, #6369, #9584, #72438, #141767, #55146, #41046, #138539, #140700, #190457 ),
 ( #204563, #56211, #172102, #23695, #7436, #173180, #73517, #24760, #139619, #205642, #186192 ) ),
 .UNSPECIFIED., .T., .F., .T. ) 
 B_SPLINE_SURFACE_WITH_KNOTS ( ( 4, 3, 4 ),
 ( 4, 1, 1, 1, 1, 1, 1, 1, 4 ),
 ( 0.000000000000000000, 0.5000000000000000000, 1.000000000000000000 ),
 ( 0.000000000000000000, 0.2257091236145174484, 0.3979912149639216468, 0.5260416812932605657, 0.6190739408849097458, 0.6862087210430605211, 0.7361363507675404705, 0.7768852254246026989, 0.9999999999999998890 ),
 .UNSPECIFIED. ) 
 GEOMETRIC_REPRESENTATION_ITEM ( )  RATIONAL_B_SPLINE_SURFACE ( (
 ( 1.000000000000000222, 1.000000000000000222, 1.000000000000000000, 1.000000000000000000, 1.000000000000000222, 1.000000000000000000, 1.000000000000000000, 1.000000000000000000, 1.000000000000000222, 1.000000000000000000, 1.000000000000000000),
 ( 0.3333333333333334259, 0.3333333333333334259, 0.3333333333333333148, 0.3333333333333333703, 0.3333333333333334259, 0.3333333333333333703, 0.3333333333333333703, 0.3333333333333334259, 0.3333333333333333703, 0.3333333333333333703, 0.3333333333333333703),
 ( 0.3333333333333334259, 0.3333333333333334259, 0.3333333333333333148, 0.3333333333333333703, 0.3333333333333334259, 0.3333333333333333703, 0.3333333333333333703, 0.3333333333333334259, 0.3333333333333333703, 0.3333333333333333703, 0.3333333333333333703),
 ( 1.000000000000000222, 1.000000000000000222, 1.000000000000000000, 1.000000000000000000, 1.000000000000000222, 1.000000000000000000, 1.000000000000000000, 1.000000000000000000, 1.000000000000000222, 1.000000000000000000, 1.000000000000000000),
 ( 0.3333333333333334259, 0.3333333333333334259, 0.3333333333333333148, 0.3333333333333333703, 0.3333333333333334259, 0.3333333333333333703, 0.3333333333333333703, 0.3333333333333334259, 0.3333333333333333703, 0.3333333333333333703, 0.3333333333333333703),
 ( 0.3333333333333334259, 0.3333333333333334259, 0.3333333333333333148, 0.3333333333333333703, 0.3333333333333334259, 0.3333333333333333703, 0.3333333333333333703, 0.3333333333333334259, 0.3333333333333333703, 0.3333333333333333703, 0.3333333333333333703),
 ( 1.000000000000000222, 1.000000000000000222, 1.000000000000000000, 1.000000000000000000, 1.000000000000000222, 1.000000000000000000, 1.000000000000000000, 1.000000000000000000, 1.000000000000000222, 1.000000000000000000, 1.000000000000000000) ) ) 
 REPRESENTATION_ITEM ( '' )  SURFACE ( )  );
#141636=CARTESIAN_POINT ( 'NONE',  ( 3.867525618572264623, -1.764951123045129577, -1.175235903013646332 ) ) ;
#141638=CARTESIAN_POINT ( 'NONE',  ( 5.207972885698374022, -2.151664816535401314, 0.2080130470862306957 ) ) ;
#141639=CARTESIAN_POINT ( 'NONE',  ( 3.720104550828434942, 1.749555917645674530, 0.5740644926693627692 ) ) ;
#141640=CARTESIAN_POINT ( 'NONE',  ( 5.014861385384292269, 0.1531656238677771009, 2.010801456750747285 ) ) ;
#141643=CARTESIAN_POINT ( 'NONE',  ( 6.615217694991038400, -1.686041314625020160, 0.4309386324203681728 ) ) ;
#141644=CARTESIAN_POINT ( 'NONE',  ( 6.827182134110200806, 7.053609659044731472, 2.309100207511079805 ) ) ;
#141647=CARTESIAN_POINT ( 'NONE',  ( 3.625982885822197410, -1.285997354380935098, -1.737435825693343094 ) ) ;
#141648=CARTESIAN_POINT ( 'NONE',  ( 6.046249930811113060, 1.863882344683247094, -0.7690052245405626374 ) ) ;
#141650=CARTESIAN_POINT ( 'NONE',  ( 3.204151765443470357, -2.159293047372488950, 0.1044485798024074874 ) ) ;
#141651=CARTESIAN_POINT ( 'NONE',  ( 3.339098322719173062, -1.740117145613935268, 0.9263661929081908886 ) ) ;
#141653=CARTESIAN_POINT ( 'NONE',  ( 1.149971759812302263, -1.820915985741960785, -1.417348977311111202 ) ) ;
#141654=CARTESIAN_POINT ( 'NONE',  ( 2.565760370094140264, 2.021647365152558606, -0.3987750144259157858 ) ) ;
#141655=CARTESIAN_POINT ( 'NONE',  ( 5.126486101458046285, 0.1468865524030492364, 1.936578770319798748 ) ) ;
#141665=CARTESIAN_POINT ( 'NONE',  ( 2.591098708763440062, -0.3764507303484417311, -2.174265822884546395 ) ) ;
#141667=CARTESIAN_POINT ( 'NONE',  ( 6.684431423333510480, 1.132142624513672091, -1.601896353945003071 ) ) ;
#141668=CARTESIAN_POINT ( 'NONE',  ( -0.02900071798685524560, 0.6937575422599016051, -2.255700163050919471 ) ) ;
#141671=CARTESIAN_POINT ( 'NONE',  ( 0.07479286986302942364, 7.629137130509078268, -2.455503679634089220 ) ) ;
#141672=CARTESIAN_POINT ( 'NONE',  ( 5.683513393433289096, -0.8240744568873883402, 1.646495476055845231 ) ) ;
#141674=CARTESIAN_POINT ( 'NONE',  ( 2.307559741017367383, -0.4527674059561050401, 2.010364544233154138 ) ) ;
#141681=CARTESIAN_POINT ( 'NONE',  ( 0.7958619820324459582, -0.7424864502722209325, 1.922671381412993652 ) ) ;
#141683=CARTESIAN_POINT ( 'NONE',  ( 1.679899622522099012, -1.030144609347281026, -1.549723197825584764 ) ) ;
#141684=CARTESIAN_POINT ( 'NONE',  ( 5.214338956685347526, 1.703448749313410282, 0.6994016148276983591 ) ) ;
#141690=CARTESIAN_POINT ( 'NONE',  ( 5.022202109028018668, -1.178465353167540197, -1.865713892744431446 ) ) ;
#141691=CARTESIAN_POINT ( 'NONE',  ( 0.4214394802095830506, -0.1064560406111268731, 2.159113264384164399 ) ) ;
#141694=CARTESIAN_POINT ( 'NONE',  ( -0.1933232215488022709, -0.4202133615931051835, -1.872389726556406897 ) ) ;
#141695=CARTESIAN_POINT ( 'NONE',  ( -0.2058462039469660110, -0.8663896114125648751, -1.819200108291472606 ) ) ;
#141699=CARTESIAN_POINT ( 'NONE',  ( 5.830699381415811899, 1.280921311228696347, -1.420062396151056117 ) ) ;
#141701=EDGE_CURVE ( 'NONE', #26543, #5628, #195896, .T. ) ;
#141702=CARTESIAN_POINT ( 'NONE',  ( 0.7955152940811484052, -0.6771210053572243037, 1.743984199989514927 ) ) ;
#141703=CARTESIAN_POINT ( 'NONE',  ( 2.167204200501818612, 1.841733140229084853, -0.8216742516050157263 ) ) ;
#141705=CARTESIAN_POINT ( 'NONE',  ( 4.283879487498391647, 1.375451533845202245, 1.594966088981208729 ) ) ;
#141710=CARTESIAN_POINT ( 'NONE',  ( 3.902606965841335818, -1.998407076283228223, -0.2920856897847978195 ) ) ;
#141713=CARTESIAN_POINT ( 'NONE',  ( 4.077527805175058973, 2.036875575534887961, -0.7240464584713502960 ) ) ;
#141719=CARTESIAN_POINT ( 'NONE',  ( 1.785821596895339702, -2.044763721651895239, 0.7304308730638265912 ) ) ;
#141722=CARTESIAN_POINT ( 'NONE',  ( 0.8020088176248600931, 1.394402496181508466, -1.202495849378336423 ) ) ;
#141725=CARTESIAN_POINT ( 'NONE',  ( 2.243918346939121733, 2.191141468336772036, 0.05030144379260945153 ) ) ;
#141727=CARTESIAN_POINT ( 'NONE',  ( 3.292113192954935208, -0.9186832275986864804, 2.067785417532372438 ) ) ;
#141733=CARTESIAN_POINT ( 'NONE',  ( 4.868267778354250730, -1.156333057219432581, 1.339767963349105528 ) ) ;
#141736=CARTESIAN_POINT ( 'NONE',  ( 0.4113322892924773377, 1.832542443981843405, 1.037592781499405259 ) ) ;
#141739=CARTESIAN_POINT ( 'NONE',  ( 0.6956774629466413451, -1.390297546174504850, -1.395334862655448260 ) ) ;
#141744=CARTESIAN_POINT ( 'NONE',  ( 4.487079325084206260, 1.670935625628103605, -0.8411387520786616223 ) ) ;
#141745=CARTESIAN_POINT ( 'NONE',  ( 4.030184149050713316, 1.145922430192683805, 1.723988044715177859 ) ) ;
#141754=CARTESIAN_POINT ( 'NONE',  ( 4.070719198475009293, 1.388998261151509039, -1.385754695631277844 ) ) ;
#141755=CARTESIAN_POINT ( 'NONE',  ( 1.757185253014027282, -2.006138798620077157, -0.2004061740628823030 ) ) ;
#141756=CARTESIAN_POINT ( 'NONE',  ( -0.1104750535120025967, -0.004616138082884357029, -2.103378236956429337 ) ) ;
#141758=CARTESIAN_POINT ( 'NONE',  ( 0.7373108528737730705, -1.318359053027039263, -1.327247110734230962 ) ) ;
#141760=CARTESIAN_POINT ( 'NONE',  ( 3.498294685330126441, -0.9886941555459362041, 1.753605845479579095 ) ) ;
#141762=CARTESIAN_POINT ( 'NONE',  ( 3.181382749799996468, 1.670748044588391990, 1.300414933884207480 ) ) ;
#141763=CARTESIAN_POINT ( 'NONE',  ( 6.825078400183572036, 7.051914997414900022, 2.742498282622223726 ) ) ;
#141764=CARTESIAN_POINT ( 'NONE',  ( 4.352052382902608763, -0.7952921280917917279, 1.911720769834825973 ) ) ;
#141766=CARTESIAN_POINT ( 'NONE',  ( 0.6266517258138035729, 0.1575598857218879489, 2.084883927750030175 ) ) ;
#141767=CARTESIAN_POINT ( 'NONE',  ( 6.620655732516615544, 2.958939621373418483, 2.526443930770333246 ) ) ;
#141768=CARTESIAN_POINT ( 'NONE',  ( 5.122008332510333162, -0.9777984688263160473, -1.541441239866998103 ) ) ;
#141776=CARTESIAN_POINT ( 'NONE',  ( -0.09351100681491937572, -0.3904691765420374439, -1.774915231904458990 ) ) ;
#141782=ORIENTED_EDGE ( 'NONE', *, *, #187807, .F. ) ;
#141784=PRODUCT_DEFINITION ( 'UNKNOWN', '', #180335, #115456 ) ;
#141787=CARTESIAN_POINT ( 'NONE',  ( 5.114861317887108072, 0.1511565883688982259, 2.010826320608386730 ) ) ;
#141790=SURFACE_SIDE_STYLE ('',( #193680 ) ) ;
#141791=CARTESIAN_POINT ( 'NONE',  ( -0.1405533004718312329, 2.055874972810427526, -2.136773944524199109 ) ) ;
#141794=CARTESIAN_POINT ( 'NONE',  ( 2.553506168856953806, 1.519147476331883517, 1.253303911792477132 ) ) ;
#141795=CARTESIAN_POINT ( 'NONE',  ( 3.093375225471244772, -0.3905761854139707667, 1.978056131710544063 ) ) ;
#141797=CARTESIAN_POINT ( 'NONE',  ( 6.727182134110176293, 6.032839922080010631, 2.883943260000087605 ) ) ;
#141798=CARTESIAN_POINT ( 'NONE',  ( 4.048915112334880106, -1.821525731582713359, -1.218098874207810933 ) ) ;
#141800=CARTESIAN_POINT ( 'NONE',  ( 2.414956338186133422, 1.719780681555121982, 0.8681123839546500687 ) ) ;
#141803=CARTESIAN_POINT ( 'NONE',  ( 0.2333540202161610289, 7.629137130509112907, -2.645727818377396900 ) ) ;
#141812=CARTESIAN_POINT ( 'NONE',  ( 5.548353751603532835, -1.447698842669535413, 1.137588655622793876 ) ) ;
#141813=CARTESIAN_POINT ( 'NONE',  ( 2.930340344496225935, -0.9942814366015439997, -1.750357268347104256 ) ) ;
#141814=CARTESIAN_POINT ( 'NONE',  ( 4.499567255430725332, 2.252980053716880704, 0.4539551632626090405 ) ) ;
#141815=CARTESIAN_POINT ( 'NONE',  ( -0.02919842301646497981, 7.629137130509056952, -2.673797582091000269 ) ) ;
#141816=CARTESIAN_POINT ( 'NONE',  ( 3.766312297878508630, -0.7504043340197141809, -1.703115836376113634 ) ) ;
#141823=CARTESIAN_POINT ( 'NONE',  ( 6.075741423153157683, -1.117747424998961403, 1.766673535877111290 ) ) ;
#141828=CARTESIAN_POINT ( 'NONE',  ( 6.287718881003963034, 1.195215413365672275, 1.243919913892058693 ) ) ;
#141830=CARTESIAN_POINT ( 'NONE',  ( 1.195528834012358210, 1.529115512818737699, 0.8178816217611245554 ) ) ;
#141833=CARTESIAN_POINT ( 'NONE',  ( 5.366168305121062687, -2.161276524852562275, 0.2057630808787509757 ) ) ;
#141834=CARTESIAN_POINT ( 'NONE',  ( 4.072732355924274295, -1.704239406772959153, -0.6552279023967976235 ) ) ;
#141835=CARTESIAN_POINT ( 'NONE',  ( 2.201936455694650796, 0.7555380192853027310, -1.810630540845730385 ) ) ;
#141840=CARTESIAN_POINT ( 'NONE',  ( 2.209781436637091367, 1.640924847721588975, 1.343087772177023131 ) ) ;
#141844=CARTESIAN_POINT ( 'NONE',  ( 1.164989683304976875, 1.570165760251106990, -1.349419213858449318 ) ) ;
#141847=CARTESIAN_POINT ( 'NONE',  ( 3.791809789012908549, 2.091298394358314550, -0.7490737107957652352 ) ) ;
#141849=CARTESIAN_POINT ( 'NONE',  ( 0.5285108043569552994, -1.967359331218739626, 1.188758619093014168 ) ) ;
#141851=CARTESIAN_POINT ( 'NONE',  ( 0.3562053913853078790, -1.961198556353323186, -0.05404869553313899899 ) ) ;
#141854=CARTESIAN_POINT ( 'NONE',  ( 6.480030769895370746, -1.807141314969593848, -0.3518929191878711338 ) ) ;
#141856=CARTESIAN_POINT ( 'NONE',  ( -0.1102773484824119410, 2.860927498608015984, -2.691535809252169731 ) ) ;
#141857=CARTESIAN_POINT ( 'NONE',  ( 2.731144534912807842, -1.610196803864067938, 0.6186328129335681991 ) ) ;
#141858=CARTESIAN_POINT ( 'NONE',  ( 0.9191581010105540628, -1.820984308097562954, 0.8666112775468014506 ) ) ;
#141859=CARTESIAN_POINT ( 'NONE',  ( 3.005426500355699915, 1.909594650917462388, 1.212984053805040041 ) ) ;
#141860=CARTESIAN_POINT ( 'NONE',  ( 5.074884281356676574, -1.982714853632736807, -0.7105774565657559938 ) ) ;
#141862=CARTESIAN_POINT ( 'NONE',  ( 3.409201082634921498, -0.3482811000503453491, 1.734931447941751692 ) ) ;
#141864=CARTESIAN_POINT ( 'NONE',  ( 6.620655732516684822, -0.005281389526603020787, 2.273887028200880511 ) ) ;
#141865=CARTESIAN_POINT ( 'NONE',  ( 5.138538782746885580, -1.577291412575715812, 0.9494700402261007088 ) ) ;
#141869=CARTESIAN_POINT ( 'NONE',  ( 4.382901342696458258, 1.958101449220098988, -0.9841704303943515919 ) ) ;
#141872=CARTESIAN_POINT ( 'NONE',  ( 6.320769956279724155, -1.466918727022302971, 1.461273828345016845 ) ) ;
#141875=CARTESIAN_POINT ( 'NONE',  ( 3.299358975845566810, 1.519210379524044585, 1.184558777233129412 ) ) ;
#141878=CARTESIAN_POINT ( 'NONE',  ( 0.1236698368150884464, 1.936885272324913698, 1.087587522935773876 ) ) ;
#141887=CARTESIAN_POINT ( 'NONE',  ( 0.7835587076311965049, -1.864072139945194717, 0.6119401183290390511 ) ) ;
#141890=CARTESIAN_POINT ( 'NONE',  ( 5.512146440779991607, 1.959692598237902761, -0.09458084330612320789 ) ) ;
#141893=CARTESIAN_POINT ( 'NONE',  ( 6.649309733611729278, -1.732918351142084035, -1.292073167451508686 ) ) ;
#141898=CARTESIAN_POINT ( 'NONE',  ( 6.872342997630815020, -1.214913955043941174, 1.553259342649115249 ) ) ;
#141899=CARTESIAN_POINT ( 'NONE',  ( 6.222016520869273926, -1.489155408782488088, -0.8877787665630013647 ) ) ;
#141901=CARTESIAN_POINT ( 'NONE',  ( 3.456733517523991051, -1.933646301634945885, -1.031433503814835007 ) ) ;
#141902=CARTESIAN_POINT ( 'NONE',  ( 4.260959797893453249, -1.712736962785869288, 1.546631824827559454 ) ) ;
#141903=CARTESIAN_POINT ( 'NONE',  ( 5.817669245088300300, -2.011504375995844196, 0.4472435552253516411 ) ) ;
#141904=CARTESIAN_POINT ( 'NONE',  ( 2.255715180780485607, 0.8305992003537970847, 1.755491392210324353 ) ) ;
#141906=CARTESIAN_POINT ( 'NONE',  ( 5.519825572852568030, -0.5132647233585425628, 2.057443900658859182 ) ) ;
#141908=CARTESIAN_POINT ( 'NONE',  ( 3.024064729735044921, -1.777011313454954999, 0.9530116517338580451 ) ) ;
#141917=CARTESIAN_POINT ( 'NONE',  ( 5.946181061342999286, 2.058424064105804696, 0.1035008386942332104 ) ) ;
#141922=CARTESIAN_POINT ( 'NONE',  ( 4.899084735882781594, -0.2492385452713632155, -2.004177415419911679 ) ) ;
#141928=CARTESIAN_POINT ( 'NONE',  ( 3.854412985283267368, 0.7401793164230722200, 1.923571582979522798 ) ) ;
#141929=CARTESIAN_POINT ( 'NONE',  ( 3.006482587178582300, -1.942541511447487990, 0.5404910644229294903 ) ) ;
#141936=CARTESIAN_POINT ( 'NONE',  ( 2.688827190807027367, -1.158510681541668141, -1.649829502315000251 ) ) ;
#141937=CARTESIAN_POINT ( 'NONE',  ( 2.571990918753517708, -1.761868631437716548, -0.5344257538507578564 ) ) ;
#141938=CARTESIAN_POINT ( 'NONE',  ( 1.383892495861089644, 2.130622466349596511, -0.8869745915042435147 ) ) ;
#141940=CARTESIAN_POINT ( 'NONE',  ( 3.409602121571019051, -0.4253414365745535886, 2.119164713334599881 ) ) ;
#141944=CARTESIAN_POINT ( 'NONE',  ( 1.744777856283234785, -1.581906188472384400, 0.9981555316627908070 ) ) ;
#141946=CARTESIAN_POINT ( 'NONE',  ( 5.928588038458690868, 1.899881307248694418, 0.5261610973047344819 ) ) ;
#141950=CARTESIAN_POINT ( 'NONE',  ( 1.049787907720298286, -1.741764784136769162, -1.355102641770723704 ) ) ;
#141954=CARTESIAN_POINT ( 'NONE',  ( 6.639320575229257670, 2.427506520031021520, 2.484945200759064665 ) ) ;
#141955=CARTESIAN_POINT ( 'NONE',  ( 4.557473252141114983, 0.4328338235230348996, -1.923210603423119780 ) ) ;
#141956=CARTESIAN_POINT ( 'NONE',  ( 5.145303760848274344, -1.981494167013456709, 1.182657305203537401 ) ) ;
#141957=CARTESIAN_POINT ( 'NONE',  ( 5.494539847903294749, 1.833519193728103014, 0.3179774322314922741 ) ) ;
#141958=CARTESIAN_POINT ( 'NONE',  ( 3.414939784243501641, -1.565044402038212379, 1.343584798420148774 ) ) ;
#141965=CARTESIAN_POINT ( 'NONE',  ( 4.861888260954045471, -0.5834894554452072502, 2.091229948656031734 ) ) ;
#141968=CARTESIAN_POINT ( 'NONE',  ( 4.352959896991869471, 0.3989296284454147412, -1.797357466088687961 ) ) ;
#141970=CARTESIAN_POINT ( 'NONE',  ( 6.720655732516649827, 2.453385726714229609, 2.309856631140958960 ) ) ;
#141971=CARTESIAN_POINT ( 'NONE',  ( 6.585463931165095985, -0.9389328202267492873, 1.978239266594773671 ) ) ;
#141973=CARTESIAN_POINT ( 'NONE',  ( 0.1755611466353265426, -0.002217706044388422469, -2.244164702216360219 ) ) ;
#141979=CARTESIAN_POINT ( 'NONE',  ( 0.7601953647339227960, -1.285989511019115517, 1.216233164963770763 ) ) ;
#141980=CARTESIAN_POINT ( 'NONE',  ( 5.496744759480266751, -1.964553546248495541, -0.4387526145827134183 ) ) ;
#141982=CARTESIAN_POINT ( 'NONE',  ( 4.629967194361879201, -1.293677666091449296, -1.661686202823991820 ) ) ;
#141983=CARTESIAN_POINT ( 'NONE',  ( 2.776846452629442297, 1.641606522343663555, -0.9870246354491112317 ) ) ;
#141984=CARTESIAN_POINT ( 'NONE',  ( -0.02244404828160086532, 2.859736408857795009, -2.677210243787793598 ) ) ;
#141985=CARTESIAN_POINT ( 'NONE',  ( 4.756286019550246102, -1.969087757444639042, -0.05037552155932183140 ) ) ;
#141986=CARTESIAN_POINT ( 'NONE',  ( 5.713150811708690213, 1.648777711927760015, -1.166343465331370455 ) ) ;
#141987=CARTESIAN_POINT ( 'NONE',  ( 2.219420098953532428, -1.815089452277141691, 0.4520615115926190919 ) ) ;
#141988=CARTESIAN_POINT ( 'NONE',  ( 5.250533987919646428, 0.5060912822462645400, 1.648968847961843620 ) ) ;
#141989=CARTESIAN_POINT ( 'NONE',  ( 0.7383556378116812313, 1.137082172773289379, -1.537495029474859276 ) ) ;
#141991=CARTESIAN_POINT ( 'NONE',  ( 2.543839704335303153, -1.636039663378138886, -1.481301067789652537 ) ) ;
#141993=( GEOMETRIC_REPRESENTATION_CONTEXT ( 3 ) GLOBAL_UNCERTAINTY_ASSIGNED_CONTEXT ( ( #117978 ) ) GLOBAL_UNIT_ASSIGNED_CONTEXT ( ( #194247, #42698, #110933 ) ) REPRESENTATION_CONTEXT ( 'NONE', 'WORKASPACE' ) );
#141995=CARTESIAN_POINT ( 'NONE',  ( 6.355910407107248083, -0.6622273607519140182, 1.846833223631501264 ) ) ;
#142000=CARTESIAN_POINT ( 'NONE',  ( 1.961466609329724164, 1.720096886549182136, 1.151944459977225055 ) ) ;
#142005=CARTESIAN_POINT ( 'NONE',  ( 6.235037545507011281, 1.978399733989940401, 0.7636319146847592165 ) ) ;
#142010=CARTESIAN_POINT ( 'NONE',  ( 5.044295983762377311, 1.882185518538554314, -0.7230303062365079914 ) ) ;
#142011=CARTESIAN_POINT ( 'NONE',  ( 5.173012249488437853, 1.686445640873093899, -0.9088423865804375890 ) ) ;
#142012=CARTESIAN_POINT ( 'NONE',  ( 2.964592600559622593, -2.025863808726846127, -0.8364240203130177687 ) ) ;
#142015=CARTESIAN_POINT ( 'NONE',  ( 5.379157392057874354, -1.821786014368693252, -0.8570216514257876783 ) ) ;
#142016=CARTESIAN_POINT ( 'NONE',  ( 1.529408426332915960, -0.2309274165002393187, 1.898302859121250519 ) ) ;
#142019=CARTESIAN_POINT ( 'NONE',  ( 0.1226730236999207246, 0.3474926252081366185, 1.986097365194151809 ) ) ;
#142021=CARTESIAN_POINT ( 'NONE',  ( 3.790639713653580767, 1.765158817303988048, -1.120165474576743536 ) ) ;
#142023=CARTESIAN_POINT ( 'NONE',  ( 1.729112849636908367, -1.625594568690587050, 0.5768372424696955880 ) ) ;
#142033=CARTESIAN_POINT ( 'NONE',  ( 2.666445455534327102, 0.6121260541337695260, 1.705033028387469285 ) ) ;
#142036=CARTESIAN_POINT ( 'NONE',  ( 3.439928307436474597, -1.081519596823855345, -1.453003583242311381 ) ) ;
#142041=CARTESIAN_POINT ( 'NONE',  ( 4.492532346964829060, 1.824898331334467549, 0.3640980636450250052 ) ) ;
#142042=CARTESIAN_POINT ( 'NONE',  ( 1.845192132668025176, 0.3254238344292461060, -1.887580106770263999 ) ) ;
#142043=CARTESIAN_POINT ( 'NONE',  ( 0.8326870614539466642, 0.1294382003846420159, 1.821050407652326619 ) ) ;
#142052=CARTESIAN_POINT ( 'NONE',  ( 6.280130250669472503, -1.091077088088190372, -1.639371140202023014 ) ) ;
#142054=B_SPLINE_CURVE_WITH_KNOTS ( 'NONE', 3,
 ( #135949, #3763, #66631, #117624, #18968, #20036, #37366, #103441, #17894, #201964, #52553 ),
 .UNSPECIFIED., .F., .F.,
 ( 4, 1, 1, 1, 1, 1, 1, 1, 4 ),
 ( 0.000000000000000000, 0.2257091236145174484, 0.3979912149639216468, 0.5260416812932605657, 0.6190739408849097458, 0.6862087210430605211, 0.7361363507675404705, 0.7768852254246026989, 0.9999999999999998890 ),
 .UNSPECIFIED. ) ;
#142056=CARTESIAN_POINT ( 'NONE',  ( 0.1465796939425691170, -1.677718324701961361, 1.247191284554289625 ) ) ;
#142058=CARTESIAN_POINT ( 'NONE',  ( 5.104483318454627216, -0.6487533354903095573, -1.814000550502705922 ) ) ;
#142060=CARTESIAN_POINT ( 'NONE',  ( 1.535882326342351334, 0.9031702520058831896, -1.586444745400449108 ) ) ;
#142061=CARTESIAN_POINT ( 'NONE',  ( 2.578998426009218470, -2.112161100990978202, -0.6396139477699358533 ) ) ;
#142063=CARTESIAN_POINT ( 'NONE',  ( 0.7910927259777954523, -0.04954035392716604758, -1.911929172785244102 ) ) ;
#142065=CARTESIAN_POINT ( 'NONE',  ( 6.895365913452266682, -1.760736289220961481, 0.8823945077177670626 ) ) ;
#142066=CARTESIAN_POINT ( 'NONE',  ( 2.120557540808472918, 0.002150750411172245441, 1.942234967187633110 ) ) ;
#142068=CARTESIAN_POINT ( 'NONE',  ( 0.8782795706883707032, -0.2985837142155840507, 1.993765709762222782 ) ) ;
#142070=CARTESIAN_POINT ( 'NONE',  ( 6.139480533765972581, 1.719935631569947221, -0.7110793932548589158 ) ) ;
#142076=CARTESIAN_POINT ( 'NONE',  ( 2.243918346939121733, 2.191141468336772036, 0.05030144379260945153 ) ) ;
#142080=CARTESIAN_POINT ( 'NONE',  ( 2.719161800852238464, -0.1789327596440904167, 1.816892639718168390 ) ) ;
#142086=CARTESIAN_POINT ( 'NONE',  ( 0.5570954828270138215, -1.626785562868319435, -1.031698974670463009 ) ) ;
#142088=CARTESIAN_POINT ( 'NONE',  ( 5.963715375765574755, -0.4800653121489819042, 1.901962685674676523 ) ) ;
#142092=CARTESIAN_POINT ( 'NONE',  ( 5.232042516939362287, 2.159042084939459816, 0.3751777721049884273 ) ) ;
#142096=CARTESIAN_POINT ( 'NONE',  ( 4.065334711822697678, 1.773058433220272789, 1.068561072119569522 ) ) ;
#142100=CARTESIAN_POINT ( 'NONE',  ( 4.623847096394516853, 0.3921523929481546267, 2.264879156731691712 ) ) ;
#142104=CARTESIAN_POINT ( 'NONE',  ( 0.4106429779945898195, 1.576260533944493503, -1.664518642746879662 ) ) ;
#142105=CARTESIAN_POINT ( 'NONE',  ( 6.620655732516647518, 0.5865983125455545011, 1.978983952526007339 ) ) ;
#142107=CARTESIAN_POINT ( 'NONE',  ( 5.296799794911354553, 1.588725326081788847, 1.116492485978479499 ) ) ;
#142110=CARTESIAN_POINT ( 'NONE',  ( 5.677967274442059953, 1.882970570262190835, -0.3333453579756898155 ) ) ;
#142111=CARTESIAN_POINT ( 'NONE',  ( 6.071300242175304618, 0.1216566699881876934, -1.720563304769450630 ) ) ;
#142112=CARTESIAN_POINT ( 'NONE',  ( 5.717982508692024624, 0.9896897593998502662, -1.756851901128737348 ) ) ;
#142116=CARTESIAN_POINT ( 'NONE',  ( 1.412182186510477777, 1.403042805649477920, -1.550086674462275216 ) ) ;
#142117=CARTESIAN_POINT ( 'NONE',  ( 0.5316681593682397455, 0.9152217321290991858, -1.514687162473850490 ) ) ;
#142118=CARTESIAN_POINT ( 'NONE',  ( 5.537732479266092689, -1.587839044716709669, 1.242724925242834066 ) ) ;
#142120=CARTESIAN_POINT ( 'NONE',  ( 2.818655624875044285, 2.158736131429010996, 0.7712820022114060814 ) ) ;
#142121=CARTESIAN_POINT ( 'NONE',  ( 1.763200577577472172, 0.8928190760214287369, 1.493706742695336764 ) ) ;
#142122=( GEOMETRIC_REPRESENTATION_CONTEXT ( 3 ) GLOBAL_UNCERTAINTY_ASSIGNED_CONTEXT ( ( #174161 ) ) GLOBAL_UNIT_ASSIGNED_CONTEXT ( ( #185150, #207546, #69258 ) ) REPRESENTATION_CONTEXT ( 'NONE', 'WORKASPACE' ) );
#142124=CARTESIAN_POINT ( 'NONE',  ( 2.002904151241869712, 1.714182390810105927, 0.2594085799107764823 ) ) ;
#142126=CARTESIAN_POINT ( 'NONE',  ( 1.521681963465530529, 1.834278628056866367, -0.3135228456460791846 ) ) ;
#142127=CARTESIAN_POINT ( 'NONE',  ( 2.840461511066312728, -1.118188532415839598, 1.860977255340636516 ) ) ;
#142128=CARTESIAN_POINT ( 'NONE',  ( 3.098842478760281516, 1.825076540557273974, 0.8578426345753201732 ) ) ;
#142129=CARTESIAN_POINT ( 'NONE',  ( 3.500000000000003109, -2.127848526677250785E-13, -2.052068128417947612 ) ) ;
#142131=CARTESIAN_POINT ( 'NONE',  ( 6.709608095207008738, -0.4227469423600908605, 1.886647698053174116 ) ) ;
#142133=CARTESIAN_POINT ( 'NONE',  ( 3.393049125975013069, -2.141818966976690497, -0.5891788363768469816 ) ) ;
#142135=CARTESIAN_POINT ( 'NONE',  ( -0.2108831679770924727, 4.091978752061476321, -2.452067053820900622 ) ) ;
#142139=CARTESIAN_POINT ( 'NONE',  ( 6.293255338728928727, -0.1078348580665164369, -2.218937141123643375 ) ) ;
#142140=COLOUR_RGB ( '', 0.09019608, 0.27058824, 0.51372549) ;
#142141=CARTESIAN_POINT ( 'NONE',  ( 4.316819842036943911, -1.455217238560998272, 1.315978175897666080 ) ) ;
#142145=CARTESIAN_POINT ( 'NONE',  ( 6.081380179524085605, 2.093784091706856199, -0.8575614380509981594 ) ) ;
#142146=CARTESIAN_POINT ( 'NONE',  ( 2.172402883950707686, -0.9704110660942105726, -1.820128386451558500 ) ) ;
#142150=CARTESIAN_POINT ( 'NONE',  ( 3.620239363633662499, 1.188986022374241225, -1.444006105232335191 ) ) ;
#142151=CARTESIAN_POINT ( 'NONE',  ( 2.355775467714062543, 0.08314403793566874090, -1.732266345623443948 ) ) ;
#142152=CARTESIAN_POINT ( 'NONE',  ( 6.058177568126345669, -1.550975213528119623, 1.548612826651605712 ) ) ;
#142153=CARTESIAN_POINT ( 'NONE',  ( 1.149787729276055437, -1.740433383357189223, -1.356609624190791008 ) ) ;
#142154=CARTESIAN_POINT ( 'NONE',  ( 5.876890087061106271, 1.793433424740819904, -0.7452851482259108540 ) ) ;
#142156=CARTESIAN_POINT ( 'NONE',  ( -0.03452862918938356951, -1.956592590566148093, -0.4871966601913205186 ) ) ;
#142157=CARTESIAN_POINT ( 'NONE',  ( -0.08743476694611679312, -2.120266877281291595, -0.04547849331201780226 ) ) ;
#142159=CARTESIAN_POINT ( 'NONE',  ( 6.434220164165640021, -1.621181005584397372, -1.198863592720422977 ) ) ;
#142163=CARTESIAN_POINT ( 'NONE',  ( 4.371595934376539816, 1.770262903079304451, -0.4459408992859363319 ) ) ;
#142164=CARTESIAN_POINT ( 'NONE',  ( 2.397764582540245382, 1.705505620506567510, 1.400368488499253994 ) ) ;
#142170=CARTESIAN_POINT ( 'NONE',  ( 1.301042304527067817, -0.3004618026806615272, -1.997203725593140078 ) ) ;
#142174=CARTESIAN_POINT ( 'NONE',  ( 2.447915292705178825, -0.8007319036262178225, 1.680036726287994719 ) ) ;
#142180=CARTESIAN_POINT ( 'NONE',  ( 3.932112477472641920, 0.9751300899686901058, -1.543267412809447681 ) ) ;
#142185=CARTESIAN_POINT ( 'NONE',  ( 6.327499943094792023, -1.427716970705223520, 1.423745300580002482 ) ) ;
#142186=CARTESIAN_POINT ( 'NONE',  ( 5.736236344406846932, 0.3633543575551900773, 1.804753862313414281 ) ) ;
#142188=CARTESIAN_POINT ( 'NONE',  ( 4.653107873243750525, -1.855428480829583338, 1.371977642438865885 ) ) ;
#142190=CARTESIAN_POINT ( 'NONE',  ( 6.837200347746461127, -1.934230338078479772, 0.9651617863762137484 ) ) ;
#142192=CARTESIAN_POINT ( 'NONE',  ( 1.979929434068830929, -1.904991468646766606, -0.3768183752349169580 ) ) ;
#142194=CARTESIAN_POINT ( 'NONE',  ( 5.290469632519504195, -2.184888740097378879, 0.7135917202819259675 ) ) ;
#142197=CARTESIAN_POINT ( 'NONE',  ( 4.873830839387755631, 1.077430855447782942, 1.529020332772989210 ) ) ;
#142199=CARTESIAN_POINT ( 'NONE',  ( 2.584119536544440265, 1.026460374567798484, 1.613398670029235538 ) ) ;
#142201=CARTESIAN_POINT ( 'NONE',  ( 4.459734715955371520, 0.4851516707722826061, -2.152740496749529608 ) ) ;
#142203=CARTESIAN_POINT ( 'NONE',  ( 6.883263157960402445, -0.003972766660574957552, 2.046037087719229319 ) ) ;
#142206=CARTESIAN_POINT ( 'NONE',  ( 1.124223373062693820, 1.177560201100100734, -1.580856549663816280 ) ) ;
#142208=CARTESIAN_POINT ( 'NONE',  ( 2.714277975868684578, -2.282582259777651501, 0.3379699517906120110 ) ) ;
#142209=CARTESIAN_POINT ( 'NONE',  ( 1.978885927095444863, 1.829411362569667743, 0.7090815385668995940 ) ) ;
#142211=CARTESIAN_POINT ( 'NONE',  ( 6.262562444065095768, -0.7369429887811511648, -1.926613908347002413 ) ) ;
#142213=CARTESIAN_POINT ( 'NONE',  ( 4.135954056172497673, 2.015980767636461835, -0.05432360925018697717 ) ) ;
#142216=CARTESIAN_POINT ( 'NONE',  ( 4.839077477813122918, -1.706110771555340744, -1.074664961451990308 ) ) ;
#142220=CARTESIAN_POINT ( 'NONE',  ( -0.2409995289980038091, -0.004801160710915519658, -2.000252362011435636 ) ) ;
#142222=CARTESIAN_POINT ( 'NONE',  ( 2.360437767749205218, -2.170642449777848260, 0.04973808404824981572 ) ) ;
#142225=CARTESIAN_POINT ( 'NONE',  ( 2.389737607000471442, -0.8038258883538219601, 1.689183408448757362 ) ) ;
#142226=CARTESIAN_POINT ( 'NONE',  ( 6.696550776676711614, -0.5693818166121329405, -2.085215994158528208 ) ) ;
#142228=FILL_AREA_STYLE ('',( #210378 ) ) ;
#142232=CARTESIAN_POINT ( 'NONE',  ( 3.773993364719562482, 1.897484654492180178, -0.2369724479281897223 ) ) ;
#142233=CARTESIAN_POINT ( 'NONE',  ( 4.153014383403249354, -1.471681513620528348, -0.9827620175600642050 ) ) ;
#142234=CARTESIAN_POINT ( 'NONE',  ( 1.365713085969634477, 0.5541664655046051324, -1.830235057661818487 ) ) ;
#142237=CARTESIAN_POINT ( 'NONE',  ( -0.2060670157024322158, -0.8220983527124374746, -1.729069022899624164 ) ) ;
#142239=CARTESIAN_POINT ( 'NONE',  ( 1.223191768902037957, -1.870915810643185795, -0.8869332102946840823 ) ) ;
#142241=CARTESIAN_POINT ( 'NONE',  ( 5.946149726614579301, 1.868617323842229894, 0.09011704611043556967 ) ) ;
#142242=CARTESIAN_POINT ( 'NONE',  ( 1.295219883412350503, 1.381147610352757127, 1.194082977437810333 ) ) ;
#142243=CARTESIAN_POINT ( 'NONE',  ( 5.602238545945851023, -2.207063162045197924, -0.003355105161521875021 ) ) ;
#142246=CARTESIAN_POINT ( 'NONE',  ( 2.963389562657412046, 1.741120879107743935, 1.105697716663532892 ) ) ;
#142254=CARTESIAN_POINT ( 'NONE',  ( 4.879381568908511824, -0.1049739508458477355, 2.067839077007492143 ) ) ;
#142256=CARTESIAN_POINT ( 'NONE',  ( 2.407699484934812784, -0.4761397456576694776, 2.108333575599189214 ) ) ;
#142258=CARTESIAN_POINT ( 'NONE',  ( 3.246744516521868018, 1.970913372098213712, 0.4403762775553735631 ) ) ;
#142259=CARTESIAN_POINT ( 'NONE',  ( 6.620655732516618208, 1.260995252412312251, 2.189931766300906801 ) ) ;
#142265=CARTESIAN_POINT ( 'NONE',  ( 1.217982839071569012, 0.9896824804975331569, -1.756856037137774162 ) ) ;
#142267=CARTESIAN_POINT ( 'NONE',  ( 5.952700804540856261, -1.878875186057769264, -1.127905468421293689 ) ) ;
#142269=CARTESIAN_POINT ( 'NONE',  ( 4.623256175466384121, 1.666654777633369555, 0.9376445158523970536 ) ) ;
#142273=CARTESIAN_POINT ( 'NONE',  ( 3.655875201264874974, 1.122517324909186653, 1.674876314423722423 ) ) ;
#142275=CARTESIAN_POINT ( 'NONE',  ( 5.666962058884261744, -1.561145826413099291, -0.7335915956277230254 ) ) ;
#142280=CARTESIAN_POINT ( 'NONE',  ( 4.182764291190976813, -0.1809548918480126112, -1.861743760598027597 ) ) ;
#142282=CARTESIAN_POINT ( 'NONE',  ( 1.077107760077404830, 1.911388382048292645, 0.7958064784282169457 ) ) ;
#142286=CARTESIAN_POINT ( 'NONE',  ( 6.393201686769759640, -0.09647555762395694512, -1.809044896826275783 ) ) ;
#142288=CARTESIAN_POINT ( 'NONE',  ( -0.03552856956758054796, -1.956598898622825766, -0.4871759670460884539 ) ) ;
#142289=CARTESIAN_POINT ( 'NONE',  ( -0.07045567476893913050, -1.776642250867260575, 0.3530574836328649324 ) ) ;
#142296=CARTESIAN_POINT ( 'NONE',  ( 0.2386218892466463737, -1.902018210125755004, -0.4804332253167050149 ) ) ;
#142298=CARTESIAN_POINT ( 'NONE',  ( 4.552287420941045326, -1.248256511182913364, 1.453175340101879875 ) ) ;
#142305=CARTESIAN_POINT ( 'NONE',  ( 1.516726440323381331, 1.451591637995581996, -1.601975981646540426 ) ) ;
#142310=CARTESIAN_POINT ( 'NONE',  ( 4.313378725478684395, -0.3118687524542098632, 1.798583714455632476 ) ) ;
#142312=CARTESIAN_POINT ( 'NONE',  ( 1.370321444179344983, -1.253680685346630019, 1.521333489566406127 ) ) ;
#142313=CARTESIAN_POINT ( 'NONE',  ( 3.427896188528327226, -1.883279545317056547, 0.3315703044584616399 ) ) ;
#142316=CARTESIAN_POINT ( 'NONE',  ( 3.402753045726066183, 0.4761229057644749130, 1.911014528907057697 ) ) ;
#142318=CARTESIAN_POINT ( 'NONE',  ( 5.601106521291020712, -0.4677194688633263264, 1.884795189151499795 ) ) ;
#142324=CARTESIAN_POINT ( 'NONE',  ( 4.020093958671668410, -1.906945023982812515, 0.1437811316862200317 ) ) ;
#142325=CARTESIAN_POINT ( 'NONE',  ( 6.983263157960370116, 1.266851337794393961, 2.060309365732877485 ) ) ;
#142328=CARTESIAN_POINT ( 'NONE',  ( 5.233069312805943341, 1.860886824452904653, 0.7683393057746935595 ) ) ;
#142330=CARTESIAN_POINT ( 'NONE',  ( 5.707590141996651489, -0.4392596013848491521, 1.771934311310577659 ) ) ;
#142331=CARTESIAN_POINT ( 'NONE',  ( 6.727182134110205602, 7.053355583909074689, 2.409100679957976165 ) ) ;
#142332=CARTESIAN_POINT ( 'NONE',  ( 2.400909748719297188, 0.4512941399696759337, 2.020426262116347349 ) ) ;
#142342=CARTESIAN_POINT ( 'NONE',  ( 0.2331713839410576306, 0.005725554726919174046, -1.953566683266183102 ) ) ;
#142347=CARTESIAN_POINT ( 'NONE',  ( 4.781731028689206298, 1.437863813525115830, -0.9690746147167289548 ) ) ;
#142349=CARTESIAN_POINT ( 'NONE',  ( 2.852461952307944415, -2.064405766265942521, -0.1567919417525542591 ) ) ;
#142350=CARTESIAN_POINT ( 'NONE',  ( 3.919616530476960126, -1.461442364795034976, -1.532149496301576486 ) ) ;
#142353=CARTESIAN_POINT ( 'NONE',  ( 1.393335261261628988, -1.782783755681414117, 0.8371470673369950655 ) ) ;
#142358=CARTESIAN_POINT ( 'NONE',  ( 4.084120828622629595, -2.267077656855093881, -0.3380819097023191055 ) ) ;
#142359=CARTESIAN_POINT ( 'NONE',  ( 0.3108172448005979138, 1.586703044182024458, 0.9029097728878652251 ) ) ;
#142364=CARTESIAN_POINT ( 'NONE',  ( 1.195565668251681535, 1.858513546554524609, -0.7743570246632487386 ) ) ;
#142365=CARTESIAN_POINT ( 'NONE',  ( 2.571086506140254357, 1.750134206675527437, 0.8865088104979682582 ) ) ;
#142369=CARTESIAN_POINT ( 'NONE',  ( 4.962875334715753262, 0.2052988877573138915, -2.080521221900538009 ) ) ;
#142370=CARTESIAN_POINT ( 'NONE',  ( 3.959615635602866668, 1.756445048235187212, -0.2166398133998989062 ) ) ;
#142372=CARTESIAN_POINT ( 'NONE',  ( 6.316396932256916230, 2.136508426756661638, 0.8310160958180726753 ) ) ;
#142373=CARTESIAN_POINT ( 'NONE',  ( 5.261534320672216936, 0.8623632012556389226, 1.511560460804670880 ) ) ;
#142375=CARTESIAN_POINT ( 'NONE',  ( 5.942043047034061942, -1.969448396301001436, -1.185220976332189924 ) ) ;
#142377=CARTESIAN_POINT ( 'NONE',  ( 5.536419981033642301, 1.670246277208887742, -0.4650152690930853816 ) ) ;
#142378=CARTESIAN_POINT ( 'NONE',  ( 5.758309058547314230, -2.171350062218261989, -0.005773456755737981470 ) ) ;
#142380=CARTESIAN_POINT ( 'NONE',  ( 6.491432910188612126, -0.4373703761123280964, 1.975813455233149218 ) ) ;
#142381=CARTESIAN_POINT ( 'NONE',  ( 4.562500000000002665, -1.451031289061298857, -1.451031289060931595 ) ) ;
#142383=CARTESIAN_POINT ( 'NONE',  ( 4.120081753510516975, -0.9896868749219210892, -1.652585292789155558 ) ) ;
#142385=CARTESIAN_POINT ( 'NONE',  ( 0.01275469579824477576, -2.220946917248843189, -0.04775700320917666830 ) ) ;
#142390=CARTESIAN_POINT ( 'NONE',  ( 2.385647502782287432, 0.1060323020976374625, -2.218877139873560278 ) ) ;
#142396=CARTESIAN_POINT ( 'NONE',  ( 0.8795299900376440938, -0.4926441280813895762, -1.955172062459666904 ) ) ;
#142398=CARTESIAN_POINT ( 'NONE',  ( 4.967260703730732807, 1.792967015482237469, 1.019669102033170516 ) ) ;
#142403=CARTESIAN_POINT ( 'NONE',  ( 0.6843625024184678551, -0.2082719882288592839, -1.757362784332392458 ) ) ;
#142404=CARTESIAN_POINT ( 'NONE',  ( 6.047464834240314779, -1.219521636822028077, 1.233209766127696616 ) ) ;
#142405=CARTESIAN_POINT ( 'NONE',  ( 5.829613671240826633, 0.8500414093583901209, -1.518663286469445151 ) ) ;
#142406=CARTESIAN_POINT ( 'NONE',  ( 2.701037021348651646, 1.938191879511786730, 1.223809664465740354 ) ) ;
#142408=CARTESIAN_POINT ( 'NONE',  ( 1.833694255977034615, 1.820935426717207317, 0.2711280389895084353 ) ) ;
#142411=CARTESIAN_POINT ( 'NONE',  ( 3.082817581614716307, -0.1327354176642106531, -1.820802398864965088 ) ) ;
#142412=CARTESIAN_POINT ( 'NONE',  ( 3.375625116643202972, -0.3961014713874110305, -1.976955985980306307 ) ) ;
#142415=CARTESIAN_POINT ( 'NONE',  ( 5.368238606676455582, 1.035150450411811640, 1.833903993397972387 ) ) ;
#142417=CARTESIAN_POINT ( 'NONE',  ( 2.154816067267216084, -0.5500195584662926906, -1.995915215819036748 ) ) ;
#142420=CARTESIAN_POINT ( 'NONE',  ( 4.582752651445391123, -1.384437811569695587, 1.606279107262520434 ) ) ;
#142421=CARTESIAN_POINT ( 'NONE',  ( 1.154767827468632824, -1.519305277103833118, 1.184426060187010465 ) ) ;
#142428=CARTESIAN_POINT ( 'NONE',  ( 6.064709079624690524, 0.6667526090060638122, 2.013086243192941716 ) ) ;
#142429=CARTESIAN_POINT ( 'NONE',  ( 2.098786246049421766, -0.5609894644466472124, -2.029802036486601846 ) ) ;
#142433=CARTESIAN_POINT ( 'NONE',  ( 6.350447304104193336, -1.851927549110881976, -0.1832485138882292142 ) ) ;
#142439=CARTESIAN_POINT ( 'NONE',  ( 0.2289750728588327566, 1.457791096766167360, -1.540313549178488284 ) ) ;
#142442=CARTESIAN_POINT ( 'NONE',  ( 2.682025323810240280, -1.127217178123595565, -1.605522638798158264 ) ) ;
#142443=CARTESIAN_POINT ( 'NONE',  ( 1.499129196564863209, 1.767075381950654611, -1.244890797856931686 ) ) ;
#142447=CARTESIAN_POINT ( 'NONE',  ( 2.431276410161122392, 0.8208083392724160321, -1.534589408508793440 ) ) ;
#142451=CARTESIAN_POINT ( 'NONE',  ( 2.337267334706777611, -1.242538083881424837, 1.587593183769491878 ) ) ;
#142454=CARTESIAN_POINT ( 'NONE',  ( 2.764479830724082543, -1.360639549628063882, 1.426867346614549836 ) ) ;
#142455=CARTESIAN_POINT ( 'NONE',  ( 5.783449990912790106, 0.1341079605299954347, -1.907733270042926810 ) ) ;
#142460=CARTESIAN_POINT ( 'NONE',  ( 1.172527652694483669, 0.8205418800426617087, 1.845675728695548745 ) ) ;
#142462=CARTESIAN_POINT ( 'NONE',  ( 6.176872536373793743, -2.188556106905717780, -0.7317919303653409591 ) ) ;
#142463=CARTESIAN_POINT ( 'NONE',  ( 5.828557447170540584, -1.245780601409246957, 1.515539014345569147 ) ) ;
#142464=CARTESIAN_POINT ( 'NONE',  ( 3.221486639279776298, 0.2924833653642990861, -1.939731193138781951 ) ) ;
#142466=CARTESIAN_POINT ( 'NONE',  ( 1.143204175302305670, 0.8197749522141674072, 1.842446510343001442 ) ) ;
#142468=CARTESIAN_POINT ( 'NONE',  ( 0.7084050413898737020, 1.255986415914780885, -1.704487872487458144 ) ) ;
#142471=CARTESIAN_POINT ( 'NONE',  ( 1.868857239601273923, 1.762127240619456803, -0.5335365013287920455 ) ) ;
#142474=CARTESIAN_POINT ( 'NONE',  ( 2.830460552442021438, -1.048868820301660953, -1.842999677239331113 ) ) ;
#142478=CARTESIAN_POINT ( 'NONE',  ( 2.706383518077785322, -0.7856088873096721548, -1.905365358233277240 ) ) ;
#142480=CARTESIAN_POINT ( 'NONE',  ( 1.346931166825489967, 0.5339940059071214273, -1.762130705996706181 ) ) ;
#142486=CARTESIAN_POINT ( 'NONE',  ( 1.313402753022639091, 1.947697196196996217, 1.037691534346518729 ) ) ;
#142487=CARTESIAN_POINT ( 'NONE',  ( 3.163607282743227334, 0.3354078767881124024, -2.237311900363625483 ) ) ;
#142490=CARTESIAN_POINT ( 'NONE',  ( 2.953145165254339233, -1.595657772652997464, 0.8577772064107972438 ) ) ;
#142491=CARTESIAN_POINT ( 'NONE',  ( 3.309697661505988986, -1.145383095959727315, -1.535415057543190409 ) ) ;
#142492=CARTESIAN_POINT ( 'NONE',  ( 4.756339170418532269, -2.069830778647030023, -0.05414847147890837487 ) ) ;
#142494=CARTESIAN_POINT ( 'NONE',  ( 2.623849442957484346, -1.133682707547468471, -1.612724008377570017 ) ) ;
#142495=CARTESIAN_POINT ( 'NONE',  ( 0.08292192553204823235, -0.1316706149618769306, -1.895886810074402185 ) ) ;
#142496=CARTESIAN_POINT ( 'NONE',  ( 3.010468980803046257, 1.356049738124785353, -1.288842618233053683 ) ) ;
#142498=CARTESIAN_POINT ( 'NONE',  ( 2.333053021162025953, 2.238922732217122125, 0.5587339331782120722 ) ) ;
#142500=CARTESIAN_POINT ( 'NONE',  ( 3.771788145607783527, -1.833817148065859604, 0.3161742572238452897 ) ) ;
#142505=CARTESIAN_POINT ( 'NONE',  ( 0.8562495616285453748, 2.103569811481691865, -0.1051806538951201714 ) ) ;
#142507=CARTESIAN_POINT ( 'NONE',  ( 5.993488848236776967, 1.632462841753023808, 1.416962642945495565 ) ) ;
#142508=CARTESIAN_POINT ( 'NONE',  ( 6.481118763745143063, -1.847444428138062422, -0.8165197575118980922 ) ) ;
#142512=CARTESIAN_POINT ( 'NONE',  ( 6.925078400183574345, 6.038986730273901316, 2.350556043039519150 ) ) ;
#142514=CARTESIAN_POINT ( 'NONE',  ( -0.2104748580754183529, 0.2283854016844401591, -2.137091067173245929 ) ) ;
#142515=CARTESIAN_POINT ( 'NONE',  ( 4.487517715496184501, -0.5331711073110931842, 1.944729879240604253 ) ) ;
#142519=CARTESIAN_POINT ( 'NONE',  ( 5.858325616802108726, 0.8718737102157668728, 1.978260574764856283 ) ) ;
#142523=CARTESIAN_POINT ( 'NONE',  ( 6.134388704033759687, 0.6352148712998658686, 1.913799669303432927 ) ) ;
#142528=CARTESIAN_POINT ( 'NONE',  ( 1.506044924156377807, -0.6181864485952697219, -1.610478869194363227 ) ) ;
#142533=CARTESIAN_POINT ( 'NONE',  ( 0.5964902553294594290, 1.476022596236561846, -0.9760666246667221158 ) ) ;
#142534=CARTESIAN_POINT ( 'NONE',  ( 1.752591402120354358, 1.991486659738419984, 0.2933061901304565011 ) ) ;
#142537=CARTESIAN_POINT ( 'NONE',  ( 3.944505925199864649, 2.195883038551619038, 0.2190369969904403802 ) ) ;
#142538=CARTESIAN_POINT ( 'NONE',  ( 5.207971749312423348, 0.6875717650507988665, -2.059362367386765591 ) ) ;
#142542=CARTESIAN_POINT ( 'NONE',  ( 3.106218681870171139, -0.8574772492565514437, 1.939554460742904274 ) ) ;
#142543=CARTESIAN_POINT ( 'NONE',  ( 3.286732619643798703, 1.587825416925658262, -1.242744175535138940 ) ) ;
#142544=CARTESIAN_POINT ( 'NONE',  ( 3.867288652163490159, -1.509380944159900428, -1.001465339209107075 ) ) ;
#142548=CARTESIAN_POINT ( 'NONE',  ( 0.7427767429722329506, -1.606530860214189893, 0.9580933318182258684 ) ) ;
#142550=CARTESIAN_POINT ( 'NONE',  ( 5.654876981934024549, -1.436564326775534806, 1.126588154728463742 ) ) ;
#142552=CARTESIAN_POINT ( 'NONE',  ( 1.077184250232362306, 1.452872634298128629, 1.248800971253192005 ) ) ;
#142556=CARTESIAN_POINT ( 'NONE',  ( 5.313408243115378404, -0.3210861823062812759, 2.137610926513198617 ) ) ;
#142560=CARTESIAN_POINT ( 'NONE',  ( 2.971057270251746374, -1.603071526910588629, 1.388259434452358665 ) ) ;
#142561=CARTESIAN_POINT ( 'NONE',  ( -0.1296875068448125057, 0.2507808023153486054, -1.861542470327881560 ) ) ;
#142563=CARTESIAN_POINT ( 'NONE',  ( 4.745367521161733215, -1.522072814771213922, -1.252777155790285590 ) ) ;
#142564=CARTESIAN_POINT ( 'NONE',  ( 6.205323455156911194, 1.660478276859885582, -0.9486371710855368011 ) ) ;
#142566=CARTESIAN_POINT ( 'NONE',  ( 0.05257324754554763141, -1.379058229334565455, 1.606613856852637356 ) ) ;
#142568=CARTESIAN_POINT ( 'NONE',  ( 1.135311898753359472, -0.04898221611688948623, -2.069941200615910581 ) ) ;
#142569=CARTESIAN_POINT ( 'NONE',  ( 2.484236259141327618, -0.3323325037456366093, -1.913154051555246316 ) ) ;
#142573=CARTESIAN_POINT ( 'NONE',  ( 3.837900784552390476, 2.080585211200749018, 0.2046572434392830431 ) ) ;
#142576=CARTESIAN_POINT ( 'NONE',  ( 0.7503001202024300875, 1.784421795204504946, 0.3107989935832651818 ) ) ;
#142578=CARTESIAN_POINT ( 'NONE',  ( 5.496761087669068679, -0.5331231007881258588, -2.141394884921154151 ) ) ;
#142581=CARTESIAN_POINT ( 'NONE',  ( 2.766872162265196611, -1.522532973755141850, 1.597636210702752635 ) ) ;
#142584=CARTESIAN_POINT ( 'NONE',  ( 1.453610327690219473, -1.385809040371610346, -1.317956379189986871 ) ) ;
#142586=CARTESIAN_POINT ( 'NONE',  ( 5.441872305809390298, 1.387781221417656141, 1.536568222347669987 ) ) ;
#142588=CARTESIAN_POINT ( 'NONE',  ( 2.360439101503517101, 0.9236781337260314695, 1.954550705658316456 ) ) ;
#142589=CARTESIAN_POINT ( 'NONE',  ( 5.372676843235411503, -0.05303982195071360595, -2.191091664329389399 ) ) ;
#142598=CARTESIAN_POINT ( 'NONE',  ( 6.069205674026176389, 1.823072449729469247, 0.9810699074010442722 ) ) ;
#142599=CARTESIAN_POINT ( 'NONE',  ( 3.897031312914517098, 1.626875583419360005, -1.031562066982329329 ) ) ;
#142600=CARTESIAN_POINT ( 'NONE',  ( 0.3160300859305562593, 1.034144755472726995, -1.730879882831819705 ) ) ;
#142605=CARTESIAN_POINT ( 'NONE',  ( 4.979337304519595442, -0.1005905848140927622, 1.967025916208066327 ) ) ;
#142606=CARTESIAN_POINT ( 'NONE',  ( 6.527265088719197195, -1.491963682546100900, -1.740339723829595453 ) ) ;
#142607=CARTESIAN_POINT ( 'NONE',  ( 5.215394836314163562, -0.2642288504575221464, 1.806346989861665087 ) ) ;
#142614=CARTESIAN_POINT ( 'NONE',  ( 3.227900028218867234, 1.797025815167479390, 0.4004103908350764573 ) ) ;
#142615=CARTESIAN_POINT ( 'NONE',  ( 5.783453021694040963, 0.1439598661895292731, -2.008088619348106896 ) ) ;
#142616=CARTESIAN_POINT ( 'NONE',  ( 1.124856824619735463, 0.4467566299657543816, -2.254411929275771609 ) ) ;
#142617=CARTESIAN_POINT ( 'NONE',  ( 5.348475771816908697, -1.946495798708135938, -0.2439133590248846462 ) ) ;
#142621=CARTESIAN_POINT ( 'NONE',  ( 0.5024991115675537801, 2.064720838319131779, 0.1538615064654233477 ) ) ;
#142623=CARTESIAN_POINT ( 'NONE',  ( 1.857086946601906652, 0.3542020299988774545, -2.060351931225719468 ) ) ;
#142624=CARTESIAN_POINT ( 'NONE',  ( 6.719637426148988624, -1.715392417075599196, 0.4352852820774539833 ) ) ;
#142627=CARTESIAN_POINT ( 'NONE',  ( -0.2102771530458458771, 0.2260464284578807270, -2.237246294970319127 ) ) ;
#142628=CARTESIAN_POINT ( 'NONE',  ( 2.383973883943972805, -0.2989522671389834851, -1.714397271258593092 ) ) ;
#142632=CARTESIAN_POINT ( 'NONE',  ( 2.261930500750704454, 0.7363377991795038158, 1.559957641100855330 ) ) ;
#142633=CARTESIAN_POINT ( 'NONE',  ( 2.314256413632868714, 1.428969747754246233, -1.661726224907192684 ) ) ;
#142634=CARTESIAN_POINT ( 'NONE',  ( 0.1231123065759693186, 0.2931380485183229800, 1.709000606096510166 ) ) ;
#142635=CARTESIAN_POINT ( 'NONE',  ( 4.846401659255799466, 2.200796399388889935, 0.1645688927329121420 ) ) ;
#142638=CARTESIAN_POINT ( 'NONE',  ( 2.958077724197702096, -0.6850214551260015439, 2.060201288156039645 ) ) ;
#142639=CARTESIAN_POINT ( 'NONE',  ( 0.9260630535584664091, 1.089557764695957554, -1.464779044915397455 ) ) ;
#142640=CARTESIAN_POINT ( 'NONE',  ( 3.837202554855035697, -1.762604653963547818, -1.172905022591600233 ) ) ;
#142642=CARTESIAN_POINT ( 'NONE',  ( 6.539320575229216281, 4.696526872534390940, 2.559412612844500057 ) ) ;
#142644=CARTESIAN_POINT ( 'NONE',  ( 4.177453601039508690, 1.497175104222212783, 1.735980874517801587 ) ) ;
#142647=CARTESIAN_POINT ( 'NONE',  ( 6.516288422252827672, -2.220882151245454850, 0.05110445944340144542 ) ) ;
#142653=CARTESIAN_POINT ( 'NONE',  ( 4.535779832184696936, -1.617819081767550182, 1.203352566194588746 ) ) ;
#142655=CARTESIAN_POINT ( 'NONE',  ( 1.692308231870808921, 1.020316376917740575, -1.792489025137546044 ) ) ;
#142660=CARTESIAN_POINT ( 'NONE',  ( 5.050807487124363782, -1.850163549229045579, -1.174163402404400092 ) ) ;
#142661=CARTESIAN_POINT ( 'NONE',  ( 4.008435526009396455, -1.928752077057366732, 0.5880193435906443389 ) ) ;
#142662=CARTESIAN_POINT ( 'NONE',  ( 1.979791773625012352, -1.805961398883266344, -0.3578489297004632808 ) ) ;
#142665=CARTESIAN_POINT ( 'NONE',  ( 5.860330175037709921, 0.7421476303169188826, 1.668095884353037128 ) ) ;
#142667=CARTESIAN_POINT ( 'NONE',  ( 5.770491790047429959, -1.440319307945096217, 1.744843718407377731 ) ) ;
#142669=CARTESIAN_POINT ( 'NONE',  ( 1.489043601129129701, -0.3103829872296200443, -2.082944856911663312 ) ) ;
#142680=CARTESIAN_POINT ( 'NONE',  ( 1.441811196653530747, -1.994930912159533332, 0.7194735443712959588 ) ) ;
#142681=CARTESIAN_POINT ( 'NONE',  ( 2.812952309885875746, -0.6487812942810657901, -2.124531788647378239 ) ) ;
#142683=CARTESIAN_POINT ( 'NONE',  ( 0.3466626200071438180, 2.201290530325435757, 0.1579762268871589825 ) ) ;
#142686=CARTESIAN_POINT ( 'NONE',  ( 4.457442142980160504, 1.574409630067734156, 1.170308293268598421 ) ) ;
#142694=CARTESIAN_POINT ( 'NONE',  ( 3.287459871768631636, 0.04819156399121089784, -2.120204644799832394 ) ) ;
#142696=CARTESIAN_POINT ( 'NONE',  ( 4.592742373648754040, -0.4705147408641910944, -2.109722102427157964 ) ) ;
#142697=CARTESIAN_POINT ( 'NONE',  ( 3.544333174469185721, -1.503253232081468216, 1.062929765333266108 ) ) ;
#142701=CARTESIAN_POINT ( 'NONE',  ( 6.263578219495629540, 0.9010232283708031753, 1.488777805958479528 ) ) ;
#142702=CARTESIAN_POINT ( 'NONE',  ( 6.727182134110209155, 1.290711256955964448, 1.927001067762003972 ) ) ;
#142705=CARTESIAN_POINT ( 'NONE',  ( 3.116266767097406909, -1.064116542966097922, -1.881565754655416756 ) ) ;
#142707=CARTESIAN_POINT ( 'NONE',  ( 5.536482449520531368, 1.943773098233076757, -0.5350085594507182352 ) ) ;
#142710=CARTESIAN_POINT ( 'NONE',  ( 1.833122199354455972, 0.2117775504973731793, 2.151289291301178075 ) ) ;
#142711=CARTESIAN_POINT ( 'NONE',  ( 3.198462767114045313, -0.5687421903855809369, -1.887558129442780341 ) ) ;
#142712=CARTESIAN_POINT ( 'NONE',  ( 0.01162390915069450026, -2.148011843722149372, 0.4338911918742721641 ) ) ;
#142713=CARTESIAN_POINT ( 'NONE',  ( 1.202667248822903989, -2.307758714249080079, 0.002725711325006137473 ) ) ;
#142714=CARTESIAN_POINT ( 'NONE',  ( 4.634287131779754709, 0.3355949523314147309, 1.912704035658734592 ) ) ;
#142723=CARTESIAN_POINT ( 'NONE',  ( 2.063769564651289912, 0.3772465526380370804, -2.174136642525636098 ) ) ;
#142725=CARTESIAN_POINT ( 'NONE',  ( 5.998874280538830206, 0.3792253423284037139, 1.924579554046601970 ) ) ;
#142729=CARTESIAN_POINT ( 'NONE',  ( 0.1747926744264659826, 0.006858446013176252437, -1.855468577918440332 ) ) ;
#142731=CARTESIAN_POINT ( 'NONE',  ( 5.138538782746885580, -1.577291412575715812, 0.9494700402261007088 ) ) ;
#142736=CARTESIAN_POINT ( 'NONE',  ( 6.521762860236213655, -0.4636855090699961712, 2.076960040381255812 ) ) ;
#142741=CARTESIAN_POINT ( 'NONE',  ( 0.3036813079041804087, -0.5503025168475895734, 1.985974332091578809 ) ) ;
#142743=CARTESIAN_POINT ( 'NONE',  ( 2.066652149400012295, 1.381653119961171239, -1.247030302550973468 ) ) ;
#142744=CARTESIAN_POINT ( 'NONE',  ( 4.880324068823122197, -0.2306306682541107433, -1.826696389425507938 ) ) ;
#142750=CARTESIAN_POINT ( 'NONE',  ( 4.459734715955371520, 0.4851516707722826061, -2.152740496749529608 ) ) ;
#142751=CARTESIAN_POINT ( 'NONE',  ( 6.485631321617453260, 1.553040037441177690, 1.645414220380213788 ) ) ;
#142753=CARTESIAN_POINT ( 'NONE',  ( 5.713115418873079498, 1.475880075617709730, -1.050242514106846992 ) ) ;
#142754=CARTESIAN_POINT ( 'NONE',  ( 0.2160302486270138655, 1.032475520995678853, -1.731998313101141163 ) ) ;
#142759=CARTESIAN_POINT ( 'NONE',  ( 5.268181577278353345, 1.909906527651853425, -0.09793718704654422180 ) ) ;
#142761=CARTESIAN_POINT ( 'NONE',  ( 0.3560485870845608858, 0.7116971694140910021, 1.730184004908103867 ) ) ;
#142762=CARTESIAN_POINT ( 'NONE',  ( 1.885954221117658092, -2.015980662343511032, 0.05432778586660082232 ) ) ;
#142764=CARTESIAN_POINT ( 'NONE',  ( 4.301466803424673913, 1.691180239654224815, 1.254954771472403641 ) ) ;
#142769=CARTESIAN_POINT ( 'NONE',  ( 3.252217677095782911, 0.9042450522839510230, -1.806111763424333105 ) ) ;
#142772=CARTESIAN_POINT ( 'NONE',  ( 3.936934155531632396, 0.3128429973590241553, 2.138701728237289768 ) ) ;
#142778=CARTESIAN_POINT ( 'NONE',  ( 1.645237833728605548, -0.3177867502775574837, -2.147667186158049191 ) ) ;
#142781=CARTESIAN_POINT ( 'NONE',  ( 0.4679805871025365382, -1.733519288248483559, -0.6209854868195128219 ) ) ;
#142784=CARTESIAN_POINT ( 'NONE',  ( 2.191216702865448784, 1.696344223602393786, 1.387594652289561248 ) ) ;
#142786=CARTESIAN_POINT ( 'NONE',  ( 2.413256113406063275, 2.020865564879420262, 1.017551375885389131 ) ) ;
#142792=CARTESIAN_POINT ( 'NONE',  ( 4.129968326689526847, 0.9481555284369269643, -1.494110371635357648 ) ) ;
#142795=CARTESIAN_POINT ( 'NONE',  ( 1.079290920250153496, -0.05147710300976635067, -2.105495365820194920 ) ) ;
#142800=CARTESIAN_POINT ( 'NONE',  ( 6.609000000000038177, 0.002801690667396730672, 2.000160786441218530 ) ) ;
#142801=CARTESIAN_POINT ( 'NONE',  ( 5.097853226644959435, 1.222535334948423813, 1.337041937662573288 ) ) ;
#142803=CARTESIAN_POINT ( 'NONE',  ( 3.379631771358857950, 1.185797501207178861, 1.446808710765794315 ) ) ;
#142804=CARTESIAN_POINT ( 'NONE',  ( 3.924723049676182018, -1.394041313093749457, 1.530695986988836799 ) ) ;
#142812=CARTESIAN_POINT ( 'NONE',  ( 3.736726379466179804, -1.890069333072645241, -0.5255722985574098338 ) ) ;
#142813=CARTESIAN_POINT ( 'NONE',  ( 1.282577132041575529, -1.967586879516727061, 0.4389604359977539172 ) ) ;
#142816=CARTESIAN_POINT ( 'NONE',  ( 6.639320575229252341, 0.005161017367553630275, 1.896863882003448021 ) ) ;
#142817=CARTESIAN_POINT ( 'NONE',  ( 1.334983872447586872, -1.693447605269988276, 0.7947349781701130711 ) ) ;
#142819=CARTESIAN_POINT ( 'NONE',  ( 3.076434440837049866, 0.9091080936043660632, 1.796352098325330715 ) ) ;
#142821=CARTESIAN_POINT ( 'NONE',  ( 2.917688350237046979, -1.423917071783699972, -1.567024636986138253 ) ) ;
#142823=CARTESIAN_POINT ( 'NONE',  ( 5.301260566756325510, -1.777534899005998481, 1.061244097098137606 ) ) ;
#142825=CARTESIAN_POINT ( 'NONE',  ( -0.02372336622697389028, -2.029015295047017720, -0.5039539365503820090 ) ) ;
#142827=CARTESIAN_POINT ( 'NONE',  ( 4.981388616008130654, 1.702979688329594676, -0.6582044668519275721 ) ) ;
#142835=CARTESIAN_POINT ( 'NONE',  ( 5.233030847706650057, 1.768443763404730307, 0.7281017474275592871 ) ) ;
#142851=CARTESIAN_POINT ( 'NONE',  ( 1.867950311876313219, -1.955179860842346296, 0.2357939167430597172 ) ) ;
#142852=CARTESIAN_POINT ( 'NONE',  ( 3.497672881252233967, -1.986097994744703721, 0.3474890017408845955 ) ) ;
#142855=CARTESIAN_POINT ( 'NONE',  ( 6.827182134110231004, 7.052068023338082803, 2.687205202894725975 ) ) ;
#142857=CARTESIAN_POINT ( 'NONE',  ( 3.714928722721734911, -0.1615716889580356697, 2.185543052782303874 ) ) ;
#142859=CARTESIAN_POINT ( 'NONE',  ( 2.573164103464478991, 0.09656903795818297387, -1.924097065980167942 ) ) ;
#142862=CARTESIAN_POINT ( 'NONE',  ( 0.2333540202161610289, 4.089650199633740435, -2.600675808310505044 ) ) ;
#142870=CARTESIAN_POINT ( 'NONE',  ( 5.812015183962491172, 1.231757822100377320, -1.368757117762291253 ) ) ;
#142871=CARTESIAN_POINT ( 'NONE',  ( 3.229155175764964802, 1.820814436659716096, 0.8588418517583608081 ) ) ;
#142872=CARTESIAN_POINT ( 'NONE',  ( 4.763194794223141848, -2.297684049645591919, -0.06285783202429616467 ) ) ;
#142873=CARTESIAN_POINT ( 'NONE',  ( -0.02900071798683095947, 5.719935618195115978, -2.767867108847458901 ) ) ;
#142874=CARTESIAN_POINT ( 'NONE',  ( 1.885388715806934679, -1.754394424870173719, 0.6211283009984622794 ) ) ;
#142880=CARTESIAN_POINT ( 'NONE',  ( 5.179275120254928311, 1.405169897584326089, 1.548284651509527210 ) ) ;
#142881=CARTESIAN_POINT ( 'NONE',  ( 3.783945140921864070, -0.9226758061156097313, 1.627204332209288395 ) ) ;
#142887=CARTESIAN_POINT ( 'NONE',  ( 6.498688201949993193, -0.4681372660274349951, -1.660085793416385513 ) ) ;
#142890=CARTESIAN_POINT ( 'NONE',  ( 1.758077109659747395, 1.659224110165247179, -0.5040892880595440051 ) ) ;
#142894=CARTESIAN_POINT ( 'NONE',  ( 5.875877563635198975, -2.119900239643329964, 0.4680052475878637708 ) ) ;
#142895=CARTESIAN_POINT ( 'NONE',  ( 4.477060521952030747, -0.002618581577289170060, -1.825872481161804561 ) ) ;
#142896=CARTESIAN_POINT ( 'NONE',  ( 2.641395077882052966, 1.795597516233004232, -0.7905247784146393064 ) ) ;
#142897=CARTESIAN_POINT ( 'NONE',  ( 6.368375629516933145, -2.076896536817146810, -0.4110353314962181259 ) ) ;
#142900=CARTESIAN_POINT ( 'NONE',  ( 2.965608807194367813, -1.734805745614193873, -1.219131234129526398 ) ) ;
#142903=EDGE_CURVE ( 'NONE', #43199, #40760, #206238, .T. ) ;
#142905=CARTESIAN_POINT ( 'NONE',  ( 0.2861044793709514589, -1.271156181823060560, -1.634742764404630844 ) ) ;
#142908=CARTESIAN_POINT ( 'NONE',  ( 3.844553043330910747, 1.187701353711614338, -1.876932147738763268 ) ) ;
#142910=CARTESIAN_POINT ( 'NONE',  ( 1.090962482291182312, -0.5517420707249369727, 2.231415953587682299 ) ) ;
#142912=CARTESIAN_POINT ( 'NONE',  ( 0.2507196182260813533, -0.4238382354822354259, -1.922440920834954436 ) ) ;
#142915=CARTESIAN_POINT ( 'NONE',  ( 0.1333542156527295908, 7.629137130509112907, -2.645925523406994717 ) ) ;
#142916=CARTESIAN_POINT ( 'NONE',  ( 6.022987620897008121, -1.731432113864934674, 0.6267441317700100933 ) ) ;
#142918=CARTESIAN_POINT ( 'NONE',  ( -0.2104748580754166321, -0.006608320950486632102, -2.103482951484026309 ) ) ;
#142919=CARTESIAN_POINT ( 'NONE',  ( 2.889346415704593607, 1.218289440699829473, 1.221169829160633435 ) ) ;
#142920=CARTESIAN_POINT ( 'NONE',  ( 1.235564962061060035, 0.5807501988173838781, -1.931125984888550695 ) ) ;
#142921=CARTESIAN_POINT ( 'NONE',  ( 3.147439182535469726, 1.035885224147353512, 2.052142740569740109 ) ) ;
#142922=CARTESIAN_POINT ( 'NONE',  ( 2.566018446761752170, 2.219231934913689308, -0.4390887803658559130 ) ) ;
#142923=CARTESIAN_POINT ( 'NONE',  ( 5.777981411418616098, 1.253425007971820326, 1.692306578934036798 ) ) ;
#142925=CARTESIAN_POINT ( 'NONE',  ( 3.198275679207917666, -0.5104862868050319413, -1.694526722652128781 ) ) ;
#142927=CARTESIAN_POINT ( 'NONE',  ( 6.093372230586791893, -0.7761969640797984349, 2.157113249652943932 ) ) ;
#142928=CARTESIAN_POINT ( 'NONE',  ( 4.400242069895500485, 1.421654421768648868, -1.169904355399861595 ) ) ;
#142932=CARTESIAN_POINT ( 'NONE',  ( 4.277398745584213735, 1.430588233724191083, 1.660156109410643177 ) ) ;
#142935=CARTESIAN_POINT ( 'NONE',  ( 5.283670394142272464, -1.967056725255760474, 0.6460906113585006549 ) ) ;
#142936=CARTESIAN_POINT ( 'NONE',  ( 0.2160302486270138655, 1.032475520995678853, -1.731998313101141163 ) ) ;
#142939=CARTESIAN_POINT ( 'NONE',  ( 3.387250987759330645, 1.741285041988534621, -0.8245012487104221854 ) ) ;
#142942=CARTESIAN_POINT ( 'NONE',  ( 0.5279477311770188752, -0.3182371573221299266, 2.198381937975202760 ) ) ;
#142952=CARTESIAN_POINT ( 'NONE',  ( 1.152704166800899932, -0.4732522875653189520, -1.903817266927515961 ) ) ;
#142955=CARTESIAN_POINT ( 'NONE',  ( 5.775826483351648832, -1.914393393812302113, 0.4282712878391075062 ) ) ;
#142958=CARTESIAN_POINT ( 'NONE',  ( 6.139563164240942506, -1.562336469324271837, -1.494251390645913613 ) ) ;
#142960=EDGE_LOOP ( 'NONE', ( #150233, #57029, #133431, #157777 ) ) ;
#142962=CARTESIAN_POINT ( 'NONE',  ( 0.1747926744264660381, 0.006858446013176254172, -1.855468577918440776 ) ) ;
#142963=CARTESIAN_POINT ( 'NONE',  ( 6.292339289836506033, -1.631180892843343999, 0.5882027141154468897 ) ) ;
#142965=CARTESIAN_POINT ( 'NONE',  ( 2.665787806004877414, 1.174844384069907655, 1.849873475113596566 ) ) ;
#142966=CARTESIAN_POINT ( 'NONE',  ( 4.700386263483860461, -2.306923794945021200, -0.06181454844297362694 ) ) ;
#142967=CARTESIAN_POINT ( 'NONE',  ( 5.448532837019475217, 0.5942636223626071024, 1.973259177745954718 ) ) ;
#142968=CARTESIAN_POINT ( 'NONE',  ( 1.095531938664672911, -1.942124713061957220, -0.0005026242578913541230 ) ) ;
#142971=CARTESIAN_POINT ( 'NONE',  ( 4.711248855110969913, 1.761570823303935551, -1.180294879073326308 ) ) ;
#142973=CARTESIAN_POINT ( 'NONE',  ( 2.549454116737331244, -1.388485404012842261, 1.462446031800922253 ) ) ;
#142975=CARTESIAN_POINT ( 'NONE',  ( 5.544034191846948900, 0.8990280053539388971, -2.015528879820461583 ) ) ;
#142978=CARTESIAN_POINT ( 'NONE',  ( 0.2053145577999641036, -0.4904175937916722128, 1.758528939493007481 ) ) ;
#142981=CARTESIAN_POINT ( 'NONE',  ( 6.639320575229282539, 7.629137130509070275, 2.703262396134015866 ) ) ;
#142984=CARTESIAN_POINT ( 'NONE',  ( 5.243067039532245843, -1.768777590322716309, 1.057421601032474623 ) ) ;
#142989=CARTESIAN_POINT ( 'NONE',  ( 4.740881522827352867, 1.933304458870839238, 0.5843455605825734755 ) ) ;
#142996=CARTESIAN_POINT ( 'NONE',  ( 4.241127833599818153, -1.794087422336073878, 1.013995622381487216 ) ) ;
#142997=CARTESIAN_POINT ( 'NONE',  ( 2.408827471728996361, -1.163269702728772392, -1.646838680093346996 ) ) ;
#143003=CARTESIAN_POINT ( 'NONE',  ( 3.356795910091507906, -0.8196482158769199389, 1.842165019812888271 ) ) ;
#143004=CARTESIAN_POINT ( 'NONE',  ( 2.431387202150552707, 0.8680758514147070004, -1.623638265414374171 ) ) ;
#143005=CARTESIAN_POINT ( 'NONE',  ( 1.278406981455294744, 1.378070038918308038, 1.850917983980376658 ) ) ;
#143007=CARTESIAN_POINT ( 'NONE',  ( 2.073706595668877384, 2.069181010895416950, -0.6253580070983978390 ) ) ;
#143010=CARTESIAN_POINT ( 'NONE',  ( 2.864987100074483539, -0.7226686165877260759, 2.181857903572166801 ) ) ;
#143014=CARTESIAN_POINT ( 'NONE',  ( 1.692057038649401601, -1.861345348035767344, -0.1864469194169729449 ) ) ;
#143016=CARTESIAN_POINT ( 'NONE',  ( 5.436387729582301098, 1.942169232299725046, 0.3377773032272758380 ) ) ;
#143020=CARTESIAN_POINT ( 'NONE',  ( 0.4697016844467936103, 0.2121168557088908557, -2.196667960996725011 ) ) ;
#143021=CARTESIAN_POINT ( 'NONE',  ( 6.197728532230423859, -1.496850047335227085, -1.430563974149069661 ) ) ;
#143024=CARTESIAN_POINT ( 'NONE',  ( 6.639320575229232801, 7.629137130509035636, 2.803262396134009737 ) ) ;
#143025=CARTESIAN_POINT ( 'NONE',  ( 4.627780688875618331, -1.211982541104269062, -1.554853849032981072 ) ) ;
#143026=CARTESIAN_POINT ( 'NONE',  ( 6.135022435551370279, 1.886083186425246971, 0.7231739236989165320 ) ) ;
#143027=CARTESIAN_POINT ( 'NONE',  ( 4.723409996707597536, -0.1167165639803491167, 2.304856601038312913 ) ) ;
#143028=CARTESIAN_POINT ( 'NONE',  ( 3.467685518289661317, -0.4070155273973393717, 2.021854410566482407 ) ) ;
#143037=CARTESIAN_POINT ( 'NONE',  ( 5.512245374570181156, 2.168932156859445737, -0.1011643165890318136 ) ) ;
#143039=CARTESIAN_POINT ( 'NONE',  ( 3.983814121021773680, -1.821778379405362136, -0.2661574599523569007 ) ) ;
#143042=CARTESIAN_POINT ( 'NONE',  ( 5.882419586753742102, -0.3201050945752722532, -2.167950725039065052 ) ) ;
#143044=CARTESIAN_POINT ( 'NONE',  ( 0.2985908658455891929, -2.261944659375872302, -0.05357643010404227607 ) ) ;
#143050=CARTESIAN_POINT ( 'NONE',  ( 1.076598688339102772, -0.03801472141184288056, -1.769612961288852926 ) ) ;
#143051=CARTESIAN_POINT ( 'NONE',  ( 5.162748661275342599, 0.5863960615675645194, 1.925778112416365317 ) ) ;
#143053=CARTESIAN_POINT ( 'NONE',  ( 4.665121749186112332, -1.880042215448823661, -0.9491155671061396459 ) ) ;
#143054=CARTESIAN_POINT ( 'NONE',  ( 3.515159831171112970, -1.768693170575957874, 0.7362056930131228860 ) ) ;
#143056=CARTESIAN_POINT ( 'NONE',  ( 4.580490420436008847, 1.213483934061266201, -1.551205257841874241 ) ) ;
#143057=CARTESIAN_POINT ( 'NONE',  ( 5.431901110126942989, -1.969610648168946376, 0.4466083225366457854 ) ) ;
#143058=CARTESIAN_POINT ( 'NONE',  ( 1.428351348257720588, 1.801920623737063520, 0.5021531274154652502 ) ) ;
#143059=CARTESIAN_POINT ( 'NONE',  ( 5.373588365490253871, 1.660756567380991866, -0.4657003604296525157 ) ) ;
#143060=CARTESIAN_POINT ( 'NONE',  ( 1.142663480069527671, 1.843847066288730074, 0.5072560978593986247 ) ) ;
#143062=CARTESIAN_POINT ( 'NONE',  ( 1.032169062358662348, -1.402649970393770484, -1.703791656331831605 ) ) ;
#143065=CARTESIAN_POINT ( 'NONE',  ( 6.672321430365630412, -0.9237476215336395402, -1.730755693189582667 ) ) ;
#143073=CARTESIAN_POINT ( 'NONE',  ( 1.662640112210824306, -0.7432673875312334477, -1.932532381715674097 ) ) ;
#143078=CARTESIAN_POINT ( 'NONE',  ( 6.199870563505585963, 1.461971410283597894, 1.536153618249151309 ) ) ;
#143083=CARTESIAN_POINT ( 'NONE',  ( 5.237657596305253627, -1.897407540178517094, -0.6818907625677357309 ) ) ;
#143085=CARTESIAN_POINT ( 'NONE',  ( 4.962082351039136086, -1.058791762104252632, 1.596325305674146433 ) ) ;
#143087=CARTESIAN_POINT ( 'NONE',  ( 2.771223791512751333, 2.080116120148074010, -0.6901165687889163625 ) ) ;
#143091=CARTESIAN_POINT ( 'NONE',  ( 5.326436552476821795, -0.9091558477445594866, -1.796327993944699219 ) ) ;
#143092=CARTESIAN_POINT ( 'NONE',  ( 1.670022949053862948, 1.907054940702715085, -0.1439945843566131367 ) ) ;
#143095=CARTESIAN_POINT ( 'NONE',  ( -0.08826282632121498772, -1.242921985031696153, -1.588411632956095110 ) ) ;
#143097=CARTESIAN_POINT ( 'NONE',  ( 3.948837864290375421, -1.739349124335771712, -1.159800787976144720 ) ) ;
#143099=CARTESIAN_POINT ( 'NONE',  ( 1.553258647468837461, 0.5056154618373939202, -1.648988316134043286 ) ) ;
#143101=CARTESIAN_POINT ( 'NONE',  ( 6.345950370838201238, -1.386202306585911925, -1.604841549997563455 ) ) ;
#143109=CARTESIAN_POINT ( 'NONE',  ( 2.297251093426439628, 1.655750149966995544, -0.7352264245090130990 ) ) ;
#143113=CIRCLE ( 'NONE', #191442, 0.05000000000000059258 ) ;
#143116=CARTESIAN_POINT ( 'NONE',  ( 4.125510307337266980, -0.3055505145112321075, 1.785335377935037826 ) ) ;
#143120=CARTESIAN_POINT ( 'NONE',  ( 3.701460696238024539, -1.407827198975480032, -1.217257945129922803 ) ) ;
#143121=CARTESIAN_POINT ( 'NONE',  ( 2.091283074759576532, -0.4175699524238601357, 1.869371669076219211 ) ) ;
#143122=CARTESIAN_POINT ( 'NONE',  ( 0.8151338971811080691, -0.2727355552937099636, 1.804975678908596226 ) ) ;
#143129=CARTESIAN_POINT ( 'NONE',  ( 5.823099318722479545, -1.778931037738925802, -0.8454068362369684397 ) ) ;
#143133=CARTESIAN_POINT ( 'NONE',  ( 0.4278232814946582585, 1.072867435734598196, -1.794206126505201837 ) ) ;
#143135=CARTESIAN_POINT ( 'NONE',  ( 5.086904980214876915, -0.2357887182157791250, -1.911833357141810241 ) ) ;
#143137=CARTESIAN_POINT ( 'NONE',  ( 1.764397251013736234, -1.293498944356825664, 1.288518760371157201 ) ) ;
#143138=CARTESIAN_POINT ( 'NONE',  ( 1.612255294781844706, -2.189918024983358080, 0.2725913246661854084 ) ) ;
#143140=CARTESIAN_POINT ( 'NONE',  ( 0.8614045922798494459, -1.509235727096858826, -1.174430983434850972 ) ) ;
#143143=CARTESIAN_POINT ( 'NONE',  ( 0.5198876536083548716, 1.948639688611382148, -0.2852860490613322031 ) ) ;
#143144=CARTESIAN_POINT ( 'NONE',  ( 2.964326597902953608, -1.795398894311397209, -0.7408281928331180710 ) ) ;
#143145=CARTESIAN_POINT ( 'NONE',  ( 1.036482258494644038, 1.943774389176852857, -0.5350038931242264706 ) ) ;
#143147=CARTESIAN_POINT ( 'NONE',  ( 5.559367761144698328, 1.520187721101939671, 1.073055572604255214 ) ) ;
#143154=CARTESIAN_POINT ( 'NONE',  ( 2.507599501126521524, -2.167277876680247850, 0.3246147914140809498 ) ) ;
#143158=CARTESIAN_POINT ( 'NONE',  ( 3.176193443437186126, -1.086901434622984830, 1.466744820640853098 ) ) ;
#143164=CARTESIAN_POINT ( 'NONE',  ( 1.066875820281657949, -1.741210523058086324, -0.8246449397346886645 ) ) ;
#143165=CARTESIAN_POINT ( 'NONE',  ( 5.225427317040848507, 0.1961275920050585819, -1.951957996302315257 ) ) ;
#143169=CARTESIAN_POINT ( 'NONE',  ( 5.442994344319362021, -1.727133847215430729, -1.348975639928217118 ) ) ;
#143173=CARTESIAN_POINT ( 'NONE',  ( 4.487213805514509879, 0.09639557921744396074, 2.068113308821089902 ) ) ;
#143178=CARTESIAN_POINT ( 'NONE',  ( 3.692236332591435577, 1.971970683719068695, 1.181021729054130054 ) ) ;
#143185=CARTESIAN_POINT ( 'NONE',  ( 3.855361883123554989, 1.927135149742021047, -0.2389370807101970084 ) ) ;
#143189=CARTESIAN_POINT ( 'NONE',  ( 5.343983030329363615, -1.218012673290536974, -1.474316871017400166 ) ) ;
#143190=CARTESIAN_POINT ( 'NONE',  ( 5.913083851878619512, 1.523424462977729599, 0.8087443918367646090 ) ) ;
#143191=CARTESIAN_POINT ( 'NONE',  ( 4.856657812281613751, -1.900414607462055816, -0.6748505307947461063 ) ) ;
#143193=CARTESIAN_POINT ( 'NONE',  ( 1.946200625105892312, 0.8427435547867198062, -2.039832142532324255 ) ) ;
#143196=CARTESIAN_POINT ( 'NONE',  ( 1.851626064562774010, 2.084957031469181654, -0.1549042654368226746 ) ) ;
#143197=CARTESIAN_POINT ( 'NONE',  ( 6.696582006438861256, -0.4751199114862921791, -1.704715723353955381 ) ) ;
#143199=CARTESIAN_POINT ( 'NONE',  ( 5.818982467333652764, 0.9914020171761170896, -1.755767668913270407 ) ) ;
#143201=CARTESIAN_POINT ( 'NONE',  ( 3.363489724395284597, 2.236470799849974878, -0.5019982374358539223 ) ) ;
#143202=CARTESIAN_POINT ( 'NONE',  ( 1.517106797927396444, -0.9646358079543941866, -1.448293472534349702 ) ) ;
#143203=CARTESIAN_POINT ( 'NONE',  ( 2.689816194747224110, 2.012238202079220439, -0.6693303307304664385 ) ) ;
#143205=CARTESIAN_POINT ( 'NONE',  ( 0.7722569432341424012, -1.726285329646786382, 0.1615719764154876226 ) ) ;
#143207=CARTESIAN_POINT ( 'NONE',  ( 1.187708300173949461, -1.176858333569561932, -1.441725857702576219 ) ) ;
#143208=CARTESIAN_POINT ( 'NONE',  ( 1.240952474410524031, -2.118199589774888647, -0.4760015480929754017 ) ) ;
#143209=CARTESIAN_POINT ( 'NONE',  ( 2.958220528980558761, -1.197304571117228100, 1.622486353517027968 ) ) ;
#143210=CARTESIAN_POINT ( 'NONE',  ( 4.843750000000003553, 1.895863743164186710, 0.7852924748297296365 ) ) ;
#143212=CARTESIAN_POINT ( 'NONE',  ( 0.2352082051719720512, -1.762675558584745783, 0.7775455664775063891 ) ) ;
#143214=CARTESIAN_POINT ( 'NONE',  ( 3.516091144284401171, -0.6417545297995127518, 2.126723297420398673 ) ) ;
#143220=CARTESIAN_POINT ( 'NONE',  ( 4.703538834289092030, -1.515240342570793430, -1.246145567450624991 ) ) ;
#143224=CARTESIAN_POINT ( 'NONE',  ( 5.378307924748570557, -1.263187946576078247, 1.876752126472463367 ) ) ;
#143225=CARTESIAN_POINT ( 'NONE',  ( 2.189955769151647580, -1.345473201219016701, -1.563545076720110227 ) ) ;
#143229=CARTESIAN_POINT ( 'NONE',  ( 3.637841704585748293, 0.8437669887123750989, -1.669527271503386201 ) ) ;
#143230=CARTESIAN_POINT ( 'NONE',  ( 2.127222352579770881, 0.3811697317757706815, 1.691523546451817683 ) ) ;
#143231=CARTESIAN_POINT ( 'NONE',  ( 0.1348729467166914497, 0.4002676433968958558, 2.257031873882467732 ) ) ;
#143232=CARTESIAN_POINT ( 'NONE',  ( 0.8509352111321017986, 0.6423128672003556305, 2.111239891224323983 ) ) ;
#143233=CARTESIAN_POINT ( 'NONE',  ( 4.100566281481184738, -0.6756360485904688851, -2.053482476349233643 ) ) ;
#143234=CARTESIAN_POINT ( 'NONE',  ( 5.472584303614713264, -0.04973451981254246174, -1.941474127069875433 ) ) ;
#143236=CARTESIAN_POINT ( 'NONE',  ( 0.2187500114561492792, -0.7852927567033060052, 1.895863743164095894 ) ) ;
#143238=CARTESIAN_POINT ( 'NONE',  ( -0.2046613956954954905, -0.1581703332043625232, -2.086340352340488646 ) ) ;
#143240=CARTESIAN_POINT ( 'NONE',  ( 5.731092321990707283, 2.014232586630093191, 0.09613807139101374077 ) ) ;
#143244=CARTESIAN_POINT ( 'NONE',  ( 3.422296110638740174, 1.157362003623555236, -1.411967061744797691 ) ) ;
#143245=CARTESIAN_POINT ( 'NONE',  ( 2.239569982544288518, -1.971322999760493300, 0.9919465654871155724 ) ) ;
#143246=ORIENTED_EDGE ( 'NONE', *, *, #204596, .F. ) ;
#143250=CARTESIAN_POINT ( 'NONE',  ( 1.072527844217635584, 0.8224262283116140493, 1.844967818783457725 ) ) ;
#143251=CARTESIAN_POINT ( 'NONE',  ( 1.506653248757179320, -2.110590818861147078, -0.2044851626497797559 ) ) ;
#143253=ORIENTED_EDGE ( 'NONE', *, *, #204318, .T. ) ;
#143255=CARTESIAN_POINT ( 'NONE',  ( 2.395144146474707636, -1.664902989962243174, 0.8314883405181148213 ) ) ;
#143257=CARTESIAN_POINT ( 'NONE',  ( 0.3741789627117291239, 1.245922373857488274, 1.766349570875298758 ) ) ;
#143258=CARTESIAN_POINT ( 'NONE',  ( 6.276017556857773627, 1.753032240926259311, -0.9962986157117934560 ) ) ;
#143262=CARTESIAN_POINT ( 'NONE',  ( 4.406759617291758246, 1.409692282476209924, -1.160130723419292353 ) ) ;
#143266=CARTESIAN_POINT ( 'NONE',  ( 6.169296033003512925, -0.7230314695168098549, -1.882185070641306801 ) ) ;
#143267=CARTESIAN_POINT ( 'NONE',  ( 6.281194495005370193, 1.273289214079580622, 1.330099835651930684 ) ) ;
#143268=CARTESIAN_POINT ( 'NONE',  ( -0.02299388927986567924, 0.7252709198883336983, -1.993311845943528837 ) ) ;
#143269=CARTESIAN_POINT ( 'NONE',  ( 4.881611394917170443, 2.154576904714616603, -0.8270325966449257882 ) ) ;
#143271=CARTESIAN_POINT ( 'NONE',  ( 0.2806372051839324810, -1.998264896860867834, -0.5032370445638265632 ) ) ;
#143272=CARTESIAN_POINT ( 'NONE',  ( 2.208448867685277150, 1.735655609654564113, 0.8713670519163093653 ) ) ;
#143274=CARTESIAN_POINT ( 'NONE',  ( 5.220190998831037987, -1.937735447606624639, -1.235822935930783517 ) ) ;
#143277=CARTESIAN_POINT ( 'NONE',  ( 4.926551758443064699, 1.790249073151507497, 0.5424879929923772659 ) ) ;
#143279=CARTESIAN_POINT ( 'NONE',  ( 2.900541297466651347, -1.884798985816903860, -0.3226963764228693576 ) ) ;
#143282=CARTESIAN_POINT ( 'NONE',  ( 4.231241840954825584, 0.1069408422738199749, 2.204416794138922331 ) ) ;
#143283=CARTESIAN_POINT ( 'NONE',  ( 6.983263157960370116, 2.036707217602062414, 2.350489458799970066 ) ) ;
#143286=CARTESIAN_POINT ( 'NONE',  ( 2.214082964306641532, -0.9260232682030484774, -1.740301080291997149 ) ) ;
#143287=CARTESIAN_POINT ( 'NONE',  ( 1.360874125193665130, 0.9374058560891560532, 2.108772699047257948 ) ) ;
#143288=CARTESIAN_POINT ( 'NONE',  ( 2.963279974173158138, 1.655882904019840840, 1.051842618152734499 ) ) ;
#143290=CARTESIAN_POINT ( 'NONE',  ( 6.086800983681886379, 1.986285820840045124, 0.5554444937589071429 ) ) ;
#143292=CARTESIAN_POINT ( 'NONE',  ( 3.784388871581423786, -0.6371526190629381858, -1.913262240507591416 ) ) ;
#143298=CARTESIAN_POINT ( 'NONE',  ( 2.026474435558190734, 1.113403481674969608, 1.863675736879222278 ) ) ;
#143302=CARTESIAN_POINT ( 'NONE',  ( 2.020564968092851021, 1.743606242109306148, 0.6777753874912320065 ) ) ;
#143303=CARTESIAN_POINT ( 'NONE',  ( 0.2806372051839324810, -1.998264896860867834, -0.5032370445638265632 ) ) ;
#143304=CARTESIAN_POINT ( 'NONE',  ( 0.07755575628183573877, 1.325091491099144259, -2.441202027401535357 ) ) ;
#143305=CARTESIAN_POINT ( 'NONE',  ( 6.827182134110178602, 3.710826266403470797, 2.225597045202745594 ) ) ;
#143308=CARTESIAN_POINT ( 'NONE',  ( 1.752457306817490457, 1.891635876823925200, 0.2793096714826873161 ) ) ;
#143309=CARTESIAN_POINT ( 'NONE',  ( 3.854177328971124084, 0.6370089842938561064, 1.651420920916975232 ) ) ;
#143310=CARTESIAN_POINT ( 'NONE',  ( 1.348149404638066873, 0.9416913409402676294, -1.664245089135652389 ) ) ;
#143312=CARTESIAN_POINT ( 'NONE',  ( 6.398046686924231174, -0.9077857338794625974, -1.686868998638735073 ) ) ;
#143314=CARTESIAN_POINT ( 'NONE',  ( 1.240778115703184303, -2.019486815914430355, -0.4554155650244652853 ) ) ;
#143316=CARTESIAN_POINT ( 'NONE',  ( 5.172658500931742509, -1.761684834526537680, -0.6294727512598657926 ) ) ;
#143317=CARTESIAN_POINT ( 'NONE',  ( 1.646812808029130215, -1.543121136568927243, 0.9753659028155501343 ) ) ;
#143318=CARTESIAN_POINT ( 'NONE',  ( 5.321004863918796346, 2.037934703285459115, 0.8473243778325880715 ) ) ;
#143321=CARTESIAN_POINT ( 'NONE',  ( 3.437984354829794142, 1.306305779046763149, 1.596332929251530253 ) ) ;
#143328=CARTESIAN_POINT ( 'NONE',  ( 5.881320641815353412, -0.05461762546566179682, 2.069818975884097689 ) ) ;
#143331=CARTESIAN_POINT ( 'NONE',  ( 3.110779230992101407, 1.568002374463087989, -1.488160049990403078 ) ) ;
#143333=CARTESIAN_POINT ( 'NONE',  ( 2.860025901456241471, 0.7249204854099660089, -1.885284610270787642 ) ) ;
#143334=CARTESIAN_POINT ( 'NONE',  ( 6.620655732516649294, 0.5674144795907026806, 2.226195167976598110 ) ) ;
#143339=CARTESIAN_POINT ( 'NONE',  ( 0.9015777671340443611, -1.966303774932298021, 0.4465067697373495403 ) ) ;
#143341=CARTESIAN_POINT ( 'NONE',  ( 6.515165533258342023, -2.126321577054360201, 0.5302794918827999915 ) ) ;
#143343=CARTESIAN_POINT ( 'NONE',  ( 5.150612376422202487, 1.885107930906554152, 0.3209214958604587054 ) ) ;
#143347=CARTESIAN_POINT ( 'NONE',  ( 3.198842376697589085, 1.824128004127192337, 0.8596145101084637918 ) ) ;
#143350=CARTESIAN_POINT ( 'NONE',  ( 4.875862107049974803, 0.9950566627994448243, 1.408581599115072747 ) ) ;
#143354=CARTESIAN_POINT ( 'NONE',  ( 4.903500725120335524, -0.5004011548357701900, 1.802273645872286334 ) ) ;
#143355=CARTESIAN_POINT ( 'NONE',  ( 1.358353136502857161, -2.070434559563800736, -0.003889755252693693176 ) ) ;
#143358=CARTESIAN_POINT ( 'NONE',  ( 6.358062532015329005, 0.6862230018901045447, -1.676680497432983641 ) ) ;
#143361=CARTESIAN_POINT ( 'NONE',  ( -0.1231740688493014324, -1.618022042794277748, -0.8147913963296258277 ) ) ;
#143364=CARTESIAN_POINT ( 'NONE',  ( 2.642740014504705748, -1.821389600533462216, 1.218302608185666491 ) ) ;
#143366=CARTESIAN_POINT ( 'NONE',  ( 0.8187140321147531319, -1.423520202335259999, 1.350257566363553208 ) ) ;
#143368=CARTESIAN_POINT ( 'NONE',  ( 4.675340500466128368, 1.422229311605049507, 1.283493733622777189 ) ) ;
#143376=CARTESIAN_POINT ( 'NONE',  ( 2.272554088390315030, -1.330374092946192688, 1.703740541667747133 ) ) ;
#143380=CARTESIAN_POINT ( 'NONE',  ( 5.069292194207453583, 0.1776299070984053985, -1.816928125296768393 ) ) ;
#143382=CARTESIAN_POINT ( 'NONE',  ( 0.7374959811429316892, -1.390993636481972606, -1.397171308748794250 ) ) ;
#143383=CARTESIAN_POINT ( 'NONE',  ( 3.603681638446740720, 1.388520161702249567, 1.315275747533505069 ) ) ;
#143386=CARTESIAN_POINT ( 'NONE',  ( 4.017982430692658369, 1.954955499905395522, -0.2386041268068790633 ) ) ;
#143388=CARTESIAN_POINT ( 'NONE',  ( 6.216353431943378638, 1.813724785205795609, 0.6947406154040984827 ) ) ;
#143395=CARTESIAN_POINT ( 'NONE',  ( 4.371672787583542608, 0.4156390277068115480, -1.866406306929219605 ) ) ;
#143398=CARTESIAN_POINT ( 'NONE',  ( 0.1654306582001447423, -1.972458130798220299, -0.9897840116655575171 ) ) ;
#143399=SURFACE_STYLE_USAGE ( .BOTH. , #49854 ) ;
#143400=CARTESIAN_POINT ( 'NONE',  ( 5.496744759480266751, -1.964553546248495541, -0.4387526145827134183 ) ) ;
#143401=CARTESIAN_POINT ( 'NONE',  ( 0.1331565106231328843, 0.003911343561965873426, -1.946049565259087455 ) ) ;
#143402=CARTESIAN_POINT ( 'NONE',  ( 6.516225534515442952, -0.8655890497146904172, -1.607451055071248636 ) ) ;
#143403=CARTESIAN_POINT ( 'NONE',  ( 5.594935472981866553, 1.780666063871166882, 0.9463038388278843804 ) ) ;
#143404=CARTESIAN_POINT ( 'NONE',  ( 1.979048004138800998, 1.930994533390210544, 0.7472069620131777112 ) ) ;
#143417=CARTESIAN_POINT ( 'NONE',  ( 3.814867129904021770, 0.9234608866974923780, -1.467580195302587986 ) ) ;
#143419=CARTESIAN_POINT ( 'NONE',  ( 1.147426569842596722, 1.827566109494669577, -0.9725325914680116313 ) ) ;
#143420=EDGE_CURVE ( 'NONE', #21442, #8341, #55730, .T. ) ;
#143421=CARTESIAN_POINT ( 'NONE',  ( 3.761412437133329068, 1.992871936191454418, -0.7152352101782408766 ) ) ;
#143424=CARTESIAN_POINT ( 'NONE',  ( 6.895378825052528526, -1.852007112603266670, 0.9253362530580526712 ) ) ;
#143429=CARTESIAN_POINT ( 'NONE',  ( 3.591970686985697547, -2.289577047158963374, -0.1132367156824985732 ) ) ;
#143430=CARTESIAN_POINT ( 'NONE',  ( 0.1701549220758866166, -1.195335944658926230, 1.380069390326914336 ) ) ;
#143431=CARTESIAN_POINT ( 'NONE',  ( 3.603681638446740720, 1.388520161702249567, 1.315275747533505069 ) ) ;
#143435=CARTESIAN_POINT ( 'NONE',  ( 1.810793108869549917, -0.5408357282137785660, -1.939109541719201912 ) ) ;
#143436=CARTESIAN_POINT ( 'NONE',  ( 2.043732491806522056, 1.349072470436333715, 1.424505092005624807 ) ) ;
#143440=CARTESIAN_POINT ( 'NONE',  ( 5.261704619121490900, 1.029696775897260830, 1.819396322279245304 ) ) ;
#143441=CARTESIAN_POINT ( 'NONE',  ( 3.590472238826939666, -0.3446705786002961514, -1.735762067166376710 ) ) ;
#143444=CARTESIAN_POINT ( 'NONE',  ( 0.05887529153619439071, -1.959562692596405364, -0.9812908054248059564 ) ) ;
#143445=CARTESIAN_POINT ( 'NONE',  ( 6.035049474595155949, -1.265358352104806183, -1.195092038424966363 ) ) ;
#143448=CARTESIAN_POINT ( 'NONE',  ( 4.798016402085652388, -1.585019518093808699, 0.7031974489903334291 ) ) ;
#143449=CARTESIAN_POINT ( 'NONE',  ( 6.373493056145338009, -0.2723341383174918695, 2.153988726128319264 ) ) ;
#143451=CARTESIAN_POINT ( 'NONE',  ( 0.5677576367011258895, 1.426771234092726104, 1.564575111376417915 ) ) ;
#143452=CARTESIAN_POINT ( 'NONE',  ( 5.656250000000004441, -1.895863743163955339, 0.7852924748302813063 ) ) ;
#143454=CARTESIAN_POINT ( 'NONE',  ( 3.311465173828963326, -0.3771673786017637475, 1.888946036755128288 ) ) ;
#143456=CARTESIAN_POINT ( 'NONE',  ( 0.3115808214643934204, 1.843292235811417878, -1.239274738845694390 ) ) ;
#143458=CARTESIAN_POINT ( 'NONE',  ( -0.1408020194050146334, 0.2351808081714431564, -2.134421755367508666 ) ) ;
#143461=CARTESIAN_POINT ( 'NONE',  ( 3.141495721539554697, 0.05644213937440466927, 2.220748567232306847 ) ) ;
#143468=CARTESIAN_POINT ( 'NONE',  ( 0.1764080092822375156, 1.496053712750060383, 1.352152247781977179 ) ) ;
#143470=CARTESIAN_POINT ( 'NONE',  ( 5.529752758335351182, 1.988887524167002985, -0.5466100825702590038 ) ) ;
#143476=CARTESIAN_POINT ( 'NONE',  ( 0.7722622890447777833, -1.663610408097391691, -0.6040080933595278756 ) ) ;
#143477=CARTESIAN_POINT ( 'NONE',  ( 5.713412806352172524, 1.673543110082301721, 0.4542079487798825199 ) ) ;
#143478=CARTESIAN_POINT ( 'NONE',  ( 5.302228144868663229, 1.312797389530523162, -1.142775443803839108 ) ) ;
#143479=CARTESIAN_POINT ( 'NONE',  ( 3.544716187562162446, -1.873399702441876480, 1.320855843532109608 ) ) ;
#143481=CARTESIAN_POINT ( 'NONE',  ( 1.974305314296275649, -0.08955604370030831318, -1.839086841257123073 ) ) ;
#143484=CARTESIAN_POINT ( 'NONE',  ( 1.975362765405625609, 1.747911882041437659, -0.5268472171036930884 ) ) ;
#143485=CARTESIAN_POINT ( 'NONE',  ( 3.006482587178582300, -1.942541511447487990, 0.5404910644229294903 ) ) ;
#143488=CARTESIAN_POINT ( 'NONE',  ( 4.753012104044548991, -1.692955597047377747, 1.252381512178860401 ) ) ;
#143492=CARTESIAN_POINT ( 'NONE',  ( 2.471216696211364638, 1.848302923701108158, 0.9330170062570308787 ) ) ;
#143495=CARTESIAN_POINT ( 'NONE',  ( 4.565154201998150363, -1.702539431995837349, 1.263830167178958463 ) ) ;
#143496=CARTESIAN_POINT ( 'NONE',  ( 0.01214912391013078102, -0.8215866570660257384, -1.740624652096602221 ) ) ;
#143503=CARTESIAN_POINT ( 'NONE',  ( 6.363548717301088509, -1.704009271243651868, -1.262090224194649446 ) ) ;
#143504=CARTESIAN_POINT ( 'NONE',  ( 1.553890309278640025, 0.6119248022173563450, -2.015079113363055452 ) ) ;
#143507=CARTESIAN_POINT ( 'NONE',  ( 6.438329693799461850, -0.9962124079390155540, 1.571646734037221105 ) ) ;
#143513=CARTESIAN_POINT ( 'NONE',  ( 0.3168469074051638024, -0.7203255543706194031, -1.994627023381766673 ) ) ;
#143516=CARTESIAN_POINT ( 'NONE',  ( 2.594135478747404022, 0.9273930874063830432, -1.728848471177657942 ) ) ;
#143517=CARTESIAN_POINT ( 'NONE',  ( 1.587033755777764510, -0.3173376132806354222, -2.138153673666403964 ) ) ;
#143522=CARTESIAN_POINT ( 'NONE',  ( 2.987300135396570688, 1.631410314640189929, 0.5874552976607245736 ) ) ;
#143523=CARTESIAN_POINT ( 'NONE',  ( 2.167524683544871600, -1.071679988950867024, 1.371128027196461208 ) ) ;
#143527=CARTESIAN_POINT ( 'NONE',  ( 6.925078400183549476, 6.033022220673083247, 2.839235739982972184 ) ) ;
#143529=CARTESIAN_POINT ( 'NONE',  ( 1.516417288619626769, 1.325465413702779482, -1.459542524610158098 ) ) ;
#143531=CARTESIAN_POINT ( 'NONE',  ( 5.994389040191065554, -1.017321598621454548, 1.619163160827830517 ) ) ;
#143538=CARTESIAN_POINT ( 'NONE',  ( 1.471359524643547134, -1.733428207583002756, -1.036219422855472194 ) ) ;
#143540=CARTESIAN_POINT ( 'NONE',  ( 6.106511577925135548, -0.8227651472764373475, -2.156109995086146647 ) ) ;
#143541=CARTESIAN_POINT ( 'NONE',  ( 6.408651779211167465, 0.6141799454031526828, 1.863335524608072502 ) ) ;
#143542=CARTESIAN_POINT ( 'NONE',  ( 2.905073028004667712, -1.633678134795817360, 1.085783093053994453 ) ) ;
#143544=CARTESIAN_POINT ( 'NONE',  ( 0.9498425221252141393, -1.824119990893595888, -0.8596288560165298298 ) ) ;
#143546=CARTESIAN_POINT ( 'NONE',  ( 0.9544967768389999163, -1.338301201188813572, 1.640804622059524043 ) ) ;
#143549=CARTESIAN_POINT ( 'NONE',  ( 2.501689010688646242, -0.7045654096689784041, -1.701190496055771550 ) ) ;
#143552=CARTESIAN_POINT ( 'NONE',  ( 2.478903650112133317, -1.459102030866548994, 1.539066919819010781 ) ) ;
#143556=CARTESIAN_POINT ( 'NONE',  ( 2.899741356312244722, -0.6498117751948685461, 1.955694574617524495 ) ) ;
#143558=CARTESIAN_POINT ( 'NONE',  ( 0.7316835000789992938, 1.813914744281470925, 0.3150931809976220133 ) ) ;
#143560=CARTESIAN_POINT ( 'NONE',  ( -0.02224634325200240681, 0.6689394325187210111, -2.369055395299427769 ) ) ;
#143563=CARTESIAN_POINT ( 'NONE',  ( 0.3115100037339203487, 1.922317768103290803, 1.083863418116323807 ) ) ;
#143564=CARTESIAN_POINT ( 'NONE',  ( 2.425404053729601550, -0.002036344795489434568, 2.262578821637390547 ) ) ;
#143566=CARTESIAN_POINT ( 'NONE',  ( 2.460951123861610412, -1.504080979915609628, 1.009397298678058164 ) ) ;
#143568=CARTESIAN_POINT ( 'NONE',  ( 3.081152777801674958, 1.513245778044673306, 1.174690267158661872 ) ) ;
#143569=CARTESIAN_POINT ( 'NONE',  ( 4.738769824615551407, -2.007376682328159134, -0.5062664373569197851 ) ) ;
#143571=CARTESIAN_POINT ( 'NONE',  ( 2.061341786089391004, 0.3389245507335619245, -1.941969530725436766 ) ) ;
#143572=CARTESIAN_POINT ( 'NONE',  ( 0.4461525089796612997, 1.920980128883168714, 0.1452595308072956448 ) ) ;
#143573=CARTESIAN_POINT ( 'NONE',  ( 2.781945002432617997, -0.9632652739061451364, 1.603442845774772474 ) ) ;
#143574=CARTESIAN_POINT ( 'NONE',  ( 2.561488099217507308, -2.008522245525693695, -1.136227173556729975 ) ) ;
#143576=CARTESIAN_POINT ( 'NONE',  ( 2.822522581191502677, -1.285663882657582580, 1.345810825326615223 ) ) ;
#143578=CARTESIAN_POINT ( 'NONE',  ( 6.338341894567316892, -1.106718111279564543, 1.740473967980406655 ) ) ;
#143582=CARTESIAN_POINT ( 'NONE',  ( 0.2058769709349675681, -0.5595275159893696726, 2.030311192619388638 ) ) ;
#143585=CARTESIAN_POINT ( 'NONE',  ( 5.624359561864977763, 1.292596479719224645, -1.732379065785584871 ) ) ;
#143586=CARTESIAN_POINT ( 'NONE',  ( 6.516272353977101695, -2.019191618876531091, 0.05163682429563941356 ) ) ;
#143594=CARTESIAN_POINT ( 'NONE',  ( 4.417204035549080920, -1.841734835922325120, 0.8216704330437707426 ) ) ;
#143599=CARTESIAN_POINT ( 'NONE',  ( 6.262596564776618635, -1.532251275270900326, 1.525113613579494709 ) ) ;
#143604=CARTESIAN_POINT ( 'NONE',  ( 0.3685665480608457667, -0.2352240095614567816, -1.901051784579368187 ) ) ;
#143607=CARTESIAN_POINT ( 'NONE',  ( 1.963112949512689553, 0.2966733001828375516, -1.698991974238444946 ) ) ;
#143611=CARTESIAN_POINT ( 'NONE',  ( 1.422737370818322633, -0.05026339470881428795, 1.769212045163440106 ) ) ;
#143612=CARTESIAN_POINT ( 'NONE',  ( 1.559240971068908355, -1.699445492770943478, 1.078823074066703747 ) ) ;
#143614=CARTESIAN_POINT ( 'NONE',  ( 3.856632026064894525, 0.7917978285330304900, 2.060012427959257764 ) ) ;
#143615=CARTESIAN_POINT ( 'NONE',  ( 5.155217109558853039, 1.808899791667990753, -1.200326510068568497 ) ) ;
#143619=CARTESIAN_POINT ( 'NONE',  ( 3.651137946248568689, 0.3127203024623700367, 2.097190470537732221 ) ) ;
#143620=CARTESIAN_POINT ( 'NONE',  ( 2.776970437579088014, 1.727991955821889025, -1.039012595151635354 ) ) ;
#143621=CARTESIAN_POINT ( 'NONE',  ( 3.058660868685322498, 0.4446918012569016643, 1.755998500949424113 ) ) ;
#143628=CARTESIAN_POINT ( 'NONE',  ( 5.971303284387838417, 0.1295235881030691594, -1.821162830480331563 ) ) ;
#143630=CARTESIAN_POINT ( 'NONE',  ( 0.9541331885446997507, -1.212804274533643145, 1.482964625430952976 ) ) ;
#143638=CARTESIAN_POINT ( 'NONE',  ( 5.172814640947125397, -2.034155943344346795, -0.7319064324283753864 ) ) ;
#143641=CARTESIAN_POINT ( 'NONE',  ( 2.900754761704402274, -2.089926006748676457, -0.3584049868644647585 ) ) ;
#143644=CARTESIAN_POINT ( 'NONE',  ( 4.042224286460029958, 1.961553563453529492, 0.1965975345302218569 ) ) ;
#143645=CARTESIAN_POINT ( 'NONE',  ( 0.1936082253880376802, 1.876963271429439750, -0.7284200309826213138 ) ) ;
#143647=CARTESIAN_POINT ( 'NONE',  ( 5.928941916292417957, -1.787427330561262906, 1.134758347235584885 ) ) ;
#143648=CARTESIAN_POINT ( 'NONE',  ( 0.4849360239999983557, 1.980737741294085419, 0.6024896509310638804 ) ) ;
#143649=CARTESIAN_POINT ( 'NONE',  ( 2.238135065718354078, 0.4255327557451081266, 1.894600943326588238 ) ) ;
#143653=CARTESIAN_POINT ( 'NONE',  ( 3.169954053886741008, -1.245012139812958996, 1.679338519663716500 ) ) ;
#143657=CARTESIAN_POINT ( 'NONE',  ( 0.8733459280946423986, 0.3543511941397787801, -1.776278655377810489 ) ) ;
#143659=CARTESIAN_POINT ( 'NONE',  ( 5.268293329372571776, 1.085216321637239023, 1.921556908365213312 ) ) ;
#143661=CARTESIAN_POINT ( 'NONE',  ( 2.714145368365259436, -2.182908968410116834, 0.3227909207665635716 ) ) ;
#143664=CARTESIAN_POINT ( 'NONE',  ( 2.156764536687346467, 0.4205103164258168769, 1.865301821287323136 ) ) ;
#143666=CARTESIAN_POINT ( 'NONE',  ( 5.037584538744971141, 1.933038169019934527, -0.7419538039311264210 ) ) ;
#143669=CARTESIAN_POINT ( 'NONE',  ( 3.397504326804317909, 1.702965868850464082, 1.331369057855802174 ) ) ;
#143670=CARTESIAN_POINT ( 'NONE',  ( 4.405938146338868933, -0.9375679901368579872, -1.981035393479456008 ) ) ;
#143678=CARTESIAN_POINT ( 'NONE',  ( 0.4225002777262388265, -1.427939226333583500, -1.423959630194884696 ) ) ;
#143682=CARTESIAN_POINT ( 'NONE',  ( 6.315297747118990834, -1.772576088781053327, -1.069364167438614732 ) ) ;
#143683=CARTESIAN_POINT ( 'NONE',  ( 4.635331898966036590, -1.760702172612697458, 0.7822757977788937778 ) ) ;
#143684=CARTESIAN_POINT ( 'NONE',  ( 0.3511856949766634095, 0.1948183440376727305, -2.006963311255556714 ) ) ;
#143688=CARTESIAN_POINT ( 'NONE',  ( 3.590635625024854338, 1.920399590389043620, 0.4359694148904534328 ) ) ;
#143689=CARTESIAN_POINT ( 'NONE',  ( 0.4104466507391414387, 1.508250410577081979, -1.590083307377434974 ) ) ;
#143690=CARTESIAN_POINT ( 'NONE',  ( 3.580510235063854019, -1.759844519496515325, -0.4856381957471164745 ) ) ;
#143697=CARTESIAN_POINT ( 'NONE',  ( 1.891909123491273492, -0.4922293657834125313, -1.774144672653771293 ) ) ;
#143698=CARTESIAN_POINT ( 'NONE',  ( 4.904545999335794271, -1.998481532559828189, -0.2423253454618880809 ) ) ;
#143699=CARTESIAN_POINT ( 'NONE',  ( 0.6678281019706671096, -0.7765434158916887375, -2.163364592831273470 ) ) ;
#143700=CARTESIAN_POINT ( 'NONE',  ( 5.190269257085567745, 1.011813749630154691, -1.680575076195559792 ) ) ;
#143704=CARTESIAN_POINT ( 'NONE',  ( 0.2388460773940295212, -2.007853281042128568, -0.5044432775610437902 ) ) ;
#143706=CARTESIAN_POINT ( 'NONE',  ( 1.294599682487684422, 1.707161730183017534, -1.206694161613943272 ) ) ;
#143707=CARTESIAN_POINT ( 'NONE',  ( 6.737169288263022082, -1.578518636041785994, 0.8004799088773879578 ) ) ;
#143709=CARTESIAN_POINT ( 'NONE',  ( -0.2104748580754201015, 5.720428293583295520, -2.697747842008205943 ) ) ;
#143710=CARTESIAN_POINT ( 'NONE',  ( 1.979654113181174901, -1.706931329119738772, -0.3388794841660112689 ) ) ;
#143714=CARTESIAN_POINT ( 'NONE',  ( 1.611479353654057034, -1.712177798104688620, 0.2083697849032482008 ) ) ;
#143715=CARTESIAN_POINT ( 'NONE',  ( 1.927518781310177509, -1.434474475899261581, -1.656937093973806396 ) ) ;
#143716=CARTESIAN_POINT ( 'NONE',  ( 3.756632125300945368, 0.7937082651479386852, 2.059386989456575279 ) ) ;
#143718=CARTESIAN_POINT ( 'NONE',  ( 3.028372864778381413, 1.157752252206078358, 1.836431199091348665 ) ) ;
#143719=CARTESIAN_POINT ( 'NONE',  ( 1.594096589105632011, -1.816728215151931058, -0.1805768397986490248 ) ) ;
#143720=CARTESIAN_POINT ( 'NONE',  ( 2.940728227222836111, -1.600293368184166898, 1.386485470145684351 ) ) ;
#143721=CARTESIAN_POINT ( 'NONE',  ( 6.539320575229279342, 6.038407674219216759, 2.491644695858772796 ) ) ;
#143723=CARTESIAN_POINT ( 'NONE',  ( 3.685359659257981146, 1.661040094275951340, 1.580089079255690088 ) ) ;
#143725=CARTESIAN_POINT ( 'NONE',  ( 0.07755575628183573877, 1.325091491099144259, -2.441202027401535357 ) ) ;
#143727=CARTESIAN_POINT ( 'NONE',  ( 6.533822986070857652, -2.155494434802426973, 0.5362405526610786177 ) ) ;
#143731=AXIS2_PLACEMENT_3D ( 'NONE', #132316, #68315, #66169 ) ;
#143733=CARTESIAN_POINT ( 'NONE',  ( 6.825078400183548055, 2.461594334264828987, 2.239602747093616841 ) ) ;
#143735=CARTESIAN_POINT ( 'NONE',  ( 3.850232551101365086, 0.2440307281281335616, -2.001511205109906655 ) ) ;
#143737=CARTESIAN_POINT ( 'NONE',  ( 2.500897397093455155, 0.4475292293845704594, 2.013297154094250807 ) ) ;
#143738=CARTESIAN_POINT ( 'NONE',  ( 6.750000000000007994, 7.629137130509070275, 2.600000000000001421 ) ) ;
#143742=CARTESIAN_POINT ( 'NONE',  ( 5.630878078874809844, -1.982435003639994031, 0.9343296635366815650 ) ) ;
#143743=CARTESIAN_POINT ( 'NONE',  ( 2.443982611291168450, -1.755769474653746665, -0.9913988478210812305 ) ) ;
#143744=CARTESIAN_POINT ( 'NONE',  ( 2.384105128782065819, -0.3166398734758494315, -1.813660976904336808 ) ) ;
#143746=CARTESIAN_POINT ( 'NONE',  ( 6.633835642106551411, -1.195214757176918496, -1.380038946949893486 ) ) ;
#143747=CARTESIAN_POINT ( 'NONE',  ( 0.3351808223112633933, 0.7127874033420987798, -2.185478155228081754 ) ) ;
#143749=CARTESIAN_POINT ( 'NONE',  ( 5.454102184832422928, 2.260192964246518166, -0.1051519175162188013 ) ) ;
#143751=CARTESIAN_POINT ( 'NONE',  ( 1.401149585966605882, 1.720815086091964652, -1.213930111015694369 ) ) ;
#143761=CARTESIAN_POINT ( 'NONE',  ( 1.775790443353560732, 0.3575140072833470906, -2.090081039791711337 ) ) ;
#143762=CARTESIAN_POINT ( 'NONE',  ( 3.041495853084168921, 0.05845243686668395028, 2.220815690970390222 ) ) ;
#143763=CARTESIAN_POINT ( 'NONE',  ( 6.883263157960393563, 4.695771316066229772, 2.508818740863460572 ) ) ;
#143766=CARTESIAN_POINT ( 'NONE',  ( 3.947668504265917644, 1.419370528949075005, 1.354593381527373186 ) ) ;
#143774=CARTESIAN_POINT ( 'NONE',  ( 3.305043459179863419, -0.4174351347619070229, -2.078937965663613774 ) ) ;
#143776=CARTESIAN_POINT ( 'NONE',  ( 4.645497774645744649, -1.668943667408796294, -1.373881373981879594 ) ) ;
#143777=CARTESIAN_POINT ( 'NONE',  ( 4.300242120186610784, 1.420457692841030850, -1.171515996850613694 ) ) ;
#143780=CARTESIAN_POINT ( 'NONE',  ( 5.947135546971048292, 0.4987507408355364991, -1.667328318302605528 ) ) ;
#143784=CARTESIAN_POINT ( 'NONE',  ( 3.344745324850742385, 0.5235245934552492653, 2.097234944377385002 ) ) ;
#143785=CARTESIAN_POINT ( 'NONE',  ( 5.378279760196133630, -0.2985789616767355326, 1.993766414912321316 ) ) ;
#143787=CARTESIAN_POINT ( 'NONE',  ( 2.501032641837992454, 1.736685530831501456, -1.287010829427559289 ) ) ;
#143788=CARTESIAN_POINT ( 'NONE',  ( 3.462146415373760444, 0.8834382129937996542, 1.762370924576799114 ) ) ;
#143790=CARTESIAN_POINT ( 'NONE',  ( 4.370608360784649093, -0.003437861098648780072, -1.942234966449083000 ) ) ;
#143800=CARTESIAN_POINT ( 'NONE',  ( 1.923171073188837843, 2.059116738528983692, 0.7940920450543451636 ) ) ;
#143802=CARTESIAN_POINT ( 'NONE',  ( 6.508651776674191147, 0.6122461511635870490, 1.863871573545019533 ) ) ;
#143806=CARTESIAN_POINT ( 'NONE',  ( 6.235036409211808461, 0.2120174297785166195, 2.196685143856290878 ) ) ;
#143808=CARTESIAN_POINT ( 'NONE',  ( 5.033073903806924321, -1.304366766181121573, -1.299653785596634137 ) ) ;
#143813=CARTESIAN_POINT ( 'NONE',  ( 6.416280414004661203, -2.120105685773795212, 0.05337830808049835035 ) ) ;
#143816=CARTESIAN_POINT ( 'NONE',  ( 0.1982117360312448395, -2.060432452642831702, -0.05102901230808094130 ) ) ;
#143818=CARTESIAN_POINT ( 'NONE',  ( 1.961162895873772127, 1.544969826164013238, 1.037258533166736996 ) ) ;
#143819=CARTESIAN_POINT ( 'NONE',  ( 3.509164994824386596, -1.813400730843343966, 0.3181347684400454012 ) ) ;
#143825=CARTESIAN_POINT ( 'NONE',  ( 3.545738602337618506, -1.670889076328873069, -1.441789439710974063 ) ) ;
#143826=CARTESIAN_POINT ( 'NONE',  ( 5.852851842114176861, -1.788828801601877849, 1.385077142625196434 ) ) ;
#143828=CARTESIAN_POINT ( 'NONE',  ( 6.170143040141627289, 1.806061762467878751, -0.1426304505553182556 ) ) ;
#143830=CARTESIAN_POINT ( 'NONE',  ( -0.2351498743046881446, -0.1506043639611966134, -1.983733596389973597 ) ) ;
#143832=CARTESIAN_POINT ( 'NONE',  ( 6.491075539335432687, 1.626419376453295706, -0.9240138038444989377 ) ) ;
#143833=CARTESIAN_POINT ( 'NONE',  ( 6.041656841763191288, -1.799011877964010520, 0.6487133288125003228 ) ) ;
#143835=CARTESIAN_POINT ( 'NONE',  ( 1.006479672118578916, 1.419055151971573059, -1.218976214888117804 ) ) ;
#143836=COLOUR_RGB ( '', 0.31764706, 0.68627451, 0.89019608) ;
#143837=CARTESIAN_POINT ( 'NONE',  ( 1.569546381206438967, 1.394087592100446971, 1.457234012747665508 ) ) ;
#143839=CARTESIAN_POINT ( 'NONE',  ( 4.336618311946851101, 2.065336219181472366, 0.4112933666130594301 ) ) ;
#143845=CARTESIAN_POINT ( 'NONE',  ( 3.480727363932310414, -1.353466037422011992, 1.499425228245174102 ) ) ;
#143849=CARTESIAN_POINT ( 'NONE',  ( 2.759224924868249662, -1.879262701025650850, -1.068020781904190253 ) ) ;
#143850=CARTESIAN_POINT ( 'NONE',  ( 6.620655732516647518, 7.053381450551401421, 2.424417106520880161 ) ) ;
#143855=CARTESIAN_POINT ( 'NONE',  ( 1.170657403521972562, -0.9760459728485239017, -1.939464792355448663 ) ) ;
#143859=CARTESIAN_POINT ( 'NONE',  ( 2.279091853667324141, 2.002311374866962979, -0.8913168663882904408 ) ) ;
#143860=CARTESIAN_POINT ( 'NONE',  ( 6.883263157960363365, 3.690127339433949327, 2.567897385111846731 ) ) ;
#143861=CARTESIAN_POINT ( 'NONE',  ( 2.184789616947193203, -2.218938341775698042, -0.4411300470171536370 ) ) ;
#143868=CARTESIAN_POINT ( 'NONE',  ( 4.551851636600127371, 1.769384361346277856, -0.04241240985469392488 ) ) ;
#143870=CARTESIAN_POINT ( 'NONE',  ( 0.4992256481273240065, 1.750750569696429171, -1.170121261866068130 ) ) ;
#143874=CARTESIAN_POINT ( 'NONE',  ( 6.433220217788329087, -1.621194592471734364, -1.198847091081943539 ) ) ;
#143875=CARTESIAN_POINT ( 'NONE',  ( 5.132992444152020717, 1.676870426783064083, 0.6860526005390086279 ) ) ;
#143878=CARTESIAN_POINT ( 'NONE',  ( 3.783945140921864070, -0.9226758061156097313, 1.627204332209288395 ) ) ;
#143879=CARTESIAN_POINT ( 'NONE',  ( 4.786024367859083029, -1.269482053145968514, -1.635305934682528717 ) ) ;
#143887=CARTESIAN_POINT ( 'NONE',  ( 4.264078424595136418, -1.956757550135434620, 0.1421211968542570592 ) ) ;
#143888=CARTESIAN_POINT ( 'NONE',  ( 0.6146109705059289441, 0.6351056948852469297, -1.913509406280079705 ) ) ;
#143892=CARTESIAN_POINT ( 'NONE',  ( 1.211929638205839765, -0.8359089839212189288, -1.673436591668895579 ) ) ;
#143894=CARTESIAN_POINT ( 'NONE',  ( 2.724860606552154785, 1.455292111517191511, -1.391298800531393765 ) ) ;
#143896=CARTESIAN_POINT ( 'NONE',  ( 2.284896850813819213, 1.698563897025050506, -1.263734059995786030 ) ) ;
#143898=CARTESIAN_POINT ( 'NONE',  ( 4.088381982606685838, 1.110138344689771239, -1.747393465062855533 ) ) ;
#143901=CARTESIAN_POINT ( 'NONE',  ( 6.456985077987440924, 0.3587005216530990692, -2.059463350302393359 ) ) ;
#143903=CARTESIAN_POINT ( 'NONE',  ( 5.772426501671443333, -1.156275361458743545, 1.412693073426966262 ) ) ;
#143908=CARTESIAN_POINT ( 'NONE',  ( 6.317417574511640765, -0.2763070477263400715, 2.189352377801502936 ) ) ;
#143910=CARTESIAN_POINT ( 'NONE',  ( 4.635362334195573197, -0.09024504784891507203, 1.910265517452472084 ) ) ;
#143918=CARTESIAN_POINT ( 'NONE',  ( 0.07680821025391608436, 0.2560392329899116026, -1.846278364303982178 ) ) ;
#143926=CARTESIAN_POINT ( 'NONE',  ( 2.588665490599820096, 1.909050991929973629, 0.4833708566103470661 ) ) ;
#143927=CARTESIAN_POINT ( 'NONE',  ( 3.585564690064909854, -0.5826378547920657569, 1.930424337232887977 ) ) ;
#143930=CARTESIAN_POINT ( 'NONE',  ( 6.727182134110199385, 7.052145554274142469, 2.687205589382557491 ) ) ;
#143931=CARTESIAN_POINT ( 'NONE',  ( 4.101666331917613206, -2.185647184384610586, 0.1603006067264350909 ) ) ;
#143933=CARTESIAN_POINT ( 'NONE',  ( 1.799704718893188282, -0.6512145186477935610, 1.813102765825167273 ) ) ;
#143936=CARTESIAN_POINT ( 'NONE',  ( 0.1329588055935578272, 2.045323036463253086, -2.262667038281248377 ) ) ;
#143942=CARTESIAN_POINT ( 'NONE',  ( 6.216338285296751920, 1.720575329815833943, 0.6561210673821931127 ) ) ;
#143943=CARTESIAN_POINT ( 'NONE',  ( 1.910792991191323065, -0.5388759818002909485, -1.939549710442307839 ) ) ;
#143944=CARTESIAN_POINT ( 'NONE',  ( 3.919517222396780909, 0.8229245375931023565, 2.146178768164926254 ) ) ;
#143945=CARTESIAN_POINT ( 'NONE',  ( -0.1291982275798911617, 0.2270562610647832436, -2.107042122458637756 ) ) ;
#143946=CARTESIAN_POINT ( 'NONE',  ( 2.588518228195731741, 1.803668244214111871, 0.4575444346353977898 ) ) ;
#143949=CARTESIAN_POINT ( 'NONE',  ( 5.097880177178074845, 1.288836597028759634, 1.412999258680311510 ) ) ;
#143952=CARTESIAN_POINT ( 'NONE',  ( 5.302318524065624317, 1.582279558761565452, -1.366676729786527211 ) ) ;
#143953=CARTESIAN_POINT ( 'NONE',  ( 3.467518583331068438, 1.825290416974333807, -0.4087457676540603990 ) ) ;
#143959=CARTESIAN_POINT ( 'NONE',  ( 5.936138232048088881, 0.8439337091313244832, -1.504256470664022238 ) ) ;
#143961=CARTESIAN_POINT ( 'NONE',  ( 1.142726939315736656, 0.7017603364856840331, 1.586018014115580188 ) ) ;
#143965=CARTESIAN_POINT ( 'NONE',  ( 5.928641807120487606, -1.383276364288194893, 1.673324517764721575 ) ) ;
#143966=CARTESIAN_POINT ( 'NONE',  ( 3.896943178251357054, 1.541351720387572843, -0.9781566455248569270 ) ) ;
#143967=CARTESIAN_POINT ( 'NONE',  ( 1.762477828903946442, -0.7011357286515782494, -1.832381215946830011 ) ) ;
#143968=CARTESIAN_POINT ( 'NONE',  ( 0.5271635063940235399, -1.813475876746664772, 1.092501443452270404 ) ) ;
#143972=CARTESIAN_POINT ( 'NONE',  ( 2.754661888675050019, 2.104750880745378083, 0.2572054321872129790 ) ) ;
#143978=CARTESIAN_POINT ( 'NONE',  ( 1.129834432590616000, 1.996231214973245516, -0.5485114149718294252 ) ) ;
#143981=CARTESIAN_POINT ( 'NONE',  ( 3.088771134150660735, -1.321542420002120855, 1.785288483701172657 ) ) ;
#143983=CARTESIAN_POINT ( 'NONE',  ( 0.3878286276588240877, -0.7819352795844608517, -2.161732420081037720 ) ) ;
#143985=CARTESIAN_POINT ( 'NONE',  ( 5.910998778867512016, -1.629530645011644463, 1.264396865911474821 ) ) ;
#143988=CARTESIAN_POINT ( 'NONE',  ( 0.1329588055935214397, 0.7520877941899367647, -1.931583167801545819 ) ) ;
#143989=CARTESIAN_POINT ( 'NONE',  ( 5.899929530298204661, -0.6689130865737795695, -1.715630562827724637 ) ) ;
#143993=CARTESIAN_POINT ( 'NONE',  ( 3.188212539307228699, -1.698978696193183202, -0.2961410920078124676 ) ) ;
#143994=CARTESIAN_POINT ( 'NONE',  ( 0.9718890779336667451, -0.9023411006064323558, 1.803417998987096427 ) ) ;
#143995=CARTESIAN_POINT ( 'NONE',  ( 2.725512391864647999, 2.281683302435618010, 0.2785734649361614745 ) ) ;
#143997=CARTESIAN_POINT ( 'NONE',  ( 2.460583821258513382, 0.9655243699240693145, 2.046139933455006776 ) ) ;
#143998=CARTESIAN_POINT ( 'NONE',  ( 5.742829910930518977, 0.4094298153964996967, 2.065706902019475599 ) ) ;
#144000=CARTESIAN_POINT ( 'NONE',  ( 3.145496161269778046, 0.6404232447230692182, -1.649968755877039506 ) ) ;
#144003=CARTESIAN_POINT ( 'NONE',  ( 0.09422489544355044933, -2.291893678819735491, -0.04953789299679511871 ) ) ;
#144004=CARTESIAN_POINT ( 'NONE',  ( 4.822110771479974467, 1.762745816080556915, 0.5315184756640098929 ) ) ;
#144008=CARTESIAN_POINT ( 'NONE',  ( 4.101666331917613206, -2.185647184384610586, 0.1603006067264350909 ) ) ;
#144013=CARTESIAN_POINT ( 'NONE',  ( 2.947785801820240970, 0.6929415146892035082, -1.797737524126517217 ) ) ;
#144016=CARTESIAN_POINT ( 'NONE',  ( 0.5807245924134795123, 1.101748585799481095, 1.928910967146231004 ) ) ;
#144026=CARTESIAN_POINT ( 'NONE',  ( 6.666866396406604167, -1.974176978123330040, -0.8811043787171415342 ) ) ;
#144027=CARTESIAN_POINT ( 'NONE',  ( 5.301206097546149465, -1.683542251207278628, 1.007010407901312465 ) ) ;
#144030=CARTESIAN_POINT ( 'NONE',  ( 5.295850518597075229, -0.7817450549502875656, 2.015575934489414411 ) ) ;
#144034=CARTESIAN_POINT ( 'NONE',  ( 0.2626887844769665303, -1.667795467377327423, -0.8471929967568125885 ) ) ;
#144035=CARTESIAN_POINT ( 'NONE',  ( 5.940742354060237318, 1.035569694170878519, 1.390440122839208703 ) ) ;
#144037=CARTESIAN_POINT ( 'NONE',  ( 2.929422067023911502, -1.473737196803912797, -1.622193633833472814 ) ) ;
#144038=CARTESIAN_POINT ( 'NONE',  ( 3.575485986712009456, 0.05928947047922557279, -2.306987226281012049 ) ) ;
#144039=CARTESIAN_POINT ( 'NONE',  ( 5.747358702077526971, -1.621750911093680081, -1.271367298817957181 ) ) ;
#144040=CARTESIAN_POINT ( 'NONE',  ( 1.113109651085980811, -1.894741734565345004, 0.4249041608528710823 ) ) ;
#144046=CARTESIAN_POINT ( 'NONE',  ( 5.572555445586866441, 0.8612648569810870125, 1.938019255899057658 ) ) ;
#144048=CARTESIAN_POINT ( 'NONE',  ( 2.074842474778653134, -0.8596299393073093542, 1.824119475507138821 ) ) ;
#144050=CARTESIAN_POINT ( 'NONE',  ( 5.930760676324511316, 2.125237774816424619, 0.5940772278362898007 ) ) ;
#144054=CARTESIAN_POINT ( 'NONE',  ( 0.1701549220758866166, -1.195335944658926230, 1.380069390326914336 ) ) ;
#144060=CARTESIAN_POINT ( 'NONE',  ( 4.434483769945627429, 2.020730376925969018, 0.4039503012724340869 ) ) ;
#144065=CARTESIAN_POINT ( 'NONE',  ( 4.195966715351859833, 1.320990344651201021, 1.527833845825769643 ) ) ;
#144070=CARTESIAN_POINT ( 'NONE',  ( 3.028252848896676674, 1.146099369071330143, -1.712595011064410366 ) ) ;
#144071=CARTESIAN_POINT ( 'NONE',  ( 2.760388869050140137, 1.913803604375517109, -0.6351994527180188088 ) ) ;
#144077=CARTESIAN_POINT ( 'NONE',  ( 3.163435312993330140, -0.5825663732807913053, -1.930122257003751063 ) ) ;
#144078=CARTESIAN_POINT ( 'NONE',  ( 1.921575063125853022, 1.060747535801230379, -1.504664925706208578 ) ) ;
#144079=CARTESIAN_POINT ( 'NONE',  ( 0.6632354941851228425, -1.667548007495605944, 1.595465711622134242 ) ) ;
#144081=CARTESIAN_POINT ( 'NONE',  ( 2.284651837757902371, -2.119410549416993916, -0.4241055355862289877 ) ) ;
#144083=CARTESIAN_POINT ( 'NONE',  ( 2.618911895557019420, 0.6142130902007210125, -2.214721005821191024 ) ) ;
#144086=CARTESIAN_POINT ( 'NONE',  ( 1.164687902950040321, -1.689591380799923215, -0.8031939614948147010 ) ) ;
#144087=CARTESIAN_POINT ( 'NONE',  ( 5.260604563723265237, -1.428518960016441186, 1.358918391201448417 ) ) ;
#144092=CARTESIAN_POINT ( 'NONE',  ( 0.2587985324217950689, 0.8487602207661277820, 2.037339956011212649 ) ) ;
#144094=CARTESIAN_POINT ( 'NONE',  ( 6.373496627357888578, -0.2573980274669443458, 2.054251119134167691 ) ) ;
#144097=CARTESIAN_POINT ( 'NONE',  ( 6.639320575229294086, 7.051910277135648997, 2.801414343313723965 ) ) ;
#144098=CARTESIAN_POINT ( 'NONE',  ( 5.418811373015061328, 1.821287777658405549, 0.7551675066918785983 ) ) ;
#144099=CARTESIAN_POINT ( 'NONE',  ( 6.416272379866970965, -2.019260422740985828, 0.05364450914858465147 ) ) ;
#144101=CARTESIAN_POINT ( 'NONE',  ( 4.934332944283116973, 1.189700906406887082, -1.977258547338469841 ) ) ;
#144103=CARTESIAN_POINT ( 'NONE',  ( 1.657159287258206604, 1.688608613550081516, -1.184165042645689558 ) ) ;
#144110=CARTESIAN_POINT ( 'NONE',  ( 4.439989079487234314, 1.414935287217274684, 1.646911713943682409 ) ) ;
#144112=CARTESIAN_POINT ( 'NONE',  ( 4.054132754448328768, -1.361571661076573792, 1.239656203754435193 ) ) ;
#144114=DIRECTION ( 'NONE',  ( -1.000000000000000000, 0.000000000000000000, 0.000000000000000000 ) ) ;
#144115=CARTESIAN_POINT ( 'NONE',  ( 5.144143540903125533, 0.6357783856077160456, 2.097287126430439130 ) ) ;
#144117=CARTESIAN_POINT ( 'NONE',  ( 5.700151306344448443, -2.262689076517818254, -0.006432940626173094985 ) ) ;
#144124=CARTESIAN_POINT ( 'NONE',  ( 0.8832604684265840111, 1.184483277375179666, 1.315230855816750921 ) ) ;
#144126=CARTESIAN_POINT ( 'NONE',  ( 4.881498389339896882, 0.1952109149471596417, -2.003590356478464507 ) ) ;
#144128=CARTESIAN_POINT ( 'NONE',  ( 3.838982076996471982, 0.3068427722541127722, 2.083350420514245016 ) ) ;
#144129=CARTESIAN_POINT ( 'NONE',  ( 2.671383988363975170, 1.356552116283934240, 1.352788525452413237 ) ) ;
#144131=CARTESIAN_POINT ( 'NONE',  ( 3.560960244297206589, 1.554118163632215444, -1.209804376587125807 ) ) ;
#144132=CARTESIAN_POINT ( 'NONE',  ( 5.554946522049384328, 0.3980760423633997180, 1.979986811436624805 ) ) ;
#144133=CARTESIAN_POINT ( 'NONE',  ( 1.920565142479381038, 1.744437793965779582, 0.6759427408406930571 ) ) ;
#144134=CARTESIAN_POINT ( 'NONE',  ( 5.057137062068671973, -1.459852279745242010, -0.9183987515692086934 ) ) ;
#144135=CARTESIAN_POINT ( 'NONE',  ( 1.670022949053862948, 1.907054940702714863, -0.1439945843566131367 ) ) ;
#144136=ORIENTED_EDGE ( 'NONE', *, *, #199668, .F. ) ;
#144137=CARTESIAN_POINT ( 'NONE',  ( 1.770444396619451632, 1.136427050704125419, 1.891651738277564831 ) ) ;
#144146=CARTESIAN_POINT ( 'NONE',  ( 2.049362625460974030, 1.802418521853879962, -1.018503948505583789 ) ) ;
#144151=CARTESIAN_POINT ( 'NONE',  ( 6.076833508651091620, -1.499762292660647311, 1.499315088411487640 ) ) ;
#144156=FACE_OUTER_BOUND ( 'NONE', #51780, .T. ) ;
#144158=CARTESIAN_POINT ( 'NONE',  ( 4.815779736370030761, -1.620933320526974031, 1.198678058543983571 ) ) ;
#144159=CARTESIAN_POINT ( 'NONE',  ( 4.258935762849770157, -0.005977556496831581273, -1.915903398800692159 ) ) ;
#144160=CARTESIAN_POINT ( 'NONE',  ( 3.034921719543516971, -1.931671641359738567, 1.035203715903771915 ) ) ;
#144163=CARTESIAN_POINT ( 'NONE',  ( 5.045186288489547977, 0.1525188484602090777, 2.007510047055609093 ) ) ;
#144167=CARTESIAN_POINT ( 'NONE',  ( 6.028941913163482269, -1.788401068206580957, 1.133005349186385402 ) ) ;
#144169=CARTESIAN_POINT ( 'NONE',  ( 3.316043925569078787, 1.324660045548868181, -1.617576387421674866 ) ) ;
#144171=CARTESIAN_POINT ( 'NONE',  ( 1.887319702290214840, 1.186364228098319762, 1.252193311579427482 ) ) ;
#144173=CARTESIAN_POINT ( 'NONE',  ( 5.080389167821143026, 1.047295930500062866, 1.843893106414703054 ) ) ;
#144184=CARTESIAN_POINT ( 'NONE',  ( 1.840194262915356260, 1.042575051921472040, -1.481162322861505620 ) ) ;
#144189=CARTESIAN_POINT ( 'NONE',  ( 2.262115610809340094, 1.811117530136572285, 0.04320712765945587674 ) ) ;
#144190=CARTESIAN_POINT ( 'NONE',  ( 6.639320575229258559, 7.629137130509072051, 2.496737603865983424 ) ) ;
#144193=CARTESIAN_POINT ( 'NONE',  ( 4.351900876113290018, -0.7134228844126557778, 1.719084262507431182 ) ) ;
#144194=CARTESIAN_POINT ( 'NONE',  ( 1.827608144986846206, 0.7312883373844185630, -1.770730004348388453 ) ) ;
#144195=CARTESIAN_POINT ( 'NONE',  ( 0.7975364289293709330, -0.6616875547802402169, 1.701626729119443127 ) ) ;
#144202=CARTESIAN_POINT ( 'NONE',  ( 5.735196696812420392, -0.04448252213613138051, -1.969098798407813433 ) ) ;
#144205=CARTESIAN_POINT ( 'NONE',  ( 0.07627643479381736313, -2.028408900457449704, -0.5058713263092640133 ) ) ;
#144207=CARTESIAN_POINT ( 'NONE',  ( 5.526370178063710448, 1.147270165450631207, -1.547347761420419188 ) ) ;
#144209=CARTESIAN_POINT ( 'NONE',  ( 0.7975364289293709330, -0.6616875547802402169, 1.701626729119443127 ) ) ;
#144210=CARTESIAN_POINT ( 'NONE',  ( 2.684424123961434816, -1.133677649706768431, 1.893296980138805319 ) ) ;
#144214=CARTESIAN_POINT ( 'NONE',  ( 0.6780957659633795043, -1.050550344063156061, -1.665771736420356808 ) ) ;
#144215=CARTESIAN_POINT ( 'NONE',  ( 2.700647863620793121, 1.641916212795376806, 1.036879047414513755 ) ) ;
#144218=CARTESIAN_POINT ( 'NONE',  ( 0.3685172633814579601, -0.5404119286356176000, 1.942243004588292354 ) ) ;
#144220=CARTESIAN_POINT ( 'NONE',  ( 5.576953945496859966, 1.718729505308995931, 0.7139912403442708611 ) ) ;
#144226=CARTESIAN_POINT ( 'NONE',  ( 1.259612756803454525, 2.158328104161820526, -0.3793702838810895095 ) ) ;
#144230=CARTESIAN_POINT ( 'NONE',  ( 3.017977635683791071, -0.9002817137206723386, -1.588204215665294461 ) ) ;
#144236=CARTESIAN_POINT ( 'NONE',  ( 0.9262474005801927257, 1.148234195015400694, -1.546785173711192840 ) ) ;
#144237=CARTESIAN_POINT ( 'NONE',  ( 5.805508902378371694, -1.544246397408255866, -1.209716981170713357 ) ) ;
#144241=CARTESIAN_POINT ( 'NONE',  ( 5.566036750361066154, -1.391122746885119499, 1.693456055751572986 ) ) ;
#144245=CARTESIAN_POINT ( 'NONE',  ( 4.311429529933403337, -1.718370896367764411, -1.154329086688666184 ) ) ;
#144249=CARTESIAN_POINT ( 'NONE',  ( 4.114144448104863017, 0.1132377192244668207, 2.296027709189680799 ) ) ;
#144256=CARTESIAN_POINT ( 'NONE',  ( 3.908095550721983447, 1.372505747409875632, -1.374073360379985065 ) ) ;
#144261=CARTESIAN_POINT ( 'NONE',  ( 4.851772015791367743, -1.356534033432246211, -1.348250844427544282 ) ) ;
#144263=CARTESIAN_POINT ( 'NONE',  ( 6.739270712165630783, -1.537707103621160476, 0.7812997327944263271 ) ) ;
#144264=CARTESIAN_POINT ( 'NONE',  ( 4.417204035549080920, -1.841734835922325120, 0.8216704330437708537 ) ) ;
#144266=CARTESIAN_POINT ( 'NONE',  ( 1.559489335033688251, -1.894147805384650995, -1.132260830144316888 ) ) ;
#144269=CARTESIAN_POINT ( 'NONE',  ( 1.183663948672460942, -0.9384196385337481017, 1.868258235111931898 ) ) ;
#144270=CARTESIAN_POINT ( 'NONE',  ( 0.1273423419134401269, -1.083036363347224418, -1.400124042496312615 ) ) ;
#144271=CARTESIAN_POINT ( 'NONE',  ( 6.328750030911493241, 0.7691242348151774433, -1.864167186630163009 ) ) ;
#144273=CARTESIAN_POINT ( 'NONE',  ( 2.801036929584544311, 1.937030572335847856, 1.225446795713614589 ) ) ;
#144274=CARTESIAN_POINT ( 'NONE',  ( 0.5502397958263847144, -1.467719461762364341, -0.9348402994967041080 ) ) ;
#144276=CARTESIAN_POINT ( 'NONE',  ( 1.440355836138224932, 1.027696236922505557, 1.396268056379332378 ) ) ;
#144278=CARTESIAN_POINT ( 'NONE',  ( 1.311231623020674419, -1.711955697424736744, 1.335301017299495685 ) ) ;
#144279=CARTESIAN_POINT ( 'NONE',  ( 2.676970549635893537, 1.727063564601112100, -1.040793759654296213 ) ) ;
#144280=CARTESIAN_POINT ( 'NONE',  ( 4.250000000000002665, 2.550977938801684432E-13, 2.052068128417944948 ) ) ;
#144283=CARTESIAN_POINT ( 'NONE',  ( 0.2703664580724125521, -1.260843473572888396, 1.456531361591931972 ) ) ;
#144285=CARTESIAN_POINT ( 'NONE',  ( 2.935994361307178391, -2.139806239105252583, 0.5962572732955830901 ) ) ;
#144290=CARTESIAN_POINT ( 'NONE',  ( 5.970193594734433340, -1.655480682217812083, -0.5374289683400793605 ) ) ;
#144292=CARTESIAN_POINT ( 'NONE',  ( 4.984793487045196869, 1.876812866478014596, 0.5713181500588762063 ) ) ;
#144296=CARTESIAN_POINT ( 'NONE',  ( 4.323666171361133514, -2.166671669000098444, 0.6512573085333557277 ) ) ;
#144297=CARTESIAN_POINT ( 'NONE',  ( 2.559094272886554666, 1.658201776010211459, -1.226620081234103266 ) ) ;
#144301=CARTESIAN_POINT ( 'NONE',  ( 3.145614842782416432, 0.6765965015090926737, -1.744060075730607950 ) ) ;
#144302=CARTESIAN_POINT ( 'NONE',  ( 2.513978358999646723, -1.617321061556979300, 0.6262005117416250544 ) ) ;
#144303=CARTESIAN_POINT ( 'NONE',  ( 6.146043800834426918, 0.6857851511376764631, 2.081541312870714311 ) ) ;
#144304=CARTESIAN_POINT ( 'NONE',  ( 0.6224627697807674220, -1.182292326766160251, -1.863150505713019989 ) ) ;
#144305=CARTESIAN_POINT ( 'NONE',  ( 3.819328725847204620, -0.1613130240520690706, 2.155748724213396361 ) ) ;
#144306=CARTESIAN_POINT ( 'NONE',  ( 4.488185891274095063, -0.4267898533511414461, -1.894319381339019559 ) ) ;
#144313=CARTESIAN_POINT ( 'NONE',  ( 6.205703963786828758, 1.882472927010571118, 0.7231429968634556227 ) ) ;
#144317=CARTESIAN_POINT ( 'NONE',  ( 2.859763506297557711, 1.816872213737670938, -0.1792109616642542924 ) ) ;
#144318=CARTESIAN_POINT ( 'NONE',  ( 2.028631293930313717, 1.270571802522667992, -1.804104215285810886 ) ) ;
#144323=CARTESIAN_POINT ( 'NONE',  ( 0.5451830133551841540, 0.1527301869948919366, 2.014097447171578903 ) ) ;
#144324=CARTESIAN_POINT ( 'NONE',  ( 1.102369588802411426, -0.9501182663193027400, 1.895776817140030213 ) ) ;
#144326=CARTESIAN_POINT ( 'NONE',  ( 2.078732565759545903, 1.734175166166322501, 0.6755533923482255343 ) ) ;
#144328=CARTESIAN_POINT ( 'NONE',  ( 0.2335756976950612018, -1.975703151049061024, 0.8776370805363906680 ) ) ;
#144333=CARTESIAN_POINT ( 'NONE',  ( 3.598116246361187542, -1.823677485248562435, -0.08826725125678223927 ) ) ;
#144337=CARTESIAN_POINT ( 'NONE',  ( 5.958361200765043719, 1.524811557412728114, 1.319025083221535333 ) ) ;
#144338=CARTESIAN_POINT ( 'NONE',  ( 6.070224334863941529, -1.749758606415029449, -0.5730458292283467925 ) ) ;
#144339=CARTESIAN_POINT ( 'NONE',  ( 0.07700591528349286230, 5.724620991219308230, -2.504819247423330175 ) ) ;
#144340=CARTESIAN_POINT ( 'NONE',  ( 4.002764008144163554, -0.7221186334790052896, -2.191863981390995253 ) ) ;
#144342=CARTESIAN_POINT ( 'NONE',  ( 6.485629946217342123, 1.485420011660616657, 1.570608065930901187 ) ) ;
#144343=CARTESIAN_POINT ( 'NONE',  ( 1.241630701082994559, 1.939900434848752964, 0.09377332689292780521 ) ) ;
#144345=CARTESIAN_POINT ( 'NONE',  ( 4.235939456923387247, -2.142719978266393710, -0.8318502446633867509 ) ) ;
#144348=CARTESIAN_POINT ( 'NONE',  ( 4.539837415608827698, 0.7997722286730184482, -1.691214532891088362 ) ) ;
#144350=CARTESIAN_POINT ( 'NONE',  ( 2.672007700615218528, 1.902801012812182169, -0.1915479950082218386 ) ) ;
#144353=CARTESIAN_POINT ( 'NONE',  ( 4.389439674793148782, 1.972019932058775016, -0.9908447712502415072 ) ) ;
#144359=CARTESIAN_POINT ( 'NONE',  ( 1.528526583484477230, 1.898816187374774200, 0.5295601200957336108 ) ) ;
#144360=CARTESIAN_POINT ( 'NONE',  ( 1.554236647822554218, 0.6679093176565461532, -2.208796357520240949 ) ) ;
#144361=CARTESIAN_POINT ( 'NONE',  ( 2.348037267531626338, -0.8415878996531295231, 1.772339229757218471 ) ) ;
#144363=CARTESIAN_POINT ( 'NONE',  ( 4.838768981748684972, -1.999376597400838174, -0.5061158833775216692 ) ) ;
#144367=( BOUNDED_SURFACE ( )  B_SPLINE_SURFACE ( 3, 3, ( 
 ( #89085, #155141, #4574, #41406, #7793, #70648, #73886, #69582, #120579, #186556, #38185, #6722, #104257, #56573, #122732, #178865, #91222, #144271, #190813, #93358, #92302, #74951, #191879, #12072, #112849, #157283, #60829, #61902, #27251, #158346, #110716, #13134, #46737, #44601, #129124, #210264, #109662, #29408, #175664, #79211, #128063, #145329, #159395, #10994, #176716, #77069, #143199, #28329, #43539, #141062, #124847, #209189, #192949, #8872, #161547, #126990, #194019, #208131, #207069, #45669, #95500, #58699, #142118, #42473, #108583, #94425, #160464, #174611, #62955, #111786, #26187, #177792, #9940, #76015, #59760, #125920, #78140, #211330, #195101, #85339, #121134, #30476, #86411, #133058, #35511, #34446, #14184, #134128, #168722, #54981, #96561, #2994, #4058, #183900, #100521, #52837, #169787, #203328, #201197, #71196, #152478, #51790, #186022, #117907, #21376, #70128, #87484, #101589, #167657, #118973, #19257, #151421, #184951, #200137, #80277, #66917, #69062, #135182, #162608, #103736, #36578, #136241, #150356, #146375, #202262, #37659, #18184, #50705, #53912, #120048, #1926, #67985, #153550, #137312, #102664, #20325, #199059, #852, #116829, #182831, #5120, #166595, #84270, #73343, #187097, #104812, #140535, #175148, #109135, #142661, #74435, #155684, #26734, #92836, #170857, #124336, #206547, #22447, #6198, #158880, #10476, #56048, #91771, #38731, #72267, #208671, #125390, #60302, #156762, #190294, #41952, #122204, #205480, #139445, #108064, #57112, #106987, #138375, #174090, #40882, #204393, #25662, #157828, #173012, #90700, #8350, #23525, #105906, #58176, #9424, #88559, #188166, #154619, #191356, #39799, #75494, #141606, #207614, #171931, #123281, #189242, #59232, #24593, #43021, #89632, #76551, #7266, #11550, #129664, #195651, #46213, #29952, #162089, #177266, #45151, #96037, #147968, #28882, #213980, #27808, #128601, #13679, #176207, #98163, #163154, #110197, #80830, #192424, #93906, #44078, #77620, #112329, #146919, #196707, #178343, #126460, #159946, #179406, #143743, #194567, #127538, #209737, #12608, #47286, #61381, #193510, #79750, #97102, #62438, #111263, #145866, #48347, #81883, #211873, #164210, #31026, #144807, #64574, #210813, #114458, #14738, #180458, #63512, #113398, #212937, #130716, #32075, #15797, #78680, #94965, #161013, #51521, #167402, #131749, #135970, #67720, #168458, #182563, #65600, #20056, #69861, #50451, #82939, #86146, #152217, #34186, #100260, #102391, #169526, #84003, #166327, #165263, #153274, #21106, #33134, #201986, #133871, #3786, #17917, #197754, #49393, #18992, #53643, #119776, #87210, #85074, #150093, #185756, #37389, #115512, #2728, #151159, #181505, #99214, #103464, #16858, #149012, #199878, #66654, #588, #1664, #200927, #132800, #198803, #35245, #36312, #117646, #116569, #68801, #183639, #101320, #134921, #52575, #184692, #118704, #157567, #23252, #141346, #57910, #207361, #6996, #73074, #24321, #89365, #155413, #156496, #105626, #54709, #38465, #205206, #106719, #70930, #75236, #139175, #107802, #121931, #4851, #173827, #9160, #204122, #22171, #25404, #91506, #187898, #39528, #41691, #108870, #56848, #171655, #104541, #92583, #174893, #186833, #58981, #123020, #125137, #188971, #137039, #203066, #172746, #191094, #42763, #26473, #90427, #40615, #120860, #170586 ),
 ( #88286, #154350, #5928, #8085, #74174, #140266, #72000, #206286, #124075, #190039, #138111, #55774, #109940, #95778, #12347, #43823, #161834, #13422, #78427, #62192, #194315, #209473, #77363, #128348, #180207, #61115, #31829, #60046, #160752, #45956, #208412, #130464, #195392, #142404, #113137, #10222, #126201, #76296, #175949, #144549, #179144, #14477, #210556, #158625, #192163, #211612, #27545, #64320, #93640, #63248, #159683, #11284, #143477, #96847, #127275, #112077, #79497, #145616, #193247, #177005, #111000, #129409, #44894, #178078, #28622, #47022, #29696, #94710, #30767, #162894, #80566, #146665, #212679, #196454, #48097, #114209, #119529, #148768, #185515, #213729, #100016, #133623, #147711, #69619, #134681, #81626, #52335, #163965, #65352, #15541, #49146, #17668, #118463, #168215, #149846, #97904, #131499, #150916, #197503, #166080, #98959, #115262, #198554, #18743, #181255, #32882, #132555, #33941, #1415, #165010, #3549, #16605, #101069, #82686, #337, #84828, #184449, #83754, #117395, #67477, #199625, #51271, #183392, #135729, #66410, #201751, #34997, #50203, #116321, #182312, #167156, #2478, #68554, #200684, #36067, #102149, #19814, #85901, #151975, #53392, #121687, #186590, #153034, #154105, #169280, #103220, #55532, #156250, #25155, #123830, #155174, #21924, #24082, #88033, #120613, #70682, #187654, #37139, #202820, #136795, #41443, #73920, #172496, #72833, #20866, #5674, #39280, #105375, #138936, #140013, #204957, #38218, #86965, #54469, #206038, #104291, #6758, #171414, #4608, #23002, #89120, #170339, #71752, #189792, #74987, #203888, #137868, #56605, #57672, #107551, #122769, #157316, #188729, #40367, #106469, #90187, #7828, #173585, #91256, #8907, #141095, #207107, #58734, #124886, #96593, #42511, #125954, #11028, #127023, #28364, #108617, #162642, #158379, #194052, #190850, #191910, #177825, #145366, #192982, #210295, #44636, #94459, #12104, #160499, #14216, #27286, #80311, #61936, #9972, #93392, #92337, #59797, #95533, #78174, #144302, #128094, #45704, #76050, #174644, #111823, #29442, #60862, #43573, #142151, #159429, #26221, #208166, #209220, #161582, #178898, #62990, #13169, #175696, #79247, #77106, #109692, #143230, #110751, #176749, #211365, #129159, #195136, #46772, #112886, #30512, #146411, #212424, #64066, #148520, #165828, #166900, #83496, #131261, #47845, #15291, #196203, #163709, #16350, #115006, #82430, #32624, #31575, #197248, #132296, #3295, #181004, #179952, #98701, #51013, #84571, #130210, #35815, #167957, #97650, #81376, #86, #116064, #49943, #199367, #134429, #149578, #113956, #147460, #213481, #198302, #65105, #99760, #100815, #66151, #48887, #1162, #52079, #85637, #67225, #19561, #34742, #182054, #68296, #33684, #118206, #183137, #184193, #17412, #133360, #117134, #18492, #150658, #2221, #200432, #164760, #101892, #151723, #171153, #135472, #139753, #71500, #172237, #186327, #69363, #23825, #73654, #54213, #86706, #89930, #155981, #37962, #104035, #106211, #173311, #87775, #170081, #169020, #157058, #24890, #36879, #205778, #137611, #7568, #21668, #201493, #53139, #22743, #57406, #123572, #90995, #88861, #153850, #189534, #41182, #119270, #6500, #154916, #185255, #102961, #107289, #20618, #152775, #188467, #4357, #70425, #136542, #202561, #120351, #39029, #72575, #138675, #5421 ),
 ( #203627, #204695, #55278, #121427, #187397, #105112, #56345, #122506, #40099, #93131, #9715, #92066, #95266, #46500, #175438, #125690, #60598, #29176, #177564, #109432, #128886, #159170, #158124, #27023, #10770, #25961, #191648, #43313, #76844, #62725, #161314, #112624, #12898, #75791, #126756, #142963, #8647, #208965, #192717, #141899, #207909, #78977, #178634, #44371, #110494, #176493, #145097, #211101, #28104, #194867, #94199, #59530, #160239, #11838, #77916, #144035, #210031, #61672, #30246, #96330, #74726, #127840, #140831, #206844, #193792, #45441, #111555, #58476, #124631, #190589, #42246, #108359, #174381, #163449, #149322, #116879, #164507, #181801, #98442, #65901, #198056, #214268, #134173, #213231, #68033, #33434, #129958, #64863, #63800, #31315, #66968, #132047, #49686, #115813, #99511, #195946, #80047, #83237, #165568, #32377, #97393, #47582, #131008, #146150, #13963, #180750, #133107, #150401, #34494, #17163, #147206, #900, #197000, #15029, #113696, #16091, #162385, #179700, #81121, #166641, #199105, #50750, #182878, #212166, #48635, #82175, #148269, #100568, #18232, #84316, #114752, #1969, #200181, #51834, #117952, #183947, #35557, #202308, #4107, #3040, #102710, #103784, #192206, #152522, #151469, #70176, #22493, #56095, #101637, #7314, #139496, #69109, #135231, #120096, #87531, #21422, #170901, #105956, #55028, #167703, #186073, #168768, #185001, #188210, #205524, #53958, #136288, #153598, #122251, #39849, #37708, #73393, #169835, #36626, #5169, #71243, #119020, #137359, #203376, #121177, #155730, #171980, #57158, #88605, #126246, #19305, #20373, #187146, #38775, #104857, #85385, #201244, #52885, #154661, #86458, #6247, #72316, #23572, #138421, #204441, #89681, #161878, #79541, #95819, #15579, #94752, #164003, #63293, #11327, #160800, #159728, #127320, #162938, #13465, #145659, #211655, #129453, #77405, #175994, #179186, #195436, #128390, #193290, #143522, #12391, #27588, #109984, #62232, #14519, #31870, #130507, #47065, #28667, #30809, #78470, #44935, #209518, #194357, #43868, #61158, #111043, #48136, #80613, #96889, #113182, #93686, #144589, #46000, #112119, #146706, #212722, #64361, #177050, #210603, #178122, #29737, #196494, #114250, #180246, #97949, #81666, #147752, #213770, #65391, #131538, #33978, #32921, #100053, #118500, #152009, #197540, #103255, #20900, #98997, #165052, #1449, #183429, #117431, #52371, #201787, #150951, #70716, #3581, #198592, #101104, #51306, #49185, #35030, #16644, #115304, #199660, #82728, #167190, #168251, #133659, #50239, #2515, #119564, #153069, #68588, #86996, #102184, #67514, #135764, #18777, #185551, #36099, #37180, #84863, #134713, #200720, #184482, #19850, #85937, #83789, #148805, #374, #69656, #53427, #181294, #169316, #4646, #66448, #166117, #132590, #116359, #182349, #17702, #149884, #91296, #25192, #39318, #105413, #173620, #26254, #155209, #171451, #21962, #10008, #92371, #104327, #58768, #138973, #75023, #23040, #136829, #54503, #90219, #124922, #190884, #158408, #24116, #89156, #42550, #108653, #120647, #73955, #156283, #186626, #170375, #174681, #202855, #5711, #41477, #38253, #88070, #154143, #141135, #71788, #106505, #140047, #206072, #137903, #6790, #72867, #57706, #204996, #56640, #203922, #123863, #122804, #55570, #189828, #107587, #188763, #40403, #172532 ),
 ( #157354, #121724, #8943, #187689, #7867, #207145, #27326, #210337, #96630, #146449, #128130, #163748, #76084, #129200, #175733, #78214, #77145, #59833, #159467, #195177, #45743, #111861, #29478, #95569, #109726, #208200, #211403, #161619, #160535, #11066, #191943, #193022, #125986, #142185, #94497, #46810, #64108, #162684, #194093, #60901, #63033, #127060, #143266, #93428, #12141, #43608, #209256, #44674, #80349, #112924, #178937, #177866, #110786, #176788, #144337, #61976, #13212, #30551, #79285, #28403, #145403, #14258, #212464, #130250, #196241, #47884, #113997, #179992, #31615, #97690, #17453, #103001, #66193, #65142, #132338, #150699, #184229, #15327, #135509, #53180, #131298, #197289, #33724, #1201, #149619, #84610, #19603, #183177, #81417, #35853, #16391, #133402, #83537, #147498, #67263, #99802, #82470, #98741, #101931, #119308, #182093, #198344, #199407, #167997, #85675, #116102, #201532, #165867, #164799, #51052, #117175, #32662, #49984, #34781, #100855, #69402, #151763, #185294, #2261, #36918, #213519, #148560, #166940, #18533, #68337, #48929, #115048, #181046, #134469, #126, #200472, #52119, #3332, #118247, #188506, #105152, #72616, #204732, #6538, #140870, #5458, #74767, #40137, #136580, #71538, #70463, #56382, #86744, #137648, #171192, #187438, #122545, #205817, #106250, #170119, #152814, #54253, #20654, #202600, #55317, #153889, #121468, #203668, #120390, #21705, #22782, #42286, #39066, #4392, #88899, #89968, #123610, #169057, #206882, #58514, #186365, #38000, #154953, #138715, #172274, #23861, #173351, #156020, #104072, #189573, #87817, #7608, #73692, #139790, #57449, #41221, #107326, #24932, #91036, #124669, #157096, #8685, #190626, #177605, #111596, #159207, #145135, #143003, #59571, #10808, #76883, #207949, #27065, #175478, #209001, #79018, #29217, #62763, #144077, #211141, #174422, #125729, #93172, #60638, #192756, #25998, #128925, #9753, #11880, #108398, #126800, #193830, #95307, #44413, #77956, #110532, #28144, #160278, #176532, #194904, #94239, #46541, #210073, #191690, #61712, #141936, #43350, #161356, #127880, #45480, #12939, #92107, #109470, #75829, #158162, #172974, #171891, #22412, #203295, #204352, #5083, #153514, #105865, #206509, #75458, #174053, #205440, #72229, #74398, #138336, #170821, #121094, #23488, #87445, #38694, #187061, #91738, #124299, #8313, #39760, #56010, #139406, #108027, #41916, #188129, #207579, #89595, #88521, #155644, #7228, #104772, #122162, #73304, #57076, #141571, #25626, #125355, #140499, #59199, #71158, #154583, #123240, #189205, #40842, #137275, #191318, #54942, #90660, #6160, #106951, #58140, #157791, #24553, #156722, #190258, #9387, #42986, #109096, #175112, #193969, #192895, #111734, #60779, #9888, #208082, #160414, #61848, #26138, #30427, #176667, #62904, #77016, #174562, #129074, #178814, #159345, #191828, #195045, #46683, #143145, #209140, #211281, #63981, #44551, #126938, #59709, #47761, #130134, #142068, #96513, #28279, #112801, #110667, #92251, #158297, #128015, #162562, #14134, #196123, #45617, #94373, #80227, #146325, #75965, #177740, #29355, #125869, #43491, #212340, #109611, #175616, #79159, #27203, #93310, #10942, #12019, #78091, #144218, #95449, #161499, #210212, #13079, #145275, #183048, #6, #33604, #65024, #50926, #181973, #213403, #117051, #34663 ),
 ( #149493, #163627, #85546, #16263, #15208, #197169, #18406, #83411, #1076, #67141, #133275, #147376, #31495, #100733, #199283, #198222, #48805, #81299, #82347, #97570, #179870, #132213, #84482, #101802, #200346, #17330, #98617, #166812, #164678, #114922, #131179, #49858, #113875, #180921, #32542, #118121, #150572, #2134, #68210, #148438, #66071, #115985, #99674, #134341, #51995, #184106, #165744, #35726, #167871, #19469, #151636, #3203, #69272, #135386, #201407, #168932, #54125, #55189, #140744, #103949, #102874, #169991, #188373, #7480, #53046, #173223, #90904, #20535, #86617, #71407, #38939, #187312, #122414, #57320, #6410, #119179, #73562, #120262, #171061, #121336, #185165, #105022, #137519, #186237, #136454, #139663, #156967, #5327, #21577, #22657, #205684, #123485, #153756, #24802, #203536, #202472, #88768, #154825, #70337, #87683, #72482, #138583, #107198, #189448, #8558, #40011, #74637, #36789, #37871, #204606, #56257, #106122, #152685, #4267, #172145, #23737, #89843, #155892, #41090, #161219, #208874, #11748, #142872, #110402, #178537, #174293, #177472, #25868, #112524, #77823, #91978, #43226, #75700, #158036, #60504, #206755, #9623, #141814, #211007, #29086, #127746, #28012, #124542, #175353, #126664, #10680, #94110, #95170, #160151, #207817, #190499, #59445, #58386, #125602, #93041, #191562, #159083, #109343, #108272, #26933, #192629, #79952, #76751, #42157, #44281, #193703, #12806, #176406, #30147, #96236, #143944, #209940, #61578, #45347, #111466, #78879, #62630, #145002, #128790, #194771, #46408, #162286, #13874, #146055, #214175, #15995, #147113, #14930, #18131, #183851, #98346, #48543, #197960, #166543, #100468, #32280, #51736, #82081, #81025, #164411, #148173, #163355, #114661, #180655, #65802, #200087, #84220, #35463, #66865, #117859, #212069, #213139, #131949, #49589, #115713, #63707, #101541, #113598, #149222, #129864, #64769, #133010, #150308, #181703, #165469, #33333, #99415, #167610, #179601, #116781, #31222, #19208, #17065, #97296, #83144, #47488, #130911, #50655, #797, #199010, #182778, #34396, #196903, #195847, #1874, #67934, #134079, #20275, #201148, #202211, #2942, #151373, #103689, #204341, #73293, #171881, #203284, #70079, #72218, #135131, #118925, #71147, #187050, #69014, #155634, #87434, #188118, #53865, #85287, #39749, #89585, #136193, #102616, #105854, #23478, #119998, #185975, #122150, #189196, #169738, #37608, #184905, #172965, #40833, #52786, #7219, #153502, #139396, #21327, #36529, #168671, #38682, #205429, #57067, #106942, #104761, #5072, #123231, #86359, #152430, #22401, #170810, #4009, #137264, #54931, #121083, #88510, #55999, #154572, #6148, #138325, #177222, #112284, #208624, #176164, #93860, #174044, #42977, #191309, #159898, #125346, #158836, #190249, #27764, #92791, #124290, #11505, #77576, #10433, #142616, #60258, #75449, #157780, #126415, #46170, #141562, #24544, #140489, #26689, #192378, #74388, #210772, #61335, #8304, #193465, #90652, #206500, #156713, #41907, #76505, #45109, #94923, #44033, #58131, #108018, #143699, #25617, #110151, #91729, #9378, #207570, #59191, #209691, #109087, #127494, #111219, #175102, #28835, #160972, #12562, #194522, #78636, #62392, #144761, #128557, #119477, #196662, #103164, #19763, #169225, #49353, #163111, #65560, #197711, #48303, #118411, #64529 ),
 ( #102095, #135675, #178300, #86913, #4556, #79708, #145823, #114414, #164170, #98118, #36016, #185465, #131707, #54418, #201700, #179361, #81839, #32032, #29907, #15755, #180414, #30983, #47241, #53343, #70630, #130674, #80787, #147923, #37085, #20817, #213939, #152981, #184396, #113356, #168165, #85845, #195606, #146877, #212897, #151922, #136741, #202768, #95992, #3495, #162045, #13635, #97058, #69565, #211828, #63465, #129620, #14692, #87980, #123775, #120559, #121632, #107498, #74932, #122714, #139959, #56554, #24027, #92283, #154054, #91201, #5621, #26165, #205982, #71702, #22951, #21873, #203833, #25099, #90130, #156197, #73864, #57618, #137814, #38166, #41387, #189735, #204900, #55479, #187601, #89065, #104239, #186537, #138882, #157262, #108563, #207049, #7773, #105320, #173526, #171357, #39228, #155123, #188676, #170285, #6705, #72782, #124828, #8853, #141042, #58681, #40310, #106417, #172440, #190795, #42455, #174591, #158328, #9921, #75995, #142100, #208113, #93340, #80258, #130159, #111764, #147404, #59742, #112829, #159376, #61878, #60808, #43520, #27232, #191859, #128043, #10975, #29386, #30456, #210242, #126969, #79191, #196151, #15238, #13113, #97597, #178845, #78119, #212370, #144249, #47791, #96542, #113905, #145306, #44583, #161528, #211311, #193998, #62936, #160444, #109643, #77048, #45647, #129104, #125901, #179900, #177771, #162589, #176696, #175646, #14163, #64011, #110696, #143178, #146357, #31523, #28309, #94405, #163656, #81325, #95480, #12051, #209170, #192927, #195078, #46716, #135418, #1111, #151669, #99706, #213430, #131209, #166844, #201439, #53080, #168963, #100762, #182002, #119215, #185198, #197197, #150605, #18440, #48836, #32573, #36823, #102904, #82379, #118154, #65053, #98649, #20567, #3240, #86650, #183081, #2165, #68242, #148470, #17361, #165778, #134376, #83445, #133307, #164706, #200380, #67172, #16294, #52028, #184138, #199312, #117082, #34693, #49892, #132244, #84517, #114950, #116016, #180950, #38, #50958, #35762, #66102, #198252, #101837, #33633, #167905, #149525, #19503, #85579, #69306, #72521, #190537, #105060, #55224, #204640, #173259, #107238, #38974, #58423, #22689, #21611, #171098, #88802, #170025, #121370, #187345, #154861, #206791, #24840, #42193, #73596, #124576, #4300, #87719, #6443, #138617, #56291, #70371, #108308, #120297, #155929, #152718, #153792, #139698, #90939, #122451, #172182, #188410, #40047, #174328, #186270, #123519, #37906, #25904, #23772, #103982, #106156, #54158, #5361, #57356, #89877, #7514, #205721, #189483, #71443, #136486, #41126, #157005, #8591, #137555, #203573, #74673, #202508, #140776, #110439, #211042, #79991, #178577, #209974, #76788, #78917, #142910, #175385, #125637, #28053, #92014, #43260, #191598, #96275, #128827, #12843, #127785, #9660, #60544, #94146, #176441, #193740, #194809, #45386, #93076, #75736, #109378, #158072, #26971, #192663, #208910, #44317, #126702, #207854, #159118, #160185, #179642, #11786, #141849, #77860, #145039, #46445, #59480, #212106, #129902, #10719, #143983, #61615, #111502, #177508, #161256, #162325, #29120, #95207, #112566, #62668, #30185, #13909, #146095, #63743, #195886, #47524, #113637, #117898, #67976, #166586, #66908, #163394, #214214, #181743, #49627, #133048, #134119, #199050, #32317, #14968, #130952, #97336 ),
 ( #148212, #18175, #200128, #31262, #151412, #69053, #147151, #213176, #115752, #17103, #165511, #100511, #35503, #50696, #118964, #51781, #98385, #149264, #99454, #81065, #83181, #33373, #164449, #114698, #183891, #135173, #198001, #65843, #843, #101580, #167648, #131992, #2986, #116820, #180692, #182822, #34438, #48582, #84262, #150347, #1917, #85329, #19249, #201188, #52827, #64805, #196942, #16036, #82119, #121124, #22438, #36569, #90691, #152469, #188157, #184942, #186013, #171921, #139436, #187088, #204383, #38722, #88549, #156753, #4049, #155675, #70119, #8342, #56039, #136230, #87475, #86402, #53904, #89623, #154610, #6189, #138366, #122195, #202253, #102655, #105897, #39790, #54972, #120039, #37649, #153541, #168712, #20316, #203321, #7257, #173003, #57103, #72258, #169778, #23517, #21367, #103727, #5110, #104803, #71187, #137304, #170848, #189234, #73333, #205471, #123272, #40873, #106978, #24584, #74427, #140527, #206539, #58169, #208663, #59224, #25654, #26726, #41944, #190287, #142653, #28872, #112320, #210805, #27800, #109126, #111255, #175140, #207605, #157820, #60294, #124327, #75487, #9416, #128593, #161005, #45143, #159937, #108057, #92828, #126452, #192415, #11542, #12600, #77612, #125382, #174082, #141598, #91764, #191348, #10468, #158872, #76542, #44070, #43013, #110189, #176199, #211864, #93898, #143735, #209729, #177258, #78672, #61372, #29944, #162080, #127530, #193502, #94957, #144798, #62430, #194559, #46204, #178335, #96029, #13669, #79741, #145858, #131741, #63503, #197746, #147959, #64565, #146911, #150084, #101312, #15789, #180449, #115503, #83995, #17909, #164202, #183630, #213972, #212929, #81875, #65592, #80821, #32066, #98155, #49384, #117638, #1655, #167393, #198794, #35237, #129657, #130708, #97092, #33126, #199870, #82931, #51513, #18984, #16848, #85065, #182555, #181498, #67712, #99206, #151151, #116562, #195641, #149004, #48339, #165255, #580, #66646, #132791, #50443, #113389, #34179, #114450, #100251, #166320, #133863, #47277, #179398, #31018, #163145, #14729, #196699, #68792, #73067, #4841, #105618, #119767, #2720, #171647, #6987, #201978, #20049, #23244, #89356, #185747, #37380, #39518, #106710, #21098, #103455, #102383, #90418, #172736, #184684, #139166, #70920, #155404, #169517, #134912, #200919, #170578, #205197, #56838, #24312, #104532, #87201, #123011, #188963, #52567, #154341, #22161, #118698, #36304, #40605, #168450, #86137, #121923, #152208, #3778, #69852, #135962, #53634, #186825, #5919, #71991, #153266, #137031, #203058, #138103, #54701, #120851, #38455, #204113, #88276, #55765, #187890, #159674, #76287, #60038, #192154, #207353, #75229, #126191, #178069, #58973, #29687, #57902, #158616, #43817, #206279, #128341, #193239, #140257, #110992, #8076, #124066, #74164, #107795, #142396, #176997, #12339, #208404, #156487, #190031, #209465, #41684, #10213, #157559, #173820, #25398, #91498, #109932, #9152, #125128, #141339, #175941, #78419, #27537, #144541, #112068, #93632, #194307, #61108, #174885, #94703, #26465, #210548, #127268, #62184, #28613, #191086, #42755, #108859, #92574, #11276, #160744, #45948, #77355, #143468, #44886, #148762, #195382, #97898, #96839, #79489, #63240, #13414, #163957, #129402, #146657, #47014, #65345, #17662, #115255, #83747, #51265, #49139, #133617 ) ),
 .UNSPECIFIED., .T., .F., .T. ) 
 B_SPLINE_SURFACE_WITH_KNOTS ( ( 4, 3, 4 ),
 ( 4, 1, 1, 1, 1, 1, 1, 1, 1, 1, 1, 1, 1, 1, 1, 1, 1, 1, 1, 1, 1, 1, 1, 1, 1, 1, 1, 1, 1, 1, 1, 1, 1, 1, 1, 1, 1, 1, 1, 1, 1, 1, 1, 1, 1, 1, 1, 1, 1, 1, 1, 1, 1, 1, 1, 1, 1, 1, 1, 1, 1, 1, 1, 1, 1, 1, 1, 1, 1, 1, 1, 1, 1, 1, 1, 1, 1, 1, 1, 1, 1, 1, 1, 1, 1, 1, 1, 1, 1, 1, 1, 1, 1, 1, 1, 1, 1, 1, 1, 1, 1, 1, 1, 1, 1, 1, 1, 1, 1, 1, 1, 1, 1, 1, 1, 1, 1, 1, 1, 1, 1, 1, 1, 1, 1, 1, 1, 1, 1, 1, 1, 1, 1, 1, 1, 1, 1, 1, 1, 1, 1, 1, 1, 1, 1, 1, 1, 1, 1, 1, 1, 1, 1, 1, 1, 1, 1, 1, 1, 1, 1, 1, 1, 1, 1, 1, 1, 1, 1, 1, 1, 1, 1, 1, 1, 1, 1, 1, 1, 1, 1, 1, 1, 1, 1, 1, 1, 1, 1, 1, 1, 1, 1, 1, 1, 1, 1, 1, 1, 1, 1, 1, 1, 1, 1, 1, 1, 1, 1, 1, 1, 1, 1, 1, 1, 1, 1, 1, 1, 1, 1, 1, 1, 1, 1, 1, 1, 1, 1, 1, 1, 1, 1, 1, 1, 1, 1, 1, 1, 1, 1, 1, 1, 1, 1, 1, 1, 1, 1, 1, 1, 1, 1, 1, 1, 1, 1, 1, 1, 1, 1, 1, 1, 1, 1, 1, 1, 1, 1, 1, 1, 1, 1, 1, 1, 1, 1, 1, 1, 1, 1, 1, 1, 1, 1, 1, 1, 1, 1, 1, 1, 1, 1, 1, 1, 1, 1, 1, 1, 1, 1, 1, 1, 1, 1, 1, 1, 1, 1, 1, 1, 1, 1, 1, 1, 1, 1, 1, 1, 1, 1, 1, 1, 1, 1, 1, 1, 1, 1, 1, 1, 1, 1, 1, 1, 1, 1, 1, 1, 1, 1, 1, 1, 1, 1, 1, 1, 1, 1, 1, 1, 1, 1, 1, 1, 1, 1, 1, 1, 1, 1, 1, 1, 1, 1, 1, 1, 1, 1, 1, 1, 1, 1, 1, 1, 1, 1, 1, 1, 1, 1, 1, 1, 1, 4 ),
 ( 0.000000000000000000, 0.5000000000000000000, 1.000000000000000000 ),
 ( 0.000000000000000000, 0.002600033395298661284, 0.005208813367820810773, 0.007813200023264601363, 0.01041635779573905213, 0.01302082523971277370, 0.01562491580351430334, 0.01822918961192645723, 0.02083333155136493989, 0.02343746137460561707, 0.02604174567981391505, 0.02864576082122225614, 0.03125012338981237453, 0.03385410379569547823, 0.03645843966640821554, 0.03906250599122108869, 0.04166672065998115043, 0.04427093656960304907, 0.04687500111868234121, 0.04947933663890847350, 0.05208331727515622817, 0.05468767913406928638, 0.05729168951085979872, 0.05989597295159828499, 0.06250011041458469752, 0.06510424634142775169, 0.06770853038940542745, 0.07031253939703428768, 0.07291690072920921362, 0.07552088074063932621, 0.07812521459448035221, 0.08072927904253822395, 0.08333349217322323643, 0.08593770650149938628, 0.08854176936806532061, 0.09114610329512429221, 0.09375008230893774885, 0.09635444258075796797, 0.09895845137230636912, 0.1015627332241899466, 0.1041668691376404637, 0.1067710034717011397, 0.1093752859901425123, 0.1119792934252105548, 0.1145836532378000650, 0.1171876317139315254, 0.1197919640503514460, 0.1223960270027875247, 0.1250002386107842423, 0.1276044514713231270, 0.1302085128224930721, 0.1328128452953424854, 0.1354168228245230532, 0.1380211816480703679, 0.1406251889951717071, 0.1432294693974442978, 0.1458336039016293884, 0.1484377367829480265, 0.1510420179109137340, 0.1536460239143070949, 0.1562503823458506746, 0.1588543594276481397, 0.1614586903853630351, 0.1640627519827278502, 0.1666669622076225599, 0.1692711737400035832, 0.1718752337163205746, 0.1744795648736557347, 0.1770835410591554138, 0.1796878985729436218, 0.1822919046164021839, 0.1848961837081005144, 0.1875003169431251615, 0.1901044485118078553, 0.1927087283883223978, 0.1953127331008320255, 0.1979170902898210183, 0.2005210661182068033, 0.2031253958358791578, 0.2057294562186703923, 0.2083336651999991573, 0.2109378755437518183, 0.2135419342857080849, 0.2161462642661750033, 0.2187502392488957503, 0.2213545955913898966, 0.2239586004719608947, 0.2265628783920732026, 0.2291670104979939837, 0.2317711408940984485, 0.2343754196581391558, 0.2369794232205082452, 0.2395837793053874898, 0.2421877540212369617, 0.2447920826374832270, 0.2473961419461526701, 0.2500003498234057431, 0.2526045591180144934, 0.2552086167660569949, 0.2578129457082574683, 0.2604169196290564980, 0.2630212749386780513, 0.2656252787970727613, 0.2682295556845439854, 0.2708336868013750398, 0.2734378161649161920, 0.2760420939554183439, 0.2786460965083475960, 0.2812504516275206035, 0.2838544253716674404, 0.2864587530250631842, 0.2890628114000217685, 0.2916670183126490179, 0.2942712266975582858, 0.2968752833920936807, 0.2994796114345903981, 0.3020835844342854570, 0.3046879388494173613, 0.3072919418263086455, 0.3098962178200457829, 0.3125003480877632800, 0.3151044765587182606, 0.3177087535145803887, 0.3203127551987332566, 0.3229171094905676220, 0.3255210824038090589, 0.3281254092328941829, 0.3307294668145174810, 0.3333336729019333866, 0.3359378805165532667, 0.3385419363979534357, 0.3411462636792753078, 0.3437502358986498918, 0.3463545895576419231, 0.3489585917936692261, 0.3515628670325462446, 0.3541669965910940188, 0.3567711243094072171, 0.3593754005694961839, 0.3619794015255044517, 0.3645837551283364619, 0.3671877273514386752, 0.3697920534947228832, 0.3723961104233561858, 0.3750003158249449187, 0.3776045228086560845, 0.3802085780172632101, 0.3828129046759103926, 0.3854168762557192984, 0.3880212292968930887, 0.3906252309326675998, 0.3932295055555311003, 0.3958336345448258409, 0.3984377616504144459, 0.4010420373535708016, 0.4036460377220391638, 0.4062503907741795706, 0.4088543624478828686, 0.4114586880438503846, 0.4140627444598136697, 0.4166669493149349202, 0.4192711558070936761, 0.4218752104832254046, 0.4244795366576747386, 0.4270835077386489487, 0.4296878603003031483, 0.4322918614764136302, 0.4348961356220873986, 0.4375002641820237570, 0.4401043908147829753, 0.4427086660998260093, 0.4453126660213379551, 0.4479170186610768045, 0.4505209899261007900, 0.4531253151132156320, 0.4557293711568096706, 0.4583335756048029785, 0.4609377817447468106, 0.4635418360287018591, 0.4661461618574116450, 0.4687501325802634344, 0.4713544848006788190, 0.4739584856576960492, 0.4765627594649867738, 0.4791668877354426925, 0.4817710140352507997, 0.4843752890409837031, 0.4869792886561065681, 0.4895836410217184742, 0.4921876120187673176, 0.4947919369354787933, 0.4973959927469893683, 0.5000001969271801183, 0.5026044028542325792, 0.5052084568862954539, 0.5078127825077110025, 0.5104167530131399344, 0.5130211050305848453, 0.5156251057090676104, 0.5182293793167697116, 0.5208335074376115870, 0.5234376335443351458, 0.5260419084095501185, 0.5286459078588399141, 0.5312502600885893322, 0.5338542309583571566, 0.5364585557431046370, 0.5390626114628084276, 0.5416668155145124564, 0.5442710213679887721, 0.5468750752884355970, 0.5494794008409938924, 0.5520833712696913143, 0.5546877232224267651, 0.5572917238629264691, 0.5598959974098275394, 0.5625001255209155504, 0.5651042515744146844, 0.5677085264378984863, 0.5703125258619060611, 0.5729168780940517847, 0.5755208489772277725, 0.5781251737684461878, 0.5807292295366155432, 0.5833334335991446906, 0.5859376395183565345, 0.5885416934674594369, 0.5911460190895951872, 0.5937499895822500040, 0.5963543416085342885, 0.5989583423516006144, 0.6015626159764864145, 0.6041667442176794633, 0.6067708703578130747, 0.6093751453583519107, 0.6119791448976270587, 0.6145834972704286026, 0.6171874683077025470, 0.6197917932438269384, 0.6223958492007358734, 0.6250000534134032559, 0.6276042595376638555, 0.6302083136556971832, 0.6328126394858472059, 0.6354166101831504321, 0.6380209624212449526, 0.6406249634074311361, 0.6432292372490908683, 0.6458333657602520761, 0.6484374921268833969, 0.6510417674032679125, 0.6536457671983656459, 0.6562501198500874100, 0.6588540911821543222, 0.6614584164016259482, 0.6640624726875546946, 0.6666666771896793131, 0.6692708836583093346, 0.6718749380855545406, 0.6744792642621626477, 0.6770832353048136243, 0.6796875878929879988, 0.6822915892628557133, 0.6848958634600870177, 0.6874999923810890534, 0.6901041191140900866, 0.6927083948051209195, 0.6953123949966061312, 0.6979167480655225075, 0.7005207198330885010, 0.7031250454743595002, 0.7057291022295995031, 0.7083333071605121267, 0.7109375141128444486, 0.7135415689895947544, 0.7161458956511181917, 0.7187498671798290273, 0.7213542202563657524, 0.7239582221504904380, 0.7265624968421051655, 0.7291666263128349090, 0.7317707535520923123, 0.7343750297965853102, 0.7369790305250381035, 0.7395833841494394711, 0.7421873564932268685, 0.7447916826947649227, 0.7473957400596251688, 0.7499999455586733310, 0.7526041531340577073, 0.7552082086006238759, 0.7578125358855373195, 0.7604165080410384414, 0.7630208617442386654, 0.7656248643032155243, 0.7682291396280439555, 0.7708332697884082707, 0.7734373976738285750, 0.7760416746106194585, 0.7786456760166404756, 0.7812500303348380859, 0.7838540033955903041, 0.7864583302958847444, 0.7890623884106959807, 0.7916665946172487534, 0.7942708029550582527, 0.7968748591517740287, 0.7994791871985751364, 0.8020831601216208417, 0.8046875145898089166, 0.8072915179542569097, 0.8098957940511537501, 0.8124999250410844809, 0.8151040537125986418, 0.8177083314805486669, 0.8203123337047645292, 0.8229166888550945025, 0.8255206627735817149, 0.8281249905111484066, 0.8307290495162685806, 0.8333332565697225691, 0.8359374658093579047, 0.8385415228765847884, 0.8411458518237998616, 0.8437498256551729803, 0.8463541810267020127, 0.8489581853372698550, 0.8515624623451190089, 0.8541665943045783083, 0.8567707239021479237, 0.8593750026401490993, 0.8619790058232168484, 0.8645833619440471685, 0.8671873368610717447, 0.8697916655744575287, 0.8723957256102774505, 0.8749999336500613456, 0.8776041439309557601, 0.8802082020090884473, 0.8828125319952765393, 0.8854165068757942070, 0.8880208632890512765, 0.8906248686864229880, 0.8932291467441429988, 0.8958332798131283248, 0.8984374104767501867, 0.9010416903237299380, 0.9036456946063434748, 0.9062500518360779855, 0.9088540278924787108, 0.9114583577202677311, 0.9140624189272162914, 0.9166666280927961985, 0.9192708395544209043, 0.9218748987838942810, 0.9244792299476556341, 0.9270832060181642964, 0.9296875636115721209, 0.9322915702365133228, 0.9348958494830461596, 0.9374999838014769216, 0.9401041156712998115, 0.9427083967663798525, 0.9453124022892170908, 0.9479167607665550666, 0.9505207380999710631, 0.9531250691809918241, 0.9557291317261836783, 0.9583333421310490374, 0.9609375547886240820, 0.9635416155522130710, 0.9661459483928183101, 0.9687499245033458495, 0.9713542829945021051, 0.9739582954330652242, 0.9765625745907361432, 0.9791667024412501474, 0.9817708385604039245, 0.9843751096149007118, 0.9869791944699233266, 0.9895836584107432499, 0.9921868132917668337, 0.9947911946869415489, 0.9973999724172807335, 1.000000000000000000 ),
 .UNSPECIFIED. ) 
 GEOMETRIC_REPRESENTATION_ITEM ( )  RATIONAL_B_SPLINE_SURFACE ( (
 ( 1.000000000000000000, 1.000000000000000000, 1.000000000000000000, 0.9999999999999997780, 1.000000000000000000, 1.000000000000000000, 1.000000000000000000, 1.000000000000000222, 1.000000000000000000, 1.000000000000000000, 1.000000000000000222, 0.9999999999999997780, 1.000000000000000222, 1.000000000000000222, 1.000000000000000000, 1.000000000000000000, 1.000000000000000000, 0.9999999999999997780, 1.000000000000000222, 0.9999999999999996669, 1.000000000000000222, 1.000000000000000000, 1.000000000000000000, 0.9999999999999996669, 1.000000000000000444, 0.9999999999999996669, 1.000000000000000444, 1.000000000000000000, 1.000000000000000000, 0.9999999999999997780, 1.000000000000000222, 0.9999999999999994449, 1.000000000000000444, 1.000000000000000000, 1.000000000000000000, 1.000000000000000000, 1.000000000000000000, 1.000000000000000444, 0.9999999999999997780, 1.000000000000000000, 1.000000000000000000, 1.000000000000000000, 1.000000000000000000, 1.000000000000000000, 1.000000000000000000, 0.9999999999999997780, 1.000000000000000000, 1.000000000000000444, 0.9999999999999997780, 1.000000000000000444, 0.9999999999999997780, 0.9999999999999997780, 1.000000000000000000, 1.000000000000000222, 1.000000000000000000, 1.000000000000000000, 1.000000000000000000, 1.000000000000000000, 0.9999999999999997780, 1.000000000000000444, 0.9999999999999997780, 1.000000000000000000, 1.000000000000000222, 0.9999999999999997780, 1.000000000000000000, 1.000000000000000222, 0.9999999999999997780, 1.000000000000000222, 1.000000000000000000, 1.000000000000000222, 1.000000000000000000, 1.000000000000000222, 0.9999999999999997780, 1.000000000000000000, 1.000000000000000222, 1.000000000000000000, 1.000000000000000222, 0.9999999999999997780, 1.000000000000000222, 0.9999999999999997780, 1.000000000000000222, 0.9999999999999997780, 1.000000000000000222, 1.000000000000000222, 0.9999999999999997780, 1.000000000000000222, 1.000000000000000222, 0.9999999999999997780, 1.000000000000000222, 1.000000000000000000, 1.000000000000000000, 1.000000000000000222, 0.9999999999999996669, 1.000000000000000444, 0.9999999999999997780, 0.9999999999999997780, 1.000000000000000000, 1.000000000000000000, 1.000000000000000000, 0.9999999999999996669, 1.000000000000000444, 1.000000000000000000, 1.000000000000000222, 1.000000000000000000, 0.9999999999999997780, 1.000000000000000222, 0.9999999999999997780, 1.000000000000000222, 1.000000000000000000, 1.000000000000000000, 1.000000000000000222, 1.000000000000000000, 1.000000000000000222, 0.9999999999999994449, 1.000000000000000444, 1.000000000000000000, 0.9999999999999996669, 1.000000000000000222, 0.9999999999999997780, 1.000000000000000222, 0.9999999999999997780, 1.000000000000000000, 1.000000000000000000, 1.000000000000000000, 1.000000000000000000, 1.000000000000000000, 1.000000000000000444, 1.000000000000000000, 1.000000000000000000, 1.000000000000000222, 1.000000000000000000, 1.000000000000000000, 0.9999999999999997780, 1.000000000000000000, 1.000000000000000222, 1.000000000000000000, 1.000000000000000222, 0.9999999999999997780, 1.000000000000000000, 0.9999999999999997780, 0.9999999999999997780, 1.000000000000000222, 0.9999999999999997780, 1.000000000000000444, 0.9999999999999997780, 1.000000000000000000, 1.000000000000000222, 1.000000000000000000, 1.000000000000000000, 0.9999999999999997780, 1.000000000000000222, 1.000000000000000000, 1.000000000000000000, 1.000000000000000000, 1.000000000000000222, 0.9999999999999996669, 1.000000000000000222, 1.000000000000000222, 0.9999999999999996669, 1.000000000000000444, 0.9999999999999996669, 1.000000000000000000, 1.000000000000000222, 0.9999999999999996669, 1.000000000000000222, 1.000000000000000000, 1.000000000000000222, 1.000000000000000000, 1.000000000000000222, 0.9999999999999997780, 1.000000000000000444, 0.9999999999999997780, 0.9999999999999997780, 1.000000000000000222, 0.9999999999999996669, 1.000000000000000222, 1.000000000000000000, 1.000000000000000000, 1.000000000000000000, 0.9999999999999997780, 1.000000000000000222, 1.000000000000000222, 0.9999999999999997780, 1.000000000000000222, 0.9999999999999997780, 1.000000000000000222, 1.000000000000000000, 1.000000000000000444, 1.000000000000000000, 1.000000000000000222, 0.9999999999999996669, 1.000000000000000444, 0.9999999999999993339, 1.000000000000000444, 0.9999999999999997780, 1.000000000000000444, 0.9999999999999997780, 1.000000000000000000, 1.000000000000000000, 0.9999999999999997780, 1.000000000000000222, 0.9999999999999997780, 0.9999999999999996669, 1.000000000000000444, 1.000000000000000222, 1.000000000000000000, 0.9999999999999997780, 1.000000000000000222, 0.9999999999999996669, 1.000000000000000222, 0.9999999999999997780, 1.000000000000000222, 1.000000000000000000, 1.000000000000000000, 1.000000000000000000, 1.000000000000000000, 0.9999999999999997780, 1.000000000000000000, 1.000000000000000000, 0.9999999999999997780, 1.000000000000000000, 1.000000000000000000, 1.000000000000000000, 1.000000000000000222, 1.000000000000000000, 1.000000000000000444, 1.000000000000000222, 1.000000000000000000, 1.000000000000000000, 0.9999999999999997780, 1.000000000000000222, 1.000000000000000000, 1.000000000000000000, 1.000000000000000000, 0.9999999999999997780, 1.000000000000000222, 0.9999999999999997780, 1.000000000000000222, 1.000000000000000444, 0.9999999999999997780, 1.000000000000000222, 1.000000000000000000, 1.000000000000000000, 1.000000000000000000, 0.9999999999999997780, 1.000000000000000444, 0.9999999999999997780, 1.000000000000000222, 0.9999999999999997780, 1.000000000000000222, 0.9999999999999994449, 1.000000000000000222, 1.000000000000000000, 1.000000000000000222, 1.000000000000000000, 0.9999999999999997780, 1.000000000000000222, 1.000000000000000000, 0.9999999999999997780, 1.000000000000000444, 0.9999999999999996669, 1.000000000000000222, 1.000000000000000000, 1.000000000000000000, 1.000000000000000222, 0.9999999999999997780, 0.9999999999999997780, 1.000000000000000444, 1.000000000000000222, 1.000000000000000000, 0.9999999999999997780, 0.9999999999999997780, 1.000000000000000222, 1.000000000000000000, 1.000000000000000222, 1.000000000000000000, 0.9999999999999997780, 1.000000000000000000, 1.000000000000000000, 1.000000000000000000, 1.000000000000000222, 0.9999999999999997780, 1.000000000000000222, 1.000000000000000000, 1.000000000000000000, 1.000000000000000000, 0.9999999999999997780, 1.000000000000000000, 1.000000000000000222, 1.000000000000000222, 0.9999999999999996669, 1.000000000000000444, 0.9999999999999996669, 1.000000000000000222, 1.000000000000000000, 1.000000000000000222, 0.9999999999999997780, 1.000000000000000444, 1.000000000000000000, 1.000000000000000444, 0.9999999999999994449, 1.000000000000000222, 0.9999999999999997780, 0.9999999999999997780, 1.000000000000000000, 1.000000000000000222, 1.000000000000000000, 1.000000000000000000, 1.000000000000000000, 1.000000000000000222, 0.9999999999999996669, 1.000000000000000222, 1.000000000000000000, 0.9999999999999996669, 1.000000000000000444, 1.000000000000000000, 1.000000000000000000, 1.000000000000000000, 0.9999999999999996669, 1.000000000000000222, 1.000000000000000000, 1.000000000000000000, 1.000000000000000222, 0.9999999999999997780, 0.9999999999999997780, 1.000000000000000000, 1.000000000000000000, 1.000000000000000222, 0.9999999999999997780, 1.000000000000000222, 1.000000000000000000, 1.000000000000000000, 0.9999999999999996669, 1.000000000000000222, 1.000000000000000000, 1.000000000000000222, 1.000000000000000000, 1.000000000000000000, 1.000000000000000000, 0.9999999999999997780, 1.000000000000000222, 0.9999999999999996669, 1.000000000000000444, 1.000000000000000000, 0.9999999999999997780, 1.000000000000000000, 1.000000000000000222, 1.000000000000000222, 0.9999999999999996669, 1.000000000000000000, 1.000000000000000000, 0.9999999999999997780, 1.000000000000000222, 1.000000000000000000, 1.000000000000000222, 0.9999999999999996669, 1.000000000000000444, 1.000000000000000000, 1.000000000000000000, 1.000000000000000000, 1.000000000000000222, 1.000000000000000000, 0.9999999999999997780, 1.000000000000000444, 1.000000000000000000, 1.000000000000000444, 0.9999999999999997780, 1.000000000000000444, 1.000000000000000000, 1.000000000000000222, 1.000000000000000222, 1.000000000000000000, 0.9999999999999996669, 1.000000000000000000, 1.000000000000000000, 1.000000000000000000, 1.000000000000000000, 1.000000000000000222, 0.9999999999999996669, 1.000000000000000000, 1.000000000000000222, 0.9999999999999997780, 0.9999999999999997780, 1.000000000000000000, 1.000000000000000000, 1.000000000000000000, 1.000000000000000000),
 ( 0.3333333333333333703, 0.3333333333333333703, 0.3333333333333333703, 0.3333333333333333148, 0.3333333333333333703, 0.3333333333333333148, 0.3333333333333333703, 0.3333333333333334259, 0.3333333333333333703, 0.3333333333333333148, 0.3333333333333334259, 0.3333333333333332593, 0.3333333333333334259, 0.3333333333333333703, 0.3333333333333333703, 0.3333333333333332593, 0.3333333333333334259, 0.3333333333333333148, 0.3333333333333334259, 0.3333333333333333148, 0.3333333333333334259, 0.3333333333333334259, 0.3333333333333333148, 0.3333333333333333148, 0.3333333333333334814, 0.3333333333333332593, 0.3333333333333334259, 0.3333333333333334259, 0.3333333333333333703, 0.3333333333333333703, 0.3333333333333334814, 0.3333333333333332038, 0.3333333333333334814, 0.3333333333333333703, 0.3333333333333334259, 0.3333333333333333148, 0.3333333333333334259, 0.3333333333333334814, 0.3333333333333333703, 0.3333333333333332593, 0.3333333333333334259, 0.3333333333333333148, 0.3333333333333333148, 0.3333333333333333703, 0.3333333333333333703, 0.3333333333333334259, 0.3333333333333333148, 0.3333333333333335369, 0.3333333333333333148, 0.3333333333333334259, 0.3333333333333333703, 0.3333333333333332038, 0.3333333333333334259, 0.3333333333333334259, 0.3333333333333333148, 0.3333333333333334259, 0.3333333333333333703, 0.3333333333333333703, 0.3333333333333334259, 0.3333333333333334259, 0.3333333333333333703, 0.3333333333333334259, 0.3333333333333334259, 0.3333333333333333148, 0.3333333333333333703, 0.3333333333333333703, 0.3333333333333333148, 0.3333333333333334259, 0.3333333333333333148, 0.3333333333333334814, 0.3333333333333333703, 0.3333333333333334259, 0.3333333333333333148, 0.3333333333333333703, 0.3333333333333334259, 0.3333333333333333703, 0.3333333333333333703, 0.3333333333333333148, 0.3333333333333334259, 0.3333333333333333148, 0.3333333333333334259, 0.3333333333333333703, 0.3333333333333334259, 0.3333333333333334814, 0.3333333333333333148, 0.3333333333333334259, 0.3333333333333334259, 0.3333333333333333148, 0.3333333333333333703, 0.3333333333333333703, 0.3333333333333333148, 0.3333333333333334814, 0.3333333333333332593, 0.3333333333333334259, 0.3333333333333333703, 0.3333333333333333148, 0.3333333333333333703, 0.3333333333333333703, 0.3333333333333334259, 0.3333333333333333148, 0.3333333333333334259, 0.3333333333333333148, 0.3333333333333334814, 0.3333333333333333148, 0.3333333333333333148, 0.3333333333333334259, 0.3333333333333333148, 0.3333333333333333703, 0.3333333333333333703, 0.3333333333333334259, 0.3333333333333333703, 0.3333333333333334259, 0.3333333333333333703, 0.3333333333333332593, 0.3333333333333334259, 0.3333333333333333703, 0.3333333333333333148, 0.3333333333333334814, 0.3333333333333333148, 0.3333333333333334259, 0.3333333333333334259, 0.3333333333333333148, 0.3333333333333333703, 0.3333333333333334259, 0.3333333333333333703, 0.3333333333333333703, 0.3333333333333334259, 0.3333333333333333703, 0.3333333333333334259, 0.3333333333333333703, 0.3333333333333334259, 0.3333333333333333148, 0.3333333333333333703, 0.3333333333333333703, 0.3333333333333333703, 0.3333333333333333703, 0.3333333333333335369, 0.3333333333333332593, 0.3333333333333333703, 0.3333333333333333703, 0.3333333333333332593, 0.3333333333333333703, 0.3333333333333333703, 0.3333333333333334259, 0.3333333333333332593, 0.3333333333333333703, 0.3333333333333333703, 0.3333333333333333703, 0.3333333333333333703, 0.3333333333333333703, 0.3333333333333334259, 0.3333333333333333148, 0.3333333333333334259, 0.3333333333333333703, 0.3333333333333334814, 0.3333333333333332593, 0.3333333333333333703, 0.3333333333333334814, 0.3333333333333332038, 0.3333333333333334259, 0.3333333333333333148, 0.3333333333333333703, 0.3333333333333334814, 0.3333333333333332038, 0.3333333333333334259, 0.3333333333333333703, 0.3333333333333333703, 0.3333333333333333703, 0.3333333333333334259, 0.3333333333333333703, 0.3333333333333335369, 0.3333333333333333148, 0.3333333333333333148, 0.3333333333333334259, 0.3333333333333333148, 0.3333333333333333703, 0.3333333333333333703, 0.3333333333333334259, 0.3333333333333333148, 0.3333333333333334259, 0.3333333333333332593, 0.3333333333333334814, 0.3333333333333333703, 0.3333333333333333703, 0.3333333333333333703, 0.3333333333333333703, 0.3333333333333333703, 0.3333333333333334259, 0.3333333333333333703, 0.3333333333333334259, 0.3333333333333333148, 0.3333333333333335369, 0.3333333333333332038, 0.3333333333333335369, 0.3333333333333333148, 0.3333333333333334259, 0.3333333333333333703, 0.3333333333333333148, 0.3333333333333334259, 0.3333333333333333148, 0.3333333333333334259, 0.3333333333333332593, 0.3333333333333333148, 0.3333333333333334259, 0.3333333333333334814, 0.3333333333333333703, 0.3333333333333333703, 0.3333333333333334259, 0.3333333333333333148, 0.3333333333333333703, 0.3333333333333333148, 0.3333333333333334259, 0.3333333333333333148, 0.3333333333333333703, 0.3333333333333333703, 0.3333333333333334259, 0.3333333333333333148, 0.3333333333333334259, 0.3333333333333333703, 0.3333333333333333148, 0.3333333333333332593, 0.3333333333333334259, 0.3333333333333333148, 0.3333333333333334259, 0.3333333333333334259, 0.3333333333333334814, 0.3333333333333334259, 0.3333333333333333703, 0.3333333333333333703, 0.3333333333333333148, 0.3333333333333334259, 0.3333333333333333703, 0.3333333333333334259, 0.3333333333333333148, 0.3333333333333333703, 0.3333333333333333703, 0.3333333333333332593, 0.3333333333333334259, 0.3333333333333335369, 0.3333333333333333148, 0.3333333333333334814, 0.3333333333333333703, 0.3333333333333333148, 0.3333333333333334259, 0.3333333333333332593, 0.3333333333333334814, 0.3333333333333333148, 0.3333333333333333703, 0.3333333333333333148, 0.3333333333333334259, 0.3333333333333333148, 0.3333333333333334259, 0.3333333333333333148, 0.3333333333333333703, 0.3333333333333333703, 0.3333333333333333148, 0.3333333333333334259, 0.3333333333333333703, 0.3333333333333333703, 0.3333333333333335369, 0.3333333333333332038, 0.3333333333333334814, 0.3333333333333333148, 0.3333333333333334259, 0.3333333333333334259, 0.3333333333333333703, 0.3333333333333333148, 0.3333333333333334814, 0.3333333333333333703, 0.3333333333333333703, 0.3333333333333333703, 0.3333333333333333703, 0.3333333333333333703, 0.3333333333333334259, 0.3333333333333333703, 0.3333333333333334259, 0.3333333333333333148, 0.3333333333333333703, 0.3333333333333334259, 0.3333333333333334259, 0.3333333333333333703, 0.3333333333333333703, 0.3333333333333334259, 0.3333333333333333703, 0.3333333333333333148, 0.3333333333333333148, 0.3333333333333333703, 0.3333333333333333703, 0.3333333333333334259, 0.3333333333333334259, 0.3333333333333333703, 0.3333333333333333703, 0.3333333333333333703, 0.3333333333333333703, 0.3333333333333333703, 0.3333333333333333148, 0.3333333333333334259, 0.3333333333333334259, 0.3333333333333333703, 0.3333333333333335369, 0.3333333333333332038, 0.3333333333333334814, 0.3333333333333332593, 0.3333333333333333703, 0.3333333333333332593, 0.3333333333333334814, 0.3333333333333333148, 0.3333333333333333703, 0.3333333333333334259, 0.3333333333333334259, 0.3333333333333332593, 0.3333333333333334259, 0.3333333333333333148, 0.3333333333333333703, 0.3333333333333334259, 0.3333333333333334814, 0.3333333333333333148, 0.3333333333333334259, 0.3333333333333333148, 0.3333333333333334814, 0.3333333333333334259, 0.3333333333333333703, 0.3333333333333334259, 0.3333333333333332593, 0.3333333333333333148, 0.3333333333333333703, 0.3333333333333333703, 0.3333333333333334259, 0.3333333333333333703, 0.3333333333333334259, 0.3333333333333333703, 0.3333333333333334259, 0.3333333333333333148, 0.3333333333333333703, 0.3333333333333334259, 0.3333333333333334259, 0.3333333333333333703, 0.3333333333333333703, 0.3333333333333333703, 0.3333333333333333148, 0.3333333333333333703, 0.3333333333333333148, 0.3333333333333334259, 0.3333333333333334259, 0.3333333333333333148, 0.3333333333333333703, 0.3333333333333334259, 0.3333333333333333703, 0.3333333333333333148, 0.3333333333333333703, 0.3333333333333333148, 0.3333333333333333703, 0.3333333333333334259, 0.3333333333333333148, 0.3333333333333334259, 0.3333333333333332593, 0.3333333333333334814, 0.3333333333333334814, 0.3333333333333333148, 0.3333333333333333703, 0.3333333333333334814, 0.3333333333333333148, 0.3333333333333333703, 0.3333333333333334814, 0.3333333333333333703, 0.3333333333333334259, 0.3333333333333334259, 0.3333333333333334814, 0.3333333333333333703, 0.3333333333333333703, 0.3333333333333333703, 0.3333333333333333148, 0.3333333333333333148, 0.3333333333333333703, 0.3333333333333333703, 0.3333333333333333703, 0.3333333333333334259, 0.3333333333333334259, 0.3333333333333333148, 0.3333333333333333148, 0.3333333333333334814, 0.3333333333333333148, 0.3333333333333333148, 0.3333333333333333703, 0.3333333333333333703, 0.3333333333333333703, 0.3333333333333333703),
 ( 0.3333333333333333703, 0.3333333333333333703, 0.3333333333333333703, 0.3333333333333333148, 0.3333333333333333703, 0.3333333333333333148, 0.3333333333333333703, 0.3333333333333334259, 0.3333333333333333703, 0.3333333333333333148, 0.3333333333333334259, 0.3333333333333332593, 0.3333333333333334259, 0.3333333333333333703, 0.3333333333333333703, 0.3333333333333332593, 0.3333333333333334259, 0.3333333333333333148, 0.3333333333333334259, 0.3333333333333333148, 0.3333333333333334259, 0.3333333333333334259, 0.3333333333333333148, 0.3333333333333333148, 0.3333333333333334814, 0.3333333333333332593, 0.3333333333333334259, 0.3333333333333334259, 0.3333333333333333703, 0.3333333333333333703, 0.3333333333333334814, 0.3333333333333332038, 0.3333333333333334814, 0.3333333333333333703, 0.3333333333333334259, 0.3333333333333333148, 0.3333333333333334259, 0.3333333333333334814, 0.3333333333333333703, 0.3333333333333332593, 0.3333333333333334259, 0.3333333333333333148, 0.3333333333333333148, 0.3333333333333333703, 0.3333333333333333703, 0.3333333333333334259, 0.3333333333333333148, 0.3333333333333335369, 0.3333333333333333148, 0.3333333333333334259, 0.3333333333333333703, 0.3333333333333332038, 0.3333333333333334259, 0.3333333333333334259, 0.3333333333333333148, 0.3333333333333334259, 0.3333333333333333703, 0.3333333333333333703, 0.3333333333333334259, 0.3333333333333334259, 0.3333333333333333703, 0.3333333333333334259, 0.3333333333333334259, 0.3333333333333333148, 0.3333333333333333703, 0.3333333333333333703, 0.3333333333333333148, 0.3333333333333334259, 0.3333333333333333148, 0.3333333333333334814, 0.3333333333333333703, 0.3333333333333334259, 0.3333333333333333148, 0.3333333333333333703, 0.3333333333333334259, 0.3333333333333333703, 0.3333333333333333703, 0.3333333333333333148, 0.3333333333333334259, 0.3333333333333333148, 0.3333333333333334259, 0.3333333333333333703, 0.3333333333333334259, 0.3333333333333334814, 0.3333333333333333148, 0.3333333333333334259, 0.3333333333333334259, 0.3333333333333333148, 0.3333333333333333703, 0.3333333333333333703, 0.3333333333333333148, 0.3333333333333334814, 0.3333333333333332593, 0.3333333333333334259, 0.3333333333333333703, 0.3333333333333333148, 0.3333333333333333703, 0.3333333333333333703, 0.3333333333333334259, 0.3333333333333333148, 0.3333333333333334259, 0.3333333333333333148, 0.3333333333333334814, 0.3333333333333333148, 0.3333333333333333148, 0.3333333333333334259, 0.3333333333333333148, 0.3333333333333333703, 0.3333333333333333703, 0.3333333333333334259, 0.3333333333333333703, 0.3333333333333334259, 0.3333333333333333703, 0.3333333333333332593, 0.3333333333333334259, 0.3333333333333333703, 0.3333333333333333148, 0.3333333333333334814, 0.3333333333333333148, 0.3333333333333334259, 0.3333333333333334259, 0.3333333333333333148, 0.3333333333333333703, 0.3333333333333334259, 0.3333333333333333703, 0.3333333333333333703, 0.3333333333333334259, 0.3333333333333333703, 0.3333333333333334259, 0.3333333333333333703, 0.3333333333333334259, 0.3333333333333333148, 0.3333333333333333703, 0.3333333333333333703, 0.3333333333333333703, 0.3333333333333333703, 0.3333333333333335369, 0.3333333333333332593, 0.3333333333333333703, 0.3333333333333333703, 0.3333333333333332593, 0.3333333333333333703, 0.3333333333333333703, 0.3333333333333334259, 0.3333333333333332593, 0.3333333333333333703, 0.3333333333333333703, 0.3333333333333333703, 0.3333333333333333703, 0.3333333333333333703, 0.3333333333333334259, 0.3333333333333333148, 0.3333333333333334259, 0.3333333333333333703, 0.3333333333333334814, 0.3333333333333332593, 0.3333333333333333703, 0.3333333333333334814, 0.3333333333333332038, 0.3333333333333334259, 0.3333333333333333148, 0.3333333333333333703, 0.3333333333333334814, 0.3333333333333332038, 0.3333333333333334259, 0.3333333333333333703, 0.3333333333333333703, 0.3333333333333333703, 0.3333333333333334259, 0.3333333333333333703, 0.3333333333333335369, 0.3333333333333333148, 0.3333333333333333148, 0.3333333333333334259, 0.3333333333333333148, 0.3333333333333333703, 0.3333333333333333703, 0.3333333333333334259, 0.3333333333333333148, 0.3333333333333334259, 0.3333333333333332593, 0.3333333333333334814, 0.3333333333333333703, 0.3333333333333333703, 0.3333333333333333703, 0.3333333333333333703, 0.3333333333333333703, 0.3333333333333334259, 0.3333333333333333703, 0.3333333333333334259, 0.3333333333333333148, 0.3333333333333335369, 0.3333333333333332038, 0.3333333333333335369, 0.3333333333333333148, 0.3333333333333334259, 0.3333333333333333703, 0.3333333333333333148, 0.3333333333333334259, 0.3333333333333333148, 0.3333333333333334259, 0.3333333333333332593, 0.3333333333333333148, 0.3333333333333334259, 0.3333333333333334814, 0.3333333333333333703, 0.3333333333333333703, 0.3333333333333334259, 0.3333333333333333148, 0.3333333333333333703, 0.3333333333333333148, 0.3333333333333334259, 0.3333333333333333148, 0.3333333333333333703, 0.3333333333333333703, 0.3333333333333334259, 0.3333333333333333148, 0.3333333333333334259, 0.3333333333333333703, 0.3333333333333333148, 0.3333333333333332593, 0.3333333333333334259, 0.3333333333333333148, 0.3333333333333334259, 0.3333333333333334259, 0.3333333333333334814, 0.3333333333333334259, 0.3333333333333333703, 0.3333333333333333703, 0.3333333333333333148, 0.3333333333333334259, 0.3333333333333333703, 0.3333333333333334259, 0.3333333333333333148, 0.3333333333333333703, 0.3333333333333333703, 0.3333333333333332593, 0.3333333333333334259, 0.3333333333333335369, 0.3333333333333333148, 0.3333333333333334814, 0.3333333333333333703, 0.3333333333333333148, 0.3333333333333334259, 0.3333333333333332593, 0.3333333333333334814, 0.3333333333333333148, 0.3333333333333333703, 0.3333333333333333148, 0.3333333333333334259, 0.3333333333333333148, 0.3333333333333334259, 0.3333333333333333148, 0.3333333333333333703, 0.3333333333333333703, 0.3333333333333333148, 0.3333333333333334259, 0.3333333333333333703, 0.3333333333333333703, 0.3333333333333335369, 0.3333333333333332038, 0.3333333333333334814, 0.3333333333333333148, 0.3333333333333334259, 0.3333333333333334259, 0.3333333333333333703, 0.3333333333333333148, 0.3333333333333334814, 0.3333333333333333703, 0.3333333333333333703, 0.3333333333333333703, 0.3333333333333333703, 0.3333333333333333703, 0.3333333333333334259, 0.3333333333333333703, 0.3333333333333334259, 0.3333333333333333148, 0.3333333333333333703, 0.3333333333333334259, 0.3333333333333334259, 0.3333333333333333703, 0.3333333333333333703, 0.3333333333333334259, 0.3333333333333333703, 0.3333333333333333148, 0.3333333333333333148, 0.3333333333333333703, 0.3333333333333333703, 0.3333333333333334259, 0.3333333333333334259, 0.3333333333333333703, 0.3333333333333333703, 0.3333333333333333703, 0.3333333333333333703, 0.3333333333333333703, 0.3333333333333333148, 0.3333333333333334259, 0.3333333333333334259, 0.3333333333333333703, 0.3333333333333335369, 0.3333333333333332038, 0.3333333333333334814, 0.3333333333333332593, 0.3333333333333333703, 0.3333333333333332593, 0.3333333333333334814, 0.3333333333333333148, 0.3333333333333333703, 0.3333333333333334259, 0.3333333333333334259, 0.3333333333333332593, 0.3333333333333334259, 0.3333333333333333148, 0.3333333333333333703, 0.3333333333333334259, 0.3333333333333334814, 0.3333333333333333148, 0.3333333333333334259, 0.3333333333333333148, 0.3333333333333334814, 0.3333333333333334259, 0.3333333333333333703, 0.3333333333333334259, 0.3333333333333332593, 0.3333333333333333148, 0.3333333333333333703, 0.3333333333333333703, 0.3333333333333334259, 0.3333333333333333703, 0.3333333333333334259, 0.3333333333333333703, 0.3333333333333334259, 0.3333333333333333148, 0.3333333333333333703, 0.3333333333333334259, 0.3333333333333334259, 0.3333333333333333703, 0.3333333333333333703, 0.3333333333333333703, 0.3333333333333333148, 0.3333333333333333703, 0.3333333333333333148, 0.3333333333333334259, 0.3333333333333334259, 0.3333333333333333148, 0.3333333333333333703, 0.3333333333333334259, 0.3333333333333333703, 0.3333333333333333148, 0.3333333333333333703, 0.3333333333333333148, 0.3333333333333333703, 0.3333333333333334259, 0.3333333333333333148, 0.3333333333333334259, 0.3333333333333332593, 0.3333333333333334814, 0.3333333333333334814, 0.3333333333333333148, 0.3333333333333333703, 0.3333333333333334814, 0.3333333333333333148, 0.3333333333333333703, 0.3333333333333334814, 0.3333333333333333703, 0.3333333333333334259, 0.3333333333333334259, 0.3333333333333334814, 0.3333333333333333703, 0.3333333333333333703, 0.3333333333333333703, 0.3333333333333333148, 0.3333333333333333148, 0.3333333333333333703, 0.3333333333333333703, 0.3333333333333333703, 0.3333333333333334259, 0.3333333333333334259, 0.3333333333333333148, 0.3333333333333333148, 0.3333333333333334814, 0.3333333333333333148, 0.3333333333333333148, 0.3333333333333333703, 0.3333333333333333703, 0.3333333333333333703, 0.3333333333333333703),
 ( 1.000000000000000000, 1.000000000000000000, 1.000000000000000000, 0.9999999999999997780, 1.000000000000000000, 1.000000000000000000, 1.000000000000000000, 1.000000000000000222, 1.000000000000000000, 1.000000000000000000, 1.000000000000000222, 0.9999999999999997780, 1.000000000000000222, 1.000000000000000222, 1.000000000000000000, 1.000000000000000000, 1.000000000000000000, 0.9999999999999997780, 1.000000000000000222, 0.9999999999999996669, 1.000000000000000222, 1.000000000000000000, 1.000000000000000000, 0.9999999999999996669, 1.000000000000000444, 0.9999999999999996669, 1.000000000000000444, 1.000000000000000000, 1.000000000000000000, 0.9999999999999997780, 1.000000000000000222, 0.9999999999999994449, 1.000000000000000444, 1.000000000000000000, 1.000000000000000000, 1.000000000000000000, 1.000000000000000000, 1.000000000000000444, 0.9999999999999997780, 1.000000000000000000, 1.000000000000000000, 1.000000000000000000, 1.000000000000000000, 1.000000000000000000, 1.000000000000000000, 0.9999999999999997780, 1.000000000000000000, 1.000000000000000444, 0.9999999999999997780, 1.000000000000000444, 0.9999999999999997780, 0.9999999999999997780, 1.000000000000000000, 1.000000000000000222, 1.000000000000000000, 1.000000000000000000, 1.000000000000000000, 1.000000000000000000, 0.9999999999999997780, 1.000000000000000444, 0.9999999999999997780, 1.000000000000000000, 1.000000000000000222, 0.9999999999999997780, 1.000000000000000000, 1.000000000000000222, 0.9999999999999997780, 1.000000000000000222, 1.000000000000000000, 1.000000000000000222, 1.000000000000000000, 1.000000000000000222, 0.9999999999999997780, 1.000000000000000000, 1.000000000000000222, 1.000000000000000000, 1.000000000000000222, 0.9999999999999997780, 1.000000000000000222, 0.9999999999999997780, 1.000000000000000222, 0.9999999999999997780, 1.000000000000000222, 1.000000000000000222, 0.9999999999999997780, 1.000000000000000222, 1.000000000000000222, 0.9999999999999997780, 1.000000000000000222, 1.000000000000000000, 1.000000000000000000, 1.000000000000000222, 0.9999999999999996669, 1.000000000000000444, 0.9999999999999997780, 0.9999999999999997780, 1.000000000000000000, 1.000000000000000000, 1.000000000000000000, 0.9999999999999996669, 1.000000000000000444, 1.000000000000000000, 1.000000000000000222, 1.000000000000000000, 0.9999999999999997780, 1.000000000000000222, 0.9999999999999997780, 1.000000000000000222, 1.000000000000000000, 1.000000000000000000, 1.000000000000000222, 1.000000000000000000, 1.000000000000000222, 0.9999999999999994449, 1.000000000000000444, 1.000000000000000000, 0.9999999999999996669, 1.000000000000000222, 0.9999999999999997780, 1.000000000000000222, 0.9999999999999997780, 1.000000000000000000, 1.000000000000000000, 1.000000000000000000, 1.000000000000000000, 1.000000000000000000, 1.000000000000000444, 1.000000000000000000, 1.000000000000000000, 1.000000000000000222, 1.000000000000000000, 1.000000000000000000, 0.9999999999999997780, 1.000000000000000000, 1.000000000000000222, 1.000000000000000000, 1.000000000000000222, 0.9999999999999997780, 1.000000000000000000, 0.9999999999999997780, 0.9999999999999997780, 1.000000000000000222, 0.9999999999999997780, 1.000000000000000444, 0.9999999999999997780, 1.000000000000000000, 1.000000000000000222, 1.000000000000000000, 1.000000000000000000, 0.9999999999999997780, 1.000000000000000222, 1.000000000000000000, 1.000000000000000000, 1.000000000000000000, 1.000000000000000222, 0.9999999999999996669, 1.000000000000000222, 1.000000000000000222, 0.9999999999999996669, 1.000000000000000444, 0.9999999999999996669, 1.000000000000000000, 1.000000000000000222, 0.9999999999999996669, 1.000000000000000222, 1.000000000000000000, 1.000000000000000222, 1.000000000000000000, 1.000000000000000222, 0.9999999999999997780, 1.000000000000000444, 0.9999999999999997780, 0.9999999999999997780, 1.000000000000000222, 0.9999999999999996669, 1.000000000000000222, 1.000000000000000000, 1.000000000000000000, 1.000000000000000000, 0.9999999999999997780, 1.000000000000000222, 1.000000000000000222, 0.9999999999999997780, 1.000000000000000222, 0.9999999999999997780, 1.000000000000000222, 1.000000000000000000, 1.000000000000000444, 1.000000000000000000, 1.000000000000000222, 0.9999999999999996669, 1.000000000000000444, 0.9999999999999993339, 1.000000000000000444, 0.9999999999999997780, 1.000000000000000444, 0.9999999999999997780, 1.000000000000000000, 1.000000000000000000, 0.9999999999999997780, 1.000000000000000222, 0.9999999999999997780, 0.9999999999999996669, 1.000000000000000444, 1.000000000000000222, 1.000000000000000000, 0.9999999999999997780, 1.000000000000000222, 0.9999999999999996669, 1.000000000000000222, 0.9999999999999997780, 1.000000000000000222, 1.000000000000000000, 1.000000000000000000, 1.000000000000000000, 1.000000000000000000, 0.9999999999999997780, 1.000000000000000000, 1.000000000000000000, 0.9999999999999997780, 1.000000000000000000, 1.000000000000000000, 1.000000000000000000, 1.000000000000000222, 1.000000000000000000, 1.000000000000000444, 1.000000000000000222, 1.000000000000000000, 1.000000000000000000, 0.9999999999999997780, 1.000000000000000222, 1.000000000000000000, 1.000000000000000000, 1.000000000000000000, 0.9999999999999997780, 1.000000000000000222, 0.9999999999999997780, 1.000000000000000222, 1.000000000000000444, 0.9999999999999997780, 1.000000000000000222, 1.000000000000000000, 1.000000000000000000, 1.000000000000000000, 0.9999999999999997780, 1.000000000000000444, 0.9999999999999997780, 1.000000000000000222, 0.9999999999999997780, 1.000000000000000222, 0.9999999999999994449, 1.000000000000000222, 1.000000000000000000, 1.000000000000000222, 1.000000000000000000, 0.9999999999999997780, 1.000000000000000222, 1.000000000000000000, 0.9999999999999997780, 1.000000000000000444, 0.9999999999999996669, 1.000000000000000222, 1.000000000000000000, 1.000000000000000000, 1.000000000000000222, 0.9999999999999997780, 0.9999999999999997780, 1.000000000000000444, 1.000000000000000222, 1.000000000000000000, 0.9999999999999997780, 0.9999999999999997780, 1.000000000000000222, 1.000000000000000000, 1.000000000000000222, 1.000000000000000000, 0.9999999999999997780, 1.000000000000000000, 1.000000000000000000, 1.000000000000000000, 1.000000000000000222, 0.9999999999999997780, 1.000000000000000222, 1.000000000000000000, 1.000000000000000000, 1.000000000000000000, 0.9999999999999997780, 1.000000000000000000, 1.000000000000000222, 1.000000000000000222, 0.9999999999999996669, 1.000000000000000444, 0.9999999999999996669, 1.000000000000000222, 1.000000000000000000, 1.000000000000000222, 0.9999999999999997780, 1.000000000000000444, 1.000000000000000000, 1.000000000000000444, 0.9999999999999994449, 1.000000000000000222, 0.9999999999999997780, 0.9999999999999997780, 1.000000000000000000, 1.000000000000000222, 1.000000000000000000, 1.000000000000000000, 1.000000000000000000, 1.000000000000000222, 0.9999999999999996669, 1.000000000000000222, 1.000000000000000000, 0.9999999999999996669, 1.000000000000000444, 1.000000000000000000, 1.000000000000000000, 1.000000000000000000, 0.9999999999999996669, 1.000000000000000222, 1.000000000000000000, 1.000000000000000000, 1.000000000000000222, 0.9999999999999997780, 0.9999999999999997780, 1.000000000000000000, 1.000000000000000000, 1.000000000000000222, 0.9999999999999997780, 1.000000000000000222, 1.000000000000000000, 1.000000000000000000, 0.9999999999999996669, 1.000000000000000222, 1.000000000000000000, 1.000000000000000222, 1.000000000000000000, 1.000000000000000000, 1.000000000000000000, 0.9999999999999997780, 1.000000000000000222, 0.9999999999999996669, 1.000000000000000444, 1.000000000000000000, 0.9999999999999997780, 1.000000000000000000, 1.000000000000000222, 1.000000000000000222, 0.9999999999999996669, 1.000000000000000000, 1.000000000000000000, 0.9999999999999997780, 1.000000000000000222, 1.000000000000000000, 1.000000000000000222, 0.9999999999999996669, 1.000000000000000444, 1.000000000000000000, 1.000000000000000000, 1.000000000000000000, 1.000000000000000222, 1.000000000000000000, 0.9999999999999997780, 1.000000000000000444, 1.000000000000000000, 1.000000000000000444, 0.9999999999999997780, 1.000000000000000444, 1.000000000000000000, 1.000000000000000222, 1.000000000000000222, 1.000000000000000000, 0.9999999999999996669, 1.000000000000000000, 1.000000000000000000, 1.000000000000000000, 1.000000000000000000, 1.000000000000000222, 0.9999999999999996669, 1.000000000000000000, 1.000000000000000222, 0.9999999999999997780, 0.9999999999999997780, 1.000000000000000000, 1.000000000000000000, 1.000000000000000000, 1.000000000000000000),
 ( 0.3333333333333333703, 0.3333333333333333703, 0.3333333333333333703, 0.3333333333333333148, 0.3333333333333333703, 0.3333333333333333148, 0.3333333333333333703, 0.3333333333333334259, 0.3333333333333333703, 0.3333333333333333148, 0.3333333333333334259, 0.3333333333333332593, 0.3333333333333334259, 0.3333333333333333703, 0.3333333333333333703, 0.3333333333333332593, 0.3333333333333334259, 0.3333333333333333148, 0.3333333333333334259, 0.3333333333333333148, 0.3333333333333334259, 0.3333333333333334259, 0.3333333333333333148, 0.3333333333333333148, 0.3333333333333334814, 0.3333333333333332593, 0.3333333333333334259, 0.3333333333333334259, 0.3333333333333333703, 0.3333333333333333703, 0.3333333333333334814, 0.3333333333333332038, 0.3333333333333334814, 0.3333333333333333703, 0.3333333333333334259, 0.3333333333333333148, 0.3333333333333334259, 0.3333333333333334814, 0.3333333333333333703, 0.3333333333333332593, 0.3333333333333334259, 0.3333333333333333148, 0.3333333333333333148, 0.3333333333333333703, 0.3333333333333333703, 0.3333333333333334259, 0.3333333333333333148, 0.3333333333333335369, 0.3333333333333333148, 0.3333333333333334259, 0.3333333333333333703, 0.3333333333333332038, 0.3333333333333334259, 0.3333333333333334259, 0.3333333333333333148, 0.3333333333333334259, 0.3333333333333333703, 0.3333333333333333703, 0.3333333333333334259, 0.3333333333333334259, 0.3333333333333333703, 0.3333333333333334259, 0.3333333333333334259, 0.3333333333333333148, 0.3333333333333333703, 0.3333333333333333703, 0.3333333333333333148, 0.3333333333333334259, 0.3333333333333333148, 0.3333333333333334814, 0.3333333333333333703, 0.3333333333333334259, 0.3333333333333333148, 0.3333333333333333703, 0.3333333333333334259, 0.3333333333333333703, 0.3333333333333333703, 0.3333333333333333148, 0.3333333333333334259, 0.3333333333333333148, 0.3333333333333334259, 0.3333333333333333703, 0.3333333333333334259, 0.3333333333333334814, 0.3333333333333333148, 0.3333333333333334259, 0.3333333333333334259, 0.3333333333333333148, 0.3333333333333333703, 0.3333333333333333703, 0.3333333333333333148, 0.3333333333333334814, 0.3333333333333332593, 0.3333333333333334259, 0.3333333333333333703, 0.3333333333333333148, 0.3333333333333333703, 0.3333333333333333703, 0.3333333333333334259, 0.3333333333333333148, 0.3333333333333334259, 0.3333333333333333148, 0.3333333333333334814, 0.3333333333333333148, 0.3333333333333333148, 0.3333333333333334259, 0.3333333333333333148, 0.3333333333333333703, 0.3333333333333333703, 0.3333333333333334259, 0.3333333333333333703, 0.3333333333333334259, 0.3333333333333333703, 0.3333333333333332593, 0.3333333333333334259, 0.3333333333333333703, 0.3333333333333333148, 0.3333333333333334814, 0.3333333333333333148, 0.3333333333333334259, 0.3333333333333334259, 0.3333333333333333148, 0.3333333333333333703, 0.3333333333333334259, 0.3333333333333333703, 0.3333333333333333703, 0.3333333333333334259, 0.3333333333333333703, 0.3333333333333334259, 0.3333333333333333703, 0.3333333333333334259, 0.3333333333333333148, 0.3333333333333333703, 0.3333333333333333703, 0.3333333333333333703, 0.3333333333333333703, 0.3333333333333335369, 0.3333333333333332593, 0.3333333333333333703, 0.3333333333333333703, 0.3333333333333332593, 0.3333333333333333703, 0.3333333333333333703, 0.3333333333333334259, 0.3333333333333332593, 0.3333333333333333703, 0.3333333333333333703, 0.3333333333333333703, 0.3333333333333333703, 0.3333333333333333703, 0.3333333333333334259, 0.3333333333333333148, 0.3333333333333334259, 0.3333333333333333703, 0.3333333333333334814, 0.3333333333333332593, 0.3333333333333333703, 0.3333333333333334814, 0.3333333333333332038, 0.3333333333333334259, 0.3333333333333333148, 0.3333333333333333703, 0.3333333333333334814, 0.3333333333333332038, 0.3333333333333334259, 0.3333333333333333703, 0.3333333333333333703, 0.3333333333333333703, 0.3333333333333334259, 0.3333333333333333703, 0.3333333333333335369, 0.3333333333333333148, 0.3333333333333333148, 0.3333333333333334259, 0.3333333333333333148, 0.3333333333333333703, 0.3333333333333333703, 0.3333333333333334259, 0.3333333333333333148, 0.3333333333333334259, 0.3333333333333332593, 0.3333333333333334814, 0.3333333333333333703, 0.3333333333333333703, 0.3333333333333333703, 0.3333333333333333703, 0.3333333333333333703, 0.3333333333333334259, 0.3333333333333333703, 0.3333333333333334259, 0.3333333333333333148, 0.3333333333333335369, 0.3333333333333332038, 0.3333333333333335369, 0.3333333333333333148, 0.3333333333333334259, 0.3333333333333333703, 0.3333333333333333148, 0.3333333333333334259, 0.3333333333333333148, 0.3333333333333334259, 0.3333333333333332593, 0.3333333333333333148, 0.3333333333333334259, 0.3333333333333334814, 0.3333333333333333703, 0.3333333333333333703, 0.3333333333333334259, 0.3333333333333333148, 0.3333333333333333703, 0.3333333333333333148, 0.3333333333333334259, 0.3333333333333333148, 0.3333333333333333703, 0.3333333333333333703, 0.3333333333333334259, 0.3333333333333333148, 0.3333333333333334259, 0.3333333333333333703, 0.3333333333333333148, 0.3333333333333332593, 0.3333333333333334259, 0.3333333333333333148, 0.3333333333333334259, 0.3333333333333334259, 0.3333333333333334814, 0.3333333333333334259, 0.3333333333333333703, 0.3333333333333333703, 0.3333333333333333148, 0.3333333333333334259, 0.3333333333333333703, 0.3333333333333334259, 0.3333333333333333148, 0.3333333333333333703, 0.3333333333333333703, 0.3333333333333332593, 0.3333333333333334259, 0.3333333333333335369, 0.3333333333333333148, 0.3333333333333334814, 0.3333333333333333703, 0.3333333333333333148, 0.3333333333333334259, 0.3333333333333332593, 0.3333333333333334814, 0.3333333333333333148, 0.3333333333333333703, 0.3333333333333333148, 0.3333333333333334259, 0.3333333333333333148, 0.3333333333333334259, 0.3333333333333333148, 0.3333333333333333703, 0.3333333333333333703, 0.3333333333333333148, 0.3333333333333334259, 0.3333333333333333703, 0.3333333333333333703, 0.3333333333333335369, 0.3333333333333332038, 0.3333333333333334814, 0.3333333333333333148, 0.3333333333333334259, 0.3333333333333334259, 0.3333333333333333703, 0.3333333333333333148, 0.3333333333333334814, 0.3333333333333333703, 0.3333333333333333703, 0.3333333333333333703, 0.3333333333333333703, 0.3333333333333333703, 0.3333333333333334259, 0.3333333333333333703, 0.3333333333333334259, 0.3333333333333333148, 0.3333333333333333703, 0.3333333333333334259, 0.3333333333333334259, 0.3333333333333333703, 0.3333333333333333703, 0.3333333333333334259, 0.3333333333333333703, 0.3333333333333333148, 0.3333333333333333148, 0.3333333333333333703, 0.3333333333333333703, 0.3333333333333334259, 0.3333333333333334259, 0.3333333333333333703, 0.3333333333333333703, 0.3333333333333333703, 0.3333333333333333703, 0.3333333333333333703, 0.3333333333333333148, 0.3333333333333334259, 0.3333333333333334259, 0.3333333333333333703, 0.3333333333333335369, 0.3333333333333332038, 0.3333333333333334814, 0.3333333333333332593, 0.3333333333333333703, 0.3333333333333332593, 0.3333333333333334814, 0.3333333333333333148, 0.3333333333333333703, 0.3333333333333334259, 0.3333333333333334259, 0.3333333333333332593, 0.3333333333333334259, 0.3333333333333333148, 0.3333333333333333703, 0.3333333333333334259, 0.3333333333333334814, 0.3333333333333333148, 0.3333333333333334259, 0.3333333333333333148, 0.3333333333333334814, 0.3333333333333334259, 0.3333333333333333703, 0.3333333333333334259, 0.3333333333333332593, 0.3333333333333333148, 0.3333333333333333703, 0.3333333333333333703, 0.3333333333333334259, 0.3333333333333333703, 0.3333333333333334259, 0.3333333333333333703, 0.3333333333333334259, 0.3333333333333333148, 0.3333333333333333703, 0.3333333333333334259, 0.3333333333333334259, 0.3333333333333333703, 0.3333333333333333703, 0.3333333333333333703, 0.3333333333333333148, 0.3333333333333333703, 0.3333333333333333148, 0.3333333333333334259, 0.3333333333333334259, 0.3333333333333333148, 0.3333333333333333703, 0.3333333333333334259, 0.3333333333333333703, 0.3333333333333333148, 0.3333333333333333703, 0.3333333333333333148, 0.3333333333333333703, 0.3333333333333334259, 0.3333333333333333148, 0.3333333333333334259, 0.3333333333333332593, 0.3333333333333334814, 0.3333333333333334814, 0.3333333333333333148, 0.3333333333333333703, 0.3333333333333334814, 0.3333333333333333148, 0.3333333333333333703, 0.3333333333333334814, 0.3333333333333333703, 0.3333333333333334259, 0.3333333333333334259, 0.3333333333333334814, 0.3333333333333333703, 0.3333333333333333703, 0.3333333333333333703, 0.3333333333333333148, 0.3333333333333333148, 0.3333333333333333703, 0.3333333333333333703, 0.3333333333333333703, 0.3333333333333334259, 0.3333333333333334259, 0.3333333333333333148, 0.3333333333333333148, 0.3333333333333334814, 0.3333333333333333148, 0.3333333333333333148, 0.3333333333333333703, 0.3333333333333333703, 0.3333333333333333703, 0.3333333333333333703),
 ( 0.3333333333333333703, 0.3333333333333333703, 0.3333333333333333703, 0.3333333333333333148, 0.3333333333333333703, 0.3333333333333333148, 0.3333333333333333703, 0.3333333333333334259, 0.3333333333333333703, 0.3333333333333333148, 0.3333333333333334259, 0.3333333333333332593, 0.3333333333333334259, 0.3333333333333333703, 0.3333333333333333703, 0.3333333333333332593, 0.3333333333333334259, 0.3333333333333333148, 0.3333333333333334259, 0.3333333333333333148, 0.3333333333333334259, 0.3333333333333334259, 0.3333333333333333148, 0.3333333333333333148, 0.3333333333333334814, 0.3333333333333332593, 0.3333333333333334259, 0.3333333333333334259, 0.3333333333333333703, 0.3333333333333333703, 0.3333333333333334814, 0.3333333333333332038, 0.3333333333333334814, 0.3333333333333333703, 0.3333333333333334259, 0.3333333333333333148, 0.3333333333333334259, 0.3333333333333334814, 0.3333333333333333703, 0.3333333333333332593, 0.3333333333333334259, 0.3333333333333333148, 0.3333333333333333148, 0.3333333333333333703, 0.3333333333333333703, 0.3333333333333334259, 0.3333333333333333148, 0.3333333333333335369, 0.3333333333333333148, 0.3333333333333334259, 0.3333333333333333703, 0.3333333333333332038, 0.3333333333333334259, 0.3333333333333334259, 0.3333333333333333148, 0.3333333333333334259, 0.3333333333333333703, 0.3333333333333333703, 0.3333333333333334259, 0.3333333333333334259, 0.3333333333333333703, 0.3333333333333334259, 0.3333333333333334259, 0.3333333333333333148, 0.3333333333333333703, 0.3333333333333333703, 0.3333333333333333148, 0.3333333333333334259, 0.3333333333333333148, 0.3333333333333334814, 0.3333333333333333703, 0.3333333333333334259, 0.3333333333333333148, 0.3333333333333333703, 0.3333333333333334259, 0.3333333333333333703, 0.3333333333333333703, 0.3333333333333333148, 0.3333333333333334259, 0.3333333333333333148, 0.3333333333333334259, 0.3333333333333333703, 0.3333333333333334259, 0.3333333333333334814, 0.3333333333333333148, 0.3333333333333334259, 0.3333333333333334259, 0.3333333333333333148, 0.3333333333333333703, 0.3333333333333333703, 0.3333333333333333148, 0.3333333333333334814, 0.3333333333333332593, 0.3333333333333334259, 0.3333333333333333703, 0.3333333333333333148, 0.3333333333333333703, 0.3333333333333333703, 0.3333333333333334259, 0.3333333333333333148, 0.3333333333333334259, 0.3333333333333333148, 0.3333333333333334814, 0.3333333333333333148, 0.3333333333333333148, 0.3333333333333334259, 0.3333333333333333148, 0.3333333333333333703, 0.3333333333333333703, 0.3333333333333334259, 0.3333333333333333703, 0.3333333333333334259, 0.3333333333333333703, 0.3333333333333332593, 0.3333333333333334259, 0.3333333333333333703, 0.3333333333333333148, 0.3333333333333334814, 0.3333333333333333148, 0.3333333333333334259, 0.3333333333333334259, 0.3333333333333333148, 0.3333333333333333703, 0.3333333333333334259, 0.3333333333333333703, 0.3333333333333333703, 0.3333333333333334259, 0.3333333333333333703, 0.3333333333333334259, 0.3333333333333333703, 0.3333333333333334259, 0.3333333333333333148, 0.3333333333333333703, 0.3333333333333333703, 0.3333333333333333703, 0.3333333333333333703, 0.3333333333333335369, 0.3333333333333332593, 0.3333333333333333703, 0.3333333333333333703, 0.3333333333333332593, 0.3333333333333333703, 0.3333333333333333703, 0.3333333333333334259, 0.3333333333333332593, 0.3333333333333333703, 0.3333333333333333703, 0.3333333333333333703, 0.3333333333333333703, 0.3333333333333333703, 0.3333333333333334259, 0.3333333333333333148, 0.3333333333333334259, 0.3333333333333333703, 0.3333333333333334814, 0.3333333333333332593, 0.3333333333333333703, 0.3333333333333334814, 0.3333333333333332038, 0.3333333333333334259, 0.3333333333333333148, 0.3333333333333333703, 0.3333333333333334814, 0.3333333333333332038, 0.3333333333333334259, 0.3333333333333333703, 0.3333333333333333703, 0.3333333333333333703, 0.3333333333333334259, 0.3333333333333333703, 0.3333333333333335369, 0.3333333333333333148, 0.3333333333333333148, 0.3333333333333334259, 0.3333333333333333148, 0.3333333333333333703, 0.3333333333333333703, 0.3333333333333334259, 0.3333333333333333148, 0.3333333333333334259, 0.3333333333333332593, 0.3333333333333334814, 0.3333333333333333703, 0.3333333333333333703, 0.3333333333333333703, 0.3333333333333333703, 0.3333333333333333703, 0.3333333333333334259, 0.3333333333333333703, 0.3333333333333334259, 0.3333333333333333148, 0.3333333333333335369, 0.3333333333333332038, 0.3333333333333335369, 0.3333333333333333148, 0.3333333333333334259, 0.3333333333333333703, 0.3333333333333333148, 0.3333333333333334259, 0.3333333333333333148, 0.3333333333333334259, 0.3333333333333332593, 0.3333333333333333148, 0.3333333333333334259, 0.3333333333333334814, 0.3333333333333333703, 0.3333333333333333703, 0.3333333333333334259, 0.3333333333333333148, 0.3333333333333333703, 0.3333333333333333148, 0.3333333333333334259, 0.3333333333333333148, 0.3333333333333333703, 0.3333333333333333703, 0.3333333333333334259, 0.3333333333333333148, 0.3333333333333334259, 0.3333333333333333703, 0.3333333333333333148, 0.3333333333333332593, 0.3333333333333334259, 0.3333333333333333148, 0.3333333333333334259, 0.3333333333333334259, 0.3333333333333334814, 0.3333333333333334259, 0.3333333333333333703, 0.3333333333333333703, 0.3333333333333333148, 0.3333333333333334259, 0.3333333333333333703, 0.3333333333333334259, 0.3333333333333333148, 0.3333333333333333703, 0.3333333333333333703, 0.3333333333333332593, 0.3333333333333334259, 0.3333333333333335369, 0.3333333333333333148, 0.3333333333333334814, 0.3333333333333333703, 0.3333333333333333148, 0.3333333333333334259, 0.3333333333333332593, 0.3333333333333334814, 0.3333333333333333148, 0.3333333333333333703, 0.3333333333333333148, 0.3333333333333334259, 0.3333333333333333148, 0.3333333333333334259, 0.3333333333333333148, 0.3333333333333333703, 0.3333333333333333703, 0.3333333333333333148, 0.3333333333333334259, 0.3333333333333333703, 0.3333333333333333703, 0.3333333333333335369, 0.3333333333333332038, 0.3333333333333334814, 0.3333333333333333148, 0.3333333333333334259, 0.3333333333333334259, 0.3333333333333333703, 0.3333333333333333148, 0.3333333333333334814, 0.3333333333333333703, 0.3333333333333333703, 0.3333333333333333703, 0.3333333333333333703, 0.3333333333333333703, 0.3333333333333334259, 0.3333333333333333703, 0.3333333333333334259, 0.3333333333333333148, 0.3333333333333333703, 0.3333333333333334259, 0.3333333333333334259, 0.3333333333333333703, 0.3333333333333333703, 0.3333333333333334259, 0.3333333333333333703, 0.3333333333333333148, 0.3333333333333333148, 0.3333333333333333703, 0.3333333333333333703, 0.3333333333333334259, 0.3333333333333334259, 0.3333333333333333703, 0.3333333333333333703, 0.3333333333333333703, 0.3333333333333333703, 0.3333333333333333703, 0.3333333333333333148, 0.3333333333333334259, 0.3333333333333334259, 0.3333333333333333703, 0.3333333333333335369, 0.3333333333333332038, 0.3333333333333334814, 0.3333333333333332593, 0.3333333333333333703, 0.3333333333333332593, 0.3333333333333334814, 0.3333333333333333148, 0.3333333333333333703, 0.3333333333333334259, 0.3333333333333334259, 0.3333333333333332593, 0.3333333333333334259, 0.3333333333333333148, 0.3333333333333333703, 0.3333333333333334259, 0.3333333333333334814, 0.3333333333333333148, 0.3333333333333334259, 0.3333333333333333148, 0.3333333333333334814, 0.3333333333333334259, 0.3333333333333333703, 0.3333333333333334259, 0.3333333333333332593, 0.3333333333333333148, 0.3333333333333333703, 0.3333333333333333703, 0.3333333333333334259, 0.3333333333333333703, 0.3333333333333334259, 0.3333333333333333703, 0.3333333333333334259, 0.3333333333333333148, 0.3333333333333333703, 0.3333333333333334259, 0.3333333333333334259, 0.3333333333333333703, 0.3333333333333333703, 0.3333333333333333703, 0.3333333333333333148, 0.3333333333333333703, 0.3333333333333333148, 0.3333333333333334259, 0.3333333333333334259, 0.3333333333333333148, 0.3333333333333333703, 0.3333333333333334259, 0.3333333333333333703, 0.3333333333333333148, 0.3333333333333333703, 0.3333333333333333148, 0.3333333333333333703, 0.3333333333333334259, 0.3333333333333333148, 0.3333333333333334259, 0.3333333333333332593, 0.3333333333333334814, 0.3333333333333334814, 0.3333333333333333148, 0.3333333333333333703, 0.3333333333333334814, 0.3333333333333333148, 0.3333333333333333703, 0.3333333333333334814, 0.3333333333333333703, 0.3333333333333334259, 0.3333333333333334259, 0.3333333333333334814, 0.3333333333333333703, 0.3333333333333333703, 0.3333333333333333703, 0.3333333333333333148, 0.3333333333333333148, 0.3333333333333333703, 0.3333333333333333703, 0.3333333333333333703, 0.3333333333333334259, 0.3333333333333334259, 0.3333333333333333148, 0.3333333333333333148, 0.3333333333333334814, 0.3333333333333333148, 0.3333333333333333148, 0.3333333333333333703, 0.3333333333333333703, 0.3333333333333333703, 0.3333333333333333703),
 ( 1.000000000000000000, 1.000000000000000000, 1.000000000000000000, 0.9999999999999997780, 1.000000000000000000, 1.000000000000000000, 1.000000000000000000, 1.000000000000000222, 1.000000000000000000, 1.000000000000000000, 1.000000000000000222, 0.9999999999999997780, 1.000000000000000222, 1.000000000000000222, 1.000000000000000000, 1.000000000000000000, 1.000000000000000000, 0.9999999999999997780, 1.000000000000000222, 0.9999999999999996669, 1.000000000000000222, 1.000000000000000000, 1.000000000000000000, 0.9999999999999996669, 1.000000000000000444, 0.9999999999999996669, 1.000000000000000444, 1.000000000000000000, 1.000000000000000000, 0.9999999999999997780, 1.000000000000000222, 0.9999999999999994449, 1.000000000000000444, 1.000000000000000000, 1.000000000000000000, 1.000000000000000000, 1.000000000000000000, 1.000000000000000444, 0.9999999999999997780, 1.000000000000000000, 1.000000000000000000, 1.000000000000000000, 1.000000000000000000, 1.000000000000000000, 1.000000000000000000, 0.9999999999999997780, 1.000000000000000000, 1.000000000000000444, 0.9999999999999997780, 1.000000000000000444, 0.9999999999999997780, 0.9999999999999997780, 1.000000000000000000, 1.000000000000000222, 1.000000000000000000, 1.000000000000000000, 1.000000000000000000, 1.000000000000000000, 0.9999999999999997780, 1.000000000000000444, 0.9999999999999997780, 1.000000000000000000, 1.000000000000000222, 0.9999999999999997780, 1.000000000000000000, 1.000000000000000222, 0.9999999999999997780, 1.000000000000000222, 1.000000000000000000, 1.000000000000000222, 1.000000000000000000, 1.000000000000000222, 0.9999999999999997780, 1.000000000000000000, 1.000000000000000222, 1.000000000000000000, 1.000000000000000222, 0.9999999999999997780, 1.000000000000000222, 0.9999999999999997780, 1.000000000000000222, 0.9999999999999997780, 1.000000000000000222, 1.000000000000000222, 0.9999999999999997780, 1.000000000000000222, 1.000000000000000222, 0.9999999999999997780, 1.000000000000000222, 1.000000000000000000, 1.000000000000000000, 1.000000000000000222, 0.9999999999999996669, 1.000000000000000444, 0.9999999999999997780, 0.9999999999999997780, 1.000000000000000000, 1.000000000000000000, 1.000000000000000000, 0.9999999999999996669, 1.000000000000000444, 1.000000000000000000, 1.000000000000000222, 1.000000000000000000, 0.9999999999999997780, 1.000000000000000222, 0.9999999999999997780, 1.000000000000000222, 1.000000000000000000, 1.000000000000000000, 1.000000000000000222, 1.000000000000000000, 1.000000000000000222, 0.9999999999999994449, 1.000000000000000444, 1.000000000000000000, 0.9999999999999996669, 1.000000000000000222, 0.9999999999999997780, 1.000000000000000222, 0.9999999999999997780, 1.000000000000000000, 1.000000000000000000, 1.000000000000000000, 1.000000000000000000, 1.000000000000000000, 1.000000000000000444, 1.000000000000000000, 1.000000000000000000, 1.000000000000000222, 1.000000000000000000, 1.000000000000000000, 0.9999999999999997780, 1.000000000000000000, 1.000000000000000222, 1.000000000000000000, 1.000000000000000222, 0.9999999999999997780, 1.000000000000000000, 0.9999999999999997780, 0.9999999999999997780, 1.000000000000000222, 0.9999999999999997780, 1.000000000000000444, 0.9999999999999997780, 1.000000000000000000, 1.000000000000000222, 1.000000000000000000, 1.000000000000000000, 0.9999999999999997780, 1.000000000000000222, 1.000000000000000000, 1.000000000000000000, 1.000000000000000000, 1.000000000000000222, 0.9999999999999996669, 1.000000000000000222, 1.000000000000000222, 0.9999999999999996669, 1.000000000000000444, 0.9999999999999996669, 1.000000000000000000, 1.000000000000000222, 0.9999999999999996669, 1.000000000000000222, 1.000000000000000000, 1.000000000000000222, 1.000000000000000000, 1.000000000000000222, 0.9999999999999997780, 1.000000000000000444, 0.9999999999999997780, 0.9999999999999997780, 1.000000000000000222, 0.9999999999999996669, 1.000000000000000222, 1.000000000000000000, 1.000000000000000000, 1.000000000000000000, 0.9999999999999997780, 1.000000000000000222, 1.000000000000000222, 0.9999999999999997780, 1.000000000000000222, 0.9999999999999997780, 1.000000000000000222, 1.000000000000000000, 1.000000000000000444, 1.000000000000000000, 1.000000000000000222, 0.9999999999999996669, 1.000000000000000444, 0.9999999999999993339, 1.000000000000000444, 0.9999999999999997780, 1.000000000000000444, 0.9999999999999997780, 1.000000000000000000, 1.000000000000000000, 0.9999999999999997780, 1.000000000000000222, 0.9999999999999997780, 0.9999999999999996669, 1.000000000000000444, 1.000000000000000222, 1.000000000000000000, 0.9999999999999997780, 1.000000000000000222, 0.9999999999999996669, 1.000000000000000222, 0.9999999999999997780, 1.000000000000000222, 1.000000000000000000, 1.000000000000000000, 1.000000000000000000, 1.000000000000000000, 0.9999999999999997780, 1.000000000000000000, 1.000000000000000000, 0.9999999999999997780, 1.000000000000000000, 1.000000000000000000, 1.000000000000000000, 1.000000000000000222, 1.000000000000000000, 1.000000000000000444, 1.000000000000000222, 1.000000000000000000, 1.000000000000000000, 0.9999999999999997780, 1.000000000000000222, 1.000000000000000000, 1.000000000000000000, 1.000000000000000000, 0.9999999999999997780, 1.000000000000000222, 0.9999999999999997780, 1.000000000000000222, 1.000000000000000444, 0.9999999999999997780, 1.000000000000000222, 1.000000000000000000, 1.000000000000000000, 1.000000000000000000, 0.9999999999999997780, 1.000000000000000444, 0.9999999999999997780, 1.000000000000000222, 0.9999999999999997780, 1.000000000000000222, 0.9999999999999994449, 1.000000000000000222, 1.000000000000000000, 1.000000000000000222, 1.000000000000000000, 0.9999999999999997780, 1.000000000000000222, 1.000000000000000000, 0.9999999999999997780, 1.000000000000000444, 0.9999999999999996669, 1.000000000000000222, 1.000000000000000000, 1.000000000000000000, 1.000000000000000222, 0.9999999999999997780, 0.9999999999999997780, 1.000000000000000444, 1.000000000000000222, 1.000000000000000000, 0.9999999999999997780, 0.9999999999999997780, 1.000000000000000222, 1.000000000000000000, 1.000000000000000222, 1.000000000000000000, 0.9999999999999997780, 1.000000000000000000, 1.000000000000000000, 1.000000000000000000, 1.000000000000000222, 0.9999999999999997780, 1.000000000000000222, 1.000000000000000000, 1.000000000000000000, 1.000000000000000000, 0.9999999999999997780, 1.000000000000000000, 1.000000000000000222, 1.000000000000000222, 0.9999999999999996669, 1.000000000000000444, 0.9999999999999996669, 1.000000000000000222, 1.000000000000000000, 1.000000000000000222, 0.9999999999999997780, 1.000000000000000444, 1.000000000000000000, 1.000000000000000444, 0.9999999999999994449, 1.000000000000000222, 0.9999999999999997780, 0.9999999999999997780, 1.000000000000000000, 1.000000000000000222, 1.000000000000000000, 1.000000000000000000, 1.000000000000000000, 1.000000000000000222, 0.9999999999999996669, 1.000000000000000222, 1.000000000000000000, 0.9999999999999996669, 1.000000000000000444, 1.000000000000000000, 1.000000000000000000, 1.000000000000000000, 0.9999999999999996669, 1.000000000000000222, 1.000000000000000000, 1.000000000000000000, 1.000000000000000222, 0.9999999999999997780, 0.9999999999999997780, 1.000000000000000000, 1.000000000000000000, 1.000000000000000222, 0.9999999999999997780, 1.000000000000000222, 1.000000000000000000, 1.000000000000000000, 0.9999999999999996669, 1.000000000000000222, 1.000000000000000000, 1.000000000000000222, 1.000000000000000000, 1.000000000000000000, 1.000000000000000000, 0.9999999999999997780, 1.000000000000000222, 0.9999999999999996669, 1.000000000000000444, 1.000000000000000000, 0.9999999999999997780, 1.000000000000000000, 1.000000000000000222, 1.000000000000000222, 0.9999999999999996669, 1.000000000000000000, 1.000000000000000000, 0.9999999999999997780, 1.000000000000000222, 1.000000000000000000, 1.000000000000000222, 0.9999999999999996669, 1.000000000000000444, 1.000000000000000000, 1.000000000000000000, 1.000000000000000000, 1.000000000000000222, 1.000000000000000000, 0.9999999999999997780, 1.000000000000000444, 1.000000000000000000, 1.000000000000000444, 0.9999999999999997780, 1.000000000000000444, 1.000000000000000000, 1.000000000000000222, 1.000000000000000222, 1.000000000000000000, 0.9999999999999996669, 1.000000000000000000, 1.000000000000000000, 1.000000000000000000, 1.000000000000000000, 1.000000000000000222, 0.9999999999999996669, 1.000000000000000000, 1.000000000000000222, 0.9999999999999997780, 0.9999999999999997780, 1.000000000000000000, 1.000000000000000000, 1.000000000000000000, 1.000000000000000000) ) ) 
 REPRESENTATION_ITEM ( '' )  SURFACE ( )  );
#144371=CARTESIAN_POINT ( 'NONE',  ( 1.639757756142570244, 2.007014814066264474, -0.8283606533975582664 ) ) ;
#144376=CARTESIAN_POINT ( 'NONE',  ( 2.758895227446885645, -1.625506345271657604, -0.9254698705311247275 ) ) ;
#144377=CARTESIAN_POINT ( 'NONE',  ( 0.2982115315293157320, -2.060280707965747027, -0.05303618902755858483 ) ) ;
#144378=CARTESIAN_POINT ( 'NONE',  ( -0.02224634325196597762, 7.629137130509080045, -2.889100442546748582 ) ) ;
#144379=CARTESIAN_POINT ( 'NONE',  ( 6.827182134110246103, 3.705739211453745074, 2.325493694733235195 ) ) ;
#144381=CARTESIAN_POINT ( 'NONE',  ( 2.086439996564274146, -1.175226666667992914, 1.508458442701497315 ) ) ;
#144382=CARTESIAN_POINT ( 'NONE',  ( 4.627684317651063139, -1.090007866362858291, -1.394274008033623113 ) ) ;
#144383=CARTESIAN_POINT ( 'NONE',  ( 1.980978873585538480, -1.748965405663160944, -0.7736543689686598002 ) ) ;
#144386=CARTESIAN_POINT ( 'NONE',  ( 5.360912872498101223, -0.05169663686300975808, -1.915091480415902048 ) ) ;
#144388=CARTESIAN_POINT ( 'NONE',  ( 6.566861343609567747, 1.460344857008318398, -1.321773145083295464 ) ) ;
#144391=CARTESIAN_POINT ( 'NONE',  ( 5.366025703835962446, 0.9229158262306772498, 1.627043297953718382 ) ) ;
#144392=CARTESIAN_POINT ( 'NONE',  ( 1.242498012622397674, 0.3540479964400863877, 1.790853789395550955 ) ) ;
#144394=CARTESIAN_POINT ( 'NONE',  ( 4.811249113497881424, 1.919052844561389692, 1.089612025192594258 ) ) ;
#144397=CARTESIAN_POINT ( 'NONE',  ( 3.279784535431028658, -1.988673744353728123, 0.5473864365612387539 ) ) ;
#144405=VERTEX_POINT ( 'NONE', #188448 ) ;
#144406=CARTESIAN_POINT ( 'NONE',  ( 5.195788487752976081, -1.461605715988937515, -1.466586839339318882 ) ) ;
#144408=CARTESIAN_POINT ( 'NONE',  ( 2.161604200734370096, 0.3718190433680613749, -2.129227089361292791 ) ) ;
#144410=CARTESIAN_POINT ( 'NONE',  ( 3.598311091834342612, -0.9934155151001385908, 1.758370388466141465 ) ) ;
#144411=CARTESIAN_POINT ( 'NONE',  ( 6.620655732516650183, 4.692022689331314389, 2.636326274693585159 ) ) ;
#144415=CARTESIAN_POINT ( 'NONE',  ( 1.112517963266421939, 1.944731545904467396, 0.5331650539944567946 ) ) ;
#144416=CARTESIAN_POINT ( 'NONE',  ( 5.636325218313963603, 0.4264374063192889475, 2.149501299143250055 ) ) ;
#144418=CARTESIAN_POINT ( 'NONE',  ( 5.045129621168108258, 0.1466893748028278155, 1.906852434080000824 ) ) ;
#144422=CARTESIAN_POINT ( 'NONE',  ( 3.286732619643798703, 1.587825416925658262, -1.242744175535138940 ) ) ;
#144425=CARTESIAN_POINT ( 'NONE',  ( 5.790025292147505276, -0.7713913475298206368, 1.542752225890047679 ) ) ;
#144430=CARTESIAN_POINT ( 'NONE',  ( 0.5321919801732944988, 1.189095644551215525, 1.694524325727378322 ) ) ;
#144433=CARTESIAN_POINT ( 'NONE',  ( 5.320911890206324379, 1.367686037040320768, -1.187891890861958899 ) ) ;
#144436=CARTESIAN_POINT ( 'NONE',  ( 6.604213110542080045, -0.7679849629102013520, 1.639316308541746592 ) ) ;
#144439=CARTESIAN_POINT ( 'NONE',  ( 2.730644157659181559, 0.2691629481662433099, 2.174792594416566249 ) ) ;
#144442=CARTESIAN_POINT ( 'NONE',  ( 0.3265133270617843197, -1.284392789319420913, 1.483054880892266114 ) ) ;
#144444=CARTESIAN_POINT ( 'NONE',  ( 4.640194291141960470, 0.7370120463812566136, 1.768359169405645304 ) ) ;
#144452=CARTESIAN_POINT ( 'NONE',  ( 2.413140945657660907, 1.930630709398067246, 0.9725960170764782475 ) ) ;
#144455=CARTESIAN_POINT ( 'NONE',  ( 1.676486011727536418, -1.732352342712149440, -0.5761224636358779350 ) ) ;
#144456=CARTESIAN_POINT ( 'NONE',  ( -0.1929003719821283658, -0.4722129235960636495, -2.074948700427194481 ) ) ;
#144457=CARTESIAN_POINT ( 'NONE',  ( 4.207882836062684540, -1.820678405428953095, 0.1343838851760314757 ) ) ;
#144459=CARTESIAN_POINT ( 'NONE',  ( 2.830216799141628492, -0.9462872844297947061, -1.661813493071498726 ) ) ;
#144461=CARTESIAN_POINT ( 'NONE',  ( 3.525798893484650254, 1.922080780809858114, -0.4290687576708405726 ) ) ;
#144463=CARTESIAN_POINT ( 'NONE',  ( 5.829623785595809515, 0.9536246560681378437, -1.691722214391349732 ) ) ;
#144467=CARTESIAN_POINT ( 'NONE',  ( 6.469000917296717112, -1.638331675554663747, 1.346054232038436105 ) ) ;
#144469=CARTESIAN_POINT ( 'NONE',  ( 3.897043152223302886, -0.1904361752127527174, -1.902785305300330743 ) ) ;
#144473=CARTESIAN_POINT ( 'NONE',  ( 5.567046518764520613, -1.585636444731153061, 1.240160563295252372 ) ) ;
#144475=CARTESIAN_POINT ( 'NONE',  ( 6.551389018236878137, -1.469694460105780642, -1.082916835497591324 ) ) ;
#144476=CARTESIAN_POINT ( 'NONE',  ( 0.8364851226981102617, -1.151554295457988930, 1.720357586142134076 ) ) ;
#144482=SURFACE_STYLE_USAGE ( .BOTH. , #192094 ) ;
#144488=CARTESIAN_POINT ( 'NONE',  ( 3.920349067101033036, -1.199671410015031192, -1.252466492151423694 ) ) ;
#144490=CARTESIAN_POINT ( 'NONE',  ( 1.657173498210939622, 1.694793865239911712, -1.188712540599102141 ) ) ;
#144491=CARTESIAN_POINT ( 'NONE',  ( 2.284896850813819213, 1.698563897025050506, -1.263734059995786030 ) ) ;
#144495=CARTESIAN_POINT ( 'NONE',  ( 0.3386328343033001564, -1.908876393446774955, -0.4841592594212947298 ) ) ;
#144501=CARTESIAN_POINT ( 'NONE',  ( 2.062813984423640612, -2.096776522422974409, -0.9266714075790563054 ) ) ;
#144502=CARTESIAN_POINT ( 'NONE',  ( 0.7502976729042536430, 0.5272139720400963459, 1.747899773703022408 ) ) ;
#144503=CARTESIAN_POINT ( 'NONE',  ( 3.181800181368432678, 1.864768544494728175, -0.4233684943922080834 ) ) ;
#144507=CARTESIAN_POINT ( 'NONE',  ( 1.670183121039736207, 2.007516039388768991, -0.1524388337148015193 ) ) ;
#144508=CARTESIAN_POINT ( 'NONE',  ( 1.692165188054130187, 0.9715730843921737137, -1.704227633833883759 ) ) ;
#144512=CARTESIAN_POINT ( 'NONE',  ( 4.751946794759532189, 0.7997392584290877737, 1.931828438813171456 ) ) ;
#144513=CARTESIAN_POINT ( 'NONE',  ( 2.922431196026415101, 1.665835785064853969, 0.5981315555363684311 ) ) ;
#144516=CARTESIAN_POINT ( 'NONE',  ( 6.650320093084655326, -1.776417932240816011, 1.448308594842239838 ) ) ;
#144517=CARTESIAN_POINT ( 'NONE',  ( 4.417713501739753745, 1.067903927642421591, -1.374066674465204363 ) ) ;
#144520=CARTESIAN_POINT ( 'NONE',  ( 4.745267847829638619, -1.681796892959321665, -0.4208994435666196798 ) ) ;
#144521=CARTESIAN_POINT ( 'NONE',  ( 4.158752335142390955, -0.6773029245935069387, -2.062915381819859562 ) ) ;
#144523=CARTESIAN_POINT ( 'NONE',  ( 6.280482454654814362, -0.5424645211669875122, -1.942098458069536848 ) ) ;
#144524=CARTESIAN_POINT ( 'NONE',  ( 6.312500000001141309, 1.451031289089316667, 1.451031289060858098 ) ) ;
#144527=CARTESIAN_POINT ( 'NONE',  ( 3.118101180835719521, -0.9482820236139007930, -1.676744857821835355 ) ) ;
#144529=CARTESIAN_POINT ( 'NONE',  ( 0.1533981569187261029, 0.3862642299664406642, 2.187325829255863940 ) ) ;
#144531=CARTESIAN_POINT ( 'NONE',  ( 6.883263157960393563, 1.268976584491373183, 2.060807272249213451 ) ) ;
#144534=CARTESIAN_POINT ( 'NONE',  ( 2.227449089350467482, 1.985603210742479252, 0.9958825451741261103 ) ) ;
#144541=CARTESIAN_POINT ( 'NONE',  ( 0.5279704824466545654, -1.728000714500482982, 1.038995864524896673 ) ) ;
#144543=CARTESIAN_POINT ( 'NONE',  ( 5.283662074727401681, -1.959763400824132251, 0.6436608119341418188 ) ) ;
#144548=CARTESIAN_POINT ( 'NONE',  ( 6.872336254976084469, -1.150436037642876608, 1.475500831757702969 ) ) ;
#144549=CARTESIAN_POINT ( 'NONE',  ( 5.942016496743827147, -1.492280758002052510, -0.8831153342708076837 ) ) ;
#144550=CARTESIAN_POINT ( 'NONE',  ( 6.022986557963563747, -1.635662919198093812, 0.5951793741951169059 ) ) ;
#144551=CARTESIAN_POINT ( 'NONE',  ( 2.472590379642979563, -2.194723544211283350, -0.6619992606377905764 ) ) ;
#144553=CARTESIAN_POINT ( 'NONE',  ( 0.7965151530783078915, 1.503791256141374211, 1.061989520254283059 ) ) ;
#144555=CARTESIAN_POINT ( 'NONE',  ( 1.729251940891060713, -1.720190037149814444, 0.6116943438041824166 ) ) ;
#144556=CARTESIAN_POINT ( 'NONE',  ( 1.166276502169643070, -1.387892208999995436, 1.695937554688830451 ) ) ;
#144558=CARTESIAN_POINT ( 'NONE',  ( 4.858481695672255185, 0.8034365979220282616, 1.946882858121199211 ) ) ;
#144561=CARTESIAN_POINT ( 'NONE',  ( 1.750525128138082254, -2.060206210462053988, -0.2049951091474821463 ) ) ;
#144564=CARTESIAN_POINT ( 'NONE',  ( 4.336665864168765872, 1.303721989063952424, -1.672289659653345639 ) ) ;
#144565=CARTESIAN_POINT ( 'NONE',  ( 0.2055245034400269288, -0.5150763003200479195, 1.856310442892949553 ) ) ;
#144572=CARTESIAN_POINT ( 'NONE',  ( 5.959260761812961604, -1.790568634313693730, 1.135864312162476297 ) ) ;
#144573=CARTESIAN_POINT ( 'NONE',  ( 1.290213853529555976, -0.9470325862265884798, 1.881093767389901750 ) ) ;
#144576=CARTESIAN_POINT ( 'NONE',  ( 5.383604208181901107, -1.767738693978682996, 0.5818682867176503404 ) ) ;
#144584=CARTESIAN_POINT ( 'NONE',  ( 2.172246964874047670, -0.9220853831424129510, -1.731647142839589648 ) ) ;
#144585=CARTESIAN_POINT ( 'NONE',  ( 0.7433210806352362754, -1.853469564684958382, 1.112228649290482263 ) ) ;
#144589=CARTESIAN_POINT ( 'NONE',  ( 2.582960874182936628, 1.135899660060729399, -1.309998962497432196 ) ) ;
#144590=CARTESIAN_POINT ( 'NONE',  ( 2.079653994411820417, -1.706432041406182654, -0.3408243062450431182 ) ) ;
#144594=CARTESIAN_POINT ( 'NONE',  ( 0.8255457999647041190, -1.462224166115761337, 1.388270745661695837 ) ) ;
#144595=CARTESIAN_POINT ( 'NONE',  ( 6.925078400183597438, 7.629137130509070275, 2.744348168701661095 ) ) ;
#144597=CARTESIAN_POINT ( 'NONE',  ( 0.8660190917160478508, 0.9698478150794390684, 1.716334202883246229 ) ) ;
#144598=CARTESIAN_POINT ( 'NONE',  ( 5.677967274442059953, 1.882970570262190835, -0.3333453579756898155 ) ) ;
#144603=CARTESIAN_POINT ( 'NONE',  ( 0.9264325174072656210, -0.9100096784926974269, -1.803132658094412477 ) ) ;
#144605=CARTESIAN_POINT ( 'NONE',  ( 4.841030633121579996, 0.3891503725830172677, 2.274395804800657839 ) ) ;
#144606=CARTESIAN_POINT ( 'NONE',  ( 6.215287892896892430, -1.681934637451238279, -1.009743211781432670 ) ) ;
#144607=CARTESIAN_POINT ( 'NONE',  ( 3.326955106232618586, -1.810811308836293598, -0.7551016064811162387 ) ) ;
#144611=CARTESIAN_POINT ( 'NONE',  ( 1.587271696126206111, 1.763578281176042761, 1.171447882250826522 ) ) ;
#144614=CARTESIAN_POINT ( 'NONE',  ( 1.341482821134845738, 1.838956754096718660, 0.09199767257135618714 ) ) ;
#144617=CARTESIAN_POINT ( 'NONE',  ( 2.408575119285644384, -2.115224228095522907, -0.1514441693673748146 ) ) ;
#144622=CARTESIAN_POINT ( 'NONE',  ( 3.339188440279222458, -1.819168825518402199, 0.9681599264559497264 ) ) ;
#144624=CARTESIAN_POINT ( 'NONE',  ( 0.2570343420702363435, 1.821350608449383124, -0.2692129421619017804 ) ) ;
#144628=CARTESIAN_POINT ( 'NONE',  ( 0.2587985324217950689, 0.8487602207661277820, 2.037339956011212649 ) ) ;
#144629=CARTESIAN_POINT ( 'NONE',  ( 2.249658590878771847, -1.816102774931172448, -1.348951556275684194 ) ) ;
#144631=CARTESIAN_POINT ( 'NONE',  ( 2.126969254794884634, 1.619647995875729496, 0.8116002879420233240 ) ) ;
#144632=CARTESIAN_POINT ( 'NONE',  ( 2.747180457951060362, 0.2762254639866565942, -1.895546175561702018 ) ) ;
#144633=CARTESIAN_POINT ( 'NONE',  ( 3.719242722441223226, -1.824546119899137731, -0.9785211796824041519 ) ) ;
#144635=CARTESIAN_POINT ( 'NONE',  ( 2.149238863156129220, -1.582378584423797419, -1.175707468242733977 ) ) ;
#144636=CARTESIAN_POINT ( 'NONE',  ( 0.3582593949469566885, 0.7340744485371183403, 1.781236698655277895 ) ) ;
#144637=CARTESIAN_POINT ( 'NONE',  ( 2.658895327995167701, -1.626580691111865207, -0.9237732865615968514 ) ) ;
#144638=CARTESIAN_POINT ( 'NONE',  ( 1.102667438898880192, -2.307868968971817036, 0.004735511273680144059 ) ) ;
#144640=CARTESIAN_POINT ( 'NONE',  ( 3.138934141195717675, -0.1340819638860979157, -1.856265897873999426 ) ) ;
#144642=CARTESIAN_POINT ( 'NONE',  ( 6.654736832427365911, -0.5462217193984253427, -1.988994552010774797 ) ) ;
#144647=CARTESIAN_POINT ( 'NONE',  ( 5.948290813881442318, 2.103388047956732620, 0.1067411848718266276 ) ) ;
#144649=CARTESIAN_POINT ( 'NONE',  ( 5.694645791630270182, -0.5191100231263061637, -2.098234375727751733 ) ) ;
#144650=CARTESIAN_POINT ( 'NONE',  ( 6.041667287826984811, -1.900962894602696185, 0.6825640075473203838 ) ) ;
#144654=CARTESIAN_POINT ( 'NONE',  ( 6.825078400183513416, 0.6012913621265563169, 1.809472532188656890 ) ) ;
#144657=CARTESIAN_POINT ( 'NONE',  ( 4.434779938697545276, -1.616694733667634942, 1.205040202231235869 ) ) ;
#144663=CARTESIAN_POINT ( 'NONE',  ( 6.332923096303629151, 0.2067577541180857514, 2.151790036905242953 ) ) ;
#144668=CARTESIAN_POINT ( 'NONE',  ( 6.380482474105581225, -0.5405081658083621399, -1.942537888137134461 ) ) ;
#144670=CARTESIAN_POINT ( 'NONE',  ( 6.539320575229258026, 4.689551739520863904, 2.765837357486185866 ) ) ;
#144671=CARTESIAN_POINT ( 'NONE',  ( 2.138867256381206783, -1.541494696628985528, 0.7741069473117598854 ) ) ;
#144675=CARTESIAN_POINT ( 'NONE',  ( 6.678970768140332304, -0.09217866350584581758, -1.868372134486769420 ) ) ;
#144676=CARTESIAN_POINT ( 'NONE',  ( 0.8033857101962671443, 1.774305754185826034, -0.9510189173033887222 ) ) ;
#144679=CARTESIAN_POINT ( 'NONE',  ( 3.188704395469597497, -2.173853526369253331, -0.3788738375181537332 ) ) ;
#144681=CARTESIAN_POINT ( 'NONE',  ( 5.787976215063657115, -1.371286462501415837, -1.683233787797025371 ) ) ;
#144685=CARTESIAN_POINT ( 'NONE',  ( 3.563236855010095461, -1.732559338849114727, 1.222301536229251306 ) ) ;
#144686=CARTESIAN_POINT ( 'NONE',  ( 2.653922917551009952, 1.081085551080329443, 1.701936510390425150 ) ) ;
#144687=CARTESIAN_POINT ( 'NONE',  ( 3.041053801226344611, 0.04897401433806568977, 1.811106077260196345 ) ) ;
#144691=CARTESIAN_POINT ( 'NONE',  ( 0.1978467685152424937, -1.870139902624564865, -0.05068021481659244765 ) ) ;
#144694=CARTESIAN_POINT ( 'NONE',  ( 1.235391793297924812, 0.5527703352327991704, -1.834263772151963456 ) ) ;
#144702=CARTESIAN_POINT ( 'NONE',  ( 5.682550338946038337, -2.108058120380253087, -0.4779004524640489415 ) ) ;
#144705=CARTESIAN_POINT ( 'NONE',  ( 2.707414796094851361, 1.816601298730673220, -1.093838055662835096 ) ) ;
#144708=CARTESIAN_POINT ( 'NONE',  ( 4.428955518335824237, 0.09376622492938446740, 1.969227427985324352 ) ) ;
#144709=CARTESIAN_POINT ( 'NONE',  ( 6.451426615364327155, -1.705040744490589066, 0.8662930942644477827 ) ) ;
#144712=CARTESIAN_POINT ( 'NONE',  ( 0.8189040078958352842, -1.500748464528355974, 1.426492703164506937 ) ) ;
#144713=CARTESIAN_POINT ( 'NONE',  ( 3.081904124835439074, -1.913310220277367080, -0.3314154666464886323 ) ) ;
#144717=CARTESIAN_POINT ( 'NONE',  ( 2.150438955405692631, -1.615297803084648098, 1.327229747913031055 ) ) ;
#144720=CARTESIAN_POINT ( 'NONE',  ( 0.2404698186789978875, 1.732857435387507250, 0.5278947837941138088 ) ) ;
#144722=CARTESIAN_POINT ( 'NONE',  ( 4.864015066594513215, 2.183220759563545776, -0.3215228633955333759 ) ) ;
#144724=CARTESIAN_POINT ( 'NONE',  ( 3.645738483435243982, -1.669485028154977790, -1.443228448415982079 ) ) ;
#144727=CARTESIAN_POINT ( 'NONE',  ( 2.209489775926488431, 1.479274643242427301, 1.211860329591994745 ) ) ;
#144730=CARTESIAN_POINT ( 'NONE',  ( 3.736834853878097107, -1.994506513866915576, -0.5549897870569252545 ) ) ;
#144732=CARTESIAN_POINT ( 'NONE',  ( 3.256853613824191029, -1.637998819981079990, 1.410756932016984377 ) ) ;
#144733=CARTESIAN_POINT ( 'NONE',  ( 5.267185993530860699, 2.112242253262315739, -0.5839428218426812034 ) ) ;
#144742=CARTESIAN_POINT ( 'NONE',  ( 0.6334356698059575574, 0.5880228326464317368, 1.928751028484784413 ) ) ;
#144745=CARTESIAN_POINT ( 'NONE',  ( 4.205968427668831389, 0.7022645179026367757, -1.947615878368731623 ) ) ;
#144746=CARTESIAN_POINT ( 'NONE',  ( 3.141151230849213327, -1.698683669661217754, 0.9087857633808916757 ) ) ;
#144747=CARTESIAN_POINT ( 'NONE',  ( 0.1402502066264778580, 0.7743353953559418690, 1.862009890338502505 ) ) ;
#144750=CARTESIAN_POINT ( 'NONE',  ( 4.451979310445155491, -0.7576744193203123201, 1.818072383216073007 ) ) ;
#144751=CARTESIAN_POINT ( 'NONE',  ( -0.02900071798685524560, -0.004641455105012376459, -2.173770343569726649 ) ) ;
#144752=CARTESIAN_POINT ( 'NONE',  ( 4.477060521952030747, -0.002618581577289170060, -1.825872481161804561 ) ) ;
#144753=EDGE_CURVE ( 'NONE', #40908, #202176, #108804, .T. ) ;
#144759=CARTESIAN_POINT ( 'NONE',  ( 1.610644152589552958, -0.2245515952020246675, 1.827417025815617935 ) ) ;
#144760=CARTESIAN_POINT ( 'NONE',  ( 4.886981372429439752, -1.897129443012405936, -0.6741400253723847102 ) ) ;
#144761=CARTESIAN_POINT ( 'NONE',  ( 0.3514386742532841779, -1.080868183629126067, 2.028406642177064345 ) ) ;
#144762=CARTESIAN_POINT ( 'NONE',  ( 5.893401036868160858, -1.775023410133094615, 0.8355650083611900758 ) ) ;
#144764=CARTESIAN_POINT ( 'NONE',  ( 0.2333690889706682703, 1.352610664630080839, -2.308230059406161772 ) ) ;
#144768=CARTESIAN_POINT ( 'NONE',  ( 1.277023361749257457, 1.930420895987930097, -0.8034254789068133729 ) ) ;
#144769=CARTESIAN_POINT ( 'NONE',  ( 6.403183007056281184, 1.474056081383187555, 0.9792082336040304202 ) ) ;
#144771=CARTESIAN_POINT ( 'NONE',  ( -0.1104750535120251481, 6.947232870375212421, -2.698533382536407732 ) ) ;
#144772=CARTESIAN_POINT ( 'NONE',  ( 0.8018505195637380956, 1.319035621562004934, -1.135522575981460003 ) ) ;
#144777=CARTESIAN_POINT ( 'NONE',  ( 1.998289267358617671, -0.4583927764671858474, -1.662768097037459869 ) ) ;
#144779=CARTESIAN_POINT ( 'NONE',  ( 1.769323484426460480, 2.095969018468134770, -0.6401429536977767398 ) ) ;
#144780=CARTESIAN_POINT ( 'NONE',  ( 3.580891165198408110, -2.126768340858419926, -0.5889919780145411732 ) ) ;
#144782=CARTESIAN_POINT ( 'NONE',  ( 1.182764167570474534, 1.294921473658101840, -1.742447618606123960 ) ) ;
#144783=CARTESIAN_POINT ( 'NONE',  ( 0.4690313652776016418, 0.1822212253758948297, -1.816563760317004395 ) ) ;
#144784=CARTESIAN_POINT ( 'NONE',  ( 2.870428589035282751, -2.086819620220676352, -0.3573068958101219827 ) ) ;
#144785=CARTESIAN_POINT ( 'NONE',  ( 6.639320575229255006, 7.629137130509086262, 2.396737603865983779 ) ) ;
#144788=CARTESIAN_POINT ( 'NONE',  ( 3.210744404368763405, 2.073164229931067304, 0.9784878017504093917 ) ) ;
#144790=CARTESIAN_POINT ( 'NONE',  ( 0.07755575628181145265, 6.946778278137148099, -2.783982195446454533 ) ) ;
#144792=CARTESIAN_POINT ( 'NONE',  ( 5.901095752275416828, -0.3235219084677161128, -2.197517257070471075 ) ) ;
#144798=CARTESIAN_POINT ( 'NONE',  ( 3.674454069786535548, 1.462445212485608437, 1.388486266691544957 ) ) ;
#144800=CARTESIAN_POINT ( 'NONE',  ( 1.991156689281988745, 0.1981002678682428353, 2.053003549438499054 ) ) ;
#144806=CARTESIAN_POINT ( 'NONE',  ( 5.156268285673103691, -1.588865937562380148, 1.509524371192130676 ) ) ;
#144807=CARTESIAN_POINT ( 'NONE',  ( 2.127577483945505055, 0.4445034925110411539, 1.966644524931899563 ) ) ;
#144808=CARTESIAN_POINT ( 'NONE',  ( 2.225889136967126536, 1.786374552192676823, 0.4457033907802817052 ) ) ;
#144810=CARTESIAN_POINT ( 'NONE',  ( 5.086841682847768276, -0.2248377094848166835, -1.811598703993194670 ) ) ;
#144811=CARTESIAN_POINT ( 'NONE',  ( 6.539686446881147752, -1.556848207870220602, 1.281141925495055123 ) ) ;
#144813=CARTESIAN_POINT ( 'NONE',  ( 5.629810878523249684, -1.430378642458853378, -1.753011776973804725 ) ) ;
#144815=CARTESIAN_POINT ( 'NONE',  ( 0.3464870678724129016, 2.100606130083045198, 0.1525024232564754778 ) ) ;
#144826=CARTESIAN_POINT ( 'NONE',  ( 2.443850186789862100, -2.070980460497043651, 0.8039724962528942420 ) ) ;
#144830=CARTESIAN_POINT ( 'NONE',  ( 3.736726379466179804, -1.890069333072645241, -0.5255722985574098338 ) ) ;
#144839=CARTESIAN_POINT ( 'NONE',  ( 2.830460552442021438, -1.048868820301660953, -1.842999677239331113 ) ) ;
#144841=CARTESIAN_POINT ( 'NONE',  ( 3.907220446582274853, 1.852832235905249370, 1.113321777468062823 ) ) ;
#144842=CARTESIAN_POINT ( 'NONE',  ( 2.735704033801298340, 1.827604811068459734, 0.2230458208379028084 ) ) ;
#144845=CARTESIAN_POINT ( 'NONE',  ( 5.736210779895188239, 0.3457693788900301768, 1.705448404129115580 ) ) ;
#144848=CARTESIAN_POINT ( 'NONE',  ( 6.620655732516621761, 0.004685112605665223660, 1.926407831898163003 ) ) ;
#144849=CARTESIAN_POINT ( 'NONE',  ( 3.221700144506876917, -2.083771231579465866, 0.5749860669421112958 ) ) ;
#144850=CARTESIAN_POINT ( 'NONE',  ( 4.675157572021750418, -0.8594996001172333644, -1.823839583407538267 ) ) ;
#144852=CARTESIAN_POINT ( 'NONE',  ( 2.747127081003514881, -1.797865629537301668, 1.199965651887124896 ) ) ;
#144853=CARTESIAN_POINT ( 'NONE',  ( 3.497303454036035930, 1.552041748764835249, 1.215357900914854516 ) ) ;
#144854=CARTESIAN_POINT ( 'NONE',  ( 4.669442277103274641, 1.121057080241712578, 1.585637770727834850 ) ) ;
#144863=CARTESIAN_POINT ( 'NONE',  ( 0.6224627697807674220, -1.182292326766160251, -1.863150505713019989 ) ) ;
#144865=CARTESIAN_POINT ( 'NONE',  ( 6.526224699197019419, 1.005635830909179074, 1.684226478273798788 ) ) ;
#144869=CARTESIAN_POINT ( 'NONE',  ( 0.07499057489262526965, 5.723988098492513998, -2.549530206576706259 ) ) ;
#144870=CARTESIAN_POINT ( 'NONE',  ( 5.261588992693945421, 0.9106475924270783784, 1.600083007495013643 ) ) ;
#144875=CARTESIAN_POINT ( 'NONE',  ( 6.363548717301088509, -1.704009271243651868, -1.262090224194649446 ) ) ;
#144879=CARTESIAN_POINT ( 'NONE',  ( 6.485628570817172367, 1.417799985879987901, 1.495801911481582813 ) ) ;
#144881=CARTESIAN_POINT ( 'NONE',  ( 2.119380567849386665, 0.3219547178687692801, -1.832826937841147252 ) ) ;
#144882=CARTESIAN_POINT ( 'NONE',  ( 3.157574601152390414, 0.8305207305269333151, 1.643389852989694200 ) ) ;
#144887=CARTESIAN_POINT ( 'NONE',  ( 3.528125218122651230, -1.314342534882004809, -1.772652456903674567 ) ) ;
#144888=CARTESIAN_POINT ( 'NONE',  ( 5.923173471921922228, -0.06425113298673529316, 2.261675518886300473 ) ) ;
#144890=CARTESIAN_POINT ( 'NONE',  ( 5.291193953664572902, -0.05252268709225348109, -1.811016617013387009 ) ) ;
#144891=CARTESIAN_POINT ( 'NONE',  ( -0.1355283706049141557, -1.957205112593700003, -0.4852584411360050254 ) ) ;
#144893=CARTESIAN_POINT ( 'NONE',  ( 6.702024585102262400, -1.870183347854617040, 0.04844413084104796929 ) ) ;
#144895=CARTESIAN_POINT ( 'NONE',  ( 6.737169288263022082, -1.578518636041785994, 0.8004799088773879578 ) ) ;
#144896=CARTESIAN_POINT ( 'NONE',  ( 1.481658059775035952, -0.6748446255696785023, 1.900416712880992343 ) ) ;
#144898=CARTESIAN_POINT ( 'NONE',  ( 2.526118869349633034, -1.213293402057673775, -1.721263080769465992 ) ) ;
#144903=CARTESIAN_POINT ( 'NONE',  ( 2.566670905829854021, 0.6845714803544473703, 1.900350667086497580 ) ) ;
#144907=CARTESIAN_POINT ( 'NONE',  ( 3.515052679271633895, 1.952536648612019921, 0.9277410485990513767 ) ) ;
#144912=CARTESIAN_POINT ( 'NONE',  ( 0.2917819264270337110, -1.984717812412156501, 0.8806528889930710369 ) ) ;
#144916=CARTESIAN_POINT ( 'NONE',  ( 2.156058135970494227, 0.9403143569667195001, 1.979733194660021622 ) ) ;
#144918=CARTESIAN_POINT ( 'NONE',  ( 2.448426410784361185, 2.261989705503023806, 0.05584468559862928311 ) ) ;
#144926=CARTESIAN_POINT ( 'NONE',  ( 3.866244329565728943, -1.190307266767919536, 1.309773914726497734 ) ) ;
#144928=CARTESIAN_POINT ( 'NONE',  ( 0.2355646933672841947, -1.925288835042149760, 0.8538303211676525617 ) ) ;
#144932=CARTESIAN_POINT ( 'NONE',  ( 6.099232498865051255, -0.2440123228986730841, 2.001514574626765075 ) ) ;
#144936=CARTESIAN_POINT ( 'NONE',  ( 4.082764389539480732, -0.1829629792115642917, -1.861669828791753467 ) ) ;
#144937=CARTESIAN_POINT ( 'NONE',  ( 3.573154620739454668, 1.869565233029608420, 0.8895530118792621677 ) ) ;
#144940=CARTESIAN_POINT ( 'NONE',  ( 6.157120911006637165, -1.851533521339579380, -1.115484332758958974 ) ) ;
#144942=CARTESIAN_POINT ( 'NONE',  ( 3.279693232472491893, -1.891448704997201302, 0.5207070127687256633 ) ) ;
#144943=CARTESIAN_POINT ( 'NONE',  ( 0.6321852052597470850, 0.2004073784105386835, -2.006138679842318862 ) ) ;
#144947=CARTESIAN_POINT ( 'NONE',  ( 0.7197278698120103124, -0.9953326032119573785, -1.583558375183778288 ) ) ;
#144949=CARTESIAN_POINT ( 'NONE',  ( 2.689700119490782360, 1.910346015757229177, -0.6353908363993918673 ) ) ;
#144951=CARTESIAN_POINT ( 'NONE',  ( 2.161849840330143824, 1.305120488479810659, 1.667033946717882742 ) ) ;
#144953=CARTESIAN_POINT ( 'NONE',  ( 3.982925052038261526, 1.964963782255540359, 0.6523228965355857278 ) ) ;
#144955=CARTESIAN_POINT ( 'NONE',  ( 6.562449924160270065, -1.910870307864566575, -0.8485530564429457634 ) ) ;
#144957=CARTESIAN_POINT ( 'NONE',  ( 4.928627555176230857, 1.747287423663802075, 0.5288322122747670662 ) ) ;
#144962=CARTESIAN_POINT ( 'NONE',  ( 6.633804142636003931, -1.436369002829580133, -1.675418478561958802 ) ) ;
#144964=CARTESIAN_POINT ( 'NONE',  ( 5.268181577278353345, 1.909906527651853425, -0.09793718704654422180 ) ) ;
#144974=CARTESIAN_POINT ( 'NONE',  ( 4.499188554602613799, 1.501106652244098116, 1.115835331622745841 ) ) ;
#144975=CARTESIAN_POINT ( 'NONE',  ( 0.07680821025396293578, 0.7488618828427398011, -1.895266105024134839 ) ) ;
#144982=CARTESIAN_POINT ( 'NONE',  ( 1.305442304231837714, -1.549127766076626056, -1.215949579239549161 ) ) ;
#144983=CARTESIAN_POINT ( 'NONE',  ( 2.935172905452135161, -1.650095542580119812, -1.158671029019647358 ) ) ;
#144987=CARTESIAN_POINT ( 'NONE',  ( 4.084055714405177895, -2.167483682527316713, -0.3223708474724209516 ) ) ;
#144989=CARTESIAN_POINT ( 'NONE',  ( 2.028227463090884974, 1.110962183858194452, -1.573585318204050676 ) ) ;
#144992=CARTESIAN_POINT ( 'NONE',  ( 0.1331565106231363538, 7.629137130509071163, -2.545925718843544239 ) ) ;
#145000=CARTESIAN_POINT ( 'NONE',  ( 4.493604616018744835, -1.840970053361364656, -0.04044509776383875543 ) ) ;
#145001=CARTESIAN_POINT ( 'NONE',  ( 1.559240971068908355, -1.699445492770943478, 1.078823074066703747 ) ) ;
#145002=CARTESIAN_POINT ( 'NONE',  ( 3.796502476701520301, -2.125173906124724343, 0.8757568767029444423 ) ) ;
#145003=CARTESIAN_POINT ( 'NONE',  ( -0.02900071798682749002, 0.2267074960015900975, -2.207170277039482986 ) ) ;
#145004=CARTESIAN_POINT ( 'NONE',  ( 2.606119654932341767, 1.860434991719280173, 0.05107381154999082046 ) ) ;
#145007=CARTESIAN_POINT ( 'NONE',  ( 5.467032840998240495, -1.503656711810175350, 1.181500457595338505 ) ) ;
#145010=CARTESIAN_POINT ( 'NONE',  ( 4.581631739359020017, -0.9839878911236143999, 1.844693108308750551 ) ) ;
#145011=CARTESIAN_POINT ( 'NONE',  ( 3.889402362484274622, 1.354500474538382626, 1.290456140434749654 ) ) ;
#145016=CARTESIAN_POINT ( 'NONE',  ( 5.549328304323321248, -1.363462989569711681, -1.056374310239334591 ) ) ;
#145018=CARTESIAN_POINT ( 'NONE',  ( 0.6856605700745866949, 1.416429869936095542, 1.000165270844357801 ) ) ;
#145022=CARTESIAN_POINT ( 'NONE',  ( 5.506739464099510428, 0.6230791789904217559, 2.079776831526482628 ) ) ;
#145023=CARTESIAN_POINT ( 'NONE',  ( 4.582524934692378871, -1.771534430979417429, -0.4408631061849078714 ) ) ;
#145024=CARTESIAN_POINT ( 'NONE',  ( 1.147228161472005681, 1.732707765124143817, -0.9198407203683529598 ) ) ;
#145025=CARTESIAN_POINT ( 'NONE',  ( 0.4216853220532343904, -1.500587716210170841, -1.493872543894637417 ) ) ;
#145029=CARTESIAN_POINT ( 'NONE',  ( 2.297662419472700002, 1.937625723843895864, -0.8618613456389671024 ) ) ;
#145034=CARTESIAN_POINT ( 'NONE',  ( 0.6376584384039893916, 1.932990051301992418, -0.7417924570976216492 ) ) ;
#145035=CARTESIAN_POINT ( 'NONE',  ( 6.983263157960362122, 2.430545403621493072, 2.435370848939223620 ) ) ;
#145037=CARTESIAN_POINT ( 'NONE',  ( 2.227449089350467482, 1.985603210742479252, 0.9958825451741261103 ) ) ;
#145039=CARTESIAN_POINT ( 'NONE',  ( 0.4933721672778153544, -2.286813510910344682, 0.2336738355162761571 ) ) ;
#145041=CARTESIAN_POINT ( 'NONE',  ( 5.348506707712929575, -2.046340616697607473, -0.2579891923277094490 ) ) ;
#145046=CARTESIAN_POINT ( 'NONE',  ( 0.1333542156527660338, 2.021264325465597977, -2.461897275464264290 ) ) ;
#145047=CARTESIAN_POINT ( 'NONE',  ( 5.935073298327618652, -1.338256116417003927, -1.264887592264056559 ) ) ;
#145051=CARTESIAN_POINT ( 'NONE',  ( 1.658790106635851469, -1.476843439067159425, -0.8906862264850596844 ) ) ;
#145052=CARTESIAN_POINT ( 'NONE',  ( 1.077361674225948418, 1.530160568918725872, 1.313541346884480987 ) ) ;
#145054=CARTESIAN_POINT ( 'NONE',  ( 2.232027051843707532, -1.476457111770380415, -1.714336117487671007 ) ) ;
#145055=CARTESIAN_POINT ( 'NONE',  ( 4.037795408393930252, -1.452196710024173276, -1.525570609991099502 ) ) ;
#145057=CARTESIAN_POINT ( 'NONE',  ( 2.688433849602299031, -0.2980574676569973658, -1.744271549386553932 ) ) ;
#145060=CARTESIAN_POINT ( 'NONE',  ( 6.515150198369638268, -2.224820657066893137, 0.5519656782505685255 ) ) ;
#145061=CARTESIAN_POINT ( 'NONE',  ( 4.224425198852012286, 0.09258891237720960621, 1.838934309869838968 ) ) ;
#145067=CARTESIAN_POINT ( 'NONE',  ( 4.664136352776428573, -1.432711980460563250, 1.658340198327029613 ) ) ;
#145072=CARTESIAN_POINT ( 'NONE',  ( 2.772000617051553206, 1.030904977978854609, 1.627292194166103600 ) ) ;
#145075=CARTESIAN_POINT ( 'NONE',  ( -0.1575499713504755483, -1.374138184231291415, -1.746309953600865716 ) ) ;
#145085=CARTESIAN_POINT ( 'NONE',  ( 2.612550116648149512, -0.1684838578246611873, 1.732238525843646570 ) ) ;
#145086=CARTESIAN_POINT ( 'NONE',  ( 0.5550359226569913096, 1.633180182981083028, -1.086726831054436682 ) ) ;
#145089=CARTESIAN_POINT ( 'NONE',  ( 6.245025451202089073, -1.828886558906620774, 1.152162773130911644 ) ) ;
#145092=CARTESIAN_POINT ( 'NONE',  ( 6.174726448494309849, -2.051094451480539149, -0.6828207641706719455 ) ) ;
#145093=CARTESIAN_POINT ( 'NONE',  ( -0.2104748580754408904, 1.337026610731705700, -2.356057411969681326 ) ) ;
#145096=CARTESIAN_POINT ( 'NONE',  ( 0.8076147168173102298, -1.862120749842037570, 0.1771838942275505424 ) ) ;
#145097=CARTESIAN_POINT ( 'NONE',  ( 6.098968314571592053, 0.8511620794300640558, -1.510462927660038090 ) ) ;
#145099=CARTESIAN_POINT ( 'NONE',  ( 2.859115728684503477, 0.3189004193784421015, -2.168101852914063876 ) ) ;
#145100=CARTESIAN_POINT ( 'NONE',  ( 3.417284581939382448, 2.085149140145211799, 0.9887805580795704374 ) ) ;
#145101=CARTESIAN_POINT ( 'NONE',  ( 6.468051757712944827, 1.055310785928347928, 1.769903775486596054 ) ) ;
#145102=CARTESIAN_POINT ( 'NONE',  ( 1.640467198872105348, -1.640604414344963180, 1.038759544029205895 ) ) ;
#145105=CARTESIAN_POINT ( 'NONE',  ( 4.043311264919998038, 0.1072909356813686182, 2.118029240109862155 ) ) ;
#145106=CARTESIAN_POINT ( 'NONE',  ( 2.162732623366144136, 1.242727809108796322, 1.587836805404294171 ) ) ;
#145108=CARTESIAN_POINT ( 'NONE',  ( 5.280388062626482970, -1.229865305990836877, 1.832093573602276759 ) ) ;
#145116=ORIENTED_EDGE ( 'NONE', *, *, #118204, .F. ) ;
#145117=CARTESIAN_POINT ( 'NONE',  ( 4.680574674004650326, -1.998471466470305602, -0.5028169189831372954 ) ) ;
#145122=CARTESIAN_POINT ( 'NONE',  ( 3.176430186773027575, 0.9099569689122315452, 1.803159259486881938 ) ) ;
#145127=CARTESIAN_POINT ( 'NONE',  ( 3.239188564323669528, -1.818332144261879613, 0.9699876223461401104 ) ) ;
#145128=CARTESIAN_POINT ( 'NONE',  ( 3.305314717767214638, 1.277042846462652204, -1.560500556308255460 ) ) ;
#145135=CARTESIAN_POINT ( 'NONE',  ( 3.374374892241317703, -0.3960410224921434574, 1.976653181598592601 ) ) ;
#145136=CARTESIAN_POINT ( 'NONE',  ( 0.9723034553027898319, -0.04304006056080753040, -1.840805954149108858 ) ) ;
#145137=CARTESIAN_POINT ( 'NONE',  ( 0.4171991508139940574, 1.586773611656131289, -1.675818712001175381 ) ) ;
#145139=CARTESIAN_POINT ( 'NONE',  ( 2.706508253401081809, -0.8245430293080566742, -1.998349536214229616 ) ) ;
#145141=CARTESIAN_POINT ( 'NONE',  ( 5.120359440597627376, 2.086519121862129289, 0.3590335527714014763 ) ) ;
#145142=CARTESIAN_POINT ( 'NONE',  ( 2.530986164375541581, 2.254368048762548593, -0.4469772407268405301 ) ) ;
#145144=CARTESIAN_POINT ( 'NONE',  ( 0.7779422811538607707, -1.042605501850740080, 1.552959968518424771 ) ) ;
#145145=CARTESIAN_POINT ( 'NONE',  ( 5.330923369760363961, 0.1444485787395009269, 1.966219458991929514 ) ) ;
#145149=CARTESIAN_POINT ( 'NONE',  ( 6.516252164726425100, -0.9909202252585481707, -1.858390699035996407 ) ) ;
#145150=CARTESIAN_POINT ( 'NONE',  ( 5.969205681473694902, 1.824102622056431811, 0.9793482939001868504 ) ) ;
#145153=CARTESIAN_POINT ( 'NONE',  ( 6.639320575229263888, 1.250520135805782251, 2.217830841512329787 ) ) ;
#145154=CARTESIAN_POINT ( 'NONE',  ( 5.278184311449350297, -1.095828550124495981, 1.638662057970756925 ) ) ;
#145155=CARTESIAN_POINT ( 'NONE',  ( 6.310808155552376952, -0.5427901682961560059, -1.945386456709609524 ) ) ;
#145157=CARTESIAN_POINT ( 'NONE',  ( 4.793776464392771608, 1.707650450486393190, 1.552408976560351483 ) ) ;
#145159=CARTESIAN_POINT ( 'NONE',  ( 2.272402725641348820, -0.9685827254542198617, -1.820965734949228310 ) ) ;
#145166=CARTESIAN_POINT ( 'NONE',  ( 4.633362100890871638, 0.004430012494727622249, -2.171350061612055349 ) ) ;
#145169=CARTESIAN_POINT ( 'NONE',  ( 3.649809678215182096, 0.6660801477775115664, 1.716721118343276453 ) ) ;
#145171=CARTESIAN_POINT ( 'NONE',  ( 6.620655732516651071, 1.309889148221474509, 1.844503626996786938 ) ) ;
#145172=CARTESIAN_POINT ( 'NONE',  ( 5.478137895480934105, -2.137967713159651506, -0.4810252310911074525 ) ) ;
#145174=CARTESIAN_POINT ( 'NONE',  ( 5.963815663052111304, 2.230244011310183794, -0.3799797021378086836 ) ) ;
#145181=CARTESIAN_POINT ( 'NONE',  ( 0.6898892245524823608, -1.755727311204742680, -0.2225690630779184609 ) ) ;
#145182=CARTESIAN_POINT ( 'NONE',  ( 5.567046518764520613, -1.585636444731153061, 1.240160563295252372 ) ) ;
#145184=CARTESIAN_POINT ( 'NONE',  ( 4.682709062318923365, -2.042047207266047604, -0.5143438382350475901 ) ) ;
#145185=CARTESIAN_POINT ( 'NONE',  ( 1.968237613432867184, -1.879027187823999245, -0.3716057669084034676 ) ) ;
#145187=CARTESIAN_POINT ( 'NONE',  ( 2.646873730718673379, -0.3338169989568114948, -1.940879108454116375 ) ) ;
#145188=CARTESIAN_POINT ( 'NONE',  ( 5.730724961554885866, 1.353511160402442570, -1.499384403026276180 ) ) ;
#145189=CARTESIAN_POINT ( 'NONE',  ( 1.692057038649401601, -1.861345348035767344, -0.1864469194169729449 ) ) ;
#145190=CARTESIAN_POINT ( 'NONE',  ( 2.330453122711079850, -1.209328770571056921, 1.544706564130463811 ) ) ;
#145191=CARTESIAN_POINT ( 'NONE',  ( 4.846200500028392533, 1.720618765505038006, 0.1221847348328516936 ) ) ;
#145192=CARTESIAN_POINT ( 'NONE',  ( 1.107505169401588274, 1.450017293480215352, 1.247013401884336403 ) ) ;
#145194=CARTESIAN_POINT ( 'NONE',  ( 1.084930333755677045, -2.153824616689365978, -0.4803136671489223741 ) ) ;
#145202=CARTESIAN_POINT ( 'NONE',  ( 6.895378825052528526, -1.852007112603266670, 0.9253362530580526712 ) ) ;
#145203=CARTESIAN_POINT ( 'NONE',  ( 1.152881054890652957, -0.5012615762394446728, -2.008655542368184221 ) ) ;
#145208=CARTESIAN_POINT ( 'NONE',  ( 5.303433364654348559, 1.869980213031800398, -0.9998494819224086338 ) ) ;
#145212=CARTESIAN_POINT ( 'NONE',  ( 6.566857081534598350, 1.454584517406570132, -1.316677807353151097 ) ) ;
#145214=CARTESIAN_POINT ( 'NONE',  ( 4.604842190751081255, 0.8645911521153251122, -1.821463593394745395 ) ) ;
#145215=CARTESIAN_POINT ( 'NONE',  ( 4.118306542938309889, 1.879866726353071060, 0.3679503660072875881 ) ) ;
#145217=CARTESIAN_POINT ( 'NONE',  ( 1.804482060849887270, 1.621174160030929068, -1.474864209862189579 ) ) ;
#145220=CARTESIAN_POINT ( 'NONE',  ( 4.834244255588106221, -1.080646305101562232, -1.698427166264226518 ) ) ;
#145223=CARTESIAN_POINT ( 'NONE',  ( 6.046512527486515687, -1.496967179435993778, 1.497493072882298382 ) ) ;
#145225=CARTESIAN_POINT ( 'NONE',  ( 4.001575260567552306, -2.085028717228009310, 0.1556281442064103848 ) ) ;
#145227=CARTESIAN_POINT ( 'NONE',  ( 2.098289149679245735, -0.4564329974444079618, -1.663208130003128948 ) ) ;
#145229=CARTESIAN_POINT ( 'NONE',  ( 5.730757696090862829, 1.422813033107739988, -1.572628729999878905 ) ) ;
#145238=CARTESIAN_POINT ( 'NONE',  ( 1.400706157114139261, -0.2655193030335687987, -1.791778796870816759 ) ) ;
#145244=CARTESIAN_POINT ( 'NONE',  ( 3.053145041208281452, -1.596494782498259157, 0.8559496646718143253 ) ) ;
#145245=CARTESIAN_POINT ( 'NONE',  ( 6.539320575229256249, 2.979067782826943844, 2.350490835693248126 ) ) ;
#145250=CARTESIAN_POINT ( 'NONE',  ( 3.472968545230222581, 1.681562272349636622, 0.7977436208898255332 ) ) ;
#145251=CARTESIAN_POINT ( 'NONE',  ( 2.108866759644252298, 0.002224897612410503371, 1.915793139840407333 ) ) ;
#145252=CARTESIAN_POINT ( 'NONE',  ( 0.2526013166088726392, -1.469656019175567208, 1.082793315970068004 ) ) ;
#145259=CARTESIAN_POINT ( 'NONE',  ( 5.102387438446081447, 1.963913563476852309, 0.1487572088093111478 ) ) ;
#145261=CARTESIAN_POINT ( 'NONE',  ( 0.7442207691023922100, 0.6088243375477386810, 2.000016368695969327 ) ) ;
#145263=CARTESIAN_POINT ( 'NONE',  ( 5.666998703487860389, -1.741597003894586937, -0.8236021136211798543 ) ) ;
#145265=CARTESIAN_POINT ( 'NONE',  ( 0.7447965706881399806, -1.568309060004613231, 0.9341869532639992535 ) ) ;
#145266=CARTESIAN_POINT ( 'NONE',  ( 2.034064749695370100, -1.442962035976073309, -1.669870808145665020 ) ) ;
#145269=CARTESIAN_POINT ( 'NONE',  ( -0.05268457437105152075, -1.747710896673961622, 0.7768168958157274373 ) ) ;
#145272=CARTESIAN_POINT ( 'NONE',  ( 0.3089591345776849241, -1.584006439100977603, 1.170298647042963935 ) ) ;
#145273=CARTESIAN_POINT ( 'NONE',  ( 1.347104335016526599, 0.5619601930287048130, -1.858996895088180556 ) ) ;
#145275=CARTESIAN_POINT ( 'NONE',  ( 0.2806244687772480040, -1.977743564115455932, 0.3905345501400147024 ) ) ;
#145277=CARTESIAN_POINT ( 'NONE',  ( 4.996841193152741667, 0.3155067605547862142, 1.833815385591957448 ) ) ;
#145283=CARTESIAN_POINT ( 'NONE',  ( 1.400213348495438437, -0.7931047570679079506, -2.043190674350242819 ) ) ;
#145288=CARTESIAN_POINT ( 'NONE',  ( 2.156629195875509719, -1.411784796728832392, 1.157573153174975111 ) ) ;
#145293=CARTESIAN_POINT ( 'NONE',  ( 6.609000000000034625, 7.052688111495289291, 2.598153854230552895 ) ) ;
#145295=CARTESIAN_POINT ( 'NONE',  ( 1.277817996239123177, 1.146848889641904234, 1.547804080865310850 ) ) ;
#145296=CARTESIAN_POINT ( 'NONE',  ( 6.016451032921247055, 0.7918200671565789328, 1.795022358689959185 ) ) ;
#145299=CARTESIAN_POINT ( 'NONE',  ( 5.425378541715013547, -1.389685604419872655, -1.694579525865948844 ) ) ;
#145301=CARTESIAN_POINT ( 'NONE',  ( 3.784089331405198209, -1.229265877060268242, -1.665672133652921660 ) ) ;
#145306=CARTESIAN_POINT ( 'NONE',  ( 4.043764476089898530, -1.703284420474758143, 1.543771250003633355 ) ) ;
#145315=CARTESIAN_POINT ( 'NONE',  ( 3.890518024738118807, 1.639914603359222456, -1.039847546996591765 ) ) ;
#145319=CARTESIAN_POINT ( 'NONE',  ( 5.220932206144772714, 1.444093599275039885, -1.253800916539760113 ) ) ;
#145321=CARTESIAN_POINT ( 'NONE',  ( 6.545920775329808983, 0.6544052999908689383, -1.596017746584824426 ) ) ;
#145322=CARTESIAN_POINT ( 'NONE',  ( 4.874232570624013050, -2.001857581374043349, -0.2420344392276354561 ) ) ;
#145324=CARTESIAN_POINT ( 'NONE',  ( 1.911028901235469313, 1.633884665098099598, -1.483674895440662667 ) ) ;
#145327=CARTESIAN_POINT ( 'NONE',  ( 1.904351452098542063, 1.548259960728815665, -1.405051437006714643 ) ) ;
#145328=CARTESIAN_POINT ( 'NONE',  ( 0.3207183204587023551, -0.09351970983179427876, 1.767511165302604326 ) ) ;
#145329=CARTESIAN_POINT ( 'NONE',  ( 5.906875006520014182, -1.122496024291631755, -1.674889250513518446 ) ) ;
#145331=CARTESIAN_POINT ( 'NONE',  ( 2.976851957573245944, -0.1693691376928093406, -2.286062073229557345 ) ) ;
#145332=CARTESIAN_POINT ( 'NONE',  ( 0.6205767395346533100, -1.653899685646512019, 0.5418069113267124370 ) ) ;
#145335=CARTESIAN_POINT ( 'NONE',  ( 0.7899210882133401723, -1.648783996043493350, 0.5366646198887611297 ) ) ;
#145338=CARTESIAN_POINT ( 'NONE',  ( 1.592468369012179918, 1.070935286220242366, -1.888628467986789738 ) ) ;
#145339=CARTESIAN_POINT ( 'NONE',  ( 2.800017839408690090, -0.9981255096969069429, -1.752139039461996006 ) ) ;
#145340=CARTESIAN_POINT ( 'NONE',  ( 3.718750000000002220, -0.7852924748297895885, 1.895863743164163617 ) ) ;
#145342=CARTESIAN_POINT ( 'NONE',  ( 6.094356125077982078, -1.917462007409322267, -0.1864201481798656301 ) ) ;
#145344=CARTESIAN_POINT ( 'NONE',  ( 3.973042321754824524, -1.644474126697339944, 1.493583396047935219 ) ) ;
#145351=CARTESIAN_POINT ( 'NONE',  ( 5.811982450300033243, 1.162468279597946630, -1.295502344845029574 ) ) ;
#145353=CARTESIAN_POINT ( 'NONE',  ( 3.666413850373055450, -0.7928392042928497085, -1.794698522912529182 ) ) ;
#145358=CARTESIAN_POINT ( 'NONE',  ( 4.130342294306089457, 1.214786636354926452, -1.908452007788311366 ) ) ;
#145359=CARTESIAN_POINT ( 'NONE',  ( 2.154800422482431532, -0.5477745769525663722, -1.988566864369076592 ) ) ;
#145362=CARTESIAN_POINT ( 'NONE',  ( 2.448426410784361185, 2.261989705503023806, 0.05584468559862928311 ) ) ;
#145365=CARTESIAN_POINT ( 'NONE',  ( 4.006994748872731549, 1.602975652146242380, 0.9638501484771769823 ) ) ;
#145366=CARTESIAN_POINT ( 'NONE',  ( 2.812812116114179251, 0.9611239539163253243, -1.443176275507858319 ) ) ;
#145367=CARTESIAN_POINT ( 'NONE',  ( 6.198795224570643470, 1.821041368708445907, 1.219022265761634971 ) ) ;
#145368=CARTESIAN_POINT ( 'NONE',  ( 0.2357703454196959370, -2.016519153289020760, 0.8967723332334791575 ) ) ;
#145369=CARTESIAN_POINT ( 'NONE',  ( 4.522454563201145028, 1.332364063043836033, -1.702191164408660251 ) ) ;
#145370=CARTESIAN_POINT ( 'NONE',  ( 4.804598357785225815, 1.690330731384475094, 0.9558792251623483560 ) ) ;
#145378=CARTESIAN_POINT ( 'NONE',  ( 6.170546107226446253, 1.392543322632183722, 1.458558933167881211 ) ) ;
#145382=CARTESIAN_POINT ( 'NONE',  ( 2.754317325142870754, 0.6151756178996542479, 1.719052816137212503 ) ) ;
#145388=CARTESIAN_POINT ( 'NONE',  ( 1.125267019654611733, 1.783345095244772249, 0.9482059100444378830 ) ) ;
#145389=CARTESIAN_POINT ( 'NONE',  ( 0.8738735914427527840, 0.4098651554323496926, -2.080331290949386513 ) ) ;
#145392=CARTESIAN_POINT ( 'NONE',  ( 2.008444763995967275, 0.5780311502073384178, 1.769000597778628947 ) ) ;
#145394=CARTESIAN_POINT ( 'NONE',  ( 6.631718597260928050, -1.344210725561691300, -1.562263648894322898 ) ) ;
#145395=CARTESIAN_POINT ( 'NONE',  ( 6.135388727473008785, 0.6351960432287793168, 1.913804721665197883 ) ) ;
#145399=CARTESIAN_POINT ( 'NONE',  ( 3.615676881913011176, -1.798418494116042821, 0.3134422064149794407 ) ) ;
#145403=CARTESIAN_POINT ( 'NONE',  ( 5.852888695852590750, -0.9090035733541059759, 1.799648235488074732 ) ) ;
#145404=CARTESIAN_POINT ( 'NONE',  ( 5.296754776809613041, 1.507285696749562476, 1.057021923447129197 ) ) ;
#145405=CARTESIAN_POINT ( 'NONE',  ( 0.07680821025393863577, 5.725641208404781857, -2.404836704152548688 ) ) ;
#145406=CARTESIAN_POINT ( 'NONE',  ( 3.440313875665978127, 1.038139129215289946, -2.061066213440334582 ) ) ;
#145408=CARTESIAN_POINT ( 'NONE',  ( 6.345025448074324892, -1.829860219143174982, 1.150409744987097804 ) ) ;
#145410=CARTESIAN_POINT ( 'NONE',  ( 1.593202639421680278, -0.6524502387153191529, 1.829324111618094717 ) ) ;
#145412=CARTESIAN_POINT ( 'NONE',  ( 4.464446571738351466, 1.842799458866357210, 1.373389552433499139 ) ) ;
#145415=CARTESIAN_POINT ( 'NONE',  ( 4.592568387165754551, -0.4099775813008778025, -1.825014511474598589 ) ) ;
#145417=CARTESIAN_POINT ( 'NONE',  ( 2.777492966359981441, 0.2764497561681695803, -1.892163382976944419 ) ) ;
#145420=CARTESIAN_POINT ( 'NONE',  ( 4.055453297694236348, -1.834216022232620702, -1.226887332174103173 ) ) ;
#145421=CARTESIAN_POINT ( 'NONE',  ( 6.883263157960364254, 6.036844454314826081, 2.541088405340941492 ) ) ;
#145426=CARTESIAN_POINT ( 'NONE',  ( 1.792193567899300177, -1.961476155570774926, -0.1973719964898524026 ) ) ;
#145427=CARTESIAN_POINT ( 'NONE',  ( 1.536587678696316184, 1.135727589777148605, -2.008695742776007709 ) ) ;
#145428=CARTESIAN_POINT ( 'NONE',  ( 2.137090596337941406, -0.09316805448006218460, -1.959763546484971197 ) ) ;
#145430=CARTESIAN_POINT ( 'NONE',  ( 5.858276910504900847, -2.062741130177087268, -0.005609060510954055022 ) ) ;
#145437=CARTESIAN_POINT ( 'NONE',  ( 0.5499837882529658994, 1.607816289776839991, 1.459057700483844311 ) ) ;
#145441=CARTESIAN_POINT ( 'NONE',  ( 2.161206213664386144, 0.3243885794495802721, -1.842051381961368639 ) ) ;
#145442=CARTESIAN_POINT ( 'NONE',  ( 6.608665842073913943, 1.606649649811153990, -1.446306907624186344 ) ) ;
#145444=CARTESIAN_POINT ( 'NONE',  ( -0.02244404828157658613, 0.6916080914694566761, -2.270927585766496559 ) ) ;
#145445=CARTESIAN_POINT ( 'NONE',  ( 6.727182134110202050, 7.629137130509070275, 2.410944104600750038 ) ) ;
#145447=CARTESIAN_POINT ( 'NONE',  ( 2.350135150926917493, 0.8998847150011924922, -1.687291145760522859 ) ) ;
#145449=CARTESIAN_POINT ( 'NONE',  ( 3.783871084116468886, -0.8724064270978303393, 1.539809854060821603 ) ) ;
#145450=CARTESIAN_POINT ( 'NONE',  ( 2.174333686202088334, 0.8191313854410250395, 1.728107290330855639 ) ) ;
#145453=CARTESIAN_POINT ( 'NONE',  ( 5.343340938886254499, 0.3690371538600076273, -1.879538113519742204 ) ) ;
#145454=CARTESIAN_POINT ( 'NONE',  ( 6.637161372131059167, -0.09511470475139816028, -1.967365288627285214 ) ) ;
#145456=CARTESIAN_POINT ( 'NONE',  ( 2.373420902723611725, -1.847293605357634982, -1.041186957106011723 ) ) ;
#145459=CARTESIAN_POINT ( 'NONE',  ( 4.768341783539651324, -1.221614081569386334, 1.416756073533788518 ) ) ;
#145460=CARTESIAN_POINT ( 'NONE',  ( 2.174178736149934732, -1.123764393468742684, 1.438770255985911684 ) ) ;
#145462=CARTESIAN_POINT ( 'NONE',  ( 4.143358556170802842, -1.920740624720223666, 1.086653567583625746 ) ) ;
#145465=CARTESIAN_POINT ( 'NONE',  ( 1.381380011782725958, -0.05272402391268657396, 2.062171479924046036 ) ) ;
#145474=CARTESIAN_POINT ( 'NONE',  ( 3.877443546529443452, -0.1552652338182025915, 2.064615508632794860 ) ) ;
#145476=CARTESIAN_POINT ( 'NONE',  ( 2.108864864398530159, 1.603267699958549342, -1.450045708023157687 ) ) ;
#145478=CARTESIAN_POINT ( 'NONE',  ( 3.194014839594649491, 1.283080201803546538, 1.559715919771433867 ) ) ;
#145479=CARTESIAN_POINT ( 'NONE',  ( 6.620655732516679493, 3.689697857139722981, 2.587825964709880910 ) ) ;
#145484=CARTESIAN_POINT ( 'NONE',  ( 1.481658059775035952, -0.6748446255696785023, 1.900416712880992343 ) ) ;
#145485=CARTESIAN_POINT ( 'NONE',  ( 6.339412547452306868, 0.8406370108028878851, -2.024118718474729128 ) ) ;
#145488=CARTESIAN_POINT ( 'NONE',  ( 4.939673314881130040, -1.814047719456039154, 0.6055163330952323397 ) ) ;
#145492=CARTESIAN_POINT ( 'NONE',  ( 2.460564738353550496, -1.930424690641812768, -0.5826366834433827080 ) ) ;
#145495=CARTESIAN_POINT ( 'NONE',  ( 5.385687109042746279, 1.161108558237003985, 1.275598767315838211 ) ) ;
#145496=CARTESIAN_POINT ( 'NONE',  ( -0.1394461523060988861, 1.283499747810852520, -2.524650647122913316 ) ) ;
#145501=CARTESIAN_POINT ( 'NONE',  ( 0.9540663221972445207, -0.7486024665571254788, 1.930331157511067097 ) ) ;
#145503=CARTESIAN_POINT ( 'NONE',  ( 4.635318128526639825, -0.08385371298775616544, 1.809651570580686819 ) ) ;
#145506=CARTESIAN_POINT ( 'NONE',  ( 6.340474544234134591, 1.036764729950395258, -1.485249760763515114 ) ) ;
#145509=CARTESIAN_POINT ( 'NONE',  ( 3.433693710695666201, 0.9853049363134911420, -1.957518807868402044 ) ) ;
#145511=CARTESIAN_POINT ( 'NONE',  ( 0.1683002474503410839, -0.8351952195557797998, -1.773497582445908938 ) ) ;
#145513=CARTESIAN_POINT ( 'NONE',  ( 4.394081885627950435, -0.8225995951327015332, -1.730150695830068308 ) ) ;
#145519=CARTESIAN_POINT ( 'NONE',  ( 1.499129196564862987, 1.767075381950654611, -1.244890797856931686 ) ) ;
#145522=CARTESIAN_POINT ( 'NONE',  ( 2.485134345765506847, 1.670108983700506977, -0.7376146046164517855 ) ) ;
#145524=CARTESIAN_POINT ( 'NONE',  ( 4.330939430599492823, 0.08983702179986637060, 1.823481399301420947 ) ) ;
#145527=CARTESIAN_POINT ( 'NONE',  ( 2.724755696555291262, 1.382288352666941389, -1.321784923088549446 ) ) ;
#145529=CARTESIAN_POINT ( 'NONE',  ( 3.596117507753269660, 0.8876951776618343670, -1.758253228584506944 ) ) ;
#145531=CARTESIAN_POINT ( 'NONE',  ( 6.181195893160847277, 1.342424930544680928, 1.403604608442722057 ) ) ;
#145535=CARTESIAN_POINT ( 'NONE',  ( 5.554972086574996304, 0.4156608669513594534, 2.079290889414136423 ) ) ;
#145537=CARTESIAN_POINT ( 'NONE',  ( 2.895058368816882499, -0.1428820475998151818, -1.907012587803847303 ) ) ;
#145540=ORIENTED_EDGE ( 'NONE', *, *, #159892, .T. ) ;
#145543=CARTESIAN_POINT ( 'NONE',  ( 5.197907085625908863, 1.353584514550598472, 1.490229472901122065 ) ) ;
#145545=CARTESIAN_POINT ( 'NONE',  ( 6.340460056601358474, 1.806591233369018834, 0.2625940548972791611 ) ) ;
#145546=CARTESIAN_POINT ( 'NONE',  ( 1.170471352854907776, -0.9292243337341490328, -1.850172451097586990 ) ) ;
#145559=CARTESIAN_POINT ( 'NONE',  ( 1.815371668717490339, -1.773540675419151169, -1.067758146248848128 ) ) ;
#145560=CARTESIAN_POINT ( 'NONE',  ( 2.741944773236061117, 2.106750310803459758, -0.2105854985169057503 ) ) ;
#145563=CARTESIAN_POINT ( 'NONE',  ( 1.059349595761612584, 1.606854154984382443, 1.138435182648824373 ) ) ;
#145568=CARTESIAN_POINT ( 'NONE',  ( 2.642860430951101680, -1.905069302404806875, 1.274549645703947132 ) ) ;
#145569=CARTESIAN_POINT ( 'NONE',  ( 0.3283667639546791195, 1.746078182827022429, 0.5332771064449209897 ) ) ;
#145571=CARTESIAN_POINT ( 'NONE',  ( 2.144650067465687648, 1.855875215511919363, 0.4610605321611755958 ) ) ;
#145574=CARTESIAN_POINT ( 'NONE',  ( 1.283448800676566970, 0.1440664973490720091, -2.008080635846798856 ) ) ;
#145575=CARTESIAN_POINT ( 'NONE',  ( 2.377722661024490147, -1.904092233959910896, 0.4717398701708991893 ) ) ;
#145580=CARTESIAN_POINT ( 'NONE',  ( 4.664062431145298504, -1.365975323770602268, 1.582769587995744853 ) ) ;
#145581=CARTESIAN_POINT ( 'NONE',  ( 3.660817930519409291, -1.560716028760079421, -0.8345783561882027524 ) ) ;
#145584=CARTESIAN_POINT ( 'NONE',  ( 6.439416457043729558, 0.8834936782941483768, -2.115358923741214259 ) ) ;
#145585=CARTESIAN_POINT ( 'NONE',  ( 4.611116368171574109, -1.705915267380184286, 0.3434222965797654181 ) ) ;
#145588=CARTESIAN_POINT ( 'NONE',  ( 4.024493581903946016, 1.720846971656955438, -0.2109413284564972679 ) ) ;
#145590=CARTESIAN_POINT ( 'NONE',  ( 4.141221389272289777, -0.2091070545618961274, -2.161069556037761519 ) ) ;
#145592=CARTESIAN_POINT ( 'NONE',  ( 5.928922775424462444, -1.700964743930567513, 1.082835439959836776 ) ) ;
#145593=CARTESIAN_POINT ( 'NONE',  ( 5.968750000000003553, 0.7852924748296689073, -1.895863743164208026 ) ) ;
#145595=CARTESIAN_POINT ( 'NONE',  ( 3.135679483595578798, -1.292546426170533058, -1.428565414989799054 ) ) ;
#145597=CARTESIAN_POINT ( 'NONE',  ( 0.5576789645300848086, -1.902086909048054331, 1.147088156025797057 ) ) ;
#145599=CARTESIAN_POINT ( 'NONE',  ( 6.883263157960418432, 2.078485899884211285, 2.154856264959764012 ) ) ;
#145603=CARTESIAN_POINT ( 'NONE',  ( 1.823182589357236205, 1.643363032943769397, -1.494666050352111863 ) ) ;
#145610=CARTESIAN_POINT ( 'NONE',  ( 5.143062936040889710, -0.2492579690161021710, -2.047486851065055458 ) ) ;
#145615=CARTESIAN_POINT ( 'NONE',  ( 6.819622122755134797, -1.814287395386984691, 0.4549875680220638596 ) ) ;
#145616=CARTESIAN_POINT ( 'NONE',  ( 5.625553438129872852, 0.3468616029342861951, 1.698903693450015684 ) ) ;
#145617=CARTESIAN_POINT ( 'NONE',  ( 5.583501753226309816, -0.7750115735715494836, 1.558442325393385897 ) ) ;
#145619=CARTESIAN_POINT ( 'NONE',  ( 3.070184882724129594, -1.363667385223182871, 1.842535374393680980 ) ) ;
#145622=CARTESIAN_POINT ( 'NONE',  ( 1.218424693763892730, -0.04700249260505655335, 1.840701667592301138 ) ) ;
#145625=CARTESIAN_POINT ( 'NONE',  ( 2.432394421669949569, 1.770131964307398498, 0.4459858026567494194 ) ) ;
#145626=CARTESIAN_POINT ( 'NONE',  ( 1.605704095283020605, -2.174604996184846595, 0.2706701637196773369 ) ) ;
#145628=CARTESIAN_POINT ( 'NONE',  ( 4.278421442896533478, -1.214510211351152336, 1.720268157014235078 ) ) ;
#145632=CARTESIAN_POINT ( 'NONE',  ( 1.029834584532058672, 1.995790600324919506, -0.5504719462680053299 ) ) ;
#145635=CARTESIAN_POINT ( 'NONE',  ( 4.055424778641623540, -1.844328037693225397, 1.046277804987456372 ) ) ;
#145637=CARTESIAN_POINT ( 'NONE',  ( 6.129513044595952032, -1.717388127611047421, 0.6198453807191862674 ) ) ;
#145644=CARTESIAN_POINT ( 'NONE',  ( 6.539320575229233157, 0.001224430076711413356, 2.103502572931112091 ) ) ;
#145645=CARTESIAN_POINT ( 'NONE',  ( 1.325372091284286569, -0.05194335737490791277, 2.105495032795675847 ) ) ;
#145648=CARTESIAN_POINT ( 'NONE',  ( 5.365987026107917224, -1.852166562183876986, 0.1801111341232768115 ) ) ;
#145654=CARTESIAN_POINT ( 'NONE',  ( 2.066782613880484565, 1.455849762852476248, -1.315278764014264912 ) ) ;
#145655=CARTESIAN_POINT ( 'NONE',  ( 0.5851287433712646369, -0.2658872486876809327, -2.145209338178376335 ) ) ;
#145659=CARTESIAN_POINT ( 'NONE',  ( 3.145509197426650694, -0.1243275703598344523, -1.729419848027229367 ) ) ;
#145660=CARTESIAN_POINT ( 'NONE',  ( 2.501564275351343181, -0.6656319730054968131, -1.608207657179961947 ) ) ;
#145663=CARTESIAN_POINT ( 'NONE',  ( 2.249358885376837591, -1.653154358101496246, -1.230164295365917537 ) ) ;
#145664=CARTESIAN_POINT ( 'NONE',  ( 0.7024996975148189993, -1.423740904080775138, -1.427721366232127753 ) ) ;
#145665=CARTESIAN_POINT ( 'NONE',  ( 6.925078400183553029, 2.042159606913606762, 2.349846261904017464 ) ) ;
#145668=CARTESIAN_POINT ( 'NONE',  ( 1.006637970050362929, 1.494420418981519338, -1.285951363188575058 ) ) ;
#145669=CARTESIAN_POINT ( 'NONE',  ( 6.152599605923961157, 1.892562589925715466, 0.2737767527046449101 ) ) ;
#145674=CARTESIAN_POINT ( 'NONE',  ( 0.7154971248738207779, 1.652399868344236245, 1.161036454668294304 ) ) ;
#145676=CARTESIAN_POINT ( 'NONE',  ( 4.278580467222413475, -1.332036844872594994, 1.884138376372360479 ) ) ;
#145677=CARTESIAN_POINT ( 'NONE',  ( 5.564887814092526419, 1.486691789297951871, -1.280227714881218892 ) ) ;
#145678=CARTESIAN_POINT ( 'NONE',  ( 1.832786370036399326, -1.861117592713131819, -0.6203919267877275878 ) ) ;
#145680=CARTESIAN_POINT ( 'NONE',  ( -0.06968618116158857567, -1.560424145883563929, -1.276814929289785239 ) ) ;
#145681=ORIENTED_EDGE ( 'NONE', *, *, #7153, .T. ) ;
#145682=CARTESIAN_POINT ( 'NONE',  ( 1.552129107922173068, 1.093532845977844170, 1.812997832068358850 ) ) ;
#145685=CARTESIAN_POINT ( 'NONE',  ( 1.218424693763892730, -0.04700249260505655335, 1.840701667592301138 ) ) ;
#145687=CARTESIAN_POINT ( 'NONE',  ( 4.012681996134721096, 0.7761599038508348869, 2.027777647250021076 ) ) ;
#145689=CARTESIAN_POINT ( 'NONE',  ( 2.232824136269210502, 1.381628265877183903, -1.608862310199298928 ) ) ;
#145693=CARTESIAN_POINT ( 'NONE',  ( 3.145831276397454079, 0.7450406991881215468, -1.921561753228885783 ) ) ;
#145696=CARTESIAN_POINT ( 'NONE',  ( 0.6086344939593493208, -0.2706599535906920040, 1.821105742621460744 ) ) ;
#145699=CARTESIAN_POINT ( 'NONE',  ( 0.1533209562146371774, -1.769702838771534559, 1.318327933512997152 ) ) ;
#145700=CARTESIAN_POINT ( 'NONE',  ( 2.601149388587006950, 1.818552668380982951, -1.345706882341807242 ) ) ;
#145702=CARTESIAN_POINT ( 'NONE',  ( 2.654344044762357413, 1.798353594787518217, 0.2176890031466270636 ) ) ;
#145704=CARTESIAN_POINT ( 'NONE',  ( 2.448326871961825191, -1.317826014703428639, 1.390694818219958107 ) ) ;
#145705=CARTESIAN_POINT ( 'NONE',  ( 3.402844027952243167, 0.5003511028610057032, 2.008882729757965890 ) ) ;
#145708=CARTESIAN_POINT ( 'NONE',  ( 2.008605748815388559, 1.462198227207864853, -1.322556311574287768 ) ) ;
#145709=CARTESIAN_POINT ( 'NONE',  ( 6.111935756226617222, -1.911612718183410387, 0.2385651428990897549 ) ) ;
#145710=CARTESIAN_POINT ( 'NONE',  ( 3.186256133050053840, -1.842714570631575510, -0.3211874441736498054 ) ) ;
#145711=CARTESIAN_POINT ( 'NONE',  ( 1.348709242277994269, 2.305235852375675076, 0.1091458774659745806 ) ) ;
#145713=CARTESIAN_POINT ( 'NONE',  ( 2.699463648093935575, -1.376791127151571592, -1.252357159445316670 ) ) ;
#145715=CARTESIAN_POINT ( 'NONE',  ( 5.371554553765571782, -0.3061699256626281840, 2.039728424269163121 ) ) ;
#145719=CARTESIAN_POINT ( 'NONE',  ( 5.842829903504588529, 0.4074447676574670107, 2.065989314711280667 ) ) ;
#145721=CARTESIAN_POINT ( 'NONE',  ( 5.554052124568396920, 2.159397089200214559, -0.09991998142631912383 ) ) ;
#145722=CARTESIAN_POINT ( 'NONE',  ( 6.287761640583830136, 1.932026593981367002, -0.5884565063561957299 ) ) ;
#145729=CARTESIAN_POINT ( 'NONE',  ( 4.645720405014278853, 1.993893748393640086, -0.3006458143828410479 ) ) ;
#145734=CARTESIAN_POINT ( 'NONE',  ( 5.647404790089923132, -1.701416311724871067, -1.333359258283283166 ) ) ;
#145739=CARTESIAN_POINT ( 'NONE',  ( 5.642203898613793456, 0.8197873783117490820, 1.842442240159094080 ) ) ;
#145741=CARTESIAN_POINT ( 'NONE',  ( 1.365380774817010368, 1.699871498885496379, -0.2916373863959387802 ) ) ;
#145746=CARTESIAN_POINT ( 'NONE',  ( 6.837182164354378422, -1.670574593475544489, 0.8415915117672703172 ) ) ;
#145747=CARTESIAN_POINT ( 'NONE',  ( 1.348292448571129842, 0.9904378492491233699, -1.752504823097464692 ) ) ;
#145749=CARTESIAN_POINT ( 'NONE',  ( 2.995379075007987613, 1.893430763284314811, -1.133229021217339483 ) ) ;
#145750=CARTESIAN_POINT ( 'NONE',  ( 5.172805277531332457, 1.502137693623846193, -1.567733665727601089 ) ) ;
#145755=CARTESIAN_POINT ( 'NONE',  ( 3.510498622083501719, -2.118129049236017192, -0.1023006277712720374 ) ) ;
#145756=CARTESIAN_POINT ( 'NONE',  ( 1.862907868837269998, -0.1017702599966328891, -2.013986063733465226 ) ) ;
#145757=CARTESIAN_POINT ( 'NONE',  ( 2.460951123861610412, -1.504080979915609628, 1.009397298678058164 ) ) ;
#145762=CARTESIAN_POINT ( 'NONE',  ( 1.165091096179095675, 1.768693976065521589, -0.7364918582971339278 ) ) ;
#145770=CARTESIAN_POINT ( 'NONE',  ( 5.067319851952804655, 0.2155487944876262052, -2.150937003660175151 ) ) ;
#145773=CARTESIAN_POINT ( 'NONE',  ( 2.742561299210785286, 1.174483946500170184, -1.765453564165630596 ) ) ;
#145776=CARTESIAN_POINT ( 'NONE',  ( 2.934795777137487516, 0.2378783870938088740, 1.956871125110821952 ) ) ;
#145778=CARTESIAN_POINT ( 'NONE',  ( 0.9243811426856913815, 1.018911950503737174, 1.802186752163869699 ) ) ;
#145779=CARTESIAN_POINT ( 'NONE',  ( 2.536971540620248433, -1.439279119694805820, -1.303886525222669901 ) ) ;
#145784=CARTESIAN_POINT ( 'NONE',  ( 2.853556533831374420, 2.080516846217596250, -0.2054353837145187767 ) ) ;
#145787=CARTESIAN_POINT ( 'NONE',  ( 6.516268831907007453, -1.911747763583053317, 0.05203757306279645223 ) ) ;
#145789=CARTESIAN_POINT ( 'NONE',  ( 3.879664727460280904, 2.078262106501146622, -0.7427522710690689367 ) ) ;
#145790=CARTESIAN_POINT ( 'NONE',  ( 2.942613154609276194, 2.189964478704994555, 0.2713889102748042736 ) ) ;
#145792=CARTESIAN_POINT ( 'NONE',  ( 2.279812546382542493, 1.875032136476075584, -0.3747091278499328770 ) ) ;
#145794=CARTESIAN_POINT ( 'NONE',  ( 4.562978833902987752, 1.602482145440896399, -1.310924660355553106 ) ) ;
#145796=CARTESIAN_POINT ( 'NONE',  ( 2.659225025413253007, -1.880336703546074073, -1.066323988048665017 ) ) ;
#145797=CARTESIAN_POINT ( 'NONE',  ( 4.634432875810733599, 0.3748786239917039631, 2.159109584303263940 ) ) ;
#145803=CARTESIAN_POINT ( 'NONE',  ( 0.07093568767341934533, -0.9480374005119349690, 1.779628194860154222 ) ) ;
#145806=CARTESIAN_POINT ( 'NONE',  ( 4.786024367859083029, -1.269482053145968514, -1.635305934682528717 ) ) ;
#145807=CARTESIAN_POINT ( 'NONE',  ( 2.772000617051553206, 1.030904977978854609, 1.627292194166103600 ) ) ;
#145808=CARTESIAN_POINT ( 'NONE',  ( 5.905892042933183816, -1.176582040423958642, -1.760015123184681007 ) ) ;
#145811=CARTESIAN_POINT ( 'NONE',  ( 4.188306824812327633, 1.057184280071225890, -1.661461291525099693 ) ) ;
#145812=CARTESIAN_POINT ( 'NONE',  ( 6.386719491623852996, 1.997645938776301477, -1.124140632904375936 ) ) ;
#145813=CARTESIAN_POINT ( 'NONE',  ( 3.615676881913011176, -1.798418494116042821, 0.3134422064149794407 ) ) ;
#145821=CARTESIAN_POINT ( 'NONE',  ( 1.048114208743459619, -1.451426956872736262, 1.132798186660122441 ) ) ;
#145822=CARTESIAN_POINT ( 'NONE',  ( 4.869394097828703138, -1.702981969582622046, -1.073415598185305964 ) ) ;
#145823=CARTESIAN_POINT ( 'NONE',  ( 6.522148393938469901, -2.055459957301557949, 1.029436805849759828 ) ) ;
#145824=CARTESIAN_POINT ( 'NONE',  ( 5.787936641206399280, -1.241742415844361291, -1.518776266119965745 ) ) ;
#145829=CARTESIAN_POINT ( 'NONE',  ( 2.032869862874300271, -1.866249813966861515, 0.9426962998228316515 ) ) ;
#145830=CARTESIAN_POINT ( 'NONE',  ( 0.3033014811697418711, -0.5033704626738467747, 1.801585485020948951 ) ) ;
#145833=CARTESIAN_POINT ( 'NONE',  ( 0.7315135518511396429, 1.714293348657709881, 0.2994600772705089953 ) ) ;
#145838=CARTESIAN_POINT ( 'NONE',  ( 1.541173760317329666, -1.247365581009220126, -1.191596266039594010 ) ) ;
#145839=CARTESIAN_POINT ( 'NONE',  ( 1.804482060849887270, 1.621174160030929068, -1.474864209862189579 ) ) ;
#145840=CARTESIAN_POINT ( 'NONE',  ( 4.002700589841681200, -0.6913439845411989415, -2.095861086919461602 ) ) ;
#145842=CARTESIAN_POINT ( 'NONE',  ( 1.885821443427546207, -2.045346407173433967, 0.7285060392495151804 ) ) ;
#145843=CARTESIAN_POINT ( 'NONE',  ( 0.08226035653636187828, -1.769965142718381124, -0.4472663993063328847 ) ) ;
#145844=CARTESIAN_POINT ( 'NONE',  ( 2.764987222883477980, -0.1607348756041589999, -2.111328481229361564 ) ) ;
#145847=CARTESIAN_POINT ( 'NONE',  ( 2.859215333236740264, 0.3337469566037793989, -2.267824818490314254 ) ) ;
#145851=CARTESIAN_POINT ( 'NONE',  ( 6.322901860479969827, 1.648133277211549563, -1.489392227938668434 ) ) ;
#145858=CARTESIAN_POINT ( 'NONE',  ( 3.533827422916273164, -1.646839391163470223, 1.163268690995450383 ) ) ;
#145860=CARTESIAN_POINT ( 'NONE',  ( 2.237243932873288710, -0.09700783546583501005, -2.060382906607181930 ) ) ;
#145865=CARTESIAN_POINT ( 'NONE',  ( 4.857479518068650748, 2.167902099161696849, -0.3196092617779102696 ) ) ;
#145866=CARTESIAN_POINT ( 'NONE',  ( 2.233046271152541618, 2.016033844848092560, 0.04667593304989729741 ) ) ;
#145867=CARTESIAN_POINT ( 'NONE',  ( 2.138008341990283778, 0.4048980806483238326, 1.796005048712509655 ) ) ;
#145869=CARTESIAN_POINT ( 'NONE',  ( 5.403274641334286699, 1.493489847867332854, 1.049580640413529276 ) ) ;
#145870=CARTESIAN_POINT ( 'NONE',  ( 5.678361341766085424, 1.528739221709461082, 1.314999087022615587 ) ) ;
#145872=CARTESIAN_POINT ( 'NONE',  ( 5.383742603502962965, 1.515107113446222398, 1.680479692888930288 ) ) ;
#145874=CARTESIAN_POINT ( 'NONE',  ( 0.7507728315698600774, 0.6134373412659529512, 2.014746520763583959 ) ) ;
#145884=CARTESIAN_POINT ( 'NONE',  ( 2.320824347369263574, -0.8547976213506520704, -2.050556073580122707 ) ) ;
#145888=CARTESIAN_POINT ( 'NONE',  ( 3.789464544343919883, -1.813617537123424661, 0.7486148740368094856 ) ) ;
#145895=CARTESIAN_POINT ( 'NONE',  ( 2.637105894733019262, 1.998242115483703341, 0.7103459930332192140 ) ) ;
#145897=CARTESIAN_POINT ( 'NONE',  ( 4.856408821558930278, 0.8241108818672329139, 1.998647875481096126 ) ) ;
#145898=CARTESIAN_POINT ( 'NONE',  ( 2.647807870277216757, 0.6224553824519338807, 1.732961026760751366 ) ) ;
#145902=CARTESIAN_POINT ( 'NONE',  ( 6.105355155539634815, -1.726289741429184899, 0.2200517785161565654 ) ) ;
#145906=CARTESIAN_POINT ( 'NONE',  ( 2.711983997553393699, -2.138339778157403615, 0.3160903847422363300 ) ) ;
#145907=CARTESIAN_POINT ( 'NONE',  ( 4.182970119252515495, -1.034007530860373336, -1.730600854597413640 ) ) ;
#145909=CARTESIAN_POINT ( 'NONE',  ( 2.026462046419864826, 1.244889377058140845, -1.767065586814352773 ) ) ;
#145910=CARTESIAN_POINT ( 'NONE',  ( 3.075414692445295195, 1.873101151500027317, -0.6148835396118810248 ) ) ;
#145911=CARTESIAN_POINT ( 'NONE',  ( 6.509000000000039421, 2.968845098214093703, 2.453284407971462411 ) ) ;
#145912=CARTESIAN_POINT ( 'NONE',  ( 4.687022505062548916, 1.441580155910677785, 1.301524815871560214 ) ) ;
#145921=CARTESIAN_POINT ( 'NONE',  ( 1.325528760500709780, -0.05309137938146882979, 2.206304558879538025 ) ) ;
#145923=CARTESIAN_POINT ( 'NONE',  ( 4.733228419949464971, 0.004064956161661801778, -1.961936380062332397 ) ) ;
#145928=CARTESIAN_POINT ( 'NONE',  ( 4.154132678086497776, -1.362845063541193946, 1.238102162693654362 ) ) ;
#145933=CARTESIAN_POINT ( 'NONE',  ( 6.135037582782754129, 1.979230198018981701, 0.7618025574447004900 ) ) ;
#145936=CARTESIAN_POINT ( 'NONE',  ( 6.854767756753092023, -1.595935894175725123, 1.303543064889536751 ) ) ;
#145938=CARTESIAN_POINT ( 'NONE',  ( 1.416206177014844192, 0.7498276349873562729, 1.703500622989342572 ) ) ;
#145939=CARTESIAN_POINT ( 'NONE',  ( 4.194743914777058436, 1.481411246205705412, 1.093257649623424754 ) ) ;
#145944=CARTESIAN_POINT ( 'NONE',  ( 2.825073394047578734, 2.078234123670623212, 0.7428476018367863309 ) ) ;
#145945=CARTESIAN_POINT ( 'NONE',  ( 6.046200420459929781, 2.259369630126391471, 0.1200006983746708389 ) ) ;
#145947=CARTESIAN_POINT ( 'NONE',  ( 6.398695480837623961, -1.778505541023298386, -0.3437013697835926140 ) ) ;
#145948=CARTESIAN_POINT ( 'NONE',  ( 4.944510238519550072, -1.383032091829504928, 1.325833103116050626 ) ) ;
#145951=CARTESIAN_POINT ( 'NONE',  ( 6.121928861531041655, -1.040746078065577063, -1.554202398018275755 ) ) ;
#145952=CARTESIAN_POINT ( 'NONE',  ( 6.338329682780378782, -0.9945775373912761896, 1.572806762946916903 ) ) ;
#145954=CARTESIAN_POINT ( 'NONE',  ( 6.016413156365523207, 1.185731173915012038, -1.314077388775713784 ) ) ;
#145955=CARTESIAN_POINT ( 'NONE',  ( 1.710173085450257924, 1.157096902994741772, -1.651345047625000007 ) ) ;
#145957=CARTESIAN_POINT ( 'NONE',  ( 3.246800538002168945, 0.5120957664956159450, 2.042728137747833461 ) ) ;
#145962=CARTESIAN_POINT ( 'NONE',  ( 3.533467377359212680, -0.1442520194480846618, 2.014668725452229303 ) ) ;
#145965=CARTESIAN_POINT ( 'NONE',  ( 3.778741785029844369, -2.082091666206013159, -0.5805316298483630399 ) ) ;
#145969=CARTESIAN_POINT ( 'NONE',  ( 0.8542542287434266024, -0.7813174834335520069, 2.025881038206469587 ) ) ;
#145973=CARTESIAN_POINT ( 'NONE',  ( 2.068174269828721101, -1.345378145056834063, 1.729934933326432445 ) ) ;
#145975=CARTESIAN_POINT ( 'NONE',  ( 2.940562510593609513, 2.245292490812002661, 0.2782218841625680450 ) ) ;
#145983=CARTESIAN_POINT ( 'NONE',  ( 3.637761035129345455, 0.7980134727624802471, -1.579695959945091044 ) ) ;
#145985=CARTESIAN_POINT ( 'NONE',  ( 6.106501571484221458, -0.7887142981495840477, -2.061199855587454444 ) ) ;
#145989=CARTESIAN_POINT ( 'NONE',  ( 5.730092268227672037, 2.014234620932173758, 0.09611943034040781875 ) ) ;
#145991=CARTESIAN_POINT ( 'NONE',  ( 3.608139902456270143, -0.7572706533398064765, -1.710698989992056829 ) ) ;
#145992=CARTESIAN_POINT ( 'NONE',  ( 3.080986915251407776, 1.947773190787219555, 0.7018234266842755531 ) ) ;
#145996=( LENGTH_UNIT ( ) NAMED_UNIT ( * ) SI_UNIT ( .MILLI., .METRE. ) );
#145997=ADVANCED_FACE ( 'NONE', ( #30191 ), #47537, .F. ) ;
#146000=CARTESIAN_POINT ( 'NONE',  ( 2.769914238037580745, -1.940913097850523128, 0.2850433363836765155 ) ) ;
#146001=CARTESIAN_POINT ( 'NONE',  ( 1.493517298738750609, 1.942243344100362590, 0.5404107738020345053 ) ) ;
#146004=CARTESIAN_POINT ( 'NONE',  ( 6.907508285686359883, -0.4377196890756588910, 1.929438547640258017 ) ) ;
#146006=CARTESIAN_POINT ( 'NONE',  ( 1.898691433116481031, -1.975183796067316866, -0.3886032139628642912 ) ) ;
#146008=CARTESIAN_POINT ( 'NONE',  ( 2.214611691679416072, 2.054518390865597954, 0.5110800211125585690 ) ) ;
#146010=CARTESIAN_POINT ( 'NONE',  ( 4.193848433072798088, -1.425472641756184489, -1.501718461524886195 ) ) ;
#146012=CARTESIAN_POINT ( 'NONE',  ( 5.859345120547017949, 2.059885262428410968, -0.3562953063034664525 ) ) ;
#146014=CARTESIAN_POINT ( 'NONE',  ( 4.471595891589618788, 1.770651423122941548, -0.4439726157009425411 ) ) ;
#146019=CARTESIAN_POINT ( 'NONE',  ( 6.545939543708723107, 0.8506627741289953804, -2.036432556493542823 ) ) ;
#146021=( BOUNDED_SURFACE ( )  B_SPLINE_SURFACE ( 3, 3, ( 
 ( #139826, #206920, #205855, #141971, #91072, #72654, #87855, #57487, #123648, #8724, #189610, #173387, #74806, #124703, #41256, #190662, #42322, #174458, #125767, #26034, #207983, #105190, #5495, #92146, #21746, #158200, #9790, #75864, #59611, #191729, #71576, #137684, #104109, #170158, #31389, #94275, #28180, #147274, #46580, #44451, #112699, #43385, #209037, #143042, #47658, #146226, #113769, #110568, #11920, #80121, #15107, #194944, #212243, #30325, #60673, #96409, #161396, #179772, #29254, #126836, #97464, #163520, #12980, #128964, #62803, #45518, #145172, #14035, #176570, #111634, #131081, #109506, #63877, #64931, #160316, #130031, #178709, #196022, #81196, #77993, #177645, #175513, #27103, #213306, #93210, #144115, #159242, #162459, #10842, #76916, #192793, #210109, #61749, #127916, #193869, #95346, #79055, #211177, #68106, #214338, #197070, #50824, #67041, #198127, #201310, #115885, #34565, #181870, #65968, #36694, #135296, #49759, #167776, #17231, #100636, #116951, #151537, #152587, #86522, #33506, #98515, #132117, #16162, #166713, #99579, #3105, #18303, #52950, #119088, #48707, #4174, #69176, #185068, #148338, #182950, #32446, #20440, #84389, #199178, #150476, #85452, #2036, #70243, #184012, #165643, #180819, #83306, #149393, #118023, #133178, #51901, #200249, #102779, #134242, #35626, #101704, #975, #114821, #19372, #164577, #168836, #82247, #139567, #54028, #188281, #123392, #71312, #137424, #9539, #120165, #186141, #189356, #40996, #124452, #187216, #121246, #25780, #205594, #203443, #57231, #136358, #87597, #21487, #140651, #24711, #206664, #55097, #104928, #173130, #108181, #73466, #90813, #107107, #153668, #156877, #39922, #58296, #122324, #5236, #190411, #42067, #106030, #7386, #155803, #138491, #23645, #8464, #38845, #202378, #37776, #103850, #74551, #174207, #91892, #170970, #22569, #157948, #169898, #88675, #154734, #6317, #72391, #204512, #56161, #172052, #89753, #76669, #44194, #112441, #47400, #12720, #30063, #62549, #26849, #128712, #193619, #211985, #61490, #92953, #63626, #79864, #45260, #161132, #95084, #77738, #177383, #46325, #208789, #143859, #163266, #141725, #178454, #97214, #142784, #96152, #144916, #13790, #129780, #195761, #162203, #145973, #78793, #60420, #127655, #210923, #176321, #194683, #159000, #75614, #209852, #160060, #126580, #113512, #192541, #111380, #110314, #10593, #179521, #31139, #27927, #207733, #94021, #28997, #59356, #125513, #191475, #43143, #11664, #109256, #175264, #48461, #66775, #214088, #183762, #50567, #19116, #167519, #14848, #36442, #130827, #180567, #118826, #81996, #18043, #133992, #49503, #114575, #85195, #117771, #196819, #15913, #199998, #35371, #131864, #148083, #32189, #711, #16973, #83054, #101446, #151280, #80938, #150216, #184812, #197871, #65716, #115623, #181618, #164323, #132916, #2851, #98265, #99331, #68920, #198921, #84130, #135041, #165380, #116689, #1788, #33247, #102516, #51648, #52695, #149130, #182688, #67845, #147030, #34306, #201054, #100381, #166453, #213052, #64681, #86266, #188022, #39651, #205333, #21233, #87338, #40735, #204249, #37515, #55901, #168579, #119905, #53772, #139304, #23381, #56971, #103591, #4975, #171785, #106841, #122058, #89491, #105760, #185880, #155546, #22299, #123145, #104666, #169648, #189102, #172872, #88411, #138235 ),
 ( #7125, #73198, #24443, #20179, #152337, #3915, #69984, #136096, #71053, #202112, #153406, #137169, #203193, #154479, #54839, #120990, #186957, #38589, #170714, #6057, #72128, #132560, #16610, #201755, #85905, #342, #118468, #182317, #199630, #67483, #102154, #103225, #37143, #198560, #49151, #165015, #181260, #51276, #50208, #168220, #183397, #151979, #35002, #147716, #149851, #1420, #3553, #98964, #133628, #197508, #185519, #117400, #101074, #167161, #36072, #18748, #169284, #134686, #116326, #131504, #66415, #33946, #68559, #17673, #2483, #84833, #150922, #200689, #52340, #184454, #19820, #100021, #69623, #20870, #213734, #135733, #65358, #148773, #53396, #119534, #115268, #32887, #82691, #166085, #83759, #106473, #88037, #72837, #172500, #187658, #24086, #104295, #86969, #155178, #171418, #154109, #91261, #5678, #138941, #71756, #170343, #141099, #25159, #137872, #57676, #121691, #204961, #6762, #41447, #42514, #190853, #203892, #202824, #21928, #120617, #56609, #55537, #107555, #122773, #157320, #188733, #153038, #89124, #40371, #8911, #38222, #90191, #136799, #124889, #156254, #7833, #73924, #189796, #140017, #108620, #206042, #39285, #70686, #105379, #23006, #123834, #173589, #74991, #207110, #58737, #174648, #4612, #54473, #186595, #204552, #145225, #158254, #174513, #143097, #45570, #124757, #109563, #111686, #209090, #125822, #175567, #177693, #142021, #193923, #92204, #208036, #191783, #9843, #108489, #58603, #210161, #78045, #43439, #25022, #157181, #192846, #11971, #61802, #46630, #59663, #10895, #60725, #126888, #27158, #190717, #211230, #79107, #93263, #42379, #144169, #159296, #29304, #62855, #127971, #75918, #8776, #76970, #44505, #160369, #110622, #94327, #28234, #95398, #176623, #161450, #13030, #129020, #194996, #91122, #74859, #26089, #140962, #112753, #206972, #16214, #165694, #113823, #179822, #51953, #96464, #162513, #17283, #83359, #166765, #15159, #163576, #68162, #181925, #31441, #33556, #178765, #130081, #63926, #183000, #67091, #34617, #97520, #147327, #1026, #150527, #115936, #133226, #149444, #196076, #199231, #82298, #100687, #164630, #47708, #18360, #84438, #148391, #49809, #198176, #180872, #66021, #50878, #81247, #32494, #30378, #14085, #117001, #200301, #213355, #2088, #99628, #134294, #80176, #146281, #212294, #64976, #131131, #197120, #214392, #48759, #114871, #98568, #132170, #118075, #186191, #202426, #119137, #122374, #36744, #169948, #102830, #201361, #172101, #56210, #185119, #88725, #152639, #21536, #37824, #72437, #73516, #7435, #168885, #19424, #135347, #151590, #87646, #20489, #138538, #153716, #188331, #5284, #184062, #120217, #103902, #39971, #69229, #71362, #167825, #155848, #137478, #203492, #55145, #6368, #121291, #187267, #205641, #35680, #204562, #139618, #86575, #154783, #38893, #106078, #23694, #89804, #101758, #85503, #104979, #4224, #171019, #22616, #70294, #3157, #53002, #136410, #54081, #141766, #58341, #61532, #190456, #109296, #42115, #140699, #111420, #209894, #124497, #27969, #91934, #175305, #191518, #11706, #12760, #161174, #108227, #173179, #74595, #90861, #26892, #174252, #77780, #92996, #127698, #159040, #57280, #59401, #125557, #193658, #8514, #43183, #107154, #95125, #10633, #76709, #142825, #160103, #208832, #78834, #44237, #25824, #41045, #157994 ),
 ( #123441, #189403, #9583, #24759, #60462, #156925, #126619, #110358, #206713, #75659, #144955, #207774, #192582, #176362, #94063, #45301, #143901, #177424, #29042, #214130, #212023, #65758, #210961, #162243, #96192, #754, #99372, #66820, #63666, #179557, #33288, #182734, #148129, #165424, #197913, #13829, #49541, #114616, #132963, #196859, #79904, #198966, #50610, #180607, #82035, #15952, #213091, #98303, #181661, #129820, #146012, #34353, #116735, #97251, #195802, #115667, #31178, #17022, #32232, #83098, #46363, #163305, #47439, #131905, #64721, #164368, #149178, #113554, #112483, #14886, #30102, #130863, #100426, #178492, #166497, #62588, #18088, #128751, #80981, #84176, #147070, #194724, #48497, #187008, #5030, #53823, #23430, #51696, #152386, #185928, #86314, #103644, #121041, #3964, #117818, #200045, #21284, #87390, #70032, #37564, #134037, #204299, #202165, #55955, #201102, #38639, #104718, #72176, #168626, #19166, #20229, #136148, #122108, #153457, #151328, #183808, #85240, #35418, #101496, #39702, #2896, #71105, #54887, #184862, #167566, #88467, #170766, #68969, #135088, #22355, #154527, #52742, #118876, #36489, #119953, #169696, #137223, #6106, #138284, #150265, #203243, #105811, #102566, #188073, #171837, #1833, #67892, #207530, #110110, #189152, #174004, #176121, #59149, #190206, #25575, #27721, #206459, #43992, #156668, #58086, #41866, #74344, #172922, #123191, #60213, #142573, #107975, #89541, #7177, #42931, #76464, #126374, #111176, #124248, #75409, #125307, #191265, #91686, #26647, #90609, #73248, #24498, #205385, #40791, #193421, #8260, #92748, #208580, #157739, #106896, #93815, #192333, #57024, #140448, #159856, #11459, #9336, #141522, #109041, #175060, #158792, #10389, #77532, #143653, #155592, #209648, #45065, #61289, #127450, #177178, #139355, #178255, #146834, #49315, #128516, #113315, #115432, #212853, #129577, #179321, #181423, #145784, #197671, #95951, #211787, #195564, #13595, #112244, #62355, #213900, #81801, #47200, #28794, #160930, #196624, #15716, #65523, #53303, #63425, #14652, #64490, #130632, #30942, #194484, #506, #82858, #97017, #46127, #147884, #163071, #33053, #48263, #99131, #78597, #80746, #29868, #180372, #114377, #31996, #98077, #79669, #144717, #164132, #162006, #131668, #165180, #210729, #16774, #94878, #135633, #12524, #148934, #69526, #201654, #119435, #41348, #7733, #40263, #89023, #58639, #86870, #187559, #6664, #121587, #138838, #156152, #39186, #152936, #20774, #56509, #122670, #105275, #72740, #169182, #25060, #22907, #91162, #21829, #73819, #139913, #107457, #203789, #54377, #55435, #171312, #157218, #188632, #186493, #4513, #120515, #70586, #136701, #74892, #38124, #106374, #90088, #5577, #202725, #123734, #205944, #104197, #170244, #57575, #189695, #87937, #154011, #71657, #155076, #204854, #172398, #173483, #8816, #185422, #23986, #141000, #137771, #207008, #37040, #103124, #59696, #28270, #145261, #9877, #209128, #211268, #94362, #10930, #60766, #62892, #27192, #79145, #191815, #93298, #77006, #109598, #208070, #158287, #95437, #177730, #143133, #124792, #42416, #78081, #111722, #161488, #146313, #159334, #110656, #160404, #12007, #126926, #75953, #96500, #178801, #192883, #142056, #29342, #44540, #129061, #144205, #195034, #174550, #176657, #125858, #61837, #210201, #128004 ),
 ( #46668, #193958, #43480, #45605, #13066, #112789, #30416, #175603, #190753, #162550, #14121, #80213, #212327, #108521, #26126, #92237, #147363, #118110, #2122, #131166, #34652, #98606, #115972, #198210, #18393, #19458, #167860, #48793, #179857, #81286, #97556, #181962, #114910, #84470, #99662, #68197, #65013, #32531, #100722, #35715, #1064, #150561, #50913, #15195, #117041, #33590, #200334, #49845, #213389, #51985, #134329, #165731, #149481, #83399, #66059, #17319, #166801, #197156, #132202, #151623, #130122, #184095, #85533, #180908, #101791, #133262, #63966, #196110, #47748, #113863, #31481, #67129, #164667, #199270, #183036, #16250, #163614, #82335, #148427, #38386, #87672, #4255, #7467, #136442, #55176, #202458, #86606, #57308, #155878, #70325, #188359, #37856, #121321, #137505, #172129, #173209, #107184, #54113, #119167, #20522, #36777, #187297, #120247, #23724, #38923, #73546, #105006, #3189, #5312, #71394, #139649, #168918, #203522, #53032, #41076, #171046, #22645, #88754, #106108, #154811, #24789, #204590, #186224, #201395, #103935, #169978, #138569, #153744, #72469, #6396, #89830, #56242, #122401, #39999, #205670, #123472, #69260, #135376, #21566, #185152, #189434, #102861, #90892, #152672, #91964, #158023, #30135, #74625, #140730, #209926, #143931, #144987, #207802, #141798, #46395, #160135, #9611, #11735, #156951, #108258, #42143, #161206, #45333, #12792, #159069, #78866, #174279, #10665, #206742, #194758, #126649, #76737, #142857, #111453, #192615, #112511, #61565, #59431, #58373, #75688, #125588, #77810, #26919, #127731, #193689, #177457, #93028, #44268, #29071, #208860, #110389, #8543, #124527, #191548, #190485, #95155, #25854, #60491, #210992, #43213, #109329, #175338, #176394, #27999, #62619, #128780, #178524, #94096, #81013, #200078, #99403, #97285, #165456, #96223, #47474, #195834, #100456, #198997, #166531, #163340, #64756, #132996, #67924, #33322, #50643, #83131, #113587, #149210, #214162, #18121, #82069, #179589, #84209, #150297, #65787, #181692, #115700, #98334, #197948, #66852, #14919, #164400, #183840, #162274, #116770, #117848, #147101, #182767, #17051, #34384, #1863, #134069, #51727, #13861, #785, #213125, #148160, #79938, #196891, #146043, #31211, #212056, #15983, #180642, #130898, #63697, #48529, #131937, #114649, #32267, #129851, #49575, #102606, #6137, #70068, #87424, #169728, #204329, #205419, #139386, #20265, #151362, #52775, #69004, #153491, #86349, #55988, #71136, #39737, #137254, #35451, #37597, #5061, #152420, #122139, #203273, #105842, #54920, #101530, #103680, #21317, #171869, #201137, #121071, #85276, #73282, #187039, #38671, #104750, #138314, #170799, #57056, #22388, #3999, #19198, #168660, #136181, #88498, #119988, #154560, #72207, #188107, #185965, #23465, #89575, #155624, #7209, #167599, #2932, #36519, #135121, #123221, #118913, #184894, #202199, #53855, #190239, #62383, #106931, #172955, #27755, #176155, #177212, #25607, #174035, #78627, #192365, #41897, #44024, #189185, #140479, #74377, #193456, #77567, #45100, #108008, #157770, #11495, #160962, #126405, #143689, #93850, #206491, #159888, #92782, #111209, #175092, #58121, #28825, #94913, #158827, #60248, #208615, #191300, #76495, #209681, #91719, #42968, #40822, #24534, #61325, #210763, #9369, #127485, #110142, #12552, #144751 ),
 ( #109076, #59180, #75440, #90642, #141552, #26680, #207559, #124280, #156702, #8293, #125337, #10423, #142606, #180405, #48294, #82888, #83950, #17867, #113347, #29897, #145812, #162035, #178289, #179352, #13626, #196654, #50399, #95983, #197703, #128547, #150041, #194513, #146867, #49345, #79699, #46161, #198752, #165213, #115464, #32024, #1612, #211819, #130665, #164161, #64519, #81831, #99160, #114406, #63456, #129610, #213930, #65552, #98109, #15746, #112274, #182510, #147914, #34140, #30974, #16803, #148964, #116519, #212888, #195595, #131697, #181455, #100209, #33085, #47230, #97049, #163102, #14682, #80779, #536, #66603, #132749, #166276, #102340, #101268, #5876, #170536, #183585, #68751, #38411, #22121, #184643, #134873, #18939, #53594, #69813, #135919, #88233, #204073, #67671, #203018, #171607, #167352, #121879, #187850, #200880, #2679, #185707, #154302, #85024, #152169, #71950, #37341, #168412, #3738, #138060, #36262, #55725, #52525, #20009, #86093, #118659, #151113, #201938, #104493, #120808, #119728, #133815, #199829, #21060, #54660, #39476, #89316, #103415, #169475, #87157, #153228, #4798, #70878, #105575, #23201, #136991, #186785, #155363, #51470, #117594, #35193, #93596, #56797, #41642, #106670, #158576, #75189, #125091, #26424, #206236, #25357, #142358, #122966, #139127, #77316, #43779, #76249, #191049, #94663, #188925, #9113, #42714, #157518, #174847, #192115, #141301, #40563, #172694, #92536, #10175, #207310, #108822, #205154, #61070, #58933, #127229, #57863, #109892, #175905, #143429, #91457, #90378, #208368, #59999, #193198, #126152, #8031, #24272, #156447, #74121, #140217, #110952, #124025, #27496, #159640, #107756, #189991, #11237, #209425, #173782, #44846, #176959, #28575, #6948, #73028, #112029, #146617, #162851, #14429, #181207, #82639, #160706, #81583, #50153, #194265, #293, #66363, #79452, #95734, #64275, #32835, #45911, #30719, #98912, #130420, #46975, #96802, #164964, #63201, #115217, #13377, #129365, #113091, #145568, #29649, #178031, #131455, #213683, #179097, #12300, #78380, #114165, #147666, #197456, #182266, #195343, #212634, #196407, #48052, #80519, #161786, #132510, #198508, #180158, #211567, #65306, #31784, #16556, #97856, #148723, #210508, #163919, #15495, #49097, #116276, #33891, #144501, #62143, #128303, #84780, #133572, #168168, #21877, #1367, #169229, #99969, #203837, #166034, #184400, #101019, #104243, #18698, #151925, #150867, #183343, #154058, #38170, #167111, #70634, #134634, #3499, #19766, #54422, #55483, #121636, #2429, #67429, #117346, #199578, #69569, #68506, #120564, #135679, #170289, #201703, #17619, #102098, #85848, #87983, #51222, #53347, #149793, #137818, #119481, #185468, #37089, #202772, #103168, #187605, #86917, #200638, #83704, #52286, #118415, #20820, #36020, #152985, #4559, #186541, #136745, #5624, #71705, #34947, #141046, #105324, #171361, #40315, #155127, #42458, #22955, #91205, #26169, #188680, #106421, #129888, #89069, #6709, #92287, #158331, #30170, #90134, #24031, #146081, #108567, #172444, #174594, #39232, #204904, #138886, #46432, #142104, #112550, #156201, #7777, #75999, #13896, #190799, #208117, #9925, #56558, #59745, #157266, #178561, #25103, #122718, #96259, #162311, #8857, #124832, #58684, #41391, #207053, #125905, #73868, #107502, #72785, #139963 ),
 ( #205986, #74936, #194795, #57622, #79978, #123779, #189739, #173530, #212093, #63729, #50683, #99442, #69041, #97324, #197986, #17091, #131978, #149253, #166574, #49614, #163380, #31248, #66896, #133036, #115739, #83169, #179627, #35491, #33360, #101569, #32304, #18161, #150335, #117886, #214199, #64792, #65829, #181729, #167636, #199035, #196929, #14954, #130936, #81052, #147136, #85318, #48567, #116808, #100498, #16020, #213162, #134106, #84249, #114687, #180679, #1903, #67962, #98371, #164434, #82106, #165498, #826, #182808, #200115, #183879, #195872, #34425, #151401, #148199, #19238, #2973, #51766, #47511, #113623, #155663, #20304, #5099, #7246, #38711, #21356, #71175, #73323, #37637, #89612, #202239, #103715, #87462, #120026, #4037, #168700, #105885, #188148, #153530, #135158, #52815, #88538, #122182, #171910, #156741, #169766, #121113, #104791, #170837, #137293, #86389, #106968, #189223, #203311, #152457, #39779, #54961, #139425, #22428, #205460, #184932, #187078, #70106, #72247, #154600, #6179, #138355, #186002, #36556, #204372, #136219, #56029, #57093, #102644, #23507, #201177, #24573, #118953, #123258, #40863, #53891, #172992, #90680, #8331, #27789, #45133, #142644, #41933, #124317, #159927, #11530, #208652, #110179, #58159, #128582, #126441, #194548, #125372, #111243, #28860, #210795, #92817, #157807, #158861, #60283, #46192, #77600, #75476, #190276, #9405, #108046, #25643, #178325, #141588, #143723, #193491, #109114, #174071, #12587, #177248, #91754, #207595, #94947, #160995, #191335, #59214, #43001, #192404, #76531, #44059, #78660, #62418, #74416, #209716, #29933, #175128, #112310, #96017, #26715, #10458, #176189, #144788, #93887, #61361, #162070, #127520, #140515, #206527, #34168, #130696, #182542, #80809, #196688, #180437, #212919, #97082, #47265, #198782, #66634, #114437, #13659, #145847, #181486, #567, #50431, #35225, #48327, #213961, #131728, #197733, #32054, #113380, #199858, #67701, #98142, #179387, #132779, #164191, #100240, #49374, #166308, #63490, #15777, #31007, #165243, #81863, #115491, #33115, #64553, #129646, #147947, #163134, #65581, #150071, #195631, #82919, #79731, #117627, #211854, #99192, #148992, #14718, #146899, #83983, #116550, #17897, #16837, #101301, #1643, #133848, #51501, #183618, #203047, #167381, #118688, #52556, #138090, #22149, #204103, #102370, #3766, #170567, #39507, #54688, #88264, #186814, #184672, #38442, #21087, #55755, #103445, #36294, #121911, #187880, #87190, #137020, #70910, #119757, #153255, #104522, #20039, #185736, #18971, #151141, #154332, #85055, #86126, #5907, #71980, #105606, #171637, #23234, #2708, #68782, #134901, #69841, #120839, #200907, #168440, #152199, #4830, #135952, #201967, #53625, #37369, #169505, #65232, #198432, #131382, #15418, #200559, #84701, #213605, #117264, #181134, #50078, #66284, #100940, #102021, #35942, #197378, #47974, #163839, #180081, #116199, #49019, #167027, #182186, #150788, #33814, #146543, #148647, #213, #2351, #97779, #132431, #196330, #184317, #99893, #165954, #17538, #34866, #83627, #168090, #133493, #115138, #130341, #32754, #98836, #67348, #16480, #1290, #149710, #18622, #82561, #199496, #51140, #183262, #68427, #212561, #64200, #147587, #114090, #134556, #31704, #52206, #118332, #81508, #164886, #19689, #3424, #69491, #138800 ),
 ( #171279, #186454, #22871, #103089, #85767, #153976, #170210, #86835, #90054, #4478, #137737, #70549, #169147, #139875, #23950, #152900, #56471, #120482, #203757, #5543, #40227, #41311, #189659, #136668, #201619, #20740, #119399, #55400, #202693, #106338, #121554, #156114, #187525, #151848, #87903, #71624, #7696, #37007, #39156, #135598, #123698, #105239, #88987, #155040, #188596, #6626, #107418, #72705, #54343, #53268, #38091, #104162, #204820, #21795, #122633, #172360, #73779, #205906, #57541, #173443, #185388, #144241, #93333, #191852, #208107, #176690, #79184, #158322, #143169, #145299, #28303, #159369, #209164, #211304, #175641, #13105, #125893, #27227, #10968, #43514, #142092, #92275, #29378, #111758, #77042, #58673, #190787, #12042, #45641, #95473, #80251, #60803, #44577, #94398, #160436, #126961, #9914, #30451, #112823, #192921, #75989, #177762, #110691, #62929, #78113, #129098, #108554, #210235, #59735, #61872, #128037, #193991, #161521, #109635, #174585, #195069, #46708, #178837, #96536, #26161, #162583, #14157, #146350, #124822, #42450, #32564, #187069, #213423, #113899, #4027, #130154, #52807, #202231, #147397, #65046, #88529, #196144, #47785, #53883, #131202, #114944, #167628, #197191, #81320, #31516, #185993, #120017, #98641, #212362, #179893, #168691, #37627, #103707, #22419, #19229, #201167, #118945, #184924, #180944, #97591, #38702, #54949, #85307, #163650, #169758, #151393, #21346, #36548, #87455, #15230, #2963, #48829, #152449, #69034, #102634, #20295, #135151, #86381, #70097, #136212, #153522, #137283, #5091, #71166, #64004, #104781, #203302, #121102, #170828, #56018, #72237, #10449, #191326, #9395, #58150, #27780, #122172, #156732, #190268, #90669, #108036, #125362, #8322, #188138, #204362, #25634, #91746, #74407, #41925, #138345, #208643, #206518, #60275, #205450, #42992, #109105, #76522, #172984, #23497, #24563, #140507, #126432, #157799, #155654, #39769, #89603, #105874, #171899, #44050, #7236, #75467, #59206, #189212, #73313, #92809, #175120, #139416, #57084, #26706, #158852, #123249, #40852, #106959, #124308, #174062, #141579, #142633, #192395, #154590, #110170, #6169, #207586, #176180, #209707, #11522, #164184, #130689, #163126, #211843, #181477, #61351, #96007, #129636, #29924, #47257, #64545, #162061, #127511, #143715, #179377, #30998, #13650, #195622, #77591, #147937, #145839, #213953, #144779, #196679, #48318, #15770, #112299, #177238, #178315, #79722, #65574, #97073, #94939, #193481, #28851, #45125, #111235, #197725, #160987, #14708, #212912, #128574, #12579, #32046, #114430, #78651, #210787, #180429, #98134, #62410, #194538, #46185, #63481, #113371, #80802, #81855, #131721, #93878, #146892, #49365, #115484, #159916, #67693, #166298, #182532, #151133, #53615, #132770, #117615, #119748, #2700, #133839, #20028, #100230, #153245, #86117, #17889, #150062, #199850, #83974, #116542, #66623, #3757, #152188, #51492, #33107, #165234, #200899, #69832, #135940, #54678, #183607, #18961, #68773, #134892, #1634, #198773, #4818, #87179, #35216, #50422, #201958, #101291, #185726, #52546, #37359, #82911, #167373, #34160, #184663, #85045, #118678, #36282, #102360, #148984, #168432, #103434, #169495, #21077, #559, #70899, #99183, #137010, #203037, #120827, #16827, #6966, #105594, #121900, #90396, #207332, #71968 ) ),
 .UNSPECIFIED., .T., .F., .F. ) 
 B_SPLINE_SURFACE_WITH_KNOTS ( ( 4, 3, 4 ),
 ( 4, 1, 1, 1, 1, 1, 1, 1, 1, 1, 1, 1, 1, 1, 1, 1, 1, 1, 1, 1, 1, 1, 1, 1, 1, 1, 1, 1, 1, 1, 1, 1, 1, 1, 1, 1, 1, 1, 1, 1, 1, 1, 1, 1, 1, 1, 1, 1, 1, 1, 1, 1, 1, 1, 1, 1, 1, 1, 1, 1, 1, 1, 1, 1, 1, 1, 1, 1, 1, 1, 1, 1, 1, 1, 1, 1, 1, 1, 1, 1, 1, 1, 1, 1, 1, 1, 1, 1, 1, 1, 1, 1, 1, 1, 1, 1, 1, 1, 1, 1, 1, 1, 1, 1, 1, 1, 1, 1, 1, 1, 1, 1, 1, 1, 1, 1, 1, 1, 1, 1, 1, 1, 1, 1, 1, 1, 1, 1, 1, 1, 1, 1, 1, 1, 1, 1, 1, 1, 1, 1, 1, 1, 1, 1, 1, 1, 1, 1, 1, 1, 1, 1, 1, 1, 1, 1, 1, 1, 1, 1, 1, 1, 1, 1, 1, 1, 1, 1, 1, 1, 1, 1, 1, 1, 1, 1, 1, 1, 1, 1, 1, 1, 1, 1, 1, 1, 1, 1, 1, 1, 1, 1, 1, 1, 1, 1, 1, 1, 1, 1, 1, 1, 1, 1, 1, 1, 1, 1, 1, 1, 1, 1, 1, 1, 1, 1, 1, 1, 1, 1, 1, 1, 1, 1, 1, 1, 1, 1, 1, 1, 1, 1, 1, 1, 1, 1, 1, 1, 1, 1, 1, 1, 1, 1, 1, 1, 1, 1, 1, 1, 1, 1, 1, 1, 1, 1, 1, 1, 1, 1, 1, 1, 1, 1, 1, 1, 1, 1, 1, 1, 1, 1, 1, 1, 1, 1, 1, 1, 1, 1, 1, 1, 1, 1, 1, 1, 1, 1, 1, 1, 1, 1, 1, 1, 1, 1, 1, 1, 1, 1, 1, 1, 1, 1, 1, 1, 1, 1, 1, 1, 1, 1, 1, 1, 1, 1, 1, 1, 1, 1, 1, 1, 1, 1, 1, 1, 1, 1, 1, 1, 1, 1, 1, 1, 1, 1, 1, 1, 1, 1, 1, 1, 1, 1, 1, 1, 1, 1, 1, 1, 1, 1, 1, 1, 1, 1, 1, 1, 1, 1, 1, 1, 1, 1, 1, 1, 1, 1, 1, 1, 1, 1, 1, 1, 1, 1, 1, 1, 1, 1, 1, 1, 1, 1, 4 ),
 ( 0.000000000000000000, 0.5000000000000000000, 1.000000000000000000 ),
 ( 0.000000000000000000, 0.002599888508634240914, 0.005208754120092145765, 0.007813069968323356138, 0.01041690100177071650, 0.01302019566086259385, 0.01562517182793091500, 0.01822893254318404960, 0.02083328139698771564, 0.02343764900838959594, 0.02604139750447371365, 0.02864615928571910553, 0.03124958462592061434, 0.03385442086835698666, 0.03645794792899405279, 0.03906256697173399878, 0.04166661757251870907, 0.04427067912273281725, 0.04687528696281444140, 0.04947881815967773017, 0.05208365228821221909, 0.05468707701066444909, 0.05729184299815447134, 0.05989557646906591704, 0.06249996333325048142, 0.06510433798480201595, 0.06770807906337909798, 0.07031283757201339801, 0.07291626355048291819, 0.07552109983967189577, 0.07812462590386089201, 0.08072924387304455940, 0.08333329402460390445, 0.08593735478041557296, 0.08854196204427712547, 0.09114549249794960672, 0.09375032597506528786, 0.09635375006294695510, 0.09895851527076646170, 0.1015622481948881828, 0.1041666342325376776, 0.1067710083972730206, 0.1093747487337090180, 0.1119795066911244419, 0.1145829320296284648, 0.1171877676425944481, 0.1197912931610935483, 0.1223959103579086161, 0.1249999600491941698, 0.1276040200539713398, 0.1302086268569593308, 0.1328121566649932417, 0.1354169895755736042, 0.1380204131161003600, 0.1406251776355303407, 0.1432289101024236955, 0.1458332954032181272, 0.1484376691708411133, 0.1510414088543486633, 0.1536461663508109643, 0.1562495911381983071, 0.1588544261652600487, 0.1614579512270202244, 0.1640625677415503691, 0.1666666170620310916, 0.1692706764052687440, 0.1718752828374313091, 0.1744788120887783289, 0.1770836445231302458, 0.1796870676051354199, 0.1822918315264069888, 0.1848955636252137269, 0.1874999482789682093, 0.1901043217392619777, 0.1927080608589964439, 0.1953128179847096746, 0.1979162423098047296, 0.2005210768412587219, 0.2031246015352002054, 0.2057292174574958665, 0.2083332664966131842, 0.2109373252677763377, 0.2135419314191336626, 0.2161454602027163274, 0.2187502922511180836, 0.2213537149634070833, 0.2239584783767220588, 0.2265622101965570623, 0.2291665942930569411, 0.2317709675357785548, 0.2343747061808670040, 0.2369794630260087243, 0.2395828869776091552, 0.2421877211037245237, 0.2447912455187418734, 0.2473958609388257068, 0.2499999097859964270, 0.2526039680745227334, 0.2552085740350705789, 0.2578121024397855843, 0.2604169341924902348, 0.2630203566238439872, 0.2656251196193780695, 0.2682288512493328225, 0.2708332348783377697, 0.2734376079932215875, 0.2760413462527663842, 0.2786461029074911444, 0.2812495265743710227, 0.2838543603853929120, 0.2864578846103582599, 0.2890624996182282747, 0.2916665483628478883, 0.2942706062581511572, 0.2968752121178640513, 0.2994787402325856385, 0.3020835717798243114, 0.3046869940190023440, 0.3072917566869088346, 0.3098954882160545599, 0.3124998714673014044, 0.3151042445440625506, 0.3177079825071445485, 0.3203127390615869707, 0.3229161625325003282, 0.3255209961186533163, 0.3281245202424198926, 0.3307291349280532256, 0.3333331836594992104, 0.3359372412509727956, 0.3385418470998076690, 0.3411453750133909280, 0.3437502064453764050, 0.3463536285811206206, 0.3489583910115333087, 0.3515621225289245477, 0.3541665054921307454, 0.3567708786204680238, 0.3593746163761498691, 0.3619793729204284771, 0.3645827962841124981, 0.3671876297356038710, 0.3697911538470093351, 0.3723957683003653041, 0.3749998171080005105, 0.3776038744850206963, 0.3802084804129200468, 0.3828120082142042468, 0.3854168396211344327, 0.3880202617421720235, 0.3906250240252089334, 0.3932287556198868494, 0.3958331383847540352, 0.3984375116543538153, 0.4010412492916836102, 0.4036460059159037717, 0.4062494292610819846, 0.4088542626681055392, 0.4114577868559751161, 0.4140624011669984950, 0.4166664501401745602, 0.4192705073921035863, 0.4218751134889988097, 0.4244786412668108966, 0.4270834727388717056, 0.4296868949339185950, 0.4322916571596854274, 0.4348953889206810253, 0.4374997715768980666, 0.4401041450774376140, 0.4427078826854516369, 0.4453126394797092824, 0.4479160628950952239, 0.4505208963478340434, 0.4531244207009840763, 0.4557290349596088697, 0.4583330841876695483, 0.4609371414038593850, 0.4635417477596745495, 0.4661452756028321986, 0.4687501072302013849, 0.4713535295879656695, 0.4739582918465587991, 0.4765620238628961447, 0.4791664065001429718, 0.4817707803212932793, 0.4843745179890200370, 0.4869792750434049911, 0.4895826986177053142, 0.4921875322063354874, 0.4947910568135764908, 0.4973956711097291539, 0.4999997206820134821, 0.5026037779518089943, 0.5052083846564635605, 0.5078119126537786743, 0.5104167445266291070, 0.5130201671358142201, 0.5156249295173244152, 0.5182286618780244103, 0.5208330445859747915, 0.5234374188174044651, 0.5260411566338674128, 0.5286459140384663913, 0.5312493378603841965, 0.5338541716750782040, 0.5364576966252184720, 0.5390623110488209635, 0.5416663610546670338, 0.5442704184674093115, 0.5468750256108222407, 0.5494785538511040013, 0.5520833860596070508, 0.5546868090089153158, 0.5572915716034309019, 0.5598953043975141153, 0.5624996872658396541, 0.5651040619972180767, 0.5677078000514395040, 0.5703125578963399445, 0.5729159820545779436, 0.5755208161855079885, 0.5781243415673570363, 0.5807289562083304268, 0.5833330067370782190, 0.5859370643821081304, 0.5885416720542003821, 0.5911452006262593040, 0.5937500332605881725, 0.5963534566387238556, 0.5989582195363342132, 0.6015619528528246551, 0.6041663359711972880, 0.6067707112921981727, 0.6093744496732020899, 0.6119792080484952601, 0.6145826326317597177, 0.6171874671691013337, 0.6197909930714722293, 0.6223956080197403651, 0.6249996591607356322, 0.6276037171273963766, 0.6302083254180952387, 0.6328118544107458332, 0.6354166875610788301, 0.6380201114567515264, 0.6406248747475506988, 0.6432286086754787080, 0.6458329921335752566, 0.6484373681338796436, 0.6510411069306952792, 0.6536458659264798854, 0.6562492910234830612, 0.6588541260574176661, 0.6614576525691320263, 0.6640622679146246377, 0.6666663197572214594, 0.6692703781348633418, 0.6718749871341050950, 0.6744785166361690898, 0.6770833503926931840, 0.6796867748946214816, 0.6822915386687108397, 0.6848952732971168578, 0.6874996571846213600, 0.6901040339539210589, 0.6927077732555863010, 0.6953125329619718187, 0.6979159586614360755, 0.7005207942821553013, 0.7031243214920454010, 0.7057289373247008779, 0.7083329899582661016, 0.7109370488362486418, 0.7135416586339821121, 0.7161451887342924483, 0.7187500231872065992, 0.7213534483841206324, 0.7239582127316128712, 0.7265619481495508847, 0.7291663325561579256, 0.7317707101841592898, 0.7343744500797240171, 0.7369792105868335774, 0.7395826369774940456, 0.7421874732752028470, 0.7447910012721150608, 0.7473956176818850050, 0.7499996711958007989, 0.7526037306634962842, 0.7552083413496862851, 0.7578118721370898925, 0.7604167073766084917, 0.7630201333572542710, 0.7656248983682768516, 0.7682286346648167230, 0.7708330196802359868, 0.7734373982566630223, 0.7760411388351919904, 0.7786459002331664880, 0.7812493274037752844, 0.7838541644686951582, 0.7864576933414935134, 0.7890623104183455139, 0.7916663649020125870, 0.7942704250488100692, 0.7968750367134410650, 0.7994785682768023038, 0.8020834043931583945, 0.8046868312463003603, 0.8072915970109983963, 0.8098953342752303053, 0.8124997199891885735, 0.8151040996037859365, 0.8177078409543626636, 0.8203126033333638656, 0.8229160313726919806, 0.8255208692950642968, 0.8281243991326340259, 0.8307290169665545454, 0.8333330725093962554, 0.8359371334247044372, 0.8385417461577832077, 0.8411452785859873105, 0.8437501156694361404, 0.8463535434838604932, 0.8489583100924004144, 0.8515620484134380774, 0.8541664349156833369, 0.8567708156582201084, 0.8593745578699503174, 0.8619793213201638604, 0.8645827503170061545, 0.8671875891870957087, 0.8697911200783463581, 0.8723957387593448409, 0.8749997954508100806, 0.8776038572240605351, 0.8802084711156200614, 0.8828120044975765746, 0.8854168426383988155, 0.8880202715029178462, 0.8906250390454908406, 0.8932287785124739532, 0.8958331658927787267, 0.8984375478530519654, 0.9010412910150662480, 0.9036460556267057465, 0.9062494856698833923, 0.9088543255779816255, 0.9114578576118502751, 0.9140624772299625889, 0.9166665351595286726, 0.9192705978801787303, 0.9218752130202838568, 0.9244787474449313036, 0.9270835867334279445, 0.9296870167368762594, 0.9322917853037333558, 0.9348955260058576799, 0.9374999143539141100, 0.9401042976215825409, 0.9427080418234272674, 0.9453128076877782560, 0.9479162388645026027, 0.9505210798953250828, 0.9531246131693177359, 0.9557292338404025367, 0.9583332930514818493, 0.9609373567081632705, 0.9635419734050364449, 0.9661455093234165847, 0.9687503490003109841, 0.9713537788664922124, 0.9739585512809396661, 0.9765622998769101226, 0.9791666815729623830, 0.9817710277688282972, 0.9843747994658795797, 0.9869797739623470401, 0.9895830763955310028, 0.9921869177308453303, 0.9947912343601759133, 0.9974001139318913189, 1.000000000000000000 ),
 .UNSPECIFIED. ) 
 GEOMETRIC_REPRESENTATION_ITEM ( )  RATIONAL_B_SPLINE_SURFACE ( (
 ( 1.000000000000000222, 1.000000000000000222, 1.000000000000000222, 1.000000000000000000, 1.000000000000000000, 1.000000000000000444, 1.000000000000000000, 0.9999999999999997780, 1.000000000000000444, 0.9999999999999997780, 0.9999999999999997780, 1.000000000000000222, 0.9999999999999997780, 0.9999999999999997780, 1.000000000000000444, 0.9999999999999997780, 1.000000000000000222, 1.000000000000000222, 0.9999999999999996669, 1.000000000000000222, 0.9999999999999996669, 1.000000000000000444, 0.9999999999999994449, 1.000000000000000444, 0.9999999999999996669, 1.000000000000000222, 1.000000000000000000, 0.9999999999999997780, 1.000000000000000222, 0.9999999999999997780, 1.000000000000000000, 0.9999999999999997780, 1.000000000000000000, 1.000000000000000222, 0.9999999999999996669, 1.000000000000000000, 0.9999999999999997780, 1.000000000000000000, 1.000000000000000444, 0.9999999999999996669, 1.000000000000000222, 1.000000000000000000, 1.000000000000000222, 1.000000000000000222, 0.9999999999999997780, 0.9999999999999997780, 1.000000000000000222, 0.9999999999999997780, 1.000000000000000222, 0.9999999999999997780, 0.9999999999999997780, 0.9999999999999997780, 1.000000000000000444, 1.000000000000000000, 0.9999999999999997780, 1.000000000000000222, 1.000000000000000000, 1.000000000000000000, 0.9999999999999997780, 1.000000000000000222, 1.000000000000000000, 1.000000000000000000, 1.000000000000000222, 1.000000000000000000, 1.000000000000000000, 1.000000000000000000, 1.000000000000000222, 1.000000000000000000, 0.9999999999999997780, 1.000000000000000444, 1.000000000000000000, 0.9999999999999997780, 1.000000000000000000, 1.000000000000000222, 0.9999999999999997780, 1.000000000000000222, 0.9999999999999996669, 1.000000000000000222, 1.000000000000000000, 1.000000000000000000, 1.000000000000000000, 1.000000000000000222, 0.9999999999999997780, 1.000000000000000000, 1.000000000000000222, 0.9999999999999997780, 1.000000000000000000, 1.000000000000000000, 0.9999999999999996669, 1.000000000000000000, 1.000000000000000000, 1.000000000000000222, 1.000000000000000000, 0.9999999999999997780, 1.000000000000000222, 0.9999999999999996669, 1.000000000000000222, 0.9999999999999997780, 1.000000000000000000, 1.000000000000000000, 1.000000000000000222, 0.9999999999999996669, 1.000000000000000444, 1.000000000000000000, 0.9999999999999997780, 1.000000000000000000, 1.000000000000000000, 1.000000000000000222, 0.9999999999999997780, 1.000000000000000000, 1.000000000000000222, 1.000000000000000444, 1.000000000000000000, 1.000000000000000000, 1.000000000000000444, 1.000000000000000000, 0.9999999999999997780, 1.000000000000000222, 1.000000000000000000, 1.000000000000000000, 1.000000000000000000, 1.000000000000000000, 1.000000000000000000, 1.000000000000000000, 0.9999999999999996669, 1.000000000000000222, 0.9999999999999997780, 1.000000000000000222, 1.000000000000000000, 0.9999999999999997780, 1.000000000000000222, 0.9999999999999997780, 0.9999999999999997780, 0.9999999999999997780, 1.000000000000000000, 1.000000000000000000, 0.9999999999999996669, 1.000000000000000444, 1.000000000000000222, 1.000000000000000000, 1.000000000000000000, 1.000000000000000222, 1.000000000000000222, 1.000000000000000000, 1.000000000000000222, 0.9999999999999996669, 1.000000000000000444, 0.9999999999999997780, 0.9999999999999997780, 1.000000000000000444, 1.000000000000000000, 1.000000000000000222, 0.9999999999999997780, 1.000000000000000222, 1.000000000000000000, 1.000000000000000222, 1.000000000000000000, 1.000000000000000000, 0.9999999999999996669, 1.000000000000000444, 1.000000000000000000, 1.000000000000000222, 0.9999999999999997780, 1.000000000000000000, 1.000000000000000000, 1.000000000000000000, 1.000000000000000000, 0.9999999999999997780, 1.000000000000000000, 1.000000000000000000, 1.000000000000000000, 1.000000000000000222, 1.000000000000000222, 0.9999999999999997780, 1.000000000000000000, 1.000000000000000000, 0.9999999999999997780, 1.000000000000000000, 1.000000000000000000, 1.000000000000000000, 1.000000000000000000, 1.000000000000000444, 0.9999999999999997780, 1.000000000000000222, 0.9999999999999997780, 1.000000000000000000, 1.000000000000000222, 0.9999999999999997780, 1.000000000000000222, 1.000000000000000000, 1.000000000000000000, 1.000000000000000000, 1.000000000000000000, 0.9999999999999997780, 1.000000000000000000, 1.000000000000000000, 1.000000000000000000, 1.000000000000000000, 1.000000000000000000, 1.000000000000000222, 1.000000000000000000, 1.000000000000000222, 0.9999999999999997780, 1.000000000000000222, 0.9999999999999997780, 1.000000000000000222, 1.000000000000000000, 0.9999999999999997780, 1.000000000000000222, 0.9999999999999996669, 1.000000000000000444, 1.000000000000000000, 0.9999999999999996669, 1.000000000000000222, 1.000000000000000000, 1.000000000000000222, 0.9999999999999997780, 1.000000000000000444, 1.000000000000000000, 1.000000000000000000, 0.9999999999999997780, 1.000000000000000222, 1.000000000000000000, 1.000000000000000000, 1.000000000000000000, 1.000000000000000222, 0.9999999999999997780, 1.000000000000000222, 1.000000000000000000, 0.9999999999999997780, 1.000000000000000000, 0.9999999999999997780, 1.000000000000000222, 0.9999999999999996669, 1.000000000000000000, 1.000000000000000000, 1.000000000000000000, 1.000000000000000444, 1.000000000000000222, 1.000000000000000000, 1.000000000000000000, 0.9999999999999997780, 0.9999999999999997780, 1.000000000000000444, 0.9999999999999996669, 1.000000000000000444, 0.9999999999999997780, 0.9999999999999997780, 1.000000000000000222, 0.9999999999999997780, 0.9999999999999996669, 1.000000000000000444, 0.9999999999999997780, 1.000000000000000222, 1.000000000000000222, 1.000000000000000000, 0.9999999999999997780, 1.000000000000000222, 1.000000000000000000, 1.000000000000000222, 1.000000000000000000, 1.000000000000000000, 0.9999999999999997780, 0.9999999999999997780, 1.000000000000000444, 0.9999999999999997780, 0.9999999999999997780, 1.000000000000000222, 0.9999999999999994449, 1.000000000000000222, 0.9999999999999997780, 1.000000000000000000, 0.9999999999999997780, 1.000000000000000000, 1.000000000000000000, 1.000000000000000000, 1.000000000000000000, 1.000000000000000000, 1.000000000000000000, 1.000000000000000000, 1.000000000000000222, 1.000000000000000000, 1.000000000000000000, 1.000000000000000000, 1.000000000000000000, 1.000000000000000000, 1.000000000000000000, 1.000000000000000000, 1.000000000000000222, 1.000000000000000000, 1.000000000000000222, 0.9999999999999997780, 1.000000000000000000, 1.000000000000000444, 1.000000000000000000, 1.000000000000000000, 1.000000000000000000, 1.000000000000000222, 0.9999999999999997780, 1.000000000000000444, 0.9999999999999997780, 1.000000000000000222, 1.000000000000000000, 1.000000000000000000, 1.000000000000000000, 1.000000000000000222, 0.9999999999999994449, 1.000000000000000222, 1.000000000000000000, 1.000000000000000000, 1.000000000000000000, 0.9999999999999997780, 0.9999999999999997780, 1.000000000000000444, 0.9999999999999996669, 1.000000000000000222, 0.9999999999999997780, 1.000000000000000444, 0.9999999999999997780, 1.000000000000000222, 1.000000000000000222, 0.9999999999999996669, 1.000000000000000222, 1.000000000000000000, 1.000000000000000444, 1.000000000000000000, 1.000000000000000000, 1.000000000000000222, 1.000000000000000000, 1.000000000000000000, 0.9999999999999997780, 0.9999999999999997780, 1.000000000000000000, 0.9999999999999997780, 1.000000000000000222, 1.000000000000000222, 1.000000000000000000, 1.000000000000000222, 1.000000000000000222, 1.000000000000000000, 0.9999999999999997780, 0.9999999999999997780, 1.000000000000000222, 0.9999999999999997780, 1.000000000000000222, 1.000000000000000000, 1.000000000000000000, 1.000000000000000000, 0.9999999999999996669, 1.000000000000000222, 0.9999999999999997780, 1.000000000000000000, 0.9999999999999997780, 1.000000000000000222, 0.9999999999999997780, 1.000000000000000444, 0.9999999999999996669, 1.000000000000000222, 1.000000000000000222, 1.000000000000000000, 1.000000000000000000, 0.9999999999999997780, 1.000000000000000222, 0.9999999999999997780, 1.000000000000000222, 0.9999999999999997780, 0.9999999999999997780, 1.000000000000000000, 1.000000000000000000, 1.000000000000000222, 1.000000000000000000, 1.000000000000000444, 0.9999999999999997780, 1.000000000000000222, 0.9999999999999997780, 0.9999999999999997780, 1.000000000000000222, 1.000000000000000000, 0.9999999999999997780, 1.000000000000000000, 1.000000000000000000, 1.000000000000000000, 0.9999999999999997780, 1.000000000000000444, 0.9999999999999997780, 1.000000000000000000, 1.000000000000000000),
 ( 0.3333333333333334259, 0.3333333333333334259, 0.3333333333333333703, 0.3333333333333334259, 0.3333333333333334259, 0.3333333333333334259, 0.3333333333333334259, 0.3333333333333332593, 0.3333333333333335369, 0.3333333333333332593, 0.3333333333333333703, 0.3333333333333334259, 0.3333333333333333703, 0.3333333333333332593, 0.3333333333333334814, 0.3333333333333332593, 0.3333333333333334259, 0.3333333333333334259, 0.3333333333333332593, 0.3333333333333335369, 0.3333333333333332038, 0.3333333333333335369, 0.3333333333333331483, 0.3333333333333334814, 0.3333333333333333148, 0.3333333333333333703, 0.3333333333333333703, 0.3333333333333333148, 0.3333333333333333703, 0.3333333333333333148, 0.3333333333333333703, 0.3333333333333333703, 0.3333333333333333703, 0.3333333333333333703, 0.3333333333333333703, 0.3333333333333333703, 0.3333333333333333148, 0.3333333333333333148, 0.3333333333333334259, 0.3333333333333332593, 0.3333333333333334259, 0.3333333333333333148, 0.3333333333333334259, 0.3333333333333333703, 0.3333333333333333148, 0.3333333333333334259, 0.3333333333333333703, 0.3333333333333333703, 0.3333333333333334259, 0.3333333333333333148, 0.3333333333333333703, 0.3333333333333332593, 0.3333333333333335369, 0.3333333333333333703, 0.3333333333333333148, 0.3333333333333334259, 0.3333333333333333703, 0.3333333333333333703, 0.3333333333333333148, 0.3333333333333333703, 0.3333333333333333703, 0.3333333333333334259, 0.3333333333333334259, 0.3333333333333334259, 0.3333333333333333703, 0.3333333333333333703, 0.3333333333333334259, 0.3333333333333333148, 0.3333333333333333703, 0.3333333333333334259, 0.3333333333333334259, 0.3333333333333332593, 0.3333333333333333703, 0.3333333333333334259, 0.3333333333333333703, 0.3333333333333334259, 0.3333333333333333148, 0.3333333333333334814, 0.3333333333333333148, 0.3333333333333332593, 0.3333333333333334259, 0.3333333333333333703, 0.3333333333333333148, 0.3333333333333333703, 0.3333333333333334259, 0.3333333333333334259, 0.3333333333333333148, 0.3333333333333333703, 0.3333333333333332593, 0.3333333333333333703, 0.3333333333333333703, 0.3333333333333333703, 0.3333333333333333703, 0.3333333333333333148, 0.3333333333333333703, 0.3333333333333333148, 0.3333333333333334259, 0.3333333333333333703, 0.3333333333333334259, 0.3333333333333333148, 0.3333333333333333703, 0.3333333333333333148, 0.3333333333333334259, 0.3333333333333333703, 0.3333333333333333703, 0.3333333333333333703, 0.3333333333333333703, 0.3333333333333333703, 0.3333333333333332593, 0.3333333333333333703, 0.3333333333333333703, 0.3333333333333335369, 0.3333333333333334259, 0.3333333333333333148, 0.3333333333333335369, 0.3333333333333333148, 0.3333333333333333703, 0.3333333333333333703, 0.3333333333333334259, 0.3333333333333333148, 0.3333333333333333703, 0.3333333333333334259, 0.3333333333333334259, 0.3333333333333333703, 0.3333333333333332593, 0.3333333333333334259, 0.3333333333333333703, 0.3333333333333334814, 0.3333333333333333148, 0.3333333333333333703, 0.3333333333333334259, 0.3333333333333333703, 0.3333333333333333148, 0.3333333333333333703, 0.3333333333333333148, 0.3333333333333334259, 0.3333333333333332593, 0.3333333333333334814, 0.3333333333333333703, 0.3333333333333334259, 0.3333333333333333703, 0.3333333333333333703, 0.3333333333333334259, 0.3333333333333333703, 0.3333333333333333703, 0.3333333333333333148, 0.3333333333333335924, 0.3333333333333333148, 0.3333333333333333703, 0.3333333333333334259, 0.3333333333333333148, 0.3333333333333334259, 0.3333333333333333148, 0.3333333333333334259, 0.3333333333333333703, 0.3333333333333334259, 0.3333333333333333703, 0.3333333333333333703, 0.3333333333333333703, 0.3333333333333334259, 0.3333333333333333703, 0.3333333333333334814, 0.3333333333333333148, 0.3333333333333334814, 0.3333333333333333148, 0.3333333333333333703, 0.3333333333333333148, 0.3333333333333333703, 0.3333333333333333703, 0.3333333333333333703, 0.3333333333333333703, 0.3333333333333333703, 0.3333333333333334259, 0.3333333333333333148, 0.3333333333333334259, 0.3333333333333333703, 0.3333333333333333703, 0.3333333333333333703, 0.3333333333333333703, 0.3333333333333333148, 0.3333333333333333703, 0.3333333333333334259, 0.3333333333333333148, 0.3333333333333334259, 0.3333333333333333148, 0.3333333333333333703, 0.3333333333333333703, 0.3333333333333333148, 0.3333333333333333703, 0.3333333333333334259, 0.3333333333333333148, 0.3333333333333334259, 0.3333333333333333703, 0.3333333333333332593, 0.3333333333333334814, 0.3333333333333332593, 0.3333333333333334259, 0.3333333333333333148, 0.3333333333333333703, 0.3333333333333334814, 0.3333333333333333703, 0.3333333333333333703, 0.3333333333333332593, 0.3333333333333334814, 0.3333333333333333148, 0.3333333333333333703, 0.3333333333333334259, 0.3333333333333333148, 0.3333333333333334259, 0.3333333333333333148, 0.3333333333333333703, 0.3333333333333333703, 0.3333333333333332593, 0.3333333333333333703, 0.3333333333333333703, 0.3333333333333334259, 0.3333333333333333148, 0.3333333333333334814, 0.3333333333333333703, 0.3333333333333334259, 0.3333333333333333148, 0.3333333333333334259, 0.3333333333333333703, 0.3333333333333333703, 0.3333333333333333703, 0.3333333333333333703, 0.3333333333333333148, 0.3333333333333334814, 0.3333333333333333703, 0.3333333333333333703, 0.3333333333333333148, 0.3333333333333334259, 0.3333333333333333703, 0.3333333333333332593, 0.3333333333333333703, 0.3333333333333333703, 0.3333333333333333703, 0.3333333333333334259, 0.3333333333333334259, 0.3333333333333333703, 0.3333333333333333703, 0.3333333333333333703, 0.3333333333333333703, 0.3333333333333334259, 0.3333333333333332593, 0.3333333333333335369, 0.3333333333333332038, 0.3333333333333333148, 0.3333333333333333703, 0.3333333333333333148, 0.3333333333333333148, 0.3333333333333334259, 0.3333333333333333703, 0.3333333333333333703, 0.3333333333333333703, 0.3333333333333334259, 0.3333333333333333148, 0.3333333333333334814, 0.3333333333333333703, 0.3333333333333334259, 0.3333333333333333703, 0.3333333333333333703, 0.3333333333333332593, 0.3333333333333333148, 0.3333333333333334814, 0.3333333333333333148, 0.3333333333333332593, 0.3333333333333334259, 0.3333333333333332038, 0.3333333333333334259, 0.3333333333333333148, 0.3333333333333333148, 0.3333333333333334259, 0.3333333333333333703, 0.3333333333333333703, 0.3333333333333333703, 0.3333333333333333703, 0.3333333333333334259, 0.3333333333333333148, 0.3333333333333333148, 0.3333333333333334259, 0.3333333333333333148, 0.3333333333333334259, 0.3333333333333333148, 0.3333333333333333703, 0.3333333333333334259, 0.3333333333333333148, 0.3333333333333334814, 0.3333333333333333148, 0.3333333333333334259, 0.3333333333333334259, 0.3333333333333333148, 0.3333333333333333148, 0.3333333333333335369, 0.3333333333333333148, 0.3333333333333333148, 0.3333333333333333703, 0.3333333333333335369, 0.3333333333333332593, 0.3333333333333335369, 0.3333333333333333148, 0.3333333333333333148, 0.3333333333333334259, 0.3333333333333333148, 0.3333333333333334259, 0.3333333333333333703, 0.3333333333333332593, 0.3333333333333333703, 0.3333333333333333148, 0.3333333333333334259, 0.3333333333333333148, 0.3333333333333334259, 0.3333333333333332593, 0.3333333333333335369, 0.3333333333333332038, 0.3333333333333334259, 0.3333333333333332593, 0.3333333333333335369, 0.3333333333333333148, 0.3333333333333334259, 0.3333333333333334259, 0.3333333333333333148, 0.3333333333333333148, 0.3333333333333334259, 0.3333333333333334814, 0.3333333333333333148, 0.3333333333333333148, 0.3333333333333334259, 0.3333333333333333703, 0.3333333333333334259, 0.3333333333333333148, 0.3333333333333333148, 0.3333333333333333703, 0.3333333333333333703, 0.3333333333333334814, 0.3333333333333333148, 0.3333333333333334259, 0.3333333333333333703, 0.3333333333333334259, 0.3333333333333334259, 0.3333333333333333148, 0.3333333333333333703, 0.3333333333333334259, 0.3333333333333333148, 0.3333333333333334814, 0.3333333333333333703, 0.3333333333333333148, 0.3333333333333333703, 0.3333333333333333148, 0.3333333333333334259, 0.3333333333333333148, 0.3333333333333333703, 0.3333333333333332593, 0.3333333333333334814, 0.3333333333333333703, 0.3333333333333334814, 0.3333333333333333148, 0.3333333333333334259, 0.3333333333333334814, 0.3333333333333333148, 0.3333333333333334259, 0.3333333333333332593, 0.3333333333333334259, 0.3333333333333333703, 0.3333333333333333703, 0.3333333333333333148, 0.3333333333333333148, 0.3333333333333334259, 0.3333333333333333148, 0.3333333333333334814, 0.3333333333333333148, 0.3333333333333335924, 0.3333333333333333148, 0.3333333333333334259, 0.3333333333333333148, 0.3333333333333333703, 0.3333333333333333703, 0.3333333333333334814, 0.3333333333333332593, 0.3333333333333333703, 0.3333333333333333703, 0.3333333333333334259, 0.3333333333333333148, 0.3333333333333334259, 0.3333333333333333703, 0.3333333333333333703, 0.3333333333333333703),
 ( 0.3333333333333334259, 0.3333333333333334259, 0.3333333333333333703, 0.3333333333333334259, 0.3333333333333334259, 0.3333333333333334259, 0.3333333333333334259, 0.3333333333333332593, 0.3333333333333335369, 0.3333333333333332593, 0.3333333333333333703, 0.3333333333333334259, 0.3333333333333333703, 0.3333333333333332593, 0.3333333333333334814, 0.3333333333333332593, 0.3333333333333334259, 0.3333333333333334259, 0.3333333333333332593, 0.3333333333333335369, 0.3333333333333332038, 0.3333333333333335369, 0.3333333333333331483, 0.3333333333333334814, 0.3333333333333333148, 0.3333333333333333703, 0.3333333333333333703, 0.3333333333333333148, 0.3333333333333333703, 0.3333333333333333148, 0.3333333333333333703, 0.3333333333333333703, 0.3333333333333333703, 0.3333333333333333703, 0.3333333333333333703, 0.3333333333333333703, 0.3333333333333333148, 0.3333333333333333148, 0.3333333333333334259, 0.3333333333333332593, 0.3333333333333334259, 0.3333333333333333148, 0.3333333333333334259, 0.3333333333333333703, 0.3333333333333333148, 0.3333333333333334259, 0.3333333333333333703, 0.3333333333333333703, 0.3333333333333334259, 0.3333333333333333148, 0.3333333333333333703, 0.3333333333333332593, 0.3333333333333335369, 0.3333333333333333703, 0.3333333333333333148, 0.3333333333333334259, 0.3333333333333333703, 0.3333333333333333703, 0.3333333333333333148, 0.3333333333333333703, 0.3333333333333333703, 0.3333333333333334259, 0.3333333333333334259, 0.3333333333333334259, 0.3333333333333333703, 0.3333333333333333703, 0.3333333333333334259, 0.3333333333333333148, 0.3333333333333333703, 0.3333333333333334259, 0.3333333333333334259, 0.3333333333333332593, 0.3333333333333333703, 0.3333333333333334259, 0.3333333333333333703, 0.3333333333333334259, 0.3333333333333333148, 0.3333333333333334814, 0.3333333333333333148, 0.3333333333333332593, 0.3333333333333334259, 0.3333333333333333703, 0.3333333333333333148, 0.3333333333333333703, 0.3333333333333334259, 0.3333333333333334259, 0.3333333333333333148, 0.3333333333333333703, 0.3333333333333332593, 0.3333333333333333703, 0.3333333333333333703, 0.3333333333333333703, 0.3333333333333333703, 0.3333333333333333148, 0.3333333333333333703, 0.3333333333333333148, 0.3333333333333334259, 0.3333333333333333703, 0.3333333333333334259, 0.3333333333333333148, 0.3333333333333333703, 0.3333333333333333148, 0.3333333333333334259, 0.3333333333333333703, 0.3333333333333333703, 0.3333333333333333703, 0.3333333333333333703, 0.3333333333333333703, 0.3333333333333332593, 0.3333333333333333703, 0.3333333333333333703, 0.3333333333333335369, 0.3333333333333334259, 0.3333333333333333148, 0.3333333333333335369, 0.3333333333333333148, 0.3333333333333333703, 0.3333333333333333703, 0.3333333333333334259, 0.3333333333333333148, 0.3333333333333333703, 0.3333333333333334259, 0.3333333333333334259, 0.3333333333333333703, 0.3333333333333332593, 0.3333333333333334259, 0.3333333333333333703, 0.3333333333333334814, 0.3333333333333333148, 0.3333333333333333703, 0.3333333333333334259, 0.3333333333333333703, 0.3333333333333333148, 0.3333333333333333703, 0.3333333333333333148, 0.3333333333333334259, 0.3333333333333332593, 0.3333333333333334814, 0.3333333333333333703, 0.3333333333333334259, 0.3333333333333333703, 0.3333333333333333703, 0.3333333333333334259, 0.3333333333333333703, 0.3333333333333333703, 0.3333333333333333148, 0.3333333333333335924, 0.3333333333333333148, 0.3333333333333333703, 0.3333333333333334259, 0.3333333333333333148, 0.3333333333333334259, 0.3333333333333333148, 0.3333333333333334259, 0.3333333333333333703, 0.3333333333333334259, 0.3333333333333333703, 0.3333333333333333703, 0.3333333333333333703, 0.3333333333333334259, 0.3333333333333333703, 0.3333333333333334814, 0.3333333333333333148, 0.3333333333333334814, 0.3333333333333333148, 0.3333333333333333703, 0.3333333333333333148, 0.3333333333333333703, 0.3333333333333333703, 0.3333333333333333703, 0.3333333333333333703, 0.3333333333333333703, 0.3333333333333334259, 0.3333333333333333148, 0.3333333333333334259, 0.3333333333333333703, 0.3333333333333333703, 0.3333333333333333703, 0.3333333333333333703, 0.3333333333333333148, 0.3333333333333333703, 0.3333333333333334259, 0.3333333333333333148, 0.3333333333333334259, 0.3333333333333333148, 0.3333333333333333703, 0.3333333333333333703, 0.3333333333333333148, 0.3333333333333333703, 0.3333333333333334259, 0.3333333333333333148, 0.3333333333333334259, 0.3333333333333333703, 0.3333333333333332593, 0.3333333333333334814, 0.3333333333333332593, 0.3333333333333334259, 0.3333333333333333148, 0.3333333333333333703, 0.3333333333333334814, 0.3333333333333333703, 0.3333333333333333703, 0.3333333333333332593, 0.3333333333333334814, 0.3333333333333333148, 0.3333333333333333703, 0.3333333333333334259, 0.3333333333333333148, 0.3333333333333334259, 0.3333333333333333148, 0.3333333333333333703, 0.3333333333333333703, 0.3333333333333332593, 0.3333333333333333703, 0.3333333333333333703, 0.3333333333333334259, 0.3333333333333333148, 0.3333333333333334814, 0.3333333333333333703, 0.3333333333333334259, 0.3333333333333333148, 0.3333333333333334259, 0.3333333333333333703, 0.3333333333333333703, 0.3333333333333333703, 0.3333333333333333703, 0.3333333333333333148, 0.3333333333333334814, 0.3333333333333333703, 0.3333333333333333703, 0.3333333333333333148, 0.3333333333333334259, 0.3333333333333333703, 0.3333333333333332593, 0.3333333333333333703, 0.3333333333333333703, 0.3333333333333333703, 0.3333333333333334259, 0.3333333333333334259, 0.3333333333333333703, 0.3333333333333333703, 0.3333333333333333703, 0.3333333333333333703, 0.3333333333333334259, 0.3333333333333332593, 0.3333333333333335369, 0.3333333333333332038, 0.3333333333333333148, 0.3333333333333333703, 0.3333333333333333148, 0.3333333333333333148, 0.3333333333333334259, 0.3333333333333333703, 0.3333333333333333703, 0.3333333333333333703, 0.3333333333333334259, 0.3333333333333333148, 0.3333333333333334814, 0.3333333333333333703, 0.3333333333333334259, 0.3333333333333333703, 0.3333333333333333703, 0.3333333333333332593, 0.3333333333333333148, 0.3333333333333334814, 0.3333333333333333148, 0.3333333333333332593, 0.3333333333333334259, 0.3333333333333332038, 0.3333333333333334259, 0.3333333333333333148, 0.3333333333333333148, 0.3333333333333334259, 0.3333333333333333703, 0.3333333333333333703, 0.3333333333333333703, 0.3333333333333333703, 0.3333333333333334259, 0.3333333333333333148, 0.3333333333333333148, 0.3333333333333334259, 0.3333333333333333148, 0.3333333333333334259, 0.3333333333333333148, 0.3333333333333333703, 0.3333333333333334259, 0.3333333333333333148, 0.3333333333333334814, 0.3333333333333333148, 0.3333333333333334259, 0.3333333333333334259, 0.3333333333333333148, 0.3333333333333333148, 0.3333333333333335369, 0.3333333333333333148, 0.3333333333333333148, 0.3333333333333333703, 0.3333333333333335369, 0.3333333333333332593, 0.3333333333333335369, 0.3333333333333333148, 0.3333333333333333148, 0.3333333333333334259, 0.3333333333333333148, 0.3333333333333334259, 0.3333333333333333703, 0.3333333333333332593, 0.3333333333333333703, 0.3333333333333333148, 0.3333333333333334259, 0.3333333333333333148, 0.3333333333333334259, 0.3333333333333332593, 0.3333333333333335369, 0.3333333333333332038, 0.3333333333333334259, 0.3333333333333332593, 0.3333333333333335369, 0.3333333333333333148, 0.3333333333333334259, 0.3333333333333334259, 0.3333333333333333148, 0.3333333333333333148, 0.3333333333333334259, 0.3333333333333334814, 0.3333333333333333148, 0.3333333333333333148, 0.3333333333333334259, 0.3333333333333333703, 0.3333333333333334259, 0.3333333333333333148, 0.3333333333333333148, 0.3333333333333333703, 0.3333333333333333703, 0.3333333333333334814, 0.3333333333333333148, 0.3333333333333334259, 0.3333333333333333703, 0.3333333333333334259, 0.3333333333333334259, 0.3333333333333333148, 0.3333333333333333703, 0.3333333333333334259, 0.3333333333333333148, 0.3333333333333334814, 0.3333333333333333703, 0.3333333333333333148, 0.3333333333333333703, 0.3333333333333333148, 0.3333333333333334259, 0.3333333333333333148, 0.3333333333333333703, 0.3333333333333332593, 0.3333333333333334814, 0.3333333333333333703, 0.3333333333333334814, 0.3333333333333333148, 0.3333333333333334259, 0.3333333333333334814, 0.3333333333333333148, 0.3333333333333334259, 0.3333333333333332593, 0.3333333333333334259, 0.3333333333333333703, 0.3333333333333333703, 0.3333333333333333148, 0.3333333333333333148, 0.3333333333333334259, 0.3333333333333333148, 0.3333333333333334814, 0.3333333333333333148, 0.3333333333333335924, 0.3333333333333333148, 0.3333333333333334259, 0.3333333333333333148, 0.3333333333333333703, 0.3333333333333333703, 0.3333333333333334814, 0.3333333333333332593, 0.3333333333333333703, 0.3333333333333333703, 0.3333333333333334259, 0.3333333333333333148, 0.3333333333333334259, 0.3333333333333333703, 0.3333333333333333703, 0.3333333333333333703),
 ( 1.000000000000000222, 1.000000000000000222, 1.000000000000000222, 1.000000000000000000, 1.000000000000000000, 1.000000000000000444, 1.000000000000000000, 0.9999999999999997780, 1.000000000000000444, 0.9999999999999997780, 0.9999999999999997780, 1.000000000000000222, 0.9999999999999997780, 0.9999999999999997780, 1.000000000000000444, 0.9999999999999997780, 1.000000000000000222, 1.000000000000000222, 0.9999999999999996669, 1.000000000000000222, 0.9999999999999996669, 1.000000000000000444, 0.9999999999999994449, 1.000000000000000444, 0.9999999999999996669, 1.000000000000000222, 1.000000000000000000, 0.9999999999999997780, 1.000000000000000222, 0.9999999999999997780, 1.000000000000000000, 0.9999999999999997780, 1.000000000000000000, 1.000000000000000222, 0.9999999999999996669, 1.000000000000000000, 0.9999999999999997780, 1.000000000000000000, 1.000000000000000444, 0.9999999999999996669, 1.000000000000000222, 1.000000000000000000, 1.000000000000000222, 1.000000000000000222, 0.9999999999999997780, 0.9999999999999997780, 1.000000000000000222, 0.9999999999999997780, 1.000000000000000222, 0.9999999999999997780, 0.9999999999999997780, 0.9999999999999997780, 1.000000000000000444, 1.000000000000000000, 0.9999999999999997780, 1.000000000000000222, 1.000000000000000000, 1.000000000000000000, 0.9999999999999997780, 1.000000000000000222, 1.000000000000000000, 1.000000000000000000, 1.000000000000000222, 1.000000000000000000, 1.000000000000000000, 1.000000000000000000, 1.000000000000000222, 1.000000000000000000, 0.9999999999999997780, 1.000000000000000444, 1.000000000000000000, 0.9999999999999997780, 1.000000000000000000, 1.000000000000000222, 0.9999999999999997780, 1.000000000000000222, 0.9999999999999996669, 1.000000000000000222, 1.000000000000000000, 1.000000000000000000, 1.000000000000000000, 1.000000000000000222, 0.9999999999999997780, 1.000000000000000000, 1.000000000000000222, 0.9999999999999997780, 1.000000000000000000, 1.000000000000000000, 0.9999999999999996669, 1.000000000000000000, 1.000000000000000000, 1.000000000000000222, 1.000000000000000000, 0.9999999999999997780, 1.000000000000000222, 0.9999999999999996669, 1.000000000000000222, 0.9999999999999997780, 1.000000000000000000, 1.000000000000000000, 1.000000000000000222, 0.9999999999999996669, 1.000000000000000444, 1.000000000000000000, 0.9999999999999997780, 1.000000000000000000, 1.000000000000000000, 1.000000000000000222, 0.9999999999999997780, 1.000000000000000000, 1.000000000000000222, 1.000000000000000444, 1.000000000000000000, 1.000000000000000000, 1.000000000000000444, 1.000000000000000000, 0.9999999999999997780, 1.000000000000000222, 1.000000000000000000, 1.000000000000000000, 1.000000000000000000, 1.000000000000000000, 1.000000000000000000, 1.000000000000000000, 0.9999999999999996669, 1.000000000000000222, 0.9999999999999997780, 1.000000000000000222, 1.000000000000000000, 0.9999999999999997780, 1.000000000000000222, 0.9999999999999997780, 0.9999999999999997780, 0.9999999999999997780, 1.000000000000000000, 1.000000000000000000, 0.9999999999999996669, 1.000000000000000444, 1.000000000000000222, 1.000000000000000000, 1.000000000000000000, 1.000000000000000222, 1.000000000000000222, 1.000000000000000000, 1.000000000000000222, 0.9999999999999996669, 1.000000000000000444, 0.9999999999999997780, 0.9999999999999997780, 1.000000000000000444, 1.000000000000000000, 1.000000000000000222, 0.9999999999999997780, 1.000000000000000222, 1.000000000000000000, 1.000000000000000222, 1.000000000000000000, 1.000000000000000000, 0.9999999999999996669, 1.000000000000000444, 1.000000000000000000, 1.000000000000000222, 0.9999999999999997780, 1.000000000000000000, 1.000000000000000000, 1.000000000000000000, 1.000000000000000000, 0.9999999999999997780, 1.000000000000000000, 1.000000000000000000, 1.000000000000000000, 1.000000000000000222, 1.000000000000000222, 0.9999999999999997780, 1.000000000000000000, 1.000000000000000000, 0.9999999999999997780, 1.000000000000000000, 1.000000000000000000, 1.000000000000000000, 1.000000000000000000, 1.000000000000000444, 0.9999999999999997780, 1.000000000000000222, 0.9999999999999997780, 1.000000000000000000, 1.000000000000000222, 0.9999999999999997780, 1.000000000000000222, 1.000000000000000000, 1.000000000000000000, 1.000000000000000000, 1.000000000000000000, 0.9999999999999997780, 1.000000000000000000, 1.000000000000000000, 1.000000000000000000, 1.000000000000000000, 1.000000000000000000, 1.000000000000000222, 1.000000000000000000, 1.000000000000000222, 0.9999999999999997780, 1.000000000000000222, 0.9999999999999997780, 1.000000000000000222, 1.000000000000000000, 0.9999999999999997780, 1.000000000000000222, 0.9999999999999996669, 1.000000000000000444, 1.000000000000000000, 0.9999999999999996669, 1.000000000000000222, 1.000000000000000000, 1.000000000000000222, 0.9999999999999997780, 1.000000000000000444, 1.000000000000000000, 1.000000000000000000, 0.9999999999999997780, 1.000000000000000222, 1.000000000000000000, 1.000000000000000000, 1.000000000000000000, 1.000000000000000222, 0.9999999999999997780, 1.000000000000000222, 1.000000000000000000, 0.9999999999999997780, 1.000000000000000000, 0.9999999999999997780, 1.000000000000000222, 0.9999999999999996669, 1.000000000000000000, 1.000000000000000000, 1.000000000000000000, 1.000000000000000444, 1.000000000000000222, 1.000000000000000000, 1.000000000000000000, 0.9999999999999997780, 0.9999999999999997780, 1.000000000000000444, 0.9999999999999996669, 1.000000000000000444, 0.9999999999999997780, 0.9999999999999997780, 1.000000000000000222, 0.9999999999999997780, 0.9999999999999996669, 1.000000000000000444, 0.9999999999999997780, 1.000000000000000222, 1.000000000000000222, 1.000000000000000000, 0.9999999999999997780, 1.000000000000000222, 1.000000000000000000, 1.000000000000000222, 1.000000000000000000, 1.000000000000000000, 0.9999999999999997780, 0.9999999999999997780, 1.000000000000000444, 0.9999999999999997780, 0.9999999999999997780, 1.000000000000000222, 0.9999999999999994449, 1.000000000000000222, 0.9999999999999997780, 1.000000000000000000, 0.9999999999999997780, 1.000000000000000000, 1.000000000000000000, 1.000000000000000000, 1.000000000000000000, 1.000000000000000000, 1.000000000000000000, 1.000000000000000000, 1.000000000000000222, 1.000000000000000000, 1.000000000000000000, 1.000000000000000000, 1.000000000000000000, 1.000000000000000000, 1.000000000000000000, 1.000000000000000000, 1.000000000000000222, 1.000000000000000000, 1.000000000000000222, 0.9999999999999997780, 1.000000000000000000, 1.000000000000000444, 1.000000000000000000, 1.000000000000000000, 1.000000000000000000, 1.000000000000000222, 0.9999999999999997780, 1.000000000000000444, 0.9999999999999997780, 1.000000000000000222, 1.000000000000000000, 1.000000000000000000, 1.000000000000000000, 1.000000000000000222, 0.9999999999999994449, 1.000000000000000222, 1.000000000000000000, 1.000000000000000000, 1.000000000000000000, 0.9999999999999997780, 0.9999999999999997780, 1.000000000000000444, 0.9999999999999996669, 1.000000000000000222, 0.9999999999999997780, 1.000000000000000444, 0.9999999999999997780, 1.000000000000000222, 1.000000000000000222, 0.9999999999999996669, 1.000000000000000222, 1.000000000000000000, 1.000000000000000444, 1.000000000000000000, 1.000000000000000000, 1.000000000000000222, 1.000000000000000000, 1.000000000000000000, 0.9999999999999997780, 0.9999999999999997780, 1.000000000000000000, 0.9999999999999997780, 1.000000000000000222, 1.000000000000000222, 1.000000000000000000, 1.000000000000000222, 1.000000000000000222, 1.000000000000000000, 0.9999999999999997780, 0.9999999999999997780, 1.000000000000000222, 0.9999999999999997780, 1.000000000000000222, 1.000000000000000000, 1.000000000000000000, 1.000000000000000000, 0.9999999999999996669, 1.000000000000000222, 0.9999999999999997780, 1.000000000000000000, 0.9999999999999997780, 1.000000000000000222, 0.9999999999999997780, 1.000000000000000444, 0.9999999999999996669, 1.000000000000000222, 1.000000000000000222, 1.000000000000000000, 1.000000000000000000, 0.9999999999999997780, 1.000000000000000222, 0.9999999999999997780, 1.000000000000000222, 0.9999999999999997780, 0.9999999999999997780, 1.000000000000000000, 1.000000000000000000, 1.000000000000000222, 1.000000000000000000, 1.000000000000000444, 0.9999999999999997780, 1.000000000000000222, 0.9999999999999997780, 0.9999999999999997780, 1.000000000000000222, 1.000000000000000000, 0.9999999999999997780, 1.000000000000000000, 1.000000000000000000, 1.000000000000000000, 0.9999999999999997780, 1.000000000000000444, 0.9999999999999997780, 1.000000000000000000, 1.000000000000000000),
 ( 0.3333333333333334259, 0.3333333333333334259, 0.3333333333333333703, 0.3333333333333334259, 0.3333333333333334259, 0.3333333333333334259, 0.3333333333333334259, 0.3333333333333332593, 0.3333333333333335369, 0.3333333333333332593, 0.3333333333333333703, 0.3333333333333334259, 0.3333333333333333703, 0.3333333333333332593, 0.3333333333333334814, 0.3333333333333332593, 0.3333333333333334259, 0.3333333333333334259, 0.3333333333333332593, 0.3333333333333335369, 0.3333333333333332038, 0.3333333333333335369, 0.3333333333333331483, 0.3333333333333334814, 0.3333333333333333148, 0.3333333333333333703, 0.3333333333333333703, 0.3333333333333333148, 0.3333333333333333703, 0.3333333333333333148, 0.3333333333333333703, 0.3333333333333333703, 0.3333333333333333703, 0.3333333333333333703, 0.3333333333333333703, 0.3333333333333333703, 0.3333333333333333148, 0.3333333333333333148, 0.3333333333333334259, 0.3333333333333332593, 0.3333333333333334259, 0.3333333333333333148, 0.3333333333333334259, 0.3333333333333333703, 0.3333333333333333148, 0.3333333333333334259, 0.3333333333333333703, 0.3333333333333333703, 0.3333333333333334259, 0.3333333333333333148, 0.3333333333333333703, 0.3333333333333332593, 0.3333333333333335369, 0.3333333333333333703, 0.3333333333333333148, 0.3333333333333334259, 0.3333333333333333703, 0.3333333333333333703, 0.3333333333333333148, 0.3333333333333333703, 0.3333333333333333703, 0.3333333333333334259, 0.3333333333333334259, 0.3333333333333334259, 0.3333333333333333703, 0.3333333333333333703, 0.3333333333333334259, 0.3333333333333333148, 0.3333333333333333703, 0.3333333333333334259, 0.3333333333333334259, 0.3333333333333332593, 0.3333333333333333703, 0.3333333333333334259, 0.3333333333333333703, 0.3333333333333334259, 0.3333333333333333148, 0.3333333333333334814, 0.3333333333333333148, 0.3333333333333332593, 0.3333333333333334259, 0.3333333333333333703, 0.3333333333333333148, 0.3333333333333333703, 0.3333333333333334259, 0.3333333333333334259, 0.3333333333333333148, 0.3333333333333333703, 0.3333333333333332593, 0.3333333333333333703, 0.3333333333333333703, 0.3333333333333333703, 0.3333333333333333703, 0.3333333333333333148, 0.3333333333333333703, 0.3333333333333333148, 0.3333333333333334259, 0.3333333333333333703, 0.3333333333333334259, 0.3333333333333333148, 0.3333333333333333703, 0.3333333333333333148, 0.3333333333333334259, 0.3333333333333333703, 0.3333333333333333703, 0.3333333333333333703, 0.3333333333333333703, 0.3333333333333333703, 0.3333333333333332593, 0.3333333333333333703, 0.3333333333333333703, 0.3333333333333335369, 0.3333333333333334259, 0.3333333333333333148, 0.3333333333333335369, 0.3333333333333333148, 0.3333333333333333703, 0.3333333333333333703, 0.3333333333333334259, 0.3333333333333333148, 0.3333333333333333703, 0.3333333333333334259, 0.3333333333333334259, 0.3333333333333333703, 0.3333333333333332593, 0.3333333333333334259, 0.3333333333333333703, 0.3333333333333334814, 0.3333333333333333148, 0.3333333333333333703, 0.3333333333333334259, 0.3333333333333333703, 0.3333333333333333148, 0.3333333333333333703, 0.3333333333333333148, 0.3333333333333334259, 0.3333333333333332593, 0.3333333333333334814, 0.3333333333333333703, 0.3333333333333334259, 0.3333333333333333703, 0.3333333333333333703, 0.3333333333333334259, 0.3333333333333333703, 0.3333333333333333703, 0.3333333333333333148, 0.3333333333333335924, 0.3333333333333333148, 0.3333333333333333703, 0.3333333333333334259, 0.3333333333333333148, 0.3333333333333334259, 0.3333333333333333148, 0.3333333333333334259, 0.3333333333333333703, 0.3333333333333334259, 0.3333333333333333703, 0.3333333333333333703, 0.3333333333333333703, 0.3333333333333334259, 0.3333333333333333703, 0.3333333333333334814, 0.3333333333333333148, 0.3333333333333334814, 0.3333333333333333148, 0.3333333333333333703, 0.3333333333333333148, 0.3333333333333333703, 0.3333333333333333703, 0.3333333333333333703, 0.3333333333333333703, 0.3333333333333333703, 0.3333333333333334259, 0.3333333333333333148, 0.3333333333333334259, 0.3333333333333333703, 0.3333333333333333703, 0.3333333333333333703, 0.3333333333333333703, 0.3333333333333333148, 0.3333333333333333703, 0.3333333333333334259, 0.3333333333333333148, 0.3333333333333334259, 0.3333333333333333148, 0.3333333333333333703, 0.3333333333333333703, 0.3333333333333333148, 0.3333333333333333703, 0.3333333333333334259, 0.3333333333333333148, 0.3333333333333334259, 0.3333333333333333703, 0.3333333333333332593, 0.3333333333333334814, 0.3333333333333332593, 0.3333333333333334259, 0.3333333333333333148, 0.3333333333333333703, 0.3333333333333334814, 0.3333333333333333703, 0.3333333333333333703, 0.3333333333333332593, 0.3333333333333334814, 0.3333333333333333148, 0.3333333333333333703, 0.3333333333333334259, 0.3333333333333333148, 0.3333333333333334259, 0.3333333333333333148, 0.3333333333333333703, 0.3333333333333333703, 0.3333333333333332593, 0.3333333333333333703, 0.3333333333333333703, 0.3333333333333334259, 0.3333333333333333148, 0.3333333333333334814, 0.3333333333333333703, 0.3333333333333334259, 0.3333333333333333148, 0.3333333333333334259, 0.3333333333333333703, 0.3333333333333333703, 0.3333333333333333703, 0.3333333333333333703, 0.3333333333333333148, 0.3333333333333334814, 0.3333333333333333703, 0.3333333333333333703, 0.3333333333333333148, 0.3333333333333334259, 0.3333333333333333703, 0.3333333333333332593, 0.3333333333333333703, 0.3333333333333333703, 0.3333333333333333703, 0.3333333333333334259, 0.3333333333333334259, 0.3333333333333333703, 0.3333333333333333703, 0.3333333333333333703, 0.3333333333333333703, 0.3333333333333334259, 0.3333333333333332593, 0.3333333333333335369, 0.3333333333333332038, 0.3333333333333333148, 0.3333333333333333703, 0.3333333333333333148, 0.3333333333333333148, 0.3333333333333334259, 0.3333333333333333703, 0.3333333333333333703, 0.3333333333333333703, 0.3333333333333334259, 0.3333333333333333148, 0.3333333333333334814, 0.3333333333333333703, 0.3333333333333334259, 0.3333333333333333703, 0.3333333333333333703, 0.3333333333333332593, 0.3333333333333333148, 0.3333333333333334814, 0.3333333333333333148, 0.3333333333333332593, 0.3333333333333334259, 0.3333333333333332038, 0.3333333333333334259, 0.3333333333333333148, 0.3333333333333333148, 0.3333333333333334259, 0.3333333333333333703, 0.3333333333333333703, 0.3333333333333333703, 0.3333333333333333703, 0.3333333333333334259, 0.3333333333333333148, 0.3333333333333333148, 0.3333333333333334259, 0.3333333333333333148, 0.3333333333333334259, 0.3333333333333333148, 0.3333333333333333703, 0.3333333333333334259, 0.3333333333333333148, 0.3333333333333334814, 0.3333333333333333148, 0.3333333333333334259, 0.3333333333333334259, 0.3333333333333333148, 0.3333333333333333148, 0.3333333333333335369, 0.3333333333333333148, 0.3333333333333333148, 0.3333333333333333703, 0.3333333333333335369, 0.3333333333333332593, 0.3333333333333335369, 0.3333333333333333148, 0.3333333333333333148, 0.3333333333333334259, 0.3333333333333333148, 0.3333333333333334259, 0.3333333333333333703, 0.3333333333333332593, 0.3333333333333333703, 0.3333333333333333148, 0.3333333333333334259, 0.3333333333333333148, 0.3333333333333334259, 0.3333333333333332593, 0.3333333333333335369, 0.3333333333333332038, 0.3333333333333334259, 0.3333333333333332593, 0.3333333333333335369, 0.3333333333333333148, 0.3333333333333334259, 0.3333333333333334259, 0.3333333333333333148, 0.3333333333333333148, 0.3333333333333334259, 0.3333333333333334814, 0.3333333333333333148, 0.3333333333333333148, 0.3333333333333334259, 0.3333333333333333703, 0.3333333333333334259, 0.3333333333333333148, 0.3333333333333333148, 0.3333333333333333703, 0.3333333333333333703, 0.3333333333333334814, 0.3333333333333333148, 0.3333333333333334259, 0.3333333333333333703, 0.3333333333333334259, 0.3333333333333334259, 0.3333333333333333148, 0.3333333333333333703, 0.3333333333333334259, 0.3333333333333333148, 0.3333333333333334814, 0.3333333333333333703, 0.3333333333333333148, 0.3333333333333333703, 0.3333333333333333148, 0.3333333333333334259, 0.3333333333333333148, 0.3333333333333333703, 0.3333333333333332593, 0.3333333333333334814, 0.3333333333333333703, 0.3333333333333334814, 0.3333333333333333148, 0.3333333333333334259, 0.3333333333333334814, 0.3333333333333333148, 0.3333333333333334259, 0.3333333333333332593, 0.3333333333333334259, 0.3333333333333333703, 0.3333333333333333703, 0.3333333333333333148, 0.3333333333333333148, 0.3333333333333334259, 0.3333333333333333148, 0.3333333333333334814, 0.3333333333333333148, 0.3333333333333335924, 0.3333333333333333148, 0.3333333333333334259, 0.3333333333333333148, 0.3333333333333333703, 0.3333333333333333703, 0.3333333333333334814, 0.3333333333333332593, 0.3333333333333333703, 0.3333333333333333703, 0.3333333333333334259, 0.3333333333333333148, 0.3333333333333334259, 0.3333333333333333703, 0.3333333333333333703, 0.3333333333333333703),
 ( 0.3333333333333334259, 0.3333333333333334259, 0.3333333333333333703, 0.3333333333333334259, 0.3333333333333334259, 0.3333333333333334259, 0.3333333333333334259, 0.3333333333333332593, 0.3333333333333335369, 0.3333333333333332593, 0.3333333333333333703, 0.3333333333333334259, 0.3333333333333333703, 0.3333333333333332593, 0.3333333333333334814, 0.3333333333333332593, 0.3333333333333334259, 0.3333333333333334259, 0.3333333333333332593, 0.3333333333333335369, 0.3333333333333332038, 0.3333333333333335369, 0.3333333333333331483, 0.3333333333333334814, 0.3333333333333333148, 0.3333333333333333703, 0.3333333333333333703, 0.3333333333333333148, 0.3333333333333333703, 0.3333333333333333148, 0.3333333333333333703, 0.3333333333333333703, 0.3333333333333333703, 0.3333333333333333703, 0.3333333333333333703, 0.3333333333333333703, 0.3333333333333333148, 0.3333333333333333148, 0.3333333333333334259, 0.3333333333333332593, 0.3333333333333334259, 0.3333333333333333148, 0.3333333333333334259, 0.3333333333333333703, 0.3333333333333333148, 0.3333333333333334259, 0.3333333333333333703, 0.3333333333333333703, 0.3333333333333334259, 0.3333333333333333148, 0.3333333333333333703, 0.3333333333333332593, 0.3333333333333335369, 0.3333333333333333703, 0.3333333333333333148, 0.3333333333333334259, 0.3333333333333333703, 0.3333333333333333703, 0.3333333333333333148, 0.3333333333333333703, 0.3333333333333333703, 0.3333333333333334259, 0.3333333333333334259, 0.3333333333333334259, 0.3333333333333333703, 0.3333333333333333703, 0.3333333333333334259, 0.3333333333333333148, 0.3333333333333333703, 0.3333333333333334259, 0.3333333333333334259, 0.3333333333333332593, 0.3333333333333333703, 0.3333333333333334259, 0.3333333333333333703, 0.3333333333333334259, 0.3333333333333333148, 0.3333333333333334814, 0.3333333333333333148, 0.3333333333333332593, 0.3333333333333334259, 0.3333333333333333703, 0.3333333333333333148, 0.3333333333333333703, 0.3333333333333334259, 0.3333333333333334259, 0.3333333333333333148, 0.3333333333333333703, 0.3333333333333332593, 0.3333333333333333703, 0.3333333333333333703, 0.3333333333333333703, 0.3333333333333333703, 0.3333333333333333148, 0.3333333333333333703, 0.3333333333333333148, 0.3333333333333334259, 0.3333333333333333703, 0.3333333333333334259, 0.3333333333333333148, 0.3333333333333333703, 0.3333333333333333148, 0.3333333333333334259, 0.3333333333333333703, 0.3333333333333333703, 0.3333333333333333703, 0.3333333333333333703, 0.3333333333333333703, 0.3333333333333332593, 0.3333333333333333703, 0.3333333333333333703, 0.3333333333333335369, 0.3333333333333334259, 0.3333333333333333148, 0.3333333333333335369, 0.3333333333333333148, 0.3333333333333333703, 0.3333333333333333703, 0.3333333333333334259, 0.3333333333333333148, 0.3333333333333333703, 0.3333333333333334259, 0.3333333333333334259, 0.3333333333333333703, 0.3333333333333332593, 0.3333333333333334259, 0.3333333333333333703, 0.3333333333333334814, 0.3333333333333333148, 0.3333333333333333703, 0.3333333333333334259, 0.3333333333333333703, 0.3333333333333333148, 0.3333333333333333703, 0.3333333333333333148, 0.3333333333333334259, 0.3333333333333332593, 0.3333333333333334814, 0.3333333333333333703, 0.3333333333333334259, 0.3333333333333333703, 0.3333333333333333703, 0.3333333333333334259, 0.3333333333333333703, 0.3333333333333333703, 0.3333333333333333148, 0.3333333333333335924, 0.3333333333333333148, 0.3333333333333333703, 0.3333333333333334259, 0.3333333333333333148, 0.3333333333333334259, 0.3333333333333333148, 0.3333333333333334259, 0.3333333333333333703, 0.3333333333333334259, 0.3333333333333333703, 0.3333333333333333703, 0.3333333333333333703, 0.3333333333333334259, 0.3333333333333333703, 0.3333333333333334814, 0.3333333333333333148, 0.3333333333333334814, 0.3333333333333333148, 0.3333333333333333703, 0.3333333333333333148, 0.3333333333333333703, 0.3333333333333333703, 0.3333333333333333703, 0.3333333333333333703, 0.3333333333333333703, 0.3333333333333334259, 0.3333333333333333148, 0.3333333333333334259, 0.3333333333333333703, 0.3333333333333333703, 0.3333333333333333703, 0.3333333333333333703, 0.3333333333333333148, 0.3333333333333333703, 0.3333333333333334259, 0.3333333333333333148, 0.3333333333333334259, 0.3333333333333333148, 0.3333333333333333703, 0.3333333333333333703, 0.3333333333333333148, 0.3333333333333333703, 0.3333333333333334259, 0.3333333333333333148, 0.3333333333333334259, 0.3333333333333333703, 0.3333333333333332593, 0.3333333333333334814, 0.3333333333333332593, 0.3333333333333334259, 0.3333333333333333148, 0.3333333333333333703, 0.3333333333333334814, 0.3333333333333333703, 0.3333333333333333703, 0.3333333333333332593, 0.3333333333333334814, 0.3333333333333333148, 0.3333333333333333703, 0.3333333333333334259, 0.3333333333333333148, 0.3333333333333334259, 0.3333333333333333148, 0.3333333333333333703, 0.3333333333333333703, 0.3333333333333332593, 0.3333333333333333703, 0.3333333333333333703, 0.3333333333333334259, 0.3333333333333333148, 0.3333333333333334814, 0.3333333333333333703, 0.3333333333333334259, 0.3333333333333333148, 0.3333333333333334259, 0.3333333333333333703, 0.3333333333333333703, 0.3333333333333333703, 0.3333333333333333703, 0.3333333333333333148, 0.3333333333333334814, 0.3333333333333333703, 0.3333333333333333703, 0.3333333333333333148, 0.3333333333333334259, 0.3333333333333333703, 0.3333333333333332593, 0.3333333333333333703, 0.3333333333333333703, 0.3333333333333333703, 0.3333333333333334259, 0.3333333333333334259, 0.3333333333333333703, 0.3333333333333333703, 0.3333333333333333703, 0.3333333333333333703, 0.3333333333333334259, 0.3333333333333332593, 0.3333333333333335369, 0.3333333333333332038, 0.3333333333333333148, 0.3333333333333333703, 0.3333333333333333148, 0.3333333333333333148, 0.3333333333333334259, 0.3333333333333333703, 0.3333333333333333703, 0.3333333333333333703, 0.3333333333333334259, 0.3333333333333333148, 0.3333333333333334814, 0.3333333333333333703, 0.3333333333333334259, 0.3333333333333333703, 0.3333333333333333703, 0.3333333333333332593, 0.3333333333333333148, 0.3333333333333334814, 0.3333333333333333148, 0.3333333333333332593, 0.3333333333333334259, 0.3333333333333332038, 0.3333333333333334259, 0.3333333333333333148, 0.3333333333333333148, 0.3333333333333334259, 0.3333333333333333703, 0.3333333333333333703, 0.3333333333333333703, 0.3333333333333333703, 0.3333333333333334259, 0.3333333333333333148, 0.3333333333333333148, 0.3333333333333334259, 0.3333333333333333148, 0.3333333333333334259, 0.3333333333333333148, 0.3333333333333333703, 0.3333333333333334259, 0.3333333333333333148, 0.3333333333333334814, 0.3333333333333333148, 0.3333333333333334259, 0.3333333333333334259, 0.3333333333333333148, 0.3333333333333333148, 0.3333333333333335369, 0.3333333333333333148, 0.3333333333333333148, 0.3333333333333333703, 0.3333333333333335369, 0.3333333333333332593, 0.3333333333333335369, 0.3333333333333333148, 0.3333333333333333148, 0.3333333333333334259, 0.3333333333333333148, 0.3333333333333334259, 0.3333333333333333703, 0.3333333333333332593, 0.3333333333333333703, 0.3333333333333333148, 0.3333333333333334259, 0.3333333333333333148, 0.3333333333333334259, 0.3333333333333332593, 0.3333333333333335369, 0.3333333333333332038, 0.3333333333333334259, 0.3333333333333332593, 0.3333333333333335369, 0.3333333333333333148, 0.3333333333333334259, 0.3333333333333334259, 0.3333333333333333148, 0.3333333333333333148, 0.3333333333333334259, 0.3333333333333334814, 0.3333333333333333148, 0.3333333333333333148, 0.3333333333333334259, 0.3333333333333333703, 0.3333333333333334259, 0.3333333333333333148, 0.3333333333333333148, 0.3333333333333333703, 0.3333333333333333703, 0.3333333333333334814, 0.3333333333333333148, 0.3333333333333334259, 0.3333333333333333703, 0.3333333333333334259, 0.3333333333333334259, 0.3333333333333333148, 0.3333333333333333703, 0.3333333333333334259, 0.3333333333333333148, 0.3333333333333334814, 0.3333333333333333703, 0.3333333333333333148, 0.3333333333333333703, 0.3333333333333333148, 0.3333333333333334259, 0.3333333333333333148, 0.3333333333333333703, 0.3333333333333332593, 0.3333333333333334814, 0.3333333333333333703, 0.3333333333333334814, 0.3333333333333333148, 0.3333333333333334259, 0.3333333333333334814, 0.3333333333333333148, 0.3333333333333334259, 0.3333333333333332593, 0.3333333333333334259, 0.3333333333333333703, 0.3333333333333333703, 0.3333333333333333148, 0.3333333333333333148, 0.3333333333333334259, 0.3333333333333333148, 0.3333333333333334814, 0.3333333333333333148, 0.3333333333333335924, 0.3333333333333333148, 0.3333333333333334259, 0.3333333333333333148, 0.3333333333333333703, 0.3333333333333333703, 0.3333333333333334814, 0.3333333333333332593, 0.3333333333333333703, 0.3333333333333333703, 0.3333333333333334259, 0.3333333333333333148, 0.3333333333333334259, 0.3333333333333333703, 0.3333333333333333703, 0.3333333333333333703),
 ( 1.000000000000000222, 1.000000000000000222, 1.000000000000000222, 1.000000000000000000, 1.000000000000000000, 1.000000000000000444, 1.000000000000000000, 0.9999999999999997780, 1.000000000000000444, 0.9999999999999997780, 0.9999999999999997780, 1.000000000000000222, 0.9999999999999997780, 0.9999999999999997780, 1.000000000000000444, 0.9999999999999997780, 1.000000000000000222, 1.000000000000000222, 0.9999999999999996669, 1.000000000000000222, 0.9999999999999996669, 1.000000000000000444, 0.9999999999999994449, 1.000000000000000444, 0.9999999999999996669, 1.000000000000000222, 1.000000000000000000, 0.9999999999999997780, 1.000000000000000222, 0.9999999999999997780, 1.000000000000000000, 0.9999999999999997780, 1.000000000000000000, 1.000000000000000222, 0.9999999999999996669, 1.000000000000000000, 0.9999999999999997780, 1.000000000000000000, 1.000000000000000444, 0.9999999999999996669, 1.000000000000000222, 1.000000000000000000, 1.000000000000000222, 1.000000000000000222, 0.9999999999999997780, 0.9999999999999997780, 1.000000000000000222, 0.9999999999999997780, 1.000000000000000222, 0.9999999999999997780, 0.9999999999999997780, 0.9999999999999997780, 1.000000000000000444, 1.000000000000000000, 0.9999999999999997780, 1.000000000000000222, 1.000000000000000000, 1.000000000000000000, 0.9999999999999997780, 1.000000000000000222, 1.000000000000000000, 1.000000000000000000, 1.000000000000000222, 1.000000000000000000, 1.000000000000000000, 1.000000000000000000, 1.000000000000000222, 1.000000000000000000, 0.9999999999999997780, 1.000000000000000444, 1.000000000000000000, 0.9999999999999997780, 1.000000000000000000, 1.000000000000000222, 0.9999999999999997780, 1.000000000000000222, 0.9999999999999996669, 1.000000000000000222, 1.000000000000000000, 1.000000000000000000, 1.000000000000000000, 1.000000000000000222, 0.9999999999999997780, 1.000000000000000000, 1.000000000000000222, 0.9999999999999997780, 1.000000000000000000, 1.000000000000000000, 0.9999999999999996669, 1.000000000000000000, 1.000000000000000000, 1.000000000000000222, 1.000000000000000000, 0.9999999999999997780, 1.000000000000000222, 0.9999999999999996669, 1.000000000000000222, 0.9999999999999997780, 1.000000000000000000, 1.000000000000000000, 1.000000000000000222, 0.9999999999999996669, 1.000000000000000444, 1.000000000000000000, 0.9999999999999997780, 1.000000000000000000, 1.000000000000000000, 1.000000000000000222, 0.9999999999999997780, 1.000000000000000000, 1.000000000000000222, 1.000000000000000444, 1.000000000000000000, 1.000000000000000000, 1.000000000000000444, 1.000000000000000000, 0.9999999999999997780, 1.000000000000000222, 1.000000000000000000, 1.000000000000000000, 1.000000000000000000, 1.000000000000000000, 1.000000000000000000, 1.000000000000000000, 0.9999999999999996669, 1.000000000000000222, 0.9999999999999997780, 1.000000000000000222, 1.000000000000000000, 0.9999999999999997780, 1.000000000000000222, 0.9999999999999997780, 0.9999999999999997780, 0.9999999999999997780, 1.000000000000000000, 1.000000000000000000, 0.9999999999999996669, 1.000000000000000444, 1.000000000000000222, 1.000000000000000000, 1.000000000000000000, 1.000000000000000222, 1.000000000000000222, 1.000000000000000000, 1.000000000000000222, 0.9999999999999996669, 1.000000000000000444, 0.9999999999999997780, 0.9999999999999997780, 1.000000000000000444, 1.000000000000000000, 1.000000000000000222, 0.9999999999999997780, 1.000000000000000222, 1.000000000000000000, 1.000000000000000222, 1.000000000000000000, 1.000000000000000000, 0.9999999999999996669, 1.000000000000000444, 1.000000000000000000, 1.000000000000000222, 0.9999999999999997780, 1.000000000000000000, 1.000000000000000000, 1.000000000000000000, 1.000000000000000000, 0.9999999999999997780, 1.000000000000000000, 1.000000000000000000, 1.000000000000000000, 1.000000000000000222, 1.000000000000000222, 0.9999999999999997780, 1.000000000000000000, 1.000000000000000000, 0.9999999999999997780, 1.000000000000000000, 1.000000000000000000, 1.000000000000000000, 1.000000000000000000, 1.000000000000000444, 0.9999999999999997780, 1.000000000000000222, 0.9999999999999997780, 1.000000000000000000, 1.000000000000000222, 0.9999999999999997780, 1.000000000000000222, 1.000000000000000000, 1.000000000000000000, 1.000000000000000000, 1.000000000000000000, 0.9999999999999997780, 1.000000000000000000, 1.000000000000000000, 1.000000000000000000, 1.000000000000000000, 1.000000000000000000, 1.000000000000000222, 1.000000000000000000, 1.000000000000000222, 0.9999999999999997780, 1.000000000000000222, 0.9999999999999997780, 1.000000000000000222, 1.000000000000000000, 0.9999999999999997780, 1.000000000000000222, 0.9999999999999996669, 1.000000000000000444, 1.000000000000000000, 0.9999999999999996669, 1.000000000000000222, 1.000000000000000000, 1.000000000000000222, 0.9999999999999997780, 1.000000000000000444, 1.000000000000000000, 1.000000000000000000, 0.9999999999999997780, 1.000000000000000222, 1.000000000000000000, 1.000000000000000000, 1.000000000000000000, 1.000000000000000222, 0.9999999999999997780, 1.000000000000000222, 1.000000000000000000, 0.9999999999999997780, 1.000000000000000000, 0.9999999999999997780, 1.000000000000000222, 0.9999999999999996669, 1.000000000000000000, 1.000000000000000000, 1.000000000000000000, 1.000000000000000444, 1.000000000000000222, 1.000000000000000000, 1.000000000000000000, 0.9999999999999997780, 0.9999999999999997780, 1.000000000000000444, 0.9999999999999996669, 1.000000000000000444, 0.9999999999999997780, 0.9999999999999997780, 1.000000000000000222, 0.9999999999999997780, 0.9999999999999996669, 1.000000000000000444, 0.9999999999999997780, 1.000000000000000222, 1.000000000000000222, 1.000000000000000000, 0.9999999999999997780, 1.000000000000000222, 1.000000000000000000, 1.000000000000000222, 1.000000000000000000, 1.000000000000000000, 0.9999999999999997780, 0.9999999999999997780, 1.000000000000000444, 0.9999999999999997780, 0.9999999999999997780, 1.000000000000000222, 0.9999999999999994449, 1.000000000000000222, 0.9999999999999997780, 1.000000000000000000, 0.9999999999999997780, 1.000000000000000000, 1.000000000000000000, 1.000000000000000000, 1.000000000000000000, 1.000000000000000000, 1.000000000000000000, 1.000000000000000000, 1.000000000000000222, 1.000000000000000000, 1.000000000000000000, 1.000000000000000000, 1.000000000000000000, 1.000000000000000000, 1.000000000000000000, 1.000000000000000000, 1.000000000000000222, 1.000000000000000000, 1.000000000000000222, 0.9999999999999997780, 1.000000000000000000, 1.000000000000000444, 1.000000000000000000, 1.000000000000000000, 1.000000000000000000, 1.000000000000000222, 0.9999999999999997780, 1.000000000000000444, 0.9999999999999997780, 1.000000000000000222, 1.000000000000000000, 1.000000000000000000, 1.000000000000000000, 1.000000000000000222, 0.9999999999999994449, 1.000000000000000222, 1.000000000000000000, 1.000000000000000000, 1.000000000000000000, 0.9999999999999997780, 0.9999999999999997780, 1.000000000000000444, 0.9999999999999996669, 1.000000000000000222, 0.9999999999999997780, 1.000000000000000444, 0.9999999999999997780, 1.000000000000000222, 1.000000000000000222, 0.9999999999999996669, 1.000000000000000222, 1.000000000000000000, 1.000000000000000444, 1.000000000000000000, 1.000000000000000000, 1.000000000000000222, 1.000000000000000000, 1.000000000000000000, 0.9999999999999997780, 0.9999999999999997780, 1.000000000000000000, 0.9999999999999997780, 1.000000000000000222, 1.000000000000000222, 1.000000000000000000, 1.000000000000000222, 1.000000000000000222, 1.000000000000000000, 0.9999999999999997780, 0.9999999999999997780, 1.000000000000000222, 0.9999999999999997780, 1.000000000000000222, 1.000000000000000000, 1.000000000000000000, 1.000000000000000000, 0.9999999999999996669, 1.000000000000000222, 0.9999999999999997780, 1.000000000000000000, 0.9999999999999997780, 1.000000000000000222, 0.9999999999999997780, 1.000000000000000444, 0.9999999999999996669, 1.000000000000000222, 1.000000000000000222, 1.000000000000000000, 1.000000000000000000, 0.9999999999999997780, 1.000000000000000222, 0.9999999999999997780, 1.000000000000000222, 0.9999999999999997780, 0.9999999999999997780, 1.000000000000000000, 1.000000000000000000, 1.000000000000000222, 1.000000000000000000, 1.000000000000000444, 0.9999999999999997780, 1.000000000000000222, 0.9999999999999997780, 0.9999999999999997780, 1.000000000000000222, 1.000000000000000000, 0.9999999999999997780, 1.000000000000000000, 1.000000000000000000, 1.000000000000000000, 0.9999999999999997780, 1.000000000000000444, 0.9999999999999997780, 1.000000000000000000, 1.000000000000000000) ) ) 
 REPRESENTATION_ITEM ( '' )  SURFACE ( )  );
#146022=CARTESIAN_POINT ( 'NONE',  ( 5.479139036522528983, -1.730609802697373079, -0.8137914003483390779 ) ) ;
#146029=CARTESIAN_POINT ( 'NONE',  ( 0.5031362391596030381, -1.832460416942282011, 0.1798594046882526221 ) ) ;
#146032=CARTESIAN_POINT ( 'NONE',  ( 4.217926093758465278, -0.9595593063399066036, -1.605508702137818045 ) ) ;
#146033=CARTESIAN_POINT ( 'NONE',  ( -0.02299388927986567924, 0.7252709198883336983, -1.993311845943528837 ) ) ;
#146038=CARTESIAN_POINT ( 'NONE',  ( 1.446085390411493199, -0.8901679511373729037, 1.756898273940428634 ) ) ;
#146039=CARTESIAN_POINT ( 'NONE',  ( 2.196888872880573551, 1.802427395782604247, 0.9040921628407010413 ) ) ;
#146043=CARTESIAN_POINT ( 'NONE',  ( 2.185716925580234449, -0.9354795820612994417, 1.981881815340847730 ) ) ;
#146046=FACE_OUTER_BOUND ( 'NONE', #82457, .T. ) ;
#146053=CARTESIAN_POINT ( 'NONE',  ( 5.108874002337426390, -0.2646564886703614006, 1.822002613180016883 ) ) ;
#146054=CARTESIAN_POINT ( 'NONE',  ( 1.699859389132576837, 1.389752512480733060, 1.456620396263593520 ) ) ;
#146055=CARTESIAN_POINT ( 'NONE',  ( 3.691010296293754323, -1.365721494773973754, -1.848513781679576251 ) ) ;
#146057=CARTESIAN_POINT ( 'NONE',  ( 1.674410341579468442, 1.254762736130067502, -1.374450116433557856 ) ) ;
#146059=CARTESIAN_POINT ( 'NONE',  ( 5.537344615273096515, -0.04053095765194079242, 1.912125305397804009 ) ) ;
#146063=CARTESIAN_POINT ( 'NONE',  ( 4.950766902526997804, -1.767019275552136115, -1.117201988274316049 ) ) ;
#146064=CARTESIAN_POINT ( 'NONE',  ( 3.836663719693265584, 0.2738035037005565053, 1.850374562403465983 ) ) ;
#146066=CARTESIAN_POINT ( 'NONE',  ( 6.269096963164666469, 1.759884223096353173, -0.5412972069449849544 ) ) ;
#146070=CARTESIAN_POINT ( 'NONE',  ( 5.180183349501196410, -0.9537450585986576579, 1.436990496349071833 ) ) ;
#146072=CARTESIAN_POINT ( 'NONE',  ( 0.8263334968928169877, 0.7041814825227004082, -1.584920328518927279 ) ) ;
#146077=CARTESIAN_POINT ( 'NONE',  ( 4.381792451580825976, -2.079388800107518698, 0.6243644347086656499 ) ) ;
#146078=CARTESIAN_POINT ( 'NONE',  ( 3.334410585898534674, 1.781380905032422746, 0.3990451814587444024 ) ) ;
#146079=CARTESIAN_POINT ( 'NONE',  ( 0.8659734994756922433, -1.952832785578303199, 0.1866259229855101731 ) ) ;
#146080=CARTESIAN_POINT ( 'NONE',  ( 0.1404439707000069981, 0.8148842331482269996, 1.954324566802398744 ) ) ;
#146081=CARTESIAN_POINT ( 'NONE',  ( 0.5512257746139355152, -1.939593085364198721, -1.221404215731338283 ) ) ;
#146085=CARTESIAN_POINT ( 'NONE',  ( 2.508575005364023003, -2.114979441823850337, -0.1534387461676611220 ) ) ;
#146090=CARTESIAN_POINT ( 'NONE',  ( 0.6552395816744536194, 1.723207459482085202, -1.147090658606984892 ) ) ;
#146091=CARTESIAN_POINT ( 'NONE',  ( 6.983263157960360346, 2.057644363497754814, 2.260506123227977948 ) ) ;
#146093=CARTESIAN_POINT ( 'NONE',  ( 2.157158246434082827, 0.4899616716134093108, 2.166440146811992040 ) ) ;
#146095=CARTESIAN_POINT ( 'NONE',  ( 0.1769827672329090662, 1.709356359883105636, 1.537109589704383827 ) ) ;
#146097=CARTESIAN_POINT ( 'NONE',  ( 5.735237406732953680, -0.04512126716067199617, -2.062225806692425945 ) ) ;
#146102=CARTESIAN_POINT ( 'NONE',  ( 0.1331565106231363538, 0.2470099659030860484, -1.980838409567912572 ) ) ;
#146103=CARTESIAN_POINT ( 'NONE',  ( 5.917501325027624048, -1.028386522942719816, -1.527094029191010893 ) ) ;
#146106=CARTESIAN_POINT ( 'NONE',  ( 1.957592155046536941, 1.720466030779904454, -0.1226356519287794405 ) ) ;
#146107=CARTESIAN_POINT ( 'NONE',  ( 0.6730650033222317363, 1.776164188848127878, -0.9548607967814757291 ) ) ;
#146109=CARTESIAN_POINT ( 'NONE',  ( 2.706632988724329891, -0.8634771713065221288, -2.091333714195188431 ) ) ;
#146110=CARTESIAN_POINT ( 'NONE',  ( 4.389357127182037743, 1.881541760944308139, -0.9463713395347850277 ) ) ;
#146112=CARTESIAN_POINT ( 'NONE',  ( 2.670886861492921316, 0.09125233944726543478, -1.767527270347787116 ) ) ;
#146115=CARTESIAN_POINT ( 'NONE',  ( 5.109026413134919231, -0.3384823820529453964, 2.267118282965301379 ) ) ;
#146118=CARTESIAN_POINT ( 'NONE',  ( -0.1102773484824119410, -0.006951161900758255283, -2.203378182130751206 ) ) ;
#146119=CARTESIAN_POINT ( 'NONE',  ( 4.646525747415945595, -1.761044916313101671, 1.304081410864160739 ) ) ;
#146122=CARTESIAN_POINT ( 'NONE',  ( 6.621762855810419346, -0.4656160214656123730, 2.076383538966434017 ) ) ;
#146124=CARTESIAN_POINT ( 'NONE',  ( 3.158729500758109765, -1.458545141725621219, 1.258684350631077642 ) ) ;
#146127=CARTESIAN_POINT ( 'NONE',  ( 5.467072749063267345, -1.670387955228332277, 1.306269166133757986 ) ) ;
#146133=CARTESIAN_POINT ( 'NONE',  ( 6.567912610837368881, -1.126952994821692533, 1.456688911285822119 ) ) ;
#146137=CARTESIAN_POINT ( 'NONE',  ( 2.260927701655718103, 1.706565837815830822, -0.3407169315452397984 ) ) ;
#146142=CARTESIAN_POINT ( 'NONE',  ( 6.561405286136595905, 0.3748316153167965403, -2.128808860954830795 ) ) ;
#146145=CARTESIAN_POINT ( 'NONE',  ( 6.104392421991035711, -0.7735064434604683736, -2.018760209060527888 ) ) ;
#146149=CARTESIAN_POINT ( 'NONE',  ( 5.870382883074816149, -1.252475921811508019, 1.522319303672705848 ) ) ;
#146150=CARTESIAN_POINT ( 'NONE',  ( 5.096919866207451300, 0.8898786499993548427, -1.487894112255260692 ) ) ;
#146152=CARTESIAN_POINT ( 'NONE',  ( 1.874823134854076923, -0.1115055541827478930, -2.188858692977871279 ) ) ;
#146153=CARTESIAN_POINT ( 'NONE',  ( 3.030630200643165573, 1.283085264563757599, -1.917795831646688320 ) ) ;
#146154=CARTESIAN_POINT ( 'NONE',  ( 5.923136198411797615, -0.05496255519776967885, 2.060232511946280098 ) ) ;
#146155=CARTESIAN_POINT ( 'NONE',  ( 0.9724825242501096145, -0.04715749842807348546, -1.941539141333733953 ) ) ;
#146159=CARTESIAN_POINT ( 'NONE',  ( 4.254221937059123881, 0.9039275175388861161, -1.918405034562712830 ) ) ;
#146161=CARTESIAN_POINT ( 'NONE',  ( 2.285779929129946098, 1.617817622347239803, -1.203354541732377658 ) ) ;
#146163=CARTESIAN_POINT ( 'NONE',  ( 4.981566806912656631, 2.060606067865732527, -0.7902562557115796471 ) ) ;
#146169=CARTESIAN_POINT ( 'NONE',  ( 6.825078400183572036, 7.629137130509069387, 2.744348168701661095 ) ) ;
#146172=CARTESIAN_POINT ( 'NONE',  ( 4.996976137430897857, 1.714615628211055398, -1.143075302399678472 ) ) ;
#146174=CARTESIAN_POINT ( 'NONE',  ( 0.2331563151865486683, 0.005903526429595904942, -1.945944850731482934 ) ) ;
#146177=CARTESIAN_POINT ( 'NONE',  ( 3.422525317731230032, -0.8204878289409988090, -1.845699721510121183 ) ) ;
#146181=CARTESIAN_POINT ( 'NONE',  ( 2.518495319897054330, 1.347246837915631490, -1.559621528479130825 ) ) ;
#146182=CARTESIAN_POINT ( 'NONE',  ( 3.129529892704606020, 0.4926417352555876872, 1.955172657653013957 ) ) ;
#146187=CARTESIAN_POINT ( 'NONE',  ( 0.8140990769837243013, 1.700254657383609036, 0.7068247239481675326 ) ) ;
#146189=CARTESIAN_POINT ( 'NONE',  ( 6.410767893487317792, 1.638320036227768783, -1.478771730184471389 ) ) ;
#146191=CARTESIAN_POINT ( 'NONE',  ( 2.899875653925917174, -0.6810940995312758650, 2.051530325002319799 ) ) ;
#146193=CARTESIAN_POINT ( 'NONE',  ( 4.065693644434860587, 1.385821322041587145, 1.600864752689701076 ) ) ;
#146194=CARTESIAN_POINT ( 'NONE',  ( 2.829810162582825139, -1.586297295151902986, 1.663386555757565555 ) ) ;
#146197=CARTESIAN_POINT ( 'NONE',  ( 1.287742131874554552, -0.8442722623961744777, 1.669378388412197767 ) ) ;
#146198=CARTESIAN_POINT ( 'NONE',  ( 4.557473252141114983, 0.4328338235230348996, -1.923210603423119780 ) ) ;
#146199=CARTESIAN_POINT ( 'NONE',  ( 5.050017674172561755, 0.9981218692422781924, 1.752141108012375437 ) ) ;
#146203=CARTESIAN_POINT ( 'NONE',  ( 5.918611218600786650, 1.415673333675367296, -1.559471542009479350 ) ) ;
#146207=CARTESIAN_POINT ( 'NONE',  ( 6.539320575229274013, 2.055156488754609878, 2.310649141506931681 ) ) ;
#146208=CARTESIAN_POINT ( 'NONE',  ( 4.662937792257120684, -1.760523130880174314, -0.8874255463059472770 ) ) ;
#146209=CARTESIAN_POINT ( 'NONE',  ( 5.906511930418064438, -2.010445946205151380, -0.1936997237232794822 ) ) ;
#146211=CARTESIAN_POINT ( 'NONE',  ( 5.075001523147505189, -2.171532227461204556, -0.7813444033149226087 ) ) ;
#146213=CARTESIAN_POINT ( 'NONE',  ( 2.114201203919101157, 2.057314814202032771, -0.1476098556340669499 ) ) ;
#146220=CARTESIAN_POINT ( 'NONE',  ( 4.668535151219040280, -0.9243884330643321601, -1.964686384670484953 ) ) ;
#146223=CARTESIAN_POINT ( 'NONE',  ( 2.419273308677453826, -1.061688697878185206, -1.504126257600538974 ) ) ;
#146225=CARTESIAN_POINT ( 'NONE',  ( 6.620655732516659064, 6.039214117936751336, 2.421170424969817603 ) ) ;
#146226=CARTESIAN_POINT ( 'NONE',  ( 5.847271748948593029, 0.6375361197438635941, -2.096799129279611762 ) ) ;
#146228=CARTESIAN_POINT ( 'NONE',  ( 6.174757231500850096, -2.146110616029934803, -0.7165941539545512828 ) ) ;
#146233=CARTESIAN_POINT ( 'NONE',  ( 6.714108650864204719, -0.8368934294483711955, -1.559304158387794015 ) ) ;
#146234=CARTESIAN_POINT ( 'NONE',  ( 4.195951375888273382, 1.316525029674735947, 1.522990447314742424 ) ) ;
#146236=CARTESIAN_POINT ( 'NONE',  ( 3.083145409929681335, -0.1532580487927890645, -2.100430568508942830 ) ) ;
#146237=CARTESIAN_POINT ( 'NONE',  ( 2.196773704658647297, 1.712196953037805613, 0.8591283806286521552 ) ) ;
#146240=CARTESIAN_POINT ( 'NONE',  ( 2.928127725102438461, 1.051234477803453027, 1.665338043752979447 ) ) ;
#146241=CARTESIAN_POINT ( 'NONE',  ( 1.393192293617943944, 1.414286473764417185, 1.224485199485196629 ) ) ;
#146242=CARTESIAN_POINT ( 'NONE',  ( 2.154674626568295892, -0.5202524484802829585, -1.891573884155263396 ) ) ;
#146243=CARTESIAN_POINT ( 'NONE',  ( 3.703458238649427692, -0.4988927697323896071, 1.651148375757867326 ) ) ;
#146244=CARTESIAN_POINT ( 'NONE',  ( 0.8262462788446511830, -0.8622288892402606431, -1.707089296137359158 ) ) ;
#146246=CARTESIAN_POINT ( 'NONE',  ( 1.313402753022639091, 1.947697196196996217, 1.037691534346518729 ) ) ;
#146249=CARTESIAN_POINT ( 'NONE',  ( 6.702024585102262400, -1.870183347854617262, 0.04844413084104796929 ) ) ;
#146254=CARTESIAN_POINT ( 'NONE',  ( 6.702015291077846548, 0.7979701500827086624, -1.910492173269620508 ) ) ;
#146256=CARTESIAN_POINT ( 'NONE',  ( 0.5376586404672692998, 1.932363751568724641, -0.7437053376125392079 ) ) ;
#146261=CARTESIAN_POINT ( 'NONE',  ( 5.707716976326653757, 1.605689621071492601, 1.385122894465253607 ) ) ;
#146267=CARTESIAN_POINT ( 'NONE',  ( 6.637165056451467038, -0.09505199798197358496, -1.959668910398344233 ) ) ;
#146269=CARTESIAN_POINT ( 'NONE',  ( 4.042342166264912606, 1.899327733865596946, -0.6766104081444987983 ) ) ;
#146270=CARTESIAN_POINT ( 'NONE',  ( 3.749167220118687638, 0.2288279286139145163, -1.901904479094515210 ) ) ;
#146273=CARTESIAN_POINT ( 'NONE',  ( 1.857222401600963302, 0.3706860215506869727, -2.159823580554325329 ) ) ;
#146274=CARTESIAN_POINT ( 'NONE',  ( 0.1335669894368813060, 0.6916768264315333870, -2.234939561487662818 ) ) ;
#146276=CARTESIAN_POINT ( 'NONE',  ( 4.728775500204083215, 1.385159600073909258, -1.461172115097974622 ) ) ;
#146279=CARTESIAN_POINT ( 'NONE',  ( 5.677400705446850715, 1.603760038662904286, 1.382376383168891998 ) ) ;
#146281=CARTESIAN_POINT ( 'NONE',  ( 1.927394988521138774, -1.368145043076029133, -1.581016005797744262 ) ) ;
#146283=CARTESIAN_POINT ( 'NONE',  ( 0.3402809042804251227, 0.2871511109263942818, 1.700534619074739906 ) ) ;
#146294=CARTESIAN_POINT ( 'NONE',  ( 2.156637704053586901, 0.3978940469637832766, 1.767043172555267772 ) ) ;
#146298=CARTESIAN_POINT ( 'NONE',  ( 6.639320575229249677, 4.701313753536039641, 2.359456658813867236 ) ) ;
#146302=CARTESIAN_POINT ( 'NONE',  ( 3.349909636924102596, -0.7564274094383013347, 1.700591413421480125 ) ) ;
#146303=CARTESIAN_POINT ( 'NONE',  ( 0.08730790862205867198, -0.5103928513382477439, 1.846301284274171728 ) ) ;
#146304=CARTESIAN_POINT ( 'NONE',  ( 6.792047303494690880, -0.8216981310003536043, 1.740383667632472875 ) ) ;
#146309=CARTESIAN_POINT ( 'NONE',  ( 4.205875300247041260, 0.6677108253347485700, -1.852911535531636789 ) ) ;
#146313=CARTESIAN_POINT ( 'NONE',  ( 0.3223637989299525941, 2.001183132641819906, 0.6049928108779398794 ) ) ;
#146315=CARTESIAN_POINT ( 'NONE',  ( 5.877940811483009398, 1.147681995895684315, 1.547064007116766060 ) ) ;
#146318=CARTESIAN_POINT ( 'NONE',  ( 1.946200625105892312, 0.8427435547867198062, -2.039832142532324255 ) ) ;
#146320=CARTESIAN_POINT ( 'NONE',  ( 0.3692113334803036606, -1.616751421056546789, -1.021125667832627260 ) ) ;
#146323=CARTESIAN_POINT ( 'NONE',  ( 0.2034765232073352526, -1.520001300341488948, -1.252246736068510335 ) ) ;
#146324=CARTESIAN_POINT ( 'NONE',  ( 1.628360684195095054, 0.1923838640373880249, 1.932526033267305765 ) ) ;
#146325=CARTESIAN_POINT ( 'NONE',  ( 0.6321852052597470850, 0.2004073784105386835, -2.006138679842318862 ) ) ;
#146327=CARTESIAN_POINT ( 'NONE',  ( 5.981279135395962676, -0.04703572473597864706, 1.860536724379359574 ) ) ;
#146334=CARTESIAN_POINT ( 'NONE',  ( 1.347511689332027807, 0.6317163119916607839, -2.098556723903362009 ) ) ;
#146339=CARTESIAN_POINT ( 'NONE',  ( 1.242498012622397674, 0.3540479964400863877, 1.790853789395550955 ) ) ;
#146343=CARTESIAN_POINT ( 'NONE',  ( 6.609000000000036401, 0.5823242425131782696, 2.053003180352876100 ) ) ;
#146346=CARTESIAN_POINT ( 'NONE',  ( 0.4340449649811276012, 0.9916047912509761142, -1.651568591070247116 ) ) ;
#146347=CARTESIAN_POINT ( 'NONE',  ( 4.539869136473917877, 1.278287603951251183, 1.488235606430035274 ) ) ;
#146350=CARTESIAN_POINT ( 'NONE',  ( 4.493798347139664529, -2.191065130646638437, -0.05333993539427539510 ) ) ;
#146352=CARTESIAN_POINT ( 'NONE',  ( 6.609000000000034625, 7.052688111495289291, 2.598153854230552895 ) ) ;
#146353=CARTESIAN_POINT ( 'NONE',  ( 4.012602964903419611, 0.7404812365185129419, 1.933494928807255375 ) ) ;
#146357=CARTESIAN_POINT ( 'NONE',  ( 3.674713919220749414, 1.665813291469726787, 1.584223201981638685 ) ) ;
#146361=CARTESIAN_POINT ( 'NONE',  ( 6.620655732516652847, 2.468432086671234149, 2.210906647470804565 ) ) ;
#146363=CARTESIAN_POINT ( 'NONE',  ( 3.275267064432846098, 1.232403799581788251, 1.500778006584954749 ) ) ;
#146366=CARTESIAN_POINT ( 'NONE',  ( 5.115449499555525747, 1.566912803841558732, 1.096118974231160781 ) ) ;
#146367=CARTESIAN_POINT ( 'NONE',  ( 4.664925512212582781, -1.541612441252750543, -0.7736475682248912245 ) ) ;
#146368=CARTESIAN_POINT ( 'NONE',  ( 4.469935555517978720, -0.9463019959239076240, 1.780667052345537238 ) ) ;
#146369=CARTESIAN_POINT ( 'NONE',  ( 5.432396523169654934, -1.810675156642663541, -1.416092387804610553 ) ) ;
#146371=CARTESIAN_POINT ( 'NONE',  ( 0.3291288957359936318, 2.113116833900237967, 0.6364493931270903682 ) ) ;
#146374=CARTESIAN_POINT ( 'NONE',  ( 6.380137019068807369, -0.9445444496645590826, 1.496399839161892897 ) ) ;
#146375=CARTESIAN_POINT ( 'NONE',  ( 4.465470312728934132, -1.956561007648183192, -0.4872041746135646889 ) ) ;
#146377=CARTESIAN_POINT ( 'NONE',  ( 2.150677785613893889, -1.770481577899532644, 1.455972101185269985 ) ) ;
#146378=CARTESIAN_POINT ( 'NONE',  ( 1.481926975991064710, -0.2526488567047910361, -1.721760536436983680 ) ) ;
#146381=CARTESIAN_POINT ( 'NONE',  ( 1.053531109644106678, 1.532759392139435128, -0.8104334526845609066 ) ) ;
#146384=CARTESIAN_POINT ( 'NONE',  ( 1.434277768017662824, 1.292756205793591517, 1.744237601605197252 ) ) ;
#146385=CARTESIAN_POINT ( 'NONE',  ( 2.624232735793774030, 2.001858099149746550, 0.2420302859193757539 ) ) ;
#146387=CARTESIAN_POINT ( 'NONE',  ( 0.2527871956496882122, -1.549381263408876830, 1.144551880545265465 ) ) ;
#146389=CARTESIAN_POINT ( 'NONE',  ( 2.180208177693909288, 2.177553952664741388, -0.4384792121874846460 ) ) ;
#146396=CARTESIAN_POINT ( 'NONE',  ( 5.144012499716256848, 0.5123920008897012712, 1.663301317158589754 ) ) ;
#146397=CARTESIAN_POINT ( 'NONE',  ( 3.262109210011232108, -1.959739898415867154, 0.09363895518171151677 ) ) ;
#146402=CARTESIAN_POINT ( 'NONE',  ( 4.183118113821016948, -0.2165105290278953043, -2.252005913828499573 ) ) ;
#146405=CARTESIAN_POINT ( 'NONE',  ( 0.8892172652632176488, 0.1500229334146038762, 2.057259515242230830 ) ) ;
#146407=CARTESIAN_POINT ( 'NONE',  ( 2.149658728627835469, -1.817393572686412107, -1.347411789871997057 ) ) ;
#146408=EDGE_LOOP ( 'NONE', ( #90662, #19131 ) ) ;
#146410=CARTESIAN_POINT ( 'NONE',  ( 3.462029368274913477, 0.8381641302350505418, 1.672297462726477946 ) ) ;
#146411=CARTESIAN_POINT ( 'NONE',  ( 1.968989728591052479, -1.700769290752032870, -0.3374826141460812168 ) ) ;
#146412=CARTESIAN_POINT ( 'NONE',  ( 5.970311429539967740, -2.080533979117826782, -0.6889730390344513955 ) ) ;
#146413=CARTESIAN_POINT ( 'NONE',  ( 0.09513611692719620150, -0.4880922032983874281, -2.160105283315365998 ) ) ;
#146414=CARTESIAN_POINT ( 'NONE',  ( 4.206063578812153203, -2.156103337031569200, 0.1562769059922017589 ) ) ;
#146415=CARTESIAN_POINT ( 'NONE',  ( 4.417874594837376101, 1.193482090904834925, -1.531842204047480616 ) ) ;
#146419=CARTESIAN_POINT ( 'NONE',  ( 0.1249994045006353610, -2.052053476427470269, 7.016016019767730053E-15 ) ) ;
#146423=CARTESIAN_POINT ( 'NONE',  ( 6.047500043413473136, -1.423963828944514010, 1.427935028000301809 ) ) ;
#146427=CARTESIAN_POINT ( 'NONE',  ( 2.824607995650964209, 1.719152210223941823, 0.6149139946348627372 ) ) ;
#146434=CARTESIAN_POINT ( 'NONE',  ( 0.2112021888033519534, 1.676852382702203714, -1.125601893279993160 ) ) ;
#146435=CARTESIAN_POINT ( 'NONE',  ( 0.6453774867190856801, 0.1600191834128759094, 2.114519675249281416 ) ) ;
#146440=CARTESIAN_POINT ( 'NONE',  ( 0.1456854043008250221, -1.672057201651616642, -1.369741535119282982 ) ) ;
#146441=CARTESIAN_POINT ( 'NONE',  ( 5.889296118903345700, -0.7283762112263308941, -1.880435897373772258 ) ) ;
#146449=CARTESIAN_POINT ( 'NONE',  ( 6.749375321999433908, -1.976647572034227140, -0.3960365597561604778 ) ) ;
#146450=CARTESIAN_POINT ( 'NONE',  ( 4.136529068399773301, -1.600833271991594531, 0.9093273525555561898 ) ) ;
#146451=CARTESIAN_POINT ( 'NONE',  ( 0.07700591528352926374, 4.093948292925152721, -2.465843965391618209 ) ) ;
#146452=CARTESIAN_POINT ( 'NONE',  ( 3.616130377633751003, -2.273733826016415716, 0.3936331181264277612 ) ) ;
#146454=CARTESIAN_POINT ( 'NONE',  ( 5.729794944320468097, -1.366427417996706417, -1.674954217032841974 ) ) ;
#146456=CARTESIAN_POINT ( 'NONE',  ( 1.294366139777222369, 1.586748096885544745, -1.119478687268110173 ) ) ;
#146459=CARTESIAN_POINT ( 'NONE',  ( 4.815913765717094286, -1.849969270989433534, 1.363755144342413850 ) ) ;
#146462=CARTESIAN_POINT ( 'NONE',  ( 4.750782166719051069, -1.502237938222051650, 1.114538048626475986 ) ) ;
#146463=CARTESIAN_POINT ( 'NONE',  ( 1.388764059443419407, -1.816923020173771830, -0.5969786173363604842 ) ) ;
#146466=CARTESIAN_POINT ( 'NONE',  ( 3.141465813989018141, -1.946189201368169641, 1.040519825639886431 ) ) ;
#146471=CARTESIAN_POINT ( 'NONE',  ( 1.247272744223869356, -1.551563771690873006, -1.215972028847669417 ) ) ;
#146472=CARTESIAN_POINT ( 'NONE',  ( 0.7280630558558630616, -2.190032360377992315, 0.7273814547973026512 ) ) ;
#146473=CARTESIAN_POINT ( 'NONE',  ( 3.086327779807009009, 1.092107249913790712, -1.629585102321646328 ) ) ;
#146475=CARTESIAN_POINT ( 'NONE',  ( 5.172745336439665387, 1.426162745032448109, -1.490257803364034128 ) ) ;
#146482=CARTESIAN_POINT ( 'NONE',  ( 0.7433368588017514877, -0.2641965325859591540, -2.154838077344235714 ) ) ;
#146487=CARTESIAN_POINT ( 'NONE',  ( 2.653401028632852654, 0.5028369177751991215, -1.801603059227441239 ) ) ;
#146488=CARTESIAN_POINT ( 'NONE',  ( 6.907524304660562109, -0.4813806915026208055, 2.115094849305596103 ) ) ;
#146490=CARTESIAN_POINT ( 'NONE',  ( 6.727182134110196721, 2.084960209934753284, 2.120171393779949565 ) ) ;
#146493=CARTESIAN_POINT ( 'NONE',  ( 2.719282321824310511, 1.616554633311767297, 1.021241153818429614 ) ) ;
#146495=CARTESIAN_POINT ( 'NONE',  ( 3.801397759637317186, -0.5140543387622575899, 1.693523888807080047 ) ) ;
#146496=CARTESIAN_POINT ( 'NONE',  ( 1.857924044808876296, 0.7306008629870773818, -1.767408594711167735 ) ) ;
#146500=CARTESIAN_POINT ( 'NONE',  ( 5.765228759176680207, 1.768025090248021902, -0.7378185885129113775 ) ) ;
#146501=CARTESIAN_POINT ( 'NONE',  ( 6.760212172060996672, -1.969150147884619173, 0.04690145372830689663 ) ) ;
#146503=CARTESIAN_POINT ( 'NONE',  ( 2.215225606797793567, 1.700350911433265555, -1.266953333846132512 ) ) ;
#146505=CARTESIAN_POINT ( 'NONE',  ( 5.559403950928493821, 0.3636877230743483236, -1.834782481876767291 ) ) ;
#146506=CARTESIAN_POINT ( 'NONE',  ( 0.3811277156573149583, 1.704729334087114578, -0.6539457117896373406 ) ) ;
#146508=CARTESIAN_POINT ( 'NONE',  ( 4.617920694193921705, -2.164688156338661962, 0.4286357439418769788 ) ) ;
#146511=CARTESIAN_POINT ( 'NONE',  ( 1.926308760915905527, 1.058537693354057785, 1.770204612073868145 ) ) ;
#146520=CARTESIAN_POINT ( 'NONE',  ( 4.475093801846619535, 1.891600172242546840, 0.8420093967692193759 ) ) ;
#146522=CARTESIAN_POINT ( 'NONE',  ( 1.177287030172860183, -0.05180490295666683592, -2.161124318685260004 ) ) ;
#146524=CARTESIAN_POINT ( 'NONE',  ( 2.139325021376851765, 0.002241307429765720949, 2.019862492052142855 ) ) ;
#146533=CARTESIAN_POINT ( 'NONE',  ( 0.5324358445358172709, 0.5899921999869184308, 1.928256190492839028 ) ) ;
#146534=CARTESIAN_POINT ( 'NONE',  ( 5.372676843235411503, -0.05303982195071360595, -2.191091664329389399 ) ) ;
#146536=CARTESIAN_POINT ( 'NONE',  ( 5.203337695038355193, 1.683698669361912259, -0.9069238330124268499 ) ) ;
#146540=CARTESIAN_POINT ( 'NONE',  ( 2.689077551358230789, 1.704951624378052033, 1.076298511635757738 ) ) ;
#146543=CARTESIAN_POINT ( 'NONE',  ( 0.5918695612782381987, -0.8180161699140885423, 2.141640516796620375 ) ) ;
#146545=CARTESIAN_POINT ( 'NONE',  ( 5.315364200056264643, -0.2495996188201006494, 1.706489999720143480 ) ) ;
#146552=CARTESIAN_POINT ( 'NONE',  ( 5.619718922174004483, -0.4339147374951453084, 1.758609293272636487 ) ) ;
#146555=CARTESIAN_POINT ( 'NONE',  ( 5.637325938770506362, -0.03788160184842354061, 1.811251791611239170 ) ) ;
#146558=CARTESIAN_POINT ( 'NONE',  ( 3.380998015235132215, 1.981133383611884735, -0.9370748116589098231 ) ) ;
#146560=CARTESIAN_POINT ( 'NONE',  ( 0.9769180011504545735, 1.811320799089161993, 0.7541596914439269161 ) ) ;
#146563=CARTESIAN_POINT ( 'NONE',  ( 4.112823271221511590, 0.09766498815510017695, 1.913256991299339793 ) ) ;
#146570=CARTESIAN_POINT ( 'NONE',  ( 1.710078970767275885, -2.145365142986368934, 0.2646356489638818088 ) ) ;
#146573=CARTESIAN_POINT ( 'NONE',  ( 1.887459117809231701, 1.256508940344562397, 1.324596713471258402 ) ) ;
#146575=CARTESIAN_POINT ( 'NONE',  ( 3.733261478165556646, -1.687024869733319221, 0.6981082995600741414 ) ) ;
#146578=CARTESIAN_POINT ( 'NONE',  ( 2.496234081663367022, -0.9796988711565941532, 1.642222327643327873 ) ) ;
#146580=CARTESIAN_POINT ( 'NONE',  ( 3.297268302959563524, -1.738273807845453600, 0.9259864402798111405 ) ) ;
#146582=CARTESIAN_POINT ( 'NONE',  ( 4.599131018191075171, -0.5143685224620330176, 1.872658368587260647 ) ) ;
#146586=CARTESIAN_POINT ( 'NONE',  ( 5.765915565743810589, 0.6138260544302427402, -2.029845472315944921 ) ) ;
#146591=CARTESIAN_POINT ( 'NONE',  ( 4.424480750451430744, -0.8629065238535367222, -1.818916818396177026 ) ) ;
#146593=CARTESIAN_POINT ( 'NONE',  ( 5.057177669875371429, -1.544152220135000420, -0.9737345633797565014 ) ) ;
#146594=CARTESIAN_POINT ( 'NONE',  ( 1.223191768902037957, -1.870915810643185795, -0.8869332102946840823 ) ) ;
#146598=CARTESIAN_POINT ( 'NONE',  ( 5.348468966913380029, 0.5439794105128460400, 1.789823788735760646 ) ) ;
#146606=CARTESIAN_POINT ( 'NONE',  ( 1.727480438796034745, 0.1563249218069600044, -2.064440809470533544 ) ) ;
#146607=( BOUNDED_SURFACE ( )  B_SPLINE_SURFACE ( 3, 3, ( 
 ( #136447, #188364, #40004, #20528, #106113, #54118, #155883, #3194, #186229, #169983 ),
 ( #152677, #119172, #4260, #102866, #25858, #9615, #76741, #45338, #42148, #8549 ),
 ( #110394, #111457, #109334, #75692, #140735, #127737, #142862, #207807, #94101, #141803 ),
 ( #43217, #59436, #58376, #158027, #159074, #30139, #125593, #178528, #176399, #175344 ),
 ( #206747, #191553, #126654, #124532, #128783, #26924, #28004, #93033, #174284, #193694 ),
 ( #160140, #12797, #10670, #208865, #143936, #108262, #209931, #91970, #60495, #192620 ),
 ( #44273, #177461, #78870, #11739, #77814, #61569, #29076, #95160, #161210, #144992 ) ),
 .UNSPECIFIED., .T., .F., .T. ) 
 B_SPLINE_SURFACE_WITH_KNOTS ( ( 4, 3, 4 ),
 ( 4, 1, 1, 1, 1, 1, 1, 4 ),
 ( 0.000000000000000000, 0.5000000000000000000, 1.000000000000000000 ),
 ( 0.000000000000000000, 0.09599525230796020214, 0.1893027314675523320, 0.2592390727089966540, 0.3619855251144610819, 0.5211967264240887632, 0.7336899926499302893, 1.000000000000000000 ),
 .UNSPECIFIED. ) 
 GEOMETRIC_REPRESENTATION_ITEM ( )  RATIONAL_B_SPLINE_SURFACE ( (
 ( 1.000000000000000222, 1.000000000000000222, 0.9999999999999997780, 1.000000000000000444, 1.000000000000000222, 1.000000000000000222, 1.000000000000000222, 1.000000000000000222, 1.000000000000000222, 1.000000000000000222),
 ( 0.3333333333333334259, 0.3333333333333334259, 0.3333333333333333148, 0.3333333333333335369, 0.3333333333333334259, 0.3333333333333333703, 0.3333333333333334259, 0.3333333333333333703, 0.3333333333333334259, 0.3333333333333334259),
 ( 0.3333333333333334259, 0.3333333333333334259, 0.3333333333333333148, 0.3333333333333335369, 0.3333333333333334259, 0.3333333333333333703, 0.3333333333333334259, 0.3333333333333333703, 0.3333333333333334259, 0.3333333333333334259),
 ( 1.000000000000000222, 1.000000000000000222, 0.9999999999999997780, 1.000000000000000444, 1.000000000000000222, 1.000000000000000222, 1.000000000000000222, 1.000000000000000222, 1.000000000000000222, 1.000000000000000222),
 ( 0.3333333333333334259, 0.3333333333333334259, 0.3333333333333333148, 0.3333333333333335369, 0.3333333333333334259, 0.3333333333333333703, 0.3333333333333334259, 0.3333333333333333703, 0.3333333333333334259, 0.3333333333333334259),
 ( 0.3333333333333334259, 0.3333333333333334259, 0.3333333333333333148, 0.3333333333333335369, 0.3333333333333334259, 0.3333333333333333703, 0.3333333333333334259, 0.3333333333333333703, 0.3333333333333334259, 0.3333333333333334259),
 ( 1.000000000000000222, 1.000000000000000222, 0.9999999999999997780, 1.000000000000000444, 1.000000000000000222, 1.000000000000000222, 1.000000000000000222, 1.000000000000000222, 1.000000000000000222, 1.000000000000000222) ) ) 
 REPRESENTATION_ITEM ( '' )  SURFACE ( )  );
#146608=CARTESIAN_POINT ( 'NONE',  ( 2.091562808734966250, -0.4604446976123123814, 2.066416142659666111 ) ) ;
#146611=CARTESIAN_POINT ( 'NONE',  ( 0.7956772557287052905, -1.388798143503049420, -1.396678344884971112 ) ) ;
#146617=CARTESIAN_POINT ( 'NONE',  ( 3.117397163603967680, -2.209095822378583929, 0.6116082133489489925 ) ) ;
#146618=CARTESIAN_POINT ( 'NONE',  ( 0.9964003531478006215, -0.4411313887022934033, -1.771462291394958255 ) ) ;
#146619=CARTESIAN_POINT ( 'NONE',  ( 2.636851627972558454, 1.802111047976437508, 0.6404684511054498097 ) ) ;
#146622=CARTESIAN_POINT ( 'NONE',  ( 1.230727935554910557, 1.348888731755660153, -1.494678444409401896 ) ) ;
#146623=CARTESIAN_POINT ( 'NONE',  ( 1.112071775475082402, 1.959765382314464732, -0.09068415226199526280 ) ) ;
#146627=CARTESIAN_POINT ( 'NONE',  ( 3.750014218873336969, 0.7526759941024010470, 1.950626372838085265 ) ) ;
#146628=CARTESIAN_POINT ( 'NONE',  ( 2.131405713275540847, -1.153620894759581184, -1.342296593837268848 ) ) ;
#146631=CARTESIAN_POINT ( 'NONE',  ( 5.384854118993849248, 2.023671607873143152, -1.076698936902406922 ) ) ;
#146632=CARTESIAN_POINT ( 'NONE',  ( 4.312277775531628166, 1.592579213294993634, 0.7021690120074929320 ) ) ;
#146633=ADVANCED_FACE ( 'NONE', ( #166369 ), #52618, .T. ) ;
#146635=CARTESIAN_POINT ( 'NONE',  ( -0.1104750535120251204, 2.866086309876151539, -2.591737134608104842 ) ) ;
#146636=CARTESIAN_POINT ( 'NONE',  ( 4.868316058674494684, -0.4618845756635507893, 1.671066720262862182 ) ) ;
#146638=CARTESIAN_POINT ( 'NONE',  ( 4.809118753965334392, -1.746635306876740401, 1.289517135737711540 ) ) ;
#146640=CARTESIAN_POINT ( 'NONE',  ( 5.384000029850495750, -2.016708404008683786, 0.004832792792668073358 ) ) ;
#146641=CARTESIAN_POINT ( 'NONE',  ( 1.468750000000000888, 0.7852924748299092705, -1.895863743164120097 ) ) ;
#146643=CARTESIAN_POINT ( 'NONE',  ( 3.698194863803183630, -1.924136204678703832, -0.09579085892482024078 ) ) ;
#146645=CARTESIAN_POINT ( 'NONE',  ( 0.3643397115577310941, 0.6907578271265965020, -2.111251545739430302 ) ) ;
#146647=CARTESIAN_POINT ( 'NONE',  ( 6.983263157960366563, 2.446371134953594151, 2.328889586965996905 ) ) ;
#146651=CARTESIAN_POINT ( 'NONE',  ( 1.717743135698499124, 1.849103211704594463, 1.230578002476825583 ) ) ;
#146657=CARTESIAN_POINT ( 'NONE',  ( -0.01695367945527340853, -2.016028864686558730, -0.04667425414178058563 ) ) ;
#146659=CARTESIAN_POINT ( 'NONE',  ( 5.441865409415975741, 1.382631645094612338, 1.530856317113358678 ) ) ;
#146664=CARTESIAN_POINT ( 'NONE',  ( 0.6492013947936903229, 0.5632195774387914744, -1.677790250104938874 ) ) ;
#146665=CARTESIAN_POINT ( 'NONE',  ( 5.379468213355050210, -0.4295577260071090087, -1.679954900457746980 ) ) ;
#146666=CARTESIAN_POINT ( 'NONE',  ( 4.880260771415650289, -0.2196809260722985546, -1.726461634439285797 ) ) ;
#146668=CARTESIAN_POINT ( 'NONE',  ( 2.982263410219893274, -2.258884913406122408, -0.3895283529634691599 ) ) ;
#146670=CARTESIAN_POINT ( 'NONE',  ( 1.429379046243149931, 0.9088080074306194023, -1.601118750654044964 ) ) ;
#146673=CARTESIAN_POINT ( 'NONE',  ( 1.992912282819898850, 1.589903476415389871, -0.8970392876451321884 ) ) ;
#146674=CARTESIAN_POINT ( 'NONE',  ( 2.918592439375994552, -1.356299846568160827, -1.492255409411530120 ) ) ;
#146675=CARTESIAN_POINT ( 'NONE',  ( 1.254151665356119549, 0.8908215700371600043, 2.002402562943622844 ) ) ;
#146677=CARTESIAN_POINT ( 'NONE',  ( 3.926872384942071914, 1.999011803875171189, 0.6627620907858290389 ) ) ;
#146680=CARTESIAN_POINT ( 'NONE',  ( 1.258353326579707776, -2.070544811992577561, -0.001879966208345739808 ) ) ;
#146683=CARTESIAN_POINT ( 'NONE',  ( 3.897227946829431300, -0.2092540311423168320, -2.110150122182581356 ) ) ;
#146684=CARTESIAN_POINT ( 'NONE',  ( 0.2582596107527914131, 0.7359740259155130859, 1.780569212123730871 ) ) ;
#146691=CARTESIAN_POINT ( 'NONE',  ( 2.742449504557340489, 1.118516972803576870, -1.681586373676981827 ) ) ;
#146692=CARTESIAN_POINT ( 'NONE',  ( 1.589043446250279601, -0.3083810453359912551, -2.083120927691509916 ) ) ;
#146695=CARTESIAN_POINT ( 'NONE',  ( 5.559367761144698328, 1.520187721101939671, 1.073055572604255214 ) ) ;
#146702=CARTESIAN_POINT ( 'NONE',  ( 6.789916310432966284, -0.8843476597930698402, 1.859958747594625317 ) ) ;
#146706=CARTESIAN_POINT ( 'NONE',  ( 2.530263549637286502, 1.701127810229096982, -0.3340974653274173534 ) ) ;
#146707=CARTESIAN_POINT ( 'NONE',  ( 1.534671620441448558, -1.258764033546970529, -1.202027791382529909 ) ) ;
#146708=CARTESIAN_POINT ( 'NONE',  ( 6.481126831302748137, -0.1059855822947413234, -2.305399816445557359 ) ) ;
#146711=CARTESIAN_POINT ( 'NONE',  ( 2.811851269462920744, -2.038842655386669644, 0.2989082417928933810 ) ) ;
#146712=CARTESIAN_POINT ( 'NONE',  ( 1.388045824401448414, -0.05229234656609069859, 2.015604296821980057 ) ) ;
#146713=CARTESIAN_POINT ( 'NONE',  ( 6.825078400183577365, 2.023440267519378999, 2.448151054272352578 ) ) ;
#146716=CARTESIAN_POINT ( 'NONE',  ( 0.7429697149608678330, -1.692012040804885098, 1.011587418319284781 ) ) ;
#146718=CARTESIAN_POINT ( 'NONE',  ( 5.009976098083095408, -0.6827417919906975108, 1.786564173047608062 ) ) ;
#146723=CARTESIAN_POINT ( 'NONE',  ( 0.8912779446055114629, -0.05177971647825175411, -2.019189627193836323 ) ) ;
#146725=CARTESIAN_POINT ( 'NONE',  ( 4.928937574911031128, 2.206605557787114869, 0.6751633795739877542 ) ) ;
#146726=CARTESIAN_POINT ( 'NONE',  ( 6.092239754786219486, 0.9682357284593717806, -1.706234036142616928 ) ) ;
#146728=CARTESIAN_POINT ( 'NONE',  ( 1.621847549879053885, 1.933622029546874010, -0.3300716771732490895 ) ) ;
#146732=CARTESIAN_POINT ( 'NONE',  ( 1.042374724401398334, 0.8638241406289723923, 1.933313940807819487 ) ) ;
#146735=CARTESIAN_POINT ( 'NONE',  ( 1.095364067855080448, -1.841320589428995236, -0.001981933617903330457 ) ) ;
#146737=CARTESIAN_POINT ( 'NONE',  ( 4.065408448962204879, 1.859168595270783042, 1.121007083124803572 ) ) ;
#146739=CARTESIAN_POINT ( 'NONE',  ( 1.933984528066152953, -2.055706711753771287, 0.5200354980386610038 ) ) ;
#146742=CARTESIAN_POINT ( 'NONE',  ( 3.356764223755447141, -1.562743594079138321, 1.343508228479517230 ) ) ;
#146744=CARTESIAN_POINT ( 'NONE',  ( 0.1164230846485321547, -0.09151219166612066525, 1.839079034809627755 ) ) ;
#146749=CARTESIAN_POINT ( 'NONE',  ( 0.1357705729100426029, -2.015811560716780360, 0.8986578214904348272 ) ) ;
#146750=CARTESIAN_POINT ( 'NONE',  ( 1.476233607035297490, 1.347422320225545089, 1.817282701917295240 ) ) ;
#146752=CARTESIAN_POINT ( 'NONE',  ( 2.548825626188336635, 0.2254045845835982720, 1.797452833117135329 ) ) ;
#146753=CARTESIAN_POINT ( 'NONE',  ( 1.604551054648394537, 1.788909703809701712, 0.6859268596576766353 ) ) ;
#146754=CARTESIAN_POINT ( 'NONE',  ( 2.928250347896840022, 1.105370970781336837, 1.750397071514836478 ) ) ;
#146756=CARTESIAN_POINT ( 'NONE',  ( 1.200003858469798956, -1.971640592295399896, -0.002163809803111190443 ) ) ;
#146757=CARTESIAN_POINT ( 'NONE',  ( 6.551400848983751857, -1.549099897634421685, -1.145107510758677893 ) ) ;
#146758=CARTESIAN_POINT ( 'NONE',  ( 3.203821283898714345, -1.868584281295191607, 0.09040415888627445495 ) ) ;
#146759=CARTESIAN_POINT ( 'NONE',  ( 1.717812883538033297, -0.2792282863031622653, 2.290681961221084695 ) ) ;
#146761=CARTESIAN_POINT ( 'NONE',  ( 2.752234738034575301, -1.855867026150724186, -0.1399345609422244507 ) ) ;
#146763=CARTESIAN_POINT ( 'NONE',  ( 5.248506731170051509, -2.046683549694120252, -0.2560125357965719606 ) ) ;
#146767=CARTESIAN_POINT ( 'NONE',  ( 6.422895033429510292, 1.963595603779586973, 0.7616278367365038049 ) ) ;
#146769=CARTESIAN_POINT ( 'NONE',  ( 6.186834690482100108, -0.3103498281695793448, -2.139073744226393181 ) ) ;
#146770=CARTESIAN_POINT ( 'NONE',  ( 0.4152503475762688856, -0.9843521281015167324, -1.555853522519357934 ) ) ;
#146771=CARTESIAN_POINT ( 'NONE',  ( 5.707677564275420501, 1.530686452870811065, 1.317726828763097435 ) ) ;
#146780=CARTESIAN_POINT ( 'NONE',  ( 3.555875268649951959, 1.124244472066991518, 1.673854899288424347 ) ) ;
#146785=CARTESIAN_POINT ( 'NONE',  ( 6.139563164240942506, -1.562336469324271837, -1.494251390645913613 ) ) ;
#146790=CARTESIAN_POINT ( 'NONE',  ( 5.923453886551514280, -1.462456689723025782, -1.388475849216065372 ) ) ;
#146792=CARTESIAN_POINT ( 'NONE',  ( 1.681838029686154146, -0.9247999101687879309, 1.455793735983588633 ) ) ;
#146797=CARTESIAN_POINT ( 'NONE',  ( 0.2273421782777407807, -1.081390543313685226, -1.401283913643845969 ) ) ;
#146798=CARTESIAN_POINT ( 'NONE',  ( 0.2936080233231981862, 1.877589464902774674, -0.7265071302150533095 ) ) ;
#146800=CARTESIAN_POINT ( 'NONE',  ( 2.766872162265196611, -1.522532973755141850, 1.597636210702752635 ) ) ;
#146801=CARTESIAN_POINT ( 'NONE',  ( 5.471592230178073279, -0.3258623020658823477, 2.146390899824067056 ) ) ;
#146804=CARTESIAN_POINT ( 'NONE',  ( 2.965608807194367813, -1.734805745614193873, -1.219131234129526398 ) ) ;
#146805=CARTESIAN_POINT ( 'NONE',  ( 1.564077599769473803, -1.076297475396456704, 1.704952281334138675 ) ) ;
#146806=CARTESIAN_POINT ( 'NONE',  ( 2.074188967152798657, 0.7772732722058082189, 1.636524323399509928 ) ) ;
#146812=CARTESIAN_POINT ( 'NONE',  ( 0.9014164429375628451, -1.868237418080781254, 0.4230343950424199084 ) ) ;
#146819=CARTESIAN_POINT ( 'NONE',  ( 4.750933126423753095, -1.738186171353903742, 1.284983810367075208 ) ) ;
#146822=CARTESIAN_POINT ( 'NONE',  ( 1.758217466200185042, 0.8068918862002281145, -1.961288232260410380 ) ) ;
#146824=CARTESIAN_POINT ( 'NONE',  ( 3.462146415373760444, 0.8834382129937996542, 1.762370924576799114 ) ) ;
#146825=CARTESIAN_POINT ( 'NONE',  ( 6.011958326525193463, -0.6379227081053112647, 1.803018720113582773 ) ) ;
#146826=ORIENTED_EDGE ( 'NONE', *, *, #90321, .F. ) ;
#146828=CARTESIAN_POINT ( 'NONE',  ( 0.6607010325807397555, -0.6960017893198193750, -1.950014918625786020 ) ) ;
#146829=CARTESIAN_POINT ( 'NONE',  ( 1.640467198872105348, -1.640604414344963180, 1.038759544029205895 ) ) ;
#146834=CARTESIAN_POINT ( 'NONE',  ( 3.011755509560889443, -1.030818127458534184, -1.818759449385324078 ) ) ;
#146837=CARTESIAN_POINT ( 'NONE',  ( 6.498695769366850783, -1.876353784076413067, -0.3680397143606057853 ) ) ;
#146839=CARTESIAN_POINT ( 'NONE',  ( 4.565167970240332274, -1.970479184476852108, -0.9938812724585781577 ) ) ;
#146840=CARTESIAN_POINT ( 'NONE',  ( 2.608667852368121043, -0.8438080161984360394, -2.039271889284439254 ) ) ;
#146843=CARTESIAN_POINT ( 'NONE',  ( 1.717294761138322912, 1.590556852780611097, 1.061263400373997134 ) ) ;
#146846=CARTESIAN_POINT ( 'NONE',  ( 4.105968538015460467, 0.7004154448949986289, -1.948405661837959713 ) ) ;
#146849=CARTESIAN_POINT ( 'NONE',  ( 1.288190726105652217, -0.9714702286227733241, 1.931199087792371261 ) ) ;
#146850=CARTESIAN_POINT ( 'NONE',  ( 4.036819321710017228, -1.906298169312226953, 1.081085072550565407 ) ) ;
#146858=CARTESIAN_POINT ( 'NONE',  ( -0.1399997263889594112, -0.002789056014654289761, -2.000146600338557956 ) ) ;
#146860=CARTESIAN_POINT ( 'NONE',  ( 4.452052287080165982, -0.7971045336818067817, 1.910850710330507907 ) ) ;
#146861=CARTESIAN_POINT ( 'NONE',  ( 2.736843622788497132, 0.2362483484473417716, 1.911901653511848931 ) ) ;
#146862=CARTESIAN_POINT ( 'NONE',  ( 5.941034585168498694, -1.816085283887830082, -1.088097372982429034 ) ) ;
#146866=CARTESIAN_POINT ( 'NONE',  ( 4.030098220014290078, 1.090402053431119622, 1.639822181875214557 ) ) ;
#146867=CARTESIAN_POINT ( 'NONE',  ( 6.175753646036172384, -1.231511006544892206, 1.933186584637256678 ) ) ;
#146868=CARTESIAN_POINT ( 'NONE',  ( 4.037589748876240670, -1.260430739550026047, -1.321009972365666085 ) ) ;
#146875=CARTESIAN_POINT ( 'NONE',  ( 4.992444313356595664, -1.114831962662912845, 1.676160436541684229 ) ) ;
#146877=CARTESIAN_POINT ( 'NONE',  ( 5.977181698541591537, -2.287177818765488091, -0.2295778655121790968 ) ) ;
#146878=CARTESIAN_POINT ( 'NONE',  ( 4.733228419949464971, 0.004064956161661801778, -1.961936380062332397 ) ) ;
#146883=CARTESIAN_POINT ( 'NONE',  ( 1.101248736683122953, -0.5045743719560727980, 2.028828713580214771 ) ) ;
#146884=CARTESIAN_POINT ( 'NONE',  ( 0.5318453760667535279, 0.9654296485097979552, -1.602142582367314549 ) ) ;
#146886=CARTESIAN_POINT ( 'NONE',  ( 6.597608361038971303, -1.941456323438792042, 0.05037571119943275166 ) ) ;
#146887=CARTESIAN_POINT ( 'NONE',  ( -0.2102771530458276972, -0.008943344768331040057, -2.203482896658352175 ) ) ;
#146888=CARTESIAN_POINT ( 'NONE',  ( 1.434671803396998291, -1.260233744827907953, -1.200652698350104686 ) ) ;
#146891=CARTESIAN_POINT ( 'NONE',  ( 2.068594797844982125, -1.576417056545238893, -0.7005022305992656406 ) ) ;
#146892=CARTESIAN_POINT ( 'NONE',  ( 1.136565065649897344, 0.4323997850379875385, 2.148315308122191514 ) ) ;
#146893=CARTESIAN_POINT ( 'NONE',  ( 4.283934280384479543, 1.440456688004333019, 1.672026782002330458 ) ) ;
#146894=CARTESIAN_POINT ( 'NONE',  ( 1.200314488179974326, 0.8819602860624680130, -1.984045050410755406 ) ) ;
#146896=CARTESIAN_POINT ( 'NONE',  ( 2.466138310383278132, -1.084178177903678320, 1.818555153620523779 ) ) ;
#146899=CARTESIAN_POINT ( 'NONE',  ( 2.138584244316643179, 0.5063124247480701445, 2.235611027800854078 ) ) ;
#146904=CARTESIAN_POINT ( 'NONE',  ( 4.951916289638909063, -1.570117426187572107, -1.571520405092931005 ) ) ;
#146910=VERTEX_POINT ( 'NONE', #105121 ) ;
#146911=CARTESIAN_POINT ( 'NONE',  ( 3.428361437285933455, -1.528740797599713153, -1.314997250469025936 ) ) ;
#146913=CARTESIAN_POINT ( 'NONE',  ( 2.043871907009750633, 1.419221230981766668, 1.496905473486829230 ) ) ;
#146918=CARTESIAN_POINT ( 'NONE',  ( 4.576244502665470115, -2.125281509430646754, -0.5339713055512520512 ) ) ;
#146919=CARTESIAN_POINT ( 'NONE',  ( 2.549454116737331244, -1.388485404012842261, 1.462446031800922253 ) ) ;
#146920=CARTESIAN_POINT ( 'NONE',  ( 0.5910386730991653570, -0.6632029860377097741, 1.717849102829023922 ) ) ;
#146924=CARTESIAN_POINT ( 'NONE',  ( 5.297797529045338294, -0.6555159417414997414, 1.704002486358429325 ) ) ;
#146925=CARTESIAN_POINT ( 'NONE',  ( 6.047500043413473136, -1.423963828944514010, 1.427935028000301809 ) ) ;
#146927=CARTESIAN_POINT ( 'NONE',  ( 4.750980993940300046, -1.819980134924009452, 1.343945550547174239 ) ) ;
#146929=CARTESIAN_POINT ( 'NONE',  ( 0.9089716955857042313, 1.593442362523834754, -1.377222155420864347 ) ) ;
#146931=CARTESIAN_POINT ( 'NONE',  ( 4.211429588753928144, -1.719575573843846072, -1.152724658989822348 ) ) ;
#146941=CARTESIAN_POINT ( 'NONE',  ( 1.951734608585634190, -1.981729029064113856, 1.003908989668365948 ) ) ;
#146945=CARTESIAN_POINT ( 'NONE',  ( 3.209375601822930690, -1.602329130913646926, -1.131729396966949963 ) ) ;
#146951=CARTESIAN_POINT ( 'NONE',  ( 2.760144723603759065, 0.7592700852765141839, -1.980205354017528840 ) ) ;
#146953=CARTESIAN_POINT ( 'NONE',  ( 4.557600102482579629, 0.4766696971462945909, -2.108333899287537339 ) ) ;
#146954=CARTESIAN_POINT ( 'NONE',  ( 2.753256032281672372, 1.832158412346639453, -0.1828795585285883096 ) ) ;
#146957=CARTESIAN_POINT ( 'NONE',  ( 6.175711810462381379, -0.9247362235058408375, 1.474125693279482174 ) ) ;
#146961=CARTESIAN_POINT ( 'NONE',  ( 3.379894511112140787, 1.369989894601089775, 1.672159933133889442 ) ) ;
#146963=CARTESIAN_POINT ( 'NONE',  ( 4.270861128529729989, -2.010896307770511537, 0.1455111863851859810 ) ) ;
#146965=CARTESIAN_POINT ( 'NONE',  ( 1.938557520917514987, 2.138169252768943984, 0.3173444169591658204 ) ) ;
#146966=CARTESIAN_POINT ( 'NONE',  ( 2.917208927397921592, -0.1969847599093167145, 1.961514860040159292 ) ) ;
#146967=CARTESIAN_POINT ( 'NONE',  ( 6.509000000000011887, 3.696273625755361447, 2.514342382328867753 ) ) ;
#146968=CARTESIAN_POINT ( 'NONE',  ( 4.089352007823720214, -0.7402336266850146895, 1.795645171352943770 ) ) ;
#146977=CARTESIAN_POINT ( 'NONE',  ( 0.9564373720404686363, 2.204146663617879476, -0.1098798544595935567 ) ) ;
#146980=CARTESIAN_POINT ( 'NONE',  ( 4.996903459272755477, 0.3314677610860050083, 1.933379042443456486 ) ) ;
#146983=CARTESIAN_POINT ( 'NONE',  ( 0.07459516483343267557, 2.058153987855536382, -2.173125978204577535 ) ) ;
#146984=CARTESIAN_POINT ( 'NONE',  ( 4.400242069895500485, 1.421654421768648868, -1.169904355399861595 ) ) ;
#146988=CARTESIAN_POINT ( 'NONE',  ( 5.185831674374465905, 2.043064739972153543, -0.5678235988075125418 ) ) ;
#146993=CARTESIAN_POINT ( 'NONE',  ( 6.503207061003255518, 1.710746398682884140, 1.148667516769467767 ) ) ;
#146995=CARTESIAN_POINT ( 'NONE',  ( 1.240418688720058560, -1.814558931778247119, -0.4126190233522536444 ) ) ;
#146996=CARTESIAN_POINT ( 'NONE',  ( 3.526749072549471453, -1.699942963128863838, 0.7078653300200200560 ) ) ;
#147001=CARTESIAN_POINT ( 'NONE',  ( 3.440233207309027375, 0.9924059104887033023, -1.971224004288201881 ) ) ;
#147002=CARTESIAN_POINT ( 'NONE',  ( 6.520815820410102326, 2.107438871474434983, 0.8233813407293107955 ) ) ;
#147004=CARTESIAN_POINT ( 'NONE',  ( 5.537325978022108686, -0.03587880057049273180, 1.811405195203552587 ) ) ;
#147005=CARTESIAN_POINT ( 'NONE',  ( 5.296063324668989658, -0.8673027158061608066, -1.708257925969633551 ) ) ;
#147007=CARTESIAN_POINT ( 'NONE',  ( 6.297708355432167338, -0.6282832542035889922, 1.762108908958268216 ) ) ;
#147008=CARTESIAN_POINT ( 'NONE',  ( 6.074623017180313944, 1.249363044128497524, -1.379498876745478109 ) ) ;
#147009=CARTESIAN_POINT ( 'NONE',  ( 6.614108672291515667, -0.8387186360741160085, -1.558468296174354784 ) ) ;
#147010=CARTESIAN_POINT ( 'NONE',  ( 1.288296401830712368, -0.7303101666344159471, -1.879802715551846859 ) ) ;
#147012=CARTESIAN_POINT ( 'NONE',  ( 2.614012881481563522, -2.083059734262616036, 0.3096129728813925008 ) ) ;
#147017=CARTESIAN_POINT ( 'NONE',  ( 1.441672106306312484, -1.900340447277752087, 0.6846001189487918026 ) ) ;
#147021=CARTESIAN_POINT ( 'NONE',  ( 3.145949958485740883, 0.7812230816454240889, -2.015650884352723882 ) ) ;
#147022=CARTESIAN_POINT ( 'NONE',  ( 6.610000000000009202, 6.036727194997777879, 2.594899704271665275 ) ) ;
#147030=CARTESIAN_POINT ( 'NONE',  ( 0.5389544483674936215, -1.876709678404146153, 1.131566444868239874 ) ) ;
#147032=CARTESIAN_POINT ( 'NONE',  ( 2.852682258652036840, 0.7612096163719231923, 2.130753183350143409 ) ) ;
#147039=CARTESIAN_POINT ( 'NONE',  ( 3.584973236653755002, 1.601158291227417152, -0.7540797108817003380 ) ) ;
#147040=CARTESIAN_POINT ( 'NONE',  ( 6.739307351729481255, -1.974284904759715298, 0.9861035376414882814 ) ) ;
#147044=CARTESIAN_POINT ( 'NONE',  ( 4.710564641745673242, 1.930423983604495630, 0.5826390268678025564 ) ) ;
#147047=CARTESIAN_POINT ( 'NONE',  ( 3.326877442632663939, 0.04465521416292458912, 1.870282673472216439 ) ) ;
#147048=CARTESIAN_POINT ( 'NONE',  ( 3.450112209602332669, -0.8433740631265237431, 1.890881698631073249 ) ) ;
#147055=CARTESIAN_POINT ( 'NONE',  ( 1.300873410958070409, -0.2835801433653042380, -1.891145142470892715 ) ) ;
#147057=CARTESIAN_POINT ( 'NONE',  ( 2.348037267531626338, -0.8415878996531295231, 1.772339229757218471 ) ) ;
#147058=CARTESIAN_POINT ( 'NONE',  ( 1.001327120302420548, 1.985796081718914419, 0.3474166314290441648 ) ) ;
#147062=CARTESIAN_POINT ( 'NONE',  ( 0.1747926744264660381, 0.006858446013176254172, -1.855468577918440776 ) ) ;
#147064=CARTESIAN_POINT ( 'NONE',  ( 2.074478728756317114, 0.8647236062047275462, 1.818190761793165189 ) ) ;
#147066=CARTESIAN_POINT ( 'NONE',  ( 2.038805038046047624, -1.634495437704911458, 1.345740563223641217 ) ) ;
#147068=CARTESIAN_POINT ( 'NONE',  ( 3.877443546529443452, -0.1552652338182025915, 2.064615508632794860 ) ) ;
#147070=CARTESIAN_POINT ( 'NONE',  ( 5.332010518800971433, 2.059573894497103819, 0.3580650863252275440 ) ) ;
#147072=CARTESIAN_POINT ( 'NONE',  ( 4.348545414961950684, 0.4871326187540457875, 1.759326811173238303 ) ) ;
#147077=CARTESIAN_POINT ( 'NONE',  ( 6.440462174652990868, 2.181831651002089423, 0.3301269925025315799 ) ) ;
#147079=CARTESIAN_POINT ( 'NONE',  ( 5.443983014310386892, -1.216401775450553169, -1.475513148251464068 ) ) ;
#147086=CARTESIAN_POINT ( 'NONE',  ( 0.8898994657863326108, -0.4472179738511591895, -1.785967584704901912 ) ) ;
#147089=CARTESIAN_POINT ( 'NONE',  ( 4.674985431947434655, 0.001863223488791227334, -1.870726058175266715 ) ) ;
#147090=CARTESIAN_POINT ( 'NONE',  ( -0.02299388927986567924, 4.093419149701410298, -2.466026074291859160 ) ) ;
#147096=CARTESIAN_POINT ( 'NONE',  ( 1.340603599695965764, -1.920222134930357427, -0.4367614745469716730 ) ) ;
#147097=CARTESIAN_POINT ( 'NONE',  ( 1.968375273883906429, -1.978056371059619511, -0.3905749819678172585 ) ) ;
#147101=CARTESIAN_POINT ( 'NONE',  ( 2.414256260463796711, 1.430409426244143134, -1.660321623440104810 ) ) ;
#147111=CARTESIAN_POINT ( 'NONE',  ( 5.425302022954732628, -1.172690680311109901, -1.419496581506813904 ) ) ;
#147112=CARTESIAN_POINT ( 'NONE',  ( 2.297522961200649139, 1.839619113207457524, -0.8179307585152847393 ) ) ;
#147113=CARTESIAN_POINT ( 'NONE',  ( 3.638291363623618047, 0.06041265439583366065, -2.297745614018332105 ) ) ;
#147114=CARTESIAN_POINT ( 'NONE',  ( -0.1290005225502432740, 4.081813041011835175, -2.728655865233818201 ) ) ;
#147115=CARTESIAN_POINT ( 'NONE',  ( 1.586513592238134374, 1.791619466816740003, 0.5028711289422735931 ) ) ;
#147118=CARTESIAN_POINT ( 'NONE',  ( 6.135011676971934058, 1.786887936952135991, 0.6819008164158719687 ) ) ;
#147121=CARTESIAN_POINT ( 'NONE',  ( 5.108965175345551835, -0.3053309577524323526, 2.068188354190988676 ) ) ;
#147122=CARTESIAN_POINT ( 'NONE',  ( 3.098369316282158614, -0.5415621961667067552, -1.790553177708480215 ) ) ;
#147124=CARTESIAN_POINT ( 'NONE',  ( 5.794452930745782382, 1.501506822132542718, -1.065412412061928160 ) ) ;
#147127=CARTESIAN_POINT ( 'NONE',  ( 4.934089290906335634, 0.8825209879863432638, -1.481864930267517089 ) ) ;
#147132=CARTESIAN_POINT ( 'NONE',  ( 4.768535058008659178, -0.9225228719554872114, -1.965435229472652479 ) ) ;
#147133=CARTESIAN_POINT ( 'NONE',  ( 3.598116246361187542, -1.823677485248562435, -0.08826725125678223927 ) ) ;
#147134=CARTESIAN_POINT ( 'NONE',  ( 0.7429250141685153075, -0.2344385519315282107, -1.947609053799495227 ) ) ;
#147135=CARTESIAN_POINT ( 'NONE',  ( 6.192584684491233560, 1.567513771475435247, -1.423521977300482577 ) ) ;
#147136=CARTESIAN_POINT ( 'NONE',  ( 5.864811835480173485, 0.1724426041235416485, -2.285918041817245783 ) ) ;
#147141=CARTESIAN_POINT ( 'NONE',  ( 1.963691422110905638, -1.704870618661393999, -1.260721693921822428 ) ) ;
#147145=CARTESIAN_POINT ( 'NONE',  ( 6.350449713519967787, -2.159805286613075470, -0.2212482231108928721 ) ) ;
#147146=CARTESIAN_POINT ( 'NONE',  ( 6.983263157960386991, 6.036006179461032239, 2.548702536770989457 ) ) ;
#147149=CARTESIAN_POINT ( 'NONE',  ( 2.280208067491045654, 2.177836876428246971, -0.4364916025852043635 ) ) ;
#147151=CARTESIAN_POINT ( 'NONE',  ( 6.522112240665402183, -1.799906897009293738, 0.9091900463213120620 ) ) ;
#147153=CARTESIAN_POINT ( 'NONE',  ( 6.034046607691841757, 1.223980295139483809, 1.660032098485002994 ) ) ;
#147158=CARTESIAN_POINT ( 'NONE',  ( 0.1333542156527582345, 4.089120883327095335, -2.600857804679152174 ) ) ;
#147159=CARTESIAN_POINT ( 'NONE',  ( 5.442854017605395889, -1.455216020186438364, -1.127989967910733915 ) ) ;
#147161=CARTESIAN_POINT ( 'NONE',  ( -0.2104748580754408904, 1.337026610731705700, -2.356057411969681326 ) ) ;
#147162=CARTESIAN_POINT ( 'NONE',  ( 2.115808521728879565, -0.8096002590626363293, -1.522937571937353241 ) ) ;
#147163=CARTESIAN_POINT ( 'NONE',  ( 0.09298292169932984019, 1.756857073293972116, 0.9896806593640145033 ) ) ;
#147164=CARTESIAN_POINT ( 'NONE',  ( 2.233388324916096845, 2.298236692437699791, 0.05235245155727624722 ) ) ;
#147166=CARTESIAN_POINT ( 'NONE',  ( 2.689068300184436655, -0.3842959826076980390, -2.229375072012912629 ) ) ;
#147167=CARTESIAN_POINT ( 'NONE',  ( 4.090527498900095260, -2.083119126933795418, -0.3091809127075405006 ) ) ;
#147169=CARTESIAN_POINT ( 'NONE',  ( 2.793947764029936831, -1.764715128225034180, -0.1343432132955291736 ) ) ;
#147175=CARTESIAN_POINT ( 'NONE',  ( 6.187741696929490054, 2.126074299989196614, -0.6436727651782292448 ) ) ;
#147176=CARTESIAN_POINT ( 'NONE',  ( 3.679775893577118318, -1.080384588543949809, 1.906543112819548913 ) ) ;
#147184=CARTESIAN_POINT ( 'NONE',  ( 5.607717026683647354, 1.607092460389969446, 1.383685132418293495 ) ) ;
#147190=CARTESIAN_POINT ( 'NONE',  ( 5.970224376651539266, -1.750504005202535796, -0.5711807346103907612 ) ) ;
#147193=CARTESIAN_POINT ( 'NONE',  ( 2.155425581425034487, 0.7450078602235529202, 1.573079536267004030 ) ) ;
#147201=CARTESIAN_POINT ( 'NONE',  ( 5.858325616802108726, 0.8718737102157668728, 1.978260574764856283 ) ) ;
#147205=CARTESIAN_POINT ( 'NONE',  ( 5.677018108359257020, -0.04579235393691384604, -1.970973552702318443 ) ) ;
#147206=CARTESIAN_POINT ( 'NONE',  ( 4.973871655188280450, 1.509253006592145452, 0.8532917887605420137 ) ) ;
#147208=CARTESIAN_POINT ( 'NONE',  ( 1.980270094416748394, -2.150034404144373301, -0.4237573071887782983 ) ) ;
#147209=CARTESIAN_POINT ( 'NONE',  ( 3.768876097860610397, -1.551941239651495108, 1.707908033328522146 ) ) ;
#147210=CARTESIAN_POINT ( 'NONE',  ( 4.815729912100211507, -2.021797975182148654, 0.3980178507551126454 ) ) ;
#147211=CARTESIAN_POINT ( 'NONE',  ( 1.341630539043844106, 1.939701883965805562, 0.09577479888067677583 ) ) ;
#147213=CIRCLE ( 'NONE', #29553, 0.04999999999999937828 ) ;
#147216=CARTESIAN_POINT ( 'NONE',  ( 3.744478000529617656, 1.131475959888720295, -1.793321066073015224 ) ) ;
#147218=CARTESIAN_POINT ( 'NONE',  ( 2.760388869050140137, 1.913803604375517109, -0.6351994527180188088 ) ) ;
#147220=CARTESIAN_POINT ( 'NONE',  ( 4.682781310676605635, -2.139571651222616833, -0.5399477217277389718 ) ) ;
#147229=CARTESIAN_POINT ( 'NONE',  ( 4.487218586473323612, 1.841840323776536614, -0.9247287835071598128 ) ) ;
#147233=CARTESIAN_POINT ( 'NONE',  ( 3.352217588874096599, 0.9059935441126705236, -1.805122612331450105 ) ) ;
#147237=CARTESIAN_POINT ( 'NONE',  ( 2.782161975763951300, -1.060548055690222702, 1.766919142140084720 ) ) ;
#147238=CARTESIAN_POINT ( 'NONE',  ( 6.983263157960365675, -0.006178392973848687020, 2.053544886540019210 ) ) ;
#147240=CARTESIAN_POINT ( 'NONE',  ( -0.2409995289980038091, 6.947781193150415646, -2.595509233728268583 ) ) ;
#147241=CARTESIAN_POINT ( 'NONE',  ( 1.482094074889642288, -0.2687121449159133313, -1.821302815977184686 ) ) ;
#147242=CARTESIAN_POINT ( 'NONE',  ( 0.4698728525199142303, 0.2201595520019784535, -2.297181220480988717 ) ) ;
#147244=CARTESIAN_POINT ( 'NONE',  ( 2.091316376603330252, 1.881825464268515269, -1.063406855978922039 ) ) ;
#147246=CARTESIAN_POINT ( 'NONE',  ( 2.290250256651988892, -0.7762311197250795214, -1.861343989391924358 ) ) ;
#147247=CARTESIAN_POINT ( 'NONE',  ( 0.5670072068131201126, 0.1877032549213939472, -1.861219751863735672 ) ) ;
#147248=CARTESIAN_POINT ( 'NONE',  ( 4.856303703212550893, 0.7536814072931929953, 1.821903339724652460 ) ) ;
#147249=CARTESIAN_POINT ( 'NONE',  ( 5.173064673083394460, 1.776168143800487043, -0.9548534231369476544 ) ) ;
#147253=CARTESIAN_POINT ( 'NONE',  ( 5.848290838822029158, 2.103586024953810085, 0.1047431163101186502 ) ) ;
#147254=CARTESIAN_POINT ( 'NONE',  ( 6.092251258522619395, 1.023830597077223903, -1.799436568697235783 ) ) ;
#147258=CARTESIAN_POINT ( 'NONE',  ( 5.976820969762068003, -1.425406409037911937, 1.431266451708369303 ) ) ;
#147260=CARTESIAN_POINT ( 'NONE',  ( 4.319161277787673114, 2.108828969982502688, 0.9375607936791326980 ) ) ;
#147261=CARTESIAN_POINT ( 'NONE',  ( 1.762625871119470000, -0.7384422231204194054, -1.926036706659232323 ) ) ;
#147268=CARTESIAN_POINT ( 'NONE',  ( 3.754478802441584495, -2.168521383071635000, -0.1100146688530565936 ) ) ;
#147271=CARTESIAN_POINT ( 'NONE',  ( 3.438839575862782549, -1.396446551253815782, -1.200180114512699792 ) ) ;
#147274=CARTESIAN_POINT ( 'NONE',  ( 5.987848539424092564, -2.180829346447300310, -0.2163489798085171945 ) ) ;
#147276=CARTESIAN_POINT ( 'NONE',  ( 5.612299388031473768, -1.011774156007083869, -2.023756622241212000 ) ) ;
#147282=CARTESIAN_POINT ( 'NONE',  ( 6.063686852112752490, 1.743171776219472280, -0.3043750889455443254 ) ) ;
#147283=CARTESIAN_POINT ( 'NONE',  ( 3.914701103513482661, -0.6334807629873323576, -1.910874176753782461 ) ) ;
#147285=CARTESIAN_POINT ( 'NONE',  ( 2.608543117039106463, -0.8048738574607334773, -1.946287526097515430 ) ) ;
#147286=CARTESIAN_POINT ( 'NONE',  ( 1.915515091613760656, -1.252924113133683237, -1.449102840280371618 ) ) ;
#147288=CARTESIAN_POINT ( 'NONE',  ( 3.719166427026363131, -1.735901824557140927, -0.9304994270666072653 ) ) ;
#147289=CARTESIAN_POINT ( 'NONE',  ( 4.904559663377827228, -2.005024252762297898, -0.2429568683046164634 ) ) ;
#147290=CARTESIAN_POINT ( 'NONE',  ( 0.9888773766892227091, 1.651582696977689890, -0.8784067438419729257 ) ) ;
#147291=CARTESIAN_POINT ( 'NONE',  ( 1.099968687278202406, 0.7983322178258808188, -1.792280776234013828 ) ) ;
#147292=CARTESIAN_POINT ( 'NONE',  ( 3.474969472568560480, 0.04075424684168299505, -1.724569731432665121 ) ) ;
#147293=CARTESIAN_POINT ( 'NONE',  ( 0.5625819312903357350, 0.5574351770905332515, 1.829310545699929458 ) ) ;
#147295=CARTESIAN_POINT ( 'NONE',  ( 1.541937560865791479, -1.600244427420342896, -1.519961040588948986 ) ) ;
#147302=CARTESIAN_POINT ( 'NONE',  ( 6.825056245572477032, -1.890314563506745316, -0.8446596084958692963 ) ) ;
#147304=CARTESIAN_POINT ( 'NONE',  ( 0.6782873735513493818, -1.106163567672680204, -1.749894625276714688 ) ) ;
#147309=CARTESIAN_POINT ( 'NONE',  ( 5.830757645730302308, 1.424217953154560012, -1.571192434731554677 ) ) ;
#147314=CARTESIAN_POINT ( 'NONE',  ( 6.320756440275016708, -1.388331291134708767, 1.386421665916007795 ) ) ;
#147316=CARTESIAN_POINT ( 'NONE',  ( 4.499374939222855474, 1.976653413780619761, 0.3960398538903551757 ) ) ;
#147317=CARTESIAN_POINT ( 'NONE',  ( 3.643669983026840420, 1.900603903897592595, -0.2398275428802750520 ) ) ;
#147319=CARTESIAN_POINT ( 'NONE',  ( 1.154151856878969928, 0.8927059368322427524, 2.001694687108931170 ) ) ;
#147321=CARTESIAN_POINT ( 'NONE',  ( 3.620239363633662499, 1.188986022374241225, -1.444006105232335191 ) ) ;
#147325=CARTESIAN_POINT ( 'NONE',  ( 5.167619242541076297, 1.422618751053092101, 1.568198848534626100 ) ) ;
#147327=CARTESIAN_POINT ( 'NONE',  ( 2.472313036883976078, -2.001511166234470007, -0.6043430715973686640 ) ) ;
#147329=CARTESIAN_POINT ( 'NONE',  ( 0.8149653058732795330, -0.2595981955949409614, 1.704996164590016683 ) ) ;
#147338=CARTESIAN_POINT ( 'NONE',  ( 1.277659230087615727, 1.784704083969153920, -0.3092532468622013475 ) ) ;
#147343=CARTESIAN_POINT ( 'NONE',  ( 6.539320575229250032, 3.707580029678263944, 2.311356139567366963 ) ) ;
#147348=CARTESIAN_POINT ( 'NONE',  ( 2.840123846975282973, -0.9592540151425684725, 1.594648687322928859 ) ) ;
#147349=CARTESIAN_POINT ( 'NONE',  ( 0.4740638213791115718, -1.901237768712552345, -0.2334040896743785343 ) ) ;
#147350=CARTESIAN_POINT ( 'NONE',  ( 6.440456187458303283, 1.905530750978209120, 0.2820203164855574207 ) ) ;
#147357=CARTESIAN_POINT ( 'NONE',  ( 4.944182365274345514, -0.9318649803399962073, 1.735062577953277563 ) ) ;
#147358=CARTESIAN_POINT ( 'NONE',  ( 1.453939175038564624, -1.538220317728825393, -1.459821603020584613 ) ) ;
#147363=CARTESIAN_POINT ( 'NONE',  ( 6.456982561897790518, 0.3786298020890948024, -2.158335565738931816 ) ) ;
#147365=CARTESIAN_POINT ( 'NONE',  ( 4.418917755230268085, 1.760988537516799068, 0.7813691060932350663 ) ) ;
#147367=CARTESIAN_POINT ( 'NONE',  ( 0.3932109892899987025, 1.349039491128176227, 1.230163767592551638 ) ) ;
#147368=CARTESIAN_POINT ( 'NONE',  ( 0.6278963055918493907, -2.094311335337955882, 0.6960538111202837497 ) ) ;
#147374=CARTESIAN_POINT ( 'NONE',  ( 6.614111185624225620, 1.964402775464332507, -0.1412838390872969141 ) ) ;
#147375=CARTESIAN_POINT ( 'NONE',  ( 0.9779546479521743496, -1.895077795344397575, -0.4239509559331255395 ) ) ;
#147376=CARTESIAN_POINT ( 'NONE',  ( 6.714253291261501388, -1.839887274036870357, -1.377324995421406628 ) ) ;
#147378=CARTESIAN_POINT ( 'NONE',  ( 5.629708122894265365, 1.793948666107824774, -0.4946651665681394139 ) ) ;
#147384=CARTESIAN_POINT ( 'NONE',  ( 1.505704256594592838, -2.174480876681058827, 0.2726767719730335826 ) ) ;
#147387=CARTESIAN_POINT ( 'NONE',  ( 1.681982107312831154, -0.9779208310041755947, 1.541497997293653555 ) ) ;
#147390=CARTESIAN_POINT ( 'NONE',  ( 6.609000000000010644, 6.035875036286768136, 2.694900582964809388 ) ) ;
#147392=CARTESIAN_POINT ( 'NONE',  ( 0.1352084326644766299, -1.761967750658991028, 0.7794309377431463126 ) ) ;
#147393=CARTESIAN_POINT ( 'NONE',  ( 4.012515129279304205, 0.7020173944642660313, 1.832041770129029468 ) ) ;
#147397=CARTESIAN_POINT ( 'NONE',  ( 4.300438532332786501, 1.693616701070689956, -1.390861761948622766 ) ) ;
#147400=CARTESIAN_POINT ( 'NONE',  ( 3.151297481648129395, 1.777980080355131109, -1.060267355625019503 ) ) ;
#147404=CARTESIAN_POINT ( 'NONE',  ( 4.518391418568163509, -2.101855750862766659, 0.9310765106353561249 ) ) ;
#147408=CARTESIAN_POINT ( 'NONE',  ( 6.720655732516650716, 2.993363686233801779, 2.180545405541700177 ) ) ;
#147410=CARTESIAN_POINT ( 'NONE',  ( 3.802622829840444751, 1.666041102563616816, 0.9975114776080131751 ) ) ;
#147414=CARTESIAN_POINT ( 'NONE',  ( 4.394721148579957770, -1.856311205515799312, -0.4593126252911489127 ) ) ;
#147416=CARTESIAN_POINT ( 'NONE',  ( 5.543893992536840010, 0.6953672157433439249, -1.578584939873737047 ) ) ;
#147417=CARTESIAN_POINT ( 'NONE',  ( 5.032435514249763209, 0.5899841883351600869, 1.928258608204669766 ) ) ;
#147418=CARTESIAN_POINT ( 'NONE',  ( 5.625696599388652963, 0.4453364752643809155, 2.255009244304376992 ) ) ;
#147420=CARTESIAN_POINT ( 'NONE',  ( 0.2939702064862387276, 1.638257335637434364, 1.478849500172851217 ) ) ;
#147423=CARTESIAN_POINT ( 'NONE',  ( 6.257089712715798058, -1.519072588978742200, -0.9077291607378096261 ) ) ;
#147426=CARTESIAN_POINT ( 'NONE',  ( 1.394904949290655116, 1.871713452925367616, -1.323071089866036276 ) ) ;
#147427=CARTESIAN_POINT ( 'NONE',  ( 1.569815774166925859, -1.651746245857487638, -0.5483857920917082351 ) ) ;
#147428=CARTESIAN_POINT ( 'NONE',  ( 6.298795234281088895, 1.819837665574381091, 1.220625243075368127 ) ) ;
#147429=CARTESIAN_POINT ( 'NONE',  ( 1.475528429365607019, 1.526226248090801318, 0.8227105958887138693 ) ) ;
#147432=CARTESIAN_POINT ( 'NONE',  ( 1.451894146256039519, 1.643730891105445346, 1.418569794807096107 ) ) ;
#147433=CARTESIAN_POINT ( 'NONE',  ( 2.184780103950241248, 1.616692242240840960, -1.205043568535242304 ) ) ;
#147435=CARTESIAN_POINT ( 'NONE',  ( 5.725206259757900540, -0.04501307181254722567, 1.926136320475122288 ) ) ;
#147437=CARTESIAN_POINT ( 'NONE',  ( 2.830584216690882116, -1.098655552678593716, -1.930667878645520474 ) ) ;
#147444=CARTESIAN_POINT ( 'NONE',  ( 5.337372294182569199, 0.6981903941610733133, -1.594458651668466898 ) ) ;
#147445=CARTESIAN_POINT ( 'NONE',  ( 3.807043925254738781, -1.605251362286563177, 1.127602784832412386 ) ) ;
#147449=CARTESIAN_POINT ( 'NONE',  ( 4.938899882951366394, 0.3800905753248150498, 2.230106783295758177 ) ) ;
#147451=CARTESIAN_POINT ( 'NONE',  ( 1.188016131547619647, -1.306928873568227623, -1.595823035580832272 ) ) ;
#147455=CARTESIAN_POINT ( 'NONE',  ( 2.483610925836767791, 2.068663895631245531, -0.9166773448976636152 ) ) ;
#147459=CARTESIAN_POINT ( 'NONE',  ( 2.899504437521780442, -0.5904213222340527478, 1.774967144274109287 ) ) ;
#147460=CARTESIAN_POINT ( 'NONE',  ( 1.318582137269165733, 0.8549262331399180015, -1.508633131004229133 ) ) ;
#147461=CARTESIAN_POINT ( 'NONE',  ( 5.882419586753742102, -0.3201050945752722532, -2.167950725039065052 ) ) ;
#147462=CARTESIAN_POINT ( 'NONE',  ( 6.821333373144921275, -0.1693730316576994299, 2.270769535942236406 ) ) ;
#147463=CARTESIAN_POINT ( 'NONE',  ( 4.346650381253648554, 0.5737703434565506466, 2.084106190491950006 ) ) ;
#147464=CARTESIAN_POINT ( 'NONE',  ( 4.980387307702104138, -0.2395764092862572303, -1.927055426435628327 ) ) ;
#147468=CARTESIAN_POINT ( 'NONE',  ( 0.6875000000000004441, -1.451031289061094132, 1.451031289061148755 ) ) ;
#147473=CARTESIAN_POINT ( 'NONE',  ( 5.221327349844218091, 1.987046161919112430, 0.3419379449052239450 ) ) ;
#147478=CARTESIAN_POINT ( 'NONE',  ( 3.176193443437186126, -1.086901434622984830, 1.466744820640853098 ) ) ;
#147484=CARTESIAN_POINT ( 'NONE',  ( 0.4221360882172753293, -2.009675015244154483, 0.2020994116621494530 ) ) ;
#147485=CARTESIAN_POINT ( 'NONE',  ( 1.014494059972574691, -2.120667955011676487, 0.003750198165439199392 ) ) ;
#147489=CARTESIAN_POINT ( 'NONE',  ( 6.280161615599199720, -1.104627599893250434, 1.739653883609869833 ) ) ;
#147490=CARTESIAN_POINT ( 'NONE',  ( 5.344375030997434273, 0.3906003880304632636, -1.978050218768567792 ) ) ;
#147498=CARTESIAN_POINT ( 'NONE',  ( 5.272814466252145671, -2.006652483137221665, 0.1948127969565379425 ) ) ;
#147499=CARTESIAN_POINT ( 'NONE',  ( 4.980324010294663317, -0.2286266671043569454, -1.826820671449409295 ) ) ;
#147501=CARTESIAN_POINT ( 'NONE',  ( 2.772455145383013519, 1.235390390761299306, 1.949004725048721243 ) ) ;
#147503=CARTESIAN_POINT ( 'NONE',  ( 5.659502677682959337, 0.4278135246765999988, -2.118672983663777654 ) ) ;
#147505=CARTESIAN_POINT ( 'NONE',  ( 1.118581540066618141, -0.04615595083166770807, 1.941663063996822869 ) ) ;
#147509=CARTESIAN_POINT ( 'NONE',  ( 5.026898302747025760, 2.274369689431681163, -0.3307130315356506256 ) ) ;
#147512=CARTESIAN_POINT ( 'NONE',  ( 3.766346201128992988, -1.256895078192099335, 1.385637336983977397 ) ) ;
#147513=CARTESIAN_POINT ( 'NONE',  ( 1.248149539447914735, 0.9399939672071171426, -1.665319807275446706 ) ) ;
#147516=CARTESIAN_POINT ( 'NONE',  ( 2.860232119962682784, 2.196193069775736362, -0.2169517147150926140 ) ) ;
#147517=CARTESIAN_POINT ( 'NONE',  ( 6.983263157960340806, 6.037546352565132501, 2.441087094350186337 ) ) ;
#147522=CARTESIAN_POINT ( 'NONE',  ( 0.8957027828950543391, -0.7134963830764933235, 1.837871659531468804 ) ) ;
#147523=CARTESIAN_POINT ( 'NONE',  ( 1.448709080243043124, 2.305037702096077723, 0.1111474144101440020 ) ) ;
#147524=CARTESIAN_POINT ( 'NONE',  ( 1.785527960060459440, -1.848404783191982315, 0.6579185095809261252 ) ) ;
#147525=CARTESIAN_POINT ( 'NONE',  ( 5.682507089483013196, 1.232960659210121879, -1.653321649057968967 ) ) ;
#147532=CARTESIAN_POINT ( 'NONE',  ( 1.393694035345336424, -1.963709693186867833, 0.9261614696171887040 ) ) ;
#147534=CARTESIAN_POINT ( 'NONE',  ( 5.864778394761136049, 0.1288883805774850844, -1.836796581567698539 ) ) ;
#147538=CARTESIAN_POINT ( 'NONE',  ( 1.247088714334358750, -1.471066981041386335, -1.155250539242147045 ) ) ;
#147539=CARTESIAN_POINT ( 'NONE',  ( 5.923154835166896781, -0.05960684409221649049, 2.160954015416292506 ) ) ;
#147541=CARTESIAN_POINT ( 'NONE',  ( -0.02264175331117417728, 0.7142767504201595896, -2.172799776233569791 ) ) ;
#147543=CARTESIAN_POINT ( 'NONE',  ( 2.332540574144434053, 1.247770424613745543, -1.449200414897835909 ) ) ;
#147544=CARTESIAN_POINT ( 'NONE',  ( 3.344378923012015115, 0.4290688666262321149, 1.716912437317794415 ) ) ;
#147545=CARTESIAN_POINT ( 'NONE',  ( 0.4867802866235851345, -1.800715477623024086, -0.6440170976053718466 ) ) ;
#147547=CARTESIAN_POINT ( 'NONE',  ( 5.554270809058080793, -1.211575977211576172, 1.483806794280813302 ) ) ;
#147548=CARTESIAN_POINT ( 'NONE',  ( 6.215292997425397203, -1.688482396400727170, -1.013753615619580106 ) ) ;
#147550=CARTESIAN_POINT ( 'NONE',  ( 0.9672155168029163974, -1.668165459610539081, 1.309123814877902969 ) ) ;
#147552=CARTESIAN_POINT ( 'NONE',  ( 4.698043743269282757, -1.870269067358639958, -0.04562963166049315705 ) ) ;
#147553=CARTESIAN_POINT ( 'NONE',  ( 0.1877650043593872553, -0.8638833939697135866, 1.608357707688967242 ) ) ;
#147555=CARTESIAN_POINT ( 'NONE',  ( 4.653060005753134831, -1.773635849817876586, 1.313014255023836618 ) ) ;
#147558=CARTESIAN_POINT ( 'NONE',  ( 1.855998075696059901, -0.6969055236651957586, 1.941492863836144611 ) ) ;
#147565=CARTESIAN_POINT ( 'NONE',  ( 4.053231837324381637, 1.750648263899981849, -1.104974720517466480 ) ) ;
#147567=CARTESIAN_POINT ( 'NONE',  ( 1.757319832705085627, -1.853012815387704570, -1.112828241397870066 ) ) ;
#147569=CARTESIAN_POINT ( 'NONE',  ( 2.104171369714701534, -0.8614446868937111201, 1.826873676003283320 ) ) ;
#147573=EDGE_CURVE ( 'NONE', #175232, #89693, #167719, .T. ) ;
#147577=CARTESIAN_POINT ( 'NONE',  ( 0.3742329010679063539, -2.001858617179689492, -0.2420261300371470137 ) ) ;
#147578=CARTESIAN_POINT ( 'NONE',  ( 5.319949580897746166, 1.306013235697962571, -1.759773446019400778 ) ) ;
#147581=CARTESIAN_POINT ( 'NONE',  ( 4.060738401289211374, 0.5150538496448524572, 1.841637258418599155 ) ) ;
#147585=CARTESIAN_POINT ( 'NONE',  ( 1.968375273883906429, -1.978056371059619511, -0.3905749819678172585 ) ) ;
#147587=CARTESIAN_POINT ( 'NONE',  ( 0.04695162158900589161, -1.836028162657590501, 1.372410674757597704 ) ) ;
#147589=CARTESIAN_POINT ( 'NONE',  ( 4.682452625960944026, -1.673401091975829091, -0.4171936932430859168 ) ) ;
#147593=CARTESIAN_POINT ( 'NONE',  ( 0.07516593201273635838, 0.2333279341363985182, -2.077802470623245856 ) ) ;
#147596=CARTESIAN_POINT ( 'NONE',  ( 5.567019150587803722, -1.423986762948417972, 1.119560556780722083 ) ) ;
#147601=CARTESIAN_POINT ( 'NONE',  ( 5.988875474321468495, -1.722281623382706073, -0.5616633497566495548 ) ) ;
#147604=CARTESIAN_POINT ( 'NONE',  ( 3.293114190187882429, 1.727671002657789057, 1.348082825637614279 ) ) ;
#147607=CARTESIAN_POINT ( 'NONE',  ( 6.619592957969418379, 0.3166511089685022928, -1.833750044983559535 ) ) ;
#147609=CARTESIAN_POINT ( 'NONE',  ( 3.444859266486454352, -1.690994526066817105, -0.8999980677824627184 ) ) ;
#147616=CARTESIAN_POINT ( 'NONE',  ( 5.278551870535488355, -0.5171574069430958653, -2.053072726559619365 ) ) ;
#147617=CARTESIAN_POINT ( 'NONE',  ( 0.9190830904215806507, 1.997680973563022766, 0.8264451868333838602 ) ) ;
#147620=CARTESIAN_POINT ( 'NONE',  ( 1.131563826228650038, -1.154680578942975044, -1.414029504508321100 ) ) ;
#147622=CARTESIAN_POINT ( 'NONE',  ( 3.276193339942961913, -1.088440757138483539, 1.465454812695582865 ) ) ;
#147624=CARTESIAN_POINT ( 'NONE',  ( 2.777492966359981441, 0.2764497561681695803, -1.892163382976944419 ) ) ;
#147626=CARTESIAN_POINT ( 'NONE',  ( 2.910559396907284047, 0.6610699718948702674, 1.855445417178583911 ) ) ;
#147628=CARTESIAN_POINT ( 'NONE',  ( 4.563973399113295137, -1.265747467430546225, 1.473022616845516053 ) ) ;
#147631=CARTESIAN_POINT ( 'NONE',  ( 5.326475955075804514, -0.9554483686352827077, -1.893264085526874974 ) ) ;
#147633=CARTESIAN_POINT ( 'NONE',  ( 2.842330330863319876, 1.060513762474508015, -1.591057744338888913 ) ) ;
#147637=CARTESIAN_POINT ( 'NONE',  ( 4.442045433088864570, -1.240138855636420567, -1.585653348822992026 ) ) ;
#147639=CARTESIAN_POINT ( 'NONE',  ( 4.951681858558426796, 0.5695450498939165218, -1.734646904759745700 ) ) ;
#147640=CARTESIAN_POINT ( 'NONE',  ( 0.8189040078958352842, -1.500748464528355974, 1.426492703164506937 ) ) ;
#147645=CARTESIAN_POINT ( 'NONE',  ( 6.192256348250350761, -1.861847689568534081, -0.1814220289034565448 ) ) ;
#147657=CARTESIAN_POINT ( 'NONE',  ( 0.9716355300813659390, -0.3074278181635254348, 2.047203142020392441 ) ) ;
#147658=CARTESIAN_POINT ( 'NONE',  ( 2.566138216211190759, -1.085845923642224209, 1.817437617555809792 ) ) ;
#147661=CARTESIAN_POINT ( 'NONE',  ( 0.3737962156708526384, -1.932529848913757897, 0.3785758322861746406 ) ) ;
#147666=CARTESIAN_POINT ( 'NONE',  ( 2.484683925703546237, -0.3935552064166462083, -2.258081804418234473 ) ) ;
#147668=CARTESIAN_POINT ( 'NONE',  ( 2.566550162062298579, 0.6480892470011965223, 1.799338185917313870 ) ) ;
#147672=CARTESIAN_POINT ( 'NONE',  ( 0.2639318008525155523, 0.6274397771241714272, -1.913028341257965170 ) ) ;
#147673=CARTESIAN_POINT ( 'NONE',  ( 1.358172466202983042, -1.961936380284023063, -0.005482119489134959674 ) ) ;
#147677=CARTESIAN_POINT ( 'NONE',  ( 3.345728622622257564, 2.090823719190892049, -0.0003901280219448939298 ) ) ;
#147678=CARTESIAN_POINT ( 'NONE',  ( 2.904884094325186350, 1.494127413938572069, 0.9483235522904243098 ) ) ;
#147681=CARTESIAN_POINT ( 'NONE',  ( 5.191491443341288203, -0.8287821522852161227, 2.137368679509048963 ) ) ;
#147682=CARTESIAN_POINT ( 'NONE',  ( 4.734162553523208139, 0.3016713478377709423, 1.713805963711847680 ) ) ;
#147685=CARTESIAN_POINT ( 'NONE',  ( 3.901445378353602944, 0.2529189268129055090, 1.715120161964154510 ) ) ;
#147686=CARTESIAN_POINT ( 'NONE',  ( 4.211506895594858690, -1.802957179857124448, -1.209418758558492568 ) ) ;
#147688=CARTESIAN_POINT ( 'NONE',  ( 5.876185452347599814, -2.007255679753978228, -0.1928398672442974138 ) ) ;
#147689=CARTESIAN_POINT ( 'NONE',  ( 0.000000000000000000, 0.000000000000000000, -1.999999999999999556 ) ) ;
#147691=CARTESIAN_POINT ( 'NONE',  ( 3.539987092570716865, 0.8674169631235107980, -1.720131978839019693 ) ) ;
#147693=CARTESIAN_POINT ( 'NONE',  ( 5.783471039277606529, 0.1639875503032099946, -2.215378355603670357 ) ) ;
#147695=CARTESIAN_POINT ( 'NONE',  ( 6.883263157960407774, 1.288564682660230831, 1.962666442651111565 ) ) ;
#147698=CARTESIAN_POINT ( 'NONE',  ( 1.682608811002960447, 1.145563986048125704, 1.903002289297763605 ) ) ;
#147699=CARTESIAN_POINT ( 'NONE',  ( 6.672321430365630412, -0.9237476215336395402, -1.730755693189582667 ) ) ;
#147705=CARTESIAN_POINT ( 'NONE',  ( 4.809062498722087575, -1.658680843151142392, 1.225972815312638353 ) ) ;
#147710=CARTESIAN_POINT ( 'NONE',  ( 6.450466390465378730, 0.5869013949594548141, 1.776180802621520005 ) ) ;
#147711=CARTESIAN_POINT ( 'NONE',  ( 5.186046676097956443, 1.422060760911178390, 0.9921614550853893322 ) ) ;
#147712=CARTESIAN_POINT ( 'NONE',  ( 4.616618505336416156, -0.07905358554981949115, 1.738770568734932853 ) ) ;
#147714=CARTESIAN_POINT ( 'NONE',  ( 1.892491709730130145, -0.6158747592755541289, -2.208019654398277520 ) ) ;
#147716=CARTESIAN_POINT ( 'NONE',  ( 5.882390464068013358, -0.3075192527470702042, -2.067890480286633803 ) ) ;
#147717=CARTESIAN_POINT ( 'NONE',  ( 0.8316833483592298570, 1.813467871694788069, 0.3170515863319539052 ) ) ;
#147720=CARTESIAN_POINT ( 'NONE',  ( 2.397230751819504402, 1.409552409829779140, 1.160114028286141075 ) ) ;
#147721=CARTESIAN_POINT ( 'NONE',  ( 3.041638857185970046, -1.525043868314728934, 1.319228477497782714 ) ) ;
#147722=CARTESIAN_POINT ( 'NONE',  ( 1.289316216709124996, 1.661312375189183399, 1.429258102917586815 ) ) ;
#147725=CARTESIAN_POINT ( 'NONE',  ( 1.152881054890652957, -0.5012615762394446728, -2.008655542368184221 ) ) ;
#147728=CARTESIAN_POINT ( 'NONE',  ( 4.108145954595856075, -0.8103754143699601897, 1.959725966023172727 ) ) ;
#147732=CARTESIAN_POINT ( 'NONE',  ( 6.199803715563785289, -0.6102442156579389598, 1.720816905678754782 ) ) ;
#147739=CARTESIAN_POINT ( 'NONE',  ( 3.234633093136650928, 1.278207680322031026, -1.563912617747134970 ) ) ;
#147740=CARTESIAN_POINT ( 'NONE',  ( 0.9210891864466156376, 1.945811402625597486, 0.8060233215861163369 ) ) ;
#147743=CARTESIAN_POINT ( 'NONE',  ( 4.961672996587167539, -0.4989766864872626217, 1.792691909438326681 ) ) ;
#147748=CARTESIAN_POINT ( 'NONE',  ( 6.157116169989634180, -1.766321488544853935, -1.061543263526150138 ) ) ;
#147752=CARTESIAN_POINT ( 'NONE',  ( 2.319350913329641717, -1.342983818224493531, 1.096632721805221200 ) ) ;
#147753=CARTESIAN_POINT ( 'NONE',  ( 1.499541640181512481, -0.6240335575410212998, -1.624780663456944385 ) ) ;
#147754=CARTESIAN_POINT ( 'NONE',  ( 6.516287943725491694, -1.081378002916585368, -2.038673766938512877 ) ) ;
#147757=CARTESIAN_POINT ( 'NONE',  ( 2.618495166727810908, 1.348686541216067347, -1.558216953862724408 ) ) ;
#147759=CARTESIAN_POINT ( 'NONE',  ( 1.528672481244568448, 1.986742605292156405, -0.3418812301651391605 ) ) ;
#147760=CARTESIAN_POINT ( 'NONE',  ( 6.925078400183526384, 2.431821113958906544, 2.425929786733098226 ) ) ;
#147762=CARTESIAN_POINT ( 'NONE',  ( 0.8484322082523039210, 0.5699466304493487900, 1.887293252202123739 ) ) ;
#147764=CARTESIAN_POINT ( 'NONE',  ( 4.728717205193702533, 1.314622909153417174, -1.389140896021365368 ) ) ;
#147766=CARTESIAN_POINT ( 'NONE',  ( 5.971336403843030105, 0.1662174427981797931, -2.200672837095698497 ) ) ;
#147770=CARTESIAN_POINT ( 'NONE',  ( 0.2584707923105635796, 2.014430608512500775, 0.1461574478831758339 ) ) ;
#147772=CARTESIAN_POINT ( 'NONE',  ( 4.348838485402671594, 0.6111939248801941948, 2.225120539556017629 ) ) ;
#147773=CARTESIAN_POINT ( 'NONE',  ( 5.037533845850875380, 1.831247050742194515, -0.7043679133837479345 ) ) ;
#147774=CARTESIAN_POINT ( 'NONE',  ( 1.410910527293834260, -1.549868713165471590, 1.202602906592651788 ) ) ;
#147778=CARTESIAN_POINT ( 'NONE',  ( -0.02988430322643093051, -0.9920087411236072628, 1.870552836459241419 ) ) ;
#147781=CARTESIAN_POINT ( 'NONE',  ( 0.5328340850149284602, -1.300071877079148841, -1.303948673260245439 ) ) ;
#147783=CARTESIAN_POINT ( 'NONE',  ( 4.276368498475341617, -1.111101898244113872, -1.865058090000100366 ) ) ;
#147785=CARTESIAN_POINT ( 'NONE',  ( 2.303126745213024851, -0.3670769733005623814, -2.088442229865586697 ) ) ;
#147790=CARTESIAN_POINT ( 'NONE',  ( 2.302092711735738373, -2.060399031734764463, 0.04731154407941646350 ) ) ;
#147792=DIRECTION ( 'NONE',  ( -3.451266460341926649E-31, -5.200010849845536803E-32, 1.000000000000000000 ) ) ;
#147794=CARTESIAN_POINT ( 'NONE',  ( 0.07755575628181145265, 0.6932613274447991802, -2.271134039238668301 ) ) ;
#147796=CARTESIAN_POINT ( 'NONE',  ( 6.076807558263135789, -1.348954070496380941, 1.355674883165632227 ) ) ;
#147799=CARTESIAN_POINT ( 'NONE',  ( 1.704739465036476442, -0.8136145326368517949, -2.111227425349770481 ) ) ;
#147801=CARTESIAN_POINT ( 'NONE',  ( 1.124954419467529831, 1.598432135740068372, 0.8524628987082534248 ) ) ;
#147802=CARTESIAN_POINT ( 'NONE',  ( 2.430754934859931549, -1.590173441703069956, 1.067998681346548961 ) ) ;
#147803=CARTESIAN_POINT ( 'NONE',  ( 2.594261239525695206, 0.9781076984213372683, -1.824767828009652426 ) ) ;
#147806=CARTESIAN_POINT ( 'NONE',  ( 1.147272922670502515, -1.552894836003695600, -1.214464739729806730 ) ) ;
#147807=CARTESIAN_POINT ( 'NONE',  ( 5.127533266204091333, -1.828772253489078237, 0.6060055780525953617 ) ) ;
#147808=CARTESIAN_POINT ( 'NONE',  ( 0.6808296902291348651, -1.277277952767090774, 1.921808783382691788 ) ) ;
#147811=CARTESIAN_POINT ( 'NONE',  ( 5.002416047594211435, 2.056911163480923843, 0.1552035700525862538 ) ) ;
#147815=CARTESIAN_POINT ( 'NONE',  ( 6.176810970088661534, -1.998525488361714508, -0.6642400113570454678 ) ) ;
#147818=CARTESIAN_POINT ( 'NONE',  ( 5.079442160427912967, 2.018932005888602887, -0.7727740077691500620 ) ) ;
#147819=CARTESIAN_POINT ( 'NONE',  ( 5.250651393837939551, 1.990147761501987800, 0.3430726210427292311 ) ) ;
#147827=CARTESIAN_POINT ( 'NONE',  ( 4.012907874177486178, 0.1037781579101039742, 2.014008197856680393 ) ) ;
#147832=CARTESIAN_POINT ( 'NONE',  ( 4.821240550277555492, -0.1094919189667045711, 2.159058991224649393 ) ) ;
#147837=CARTESIAN_POINT ( 'NONE',  ( 5.888296041240274725, -0.7283935311428509918, -1.880430420734761965 ) ) ;
#147839=CARTESIAN_POINT ( 'NONE',  ( 0.6622201036875573488, -1.252624510564132931, 1.186060005986578014 ) ) ;
#147843=CARTESIAN_POINT ( 'NONE',  ( 6.257094453949625823, -1.604276942902042480, -0.9616840659161307592 ) ) ;
#147844=CARTESIAN_POINT ( 'NONE',  ( 0.9264321329857813092, -0.9072109017984790746, -1.797169606962043309 ) ) ;
#147846=CARTESIAN_POINT ( 'NONE',  ( 3.399657359236216703, 1.738403758043248759, 1.359216269546263511 ) ) ;
#147850=CARTESIAN_POINT ( 'NONE',  ( 2.244932509249154329, 2.057497683098849617, 0.5125483897536405875 ) ) ;
#147851=CARTESIAN_POINT ( 'NONE',  ( 1.634388897023292486, 0.6352195160324504153, 1.913798142305182415 ) ) ;
#147852=CARTESIAN_POINT ( 'NONE',  ( 2.056637812947777810, 0.3998733141725440698, 1.766706770180977548 ) ) ;
#147860=CARTESIAN_POINT ( 'NONE',  ( -0.2411972340276360705, -0.002466136893084554509, -1.900252416837118430 ) ) ;
#147869=CARTESIAN_POINT ( 'NONE',  ( 3.590839768554392908, -0.4196827604958653923, -2.120402733634827452 ) ) ;
#147872=CARTESIAN_POINT ( 'NONE',  ( 1.564851893998190135, 0.6701894319398638000, 2.011955567234039677 ) ) ;
#147874=CARTESIAN_POINT ( 'NONE',  ( 3.216049615590831579, -0.9687177021495720908, -1.716833007709689607 ) ) ;
#147875=CARTESIAN_POINT ( 'NONE',  ( 5.554919272666569263, 0.3793472168572444292, 1.874222000232607765 ) ) ;
#147878=CARTESIAN_POINT ( 'NONE',  ( 6.672316266636414639, -0.9270569987065898632, -1.737699753229291710 ) ) ;
#147879=CARTESIAN_POINT ( 'NONE',  ( 1.077954490650166575, -1.894526023430597617, -0.4258829084243920260 ) ) ;
#147884=CARTESIAN_POINT ( 'NONE',  ( 2.378955762007132435, 1.911079870108543410, -0.8480884496332024014 ) ) ;
#147888=CARTESIAN_POINT ( 'NONE',  ( 5.584596538761583240, -1.209766832763665034, 1.480987728393488245 ) ) ;
#147890=CARTESIAN_POINT ( 'NONE',  ( 4.899154391205060577, 1.836108854712194649, -1.224054507610386366 ) ) ;
#147891=CARTESIAN_POINT ( 'NONE',  ( 1.870444250305805856, 1.134645063044220858, 1.892580404734986121 ) ) ;
#147893=CARTESIAN_POINT ( 'NONE',  ( 0.5219363917940004205, -1.903054291476031112, 0.1877445768119419822 ) ) ;
#147896=CARTESIAN_POINT ( 'NONE',  ( 4.088381982606685838, 1.110138344689771239, -1.747393465062855311 ) ) ;
#147898=CARTESIAN_POINT ( 'NONE',  ( 1.182749364907993206, -2.109161078630458430, -0.4729781282231394490 ) ) ;
#147899=CARTESIAN_POINT ( 'NONE',  ( 4.107102485094754840, -0.3736803571842538529, 2.159302612355806339 ) ) ;
#147906=CARTESIAN_POINT ( 'NONE',  ( 0.3873425458618062200, -0.6819987885887256462, -1.897696807414723796 ) ) ;
#147909=CARTESIAN_POINT ( 'NONE',  ( 4.258688845354158481, -0.6446009455991276171, -1.967446834807617284 ) ) ;
#147910=CARTESIAN_POINT ( 'NONE',  ( 5.308266703545434062, 1.260341450243172678, -1.701113402177101053 ) ) ;
#147913=CARTESIAN_POINT ( 'NONE',  ( 3.696117419531047776, 0.8894436365228419739, -1.757264023730123581 ) ) ;
#147914=CARTESIAN_POINT ( 'NONE',  ( 5.753944192167276483, 0.9242165444633635429, 2.097870995526931015 ) ) ;
#147915=CARTESIAN_POINT ( 'NONE',  ( 3.439906511156048285, 0.8199118703316324863, -1.631291955839441865 ) ) ;
#147922=CARTESIAN_POINT ( 'NONE',  ( 5.308844932141564499, -0.4931833774270472648, -1.951727149811402828 ) ) ;
#147923=CARTESIAN_POINT ( 'NONE',  ( 6.153027625867640182, 1.178261263523974645, 1.973664585577431518 ) ) ;
#147924=CARTESIAN_POINT ( 'NONE',  ( 4.451973756923766068, -0.7546651901383871763, 1.810992078419524365 ) ) ;
#147929=CARTESIAN_POINT ( 'NONE',  ( 0.5563344311030217204, -1.511574431613523117, 1.444666882759609194 ) ) ;
#147930=CARTESIAN_POINT ( 'NONE',  ( 5.612081123951941919, -0.7985520710115794341, -1.579504676149855458 ) ) ;
#147932=CARTESIAN_POINT ( 'NONE',  ( 2.361504994916805877, 2.148894721571582789, -0.4289216190115978100 ) ) ;
#147933=CARTESIAN_POINT ( 'NONE',  ( 1.469815953039468326, -1.652492729624547962, -0.5465173985150991731 ) ) ;
#147935=CARTESIAN_POINT ( 'NONE',  ( 0.2333690889706682703, 1.352610664630080839, -2.308230059406161772 ) ) ;
#147936=CARTESIAN_POINT ( 'NONE',  ( 1.189626395179286478, -0.7786649258869399182, 1.539184141221685787 ) ) ;
#147937=CARTESIAN_POINT ( 'NONE',  ( 1.822082775007987543, 1.258534617508931586, -1.793986466278547853 ) ) ;
#147939=CARTESIAN_POINT ( 'NONE',  ( 3.950008152305323428, 0.7444041667201054535, -2.077678867657362538 ) ) ;
#147942=CARTESIAN_POINT ( 'NONE',  ( 1.411231479646192222, -1.713112901771263630, 1.333658509791965097 ) ) ;
#147943=CARTESIAN_POINT ( 'NONE',  ( 0.02954982209854748257, -1.120125052174587577, -1.442194003765177257 ) ) ;
#147944=CARTESIAN_POINT ( 'NONE',  ( 2.430995767774553062, -1.757534028733166442, 1.180493747047051567 ) ) ;
#147945=CARTESIAN_POINT ( 'NONE',  ( 6.539320575229274901, 7.629137130509072051, 2.496737603865983424 ) ) ;
#147947=CARTESIAN_POINT ( 'NONE',  ( 2.349550187768103093, 0.6076851952682017499, -2.210314646808369421 ) ) ;
#147952=CARTESIAN_POINT ( 'NONE',  ( 4.881579437514656838, 0.2187098293420664807, -2.210487333941961285 ) ) ;
#147959=CARTESIAN_POINT ( 'NONE',  ( 3.463517678199812266, -1.944071305346905643, -0.5350885120067662148 ) ) ;
#147961=CARTESIAN_POINT ( 'NONE',  ( 0.8134211793521692879, -1.740389775365951186, -1.106656028277221537 ) ) ;
#147967=CARTESIAN_POINT ( 'NONE',  ( 4.312563266315373234, 2.003113633248252867, 0.8892094534625747393 ) ) ;
#147968=CARTESIAN_POINT ( 'NONE',  ( 2.830704105008190030, 0.7231396562890278767, -1.882474209725725434 ) ) ;
#147969=CARTESIAN_POINT ( 'NONE',  ( 1.065666191918061445, -1.167978014494171823, 1.423405568861766168 ) ) ;
#147973=CARTESIAN_POINT ( 'NONE',  ( 5.456004705108882469, 1.823398332572896186, -0.09148835057352226741 ) ) ;
#147974=CARTESIAN_POINT ( 'NONE',  ( 5.854138739207011888, 0.1455364397412381439, -2.011204036175239018 ) ) ;
#147976=CARTESIAN_POINT ( 'NONE',  ( 4.170984489290855635, -2.109804223432755865, -0.8175660662063081174 ) ) ;
#147978=CARTESIAN_POINT ( 'NONE',  ( 1.102331697304242297, -2.106257354988652075, 0.001776637707836397316 ) ) ;
#147980=CARTESIAN_POINT ( 'NONE',  ( 4.422371208857902580, 0.9731212702417373350, 1.827393648576709717 ) ) ;
#147984=B_SPLINE_CURVE_WITH_KNOTS ( 'NONE', 3,
 ( #210947, #29026, #152109, #66547, #83891, #481, #182454, #117533, #199768, #183527, #45285, #184585, #149982, #95108, #178476, #34082, #200819, #132690, #133759, #161157, #151054, #198697, #116461, #50341, #127682, #99102, #84965, #177409, #82831, #19948, #61517, #33025, #101208, #168355, #100152, #165155, #12744, #111405, #78818, #144940, #62573, #46349, #167294, #35135, #166216, #16747, #18881, #17808, #128735, #1553, #2621, #118596, #67614, #52470, #51413, #194709, #68692, #36203, #102278, #212839, #126358, #161990, #110094, #45048, #112229, #64476, #144702, #211771, #176105, #14635, #164117, #28778, #98061, #163055, #193404, #129560, #192317, #97002, #62341, #13580, #208562, #179305, #31983, #160914, #111160, #27705, #15700, #142556, #43975, #60197, #94860, #180357, #46111, #93800, #159840, #143638, #11441, #195547, #77516, #78580, #209632, #145770, #130616, #12509, #61272, #127434, #113297, #177160, #210713, #47184, #128501, #194469, #178237, #29853, #95934, #79653, #63409, #30926, #80729, #146819, #196608, #48248, #114363, #131653, #50353, #51425, #49302, #53546, #148918, #167305, #100165, #1564, #199779, #117545, #132702, #152122, #116475, #182465, #68703, #169429, #197656, #82842, #67626, #69769, #16759, #33037, #134825, #133771, #183539, #115418, #34094, #201894, #166229, #165164, #184596, #81786, #492, #86046, #35145, #151068, #99115, #101221, #135875, #83903, #17819, #181410, #84976, #66560, #3692, #198708, #2630, #149993, #119678, #102293, #200829, #52480, #185665, #18892, #118608, #37294, #36214, #168367, #19962, #103367, #65506, #147869, #213884, #42662, #23155, #40517, #171558, #139083, #74070, #156395, #140163, #4755, #141248, #106619, #202973, #138013, #205110, #89269, #170490, #204028, #122918, #189943, #155319, #72980, #6903, #87111, #55676, #41592, #136947, #39431, #190996, #21013, #121832, #57814, #125040, #105524, #187803, #5832, #7981, #207257, #188876, #56753, #71904, #123976, #206186, #172648, #24224, #107704, #90326, #22074, #173730, #25307, #75139, #91409, #157469, #9064, #154258, #108771, #88186, #58885, #153181, #70830, #54614, #120762, #186740, #38362, #104441, #48000, #144452, #111981, #29597, #10121, #208316, #26372, #176907, #76196, #143376, #210455, #93541, #80471, #92485, #113044, #95683, #179050, #128252, #174796, #28522, #94612, #44796, #30669, #158524, #160655, #110901, #175854, #12253, #162802, #109840, #27443, #96752, #212588, #45860, #159585, #126102, #78330, #195295, #14379, #59946, #194215, #146570, #64227, #129319, #161737, #62093, #177982, #130369, #13328, #79402, #11183, #196359, #142305, #145519, #192062, #43725, #77262, #211518, #63154, #209375, #46926, #61019, #127178, #193146, #102055, #49049, #65261, #167060, #99924, #17571, #115169, #131408, #33843, #134589, #184353, #213635, #133523, #118364, #35975, #68461, #100971, #83655, #1322, #168121, #116229, #50108, #147617, #117296, #181164, #19722, #197408, #32788, #85801, #183293, #199530, #98864, #81535, #135631, #182220, #51173, #165985, #149745, #18652, #34898, #84731, #97807, #151881, #150820, #164916, #16509, #3455, #67383, #2383, #82591, #200589, #201651, #246, #69524, #52237, #148678, #114118, #163870, #180110, #31734, #15446, #66318, #132462, #198464, #41347, #139912, #152934, #140999, #157217, #169180, #53301, #5576 ),
 .UNSPECIFIED., .F., .F.,
 ( 4, 1, 1, 1, 1, 1, 1, 1, 1, 1, 1, 1, 1, 1, 1, 1, 1, 1, 1, 1, 1, 1, 1, 1, 1, 1, 1, 1, 1, 1, 1, 1, 1, 1, 1, 1, 1, 1, 1, 1, 1, 1, 1, 1, 1, 1, 1, 1, 1, 1, 1, 1, 1, 1, 1, 1, 1, 1, 1, 1, 1, 1, 1, 1, 1, 1, 1, 1, 1, 1, 1, 1, 1, 1, 1, 1, 1, 1, 1, 1, 1, 1, 1, 1, 1, 1, 1, 1, 1, 1, 1, 1, 1, 1, 1, 1, 1, 1, 1, 1, 1, 1, 1, 1, 1, 1, 1, 1, 1, 1, 1, 1, 1, 1, 1, 1, 1, 1, 1, 1, 1, 1, 1, 1, 1, 1, 1, 1, 1, 1, 1, 1, 1, 1, 1, 1, 1, 1, 1, 1, 1, 1, 1, 1, 1, 1, 1, 1, 1, 1, 1, 1, 1, 1, 1, 1, 1, 1, 1, 1, 1, 1, 1, 1, 1, 1, 1, 1, 1, 1, 1, 1, 1, 1, 1, 1, 1, 1, 1, 1, 1, 1, 1, 1, 1, 1, 1, 1, 1, 1, 1, 1, 1, 1, 1, 1, 1, 1, 1, 1, 1, 1, 1, 1, 1, 1, 1, 1, 1, 1, 1, 1, 1, 1, 1, 1, 1, 1, 1, 1, 1, 1, 1, 1, 1, 1, 1, 1, 1, 1, 1, 1, 1, 1, 1, 1, 1, 1, 1, 1, 1, 1, 1, 1, 1, 1, 1, 1, 1, 1, 1, 1, 1, 1, 1, 1, 1, 1, 1, 1, 1, 1, 1, 1, 1, 1, 1, 1, 1, 1, 1, 1, 1, 1, 1, 1, 1, 1, 1, 1, 1, 1, 1, 1, 1, 1, 1, 1, 1, 1, 1, 1, 1, 1, 1, 1, 1, 1, 1, 1, 1, 1, 1, 1, 1, 1, 1, 1, 1, 1, 1, 1, 1, 1, 1, 1, 1, 1, 1, 1, 1, 1, 1, 1, 1, 1, 1, 1, 1, 1, 1, 1, 1, 1, 1, 1, 1, 1, 1, 1, 1, 1, 1, 1, 1, 1, 1, 1, 1, 1, 1, 1, 1, 1, 1, 1, 1, 1, 1, 1, 1, 1, 1, 1, 1, 1, 1, 1, 1, 1, 1, 1, 1, 1, 1, 1, 1, 1, 1, 1, 1, 1, 1, 1, 4 ),
 ( 0.000000000000000000, 0.002599909708945224215, 0.005208776875251038344, 0.007813105021672143990, 0.01041684075506122895, 0.01302033053878596733, 0.01562516449037322508, 0.01822901888718816976, 0.02083333248856494152, 0.02343767784666880849, 0.02604151204071371642, 0.02864616705684025488, 0.03124974664057501156, 0.03385445107693609706, 0.03645811663825353210, 0.03906264587105176544, 0.04166673705245293319, 0.04427082116499847508, 0.04687535697974040683, 0.04947901875943551409, 0.05208372524935509645, 0.05468730636643894666, 0.05729195276349181160, 0.05989578571700067411, 0.06250012971910297310, 0.06510448174046053194, 0.06770830932160050442, 0.07031296016926287529, 0.07291653972921435800, 0.07552124384959360559, 0.07812490789241745281, 0.08072943556986492131, 0.08333352577934262373, 0.08593760861062926804, 0.08854214333088818167, 0.09114580385899402615, 0.09375050919907033931, 0.09635408915385039463, 0.09895873428887830281, 0.1015625661591952889, 0.1041669088510773916, 0.1067712598504420435, 0.1093750861808121810, 0.1119797359579501050, 0.1145833143474069837, 0.1171880172914337714, 0.1197916802446672702, 0.1223962066585842084, 0.1250002958591681090, 0.1276043774339237491, 0.1302089111537957367, 0.1328125705047451810, 0.1354172747579587832, 0.1380208536162275679, 0.1406254975582941213, 0.1432293284131295197, 0.1458336698625422867, 0.1484380199076493767, 0.1510418450546419100, 0.1536464938294531402, 0.1562500711155297428, 0.1588547729514310503, 0.1614584348822658832, 0.1640629601007041471, 0.1666670483599762276, 0.1692711287458052438, 0.1718756615333107141, 0.1744793197742946778, 0.1770840230088624179, 0.1796876008377196188, 0.1822922436549848091, 0.1848960735616705098, 0.1875004138364584350, 0.1901047629951247708, 0.1927085870260826783, 0.1953132348667029061, 0.1979168111164897881, 0.2005215119124719170, 0.2031251728880697216, 0.2057296969790492203, 0.2083337843645647058, 0.2109378636290424602, 0.2135423955521746908, 0.2161460527503557827, 0.2187507550344668650, 0.2213543319009846355, 0.2239589736615800464, 0.2265628026874214052, 0.2291671418554001027, 0.2317714901954165685, 0.2343753131776551424, 0.2369799601521939414, 0.2395835354327550959, 0.2421882352569974250, 0.2447918953444941648, 0.2473964183760076208, 0.2500005049552969649, 0.2526045831659717300, 0.2552091142926994904, 0.2578127705152143956, 0.2604174719170327390, 0.2630210478882585856, 0.2656256886602897938, 0.2682295168725681855, 0.2708338550015275126, 0.2734382025906618163, 0.2760420245914711468, 0.2786466707680146371, 0.2812502451463897990, 0.2838549440670474211, 0.2864586033335557724, 0.2890631253735708728, 0.2916672112141422968, 0.2942712884385379479, 0.2968758188368077477, 0.2994794741507696423, 0.3020841747384366283, 0.3046877498813952978, 0.3072923897329448151, 0.3098962171989202430, 0.3125005543566263810, 0.3151049012626256918, 0.3177087223492732204, 0.3203133677958864278, 0.3229169413390938770, 0.3255216394243000688, 0.3281252979369121969, 0.3307298190533745630, 0.3333339042227165261, 0.3359379805283350118, 0.3385425102660742369, 0.3411461647385755636, 0.3437508645802123675, 0.3463544389619092612, 0.3489590779610384774, 0.3515629047479519320, 0.3541672410021501904, 0.3567715872927431642, 0.3593754075324762653, 0.3619800523172059803, 0.3645836250922447341, 0.3671883224101137877, 0.3697919802359038166, 0.3723965004967392245, 0.3750005850623230885, 0.3776046605166471504, 0.3802091896617659783, 0.3828128433598806946, 0.3854175425235913388, 0.3880211162110140388, 0.3906257544257662473, 0.3932295806008425099, 0.3958339160192597128, 0.3984382617621595180, 0.4010420812222079689, 0.4036467254130849946, 0.4062502974869375283, 0.4088549941055670267, 0.4114586513115932598, 0.4140631707847102772, 0.4166672548139925825, 0.4192713294844879757, 0.4218758581048823730, 0.4244795110956688933, 0.4270842096495421902, 0.4296877827096635682, 0.4322924202080664635, 0.4348962458385162155, 0.4375005804888632555, 0.4401049257517701263, 0.4427087444993486054, 0.4453133881643903114, 0.4479169596040251111, 0.4505216555914985932, 0.4531253122448062887, 0.4557298309980991058, 0.4583339145585244578, 0.4609379885126426157, 0.4635425166761967808, 0.4661461690266998081, 0.4687508670388120247, 0.4713544395385928509, 0.4739590763886608604, 0.4765629015416836811, 0.4791672354916582388, 0.4817715803422617515, 0.4843753984445725025, 0.4869800416517858221, 0.4895836125241597725, 0.4921883079485492862, 0.4947919641161733773, 0.4973964822175238609, 0.5000005653765271507, 0.5026046386817077938, 0.5052091664562964324, 0.5078128182335502894, 0.5104175157719683664, 0.5130210877783591972, 0.5156257240480961457, 0.5182295487908826770, 0.5208338821081714975, 0.5234382266141532902, 0.5260420441383883983, 0.5286466869557716608, 0.5312502573278325979, 0.5338549522572011430, 0.5364586080061681805, 0.5390631255234488162, 0.5416672083484578293, 0.5442712810721315186, 0.5468758085256230084, 0.5494794597966533578, 0.5520841569294364648, 0.5546877285093810839, 0.5572923642667827471, 0.5598961886665174692, 0.5625005214187991376, 0.5651048656478350196, 0.5677086826611791315, 0.5703133251567252815, 0.5729168950954143247, 0.5755215895978186280, 0.5781252449951498340, 0.5807297619962258350, 0.5833338445546641937, 0.5859379167642547737, 0.5885424439645127181, 0.5911460947963396162, 0.5937507915915425372, 0.5963543628119793993, 0.5989589981250363904, 0.6015628222488997867, 0.6041671545038470592, 0.6067714985236103420, 0.6093753150932430529, 0.6119799573349418154, 0.6145835269071964202, 0.6171882210506893784, 0.6197918761634028106, 0.6223963927161352272, 0.6250004750754242222, 0.6276045468383509851, 0.6302090738532378777, 0.6328127243128783830, 0.6354174208385534595, 0.6380209917664191321, 0.6406256267031188445, 0.6432294506182901772, 0.6458337824435727015, 0.6484381263217364744, 0.6510419425148348260, 0.6536465845706755928, 0.6562501538434313275, 0.6588548476960643940, 0.6614585025911776661, 0.6640630187634258830, 0.6666671009909873602, 0.6692711723746683772, 0.6718756992720475996, 0.6744793494265174383, 0.6770840457507175669, 0.6796876164529486175, 0.6822922510812780006, 0.6848960748549377531, 0.6875004063182246217, 0.6901047501224634173, 0.6927085660062048955, 0.6953132079441787239, 0.6979167769843723779, 0.7005214706141982273, 0.7031251253587310623, 0.7057296412183544643, 0.7083337233816132672, 0.7109377944534676086, 0.7135423213012055399, 0.7161459712175226588, 0.7187506674083037339, 0.7213542379518396164, 0.7239588723397878400, 0.7265626960391206035, 0.7291670272080824633, 0.7317713710060759214, 0.7343751866476402324, 0.7369798285357428425, 0.7395833974103146469, 0.7421880908853900616, 0.7447917455463664016, 0.7473962611612280371, 0.7500003433276148934, 0.7526044141550642941, 0.7552089410210337528, 0.7578125907662203176, 0.7604172868916432293, 0.7630208573434285046, 0.7656254915589897347, 0.7682293152511859846, 0.7708336461934980344, 0.7734379900529331220, 0.7760418055195050790, 0.7786464474257392965, 0.7812500162016354777, 0.7838547095900232353, 0.7864583642344741277, 0.7890628796724428184, 0.7916669619093961163, 0.7942710325598689725, 0.7968755595119511037, 0.7994792091530360523, 0.8020839052811703507, 0.8046874757081575735, 0.8072921098193328593, 0.8098959335715922858, 0.8125002643549369408, 0.8151046083435100620, 0.8177084237022821389, 0.8203130656946604482, 0.8229166344388356702, 0.8255213278086077633, 0.8281249825035741363, 0.8307294978325265866, 0.8333335802074958165, 0.8359376507484286289, 0.8385421778545157911, 0.8411458274585372763, 0.8437505236574627254, 0.8463540941266142204, 0.8489587282014147140, 0.8515625520809478877, 0.8541668827730166669, 0.8567712269584367712, 0.8593750422766117669, 0.8619796844231587540, 0.8645832532025788941, 0.8671879466218186394, 0.8697916014343529678, 0.8723961167221769841, 0.8750001993026245151, 0.8776042698014647758, 0.8802087971294628721, 0.8828124467634709260, 0.8854171431012803906, 0.8880207136795719158, 0.8906253477860208712, 0.8932291718600525732, 0.8958335025285494302, 0.8984378469785403443, 0.9010416623233333810, 0.9036463046920883979, 0.9062498735737328781, 0.9088545671105374701, 0.9114582221077071056, 0.9140627374223044832, 0.9166668202757080053, 0.9192708907999164181, 0.9218754184177497812, 0.9244790681488107564, 0.9270837646936044285, 0.9296873354480212903, 0.9322919696541906998, 0.9348957939899811276, 0.9375001247025137596, 0.9401044694846933947, 0.9427082849236875228, 0.9453129275835465695, 0.9479164966330613229, 0.9505211903504858784, 0.9531248456066239161, 0.9557293610412391782, 0.9583334441921064206, 0.9609375147049603605, 0.9635420428945489224, 0.9661456931510739032, 0.9687503890924937799, 0.9713539588735070618, 0.9739585961357111188, 0.9765624261165479769, 0.9791667493207181217, 0.9817710620974646751, 0.9843748983037424738, 0.9869797303524157073, 0.9895832060093603388, 0.9921869237806116848, 0.9947912468131487884, 0.9974000922265050528, 0.9999999999999998890 ),
 .UNSPECIFIED. ) ;
#147990=CARTESIAN_POINT ( 'NONE',  ( 1.230900525853476868, 1.420129835883350955, -1.575055732827963295 ) ) ;
#147991=CARTESIAN_POINT ( 'NONE',  ( 1.705654399339423311, 1.929789488239462836, -1.100201954495036549 ) ) ;
#147995=CARTESIAN_POINT ( 'NONE',  ( 3.631260574587381829, 0.05062604155347744800, -1.961386756325018021 ) ) ;
#148001=CARTESIAN_POINT ( 'NONE',  ( 1.986737319265439394, -1.300789755646198476, 1.674730562594067829 ) ) ;
#148003=CARTESIAN_POINT ( 'NONE',  ( 5.828557447170540584, -1.245780601409246957, 1.515539014345569147 ) ) ;
#148004=CARTESIAN_POINT ( 'NONE',  ( 3.256853613824191029, -1.637998819981079990, 1.410756932016984377 ) ) ;
#148005=CARTESIAN_POINT ( 'NONE',  ( 3.016969003575611818, -1.773741936391802332, 0.4936923545346691977 ) ) ;
#148008=CARTESIAN_POINT ( 'NONE',  ( 4.154071219024037198, -1.287471232310585467, 1.171156097612672253 ) ) ;
#148012=CARTESIAN_POINT ( 'NONE',  ( 1.428841412761387986, 2.083414371474631377, 0.5762002773818803991 ) ) ;
#148013=CARTESIAN_POINT ( 'NONE',  ( 4.657577273293715514, -0.4389639308803178208, -1.967586094827819654 ) ) ;
#148015=CARTESIAN_POINT ( 'NONE',  ( 1.288190726105652217, -0.9714702286227733241, 1.931199087792371261 ) ) ;
#148016=CARTESIAN_POINT ( 'NONE',  ( 2.301971997355524824, -1.971002988154029412, 0.04462483508816358219 ) ) ;
#148018=CARTESIAN_POINT ( 'NONE',  ( 3.421366544187495418, -1.159031000169882475, -1.558129983894075865 ) ) ;
#148027=CARTESIAN_POINT ( 'NONE',  ( 1.343116161061377545, 0.4315099961175078436, 2.164003993775004187 ) ) ;
#148029=CARTESIAN_POINT ( 'NONE',  ( 5.541838416980684023, 1.314774629379747539, 1.456173869884537675 ) ) ;
#148030=CARTESIAN_POINT ( 'NONE',  ( 3.802059961758995854, -1.092030603714509551, -1.813900157284773496 ) ) ;
#148032=CARTESIAN_POINT ( 'NONE',  ( 0.1747926744264451659, 0.2546335194838904581, -1.890750172325323275 ) ) ;
#148033=CARTESIAN_POINT ( 'NONE',  ( 4.681507052731401330, -0.8653998779965512700, 1.625073734443114759 ) ) ;
#148039=CARTESIAN_POINT ( 'NONE',  ( 5.590118541908202232, 1.264772504208915072, 1.701965355810124203 ) ) ;
#148042=CARTESIAN_POINT ( 'NONE',  ( 6.538362368396775537, 2.037695317216736246, 0.3068575337649599444 ) ) ;
#148044=CARTESIAN_POINT ( 'NONE',  ( 0.8185401059354965314, -1.351722143400556631, 1.279475349031534259 ) ) ;
#148045=CARTESIAN_POINT ( 'NONE',  ( 3.122423488780329492, 0.04808623196613136253, 1.840796284283818585 ) ) ;
#148052=CARTESIAN_POINT ( 'NONE',  ( 2.983271218942393332, -0.1628219013674602478, -2.200934326520533446 ) ) ;
#148053=CARTESIAN_POINT ( 'NONE',  ( 4.464347054923422320, 1.061364745222750372, 1.997979292561928633 ) ) ;
#148055=CARTESIAN_POINT ( 'NONE',  ( 4.218897050542698146, 1.396175630728054173, -1.154312599804697914 ) ) ;
#148056=CARTESIAN_POINT ( 'NONE',  ( 5.471877088563796399, -0.8550440501978623375, 1.714365851762880144 ) ) ;
#148058=CARTESIAN_POINT ( 'NONE',  ( 5.717618200960680852, -1.824738551054584379, 0.4112096411929695439 ) ) ;
#148059=CARTESIAN_POINT ( 'NONE',  ( 5.582414374887135544, 1.108435676577405937, -1.494769603722338802 ) ) ;
#148061=CARTESIAN_POINT ( 'NONE',  ( 0.1099206271272800961, -0.7955684105149689600, -1.691499381818922343 ) ) ;
#148064=CARTESIAN_POINT ( 'NONE',  ( 1.446500318503377125, -1.422605717829699801, 1.429450658469958668 ) ) ;
#148066=CARTESIAN_POINT ( 'NONE',  ( 3.229229631591294503, 0.05193219833012594627, 2.105601595880735033 ) ) ;
#148071=CARTESIAN_POINT ( 'NONE',  ( 1.635027243301078848, 1.886126948880119780, 0.7230602950082564151 ) ) ;
#148074=CARTESIAN_POINT ( 'NONE',  ( 2.882270108570818223, -1.113908571083363164, 1.852364028112465810 ) ) ;
#148075=CARTESIAN_POINT ( 'NONE',  ( 6.610000000000006537, 7.629137130509094256, 2.600000000000001421 ) ) ;
#148083=CARTESIAN_POINT ( 'NONE',  ( 1.118978350340808614, -0.04878210919301298465, 2.191179638975069732 ) ) ;
#148085=CARTESIAN_POINT ( 'NONE',  ( 0.9192595896337816264, 2.091463038127399532, 0.8634530567685079205 ) ) ;
#148093=CARTESIAN_POINT ( 'NONE',  ( 3.057584390254026729, 1.761565543986362670, -0.1695560061622681525 ) ) ;
#148096=CARTESIAN_POINT ( 'NONE',  ( 6.581111309608331794, -0.1016299978719436697, -2.204559905201553427 ) ) ;
#148100=CARTESIAN_POINT ( 'NONE',  ( 5.431267612114304200, -1.591330327768199382, -1.238307421737715019 ) ) ;
#148104=CARTESIAN_POINT ( 'NONE',  ( 2.360033908006432757, 0.7977434165707707470, 1.692156362554583460 ) ) ;
#148105=CARTESIAN_POINT ( 'NONE',  ( 3.537997267176114846, 1.309675639058418550, 1.603382541711120490 ) ) ;
#148107=CARTESIAN_POINT ( 'NONE',  ( 1.546972149855216472, 0.1906517044060058730, 1.902890584052991940 ) ) ;
#148110=DIRECTION ( 'NONE',  ( 1.214306433183764966E-17, 1.000000000000000000, 5.200010849845536803E-32 ) ) ;
#148112=CARTESIAN_POINT ( 'NONE',  ( 0.8614045922798493349, -1.509235727096858826, -1.174430983434851195 ) ) ;
#148113=CARTESIAN_POINT ( 'NONE',  ( 3.156644782993088150, -0.5669402238272451822, -1.878178299617596192 ) ) ;
#148114=CARTESIAN_POINT ( 'NONE',  ( 0.3157796101352361440, -1.620936768121715499, 1.198674607299075934 ) ) ;
#148120=CARTESIAN_POINT ( 'NONE',  ( 6.643826690903999577, 0.7566192825128185140, -1.820567107441137589 ) ) ;
#148122=CARTESIAN_POINT ( 'NONE',  ( 1.547136693356679249, 0.2016598947911317496, 2.003107868921078616 ) ) ;
#148125=CARTESIAN_POINT ( 'NONE',  ( 2.302504360600155842, 1.380385731239835323, -1.605472654339132887 ) ) ;
#148127=CARTESIAN_POINT ( 'NONE',  ( 4.035645461687249913, 1.950487776689105557, -0.6946759356915442885 ) ) ;
#148129=CARTESIAN_POINT ( 'NONE',  ( 6.175741434174033984, -1.119382356216396479, 1.765513623829425116 ) ) ;
#148131=CARTESIAN_POINT ( 'NONE',  ( 4.383705365265609721, 1.192707349210776036, 1.382196219385352309 ) ) ;
#148136=CARTESIAN_POINT ( 'NONE',  ( 5.034293675167555548, 1.138177661764948834, -1.890478833441497031 ) ) ;
#148139=CARTESIAN_POINT ( 'NONE',  ( 3.492734469894549942, -1.843672829398453228, -0.5074192597756199685 ) ) ;
#148146=CARTESIAN_POINT ( 'NONE',  ( 0.5558949066124979632, -1.334021266253348381, 1.269314063962426076 ) ) ;
#148150=CARTESIAN_POINT ( 'NONE',  ( 4.604681543780857034, 1.447206075137374759, -1.185162884121161442 ) ) ;
#148155=CARTESIAN_POINT ( 'NONE',  ( 1.358185265713553136, -1.969629313231166856, -0.005369267927731942967 ) ) ;
#148156=CARTESIAN_POINT ( 'NONE',  ( 2.759388848745081280, 1.913798524274639812, -0.6352183541234107667 ) ) ;
#148160=CARTESIAN_POINT ( 'NONE',  ( 2.238457302780196390, 0.4817095239468481283, 2.137691825660259948 ) ) ;
#148167=EDGE_CURVE ( 'NONE', #63091, #78277, #188587, .T. ) ;
#148171=CARTESIAN_POINT ( 'NONE',  ( 5.091278345985558396, -0.6575378499774006125, 1.720029930423284448 ) ) ;
#148172=CARTESIAN_POINT ( 'NONE',  ( 1.524088986950965730, -1.997618534301074833, 0.2487294023021668354 ) ) ;
#148173=CARTESIAN_POINT ( 'NONE',  ( 3.392261881094984055, 0.05328783134446976599, 2.297904267588930960 ) ) ;
#148174=CARTESIAN_POINT ( 'NONE',  ( -0.1290005225502675879, 5.719648796287211567, -2.768066027128403217 ) ) ;
#148175=CARTESIAN_POINT ( 'NONE',  ( 1.305250306655120207, -1.462593314309963866, -1.150481100809984891 ) ) ;
#148178=CARTESIAN_POINT ( 'NONE',  ( 5.625241921295836889, 1.689600096388569561, 0.8957793909229803120 ) ) ;
#148181=CARTESIAN_POINT ( 'NONE',  ( 3.702747019872438372, 1.794327276830971707, 1.072858563533698018 ) ) ;
#148182=CARTESIAN_POINT ( 'NONE',  ( 1.885419139999934934, 1.287927767047767125, 1.356919574424742203 ) ) ;
#148185=CARTESIAN_POINT ( 'NONE',  ( 6.146043377905669125, 0.5841948715668408010, 1.746183665442810007 ) ) ;
#148188=CARTESIAN_POINT ( 'NONE',  ( 4.969259055160575755, 0.1640942704066571667, -1.717058449848630985 ) ) ;
#148190=CARTESIAN_POINT ( 'NONE',  ( 0.4219819185556292207, -1.224561070735529444, -1.228170329033271724 ) ) ;
#148195=CARTESIAN_POINT ( 'NONE',  ( 4.434556658511819016, -1.254960995779637045, 1.771429847731820661 ) ) ;
#148196=CARTESIAN_POINT ( 'NONE',  ( 3.457459740917231628, 0.4424662778084071935, -1.771134634090239190 ) ) ;
#148197=CARTESIAN_POINT ( 'NONE',  ( 1.393326438508041942, -1.775833184744341375, 0.8338576968042878956 ) ) ;
#148198=CARTESIAN_POINT ( 'NONE',  ( 5.735599800244862045, 0.6120854273203913953, -2.026975329707622731 ) ) ;
#148199=CARTESIAN_POINT ( 'NONE',  ( 5.443040390997877509, -1.805468894110316080, -1.412473186189531438 ) ) ;
#148203=CARTESIAN_POINT ( 'NONE',  ( 1.366058183223411771, 0.6122477967837879342, -2.030190212274018524 ) ) ;
#148207=CARTESIAN_POINT ( 'NONE',  ( 5.981339239477990510, -0.06126731230964890806, 2.170386710549534470 ) ) ;
#148208=CARTESIAN_POINT ( 'NONE',  ( 6.983263157960386991, 3.689421308571324776, 2.567857239638075217 ) ) ;
#148210=CARTESIAN_POINT ( 'NONE',  ( 2.016565898353571473, -2.220703888365501921, 0.05821906423880519182 ) ) ;
#148212=CARTESIAN_POINT ( 'NONE',  ( 6.610000000000006537, 0.002781820520842553934, 2.000159646111852929 ) ) ;
#148214=CARTESIAN_POINT ( 'NONE',  ( 5.436407774000851845, -1.150348206634976833, 1.711801118168945202 ) ) ;
#148220=CARTESIAN_POINT ( 'NONE',  ( 0.1331565106231329398, 0.7299000548664087429, -2.029785554894456556 ) ) ;
#148221=CARTESIAN_POINT ( 'NONE',  ( 4.686955257832659427, 1.367739038236553517, 1.232883728221023212 ) ) ;
#148223=CARTESIAN_POINT ( 'NONE',  ( 1.430204257492089903, 1.660765249891223316, 0.4652242431656942179 ) ) ;
#148225=CARTESIAN_POINT ( 'NONE',  ( 2.040019973291283151, -1.774186676285171460, 1.461575674325124252 ) ) ;
#148227=CARTESIAN_POINT ( 'NONE',  ( 1.599281762659544137, 1.849886183345637258, -1.302228464298058830 ) ) ;
#148228=CARTESIAN_POINT ( 'NONE',  ( 4.002637171539184635, -0.6605693356034693098, -1.999858192447926397 ) ) ;
#148230=CARTESIAN_POINT ( 'NONE',  ( 1.985279565377489508, 1.216254750358658487, 1.285827030011628347 ) ) ;
#148236=CARTESIAN_POINT ( 'NONE',  ( 5.625276811391259457, 1.958927336128764241, 1.047432077188856780 ) ) ;
#148237=CARTESIAN_POINT ( 'NONE',  ( 3.697391623616069101, -0.6365095100077067247, 2.096977347260075231 ) ) ;
#148242=CARTESIAN_POINT ( 'NONE',  ( 6.610000000000010090, 0.5825982378308904863, 2.053072689460200273 ) ) ;
#148244=CARTESIAN_POINT ( 'NONE',  ( 5.537388447972660721, -0.05000006065614125139, 2.120159173171487055 ) ) ;
#148249=CARTESIAN_POINT ( 'NONE',  ( 6.040549724581927293, -1.551790349881351450, 0.9907606852931831742 ) ) ;
#148254=CARTESIAN_POINT ( 'NONE',  ( 1.540153114873343609, -1.470452955542918660, 0.9307524122482965234 ) ) ;
#148260=CARTESIAN_POINT ( 'NONE',  ( 5.137646372127643524, -1.526005641499485810, -1.531359247741073570 ) ) ;
#148264=CARTESIAN_POINT ( 'NONE',  ( 4.346650381253648554, 0.5737703434565506466, 2.084106190491950006 ) ) ;
#148268=CARTESIAN_POINT ( 'NONE',  ( 6.063742386902314152, 1.942598920255795392, -0.3345802184639041776 ) ) ;
#148269=CARTESIAN_POINT ( 'NONE',  ( 4.692597494581693063, -1.067344209891357032, -1.366281018423552762 ) ) ;
#148271=CARTESIAN_POINT ( 'NONE',  ( 2.243918346939121733, 2.191141468336772036, 0.05030144379260945153 ) ) ;
#148272=CARTESIAN_POINT ( 'NONE',  ( 3.680997481958053541, -2.223193225534472628, -0.6181044232122161475 ) ) ;
#148273=CARTESIAN_POINT ( 'NONE',  ( 4.903620131156614548, -0.5536938069644473659, 1.984910608926907960 ) ) ;
#148274=CARTESIAN_POINT ( 'NONE',  ( 0.07597880344310371792, -1.883441279811811642, -0.4727451468593062422 ) ) ;
#148278=CARTESIAN_POINT ( 'NONE',  ( 3.621431001533811589, 1.820626359085864454, 1.087046460333654485 ) ) ;
#148280=CARTESIAN_POINT ( 'NONE',  ( 1.477185633673218534, -2.006960102380969779, -0.1948397147320118372 ) ) ;
#148282=CARTESIAN_POINT ( 'NONE',  ( 4.840968367003476658, 0.3731960759543617723, 2.174832070070693568 ) ) ;
#148283=DIRECTION ( 'NONE',  ( -1.000000000000000000, 1.016547956922408957E-15, 1.479114432388267300E-31 ) ) ;
#148291=CARTESIAN_POINT ( 'NONE',  ( 3.977457805978751093, 1.941116309567689324, -0.6927405623450531014 ) ) ;
#148294=CARTESIAN_POINT ( 'NONE',  ( 3.492836188673923647, -1.947007740449010926, -0.5366636104956448161 ) ) ;
#148299=CARTESIAN_POINT ( 'NONE',  ( 2.957942382388091040, 2.051108442962752409, -0.2004023863233852509 ) ) ;
#148302=CARTESIAN_POINT ( 'NONE',  ( -0.1409997244346122836, 0.7174646053854060179, -2.082770303449644977 ) ) ;
#148303=CARTESIAN_POINT ( 'NONE',  ( 1.833694255977034615, 1.820935426717207317, 0.2711280389895084353 ) ) ;
#148304=CARTESIAN_POINT ( 'NONE',  ( 0.2238089703245670359, -0.1066217210726662923, 2.305362286893299917 ) ) ;
#148306=CARTESIAN_POINT ( 'NONE',  ( 1.476082264964494906, 1.286352913914396545, 1.737049067733025032 ) ) ;
#148309=CARTESIAN_POINT ( 'NONE',  ( 1.903530124611974017, -1.954778955200174861, 0.4946342604733033887 ) ) ;
#148311=CARTESIAN_POINT ( 'NONE',  ( 0.3033014811697418711, -0.5033704626738467747, 1.801585485020948951 ) ) ;
#148312=CARTESIAN_POINT ( 'NONE',  ( 5.067239680553584869, 0.1942248685237786265, -1.961885565008324006 ) ) ;
#148313=CARTESIAN_POINT ( 'NONE',  ( 4.171111447311355747, 1.799123655847803205, -0.9110083886025857058 ) ) ;
#148317=CARTESIAN_POINT ( 'NONE',  ( 5.901026713257129686, 1.722607154707327615, -1.211383145191318400 ) ) ;
#148318=CARTESIAN_POINT ( 'NONE',  ( 5.160626937512653001, -0.6942339714755951796, -1.950645400549338104 ) ) ;
#148321=CARTESIAN_POINT ( 'NONE',  ( 6.539320575229230492, 2.428701779328062749, 2.485127258459709054 ) ) ;
#148322=CARTESIAN_POINT ( 'NONE',  ( 5.730724961554885866, 1.353511160402442570, -1.499384403026276180 ) ) ;
#148324=CARTESIAN_POINT ( 'NONE',  ( 3.932480676516422413, 1.235928489987428325, -1.948660470369364628 ) ) ;
#148325=CARTESIAN_POINT ( 'NONE',  ( 1.393505825229651052, -1.866293207157668776, 0.8783701326641482066 ) ) ;
#148332=CARTESIAN_POINT ( 'NONE',  ( 4.686072593652621521, -1.332121122860012052, -1.714431229949509250 ) ) ;
#148336=CARTESIAN_POINT ( 'NONE',  ( 3.087279721815265443, -0.7436087841871074078, 1.684586988852328160 ) ) ;
#148338=CARTESIAN_POINT ( 'NONE',  ( 4.300438532332786501, 1.693616701070689956, -1.390861761948622766 ) ) ;
#148340=CARTESIAN_POINT ( 'NONE',  ( 5.788003261412111300, -1.023269635773180752, 2.017978558835635372 ) ) ;
#148345=CARTESIAN_POINT ( 'NONE',  ( 6.292257686217937795, -1.761477974832075244, -0.1709902323579186867 ) ) ;
#148347=CARTESIAN_POINT ( 'NONE',  ( 3.844392992367959838, 1.075074360472785928, -1.701806764060603161 ) ) ;
#148349=CARTESIAN_POINT ( 'NONE',  ( 3.258910125681306891, -1.595695288142566337, 1.374458643164514937 ) ) ;
#148350=CARTESIAN_POINT ( 'NONE',  ( 1.634256478289298320, 0.6027960111968011514, 1.818337931642779903 ) ) ;
#148353=CARTESIAN_POINT ( 'NONE',  ( 3.314863512866594863, -1.493043793209645864, 1.284631214971102775 ) ) ;
#148354=CARTESIAN_POINT ( 'NONE',  ( 4.799084794409138155, -0.2512425647771680537, -2.004053532012660455 ) ) ;
#148355=CARTESIAN_POINT ( 'NONE',  ( 0.7603692911175019553, -1.357789551990191246, 1.287012767582619510 ) ) ;
#148356=CARTESIAN_POINT ( 'NONE',  ( 0.5901948623465642640, 1.011764341257429978, -1.680720577067334354 ) ) ;
#148357=CARTESIAN_POINT ( 'NONE',  ( 0.2110004604562870645, 1.588762659912812403, -1.064147093309028680 ) ) ;
#148362=CARTESIAN_POINT ( 'NONE',  ( 6.280143113937574739, -0.9989825818290422044, 1.581392243879369053 ) ) ;
#148365=CARTESIAN_POINT ( 'NONE',  ( 6.491088764554701740, 0.1969099459505334604, 2.060843999385448821 ) ) ;
#148367=CARTESIAN_POINT ( 'NONE',  ( 0.5024991115675537801, 2.064720838319131779, 0.1538615064654233477 ) ) ;
#148372=CARTESIAN_POINT ( 'NONE',  ( 5.057343377742961721, -1.818460011135439869, 1.090507627184752693 ) ) ;
#148375=CARTESIAN_POINT ( 'NONE',  ( 5.969191311310417802, 1.729517061547349632, 0.9261464158661563140 ) ) ;
#148377=CARTESIAN_POINT ( 'NONE',  ( 4.306017418194902469, -1.755500069608874281, 0.9912479507018998603 ) ) ;
#148378=CARTESIAN_POINT ( 'NONE',  ( 3.169047557264609072, 1.729775434385946831, -0.8236773211035466336 ) ) ;
#148381=CARTESIAN_POINT ( 'NONE',  ( 1.206853476500208133, 1.935082376036290075, 1.028754739392373496 ) ) ;
#148383=CARTESIAN_POINT ( 'NONE',  ( 3.637841704585748293, 0.8437669887123750989, -1.669527271503386201 ) ) ;
#148385=CARTESIAN_POINT ( 'NONE',  ( 4.711194051470749322, 1.671412949727559383, -1.121937078508246755 ) ) ;
#148388=CARTESIAN_POINT ( 'NONE',  ( 5.607064690329227830, -0.05131010805739347896, 2.116756054987908531 ) ) ;
#148390=CARTESIAN_POINT ( 'NONE',  ( 6.707487347292075519, -1.660346423639452951, -1.236579608897829363 ) ) ;
#148391=CARTESIAN_POINT ( 'NONE',  ( 2.226223261843117918, 2.028672367434441792, 0.5052007718874002018 ) ) ;
#148392=FACE_OUTER_BOUND ( 'NONE', #138695, .T. ) ;
#148393=CARTESIAN_POINT ( 'NONE',  ( 0.7622199101927947806, -1.253934870956091352, 1.184532473512718509 ) ) ;
#148404=CARTESIAN_POINT ( 'NONE',  ( 2.139049582973771457, 0.0009909630806471080022, 1.811656970554485602 ) ) ;
#148409=CARTESIAN_POINT ( 'NONE',  ( 6.539320575229245591, 2.459069921018588900, 2.280790101157427419 ) ) ;
#148414=CARTESIAN_POINT ( 'NONE',  ( 3.068646357036347361, 1.349867735329785434, -1.281425607799644206 ) ) ;
#148415=CARTESIAN_POINT ( 'NONE',  ( 0.5619445578959707532, -1.063298924184744587, 1.593181094007071863 ) ) ;
#148416=CARTESIAN_POINT ( 'NONE',  ( 6.194356126197313017, -1.917168722191398000, -0.1884046653951119699 ) ) ;
#148422=CARTESIAN_POINT ( 'NONE',  ( 4.117982337901913148, 1.955079553045156127, -0.2365992483164043592 ) ) ;
#148423=CARTESIAN_POINT ( 'NONE',  ( 1.524255003590764046, -2.104078925693805502, 0.2628582283784736684 ) ) ;
#148427=CARTESIAN_POINT ( 'NONE',  ( 5.367185978643659539, 2.112682091867735146, -0.5819856738719306755 ) ) ;
#148429=CARTESIAN_POINT ( 'NONE',  ( 4.120081753510516975, -0.9896868749219210892, -1.652585292789155558 ) ) ;
#148431=CARTESIAN_POINT ( 'NONE',  ( 0.5865807246496178573, -0.2182756592755269454, -1.812417144444453232 ) ) ;
#148432=CARTESIAN_POINT ( 'NONE',  ( 1.155211076828046801, -1.737760091701185283, 1.360235214042208263 ) ) ;
#148436=CARTESIAN_POINT ( 'NONE',  ( 6.596547011414190642, 1.947522214285227760, 0.2922974700911728507 ) ) ;
#148437=CARTESIAN_POINT ( 'NONE',  ( 1.681094245561355560, 1.340559147886428271, 1.405378567840375403 ) ) ;
#148438=CARTESIAN_POINT ( 'NONE',  ( 6.222043071159490957, -1.966323047081437014, -1.189884408624383383 ) ) ;
#148440=CARTESIAN_POINT ( 'NONE',  ( 4.469486699700035537, -0.3212591861478170663, 1.832842066241076040 ) ) ;
#148445=CARTESIAN_POINT ( 'NONE',  ( 0.3983070667218471805, -0.7439898890007863308, -2.061537379893277677 ) ) ;
#148450=CARTESIAN_POINT ( 'NONE',  ( 1.910518402784128433, 1.353611321597010253, -1.225282022559864625 ) ) ;
#148452=CARTESIAN_POINT ( 'NONE',  ( 3.621445620172254021, 0.2585195360361118300, 1.714627356041095840 ) ) ;
#148454=CARTESIAN_POINT ( 'NONE',  ( 6.609000000000036401, 7.629137130509092479, 2.600000000000000977 ) ) ;
#148455=CARTESIAN_POINT ( 'NONE',  ( 0.1331565106231363538, 2.033293680964400885, -2.362282156872722805 ) ) ;
#148456=CARTESIAN_POINT ( 'NONE',  ( 6.217409598193539999, -0.2183660865492654257, 1.812524795094340835 ) ) ;
#148457=CARTESIAN_POINT ( 'NONE',  ( 4.821123798404616245, -1.750560105953799184, -0.8856655065374098301 ) ) ;
#148462=CARTESIAN_POINT ( 'NONE',  ( 5.215537505735290402, 1.733765862324820439, 1.220609238144418240 ) ) ;
#148465=CARTESIAN_POINT ( 'NONE',  ( 3.256751887857904926, -0.5965066610371800859, -1.982489643792232137 ) ) ;
#148470=CARTESIAN_POINT ( 'NONE',  ( 2.918861131495727790, -1.545587104802835565, -1.701642145805809303 ) ) ;
#148474=CARTESIAN_POINT ( 'NONE',  ( 6.720655732516666703, 0.5845450044974825898, 1.978693153076715783 ) ) ;
#148478=CARTESIAN_POINT ( 'NONE',  ( 4.078302138561982204, 0.9061299177482335931, 1.684124486321957104 ) ) ;
#148479=CARTESIAN_POINT ( 'NONE',  ( 4.946200454639571475, 1.720373684868029329, 0.1241775145462056112 ) ) ;
#148480=CARTESIAN_POINT ( 'NONE',  ( 3.766814776335784209, -0.2024620155892907503, -2.006371719556559796 ) ) ;
#148481=CARTESIAN_POINT ( 'NONE',  ( 5.414730038718025718, -1.455890720088355961, -1.778839290973016629 ) ) ;
#148483=CARTESIAN_POINT ( 'NONE',  ( 0.2236267563471248943, -0.1037379595543522215, 2.204571545119632603 ) ) ;
#148485=CARTESIAN_POINT ( 'NONE',  ( 5.501144674179510474, 1.447219185280288700, 1.018257267444661496 ) ) ;
#148486=EDGE_CURVE ( 'NONE', #76973, #53173, #79153, .T. ) ;
#148488=CARTESIAN_POINT ( 'NONE',  ( 2.027642443044708198, -1.499220162234589093, -1.734095823995058794 ) ) ;
#148489=CARTESIAN_POINT ( 'NONE',  ( 6.246043375366982175, 0.5822610321466625827, 1.746719530172704538 ) ) ;
#148494=CARTESIAN_POINT ( 'NONE',  ( 6.602015318333181781, 0.7961593463888805289, -1.911361562896146671 ) ) ;
#148495=CARTESIAN_POINT ( 'NONE',  ( 2.149625371984189126, 1.976669504256656218, -0.3981124878784659815 ) ) ;
#148497=CARTESIAN_POINT ( 'NONE',  ( 5.672470344399177300, -1.220246509433765558, 1.490775554449337070 ) ) ;
#148499=CARTESIAN_POINT ( 'NONE',  ( 1.934110000270176322, -2.153362505827714823, 0.5451143137677332273 ) ) ;
#148506=CARTESIAN_POINT ( 'NONE',  ( 5.882304624916216973, -0.2641129477329319242, -1.720170474299307806 ) ) ;
#148507=CARTESIAN_POINT ( 'NONE',  ( 3.297265573180406584, -1.731424309613574852, 0.9225008839797432802 ) ) ;
#148511=CARTESIAN_POINT ( 'NONE',  ( 4.446707141204663039, 0.5976617499744775186, 2.181999625662895959 ) ) ;
#148512=CARTESIAN_POINT ( 'NONE',  ( 0.6958484739430546018, -1.457389369856504358, -1.459923026165359516 ) ) ;
#148516=CARTESIAN_POINT ( 'NONE',  ( 2.887862062735581326, 1.599188571496454658, 1.600737006856695288 ) ) ;
#148519=CARTESIAN_POINT ( 'NONE',  ( 2.143623209005097507, 0.7202431893391960660, -1.726524797105493336 ) ) ;
#148520=CARTESIAN_POINT ( 'NONE',  ( 1.916292283401900720, -1.133531090463487212, -1.312443884513394554 ) ) ;
#148521=CARTESIAN_POINT ( 'NONE',  ( 5.653911837654605144, 0.8871495062587383407, 2.004161502255866090 ) ) ;
#148522=CARTESIAN_POINT ( 'NONE',  ( 0.4466624375424713689, 2.201045718399210038, 0.1599725512250807224 ) ) ;
#148523=CARTESIAN_POINT ( 'NONE',  ( 1.639600518753115521, -1.491979387419887892, -1.421952917470001632 ) ) ;
#148524=CARTESIAN_POINT ( 'NONE',  ( 4.031144971506396502, -1.339966268285474715, -1.405800288483616045 ) ) ;
#148527=CARTESIAN_POINT ( 'NONE',  ( 1.687500000000001110, -1.451031289061048835, 1.451031289061190055 ) ) ;
#148529=CARTESIAN_POINT ( 'NONE',  ( 6.643907658006512840, -0.09612306880287316280, -2.013924184692199137 ) ) ;
#148531=CARTESIAN_POINT ( 'NONE',  ( 5.045546153961558922, -1.458558117013383892, 1.392544180963309230 ) ) ;
#148535=CARTESIAN_POINT ( 'NONE',  ( 2.332394550857110893, 1.770734860448031300, 0.4440693575865002907 ) ) ;
#148544=CARTESIAN_POINT ( 'NONE',  ( -0.08762443420157886576, -2.019435065594810119, -0.04520711721162430641 ) ) ;
#148545=CARTESIAN_POINT ( 'NONE',  ( 0.2586463447097427926, 2.115114616003030079, 0.1516365082330217162 ) ) ;
#148550=CARTESIAN_POINT ( 'NONE',  ( 0.1105426557568081891, -0.9253945370547181914, -1.951590883024490353 ) ) ;
#148551=CARTESIAN_POINT ( 'NONE',  ( 4.553361389630797618, -1.314998166741451868, 1.528740011303417523 ) ) ;
#148560=CARTESIAN_POINT ( 'NONE',  ( 4.780624950969222020, -1.977747464269607347, 0.3905396900540994420 ) ) ;
#148561=CARTESIAN_POINT ( 'NONE',  ( 4.347483306186128438, 1.840691044367316120, -0.04759384897683878457 ) ) ;
#148563=CARTESIAN_POINT ( 'NONE',  ( 3.598509747979701690, -2.304983022191483766, -0.1141929325871558626 ) ) ;
#148565=CARTESIAN_POINT ( 'NONE',  ( 5.290363030411685763, -2.144575937485785566, -0.2703735795691122323 ) ) ;
#148566=CARTESIAN_POINT ( 'NONE',  ( 1.364679817366498904, 0.1413127912619481230, -1.936958241114185020 ) ) ;
#148571=CARTESIAN_POINT ( 'NONE',  ( 3.572993900519233712, 0.04689164532409998559, -1.870237235490713079 ) ) ;
#148572=CARTESIAN_POINT ( 'NONE',  ( 1.160255710619631397, 1.910328232974867868, 0.09094507755665059978 ) ) ;
#148575=CARTESIAN_POINT ( 'NONE',  ( 2.526237079854487089, -1.271617311931704686, -1.803507373242494438 ) ) ;
#148581=CARTESIAN_POINT ( 'NONE',  ( 0.3156150085598420363, -1.934196717871897953, 0.3801348212975861895 ) ) ;
#148582=CARTESIAN_POINT ( 'NONE',  ( 0.4116873800214932988, 2.009943462479982124, 1.133530718095694168 ) ) ;
#148583=CARTESIAN_POINT ( 'NONE',  ( 1.750371521623844462, -1.952110535733902585, -0.1955497077021361163 ) ) ;
#148584=CARTESIAN_POINT ( 'NONE',  ( 5.700070374860989553, 0.8410407859656986451, -1.883500665774339833 ) ) ;
#148591=CARTESIAN_POINT ( 'NONE',  ( 0.6202906599508707375, 2.147645164210740365, -0.3171128231679083975 ) ) ;
#148593=CARTESIAN_POINT ( 'NONE',  ( 6.286648950733226826, 1.598451336667701339, -0.9137711784916457969 ) ) ;
#148596=CARTESIAN_POINT ( 'NONE',  ( 1.211929638205839765, -0.8359089839212189288, -1.673436591668895357 ) ) ;
#148597=CARTESIAN_POINT ( 'NONE',  ( 5.395850447034295172, -0.7835752172833524432, 2.014745138864987073 ) ) ;
#148599=CARTESIAN_POINT ( 'NONE',  ( -0.02264175331117677936, 4.084751018978694859, -2.643765695431527174 ) ) ;
#148602=CARTESIAN_POINT ( 'NONE',  ( 1.646971982979036131, 0.1886418863925183043, 1.902964618272010799 ) ) ;
#148603=CARTESIAN_POINT ( 'NONE',  ( 3.080641367082480819, -0.1285219475026712632, -1.765225098288242256 ) ) ;
#148604=CARTESIAN_POINT ( 'NONE',  ( 0.7153071762652126742, 1.563590412251715911, 1.100639817434710954 ) ) ;
#148606=CARTESIAN_POINT ( 'NONE',  ( 5.413669558995096054, -1.219043080348445329, -1.477637860945772763 ) ) ;
#148607=CARTESIAN_POINT ( 'NONE',  ( 6.074653383054481104, 1.324031319358546677, -1.458257743282452834 ) ) ;
#148609=CARTESIAN_POINT ( 'NONE',  ( 0.7914572142167939361, -0.05789999323873443182, -2.119991495365561640 ) ) ;
#148611=CARTESIAN_POINT ( 'NONE',  ( 3.572993900519233712, 0.04689164532409998559, -1.870237235490713079 ) ) ;
#148612=CARTESIAN_POINT ( 'NONE',  ( 0.04711308451243316486, -1.408776630263553375, -1.161003007932148501 ) ) ;
#148614=CARTESIAN_POINT ( 'NONE',  ( 4.055453297694236348, -1.834216022232620702, -1.226887332174103173 ) ) ;
#148618=CARTESIAN_POINT ( 'NONE',  ( 1.996602216506689453, 2.039906831610329263, 0.3049752315822819027 ) ) ;
#148624=CARTESIAN_POINT ( 'NONE',  ( 6.533470333208203584, -0.1312131129157616261, 1.882018712217728318 ) ) ;
#148627=CARTESIAN_POINT ( 'NONE',  ( 3.930184216435282707, 1.147649575447948100, 1.722966636330313550 ) ) ;
#148629=CARTESIAN_POINT ( 'NONE',  ( 1.458524589769864210, 0.8745999688587955401, 1.976921506453344080 ) ) ;
#148631=CARTESIAN_POINT ( 'NONE',  ( 1.664719335976164283, 0.6358223015159381042, 1.917034779120100341 ) ) ;
#148636=CARTESIAN_POINT ( 'NONE',  ( 6.883263157960367806, 7.629137130509066722, 2.653810918356712900 ) ) ;
#148637=CARTESIAN_POINT ( 'NONE',  ( -0.2058462039469660110, -0.8663896114125648751, -1.819200108291472606 ) ) ;
#148638=CARTESIAN_POINT ( 'NONE',  ( 6.639320575229255894, 6.035237531390704291, 2.698156163645454964 ) ) ;
#148639=CARTESIAN_POINT ( 'NONE',  ( 4.757479570170550787, 2.167726397749652367, -0.3216086267831194112 ) ) ;
#148641=CARTESIAN_POINT ( 'NONE',  ( 3.867365959033176814, -1.592763314076732106, -1.058159689705892692 ) ) ;
#148645=CARTESIAN_POINT ( 'NONE',  ( 1.739861462675455828, 2.010826045486389102, -0.1511602461454417123 ) ) ;
#148647=CARTESIAN_POINT ( 'NONE',  ( 0.5742758271649881507, -1.267216683205124150, 1.910101658145799020 ) ) ;
#148649=CARTESIAN_POINT ( 'NONE',  ( 3.768305045387724928, -1.158492864085089114, 1.277938026295278418 ) ) ;
#148655=CARTESIAN_POINT ( 'NONE',  ( 0.07556134207193675179, -0.004209888911949499594, -2.244269416743961187 ) ) ;
#148659=CARTESIAN_POINT ( 'NONE',  ( 5.479120714502029976, -1.640381486070506156, -0.7687909062009666838 ) ) ;
#148664=CARTESIAN_POINT ( 'NONE',  ( 5.531847899045232886, -1.765878665049234186, 0.4030928165594855339 ) ) ;
#148668=CARTESIAN_POINT ( 'NONE',  ( 6.426204213344836269, 0.9576725794440078543, 1.595564698446788388 ) ) ;
#148670=CARTESIAN_POINT ( 'NONE',  ( 3.620622283765279725, 0.2843237153829519248, 1.894267977526209012 ) ) ;
#148677=CARTESIAN_POINT ( 'NONE',  ( 5.911343334927605220, -1.992878553188395463, 0.7155076844978009998 ) ) ;
#148678=CARTESIAN_POINT ( 'NONE',  ( 0.3390366800232989530, 0.3710982241871863541, 2.129449491308422537 ) ) ;
#148681=CARTESIAN_POINT ( 'NONE',  ( 0.9030137451815029026, 1.489685209907613439, 1.054989265776705709 ) ) ;
#148683=CARTESIAN_POINT ( 'NONE',  ( 3.627796970749700201, -1.086779551322129445, -1.466705181690882709 ) ) ;
#148686=CARTESIAN_POINT ( 'NONE',  ( 2.435944266227826116, 1.209484882827957630, 1.554366883019624668 ) ) ;
#148687=CARTESIAN_POINT ( 'NONE',  ( 5.196799823744689739, 1.589972550305688070, 1.114921412299192172 ) ) ;
#148690=CARTESIAN_POINT ( 'NONE',  ( 4.992489932941452935, -1.175987964647656536, 1.764448611491518548 ) ) ;
#148692=CARTESIAN_POINT ( 'NONE',  ( 2.525908831824146716, -1.891188341833284881, 0.2824699455093656053 ) ) ;
#148697=CARTESIAN_POINT ( 'NONE',  ( 3.756497301808682465, 2.003587623774540472, 0.1952383342433745284 ) ) ;
#148699=CARTESIAN_POINT ( 'NONE',  ( 4.635264976507449397, -1.668059998867366778, 0.7425182445051290436 ) ) ;
#148700=CARTESIAN_POINT ( 'NONE',  ( 0.3794556558127279433, -0.1030994254981998093, 2.067933115924729837 ) ) ;
#148704=CARTESIAN_POINT ( 'NONE',  ( 5.664887262500884368, -1.691755685069219695, -0.7986314380193232365 ) ) ;
#148714=CARTESIAN_POINT ( 'NONE',  ( 6.789883322502159757, -1.411316560962400768, -1.649898940422918514 ) ) ;
#148715=CARTESIAN_POINT ( 'NONE',  ( 2.443091204979094044, -1.843612287508783920, -1.040880819149572201 ) ) ;
#148718=CARTESIAN_POINT ( 'NONE',  ( 6.034052368894809781, 1.228512962337786396, 1.666229478724051027 ) ) ;
#148722=DIRECTION ( 'NONE',  ( 2.949029909160572061E-17, 1.000000000000000000, -8.673600428462541149E-15 ) ) ;
#148723=CARTESIAN_POINT ( 'NONE',  ( 2.185838763446645849, -0.9780977115210144346, 2.073240998862643458 ) ) ;
#148726=CARTESIAN_POINT ( 'NONE',  ( 2.619282413590624525, 1.617716081779559278, 1.019604094833974628 ) ) ;
#148730=CARTESIAN_POINT ( 'NONE',  ( 0.1936082253880376802, 1.876963271429439750, -0.7284200309826213138 ) ) ;
#148731=CARTESIAN_POINT ( 'NONE',  ( 1.076917802502619592, 1.810449747239597951, 0.7559744942375111743 ) ) ;
#148732=CARTESIAN_POINT ( 'NONE',  ( 0.2333690889706682703, 0.003390530909083006028, -2.053566628440507635 ) ) ;
#148735=CARTESIAN_POINT ( 'NONE',  ( 3.925792317461401559, 1.118293097838483074, -1.766204078809136657 ) ) ;
#148736=CARTESIAN_POINT ( 'NONE',  ( 2.588433964080754546, -0.3000524435079615637, -1.744042203426913629 ) ) ;
#148739=CARTESIAN_POINT ( 'NONE',  ( 5.543040349607136541, -1.804139640619137230, -1.413977440569001542 ) ) ;
#148740=CARTESIAN_POINT ( 'NONE',  ( 3.960698422707895627, 0.2102999545306425688, -1.727497421908174458 ) ) ;
#148743=CARTESIAN_POINT ( 'NONE',  ( 3.075252150474018009, 1.257817891742564642, -1.193625562640305615 ) ) ;
#148744=CARTESIAN_POINT ( 'NONE',  ( 4.861888260954045471, -0.5834894554452072502, 2.091229948656031734 ) ) ;
#148746=CARTESIAN_POINT ( 'NONE',  ( 5.770720322323381168, -0.3006437417610394736, -1.993894057904864514 ) ) ;
#148747=CARTESIAN_POINT ( 'NONE',  ( 6.562500042754934704, -1.451030237095789266, -1.451031289060847440 ) ) ;
#148749=CARTESIAN_POINT ( 'NONE',  ( 2.327063250521405724, -0.002089543651138252821, 1.926566264030280307 ) ) ;
#148751=CARTESIAN_POINT ( 'NONE',  ( 5.396815004230996138, -2.167347303010109805, -0.4865036897706440100 ) ) ;
#148753=CARTESIAN_POINT ( 'NONE',  ( 6.983263157960335477, 4.692686028926381425, 2.608776679625654182 ) ) ;
#148757=MECHANICAL_DESIGN_GEOMETRIC_PRESENTATION_REPRESENTATION('',(#83029),#141993);
#148758=CARTESIAN_POINT ( 'NONE',  ( 6.795372052238223048, -1.752927774724974297, 0.8811163259476796350 ) ) ;
#148762=CARTESIAN_POINT ( 'NONE',  ( 0.1412502902482688505, 0.7743183493036235321, 1.862015731718666078 ) ) ;
#148763=CARTESIAN_POINT ( 'NONE',  ( 4.369619704168957952, -0.3557292467365941180, 2.031631830423554774 ) ) ;
#148767=CARTESIAN_POINT ( 'NONE',  ( 5.518772846390051612, 1.727975122137341613, 0.7167417953098526029 ) ) ;
#148768=CARTESIAN_POINT ( 'NONE',  ( 5.273917847569165929, 1.525789468548454986, -0.8241785451228255122 ) ) ;
#148769=CARTESIAN_POINT ( 'NONE',  ( 5.003314770209169815, -1.731378854590956307, 0.1774945436790342501 ) ) ;
#148771=CARTESIAN_POINT ( 'NONE',  ( 1.804612524702827514, 1.695363242818634930, -1.543121881923440020 ) ) ;
#148773=CARTESIAN_POINT ( 'NONE',  ( 5.284749326355624888, 1.843379893440146633, -0.9865243283948360586 ) ) ;
#148774=CARTESIAN_POINT ( 'NONE',  ( 0.6558947131179297951, -1.335331635844772880, 1.267786537210900510 ) ) ;
#148776=CARTESIAN_POINT ( 'NONE',  ( 1.600232647554021392, -0.2440283035436350279, 2.001511509883910911 ) ) ;
#148782=CARTESIAN_POINT ( 'NONE',  ( 3.299587915756982515, 1.916203934664402198, -0.9084051299479002362 ) ) ;
#148784=CARTESIAN_POINT ( 'NONE',  ( 5.900976575431972293, 1.489821718068456979, -1.054992404821846863 ) ) ;
#148791=CARTESIAN_POINT ( 'NONE',  ( 3.410420005539113841, -2.017668111602511694, -0.09479391224248739922 ) ) ;
#148792=CARTESIAN_POINT ( 'NONE',  ( 6.616270032800761314, -1.034323699838369359, -1.949367651511712207 ) ) ;
#148795=CARTESIAN_POINT ( 'NONE',  ( 4.715577910371310466, 0.4106090485030155501, -1.814890118206938574 ) ) ;
#148801=CARTESIAN_POINT ( 'NONE',  ( 6.719606831986117967, -1.999679869198322413, 0.4981698227890380970 ) ) ;
#148805=CARTESIAN_POINT ( 'NONE',  ( 1.369977976685434751, -0.4280273037657927881, 1.680018549819038531 ) ) ;
#148806=CARTESIAN_POINT ( 'NONE',  ( 0.7787878715554141795, 1.165832476461704292, 1.292284986363402055 ) ) ;
#148807=CARTESIAN_POINT ( 'NONE',  ( 0.4996044509122186672, 1.916167126895538031, -1.285522792546058390 ) ) ;
#148810=CARTESIAN_POINT ( 'NONE',  ( 2.302092711735738373, -2.060399031734764463, 0.04731154407941646350 ) ) ;
#148811=CARTESIAN_POINT ( 'NONE',  ( 0.8782795706883707032, -0.2985837142155840507, 1.993765709762222782 ) ) ;
#148814=CARTESIAN_POINT ( 'NONE',  ( 0.5847652604651293329, -0.2391135408384200411, -1.956842742423828829 ) ) ;
#148815=CARTESIAN_POINT ( 'NONE',  ( 4.658414424252744546, 1.907665749568526747, 0.1350064596054162680 ) ) ;
#148817=CARTESIAN_POINT ( 'NONE',  ( 6.727182134110200273, -0.004969159814478123736, 2.189081792362323586 ) ) ;
#148821=CARTESIAN_POINT ( 'NONE',  ( 0.3815177477655702920, 0.1955376695662625619, -2.010167716959633033 ) ) ;
#148823=CARTESIAN_POINT ( 'NONE',  ( 4.383989010750934945, 1.503879422573949132, 1.750323999079455684 ) ) ;
#148824=CARTESIAN_POINT ( 'NONE',  ( 4.967221142815226642, 1.706001049663580460, 0.9686458024478412643 ) ) ;
#148825=CARTESIAN_POINT ( 'NONE',  ( 1.463640819124707004, -0.4818986642843925972, 1.901505326443528876 ) ) ;
#148829=CARTESIAN_POINT ( 'NONE',  ( 0.02287343425391458532, 0.3688939426326736104, 2.084831875159770753 ) ) ;
#148832=CARTESIAN_POINT ( 'NONE',  ( 0.4449246239494052402, 0.5802587426733482046, -1.747387232072565189 ) ) ;
#148834=CARTESIAN_POINT ( 'NONE',  ( 4.346645206408905615, -2.146589105242337592, -0.3245344146646060302 ) ) ;
#148836=CARTESIAN_POINT ( 'NONE',  ( 2.127334043950947606, 1.896359100603739911, 0.9491756072362851349 ) ) ;
#148841=CARTESIAN_POINT ( 'NONE',  ( 2.442714938195661212, 0.4483736453565168589, 2.011251146304892767 ) ) ;
#148845=CARTESIAN_POINT ( 'NONE',  ( 0.07755575628181145265, 0.2276780653837663093, -2.222404768597834757 ) ) ;
#148847=CARTESIAN_POINT ( 'NONE',  ( 5.004515039866801906, -1.898294113557968510, -0.2302225566794338651 ) ) ;
#148849=CARTESIAN_POINT ( 'NONE',  ( 1.862946185591638049, -1.600570176636705089, 1.599199478044037059 ) ) ;
#148851=CARTESIAN_POINT ( 'NONE',  ( 0.9842725786804270571, -1.148342222048874595, 1.401147620581437048 ) ) ;
#148853=CARTESIAN_POINT ( 'NONE',  ( 1.551812156574260637, 0.9880582627100834570, 1.641127140810652252 ) ) ;
#148854=CARTESIAN_POINT ( 'NONE',  ( 3.279797552538410876, -1.996039814156633785, 0.5495672325947635883 ) ) ;
#148856=CARTESIAN_POINT ( 'NONE',  ( 1.006637970050362929, 1.494420418981519338, -1.285951363188575058 ) ) ;
#148857=CARTESIAN_POINT ( 'NONE',  ( 6.076777883369302913, -1.830186849185039044, -0.6017253874085000120 ) ) ;
#148858=CARTESIAN_POINT ( 'NONE',  ( 1.419075709855713630, 1.546787523640520856, -1.712735560227249820 ) ) ;
#148862=CARTESIAN_POINT ( 'NONE',  ( 5.230950406320217461, -1.941087326682365832, -0.6980428833110083886 ) ) ;
#148866=CARTESIAN_POINT ( 'NONE',  ( 5.772525194315006658, -1.338739070262290110, 1.625669279078660878 ) ) ;
#148869=CARTESIAN_POINT ( 'NONE',  ( 4.763041337456088264, -1.928505312680216521, -0.9765951867335493919 ) ) ;
#148870=CARTESIAN_POINT ( 'NONE',  ( 5.865880358592049149, 0.5843737978505449959, -1.933295926576389379 ) ) ;
#148879=CARTESIAN_POINT ( 'NONE',  ( 3.362517798112668821, -1.944730434982215650, -0.5331690889110105580 ) ) ;
#148884=CARTESIAN_POINT ( 'NONE',  ( 5.331013795412237855, 0.1550192300789655642, 2.156197635354038411 ) ) ;
#148889=CARTESIAN_POINT ( 'NONE',  ( 5.765249964824501028, 1.862012222821707308, -0.7743297468396084238 ) ) ;
#148891=CARTESIAN_POINT ( 'NONE',  ( 0.2578720826223569462, 0.6548769427211723615, 1.595941719785697988 ) ) ;
#148897=CARTESIAN_POINT ( 'NONE',  ( 6.362560269511371658, -1.322780316340057549, 1.322825847358683138 ) ) ;
#148898=CARTESIAN_POINT ( 'NONE',  ( 0.9967404297962767501, -1.964529542677856622, -0.4388597091333420463 ) ) ;
#148903=CARTESIAN_POINT ( 'NONE',  ( 2.385534290476189145, 0.1013982516714604792, -2.118174289320504666 ) ) ;
#148904=CARTESIAN_POINT ( 'NONE',  ( 2.161732667986946410, 1.242745142284812365, 1.587824664567152766 ) ) ;
#148905=CARTESIAN_POINT ( 'NONE',  ( 2.039049738775432719, 0.002999869061550211602, 1.811767226593180569 ) ) ;
#148911=CARTESIAN_POINT ( 'NONE',  ( 0.6728745832610707467, 1.688094080341449033, -0.9057684134900626516 ) ) ;
#148918=CARTESIAN_POINT ( 'NONE',  ( 4.592742373648754040, -0.4705147408641910944, -2.109722102427157964 ) ) ;
#148922=CARTESIAN_POINT ( 'NONE',  ( 1.986737319265439394, -1.300789755646198476, 1.674730562594067829 ) ) ;
#148923=CARTESIAN_POINT ( 'NONE',  ( 6.493173258741942178, 1.586635928914212013, -0.9027890188317911901 ) ) ;
#148924=CARTESIAN_POINT ( 'NONE',  ( 3.374254075663080332, -1.176934739253515438, 1.581319453489488325 ) ) ;
#148925=CARTESIAN_POINT ( 'NONE',  ( 5.660397963661894849, 1.910509065610028090, 0.08734628876111423523 ) ) ;
#148928=CARTESIAN_POINT ( 'NONE',  ( 5.582459562482231519, 1.174703874196600495, -1.580708309230594688 ) ) ;
#148929=CARTESIAN_POINT ( 'NONE',  ( 1.113109651085980811, -1.894741734565345004, 0.4249041608528710823 ) ) ;
#148934=CARTESIAN_POINT ( 'NONE',  ( 1.974669457019386787, -0.1036536715517746843, -2.088194013563466012 ) ) ;
#148938=CARTESIAN_POINT ( 'NONE',  ( 6.358066468859800757, 0.7272683628555456359, -1.768788954293845528 ) ) ;
#148940=CARTESIAN_POINT ( 'NONE',  ( 4.723365791888975096, -0.1103408873950258995, 2.204240794804641190 ) ) ;
#148941=CARTESIAN_POINT ( 'NONE',  ( 1.448561363430532989, 2.204290700723564811, 0.1073905156721635390 ) ) ;
#148943=CARTESIAN_POINT ( 'NONE',  ( 0.6801455168885979230, 0.9429141125626202546, 1.663586755705208420 ) ) ;
#148947=CARTESIAN_POINT ( 'NONE',  ( 3.701679681979888503, -1.565833156357125278, -1.354537944502069102 ) ) ;
#148950=CARTESIAN_POINT ( 'NONE',  ( 1.604591590977550108, -0.7782141685120853580, -2.016947388195994062 ) ) ;
#148951=CARTESIAN_POINT ( 'NONE',  ( 4.159861740090546434, 1.033864333764370702, 1.932389678422803181 ) ) ;
#148957=CARTESIAN_POINT ( 'NONE',  ( 6.188101721744481587, 1.447254432076927166, 0.9550205611794166938 ) ) ;
#148959=CARTESIAN_POINT ( 'NONE',  ( 3.520434184366732389, 0.9265386974339048232, 1.851387837889128640 ) ) ;
#148960=CARTESIAN_POINT ( 'NONE',  ( 5.378551862015316765, -0.5151900214499178787, -2.053461258077380336 ) ) ;
#148963=CARTESIAN_POINT ( 'NONE',  ( 2.887507918447276722, -1.839357967585793840, 0.7044240162308276210 ) ) ;
#148964=CARTESIAN_POINT ( 'NONE',  ( 5.683585447934278001, -1.035311694948486183, 2.045203486727443121 ) ) ;
#148965=CARTESIAN_POINT ( 'NONE',  ( 2.982817717652554101, -0.1347461720548545627, -1.820777111243766733 ) ) ;
#148970=CARTESIAN_POINT ( 'NONE',  ( 3.638934968716364793, 1.913053428401530809, 0.6273635501436899409 ) ) ;
#148971=CARTESIAN_POINT ( 'NONE',  ( 4.153139481255548660, 1.659551801668930793, -1.045809187271130591 ) ) ;
#148975=CARTESIAN_POINT ( 'NONE',  ( -0.02372336622697389028, -2.029015295047017720, -0.5039539365503820090 ) ) ;
#148976=CARTESIAN_POINT ( 'NONE',  ( 5.963686863811354932, 1.742942877579903405, -0.3063674984340163387 ) ) ;
#148978=CARTESIAN_POINT ( 'NONE',  ( 2.080269975650438585, -2.149535124392497831, -0.4257020960420563882 ) ) ;
#148979=CARTESIAN_POINT ( 'NONE',  ( 0.6436349260668382533, 0.5032331446216579129, 1.666064694988089512 ) ) ;
#148981=CARTESIAN_POINT ( 'NONE',  ( 0.2335667940003048615, 5.721530573166598188, -2.747389403444942868 ) ) ;
#148982=CARTESIAN_POINT ( 'NONE',  ( 0.3633288501447570207, 1.706897997983588322, -0.2475752363529682698 ) ) ;
#148983=CARTESIAN_POINT ( 'NONE',  ( 1.001802975355575054, 2.264736134964080438, 0.3911735967057332064 ) ) ;
#148984=CARTESIAN_POINT ( 'NONE',  ( 0.1522426329377546128, 0.8445714516599597266, 2.022489037641273857 ) ) ;
#148985=CARTESIAN_POINT ( 'NONE',  ( 2.578998426009218470, -2.112161100990978202, -0.6396139477699357423 ) ) ;
#148986=CARTESIAN_POINT ( 'NONE',  ( 0.9542540200799983774, -0.7831509020928304476, 2.025049046554725063 ) ) ;
#148987=CARTESIAN_POINT ( 'NONE',  ( 0.2053145577999641036, -0.4904175937916722128, 1.758528939493007481 ) ) ;
#148988=CARTESIAN_POINT ( 'NONE',  ( 2.782529222840863348, -0.6191273052778034636, -2.024769726974411377 ) ) ;
#148989=CARTESIAN_POINT ( 'NONE',  ( 6.827182134110219458, 3.682144966263278363, 2.702925436647874324 ) ) ;
#148990=CARTESIAN_POINT ( 'NONE',  ( 5.983413252614310451, 1.779745538724048171, -0.7376744472527080321 ) ) ;
#148992=CARTESIAN_POINT ( 'NONE',  ( 2.173718093399327422, 1.413494431062709333, 1.804626757829434380 ) ) ;
#148996=CARTESIAN_POINT ( 'NONE',  ( 4.741020875331694029, 2.125508857184394973, 0.6453399526389347329 ) ) ;
#149004=CARTESIAN_POINT ( 'NONE',  ( 2.725232599228684993, 2.001511357256777313, 0.2440295182731533341 ) ) ;
#149006=CARTESIAN_POINT ( 'NONE',  ( 1.463816541924748638, -0.5049463793320208005, 1.999668334691290683 ) ) ;
#149011=CARTESIAN_POINT ( 'NONE',  ( 4.066501749483540706, -2.044453849244652233, -0.7895499924894524568 ) ) ;
#149012=CARTESIAN_POINT ( 'NONE',  ( 1.072888940501380839, -0.9041080511620370741, 1.802418165037560138 ) ) ;
#149013=CARTESIAN_POINT ( 'NONE',  ( 0.8195642880178370948, 1.096917009463085790, -1.478703137254427924 ) ) ;
#149014=CARTESIAN_POINT ( 'NONE',  ( 4.505690185649424251, -0.7896136771840707169, -1.663358820747300237 ) ) ;
#149018=CARTESIAN_POINT ( 'NONE',  ( 5.684540951402929920, -1.781552174421060064, -0.3977488440568625605 ) ) ;
#149019=CARTESIAN_POINT ( 'NONE',  ( 6.504528880466823537, -1.955196382115764964, 0.4926337920100053447 ) ) ;
#149021=CARTESIAN_POINT ( 'NONE',  ( 4.645576076348203465, -1.746196445045271606, -1.438666788099978389 ) ) ;
#149023=CARTESIAN_POINT ( 'NONE',  ( 0.3113324583694621617, 1.833617258854224552, 1.035894449818143270 ) ) ;
#149025=CARTESIAN_POINT ( 'NONE',  ( 4.686024408448190570, -1.271122505372159539, -1.634150330299996012 ) ) ;
#149033=CARTESIAN_POINT ( 'NONE',  ( 1.107859837811319581, 1.609452232531217275, 1.380942675281403353 ) ) ;
#149034=CARTESIAN_POINT ( 'NONE',  ( 1.424421946217780732, -2.203867130488819548, 0.2783968414596868501 ) ) ;
#149035=CARTESIAN_POINT ( 'NONE',  ( 3.856552995061765632, 0.7561154531541111057, 1.965730562608114740 ) ) ;
#149039=CARTESIAN_POINT ( 'NONE',  ( 3.350005920730843911, -0.7974703105717847462, 1.792663495558038056 ) ) ;
#149045=CARTESIAN_POINT ( 'NONE',  ( 2.443736651115399283, -1.977012053918187906, 0.7674769708189137507 ) ) ;
#149047=CARTESIAN_POINT ( 'NONE',  ( 3.912515228517557286, 0.7039278570535618673, 1.831416474553926310 ) ) ;
#149048=CARTESIAN_POINT ( 'NONE',  ( 2.747127081003514881, -1.797865629537301668, 1.199965651887124896 ) ) ;
#149049=CARTESIAN_POINT ( 'NONE',  ( 2.964219115174483665, -1.702287218311925532, -0.7022057971969236645 ) ) ;
#149052=CARTESIAN_POINT ( 'NONE',  ( 4.382551862494687533, 1.553031517084975555, -0.7855321229453329224 ) ) ;
#149057=CARTESIAN_POINT ( 'NONE',  ( 2.254944280175336324, -1.671361177491991201, 1.370965666894090385 ) ) ;
#149059=CARTESIAN_POINT ( 'NONE',  ( 4.130232389481975908, 0.2495678132241747338, -2.000550906993769473 ) ) ;
#149061=CARTESIAN_POINT ( 'NONE',  ( 1.147603855448702248, -1.704515299458901012, -1.329379018566230641 ) ) ;
#149062=CARTESIAN_POINT ( 'NONE',  ( 3.502765367584356859, 1.555092314170872347, -1.211676150289840992 ) ) ;
#149063=CARTESIAN_POINT ( 'NONE',  ( 2.460178626894731213, 0.8396039701564265156, 1.783738064433965986 ) ) ;
#149064=CARTESIAN_POINT ( 'NONE',  ( 6.508999999999979025, 4.693190036150777011, 2.662629399390674667 ) ) ;
#149065=CARTESIAN_POINT ( 'NONE',  ( 2.858853853349733409, 0.2825237051190258031, -1.921275437378862305 ) ) ;
#149074=CARTESIAN_POINT ( 'NONE',  ( 1.009129827085092135, 1.670030910484705755, -1.442630471070925458 ) ) ;
#149076=CARTESIAN_POINT ( 'NONE',  ( 5.032062496497622384, 1.126290172248314292, 1.606047186625796819 ) ) ;
#149078=CARTESIAN_POINT ( 'NONE',  ( 3.608711286396129481, 2.011918449240827744, 0.6600949426460513969 ) ) ;
#149080=CARTESIAN_POINT ( 'NONE',  ( 0.07479286986305369589, 0.004866263145587855152, -1.855573292446037970 ) ) ;
#149082=CARTESIAN_POINT ( 'NONE',  ( 3.767381502543519112, 1.024135474229198151, 1.529801857347697025 ) ) ;
#149085=CARTESIAN_POINT ( 'NONE',  ( 5.660427296577901224, 2.118236611397010805, 0.1021076702828054988 ) ) ;
#149089=CARTESIAN_POINT ( 'NONE',  ( 5.729779026133646092, -1.304086877343976880, -1.595700086769378023 ) ) ;
#149090=CARTESIAN_POINT ( 'NONE',  ( 0.5548465212725885998, 1.550470960922016861, -1.029025501433494583 ) ) ;
#149091=CARTESIAN_POINT ( 'NONE',  ( 3.034521004542716227, -1.622529355458858236, 0.8704296449140033198 ) ) ;
#149097=CARTESIAN_POINT ( 'NONE',  ( 2.332911791115964473, 2.140974936812658935, 0.5348262304398290201 ) ) ;
#149098=CARTESIAN_POINT ( 'NONE',  ( 4.675235532476687439, 0.006304645973906687281, -2.262578822721802219 ) ) ;
#149099=CARTESIAN_POINT ( 'NONE',  ( 3.626185617424378282, 2.007256095728218614, 0.1928357053486499662 ) ) ;
#149102=CARTESIAN_POINT ( 'NONE',  ( 4.429823666617582312, -1.775263289385048848, 0.3600210208860327721 ) ) ;
#149103=CARTESIAN_POINT ( 'NONE',  ( 5.823430154129352054, -1.392497453891910375, -1.315930268783272794 ) ) ;
#149104=CARTESIAN_POINT ( 'NONE',  ( 6.827182134110172385, 0.001020705822878450282, 1.910856149448317165 ) ) ;
#149105=CARTESIAN_POINT ( 'NONE',  ( 5.383624799460786647, 1.257121276536907750, 1.385457850027263182 ) ) ;
#149106=CARTESIAN_POINT ( 'NONE',  ( 5.002340964340571183, 1.856068601349126324, 0.1372510170762584192 ) ) ;
#149108=CARTESIAN_POINT ( 'NONE',  ( 5.946140033727446372, 1.768047588762114986, 0.08285011829376774661 ) ) ;
#149109=CARTESIAN_POINT ( 'NONE',  ( 0.4269707148552639997, -1.727061408318403712, 1.040797348915108111 ) ) ;
#149110=( BOUNDED_CURVE ( )  B_SPLINE_CURVE ( 3, ( #44790, #75135, #7977, #27439 ),
 .UNSPECIFIED., .F., .T. ) 
 B_SPLINE_CURVE_WITH_KNOTS ( ( 4, 4 ),
 ( 0.000000000000000000, 0.5000000000000003331 ),
 .UNSPECIFIED. ) 
 CURVE ( )  GEOMETRIC_REPRESENTATION_ITEM ( )  RATIONAL_B_SPLINE_CURVE ( ( 1.000000000000000222, 0.3333333333333329818, 0.3333333333333334259, 1.000000000000000666 ) ) 
 REPRESENTATION_ITEM ( '' )  );
#149112=CARTESIAN_POINT ( 'NONE',  ( 2.631583836753316863, -1.964825297316885155, 0.7587525405363388931 ) ) ;
#149116=CARTESIAN_POINT ( 'NONE',  ( 2.408468576312505771, -2.014670991514801113, -0.1442217307643048063 ) ) ;
#149121=CARTESIAN_POINT ( 'NONE',  ( 1.897963814661303150, -0.7301937759345776824, 2.034636513274298064 ) ) ;
#149122=CARTESIAN_POINT ( 'NONE',  ( 6.889999999999970370, 7.053389210336755255, 2.318152334880723142 ) ) ;
#149130=CARTESIAN_POINT ( 'NONE',  ( 0.5916818631664167993, -0.7834642122952638621, 2.046923429677327100 ) ) ;
#149132=CARTESIAN_POINT ( 'NONE',  ( 1.973834762636607509, 2.164947816325224039, -0.6572921511966890451 ) ) ;
#149141=CARTESIAN_POINT ( 'NONE',  ( 2.829092851278795617, -1.652813950429321999, 0.6331040572071617856 ) ) ;
#149142=CARTESIAN_POINT ( 'NONE',  ( 6.159228477734898455, -1.889628185881117695, -1.139594184263223120 ) ) ;
#149146=CARTESIAN_POINT ( 'NONE',  ( 5.255482535091188012, 1.942537579172060047, -0.5405093616211650298 ) ) ;
#149148=CARTESIAN_POINT ( 'NONE',  ( 2.465516990510143280, 1.834972510290140191, -0.3627323784974947340 ) ) ;
#149149=CARTESIAN_POINT ( 'NONE',  ( 2.852461952307944415, -2.064405766265942521, -0.1567919417525542591 ) ) ;
#149152=CARTESIAN_POINT ( 'NONE',  ( 2.443496805918866865, -1.782974011999260977, 0.6919810379762069141 ) ) ;
#149158=CARTESIAN_POINT ( 'NONE',  ( 0.7735182334044669039, 0.3705173918269571431, -1.875978362188876813 ) ) ;
#149160=CARTESIAN_POINT ( 'NONE',  ( 2.928120951529111338, 1.047165451586975049, 1.658829547137883775 ) ) ;
#149164=CARTESIAN_POINT ( 'NONE',  ( 5.115537534566191091, 1.735013203181461350, 1.219038288318145646 ) ) ;
#149167=CARTESIAN_POINT ( 'NONE',  ( 6.151636724293027214, 0.5744773170833740172, -1.885769548957224817 ) ) ;
#149169=CARTESIAN_POINT ( 'NONE',  ( 2.461191956773252087, -1.671442449460639468, 1.121892926246186306 ) ) ;
#149171=CARTESIAN_POINT ( 'NONE',  ( 0.6150561885070615631, 0.1604698007556179251, 2.111222410368835067 ) ) ;
#149173=CARTESIAN_POINT ( 'NONE',  ( 2.471216696211364638, 1.848302923701108158, 0.9330170062570308787 ) ) ;
#149178=CARTESIAN_POINT ( 'NONE',  ( 5.578101482107681974, -2.039469400243614672, -0.4589526871568836430 ) ) ;
#149180=CARTESIAN_POINT ( 'NONE',  ( 4.366094929315432083, 0.8608494910617261464, 1.609850404305966265 ) ) ;
#149186=CARTESIAN_POINT ( 'NONE',  ( 5.192482782645277517, -2.189556457885518892, -0.2746672974567528347 ) ) ;
#149189=CARTESIAN_POINT ( 'NONE',  ( 4.424404876070213710, -0.8207606565990737124, -1.727334472114170794 ) ) ;
#149197=CARTESIAN_POINT ( 'NONE',  ( -0.07694640568740516995, -1.131669979810394633, -1.452919414246391261 ) ) ;
#149200=CARTESIAN_POINT ( 'NONE',  ( 5.184763189090160651, -0.2277032997176874074, -1.856539885857370953 ) ) ;
#149205=CARTESIAN_POINT ( 'NONE',  ( 1.692182146996668912, 0.9751594699732427651, -1.711024247558447842 ) ) ;
#149206=CARTESIAN_POINT ( 'NONE',  ( 2.548454031204652637, -1.388473193742698619, 1.462459214312331168 ) ) ;
#149210=CARTESIAN_POINT ( 'NONE',  ( 2.748186945943337012, 0.7392028471469233031, 2.063141171074922120 ) ) ;
#149211=CARTESIAN_POINT ( 'NONE',  ( 6.516225534515442952, -0.8655890497146904172, -1.607451055071248636 ) ) ;
#149213=CARTESIAN_POINT ( 'NONE',  ( 6.825078400183556049, 7.053092130845653784, 2.453807127456457238 ) ) ;
#149220=CARTESIAN_POINT ( 'NONE',  ( 4.915489835137424102, -0.9894786724786635013, -1.552603174752004600 ) ) ;
#149221=CARTESIAN_POINT ( 'NONE',  ( 0.6100213217023927603, -0.7224815109628316412, 1.879156614266486391 ) ) ;
#149222=CARTESIAN_POINT ( 'NONE',  ( 3.075839645193487293, 1.666627022722726670, -1.582919517265988674 ) ) ;
#149224=CARTESIAN_POINT ( 'NONE',  ( 0.8482322855925720217, -1.845984902429298025, -0.2351823381797259749 ) ) ;
#149228=CARTESIAN_POINT ( 'NONE',  ( 3.955252344019274169, -1.661368509396843995, 0.9470704235666274062 ) ) ;
#149232=CARTESIAN_POINT ( 'NONE',  ( 3.526972370393847811, -1.930915134098612373, 0.8022322841883463562 ) ) ;
#149233=CARTESIAN_POINT ( 'NONE',  ( 2.131529507118444133, -1.219933349377068099, -1.418231869465089057 ) ) ;
#149236=CARTESIAN_POINT ( 'NONE',  ( 5.688959394570705541, 1.398425918548395153, 1.197878823674280779 ) ) ;
#149239=CARTESIAN_POINT ( 'NONE',  ( 5.197747934024010696, -0.6158827634895787106, 1.611369335837910644 ) ) ;
#149241=CARTESIAN_POINT ( 'NONE',  ( 0.8438932004057161373, 0.3398822538093429491, -1.700291973301551129 ) ) ;
#149242=CARTESIAN_POINT ( 'NONE',  ( 6.463508838306311510, 0.3818026259072569983, -2.173449913608487716 ) ) ;
#149244=EDGE_CURVE ( 'NONE', #113025, #111140, #27920, .T. ) ;
#149247=CARTESIAN_POINT ( 'NONE',  ( 4.487298306821032590, 0.1004956810540975631, 2.168842786202809680 ) ) ;
#149248=CARTESIAN_POINT ( 'NONE',  ( 2.877373901574116211, 1.733520850877915187, -0.5729475677913041798 ) ) ;
#149249=CARTESIAN_POINT ( 'NONE',  ( 0.9890223832832998330, 0.1386981244183866369, 1.956888703154149534 ) ) ;
#149250=CARTESIAN_POINT ( 'NONE',  ( 5.296159404803077564, -0.9547103268642830320, -1.889991272064439176 ) ) ;
#149253=CARTESIAN_POINT ( 'NONE',  ( 6.339416484298314280, 0.8816828672218860463, -2.116228320707528976 ) ) ;
#149256=CARTESIAN_POINT ( 'NONE',  ( 1.981254353800803836, -1.939921095825656305, -0.8566514584813913480 ) ) ;
#149259=CARTESIAN_POINT ( 'NONE',  ( 6.192256317468841864, 1.077302059837774273, -1.884901478735945046 ) ) ;
#149260=CARTESIAN_POINT ( 'NONE',  ( 6.983263157960365675, 7.052158404629149224, 2.651961988451009944 ) ) ;
#149262=CARTESIAN_POINT ( 'NONE',  ( 2.245073739244434208, 2.155446677131687139, 0.5364521487482876161 ) ) ;
#149264=CARTESIAN_POINT ( 'NONE',  ( 6.328750030911493241, 0.7691242348151774433, -1.864167186630163009 ) ) ;
#149266=CARTESIAN_POINT ( 'NONE',  ( 4.838768981748684972, -1.999376597400838174, -0.5061158833775216692 ) ) ;
#149272=CARTESIAN_POINT ( 'NONE',  ( 0.9200049341780929257, 1.243975779098299927, -1.680105788963416780 ) ) ;
#149273=CARTESIAN_POINT ( 'NONE',  ( 4.282634502089007533, 1.642705626968201216, -0.8318752211165170163 ) ) ;
#149275=CARTESIAN_POINT ( 'NONE',  ( 1.289626238417174831, -0.7804147442260088718, 1.538193839892360471 ) ) ;
#149276=CARTESIAN_POINT ( 'NONE',  ( 0.3918150239524306189, -2.006371095615328226, 0.2024682584410575914 ) ) ;
#149277=CARTESIAN_POINT ( 'NONE',  ( 1.881834863725037277, -0.6175646290925532744, -2.214118314682656852 ) ) ;
#149279=CARTESIAN_POINT ( 'NONE',  ( 1.247787707462020723, -1.783668181329477465, -1.391623327695093115 ) ) ;
#149280=CARTESIAN_POINT ( 'NONE',  ( 3.826872495277617414, 1.999758222635793947, 0.6608955202877621060 ) ) ;
#149284=CARTESIAN_POINT ( 'NONE',  ( 6.656247777566118629, -1.895918425136842833, 0.7852924748303453661 ) ) ;
#149290=CARTESIAN_POINT ( 'NONE',  ( 5.291355414077095531, -0.05489642510923819357, -2.220905102120291019 ) ) ;
#149291=CARTESIAN_POINT ( 'NONE',  ( 3.609492757825348175, -2.159078094573213757, 0.3743817768235499499 ) ) ;
#149294=CARTESIAN_POINT ( 'NONE',  ( 5.320985837513584116, 1.605487267134264595, -1.385306402853322405 ) ) ;
#149296=CARTESIAN_POINT ( 'NONE',  ( 6.889999999999965041, 7.051532193125384040, 2.878152852197481071 ) ) ;
#149298=CARTESIAN_POINT ( 'NONE',  ( 5.853796514643677007, -1.537196951383312804, -1.461068456062891041 ) ) ;
#149302=CARTESIAN_POINT ( 'NONE',  ( 6.702040708066513197, -2.161345696851162845, 0.04751196314212167288 ) ) ;
#149304=CARTESIAN_POINT ( 'NONE',  ( 6.233933901472759942, 1.822226914158030286, 0.2631550708301691466 ) ) ;
#149307=CARTESIAN_POINT ( 'NONE',  ( 0.8897394992621279197, -0.4213058873485018840, -1.688518545418623340 ) ) ;
#149313=CARTESIAN_POINT ( 'NONE',  ( 5.172814640947125397, -2.034155943344346795, -0.7319064324283753864 ) ) ;
#149317=CARTESIAN_POINT ( 'NONE',  ( 4.592742373648754040, -0.4705147408641910944, -2.109722102427157964 ) ) ;
#149321=CARTESIAN_POINT ( 'NONE',  ( 6.503199639966785739, 1.637674054957323433, 1.097108698291071827 ) ) ;
#149322=CARTESIAN_POINT ( 'NONE',  ( 5.606719662199564524, 0.7002562906495370942, -1.586348028144116462 ) ) ;
#149324=CARTESIAN_POINT ( 'NONE',  ( 1.734175692058033347, 2.168326105380265378, 0.3173973903456903112 ) ) ;
#149325=CARTESIAN_POINT ( 'NONE',  ( 2.397911878029312494, 1.783863880296262305, 1.463803424465635272 ) ) ;
#149326=CARTESIAN_POINT ( 'NONE',  ( 5.343066995996487378, -1.769704953023493399, 1.055641863377870138 ) ) ;
#149327=CARTESIAN_POINT ( 'NONE',  ( 6.427294056597427918, -1.271908742016104821, -1.467670737461545860 ) ) ;
#149331=CARTESIAN_POINT ( 'NONE',  ( 3.305043459179863419, -0.4174351347619070229, -2.078937965663613774 ) ) ;
#149333=CARTESIAN_POINT ( 'NONE',  ( 1.635388916632842360, 0.6352005984417673501, 1.913803229121699534 ) ) ;
#149335=CARTESIAN_POINT ( 'NONE',  ( 5.034293675167554660, 1.138177661764948834, -1.890478833441497031 ) ) ;
#149337=CARTESIAN_POINT ( 'NONE',  ( 2.149040161283378936, 1.622117262959487549, -0.9118680782764712056 ) ) ;
#149338=CARTESIAN_POINT ( 'NONE',  ( 0.1399997263886024468, 7.629137130509076492, -2.599723212958489516 ) ) ;
#149342=CARTESIAN_POINT ( 'NONE',  ( 6.825078400183546279, 2.419143596098617621, 2.525240329153962904 ) ) ;
#149345=CARTESIAN_POINT ( 'NONE',  ( 3.731368383135937883, -1.904846641313600708, 0.7871492865094924518 ) ) ;
#149348=CARTESIAN_POINT ( 'NONE',  ( 3.809243936906735239, 1.705047127353828351, -1.082240749027115978 ) ) ;
#149352=CARTESIAN_POINT ( 'NONE',  ( 1.393510596882661989, 1.559873972335079184, 1.346953478171313057 ) ) ;
#149356=CARTESIAN_POINT ( 'NONE',  ( -0.2408018239684278916, 2.008845716682732263, -2.515352618630611659 ) ) ;
#149357=CARTESIAN_POINT ( 'NONE',  ( 1.411775340717499994, 1.237668241052336970, -1.363247244775968259 ) ) ;
#149358=CARTESIAN_POINT ( 'NONE',  ( 6.481111342790009999, -0.1036386110354891726, -2.204582208980155222 ) ) ;
#149360=CARTESIAN_POINT ( 'NONE',  ( 1.019082891775088484, 1.996809913787592095, 0.8282600050937348746 ) ) ;
#149362=CARTESIAN_POINT ( 'NONE',  ( 2.430875351317234756, -1.673853735218135741, 1.124246214196801485 ) ) ;
#149363=CARTESIAN_POINT ( 'NONE',  ( 0.1399997263886024468, 7.629137130509076492, -2.599723212958489516 ) ) ;
#149366=CARTESIAN_POINT ( 'NONE',  ( 4.241065053910620719, -1.715758787085974957, 0.9708604712577516560 ) ) ;
#149367=CARTESIAN_POINT ( 'NONE',  ( 3.028530041973789722, 0.4946322284519070189, 1.954779462066410733 ) ) ;
#149371=CARTESIAN_POINT ( 'NONE',  ( 5.971333374016301043, 0.1563851966441217600, -2.100315135224324337 ) ) ;
#149372=CARTESIAN_POINT ( 'NONE',  ( 5.107906530550561541, 0.6527686194882609261, -1.964817160181751010 ) ) ;
#149375=CARTESIAN_POINT ( 'NONE',  ( 6.639320575229256782, 3.693993153770461113, 2.517469677323687538 ) ) ;
#149376=CARTESIAN_POINT ( 'NONE',  ( 4.869401706892690029, -1.708532917064720991, -1.076912495999365449 ) ) ;
#149378=CARTESIAN_POINT ( 'NONE',  ( 3.370030522709596355, 2.251568201494443588, -0.5052104078027676026 ) ) ;
#149379=CARTESIAN_POINT ( 'NONE',  ( 1.006769942787159033, 0.5948965838462864086, 1.974949077847313328 ) ) ;
#149387=CARTESIAN_POINT ( 'NONE',  ( 3.613895077877467443, 0.5305607931336644434, -2.105228361949755378 ) ) ;
#149391=CARTESIAN_POINT ( 'NONE',  ( 3.034521004542716227, -1.622529355458858236, 0.8704296449140033198 ) ) ;
#149393=CARTESIAN_POINT ( 'NONE',  ( 4.054362073078698891, -1.623213109359676443, 1.472610181411204922 ) ) ;
#149395=CARTESIAN_POINT ( 'NONE',  ( 4.979486748501788185, 2.112903116282875082, -0.8095491994110515233 ) ) ;
#149400=CARTESIAN_POINT ( 'NONE',  ( 6.028513167084792457, 1.705988696259161719, 0.4703064415670314413 ) ) ;
#149402=CARTESIAN_POINT ( 'NONE',  ( 4.160795161724285762, 0.5389290103979550439, 1.939535095694967959 ) ) ;
#149404=CARTESIAN_POINT ( 'NONE',  ( 3.276497419027382563, -1.255868110884267530, 1.690353172608966448 ) ) ;
#149405=CARTESIAN_POINT ( 'NONE',  ( 0.7201576878450620667, 1.887430420354209160, 0.3262839321072578125 ) ) ;
#149409=CARTESIAN_POINT ( 'NONE',  ( 2.137097444212227693, -0.09349721708603592196, -1.967446466973846952 ) ) ;
#149410=CARTESIAN_POINT ( 'NONE',  ( 0.9185735243398345240, 1.726912363944958617, 0.7195956246372691156 ) ) ;
#149411=CARTESIAN_POINT ( 'NONE',  ( 0.5726126529861442771, 1.355618539282506640, -1.418395753018865113 ) ) ;
#149412=CARTESIAN_POINT ( 'NONE',  ( -0.05268457437105152075, -1.747710896673961622, 0.7768168958157274373 ) ) ;
#149416=CARTESIAN_POINT ( 'NONE',  ( 6.227412191919261986, -1.760757567598171480, 0.6321290105378990498 ) ) ;
#149418=CARTESIAN_POINT ( 'NONE',  ( 6.192251260771239885, 1.025525066348543568, -1.798363755310352419 ) ) ;
#149420=CARTESIAN_POINT ( 'NONE',  ( 0.4321921490204432281, 1.190796696626210682, 1.693455153822187587 ) ) ;
#149429=CARTESIAN_POINT ( 'NONE',  ( 5.810985101215744741, -1.547553103248515027, 1.205733875218002238 ) ) ;
#149432=CARTESIAN_POINT ( 'NONE',  ( 3.725935337077026510, -1.776739457207517248, -0.9528653653038119398 ) ) ;
#149433=CARTESIAN_POINT ( 'NONE',  ( 3.186650014752292925, 1.506923149468800682, -1.182699731353755501 ) ) ;
#149435=CARTESIAN_POINT ( 'NONE',  ( 1.031118135130421498, -1.979082047791239418, 0.9416876394413643547 ) ) ;
#149436=CARTESIAN_POINT ( 'NONE',  ( 0.1331715793776860612, 5.723291439345874920, -2.547624684121822636 ) ) ;
#149437=CARTESIAN_POINT ( 'NONE',  ( 3.022558680773678397, 1.760047114015901526, 0.6337009143728977723 ) ) ;
#149441=CARTESIAN_POINT ( 'NONE',  ( 4.569977310993092345, -0.9968198436792906625, 1.867865768302608531 ) ) ;
#149443=CARTESIAN_POINT ( 'NONE',  ( 6.004363041306050697, 2.067815565686380364, 0.1054426792976848049 ) ) ;
#149444=CARTESIAN_POINT ( 'NONE',  ( 2.384421550557855429, -0.3601958963256215451, -2.059324561056875336 ) ) ;
#149446=CARTESIAN_POINT ( 'NONE',  ( 0.2347969022384633897, -1.580228140511737100, 0.6916409326972148275 ) ) ;
#149449=CARTESIAN_POINT ( 'NONE',  ( 6.925078400183550364, -0.007619068086212391067, 2.144148427808051594 ) ) ;
#149456=CARTESIAN_POINT ( 'NONE',  ( 1.049118701917159946, -1.638035101892039602, 0.7738018112423280526 ) ) ;
#149466=CARTESIAN_POINT ( 'NONE',  ( 3.226847753617521963, -1.718569378881330989, -0.7146659259855172586 ) ) ;
#149467=CARTESIAN_POINT ( 'NONE',  ( 0.9310837752575386039, -1.510843254991366402, -1.177573636344444896 ) ) ;
#149468=CARTESIAN_POINT ( 'NONE',  ( 6.334985678650366658, 0.1896739171414266178, 1.917017188598265420 ) ) ;
#149476=CARTESIAN_POINT ( 'NONE',  ( 4.856285946018928712, -1.968934436971051305, -0.05237921274019693985 ) ) ;
#149477=CARTESIAN_POINT ( 'NONE',  ( 1.119968162728638417, -0.5116716972351254000, 2.057716464106795318 ) ) ;
#149481=CARTESIAN_POINT ( 'NONE',  ( 5.824229312739954700, 2.111140916326431416, 0.5876101183235474812 ) ) ;
#149483=CARTESIAN_POINT ( 'NONE',  ( 4.541967935523826938, 0.8243062533531859692, -1.741262965308258970 ) ) ;
#149485=CARTESIAN_POINT ( 'NONE',  ( 0.5690311950540331010, 0.1842100624489529381, -1.816270042949569730 ) ) ;
#149486=CARTESIAN_POINT ( 'NONE',  ( 1.506762622594171930, -0.7967928049063889295, -2.058199171410409978 ) ) ;
#149491=CARTESIAN_POINT ( 'NONE',  ( 6.016450702237627901, 0.7947307017554460229, 1.802146183335861629 ) ) ;
#149492=CARTESIAN_POINT ( 'NONE',  ( 1.540467339043756434, -1.639628711884850265, 1.040515435762645380 ) ) ;
#149493=CARTESIAN_POINT ( 'NONE',  ( 6.890000000000009450, -0.01081285896028030651, 2.279840171838908525 ) ) ;
#149495=CARTESIAN_POINT ( 'NONE',  ( 4.645250437676715194, 1.663689067502411412, -0.8338919413633429922 ) ) ;
#149501=CARTESIAN_POINT ( 'NONE',  ( 0.2928600448571066495, 1.818678932476354149, -1.222557900829209121 ) ) ;
#149506=CARTESIAN_POINT ( 'NONE',  ( 1.084280211047653264, -1.780658692889337091, -0.4022698149812459212 ) ) ;
#149509=CARTESIAN_POINT ( 'NONE',  ( 3.410549273128512304, -1.036309148604511288, -1.390238610006881981 ) ) ;
#149513=CARTESIAN_POINT ( 'NONE',  ( 6.147073579019600054, -1.539581890156189292, 0.9809480439507823890 ) ) ;
#149514=CARTESIAN_POINT ( 'NONE',  ( 4.873855640358407904, -1.924671727690111966, 0.3787619532854279436 ) ) ;
#149517=CARTESIAN_POINT ( 'NONE',  ( 4.248766647586673884, 2.079802475202694900, 0.4125236972643344102 ) ) ;
#149521=CARTESIAN_POINT ( 'NONE',  ( 2.360293207207576849, -2.069885933316969240, 0.04650197241463926989 ) ) ;
#149525=CARTESIAN_POINT ( 'NONE',  ( 2.409158461118418693, -1.326566255432750197, -1.877132621748223373 ) ) ;
#149533=CARTESIAN_POINT ( 'NONE',  ( 3.779479514802902340, 0.2291398179169491789, -1.898525689255560422 ) ) ;
#149535=CARTESIAN_POINT ( 'NONE',  ( 5.332891432879703686, 0.1301960547291525494, 1.719897333435776776 ) ) ;
#149536=CARTESIAN_POINT ( 'NONE',  ( 3.415250174187448362, -1.861344788686780438, 0.7762291900053899241 ) ) ;
#149537=CARTESIAN_POINT ( 'NONE',  ( 4.834794202738506463, 0.7220915915403209873, -2.182417960738481710 ) ) ;
#149539=CARTESIAN_POINT ( 'NONE',  ( 1.032169062358662348, -1.402649970393770484, -1.703791656331831605 ) ) ;
#149541=CARTESIAN_POINT ( 'NONE',  ( 6.204346024843479412, -0.6390883176130756071, -1.650510209504873593 ) ) ;
#149543=CARTESIAN_POINT ( 'NONE',  ( 2.203457528917366570, -0.4999491416500188579, 2.236933425931705521 ) ) ;
#149544=CARTESIAN_POINT ( 'NONE',  ( 0.2337849711155593480, 0.2922425735506446465, 1.715447441342861534 ) ) ;
#149546=CARTESIAN_POINT ( 'NONE',  ( 6.404242042726283834, 1.626525233829802408, -1.468802942141099077 ) ) ;
#149550=CARTESIAN_POINT ( 'NONE',  ( 6.514133371570012265, 2.065101995627930620, -0.1482383472809906122 ) ) ;
#149551=CARTESIAN_POINT ( 'NONE',  ( 1.569546381206438967, 1.394087592100446971, 1.457234012747665508 ) ) ;
#149554=CARTESIAN_POINT ( 'NONE',  ( 5.145112535762402572, -1.651256390841379762, 0.9921342509419928124 ) ) ;
#149556=CARTESIAN_POINT ( 'NONE',  ( 2.566880079249767022, 0.7526719050801253807, 2.090118821510750458 ) ) ;
#149557=ORIENTED_EDGE ( 'NONE', *, *, #176737, .F. ) ;
#149564=CARTESIAN_POINT ( 'NONE',  ( 3.966134247641060817, -1.625707123410979449, -0.6219663355369866586 ) ) ;
#149565=CARTESIAN_POINT ( 'NONE',  ( 3.754310534785664899, -1.959519245081872585, -0.09869234604030494018 ) ) ;
#149571=CARTESIAN_POINT ( 'NONE',  ( 0.8716181059342765769, -0.3045769538833371648, 2.039966307373513033 ) ) ;
#149574=CARTESIAN_POINT ( 'NONE',  ( 1.587200854914575077, -0.3333832325802545404, -2.237697771577638051 ) ) ;
#149577=CARTESIAN_POINT ( 'NONE',  ( 2.284254421533092216, -1.833544361078912388, -0.3693468884775341077 ) ) ;
#149578=CARTESIAN_POINT ( 'NONE',  ( 1.353744004007218615, 0.1277301157788513497, -1.729473920685227428 ) ) ;
#149579=CARTESIAN_POINT ( 'NONE',  ( 5.073855206572205567, -1.217758175834412260, 1.821886007100224969 ) ) ;
#149580=CARTESIAN_POINT ( 'NONE',  ( 6.176872536373793743, -2.188556106905717780, -0.7317919303653409591 ) ) ;
#149581=CARTESIAN_POINT ( 'NONE',  ( 1.481398948507294477, 1.904550386266171902, -0.7878645111692607061 ) ) ;
#149582=CARTESIAN_POINT ( 'NONE',  ( 3.574105527548767647, -1.871835235816914578, -0.5168888941823551741 ) ) ;
#149584=CARTESIAN_POINT ( 'NONE',  ( 5.747288119592351308, -1.474170506619469023, -1.151262835514428540 ) ) ;
#149585=CARTESIAN_POINT ( 'NONE',  ( 1.343750000000001110, 1.895863743164117654, 0.7852924748299160429 ) ) ;
#149587=CARTESIAN_POINT ( 'NONE',  ( 6.274767501101933043, -2.001204493855372579, 0.2439949869823473949 ) ) ;
#149591=CARTESIAN_POINT ( 'NONE',  ( 4.553361389630797618, -1.314998166741452090, 1.528740011303417745 ) ) ;
#149595=CARTESIAN_POINT ( 'NONE',  ( 2.244514701088017539, 0.3993153960501935051, 1.781317584591130432 ) ) ;
#149602=CARTESIAN_POINT ( 'NONE',  ( 6.604167511870285168, -0.8622997358492515696, 1.824817093501039267 ) ) ;
#149603=CARTESIAN_POINT ( 'NONE',  ( -0.02259406399240069044, -1.896172633340575064, -0.9493637518730788649 ) ) ;
#149609=CARTESIAN_POINT ( 'NONE',  ( 5.963760128287220574, 2.030816783491296906, -0.3497918165830601334 ) ) ;
#149610=CARTESIAN_POINT ( 'NONE',  ( 5.537732479266092689, -1.587839044716709669, 1.242724925242834066 ) ) ;
#149619=CARTESIAN_POINT ( 'NONE',  ( 5.431017465639029318, 0.9912489969874547224, 1.755499476546865445 ) ) ;
#149620=CARTESIAN_POINT ( 'NONE',  ( 4.786955173189685553, 1.366302399619228947, 1.234289508136581892 ) ) ;
#149622=CARTESIAN_POINT ( 'NONE',  ( 3.704037377190313673, -0.6708616879335957961, 2.208036538417802230 ) ) ;
#149624=CARTESIAN_POINT ( 'NONE',  ( 5.343121995983710626, -1.856993961526328007, 1.106124453333141577 ) ) ;
#149626=CARTESIAN_POINT ( 'NONE',  ( 0.4330194205178988232, -1.374205638499223614, -1.372529395279479703 ) ) ;
#149631=CARTESIAN_POINT ( 'NONE',  ( 3.326877442632663939, 0.04465521416292458912, 1.870282673472216439 ) ) ;
#149633=CARTESIAN_POINT ( 'NONE',  ( 0.8438408207818194340, -1.215224102361469161, -1.476598726422105656 ) ) ;
#149636=CARTESIAN_POINT ( 'NONE',  ( 3.000804911251079510, -0.6410980074830170405, -2.111705341948390657 ) ) ;
#149642=CARTESIAN_POINT ( 'NONE',  ( 0.8078137629249462215, -1.962250697097242869, 0.1890654564427676487 ) ) ;
#149643=CARTESIAN_POINT ( 'NONE',  ( 0.1480895125635858234, -1.786911571543071675, -1.459641600669525197 ) ) ;
#149644=CARTESIAN_POINT ( 'NONE',  ( 1.451531895509536874, 1.483362660712842063, 1.284035263222626844 ) ) ;
#149645=CARTESIAN_POINT ( 'NONE',  ( 4.364169495198770399, -2.057374995403418172, 0.1468088122822813202 ) ) ;
#149647=ADVANCED_FACE ( 'NONE', ( #30021 ), #57010, .T. ) ;
#149654=CARTESIAN_POINT ( 'NONE',  ( 1.270657207514551246, -0.9741964446108697384, -1.940257991389877201 ) ) ;
#149656=CARTESIAN_POINT ( 'NONE',  ( 5.759284750224211713, 1.812880138157666465, -0.3211251414683007899 ) ) ;
#149660=CARTESIAN_POINT ( 'NONE',  ( 1.124039026005444475, 1.118881483734196935, -1.498852260102357725 ) ) ;
#149663=CARTESIAN_POINT ( 'NONE',  ( 0.07735805125223899070, 0.2300150639059690694, -2.122327182112139443 ) ) ;
#149666=CARTESIAN_POINT ( 'NONE',  ( 0.7328884408557727603, 1.767063509844998492, 0.7314339715377634610 ) ) ;
#149667=CARTESIAN_POINT ( 'NONE',  ( 2.482954129442132452, 1.619277697627572676, -0.7147633530761726695 ) ) ;
#149668=CARTESIAN_POINT ( 'NONE',  ( 0.6625817696367036769, 0.5554855734208345996, 1.829800363923417716 ) ) ;
#149670=CARTESIAN_POINT ( 'NONE',  ( 4.499565103457034532, -1.877818951341524878, 0.3776799693050793549 ) ) ;
#149672=CARTESIAN_POINT ( 'NONE',  ( 5.459413677600381654, 1.609035625656387802, 1.135536449648701041 ) ) ;
#149673=CARTESIAN_POINT ( 'NONE',  ( 1.424255164902767934, -2.103954720533041556, 0.2648648325892372646 ) ) ;
#149675=CARTESIAN_POINT ( 'NONE',  ( 3.467518583331068438, 1.825290416974333807, -0.4087457676540603990 ) ) ;
#149676=CARTESIAN_POINT ( 'NONE',  ( 0.2404813148422607627, 0.3085585699703840556, 1.799268721412583316 ) ) ;
#149678=CARTESIAN_POINT ( 'NONE',  ( 3.862124860921032354, 2.190326239153097543, -0.2693113811002012525 ) ) ;
#149681=CARTESIAN_POINT ( 'NONE',  ( 2.049356628244120682, 1.795697342706262578, -1.014786283375568976 ) ) ;
#149688=CARTESIAN_POINT ( 'NONE',  ( 4.703616579153604427, -1.598285800263723910, -1.315984976451072930 ) ) ;
#149690=CARTESIAN_POINT ( 'NONE',  ( 1.897963814661303150, -0.7301937759345775714, 2.034636513274298064 ) ) ;
#149692=CARTESIAN_POINT ( 'NONE',  ( 1.576825605243727502, -1.426663165427190405, 1.429853764617691647 ) ) ;
#149698=CARTESIAN_POINT ( 'NONE',  ( 6.485703859413265882, 1.880147802650249611, 0.7282652505391642439 ) ) ;
#149699=CARTESIAN_POINT ( 'NONE',  ( 0.3215004009857677092, -1.429452135790244549, -1.422604240635255479 ) ) ;
#149700=CARTESIAN_POINT ( 'NONE',  ( 6.639320575229258559, 7.052241914652472410, 2.701414248926166994 ) ) ;
#149701=CARTESIAN_POINT ( 'NONE',  ( 4.985950990042907094, -2.174969566330759996, -0.2684501861200879747 ) ) ;
#149703=CARTESIAN_POINT ( 'NONE',  ( 3.990413957267644474, -1.096855775730350757, 1.566394476586838502 ) ) ;
#149708=CARTESIAN_POINT ( 'NONE',  ( 2.372672929649359386, -0.3474902101525711440, -1.986097784353996643 ) ) ;
#149710=CARTESIAN_POINT ( 'NONE',  ( 0.2051334325893399424, 1.998568519175287328, 1.122693669494337909 ) ) ;
#149712=CARTESIAN_POINT ( 'NONE',  ( 4.295721138614797319, -0.6590762262537721572, 1.594082981517078945 ) ) ;
#149713=CARTESIAN_POINT ( 'NONE',  ( 0.1399997263886038068, 6.947785072119228467, -2.594798351071639253 ) ) ;
#149716=CARTESIAN_POINT ( 'NONE',  ( 1.504273306027693602, 1.959471947749168663, 0.09963418240711149898 ) ) ;
#149719=CARTESIAN_POINT ( 'NONE',  ( 0.1753634416057497647, 0.0001173177735149660568, -2.144164757042036573 ) ) ;
#149721=CARTESIAN_POINT ( 'NONE',  ( 0.3036855567021545244, -1.598042064648269811, -1.315789336611736138 ) ) ;
#149724=CARTESIAN_POINT ( 'NONE',  ( 3.967288593341521175, -1.508176260789632739, -1.003069782103764185 ) ) ;
#149728=CARTESIAN_POINT ( 'NONE',  ( 4.705596528438695358, 1.345619282010660500, 1.212945642518966416 ) ) ;
#149732=CARTESIAN_POINT ( 'NONE',  ( 6.057066403244290242, 1.520950583283819935, -1.072200347198979831 ) ) ;
#149734=CARTESIAN_POINT ( 'NONE',  ( 3.849167162397474140, 0.2308054593076276639, -1.901561516516042660 ) ) ;
#149737=SHAPE_REPRESENTATION ( 'coil', ( #200407 ), #124915 ) ;
#149742=B_SPLINE_CURVE_WITH_KNOTS ( 'NONE', 3,
 ( #142800, #61505, #178468, #208805, #94037, #193632, #91907, #59373, #95099, #160076, #11678, #143874, #209867, #207747, #127671, #26865, #10608, #78808, #191489, #157964, #92969, #159014, #161147, #77753, #60434, #43158, #126594, #25798, #192555, #111395, #144932, #45274, #109270, #112456, #190427, #175278, #44210, #176335, #110332, #177399, #194699, #12734, #27942, #210938, #46341, #108199, #96169, #174223, #162220, #13807, #79878, #145989, #2868, #132931, #131879, #34323, #150232, #32204, #14864, #18059, #33262, #1803, #181633, #129796, #195775, #182704, #84146, #51666, #148100, #213067, #15927, #50582, #151297, #47414, #99345, #100397, #65732, #196834, #149146, #117789, #85211, #113528, #130841, #116704, #67860, #180583, #726, #183778, #197888, #98280, #165394, #82010, #66792, #35389, #214103, #16990, #198937, #31154, #64696, #166466, #83068, #200015, #49517, #134009, #164339, #167536, #115637, #101465, #19134, #147044, #179535, #97227, #163280, #80953, #48475, #114592, #70002, #37533, #168597, #156639, #172891, #203211, #89511, #73219, #68938, #20197, #86286, #139325, #152357, #71072, #137189, #6076, #54857, #53792, #122079, #103610, #105781, #22320, #136116, #201072, #3932, #189123, #202131, #188041, #135060, #102535, #90579, #7147, #52714, #38607, #88433, #106864, #39670, #87358, #205356, #72146, #171806, #154497, #121008, #138256, #24466, #204268, #56990, #153426, #186975, #55921, #184829, #119923, #23398, #104685, #170734, #155565, #123163, #185898, #40758, #169666, #21251, #118847, #4995, #36459, #125276, #191238, #61257, #127415, #210697, #94846, #126342, #207497, #209615, #8231, #142543, #28762, #12493, #74314, #173972, #107946, #78566, #25546, #10358, #76435, #159822, #208549, #190180, #206429, #11425, #77501, #110077, #58053, #41835, #62327, #128486, #91654, #193387, #140411, #157707, #29837, #160897, #95921, #192302, #143620, #45031, #42901, #111145, #177145, #176089, #9304, #144686, #124218, #75377, #26616, #60183, #43961, #194452, #46097, #27687, #141491, #112213, #59119, #93786, #178222, #109010, #175029, #92717, #158763, #161975, #35133, #165152, #164101, #66544, #182451, #64459, #47169, #50338, #65492, #148904, #34079, #213869, #13565, #79637, #478, #116458, #195530, #131639, #63394, #15684, #199765, #82828, #96988, #196592, #98048, #197642, #145756, #67611, #129548, #16743, #51410, #117530, #81771, #132687, #211756, #48234, #113283, #166212, #179289, #147851, #49287, #99099, #115405, #146805, #198694, #130603, #100148, #181398, #163039, #30913, #14619, #80715, #212823, #114347, #180344, #31965, #183524, #17804, #33022, #83888, #149979, #1550, #133756, #119663, #53529, #170473, #118592, #185649, #137997, #37280, #169415, #200816, #104426, #22059, #20999, #4740, #188862, #55661, #102275, #70815, #87096, #101205, #153166, #103351, #168353, #136930, #6887, #19945, #152106, #202958, #135859, #154240, #54600, #120748, #39416, #204015, #187787, #186722, #167291, #18878, #5812, #121819, #23136, #38349, #184581, #201880, #88170, #122904, #84962, #71888, #105510, #171543, #86032, #89253, #155305, #56736, #139070, #72965, #205095, #151051, #2618, #68689, #134811, #52467, #36200, #3676, #69755, #125023, #26354, #176891, #107688, #190981, #74055, #92470, #142288, #106604, #208299, #59930, #140147, #126085, #91393, #75123 ),
 .UNSPECIFIED., .F., .F.,
 ( 4, 1, 1, 1, 1, 1, 1, 1, 1, 1, 1, 1, 1, 1, 1, 1, 1, 1, 1, 1, 1, 1, 1, 1, 1, 1, 1, 1, 1, 1, 1, 1, 1, 1, 1, 1, 1, 1, 1, 1, 1, 1, 1, 1, 1, 1, 1, 1, 1, 1, 1, 1, 1, 1, 1, 1, 1, 1, 1, 1, 1, 1, 1, 1, 1, 1, 1, 1, 1, 1, 1, 1, 1, 1, 1, 1, 1, 1, 1, 1, 1, 1, 1, 1, 1, 1, 1, 1, 1, 1, 1, 1, 1, 1, 1, 1, 1, 1, 1, 1, 1, 1, 1, 1, 1, 1, 1, 1, 1, 1, 1, 1, 1, 1, 1, 1, 1, 1, 1, 1, 1, 1, 1, 1, 1, 1, 1, 1, 1, 1, 1, 1, 1, 1, 1, 1, 1, 1, 1, 1, 1, 1, 1, 1, 1, 1, 1, 1, 1, 1, 1, 1, 1, 1, 1, 1, 1, 1, 1, 1, 1, 1, 1, 1, 1, 1, 1, 1, 1, 1, 1, 1, 1, 1, 1, 1, 1, 1, 1, 1, 1, 1, 1, 1, 1, 1, 1, 1, 1, 1, 1, 1, 1, 1, 1, 1, 1, 1, 1, 1, 1, 1, 1, 1, 1, 1, 1, 1, 1, 1, 1, 1, 1, 1, 1, 1, 1, 1, 1, 1, 1, 1, 1, 1, 1, 1, 1, 1, 1, 1, 1, 1, 1, 1, 1, 1, 1, 1, 1, 1, 1, 1, 1, 1, 1, 1, 1, 1, 1, 1, 1, 1, 1, 1, 1, 1, 1, 1, 1, 1, 1, 1, 1, 1, 1, 1, 1, 1, 1, 1, 1, 1, 1, 1, 1, 1, 1, 1, 1, 1, 1, 1, 1, 1, 1, 1, 1, 1, 1, 1, 1, 1, 1, 1, 1, 1, 1, 1, 1, 1, 1, 1, 1, 1, 1, 1, 1, 1, 1, 1, 1, 1, 1, 1, 1, 1, 1, 1, 1, 1, 1, 1, 1, 1, 1, 1, 1, 1, 1, 1, 1, 1, 1, 1, 1, 1, 1, 1, 1, 1, 1, 1, 1, 1, 1, 1, 1, 1, 1, 1, 1, 1, 1, 1, 1, 1, 1, 1, 1, 1, 1, 1, 1, 1, 1, 1, 1, 1, 1, 1, 1, 1, 1, 1, 1, 1, 1, 1, 1, 1, 1, 1, 1, 1, 4 ),
 ( 0.000000000000000000, 0.002600034503794030130, 0.005208798665460326327, 0.007813183304800875098, 0.01041632952039499814, 0.01302078637366306003, 0.01562487905948694092, 0.01822913957756216313, 0.02083328395591756144, 0.02343739818322774712, 0.02604168118785421884, 0.02864568517727394958, 0.03125004130332968699, 0.03385401862675675722, 0.03645834363201481965, 0.03906241290072134942, 0.04166661303991354287, 0.04427083116291704451, 0.04687488238457573897, 0.04947921467585455341, 0.05208318889621989245, 0.05468754274347345512, 0.05729155431138267807, 0.05989582568988525285, 0.06249996760622017478, 0.06510408932096034551, 0.06770837349117478365, 0.07031237295078232585, 0.07291672927807971161, 0.07552070761765239393, 0.07812503204114096267, 0.08072910085791458468, 0.08333330089851145872, 0.08593751883178461781, 0.08854156980611090078, 0.09114590188302622298, 0.09374987588873062716, 0.09635422952249227124, 0.09895824087764454324, 0.1015625120427016276, 0.1041666537503683765, 0.1067707752516706410, 0.1093750592157429480, 0.1119790584643299974, 0.1145834145867499904, 0.1171873927198607973, 0.1197917169388799108, 0.1223957855539345302, 0.1249999853896588409, 0.1276042031245507580, 0.1302082538950744550, 0.1328125857752754935, 0.1354165595809520839, 0.1380209130188291833, 0.1406249241787864424, 0.1432291951479887082, 0.1458333366646657747, 0.1484374579699756502, 0.1510417417453218114, 0.1536457408005802994, 0.1562500967354857329, 0.1588540746797905134, 0.1614583987117299280, 0.1640624671426803571, 0.1666666667910262079, 0.1692708843450304312, 0.1718749349293641482, 0.1744792666302357464, 0.1770832402535473249, 0.1796875935129024493, 0.1822916044953091785, 0.1848958752860835608, 0.1875000166293293857, 0.1901041377562054102, 0.1927084213602507368, 0.1953124202398235920, 0.1979167760045740521, 0.2005207537777317084, 0.2031250776399721736, 0.2057291459044250093, 0.2083333453828807025, 0.2109375627734847158, 0.2135416131892344249, 0.2161459447281551538, 0.2187499181867580689, 0.2213542712849473904, 0.2239582821074418695, 0.2265625527372090720, 0.2291666939245756707, 0.2317708148905701926, 0.2343750983407339450, 0.2369790970622578097, 0.2395834526742069426, 0.2421874302938704648, 0.2447917540037867212, 0.2473958221193426621, 0.2500000214453905190, 0.2526042386900758108, 0.2552082889548416555, 0.2578126203491843960, 0.2604165936607292231, 0.2630209466151033904, 0.2656249572953180982, 0.2682292277814931625, 0.2708333688305272213, 0.2734374896531870935, 0.2760417729668830367, 0.2786457715479891406, 0.2812501270244852081, 0.2838541045083020076, 0.2864584280832634389, 0.2890624960675178268, 0.2916666952586349781, 0.2942709123748779576, 0.2968749625062547248, 0.2994792937733871119, 0.3020832669555192918, 0.3046876197834237909, 0.3072916303389863768, 0.3098959006989794318, 0.3125000416272227799, 0.3151041623240899980, 0.3177084455187270673, 0.3203124439770417831, 0.3229167993354283839, 0.3255207767010412923, 0.3281251001584127303, 0.3307291680289564662, 0.3333333671026155187, 0.3359375841078879321, 0.3385416341234662174, 0.3411459652807516951, 0.3437499383511121720, 0.3463542910698884647, 0.3489583015184220538, 0.3515625717696388985, 0.3541667125946290073, 0.3567708331832410984, 0.3593751162762241491, 0.3619791146293697692, 0.3645834698869864221, 0.3671874471520340522, 0.3697917705091763874, 0.3723958382835964032, 0.3750000372572658280, 0.3776042541690359799, 0.3802083040864021046, 0.3828126351512001757, 0.3854166081274262856, 0.3880209607544118922, 0.3906249711135359459, 0.3932292412733790488, 0.3958333820126498370, 0.3984375025105409418, 0.4010417855192715542, 0.4036457837848667074, 0.4062501389590495449, 0.4088541161411674008, 0.4114584394154381930, 0.4140625071113177014, 0.4166667060024629166, 0.4192709228381954478, 0.4218749726749327911, 0.4244793036646000717, 0.4270832765643259310, 0.4296876291168554296, 0.4322916394041865784, 0.4348959094900549660, 0.4375000501611374104, 0.4401041705858387276, 0.4427084535277153732, 0.4453124517233759683, 0.4479168068314584583, 0.4505207839482789911, 0.4531251071570330247, 0.4557291747919532399, 0.4583333736180368323, 0.4609375903951940523, 0.4635416401688834398, 0.4661459711007739370, 0.4687499439416310532, 0.4713542964370365795, 0.4739583066701890113, 0.4765625766994796009, 0.4791667173199026797, 0.4817708376889431876, 0.4843751205813623395, 0.4869791187247021202, 0.4895834737840155659, 0.4921874508531692838, 0.4947917740137594000, 0.4973958416052992049, 0.5000000403837819851, 0.5026042571198243714, 0.5052083068480445194, 0.5078126377395105751, 0.5104166105391289010, 0.5130209629947408700, 0.5156249731913270518, 0.5182292431814352618, 0.5208333837687260104, 0.5234375040996330775, 0.5260417869599895990, 0.5286457850686206994, 0.5312501400964950715, 0.5338541171356111503, 0.5364584402653888029, 0.5390625078311259699, 0.5416667065794673608, 0.5442709232918542250, 0.5468749729921829061, 0.5494793038605755298, 0.5520832766365837418, 0.5546876290697317913, 0.5572916392473630243, 0.5598959092156829964, 0.5625000497873680061, 0.5651041700976676685, 0.5677084529433557014, 0.5703124510348895893, 0.5729168060486536929, 0.5755207830753605869, 0.5781251061916765632, 0.5807291737491879768, 0.5833333724848467350, 0.5859375891910368894, 0.5885416388810509325, 0.5911459697437208005, 0.5937499425137473530, 0.5963542949417601768, 0.5989583051180477069, 0.6015625750819736384, 0.6041667156555785567, 0.6067708359627971282, 0.6093751188112106476, 0.6119791169032582356, 0.6145834719202413199, 0.6171874489521673723, 0.6197917720723722379, 0.6223958396392350600, 0.6250000383796699976, 0.6276042550971219214, 0.6302083047943985994, 0.6328126356686964993, 0.6354166084503697354, 0.6380209608905765828, 0.6406249710831318778, 0.6432292410600577437, 0.6458333816531092175, 0.6484375019747732338, 0.6510417848433065480, 0.6536457829534795261, 0.6562501379910111732, 0.6588541150457848383, 0.6614584381872300467, 0.6640625057810221055, 0.6666667045436925898, 0.6692709212898660942, 0.6718749710119833463, 0.6744793019152608426, 0.6770832747262099938, 0.6796876271959411131, 0.6822916374223763070, 0.6848959074296973037, 0.6875000480597228680, 0.6901041684133596421, 0.6927084513194080584, 0.6953124494653194487, 0.6979168045407300180, 0.7005207816359816375, 0.7031251048160196415, 0.7057291724543196532, 0.7083333712566866058, 0.7109375880490425015, 0.7135416378135795989, 0.7161459687631898108, 0.7187499416210458847, 0.7213542941376326345, 0.7239583044155618596, 0.7265625744706748490, 0.7291667151552034820, 0.7317708355583423252, 0.7343751185193033715, 0.7369791167185673064, 0.7395834718491895998, 0.7421874490025512916, 0.7447917722385364314, 0.7473958399389256657, 0.7500000387984516736, 0.7526042556544531026, 0.7552083054789914263, 0.7578126364922896929, 0.7604166094146853627, 0.7630209619954617661, 0.7656249723425013753, 0.7682292424628052174, 0.7708333832193684509, 0.7734375036895410060, 0.7760417867228139865, 0.7786457849930478181, 0.7812501401962168579, 0.7838541174253229604, 0.7864584407346123518, 0.7890625085146746320, 0.7916667074488250577, 0.7942709243859374935, 0.7968749742880611997, 0.7994793053824050810, 0.8020832783869765725, 0.8046876310492792062, 0.8072916414830481058, 0.8098959116859448804, 0.8125000525320774658, 0.8151041730868179291, 0.8177084562098055898, 0.8203124545686294455, 0.8229168098616829186, 0.8255207871841712119, 0.8281251105841250792, 0.8307291784614470043, 0.8333333774876906519, 0.8359375945233833427, 0.8385416445206798075, 0.8411459757134309712, 0.8437499488178175078, 0.8463543015789862789, 0.8489583121171074831, 0.8515625824200027116, 0.8541667233732427311, 0.8567708440300897399, 0.8593751272601987123, 0.8619791257252362726, 0.8645834811255164176, 0.8671874585590289009, 0.8697917820670107991, 0.8723958500591838527, 0.8750000491949933012, 0.8776042663467393812, 0.8802083164568000884, 0.8828126477653241988, 0.8854166209871692228, 0.8880209738645485906, 0.8906249845246493324, 0.8932292549449527552, 0.8958333960228427317, 0.8984375167993386979, 0.9010418001539796107, 0.9036457987428592187, 0.9062501542677121602, 0.9088541318298947180, 0.9114584554632734203, 0.9140625235878931942, 0.9166667228507454634, 0.9192709401360219523, 0.9218749903764450471, 0.9244793218181143191, 0.9270832951750564987, 0.9296876481859919217, 0.9322916589857459524, 0.9348959295408556525, 0.9375000707608250883, 0.9401041916746273319, 0.9427084751713679101, 0.9453124739016935951, 0.9479168295687272483, 0.9505208072738278169, 0.9531251310501845930, 0.9557291993520028450, 0.9583333987332913750, 0.9609376160454207172, 0.9635416666839513589, 0.9661459986354887786, 0.9687499708159389433, 0.9713543235632202677, 0.9739583390673558494, 0.9765626083347638264, 0.9791667417950460361, 0.9817708662416058107, 0.9843751381318576188, 0.9869792129215403387, 0.9895836736503123010, 0.9921868305638316121, 0.9947912020913856068, 0.9973999845648282569, 1.000000000000000000 ),
 .UNSPECIFIED. ) ;
#149744=CARTESIAN_POINT ( 'NONE',  ( 5.876184115051023227, -2.107333617329323783, -0.2052446207758129582 ) ) ;
#149745=CARTESIAN_POINT ( 'NONE',  ( 0.6554165194554737450, -1.826866057147133349, -1.155366728873077564 ) ) ;
#149748=CARTESIAN_POINT ( 'NONE',  ( 0.8854529848611718545, 1.222500307375608886, 1.355994775097228766 ) ) ;
#149750=CARTESIAN_POINT ( 'NONE',  ( 3.909063277197013520, 1.565549990038747952, 0.9388121169797561949 ) ) ;
#149752=CARTESIAN_POINT ( 'NONE',  ( 1.793074957647671663, -0.09724762972821224261, -1.910064080951429100 ) ) ;
#149754=CARTESIAN_POINT ( 'NONE',  ( 3.086336304319175383, 1.096367280595906601, -1.635968976963786847 ) ) ;
#149755=CARTESIAN_POINT ( 'NONE',  ( 4.335450565170337001, 0.8274041267214229389, -1.757107282799404091 ) ) ;
#149758=CARTESIAN_POINT ( 'NONE',  ( 4.676102344489991403, 2.097148071331572439, -0.3138259731317455392 ) ) ;
#149760=CARTESIAN_POINT ( 'NONE',  ( 3.000541214264150547, -1.884352459892328024, -0.3246530749497905655 ) ) ;
#149767=CARTESIAN_POINT ( 'NONE',  ( 4.494645072041675071, -0.4025399330690944133, -1.780595394402582077 ) ) ;
#149768=CARTESIAN_POINT ( 'NONE',  ( 6.175017591530616023, 1.752142144017948100, -0.9981200475188132248 ) ) ;
#149773=CARTESIAN_POINT ( 'NONE',  ( 6.034044788248046132, 0.9204803733943857091, -1.628451883209979689 ) ) ;
#149783=CARTESIAN_POINT ( 'NONE',  ( 0.2392000317489213768, -0.1454578200970526591, -2.037356452166842580 ) ) ;
#149784=CARTESIAN_POINT ( 'NONE',  ( 1.124788838837559535, 0.4171406989393853793, 2.075574515046583191 ) ) ;
#149787=CARTESIAN_POINT ( 'NONE',  ( 5.735237735067806319, -0.04509738862551111033, -2.069921269439451539 ) ) ;
#149788=CARTESIAN_POINT ( 'NONE',  ( 2.102840161960460197, -0.4018910908503615653, 1.796694178532439956 ) ) ;
#149793=CARTESIAN_POINT ( 'NONE',  ( 1.271856881794002136, 1.368814058113819732, 1.838566387026792093 ) ) ;
#149796=CARTESIAN_POINT ( 'NONE',  ( 2.232540727315056373, 1.246330492051262784, -1.450604739030990187 ) ) ;
#149800=CARTESIAN_POINT ( 'NONE',  ( 1.037359019205979171, -0.04529029187893931357, 2.012842730658084278 ) ) ;
#149801=CARTESIAN_POINT ( 'NONE',  ( 0.6550357524967264089, 1.634203043994170157, -1.084997510809107446 ) ) ;
#149806=CARTESIAN_POINT ( 'NONE',  ( 4.294928614669782263, 1.678954898789623673, 1.245530301124315953 ) ) ;
#149807=CARTESIAN_POINT ( 'NONE',  ( 2.553260254243350680, 0.4745879851475919842, -1.704939281604215706 ) ) ;
#149810=CARTESIAN_POINT ( 'NONE',  ( 5.753944192167276483, 0.9242165444633635429, 2.097870995526931015 ) ) ;
#149811=CARTESIAN_POINT ( 'NONE',  ( 2.888294976258547475, 1.492474662269949182, -0.8948698564717886272 ) ) ;
#149815=CARTESIAN_POINT ( 'NONE',  ( 3.268574299048069953, -1.732005324549376279, 0.08218708453346619536 ) ) ;
#149817=CARTESIAN_POINT ( 'NONE',  ( 3.156845524303863559, -0.6275973837717390147, -2.078511276010074127 ) ) ;
#149819=CARTESIAN_POINT ( 'NONE',  ( 5.612517632836664383, 1.944729323200470095, 0.5331731267440716904 ) ) ;
#149820=CARTESIAN_POINT ( 'NONE',  ( 0.6562500000000004441, -1.895863743164078130, 0.7852924748300215141 ) ) ;
#149823=CARTESIAN_POINT ( 'NONE',  ( 2.116120358982703120, -0.9062717621706478655, -1.699889088518308222 ) ) ;
#149825=CARTESIAN_POINT ( 'NONE',  ( 5.871364357536254630, -1.904906058150414472, -1.142540087918672898 ) ) ;
#149827=CARTESIAN_POINT ( 'NONE',  ( -0.1106856583841086261, 2.025759259886884323, -2.413105898545636840 ) ) ;
#149832=CARTESIAN_POINT ( 'NONE',  ( 1.664984172775041182, 0.7006824767318786673, 2.107951039278654015 ) ) ;
#149837=CARTESIAN_POINT ( 'NONE',  ( 0.2632415847364302786, -1.930764589519979424, -0.9721467891136772455 ) ) ;
#149840=CARTESIAN_POINT ( 'NONE',  ( 4.615719743604500103, 0.4549637584481819319, -2.011722621177906678 ) ) ;
#149844=CARTESIAN_POINT ( 'NONE',  ( 5.448468942325162878, 0.5420331153751513087, 1.790312535500695024 ) ) ;
#149846=CARTESIAN_POINT ( 'NONE',  ( 4.975145882941295561, -1.721944285756441984, -0.2046304421847028043 ) ) ;
#149847=CARTESIAN_POINT ( 'NONE',  ( 4.335344899790516848, 0.7389749068974335033, -1.575905762629246309 ) ) ;
#149849=CARTESIAN_POINT ( 'NONE',  ( 2.050677904428706455, -1.769283327057631805, 1.457584778241685974 ) ) ;
#149851=CARTESIAN_POINT ( 'NONE',  ( 5.864805775728457071, 0.1527762835577218814, -2.085202849681159876 ) ) ;
#149852=CARTESIAN_POINT ( 'NONE',  ( 0.4625323210639306071, 0.1833022542275381250, -1.831979997761295165 ) ) ;
#149855=CARTESIAN_POINT ( 'NONE',  ( 1.213517774399593740, 1.944071949784083264, 0.5350861613380719639 ) ) ;
#149861=CARTESIAN_POINT ( 'NONE',  ( 4.002672028760116518, -2.097606743168555443, -0.3097674545872728946 ) ) ;
#149863=CARTESIAN_POINT ( 'NONE',  ( 5.443921307256319508, 0.7362202147598860824, -1.670853202368662860 ) ) ;
#149869=CARTESIAN_POINT ( 'NONE',  ( 2.988540512386147707, -1.199814222051265311, 1.624667845120256748 ) ) ;
#149870=CARTESIAN_POINT ( 'NONE',  ( 0.1828346100962909559, -2.042824957133956953, -0.5113311198858895290 ) ) ;
#149872=CARTESIAN_POINT ( 'NONE',  ( 3.924516644892431572, -1.252765583397809079, 1.376256255023865283 ) ) ;
#149879=CARTESIAN_POINT ( 'NONE',  ( 6.368051766976638994, 1.057089778920755840, 1.768976859881221442 ) ) ;
#149884=CARTESIAN_POINT ( 'NONE',  ( 1.141452232654313059, -0.03515412242651934360, -1.733669386235114906 ) ) ;
#149885=CARTESIAN_POINT ( 'NONE',  ( 1.728031430807571267, 0.1683455491279534644, 1.732166925338991303 ) ) ;
#149886=CARTESIAN_POINT ( 'NONE',  ( 6.182281242350501138, -1.240197753460486663, 1.945954285860839850 ) ) ;
#149889=CARTESIAN_POINT ( 'NONE',  ( 1.388040899126226302, -0.9290452130323262336, 1.839580399304826752 ) ) ;
#149890=CARTESIAN_POINT ( 'NONE',  ( 6.608760977740426590, 0.8891218545476579083, -2.119637956729656381 ) ) ;
#149893=CARTESIAN_POINT ( 'NONE',  ( 6.297708355432167338, -0.6282832542035889922, 1.762108908958268216 ) ) ;
#149894=CARTESIAN_POINT ( 'NONE',  ( 4.394721148579957770, -1.856311205515799312, -0.4593126252911489127 ) ) ;
#149896=CARTESIAN_POINT ( 'NONE',  ( 6.322910218073367616, 2.057572540570989261, 0.7984293639632376038 ) ) ;
#149900=CARTESIAN_POINT ( 'NONE',  ( 0.08268334464456467137, -1.317614589208983444, 1.530782303595918714 ) ) ;
#149902=CARTESIAN_POINT ( 'NONE',  ( 3.346982425237558179, 0.5585957852003355928, 2.238849765380794832 ) ) ;
#149903=CARTESIAN_POINT ( 'NONE',  ( 5.213317179658601752, -1.656387821537348426, -1.051046178410528942 ) ) ;
#149904=CARTESIAN_POINT ( 'NONE',  ( 2.254674508890702089, -0.5182927192734412269, -1.892014123021222627 ) ) ;
#149908=CARTESIAN_POINT ( 'NONE',  ( -0.1001773172763717329, -2.075113514603315945, 0.4199855073994100407 ) ) ;
#149911=CARTESIAN_POINT ( 'NONE',  ( -0.02900071798685524560, -0.004641455105012376459, -2.173770343569726649 ) ) ;
#149912=CARTESIAN_POINT ( 'NONE',  ( 3.942362285364631624, -1.074967207919340861, 1.886227828529878803 ) ) ;
#149914=CARTESIAN_POINT ( 'NONE',  ( 1.898838059644195386, -2.080654286433290867, -0.4088066060855889972 ) ) ;
#149919=CARTESIAN_POINT ( 'NONE',  ( 1.968112693492467979, 1.056634718301739717, 1.769108711375965148 ) ) ;
#149922=CARTESIAN_POINT ( 'NONE',  ( -0.02264175331117417728, 6.946776101658422853, -2.684156320254589279 ) ) ;
#149925=CARTESIAN_POINT ( 'NONE',  ( 4.582611755193141789, -1.246403352314252810, 1.450376384258989182 ) ) ;
#149927=CARTESIAN_POINT ( 'NONE',  ( 1.071959817704574602, 2.180298862187507680, -0.6038346756046736319 ) ) ;
#149929=CARTESIAN_POINT ( 'NONE',  ( 1.300706311995255771, -0.2675212335121620599, -1.791602419159578519 ) ) ;
#149930=CARTESIAN_POINT ( 'NONE',  ( 2.501083532561697798, -0.1830384092258540707, 1.906917772027187929 ) ) ;
#149931=CARTESIAN_POINT ( 'NONE',  ( 2.857943571468853250, -0.6518772230660694333, 1.965110387975615991 ) ) ;
#149933=CARTESIAN_POINT ( 'NONE',  ( 0.4792893823705188794, 1.840408107720743924, -0.7072656782263522235 ) ) ;
#149934=CARTESIAN_POINT ( 'NONE',  ( 5.619733630554700099, -1.879067156935828820, 0.4242066570522682878 ) ) ;
#149935=CARTESIAN_POINT ( 'NONE',  ( -0.01646294620048001714, -0.1635519927996042511, -2.271437254364586877 ) ) ;
#149938=CARTESIAN_POINT ( 'NONE',  ( 4.826661651916083429, -1.349687995210807401, 1.559865583710306147 ) ) ;
#149943=CARTESIAN_POINT ( 'NONE',  ( 4.770599357992978184, -1.377743202910805875, 1.592837501749831519 ) ) ;
#149945=CARTESIAN_POINT ( 'NONE',  ( 1.100314673101766338, 0.8801652113111978482, -1.984954624234806175 ) ) ;
#149948=CARTESIAN_POINT ( 'NONE',  ( 5.360679719606757487, -1.569739296358707570, 1.486333574453831519 ) ) ;
#149949=CARTESIAN_POINT ( 'NONE',  ( 5.549475203002828927, -1.825015992387307273, 0.8654263401719575199 ) ) ;
#149950=CARTESIAN_POINT ( 'NONE',  ( -0.1399997263889611598, 6.947783040739049731, -2.595329734540325006 ) ) ;
#149956=CARTESIAN_POINT ( 'NONE',  ( 3.837125247982266174, -1.679222704393277921, -1.116210984008485507 ) ) ;
#149961=CARTESIAN_POINT ( 'NONE',  ( 4.856408821558930278, 0.8241108818672329139, 1.998647875481096126 ) ) ;
#149966=CARTESIAN_POINT ( 'NONE',  ( 5.202749988929913805, 1.864175517894875789, 0.7691070904374335271 ) ) ;
#149968=CARTESIAN_POINT ( 'NONE',  ( 0.09967489844521590370, -1.724374414367945141, -0.04833993824084405894 ) ) ;
#149972=CARTESIAN_POINT ( 'NONE',  ( 5.940666398231567058, 0.3644617591120716260, 1.834516074763043347 ) ) ;
#149973=CARTESIAN_POINT ( 'NONE',  ( 5.871345457035325843, -1.728819661934883678, -1.031334786431532313 ) ) ;
#149974=CARTESIAN_POINT ( 'NONE',  ( 6.539320575229228716, 1.281788455817688188, 2.013036689384885225 ) ) ;
#149978=CARTESIAN_POINT ( 'NONE',  ( 2.543736517606724146, -1.977637755382474438, 0.7655657148115800892 ) ) ;
#149979=CARTESIAN_POINT ( 'NONE',  ( 1.265250157614560056, 1.862010354082011876, -0.7743342583275417690 ) ) ;
#149980=CARTESIAN_POINT ( 'NONE',  ( 2.583996913715621790, 0.9723193252555061283, 1.528341728153536305 ) ) ;
#149982=CARTESIAN_POINT ( 'NONE',  ( 6.631704542599726082, -1.407888343591977121, -1.640466528430361670 ) ) ;
#149985=CARTESIAN_POINT ( 'NONE',  ( 0.05764063133973944958, 1.105241252117078909, 1.564514492536345891 ) ) ;
#149993=CARTESIAN_POINT ( 'NONE',  ( 3.836934241894359054, 0.3148432204054998351, 2.138525872868973998 ) ) ;
#149996=CARTESIAN_POINT ( 'NONE',  ( 2.285534418239892229, 0.09939759515392716793, -2.118372479656557061 ) ) ;
#149997=CARTESIAN_POINT ( 'NONE',  ( 6.633835642106551411, -1.195214757176918496, -1.380038946949893486 ) ) ;
#149998=( BOUNDED_CURVE ( )  B_SPLINE_CURVE ( 3, ( #92766, #175077, #77549, #163088 ),
 .UNSPECIFIED., .F., .T. ) 
 B_SPLINE_CURVE_WITH_KNOTS ( ( 4, 4 ),
 ( 0.000000000000000000, 0.5000000000000017764 ),
 .UNSPECIFIED. ) 
 CURVE ( )  GEOMETRIC_REPRESENTATION_ITEM ( )  RATIONAL_B_SPLINE_CURVE ( ( 1.000000000000000000, 0.3333333333333309834, 0.3333333333333333703, 1.000000000000002442 ) ) 
 REPRESENTATION_ITEM ( '' )  );
#149999=CARTESIAN_POINT ( 'NONE',  ( 3.251204012874517879, -1.609649185575717123, -1.137836448096725794 ) ) ;
#150000=CARTESIAN_POINT ( 'NONE',  ( 5.818603510220927255, -0.6945032022064903110, -1.782003016414166474 ) ) ;
#150003=CARTESIAN_POINT ( 'NONE',  ( 5.529738209476210642, 1.898601866877418942, -0.5236614360015124925 ) ) ;
#150004=CARTESIAN_POINT ( 'NONE',  ( 1.447104159573095572, 0.5638456037007446575, -1.858296221435972617 ) ) ;
#150012=CARTESIAN_POINT ( 'NONE',  ( 6.569012486276131213, -1.474873517498687558, 1.216900358440069052 ) ) ;
#150014=CARTESIAN_POINT ( 'NONE',  ( 3.528125218122651230, -1.314342534882004809, -1.772652456903674567 ) ) ;
#150015=CARTESIAN_POINT ( 'NONE',  ( 1.835297179245497068, 0.2165863673247066801, 2.196102686035047213 ) ) ;
#150017=CARTESIAN_POINT ( 'NONE',  ( 0.4867802866235851345, -1.800715477623024086, -0.6440170976053718466 ) ) ;
#150020=CARTESIAN_POINT ( 'NONE',  ( 3.455589482447297911, 1.630370400113917873, 1.275915752658785873 ) ) ;
#150025=CARTESIAN_POINT ( 'NONE',  ( 1.446389902895691693, 2.159248346720197276, 0.1057134262518744372 ) ) ;
#150026=CARTESIAN_POINT ( 'NONE',  ( 3.404031855413204966, -0.8899279105200922357, -2.002928011436304612 ) ) ;
#150033=CARTESIAN_POINT ( 'NONE',  ( 6.328739007766592373, 0.6541968508507016722, -1.606262126034884608 ) ) ;
#150035=CARTESIAN_POINT ( 'NONE',  ( 3.907136544319700810, -1.695332804699274387, 1.187946514627869821 ) ) ;
#150036=CARTESIAN_POINT ( 'NONE',  ( 5.765271170472290763, 1.955999355395316996, -0.8108409051663100220 ) ) ;
#150039=CARTESIAN_POINT ( 'NONE',  ( 2.834760172256750810, -1.883157219239324887, -0.5764521555583942414 ) ) ;
#150040=CARTESIAN_POINT ( 'NONE',  ( 1.406358598101828283, -1.903450966454448334, -0.1843715739238485363 ) ) ;
#150041=CARTESIAN_POINT ( 'NONE',  ( 6.210887435761151210, -0.2868632742878024500, 2.274177813689901573 ) ) ;
#150042=CARTESIAN_POINT ( 'NONE',  ( 3.369579884941567016, 1.780956498284639533, -0.4009276245297774266 ) ) ;
#150048=CARTESIAN_POINT ( 'NONE',  ( 3.551042609437846220, 0.2996916850201857829, 1.990680017358969600 ) ) ;
#150049=CARTESIAN_POINT ( 'NONE',  ( 4.117980938109369937, 1.947433809354440326, -0.2358448244534834815 ) ) ;
#150052=CARTESIAN_POINT ( 'NONE',  ( 0.1753634416057497925, 7.629137130509101361, -2.744001747789548418 ) ) ;
#150053=CARTESIAN_POINT ( 'NONE',  ( 0.3981334665579424059, -0.7082897861981848342, -1.967241634975321452 ) ) ;
#150054=CARTESIAN_POINT ( 'NONE',  ( 5.242920984569427567, -1.516648554753729616, 0.9119251698698880304 ) ) ;
#150056=CARTESIAN_POINT ( 'NONE',  ( 1.746283639092637729, 0.6896231194409886411, 2.080178558289603963 ) ) ;
#150057=CARTESIAN_POINT ( 'NONE',  ( 0.08108764725259924588, -0.8233000410203991093, 1.533359828670758374 ) ) ;
#150059=CARTESIAN_POINT ( 'NONE',  ( 0.2335667940003049725, 0.6933325534057503958, -2.235178663643789143 ) ) ;
#150060=CARTESIAN_POINT ( 'NONE',  ( 0.2754634098539961440, 0.9884889332615778290, 1.413329177942000303 ) ) ;
#150061=CARTESIAN_POINT ( 'NONE',  ( 0.9138903340461038693, 0.6688396875448484602, 2.198942881657910853 ) ) ;
#150062=CARTESIAN_POINT ( 'NONE',  ( 0.8025787753177977546, 1.655945718051672566, -1.435626523826734280 ) ) ;
#150063=CARTESIAN_POINT ( 'NONE',  ( 6.151638658550825589, -0.2577636348817541334, -1.714396880517143451 ) ) ;
#150064=CARTESIAN_POINT ( 'NONE',  ( 2.719571217284349363, -0.2154062111461417517, 2.196339928330424129 ) ) ;
#150065=CARTESIAN_POINT ( 'NONE',  ( 0.6378409936122396706, 2.026330576540099404, -0.7799181171992456418 ) ) ;
#150067=CARTESIAN_POINT ( 'NONE',  ( 1.798220840057991543, -1.003180963283013982, -1.864648404631663148 ) ) ;
#150068=CARTESIAN_POINT ( 'NONE',  ( 6.727182134110234024, 7.051482179251418181, 2.887205776801844426 ) ) ;
#150069=CARTESIAN_POINT ( 'NONE',  ( 5.315425438393720725, -0.2827910679824903184, 1.905415604636887750 ) ) ;
#150071=CARTESIAN_POINT ( 'NONE',  ( 2.296762559223310074, 1.838876890742843884, -1.368561501106011713 ) ) ;
#150075=CARTESIAN_POINT ( 'NONE',  ( 4.459788417035775332, -1.717034742021033455, -1.409269467666877995 ) ) ;
#150084=CARTESIAN_POINT ( 'NONE',  ( 3.410779880581996437, -1.203353552534730309, -1.617818353255597863 ) ) ;
#150086=CARTESIAN_POINT ( 'NONE',  ( 0.5673240888519160974, 1.792687530798135143, 1.019967006830464706 ) ) ;
#150092=CARTESIAN_POINT ( 'NONE',  ( 4.347736757272718577, 2.190986304709115373, -0.05254992341368477232 ) ) ;
#150093=CARTESIAN_POINT ( 'NONE',  ( 1.248672897702383988, 1.986100274556975354, -0.3474695496914689818 ) ) ;
#150094=CARTESIAN_POINT ( 'NONE',  ( 0.6965153189463432204, 1.505040478001760107, 1.060415605250275339 ) ) ;
#150095=CARTESIAN_POINT ( 'NONE',  ( 5.056304237002312796, -1.661761009075436002, 1.579303468685322009 ) ) ;
#150096=CARTESIAN_POINT ( 'NONE',  ( 3.978315823851843014, -0.1823813840945518738, -1.832081410093854501 ) ) ;
#150099=CARTESIAN_POINT ( 'NONE',  ( 3.926616521958687045, 1.733384925006593136, 0.5729815612169064654 ) ) ;
#150100=CARTESIAN_POINT ( 'NONE',  ( 4.676407821165474488, 1.496050514612049742, 1.352155788975975437 ) ) ;
#150102=CARTESIAN_POINT ( 'NONE',  ( 4.803764043965432329, -0.6079002506334645339, 2.179255796609281148 ) ) ;
#150104=CARTESIAN_POINT ( 'NONE',  ( 6.686557493494803772, -2.064527365108769885, -0.4147649638114383475 ) ) ;
#150106=CARTESIAN_POINT ( 'NONE',  ( 4.791501694037465953, -1.894250426384593844, 0.8359921707915063394 ) ) ;
#150111=CARTESIAN_POINT ( 'NONE',  ( 2.244641533702110614, 0.4219287677580378926, 1.879577339372063838 ) ) ;
#150113=CARTESIAN_POINT ( 'NONE',  ( 6.491062224718945117, 0.1893930596480186412, 1.960278089617428554 ) ) ;
#150117=CARTESIAN_POINT ( 'NONE',  ( 0.3168469074051638024, -0.7203255543706194031, -1.994627023381766673 ) ) ;
#150118=CARTESIAN_POINT ( 'NONE',  ( 2.180208177693909288, 2.177553952664741388, -0.4384792121874846460 ) ) ;
#150119=CARTESIAN_POINT ( 'NONE',  ( 3.768672590584824178, -1.415924365303207644, 1.559078948506262385 ) ) ;
#150122=CARTESIAN_POINT ( 'NONE',  ( 0.3790724793553065797, -0.09720884262147008736, 1.858658634516747510 ) ) ;
#150128=CARTESIAN_POINT ( 'NONE',  ( 0.9496594531581278309, -1.914679731917130479, 0.9119059213342151082 ) ) ;
#150131=CARTESIAN_POINT ( 'NONE',  ( 4.738696794244872557, -1.902450960283699199, -0.4786090228221794307 ) ) ;
#150132=CARTESIAN_POINT ( 'NONE',  ( 3.397504326804317909, 1.702965868850464082, 1.331369057855802174 ) ) ;
#150133=CARTESIAN_POINT ( 'NONE',  ( 1.540310226958538475, -1.555040833713853710, 0.9856339240054690087 ) ) ;
#150137=CARTESIAN_POINT ( 'NONE',  ( 4.505614311517684101, -0.7474637548481823934, -1.571778613660354207 ) ) ;
#150141=CARTESIAN_POINT ( 'NONE',  ( 1.551884642779034262, 0.6273040060550126862, -2.068667048528524344 ) ) ;
#150142=CARTESIAN_POINT ( 'NONE',  ( 3.638045922354939954, 0.05228986736816390590, -2.015604357568132166 ) ) ;
#150144=CARTESIAN_POINT ( 'NONE',  ( 1.323354039402934390, -0.05256100377049736927, 2.161234000603563299 ) ) ;
#150145=CARTESIAN_POINT ( 'NONE',  ( 3.959811223838666905, 1.956698650606549350, -0.2402693447622703815 ) ) ;
#150148=CARTESIAN_POINT ( 'NONE',  ( 6.509000000000051855, 1.248119779622055336, 2.213941609938009591 ) ) ;
#150149=CARTESIAN_POINT ( 'NONE',  ( 3.140110198738320424, 0.4743784485543530716, 1.883105278476588706 ) ) ;
#150160=CARTESIAN_POINT ( 'NONE',  ( 6.317414003067519879, -0.2912348092876380079, 2.289091032272353221 ) ) ;
#150162=CARTESIAN_POINT ( 'NONE',  ( 5.418788444413384475, -1.423528547644649755, 1.350099487149841071 ) ) ;
#150163=CARTESIAN_POINT ( 'NONE',  ( 1.494767762416523871, -2.000856930885573259, 0.2496086726550551527 ) ) ;
#150165=CARTESIAN_POINT ( 'NONE',  ( 3.485668972010677269, -0.6104075878305641467, 2.027481811383638810 ) ) ;
#150169=CARTESIAN_POINT ( 'NONE',  ( 3.978315823851843014, -0.1823813840945518738, -1.832081410093854501 ) ) ;
#150170=ORIENTED_EDGE ( 'NONE', *, *, #60919, .T. ) ;
#150174=CARTESIAN_POINT ( 'NONE',  ( 5.449516625918088053, -1.916229881892789866, 0.9086369058012438993 ) ) ;
#150177=CARTESIAN_POINT ( 'NONE',  ( 5.905559377550752664, -0.5051061836833131702, 1.997775138168448761 ) ) ;
#150179=CARTESIAN_POINT ( 'NONE',  ( 1.011883965753940018, 1.859189825682316277, -0.08597224477241424689 ) ) ;
#150180=CARTESIAN_POINT ( 'NONE',  ( 2.261056740009634414, 1.805359621025553363, -0.3608742708730780513 ) ) ;
#150185=CARTESIAN_POINT ( 'NONE',  ( 1.928631425534212074, 1.268998755960360603, -1.805353087401928569 ) ) ;
#150186=CARTESIAN_POINT ( 'NONE',  ( 5.097078980560620920, 1.884938936817718069, -1.250935519564094767 ) ) ;
#150188=CARTESIAN_POINT ( 'NONE',  ( 5.150580392983738598, 1.786086171955153068, 0.3018458199737662495 ) ) ;
#150189=CARTESIAN_POINT ( 'NONE',  ( 5.331221607142452967, -1.514317160175217447, -1.173313937468897672 ) ) ;
#150191=CARTESIAN_POINT ( 'NONE',  ( 4.346526858336821952, 0.5246154692373095063, 1.900329053005628044 ) ) ;
#150192=CARTESIAN_POINT ( 'NONE',  ( 5.594569530875262764, -0.4557361262383100020, -1.814172972432124720 ) ) ;
#150193=CARTESIAN_POINT ( 'NONE',  ( 5.037489322368606359, 1.736649509538616964, -0.6695082933049227858 ) ) ;
#150195=CARTESIAN_POINT ( 'NONE',  ( 5.032005376881601322, 0.9078957314892305286, -1.519088338465144128 ) ) ;
#150198=CARTESIAN_POINT ( 'NONE',  ( 2.139418596640904280, -1.880839966478216052, 0.9477614987608102837 ) ) ;
#150202=CARTESIAN_POINT ( 'NONE',  ( 3.603867943843573673, 1.538443694073919898, 1.459757404076333698 ) ) ;
#150203=CARTESIAN_POINT ( 'NONE',  ( 1.933859055862125809, -1.958050917679872160, 0.4949566823095867263 ) ) ;
#150205=CARTESIAN_POINT ( 'NONE',  ( 6.720655732516688019, 6.039915720534646759, 2.321169117395345705 ) ) ;
#150208=CARTESIAN_POINT ( 'NONE',  ( 2.319794969891198821, -2.097318901067245722, 0.5227781780692899449 ) ) ;
#150216=CARTESIAN_POINT ( 'NONE',  ( 0.9783777488623355278, -2.139296967303818686, -0.4750931833387496694 ) ) ;
#150218=CARTESIAN_POINT ( 'NONE',  ( 1.850798253084064537, 0.7104643512030085484, 2.148151574381700790 ) ) ;
#150222=CARTESIAN_POINT ( 'NONE',  ( 4.434779938697545276, -1.616694733667634942, 1.205040202231235869 ) ) ;
#150228=CARTESIAN_POINT ( 'NONE',  ( 3.180641231044952555, -0.1265111898236283006, -1.765250312072360162 ) ) ;
#150229=CARTESIAN_POINT ( 'NONE',  ( 6.510767885691055135, 1.639592601025055885, -1.477219212978691409 ) ) ;
#150232=CARTESIAN_POINT ( 'NONE',  ( 5.642203898613793456, 0.8197873783117490820, 1.842442240159094080 ) ) ;
#150233=ORIENTED_EDGE ( 'NONE', *, *, #191848, .F. ) ;
#150234=CARTESIAN_POINT ( 'NONE',  ( 2.922558825391399662, 1.760836971185793187, 0.6318509464167121337 ) ) ;
#150236=CARTESIAN_POINT ( 'NONE',  ( 2.237250781069185734, -0.09733102107959035187, -2.068066387140480522 ) ) ;
#150239=CARTESIAN_POINT ( 'NONE',  ( 1.968876373762207255, -1.476028252698018628, 1.215921256797661609 ) ) ;
#150245=CARTESIAN_POINT ( 'NONE',  ( 0.6328886395040033142, 1.767934563615305654, 0.7296191750566642931 ) ) ;
#150247=CARTESIAN_POINT ( 'NONE',  ( 1.697631272820496307, -1.418720726069604865, -1.355276769646639901 ) ) ;
#150249=CARTESIAN_POINT ( 'NONE',  ( 0.2454708137151571101, -1.954895187565863779, -0.4925657318226167591 ) ) ;
#150251=CARTESIAN_POINT ( 'NONE',  ( 4.957343421279005291, -1.817532610912236724, 1.092287347377165707 ) ) ;
#150254=CARTESIAN_POINT ( 'NONE',  ( 6.204366038997092936, -0.7071694579776456324, -1.840334891991159738 ) ) ;
#150256=CARTESIAN_POINT ( 'NONE',  ( 1.476815932985692026, -1.420704281710112316, 1.426639689446000281 ) ) ;
#150259=CARTESIAN_POINT ( 'NONE',  ( 1.406030203601447592, -1.179493747730875342, -1.758069577626440116 ) ) ;
#150261=CARTESIAN_POINT ( 'NONE',  ( 2.822784111170244525, -1.429543836668966561, 1.497820115680066344 ) ) ;
#150265=CARTESIAN_POINT ( 'NONE',  ( 4.294928614669782263, 1.678954898789623673, 1.245530301124315953 ) ) ;
#150267=CARTESIAN_POINT ( 'NONE',  ( 3.891465932158610030, 1.322013910284997262, 1.259209046625270556 ) ) ;
#150268=CARTESIAN_POINT ( 'NONE',  ( 2.420317109208899531, -0.6946167411978272366, -1.673203699974361580 ) ) ;
#150270=CARTESIAN_POINT ( 'NONE',  ( 6.410767893487317792, 1.638320036227768783, -1.478771730184471611 ) ) ;
#150272=CARTESIAN_POINT ( 'NONE',  ( 5.368293279414073638, 1.083412401764087374, 1.922438065789177308 ) ) ;
#150274=CARTESIAN_POINT ( 'NONE',  ( 4.195896582043898704, 1.251535281948525036, 1.445917311372606262 ) ) ;
#150286=CARTESIAN_POINT ( 'NONE',  ( 3.919104170388473030, -0.1403237101727794756, 1.865361397874479632 ) ) ;
#150292=CARTESIAN_POINT ( 'NONE',  ( 0.4089589639980686919, -1.585120765669449261, 1.168626392425928584 ) ) ;
#150293=CARTESIAN_POINT ( 'NONE',  ( 2.776970437579088014, 1.727991955821889025, -1.039012595151635354 ) ) ;
#150297=CARTESIAN_POINT ( 'NONE',  ( 2.642740014504705748, -1.821389600533462216, 1.218302608185666491 ) ) ;
#150298=CARTESIAN_POINT ( 'NONE',  ( 6.147073579019600054, -1.539581890156189292, 0.9809480439507823890 ) ) ;
#150306=CARTESIAN_POINT ( 'NONE',  ( 3.983814121021773680, -1.821778379405362136, -0.2661574599523569007 ) ) ;
#150307=CARTESIAN_POINT ( 'NONE',  ( 0.2584475630193752149, 2.007833436562710183, 0.1460894178599257687 ) ) ;
#150308=CARTESIAN_POINT ( 'NONE',  ( 3.005512134316370432, 2.280722703800378337, 0.2841129622813722277 ) ) ;
#150310=CARTESIAN_POINT ( 'NONE',  ( 0.8833916088089890373, -1.769421289247067097, 0.5767519331581376640 ) ) ;
#150314=CARTESIAN_POINT ( 'NONE',  ( 4.570513122935188299, 0.7371126809179430195, 1.764830652192488580 ) ) ;
#150318=CARTESIAN_POINT ( 'NONE',  ( 3.737900851971903915, 2.080878125540788215, 0.2026709130291924343 ) ) ;
#150319=CARTESIAN_POINT ( 'NONE',  ( 2.289737743334671283, -0.8020533187339595749, 1.690132462187944107 ) ) ;
#150322=CARTESIAN_POINT ( 'NONE',  ( 5.425302022954732628, -1.172690680311109901, -1.419496581506813904 ) ) ;
#150325=CARTESIAN_POINT ( 'NONE',  ( 4.213312296666638979, -0.2916954692788272796, 1.699858598931931919 ) ) ;
#150327=CARTESIAN_POINT ( 'NONE',  ( 6.568967528192747096, -2.015767819289843388, -0.8987472251835016968 ) ) ;
#150328=CARTESIAN_POINT ( 'NONE',  ( 6.983263157960370116, 1.251666756963093041, 2.167287073222202931 ) ) ;
#150330=CARTESIAN_POINT ( 'NONE',  ( 5.155217109558853039, 1.808899791667990753, -1.200326510068568497 ) ) ;
#150331=CARTESIAN_POINT ( 'NONE',  ( 2.807047293222181494, 1.542382716246639474, 0.9765254425028799812 ) ) ;
#150333=CARTESIAN_POINT ( 'NONE',  ( 6.122275928298587466, 2.094602363090028785, 0.3085360351358697462 ) ) ;
#150335=CARTESIAN_POINT ( 'NONE',  ( 6.075753635015332499, -1.229876075327457130, 1.934346496684937966 ) ) ;
#150338=CARTESIAN_POINT ( 'NONE',  ( 1.119968162728638417, -0.5116716972351254000, 2.057716464106795318 ) ) ;
#150342=CARTESIAN_POINT ( 'NONE',  ( 6.262575984712966282, -0.7736541179628317888, -2.028742479192620518 ) ) ;
#150345=CARTESIAN_POINT ( 'NONE',  ( 1.489269531296941507, -2.110695925841240772, -0.6924467157797905559 ) ) ;
#150347=CARTESIAN_POINT ( 'NONE',  ( 5.942029771888944545, -1.730864577151491890, -1.034168155301495862 ) ) ;
#150349=CARTESIAN_POINT ( 'NONE',  ( 4.030177592043080459, 1.141696479982070578, 1.717582018908659025 ) ) ;
#150355=CARTESIAN_POINT ( 'NONE',  ( 0.3575176574102476579, 2.067590324638542310, -0.3087094068163088179 ) ) ;
#150356=CARTESIAN_POINT ( 'NONE',  ( 4.483046177357690176, -2.016033783801042034, -0.04667830911464498911 ) ) ;
#150357=CARTESIAN_POINT ( 'NONE',  ( 4.669393045487420402, 1.064170941109745305, 1.502380130741477693 ) ) ;
#150360=CARTESIAN_POINT ( 'NONE',  ( 0.9028307623185973796, 1.406233313734496448, 0.9983791803314099322 ) ) ;
#150362=CARTESIAN_POINT ( 'NONE',  ( 0.3878286276588240877, -0.7819352795844608517, -2.161732420081037720 ) ) ;
#150364=CARTESIAN_POINT ( 'NONE',  ( 1.388340239569575640, -1.017395381511316810, 2.020837998375684563 ) ) ;
#150365=CARTESIAN_POINT ( 'NONE',  ( 2.473383067358714715, 0.1024098097114657241, -2.103702895048992882 ) ) ;
#150369=CARTESIAN_POINT ( 'NONE',  ( 6.406249999940950346, 1.895863741710943406, -0.7852924748303196090 ) ) ;
#150373=CARTESIAN_POINT ( 'NONE',  ( 5.308899460236623291, -0.5399372957704140497, -2.154654435841397930 ) ) ;
#150374=CARTESIAN_POINT ( 'NONE',  ( 3.433693710695666201, 0.9853049363134911420, -1.957518807868402044 ) ) ;
#150378=CARTESIAN_POINT ( 'NONE',  ( 6.890000000000009450, -0.01081285896028030651, 2.279840171838913854 ) ) ;
#150380=CARTESIAN_POINT ( 'NONE',  ( 5.959260761812961604, -1.790568634313693730, 1.135864312162476297 ) ) ;
#150384=CARTESIAN_POINT ( 'NONE',  ( 6.139563164240942506, -1.562336469324271837, -1.494251390645913613 ) ) ;
#150386=CARTESIAN_POINT ( 'NONE',  ( 6.181194517112824194, 1.274813594131599226, 1.328792456347933637 ) ) ;
#150390=CARTESIAN_POINT ( 'NONE',  ( 1.118268200169919568, -0.04383651085794643132, 1.740047355671838547 ) ) ;
#150394=CARTESIAN_POINT ( 'NONE',  ( 5.805597153138060129, -0.5296426447994294628, 2.095691122003799478 ) ) ;
#150398=CARTESIAN_POINT ( 'NONE',  ( 4.329101982860062314, 0.1031891237209987822, 2.159356164053369387 ) ) ;
#150400=CARTESIAN_POINT ( 'NONE',  ( 6.309841845984305309, -1.956726702252456596, 0.2390368442499128110 ) ) ;
#150401=CARTESIAN_POINT ( 'NONE',  ( 5.026542006541363961, 1.714758565716298477, -0.2553409819617598053 ) ) ;
#150404=CARTESIAN_POINT ( 'NONE',  ( 1.646283778714407342, 0.6915601415973006150, 2.079641132013386517 ) ) ;
#150405=CARTESIAN_POINT ( 'NONE',  ( 2.011159220144568938, 1.709348158914993254, -1.550378056569144958 ) ) ;
#150406=CARTESIAN_POINT ( 'NONE',  ( 4.604794268142059721, 1.595455460008918580, -1.304385708662815002 ) ) ;
#150407=CARTESIAN_POINT ( 'NONE',  ( 6.603083112279575673, -0.4245024861969335928, 1.902271653767301007 ) ) ;
#150413=CARTESIAN_POINT ( 'NONE',  ( 1.055314813143366726, -1.277040974352643854, 1.560502084637045650 ) ) ;
#150415=CARTESIAN_POINT ( 'NONE',  ( 4.155453238874762256, -1.833011353516471154, -1.228491751752130545 ) ) ;
#150417=CARTESIAN_POINT ( 'NONE',  ( 1.410758858885716061, -1.471193852737593843, 1.139540799010074323 ) ) ;
#150418=( BOUNDED_SURFACE ( )  B_SPLINE_SURFACE ( 3, 3, ( 
 ( #65932, #49718, #167738, #133140, #17194, #16125, #198091, #113730, #147240, #85417 ),
 ( #199140, #33465, #82209, #31353, #149356, #84350, #97428, #197032, #166676, #19338 ),
 ( #18267, #163482, #181832, #117987, #48668, #132081, #183980, #195984, #116912, #151501 ),
 ( #115846, #150439, #148302, #67003, #937, #50784, #182912, #34529, #2002, #15065 ),
 ( #100600, #114785, #101669, #68067, #214301, #64896, #69141, #3070, #131042, #180783 ),
 ( #134204, #99541, #47618, #179736, #200213, #51866, #35590, #32408, #165604, #83268 ),
 ( #7349, #188243, #40959, #119049, #90779, #87562, #123355, #107067, #4139, #39883 ) ),
 .UNSPECIFIED., .T., .F., .F. ) 
 B_SPLINE_SURFACE_WITH_KNOTS ( ( 4, 3, 4 ),
 ( 4, 1, 1, 1, 1, 1, 1, 4 ),
 ( 0.000000000000000000, 0.5000000000000000000, 1.000000000000000000 ),
 ( 0.000000000000000000, 0.09489293188423997272, 0.1878783894049059211, 0.2584743716234961797, 0.3617987437640678983, 0.5212292184658617877, 0.7337638816394396191, 1.000000000000000000 ),
 .UNSPECIFIED. ) 
 GEOMETRIC_REPRESENTATION_ITEM ( )  RATIONAL_B_SPLINE_SURFACE ( (
 ( 1.000000000000000222, 1.000000000000000222, 1.000000000000000000, 1.000000000000000000, 1.000000000000000000, 1.000000000000000000, 1.000000000000000000, 0.9999999999999997780, 1.000000000000000000, 1.000000000000000000),
 ( 0.3333333333333334259, 0.3333333333333333703, 0.3333333333333334259, 0.3333333333333334259, 0.3333333333333333703, 0.3333333333333333703, 0.3333333333333333703, 0.3333333333333332038, 0.3333333333333333703, 0.3333333333333333703),
 ( 0.3333333333333334259, 0.3333333333333333703, 0.3333333333333334259, 0.3333333333333334259, 0.3333333333333333703, 0.3333333333333333703, 0.3333333333333333703, 0.3333333333333332038, 0.3333333333333333703, 0.3333333333333333703),
 ( 1.000000000000000222, 1.000000000000000222, 1.000000000000000000, 1.000000000000000000, 1.000000000000000000, 1.000000000000000000, 1.000000000000000000, 0.9999999999999997780, 1.000000000000000000, 1.000000000000000000),
 ( 0.3333333333333334259, 0.3333333333333333703, 0.3333333333333334259, 0.3333333333333334259, 0.3333333333333333703, 0.3333333333333333703, 0.3333333333333333703, 0.3333333333333332038, 0.3333333333333333703, 0.3333333333333333703),
 ( 0.3333333333333334259, 0.3333333333333333703, 0.3333333333333334259, 0.3333333333333334259, 0.3333333333333333703, 0.3333333333333333703, 0.3333333333333333703, 0.3333333333333332038, 0.3333333333333333703, 0.3333333333333333703),
 ( 1.000000000000000222, 1.000000000000000222, 1.000000000000000000, 1.000000000000000000, 1.000000000000000000, 1.000000000000000000, 1.000000000000000000, 0.9999999999999997780, 1.000000000000000000, 1.000000000000000000) ) ) 
 REPRESENTATION_ITEM ( '' )  SURFACE ( )  );
#150424=CARTESIAN_POINT ( 'NONE',  ( 6.925078400183550364, -0.007619068086212391067, 2.144148427808051594 ) ) ;
#150427=CARTESIAN_POINT ( 'NONE',  ( 3.608323775901512764, -0.8336323056173270407, -1.884943839506166174 ) ) ;
#150430=CARTESIAN_POINT ( 'NONE',  ( 2.262373273732374290, 2.019286824851754591, 0.04726863806006965929 ) ) ;
#150433=CARTESIAN_POINT ( 'NONE',  ( 2.184514296101589537, -2.020881322650217360, -0.4031914428916544280 ) ) ;
#150439=CARTESIAN_POINT ( 'NONE',  ( -0.1409997244345879697, 0.2375178066936211585, -2.034344168881811132 ) ) ;
#150440=CARTESIAN_POINT ( 'NONE',  ( 0.3394786764520755784, 1.835982197492795898, 0.1384515631646099088 ) ) ;
#150442=CARTESIAN_POINT ( 'NONE',  ( 5.233140740401229785, 0.1595256157847015632, 2.201181388321731269 ) ) ;
#150444=CARTESIAN_POINT ( 'NONE',  ( 1.423353863051743273, -0.05456730952056210171, 2.161080666180377197 ) ) ;
#150446=CARTESIAN_POINT ( 'NONE',  ( 1.868375392651611122, -1.978555653031977446, -0.3886301775877995524 ) ) ;
#150447=CARTESIAN_POINT ( 'NONE',  ( 2.355183240404590705, -0.9839461204387394133, 2.077256468512170162 ) ) ;
#150449=CARTESIAN_POINT ( 'NONE',  ( 0.6197280442463182215, -0.9970892369244135356, -1.582582228963416160 ) ) ;
#150450=CARTESIAN_POINT ( 'NONE',  ( 4.012542200100970291, 1.395003824703803685, -1.393317042198267020 ) ) ;
#150452=CARTESIAN_POINT ( 'NONE',  ( 3.819546216251490822, -1.394084564108012403, -1.457236891723237449 ) ) ;
#150456=CARTESIAN_POINT ( 'NONE',  ( 5.233084072137057063, 0.1537158111805384808, 2.100522205955375199 ) ) ;
#150457=CARTESIAN_POINT ( 'NONE',  ( 5.441872305809390298, 1.387781221417656141, 1.536568222347669987 ) ) ;
#150461=CARTESIAN_POINT ( 'NONE',  ( 5.572523036771587890, 0.8223149429010238043, 1.845017218462653208 ) ) ;
#150463=CARTESIAN_POINT ( 'NONE',  ( 0.8134211793521692879, -1.740389775365951186, -1.106656028277221537 ) ) ;
#150471=CARTESIAN_POINT ( 'NONE',  ( 3.227178390111482553, -2.005013095889785824, -0.8334813368568798619 ) ) ;
#150474=CARTESIAN_POINT ( 'NONE',  ( 2.489598673502769977, -1.836455140896048999, -0.1334285330320400531 ) ) ;
#150476=CARTESIAN_POINT ( 'NONE',  ( 4.195009555701286530, 1.760677850468267414, 1.304791629949946019 ) ) ;
#150478=CARTESIAN_POINT ( 'NONE',  ( 4.961948105735218384, 2.238643107264228327, -0.3270478844536877649 ) ) ;
#150484=CARTESIAN_POINT ( 'NONE',  ( 6.907488038778298645, -0.3811802009726448226, 1.734239976993730670 ) ) ;
#150486=CARTESIAN_POINT ( 'NONE',  ( 4.301435403400270197, 1.797132274555211184, -0.9072848608384380675 ) ) ;
#150488=CARTESIAN_POINT ( 'NONE',  ( 3.311648941680225722, -0.4124737740866398217, 2.064988983437756165 ) ) ;
#150489=CARTESIAN_POINT ( 'NONE',  ( 1.388148191917773611, -0.6910900405009687830, -1.786773533054702545 ) ) ;
#150492=CARTESIAN_POINT ( 'NONE',  ( 2.471101528187972463, 1.758070753236480988, 0.8880565435460830992 ) ) ;
#150493=CARTESIAN_POINT ( 'NONE',  ( 0.08069323953814251660, -0.1329233695197447052, -1.840450602299897431 ) ) ;
#150494=CARTESIAN_POINT ( 'NONE',  ( 1.293326634533353170, -1.775083115552608559, 0.8357255594537355003 ) ) ;
#150495=CARTESIAN_POINT ( 'NONE',  ( 6.416260824072121061, -1.810972107014690913, 0.05430519662179972284 ) ) ;
#150499=CARTESIAN_POINT ( 'NONE',  ( 6.069203928793593050, 0.1358119448514639727, -1.865795782587629681 ) ) ;
#150503=CARTESIAN_POINT ( 'NONE',  ( 5.330949937734919430, -1.947458545883517189, -0.7027056652011903770 ) ) ;
#150513=CARTESIAN_POINT ( 'NONE',  ( 4.791432466842788784, -1.794507165602466037, 0.7932701521168731285 ) ) ;
#150515=CARTESIAN_POINT ( 'NONE',  ( 3.514999820297697308, 2.016288306963448296, 0.002811503506894295987 ) ) ;
#150516=CARTESIAN_POINT ( 'NONE',  ( 2.254979328032254760, 0.08947561643129221809, -1.913730806789506245 ) ) ;
#150518=CARTESIAN_POINT ( 'NONE',  ( 0.4159077360078728969, -1.177411712353953588, -1.848246096435968600 ) ) ;
#150519=CARTESIAN_POINT ( 'NONE',  ( 0.2333690889706959148, 4.088440985731725874, -2.608190362703251441 ) ) ;
#150520=CARTESIAN_POINT ( 'NONE',  ( 3.585083614955933307, 1.692364770286663322, -0.7970176776704935850 ) ) ;
#150524=CARTESIAN_POINT ( 'NONE',  ( 4.552435263133931542, -1.381712717965150938, 1.604331009294196031 ) ) ;
#150526=CARTESIAN_POINT ( 'NONE',  ( 6.355931484454268698, -0.7012994977402075003, 1.948090369817329526 ) ) ;
#150527=CARTESIAN_POINT ( 'NONE',  ( 2.437156881564545685, -1.551092155746801815, -1.402114238623404896 ) ) ;
#150529=CARTESIAN_POINT ( 'NONE',  ( 0.8852880119799062530, 1.153610147808200370, 1.282378885572494465 ) ) ;
#150537=CARTESIAN_POINT ( 'NONE',  ( 0.7503001202024300875, 1.784421795204504946, 0.3107989935832651818 ) ) ;
#150548=CARTESIAN_POINT ( 'NONE',  ( 0.6674275129862971001, 1.287417287929611076, 1.418633514309353583 ) ) ;
#150549=CARTESIAN_POINT ( 'NONE',  ( 0.1883438084668061507, 1.224518555304452416, 1.730999496979759522 ) ) ;
#150557=CARTESIAN_POINT ( 'NONE',  ( 3.660960169446208390, 1.555274301336776022, -1.208163239264722133 ) ) ;
#150558=CARTESIAN_POINT ( 'NONE',  ( 1.366058183223411771, 0.6122477967837879342, -2.030190212274018524 ) ) ;
#150561=CARTESIAN_POINT ( 'NONE',  ( 6.017560223340764125, -1.214513600917455083, -1.823921334435735231 ) ) ;
#150563=CARTESIAN_POINT ( 'NONE',  ( 4.471652382922743030, 1.868735325311605688, -0.4673391499005700722 ) ) ;
#150565=CARTESIAN_POINT ( 'NONE',  ( 0.1998643617870856648, -1.825052844667142349, -0.05062755788937112200 ) ) ;
#150566=CARTESIAN_POINT ( 'NONE',  ( 0.7334016978863611147, 0.1661181961954381059, 2.200687262777756725 ) ) ;
#150570=CARTESIAN_POINT ( 'NONE',  ( 5.928554213991230171, -1.252361881311152558, 1.519918492727867054 ) ) ;
#150571=CARTESIAN_POINT ( 'NONE',  ( -0.05917297228825654093, -1.501800262597710267, -1.231000148999121357 ) ) ;
#150572=CARTESIAN_POINT ( 'NONE',  ( 6.274848118712046841, -2.282167594539401101, 0.2721878479114477334 ) ) ;
#150574=CARTESIAN_POINT ( 'NONE',  ( 4.487043221128726778, 0.08799343497551150028, 1.858965402599630723 ) ) ;
#150580=CARTESIAN_POINT ( 'NONE',  ( 0.8201894534925309177, 1.301127354658284663, -1.763390660798454634 ) ) ;
#150585=CARTESIAN_POINT ( 'NONE',  ( 0.6799654140086827114, -1.016662149479659494, 1.516215539243186639 ) ) ;
#150587=CARTESIAN_POINT ( 'NONE',  ( 3.726996057929339745, 1.726255173046949309, 0.1649803145151728934 ) ) ;
#150591=CARTESIAN_POINT ( 'NONE',  ( 6.551389018236878137, -1.469694460105780642, -1.082916835497591324 ) ) ;
#150592=CARTESIAN_POINT ( 'NONE',  ( 4.451973756923766068, -0.7546651901383871763, 1.810992078419524365 ) ) ;
#150595=CARTESIAN_POINT ( 'NONE',  ( 4.740951199079581180, 2.029406658027664623, 0.6148427566107574904 ) ) ;
#150600=CARTESIAN_POINT ( 'NONE',  ( 3.309495622959734096, -1.689761761210720525, -1.195817184978978043 ) ) ;
#150603=CARTESIAN_POINT ( 'NONE',  ( 5.110122900737038343, -0.8006010496643833907, 2.072185752117897461 ) ) ;
#150605=CARTESIAN_POINT ( 'NONE',  ( 3.200086968229500783, 2.078864265255635946, 0.9811947989078557697 ) ) ;
#150614=CARTESIAN_POINT ( 'NONE',  ( 4.271672842113056312, 0.4137096367802223784, -1.866957553337177611 ) ) ;
#150616=CARTESIAN_POINT ( 'NONE',  ( 4.770341545797544214, -1.125046721222152213, 1.307389476665332895 ) ) ;
#150617=CARTESIAN_POINT ( 'NONE',  ( 3.010954138651841916, 0.05432569772663428664, 2.015980714967258614 ) ) ;
#150618=CARTESIAN_POINT ( 'NONE',  ( 5.502642741134641469, -2.243371634331346343, 0.5006679109763980673 ) ) ;
#150620=CARTESIAN_POINT ( 'NONE',  ( 5.865875422609286183, 2.075172955015105014, -0.3584678469405917500 ) ) ;
#150623=CARTESIAN_POINT ( 'NONE',  ( 5.905463120178883862, -0.4284811148945049109, 1.716917210449308673 ) ) ;
#150625=CARTESIAN_POINT ( 'NONE',  ( 1.447684683128658278, 0.6615928844308440748, -2.194714443420691552 ) ) ;
#150626=CARTESIAN_POINT ( 'NONE',  ( 0.4447213192238759771, 0.5506589691408066978, -1.650998906686143464 ) ) ;
#150632=CARTESIAN_POINT ( 'NONE',  ( 6.883263157960362477, -0.004191378316371896506, 2.053658919477070910 ) ) ;
#150633=CARTESIAN_POINT ( 'NONE',  ( 1.270720652900014791, -0.3006520276036573902, -1.993892820393451615 ) ) ;
#150635=CARTESIAN_POINT ( 'NONE',  ( 5.022062012317437762, -1.032219231902216761, -1.626458924502146797 ) ) ;
#150637=CARTESIAN_POINT ( 'NONE',  ( 2.549351761953377427, 0.2766319664159795355, 2.204086880180194274 ) ) ;
#150638=VERTEX_POINT ( 'NONE', #21441 ) ;
#150645=CARTESIAN_POINT ( 'NONE',  ( 4.282551955697760704, 1.552239185393188947, -0.7873791831930468943 ) ) ;
#150646=CARTESIAN_POINT ( 'NONE',  ( 2.963279974173158138, 1.655882904019840840, 1.051842618152734499 ) ) ;
#150651=CARTESIAN_POINT ( 'NONE',  ( 0.9243725180730785196, 1.015136377070953388, 1.795498427122848017 ) ) ;
#150654=CARTESIAN_POINT ( 'NONE',  ( 1.622331739061450007, -1.257988004683800787, -1.880359251820800104 ) ) ;
#150657=CARTESIAN_POINT ( 'NONE',  ( 2.794054307841778328, -1.865266697571520194, -0.1415833504254116748 ) ) ;
#150658=CARTESIAN_POINT ( 'NONE',  ( 0.8965906023701503136, -0.7780376274850349105, -1.549907966113317270 ) ) ;
#150660=CARTESIAN_POINT ( 'NONE',  ( 5.636325218313963603, 0.4264374063192889475, 2.149501299143250055 ) ) ;
#150661=CARTESIAN_POINT ( 'NONE',  ( 5.667085135620930636, -2.082984650255703230, -0.9933455750401504192 ) ) ;
#150662=CARTESIAN_POINT ( 'NONE',  ( 1.622021928100621624, -1.144040325636319189, -1.713970819250490552 ) ) ;
#150663=CARTESIAN_POINT ( 'NONE',  ( 3.029168698193057008, -1.304570280419844686, -1.438651077900707120 ) ) ;
#150665=CARTESIAN_POINT ( 'NONE',  ( 5.817618194842750334, -1.825074353437942332, 0.4092329068215995735 ) ) ;
#150666=CARTESIAN_POINT ( 'NONE',  ( 1.906250000000001332, 1.895863743164044823, -0.7852924748300882385 ) ) ;
#150667=EDGE_CURVE ( 'NONE', #202176, #167392, #90565, .T. ) ;
#150669=CARTESIAN_POINT ( 'NONE',  ( 0.2976278659034147789, -1.588993460933589841, 0.6942472086189295233 ) ) ;
#150672=CARTESIAN_POINT ( 'NONE',  ( 4.078750125433938223, -0.7691220382576718917, 1.864168106189521890 ) ) ;
#150676=CARTESIAN_POINT ( 'NONE',  ( 1.805030607383810715, 1.517133602069477893, 1.015288170653723343 ) ) ;
#150685=CARTESIAN_POINT ( 'NONE',  ( 5.567059059060062154, -1.590727130084067964, 1.244318111769521229 ) ) ;
#150686=CARTESIAN_POINT ( 'NONE',  ( 0.1180496341894651385, -0.5612577129426484790, 2.044807062438446454 ) ) ;
#150690=CARTESIAN_POINT ( 'NONE',  ( 4.909085936489448798, 1.792118714629163057, 1.017505292531006189 ) ) ;
#150691=CARTESIAN_POINT ( 'NONE',  ( 5.151017605526479137, 0.9962996879465220168, 1.753031629501592192 ) ) ;
#150695=CARTESIAN_POINT ( 'NONE',  ( -0.2108831679770926115, 5.723481173670196043, -2.491210874135452613 ) ) ;
#150699=CARTESIAN_POINT ( 'NONE',  ( 5.589220178194088895, 1.203167956798111060, -1.617571559180859486 ) ) ;
#150700=CARTESIAN_POINT ( 'NONE',  ( 4.400242069895500485, 1.421654421768648868, -1.169904355399861595 ) ) ;
#150701=CARTESIAN_POINT ( 'NONE',  ( -0.02319159430947542386, 1.394398620246390275, -2.068318759734718792 ) ) ;
#150702=CARTESIAN_POINT ( 'NONE',  ( 1.999037954658490213, -0.6180237258119178900, -2.223338030673171151 ) ) ;
#150704=CARTESIAN_POINT ( 'NONE',  ( 4.657600047955182454, 0.4785990281669267876, -2.107782517917502929 ) ) ;
#150706=CARTESIAN_POINT ( 'NONE',  ( 0.09902944379243035222, -0.5168498253214492966, 1.871975360678623579 ) ) ;
#150708=CARTESIAN_POINT ( 'NONE',  ( 3.901994836520364718, 0.3331327188077978785, 2.274008445091058928 ) ) ;
#150712=CARTESIAN_POINT ( 'NONE',  ( 3.801501934187266230, -0.5436965770258190833, 1.789884385262895616 ) ) ;
#150714=CARTESIAN_POINT ( 'NONE',  ( 0.6504702201592416078, 1.884490048413577368, 0.3244712162126031085 ) ) ;
#150717=CARTESIAN_POINT ( 'NONE',  ( 2.737190076726934151, 0.2709513247245790013, 2.190122135706531914 ) ) ;
#150723=CARTESIAN_POINT ( 'NONE',  ( 0.4914017305483203701, 1.457842971892213235, 1.327161884117057600 ) ) ;
#150724=CARTESIAN_POINT ( 'NONE',  ( 6.498638929175646339, -0.6082784835782985011, -2.226023345802934372 ) ) ;
#150725=CARTESIAN_POINT ( 'NONE',  ( 1.029656018189710309, 1.891699080040713410, -0.5197978237033785698 ) ) ;
#150726=CARTESIAN_POINT ( 'NONE',  ( 3.836832695767174783, -1.986499165045521265, -0.5546697284559941599 ) ) ;
#150734=CARTESIAN_POINT ( 'NONE',  ( 6.355955588539900170, -0.7375000094371157999, 2.042207395130499759 ) ) ;
#150736=CARTESIAN_POINT ( 'NONE',  ( 6.614805131849967879, -0.1256686391097518729, 1.812046779126045726 ) ) ;
#150739=CARTESIAN_POINT ( 'NONE',  ( 0.9658262494645246665, 0.9167188063998463754, 1.630421345857439475 ) ) ;
#150744=CARTESIAN_POINT ( 'NONE',  ( 0.8559432719405722922, 0.7744784914341161786, -1.748599447100062321 ) ) ;
#150745=CARTESIAN_POINT ( 'NONE',  ( 2.904884094325186350, 1.494127413938572069, 0.9483235522904243098 ) ) ;
#150747=CARTESIAN_POINT ( 'NONE',  ( 1.277824965264368728, 1.883817941867833134, -0.3277997056638781714 ) ) ;
#150749=CARTESIAN_POINT ( 'NONE',  ( 4.323789496349770722, 0.8154102246901802076, -1.733521564635835732 ) ) ;
#150750=CARTESIAN_POINT ( 'NONE',  ( -0.1409997244346088141, 4.088373444016307978, -2.555100908668860082 ) ) ;
#150751=CARTESIAN_POINT ( 'NONE',  ( 5.494576857243831824, 1.940090112543988665, 0.3384423684570179724 ) ) ;
#150752=CARTESIAN_POINT ( 'NONE',  ( 0.5980879788009090259, 1.428637019467562830, 1.567290143595565066 ) ) ;
#150754=CARTESIAN_POINT ( 'NONE',  ( 3.590566789841375339, -0.3639703897368729568, -1.834726254853453087 ) ) ;
#150755=CARTESIAN_POINT ( 'NONE',  ( 1.137010146156680834, -1.651496384925277283, 0.7785749969668461778 ) ) ;
#150756=EDGE_LOOP ( 'NONE', ( #208049, #118117, #201112, #71556 ) ) ;
#150757=CARTESIAN_POINT ( 'NONE',  ( 3.071135375186518690, -2.039199700013223815, -0.8442704067812344393 ) ) ;
#150760=CARTESIAN_POINT ( 'NONE',  ( 1.223174996406689585, -1.863865272486511460, -0.8838528460363299644 ) ) ;
#150766=CARTESIAN_POINT ( 'NONE',  ( 6.469012471580376733, -1.473683540339595588, 1.218514635347216046 ) ) ;
#150768=CARTESIAN_POINT ( 'NONE',  ( 2.682155120989743402, -1.190029146579720587, -1.693995171316540427 ) ) ;
#150770=CARTESIAN_POINT ( 'NONE',  ( 1.423353863051743273, -0.05456730952056210171, 2.161080666180377197 ) ) ;
#150772=CARTESIAN_POINT ( 'NONE',  ( 1.242838512808578377, 1.947023393874779851, 0.5366068325038054754 ) ) ;
#150774=VERTEX_POINT ( 'NONE', #149911 ) ;
#150778=CARTESIAN_POINT ( 'NONE',  ( 0.5675926644314840397, 1.357872185771633156, 1.490966652548594285 ) ) ;
#150780=CARTESIAN_POINT ( 'NONE',  ( 5.108995794240286159, -0.3219066699026683631, 2.167653318578148358 ) ) ;
#150782=CARTESIAN_POINT ( 'NONE',  ( 3.656429697474584462, 1.903630103707624865, 0.1825790434749063051 ) ) ;
#150786=CARTESIAN_POINT ( 'NONE',  ( 1.581657880887325174, -0.6766953518495041342, 1.899626397962331126 ) ) ;
#150788=CARTESIAN_POINT ( 'NONE',  ( 0.6270410820986601630, 0.1761543355088228957, 2.285679397864130102 ) ) ;
#150790=CARTESIAN_POINT ( 'NONE',  ( 3.645241786196154354, -1.305741510076625644, -1.126962775032739339 ) ) ;
#150791=CARTESIAN_POINT ( 'NONE',  ( 0.1405533004714279166, 6.947787103499396544, -2.874819994463383654 ) ) ;
#150794=CARTESIAN_POINT ( 'NONE',  ( 0.8538673084422104820, -0.7095216264049221122, 1.829241926910141203 ) ) ;
#150797=CARTESIAN_POINT ( 'NONE',  ( 0.1753634416057497647, 2.004068818557998011, -2.558292918872175914 ) ) ;
#150801=CARTESIAN_POINT ( 'NONE',  ( 3.475094438140493125, -1.599078698050887981, -0.8510578468755282122 ) ) ;
#150805=CARTESIAN_POINT ( 'NONE',  ( 5.074790875859057415, -1.308146702057958910, 1.253318493144810697 ) ) ;
#150809=CARTESIAN_POINT ( 'NONE',  ( 6.303157624210896870, -1.571610030290017557, 0.9964359807085266807 ) ) ;
#150812=CARTESIAN_POINT ( 'NONE',  ( 3.304201903042072175, 1.212927065539553206, -1.482701048864635496 ) ) ;
#150820=CARTESIAN_POINT ( 'NONE',  ( 0.5499753625364013354, 0.6768306982547143136, -2.053065283773393368 ) ) ;
#150823=CARTESIAN_POINT ( 'NONE',  ( 1.237009950130557812, -1.652246606862219025, 0.7767072072360350354 ) ) ;
#150825=CARTESIAN_POINT ( 'NONE',  ( 3.293790705515726724, -0.7410340593078694749, 1.668602820345471027 ) ) ;
#150829=CARTESIAN_POINT ( 'NONE',  ( 3.103910798422233608, 0.7114650421483189602, -1.836736179910645195 ) ) ;
#150830=CARTESIAN_POINT ( 'NONE',  ( 3.878411472391342318, -0.1936643080829789088, -1.932398009575059472 ) ) ;
#150833=CARTESIAN_POINT ( 'NONE',  ( 4.588201236890728119, 1.223260742344203900, 1.732012071221388450 ) ) ;
#150842=CARTESIAN_POINT ( 'NONE',  ( 5.479063914364931343, -0.04889757770590653918, -1.825204647902956889 ) ) ;
#150847=CARTESIAN_POINT ( 'NONE',  ( 6.104356062600288624, -0.6750377415852754082, -1.744797942764392928 ) ) ;
#150849=CARTESIAN_POINT ( 'NONE',  ( 3.809137074456845795, 1.652770800469059775, 0.9896037298236616264 ) ) ;
#150854=( NAMED_UNIT ( * ) SI_UNIT ( $, .STERADIAN. ) SOLID_ANGLE_UNIT ( ) );
#150857=CARTESIAN_POINT ( 'NONE',  ( 1.089646232962078853, -0.5102306600231114597, 2.054730298310704750 ) ) ;
#150861=CARTESIAN_POINT ( 'NONE',  ( 6.842638490404138629, -2.029097751484234546, -0.4099019697717393163 ) ) ;
#150862=CARTESIAN_POINT ( 'NONE',  ( 1.645803748337611783, 0.5784278848013635344, 1.748079663633335334 ) ) ;
#150867=CARTESIAN_POINT ( 'NONE',  ( 1.764052804016162268, 1.181211026566388211, 1.964360346841328209 ) ) ;
#150869=CARTESIAN_POINT ( 'NONE',  ( 5.964781414698055784, 0.1407378593174268555, -1.936906258807554071 ) ) ;
#150873=CARTESIAN_POINT ( 'NONE',  ( 0.5979028997950117663, 1.355058449971069834, 1.489028425022032698 ) ) ;
#150874=CARTESIAN_POINT ( 'NONE',  ( 0.5671465430379521999, 1.703994235754960451, 0.9719838849941149217 ) ) ;
#150879=CARTESIAN_POINT ( 'NONE',  ( 4.453126923439646667, 0.4583234712903122565, -2.039610397757870341 ) ) ;
#150880=CARTESIAN_POINT ( 'NONE',  ( 2.623613022005319984, -1.017049183177589855, -1.448221827668960238 ) ) ;
#150883=CARTESIAN_POINT ( 'NONE',  ( 5.226663038502143088, 0.1645964690673335229, 2.286419844370500165 ) ) ;
#150884=CARTESIAN_POINT ( 'NONE',  ( 2.817972641794503019, 1.638747005868109285, 0.5862587914967545277 ) ) ;
#150887=CARTESIAN_POINT ( 'NONE',  ( 3.743219424636199832, -1.670416500854546626, -0.4642454339297346078 ) ) ;
#150888=CARTESIAN_POINT ( 'NONE',  ( 3.930270145471780996, 1.203169952209550919, 1.807132499170207351 ) ) ;
#150890=CARTESIAN_POINT ( 'NONE',  ( 4.891814693739657827, -2.006371927678828104, 0.2024599332275459629 ) ) ;
#150891=CARTESIAN_POINT ( 'NONE',  ( 0.4374999999988640753, 1.451031289089056431, -1.451031289061139651 ) ) ;
#150894=CARTESIAN_POINT ( 'NONE',  ( 2.291906413246731944, -0.8257142216546548008, 1.740595036569925647 ) ) ;
#150896=CARTESIAN_POINT ( 'NONE',  ( 5.924141181918635368, -2.204746212865996480, 0.2713366554644781603 ) ) ;
#150898=CARTESIAN_POINT ( 'NONE',  ( -0.1110810684432986112, 0.002541288824218449188, -1.796853612742685513 ) ) ;
#150903=CARTESIAN_POINT ( 'NONE',  ( 0.8564553275840697255, 0.8952667643853294832, -2.033071718549640305 ) ) ;
#150904=CARTESIAN_POINT ( 'NONE',  ( 5.705508943770692731, -1.545575431542939970, -1.208212526538715137 ) ) ;
#150907=CARTESIAN_POINT ( 'NONE',  ( 0.3511320849261707622, -1.736299752564632204, 1.287366282644891724 ) ) ;
#150910=CARTESIAN_POINT ( 'NONE',  ( 4.826661651916083429, -1.349687995210807401, 1.559865583710306147 ) ) ;
#150915=CARTESIAN_POINT ( 'NONE',  ( 6.010993879215096314, 1.649516084216671397, 0.8821100558755521348 ) ) ;
#150916=CARTESIAN_POINT ( 'NONE',  ( 4.922368227709418065, -1.231479607182428104, -1.221251793340462299 ) ) ;
#150917=CARTESIAN_POINT ( 'NONE',  ( 4.546296192243603151, -1.394137154979861570, 1.041651924218311986 ) ) ;
#150920=CARTESIAN_POINT ( 'NONE',  ( 2.156203017566417302, 0.9840264443441574249, 2.070573632387271434 ) ) ;
#150922=CARTESIAN_POINT ( 'NONE',  ( 5.478101502371197640, -2.040020603162643997, -0.4570242091310200427 ) ) ;
#150923=CARTESIAN_POINT ( 'NONE',  ( 0.3746297210940018885, 1.718982886236510854, -0.6599183738737608440 ) ) ;
#150926=CARTESIAN_POINT ( 'NONE',  ( 2.004529941291322448, -1.955172360644286789, 0.4926429297785542283 ) ) ;
#150927=CARTESIAN_POINT ( 'NONE',  ( 0.07648947921621782053, -2.126777779243053779, -0.5280787695999613618 ) ) ;
#150931=CARTESIAN_POINT ( 'NONE',  ( 2.332823983099761911, 1.383068002389773454, -1.607457772141835717 ) ) ;
#150933=CARTESIAN_POINT ( 'NONE',  ( 5.285714101943871590, 1.228958891529348785, 1.350286652578087665 ) ) ;
#150940=CARTESIAN_POINT ( 'NONE',  ( 3.146744605306639908, 1.971464920705681800, 0.4384460897248109723 ) ) ;
#150941=CARTESIAN_POINT ( 'NONE',  ( 0.2707219772894990384, -1.375384669632748524, 1.594866825539154043 ) ) ;
#150943=CARTESIAN_POINT ( 'NONE',  ( 3.608110912359719258, 1.861131631771815842, 0.004268880383616681894 ) ) ;
#150951=CARTESIAN_POINT ( 'NONE',  ( 1.985274739808037481, 1.615814429867837410, 0.6292545280836835397 ) ) ;
#150952=CARTESIAN_POINT ( 'NONE',  ( 1.130330966444204277, -1.574854822160208556, 0.7409792249596267588 ) ) ;
#150953=CARTESIAN_POINT ( 'NONE',  ( 6.568959576340373197, -2.106780069790818555, -0.9421804820441375128 ) ) ;
#150956=CARTESIAN_POINT ( 'NONE',  ( 1.282574848904423082, -2.009897191344016232, -0.4543217371432185514 ) ) ;
#150957=CARTESIAN_POINT ( 'NONE',  ( 6.749376085230743172, -2.252018642839793472, -0.4587488502729390460 ) ) ;
#150961=CARTESIAN_POINT ( 'NONE',  ( 0.3738188115672124168, 1.133047686669987675, 1.613170723887060065 ) ) ;
#150962=CARTESIAN_POINT ( 'NONE',  ( 4.816621285000030284, -0.6497861859515661198, -1.798733151862880186 ) ) ;
#150964=CARTESIAN_POINT ( 'NONE',  ( 5.795608111622330583, 1.668732747960173235, 1.444295198399044855 ) ) ;
#150969=CARTESIAN_POINT ( 'NONE',  ( -0.1106727585415967219, -0.002281114264979232885, -2.003378291782103471 ) ) ;
#150970=CARTESIAN_POINT ( 'NONE',  ( 3.786388324757625323, -1.140120265720317327, 2.006200910446949592 ) ) ;
#150971=CARTESIAN_POINT ( 'NONE',  ( 4.598074495912658044, 0.8407358649686399454, -1.772743347989129692 ) ) ;
#150972=CARTESIAN_POINT ( 'NONE',  ( 0.7077677203753615087, 0.6208407433182620005, -1.860969989990405749 ) ) ;
#150976=CARTESIAN_POINT ( 'NONE',  ( 0.1810649180928698143, 1.756560269771380911, -1.181951075121101979 ) ) ;
#150980=CARTESIAN_POINT ( 'NONE',  ( 2.747136105846450516, -0.3671824478193272956, -2.139636267262314373 ) ) ;
#150983=CARTESIAN_POINT ( 'NONE',  ( 0.1586465271753433603, 2.115359532055087310, 0.1496401998123952359 ) ) ;
#150988=CARTESIAN_POINT ( 'NONE',  ( 2.618495166727810908, 1.348686541216067347, -1.558216953862724408 ) ) ;
#150992=CARTESIAN_POINT ( 'NONE',  ( 0.07755575628181492209, 4.082361791518872352, -2.743585103993382734 ) ) ;
#150995=CARTESIAN_POINT ( 'NONE',  ( 4.477155480220369910, -1.709698060584059043, -0.8567103784868702610 ) ) ;
#150997=CARTESIAN_POINT ( 'NONE',  ( 1.739923964384773258, -1.638176463808267647, -1.560613564838263523 ) ) ;
#150999=CARTESIAN_POINT ( 'NONE',  ( 1.828075118979434865, -0.8562131971674535880, -1.596496639089627578 ) ) ;
#151000=CARTESIAN_POINT ( 'NONE',  ( 0.5849901852424718163, 1.567898511244028459, 1.100480585720535087 ) ) ;
#151001=CARTESIAN_POINT ( 'NONE',  ( 1.504437137538238600, 2.067909592606699487, 0.1035681241481553605 ) ) ;
#151003=CARTESIAN_POINT ( 'NONE',  ( 0.2683544108190681898, -1.289511475198481305, 1.491327623740832387 ) ) ;
#151004=CARTESIAN_POINT ( 'NONE',  ( 6.059198490463121090, -1.653572398999035853, -0.9882694798356050914 ) ) ;
#151005=CARTESIAN_POINT ( 'NONE',  ( 6.551417122825020201, -1.769646310455678995, -1.318412661681533260 ) ) ;
#151009=CARTESIAN_POINT ( 'NONE',  ( 4.650865732144216835, -0.4487226328800034691, -2.013136760839563166 ) ) ;
#151013=( BOUNDED_CURVE ( )  B_SPLINE_CURVE ( 3, ( #168969, #133313, #70376, #120301 ),
 .UNSPECIFIED., .F., .T. ) 
 B_SPLINE_CURVE_WITH_KNOTS ( ( 4, 4 ),
 ( 0.4999999999999988898, 1.000000000000000000 ),
 .UNSPECIFIED. ) 
 CURVE ( )  GEOMETRIC_REPRESENTATION_ITEM ( )  RATIONAL_B_SPLINE_CURVE ( ( 1.000000000000001554, 0.3333333333333333703, 0.3333333333333318715, 1.000000000000000000 ) ) 
 REPRESENTATION_ITEM ( '' )  );
#151015=CARTESIAN_POINT ( 'NONE',  ( 5.069407556592405939, 0.2091588727727889396, -2.095552839448256766 ) ) ;
#151018=CARTESIAN_POINT ( 'NONE',  ( 0.8015275938294207370, -1.862055209299150249, 1.116337150347948892 ) ) ;
#151020=CARTESIAN_POINT ( 'NONE',  ( 4.798204600472657511, -2.160985683756014630, -0.05834674948757002932 ) ) ;
#151021=CARTESIAN_POINT ( 'NONE',  ( 5.637369771878480762, -0.04735730112789998669, 2.019284605405778255 ) ) ;
#151022=CARTESIAN_POINT ( 'NONE',  ( -0.1399997263889819488, 4.088450529495776919, -2.555104583160577647 ) ) ;
#151027=CARTESIAN_POINT ( 'NONE',  ( 3.714077560468319827, 1.074663192196689376, -1.706111893292367343 ) ) ;
#151031=CARTESIAN_POINT ( 'NONE',  ( 4.733375416736937069, -1.977748744329570263, 0.8730265686548792647 ) ) ;
#151036=CARTESIAN_POINT ( 'NONE',  ( 4.341422844945469706, 0.4390097190783425196, -1.967893369681630311 ) ) ;
#151038=CARTESIAN_POINT ( 'NONE',  ( 1.119288186499637794, -1.683610015651057168, 0.3742365367947718124 ) ) ;
#151043=CARTESIAN_POINT ( 'NONE',  ( 5.044154037833219029, 1.865456107639616556, 0.1390639465682907416 ) ) ;
#151044=CARTESIAN_POINT ( 'NONE',  ( 6.064703285670603350, 0.6354670234634349768, 1.910320939954947228 ) ) ;
#151048=ORIENTED_EDGE ( 'NONE', *, *, #83695, .F. ) ;
#151050=CARTESIAN_POINT ( 'NONE',  ( 1.840644454891388282, 1.218392294859267144, -1.735325642819862013 ) ) ;
#151051=CARTESIAN_POINT ( 'NONE',  ( 0.2281389574181335589, 2.011207032379238591, 0.1455110067964115739 ) ) ;
#151052=CARTESIAN_POINT ( 'NONE',  ( 1.599580717682536291, 1.250984903983554997, 1.310507481138773800 ) ) ;
#151054=CARTESIAN_POINT ( 'NONE',  ( 6.491117449447131982, 1.883434485765375310, -1.060826435891427666 ) ) ;
#151061=CARTESIAN_POINT ( 'NONE',  ( 0.5674276921618210956, 1.288973137450568407, 1.417358193720698933 ) ) ;
#151068=CARTESIAN_POINT ( 'NONE',  ( 4.047864428982482110, 0.7307185629543844207, -2.034579650689218866 ) ) ;
#151071=CARTESIAN_POINT ( 'NONE',  ( 2.461320219219771843, -1.760565900816572826, 1.181798851529712646 ) ) ;
#151072=CARTESIAN_POINT ( 'NONE',  ( 6.387720234973090605, 1.261301916940280154, 1.320039730931761524 ) ) ;
#151073=CARTESIAN_POINT ( 'NONE',  ( 2.407442502341358814, -0.4355224260998523111, 1.922489325443673236 ) ) ;
#151076=CARTESIAN_POINT ( 'NONE',  ( 6.021921669442146907, 1.940670798679052123, -0.3350140356708011802 ) ) ;
#151077=CARTESIAN_POINT ( 'NONE',  ( 1.148265734048327769, -1.531264750074516234, 1.194210492925862344 ) ) ;
#151084=CARTESIAN_POINT ( 'NONE',  ( 4.652931681422667332, 0.3304644650514582116, 1.883354098946861344 ) ) ;
#151086=CARTESIAN_POINT ( 'NONE',  ( 3.756632125300945368, 0.7937082651479386852, 2.059386989456575279 ) ) ;
#151087=CARTESIAN_POINT ( 'NONE',  ( 1.800138458411651765, -0.7431416638853624024, 2.077998897882806784 ) ) ;
#151089=CARTESIAN_POINT ( 'NONE',  ( 1.031728963041964153, -1.865498905729731316, 0.4196304693004496156 ) ) ;
#151090=CARTESIAN_POINT ( 'NONE',  ( 0.07661050522430287724, 1.422454998960010153, -1.972067596371825715 ) ) ;
#151094=CARTESIAN_POINT ( 'NONE',  ( 2.963400493335893504, 1.747644659881589568, 1.109742091278065113 ) ) ;
#151098=CARTESIAN_POINT ( 'NONE',  ( 0.6554165194554737450, -1.826866057147133349, -1.155366728873077342 ) ) ;
#151099=CARTESIAN_POINT ( 'NONE',  ( 3.685266855566126321, 1.588411730319793769, 1.510178839762461811 ) ) ;
#151105=CARTESIAN_POINT ( 'NONE',  ( 6.205661552121055635, 1.621658882679182456, 0.6149916719311411262 ) ) ;
#151107=CARTESIAN_POINT ( 'NONE',  ( 3.889561532384704368, -1.914723906051108537, 0.7877538119766481772 ) ) ;
#151108=CARTESIAN_POINT ( 'NONE',  ( 4.394233635046361108, -0.9068805580662200327, -1.913321081533605028 ) ) ;
#151111=CARTESIAN_POINT ( 'NONE',  ( 2.518351277774394159, 0.8375136450692384216, 1.782609909039992946 ) ) ;
#151112=CARTESIAN_POINT ( 'NONE',  ( 0.2988868148526523938, -0.2362956723594503705, -1.897694653714178781 ) ) ;
#151113=CARTESIAN_POINT ( 'NONE',  ( 4.699361189290715224, -0.6141998521675575695, 2.208390280175839049 ) ) ;
#151114=CARTESIAN_POINT ( 'NONE',  ( 3.158640206316553289, -1.382037546686708973, 1.193037399656725395 ) ) ;
#151119=CARTESIAN_POINT ( 'NONE',  ( 3.726818050638240898, 1.420666359685630598, -1.426677609031762994 ) ) ;
#151120=CARTESIAN_POINT ( 'NONE',  ( 3.977359813172594905, -0.1486911861427446802, 1.956209631609528099 ) ) ;
#151124=CARTESIAN_POINT ( 'NONE',  ( 0.07536363704233395300, 5.720741966631408104, -2.738263776839637398 ) ) ;
#151125=CARTESIAN_POINT ( 'NONE',  ( 0.01142647129402651375, -2.049560973810752085, 0.4120210816158270117 ) ) ;
#151126=CARTESIAN_POINT ( 'NONE',  ( 5.524192064727496465, 1.051792464684684347, -1.423223091708211818 ) ) ;
#151127=CARTESIAN_POINT ( 'NONE',  ( 2.097856687836355150, -2.190910012095201420, 0.05558666267656967030 ) ) ;
#151128=CARTESIAN_POINT ( 'NONE',  ( 0.01074006189176902708, -1.707493591921129372, 0.3360247309564004525 ) ) ;
#151130=CARTESIAN_POINT ( 'NONE',  ( 0.2335667940002476017, 0.2385907455819072931, -2.187945659632169804 ) ) ;
#151131=CARTESIAN_POINT ( 'NONE',  ( 0.1524156081505250449, -1.388816673012055025, 1.022707173280016368 ) ) ;
#151132=CARTESIAN_POINT ( 'NONE',  ( 0.7733716040702149908, -2.287020594544288521, 0.2280439049123609840 ) ) ;
#151133=CARTESIAN_POINT ( 'NONE',  ( 1.013517375116283592, -2.137022957946862700, 0.4851717564131745597 ) ) ;
#151134=CARTESIAN_POINT ( 'NONE',  ( 6.345060247669167097, -0.9239052495037097801, 1.466952517609141138 ) ) ;
#151135=CARTESIAN_POINT ( 'NONE',  ( 2.895379187063460424, 1.892502543702856865, -1.135010264495312837 ) ) ;
#151136=CARTESIAN_POINT ( 'NONE',  ( 6.531686450800388677, 2.079676181002787061, -0.6237389289161490158 ) ) ;
#151137=CARTESIAN_POINT ( 'NONE',  ( 1.341172884435502866, -1.819006327537198153, -1.083427034744638862 ) ) ;
#151138=CARTESIAN_POINT ( 'NONE',  ( 6.827182134110235445, 7.051404648315344303, 2.887205390314013354 ) ) ;
#151139=CARTESIAN_POINT ( 'NONE',  ( 4.999011269523485623, 1.601735033023284904, -1.069960431631542752 ) ) ;
#151141=CARTESIAN_POINT ( 'NONE',  ( 1.417954980037740009, -1.278267931767061771, -1.902717450791486353 ) ) ;
#151145=CARTESIAN_POINT ( 'NONE',  ( 5.197972062552532080, 1.490711083722006780, 1.646940351458234808 ) ) ;
#151151=CARTESIAN_POINT ( 'NONE',  ( 2.777970385693105726, 1.728001979019553325, -1.038993764437286416 ) ) ;
#151153=CARTESIAN_POINT ( 'NONE',  ( 0.6903719162679988752, 1.063636609032023950, -1.767059929103020677 ) ) ;
#151158=CARTESIAN_POINT ( 'NONE',  ( 4.488337453930180132, -0.4787454259813396229, -2.138356021698713416 ) ) ;
#151159=CARTESIAN_POINT ( 'NONE',  ( 1.160779977835691312, 1.203355533934968635, 1.617816888933524710 ) ) ;
#151160=CARTESIAN_POINT ( 'NONE',  ( 1.030510548812729965, -1.664561007783531332, 0.7873658874757857307 ) ) ;
#151161=CARTESIAN_POINT ( 'NONE',  ( 5.390252792638895230, -0.5542908586613685129, -2.224220739628431254 ) ) ;
#151162=CARTESIAN_POINT ( 'NONE',  ( 3.292734131499192252, 1.452021927685825275, 1.131891246899892289 ) ) ;
#151164=CARTESIAN_POINT ( 'NONE',  ( 3.698116152863577977, -1.823479002399010396, -0.09026698595545472326 ) ) ;
#151165=CARTESIAN_POINT ( 'NONE',  ( 5.344375030997434273, 0.3906003880304632636, -1.978050218768567792 ) ) ;
#151167=CARTESIAN_POINT ( 'NONE',  ( 4.874029165478985348, 1.298689969358796770, 1.852503425883561095 ) ) ;
#151169=CARTESIAN_POINT ( 'NONE',  ( 6.317421145955757211, -0.2613792861649695265, 2.089613723330654427 ) ) ;
#151171=CARTESIAN_POINT ( 'NONE',  ( 3.174344110969638866, -1.018096006688212096, -1.802650257252853772 ) ) ;
#151176=CARTESIAN_POINT ( 'NONE',  ( 1.998540859798603408, -0.5134167636005394497, -1.856760371892735906 ) ) ;
#151179=CARTESIAN_POINT ( 'NONE',  ( 6.807475516257630588, -1.579661688080177262, -1.175915379947721773 ) ) ;
#151183=CARTESIAN_POINT ( 'NONE',  ( 1.283751863706618535, 0.1568931172264090290, -2.215910488618375584 ) ) ;
#151184=CARTESIAN_POINT ( 'NONE',  ( 3.188603428895543601, -2.074531711476882201, -0.3615289903074799249 ) ) ;
#151187=CARTESIAN_POINT ( 'NONE',  ( 6.977413160773116019, -0.1420559494431029579, 1.829748798152310174 ) ) ;
#151193=CARTESIAN_POINT ( 'NONE',  ( 1.230900525853476868, 1.420129835883350955, -1.575055732827963295 ) ) ;
#151196=CARTESIAN_POINT ( 'NONE',  ( 4.844172697165038066, -0.9265620464425131653, 1.729294158640543699 ) ) ;
#151197=CARTESIAN_POINT ( 'NONE',  ( 3.731458613173586514, -1.998165266068991253, 0.8252760040215676440 ) ) ;
#151198=CARTESIAN_POINT ( 'NONE',  ( 1.856743374925871715, 0.3135980649527739250, -1.814175028193690808 ) ) ;
#151201=CARTESIAN_POINT ( 'NONE',  ( 4.892389968643020559, 1.444305832375993637, -0.9706037289107912747 ) ) ;
#151206=CARTESIAN_POINT ( 'NONE',  ( 1.604591590977550108, -0.7782141685120853580, -2.016947388195994062 ) ) ;
#151207=CARTESIAN_POINT ( 'NONE',  ( 3.514999820297697308, 2.016288306963448296, 0.002811503506894295987 ) ) ;
#151209=CARTESIAN_POINT ( 'NONE',  ( 1.587033755777764510, -0.3173376132806354222, -2.138153673666403964 ) ) ;
#151211=CARTESIAN_POINT ( 'NONE',  ( 3.608241331778249350, -0.7978255515562487910, -1.802987302761626998 ) ) ;
#151212=CARTESIAN_POINT ( 'NONE',  ( 6.609000000000019526, 4.695354556932705314, 2.562644781943986150 ) ) ;
#151213=CARTESIAN_POINT ( 'NONE',  ( 3.157691648149099972, 0.8757969000599256093, 1.733462199761313993 ) ) ;
#151219=CARTESIAN_POINT ( 'NONE',  ( -0.1106856583841242386, 7.629137130509040965, -2.596956429031356262 ) ) ;
#151224=CARTESIAN_POINT ( 'NONE',  ( 6.809642309899604840, -0.5188996100353564511, 2.257106211077652969 ) ) ;
#151226=CARTESIAN_POINT ( 'NONE',  ( 4.504711789546460565, 0.5192035298374733099, 1.891763301562799260 ) ) ;
#151227=CARTESIAN_POINT ( 'NONE',  ( 1.248672897702383988, 1.986100274556975354, -0.3474695496914689818 ) ) ;
#151229=CARTESIAN_POINT ( 'NONE',  ( 3.538375268227810011, 0.7659831068804138221, 1.974087397274668643 ) ) ;
#151233=CARTESIAN_POINT ( 'NONE',  ( 2.642321604431462578, -1.530645349967133972, 1.022873098850234141 ) ) ;
#151237=CARTESIAN_POINT ( 'NONE',  ( 5.238584497427841491, 1.261362679698872169, -1.704546977916908457 ) ) ;
#151240=CARTESIAN_POINT ( 'NONE',  ( 5.923136198411797615, -0.05496255519776967885, 2.060232511946280098 ) ) ;
#151241=CARTESIAN_POINT ( 'NONE',  ( 0.3614606035443160836, -0.5022670859271642918, 1.791915111541013461 ) ) ;
#151242=CARTESIAN_POINT ( 'NONE',  ( 2.331387312403776946, 0.8663521307504215008, -1.624669977836174839 ) ) ;
#151247=EDGE_CURVE ( 'NONE', #111149, #21772, #175637, .T. ) ;
#151248=CARTESIAN_POINT ( 'NONE',  ( 2.034064749695370100, -1.442962035976073309, -1.669870808145665020 ) ) ;
#151249=CARTESIAN_POINT ( 'NONE',  ( 4.938899882951366394, 0.3800905753248150498, 2.230106783295758177 ) ) ;
#151251=CARTESIAN_POINT ( 'NONE',  ( 4.834136970758627250, -0.9753174380719393799, -1.526440946957215994 ) ) ;
#151252=CARTESIAN_POINT ( 'NONE',  ( 4.469893758321111576, -0.8975064867107468425, 1.692437687186749917 ) ) ;
#151254=CARTESIAN_POINT ( 'NONE',  ( 4.082859939823464401, -0.1922352567787863620, -1.962060651276048118 ) ) ;
#151255=CARTESIAN_POINT ( 'NONE',  ( 4.803500792215161574, -0.4985019455652460740, 1.802925825644098534 ) ) ;
#151256=CARTESIAN_POINT ( 'NONE',  ( 5.301151097710674165, -1.596257866726397134, 0.9565186216247966167 ) ) ;
#151258=CARTESIAN_POINT ( 'NONE',  ( 0.1457207355009884908, 1.993892511249679034, -0.3006540981884687214 ) ) ;
#151260=CARTESIAN_POINT ( 'NONE',  ( 2.297617436792959378, 1.628516202021938808, 1.335460665606647446 ) ) ;
#151263=CARTESIAN_POINT ( 'NONE',  ( 0.07479286986305369589, 1.387406912293275729, -2.112587013352088317 ) ) ;
#151264=CARTESIAN_POINT ( 'NONE',  ( 2.900754761704402274, -2.089926006748676457, -0.3584049868644647585 ) ) ;
#151266=CARTESIAN_POINT ( 'NONE',  ( 1.652609354460622626, 1.998416004623180697, 0.2920258124684270706 ) ) ;
#151270=CARTESIAN_POINT ( 'NONE',  ( 1.599129061979026822, 1.768144091905754500, -1.243190488262067683 ) ) ;
#151271=CARTESIAN_POINT ( 'NONE',  ( 6.890000000000001457, 2.439643239904603966, 2.382311923195524095 ) ) ;
#151280=CARTESIAN_POINT ( 'NONE',  ( 1.013517375116283592, -2.137022957946862700, 0.4851717564131745597 ) ) ;
#151282=CARTESIAN_POINT ( 'NONE',  ( 1.095004809772756493, -0.5519004177921453813, -2.194067758203117169 ) ) ;
#151289=CARTESIAN_POINT ( 'NONE',  ( 4.318794280271901265, 1.578467719028648686, 0.6958846415187101009 ) ) ;
#151291=CARTESIAN_POINT ( 'NONE',  ( 2.319294515261476342, -1.717818424975267932, 0.4250260156472511208 ) ) ;
#151292=CARTESIAN_POINT ( 'NONE',  ( 3.000642180831034622, -1.983674057915509881, -0.3420062109290455954 ) ) ;
#151293=CARTESIAN_POINT ( 'NONE',  ( 4.893709131440695081, 1.632385321431808256, 1.485157849447714451 ) ) ;
#151295=CARTESIAN_POINT ( 'NONE',  ( 4.728773938389556619, 1.389870793851749164, -1.465793203850384030 ) ) ;
#151297=CARTESIAN_POINT ( 'NONE',  ( 5.360953910674266965, -0.05231296482399727665, -2.015913715532565043 ) ) ;
#151298=CARTESIAN_POINT ( 'NONE',  ( 4.535318187750695174, -0.08185482751379420663, 1.809849901470663491 ) ) ;
#151301=CARTESIAN_POINT ( 'NONE',  ( 3.080767038946086611, -0.1360980058115155988, -1.865751385159146070 ) ) ;
#151303=CARTESIAN_POINT ( 'NONE',  ( 2.144650067465687648, 1.855875215511919363, 0.4610605321611755958 ) ) ;
#151308=B_SPLINE_CURVE_WITH_KNOTS ( 'NONE', 3,
 ( #72737, #58634, #5573, #87932, #26120, #189691, #171308, #22902, #154006, #6660, #25055 ),
 .UNSPECIFIED., .F., .F.,
 ( 4, 1, 1, 1, 1, 1, 1, 1, 4 ),
 ( 0.000000000000000000, 0.2256337125576066971, 0.3978389261578171299, 0.5257960283851228489, 0.6187025735204009225, 0.6856790771877526725, 0.7354782194756434022, 0.7762620033627533056, 0.9999999999999998890 ),
 .UNSPECIFIED. ) ;
#151310=CARTESIAN_POINT ( 'NONE',  ( -0.1229892814952095459, -1.709044814581164973, -0.8582256167319822771 ) ) ;
#151312=CARTESIAN_POINT ( 'NONE',  ( 1.258172656280614365, -1.962046632281065461, -0.003472340283867945618 ) ) ;
#151315=CARTESIAN_POINT ( 'NONE',  ( 5.590118541908202232, 1.264772504208915072, 1.701965355810124203 ) ) ;
#151318=CARTESIAN_POINT ( 'NONE',  ( 5.132083838642755858, 1.015972595308231474, -1.689280876731833470 ) ) ;
#151320=CARTESIAN_POINT ( 'NONE',  ( 0.7033859027741823366, 1.773467923640878796, -0.9528479892364212223 ) ) ;
#151322=CARTESIAN_POINT ( 'NONE',  ( 1.423615893443540337, -1.536295912932123642, -1.457111741773434943 ) ) ;
#151324=CARTESIAN_POINT ( 'NONE',  ( 2.629418614236479712, 0.1040367438073786233, -2.067886086930009970 ) ) ;
#151328=CARTESIAN_POINT ( 'NONE',  ( 4.734370563723459213, 0.3569306294452011530, 2.059774728693287038 ) ) ;
#151330=CARTESIAN_POINT ( 'NONE',  ( 3.170728842436408179, -1.686227525993441834, -0.7000332573987508855 ) ) ;
#151331=CARTESIAN_POINT ( 'NONE',  ( 2.701584635150193314, 1.282363399140455273, 1.279706459777726346 ) ) ;
#151336=CARTESIAN_POINT ( 'NONE',  ( 4.805825877545530922, -0.5924843665619135002, 2.125676689404366826 ) ) ;
#151338=CARTESIAN_POINT ( 'NONE',  ( 3.598220562318912741, -0.9401235635465958751, 1.665135908046413871 ) ) ;
#151342=CARTESIAN_POINT ( 'NONE',  ( 6.496543107701719499, 2.047251205643263017, 0.3077783505985449142 ) ) ;
#151345=EDGE_CURVE ( 'NONE', #200465, #33823, #123764, .T. ) ;
#151350=CARTESIAN_POINT ( 'NONE',  ( 3.338976900156843453, -1.651226333174139693, 0.8788041501476551165 ) ) ;
#151357=CARTESIAN_POINT ( 'NONE',  ( 6.965700764728601335, -0.4599482372066622249, 2.025938098699997525 ) ) ;
#151359=CARTESIAN_POINT ( 'NONE',  ( 1.335564786618839817, 0.5826355126458090394, -1.930425043884366865 ) ) ;
#151362=CARTESIAN_POINT ( 'NONE',  ( 1.799034956846547795, 1.823213324544867397, 1.215573211712846158 ) ) ;
#151363=CARTESIAN_POINT ( 'NONE',  ( 6.533835636172961259, -1.196796279342365210, -1.378804128639096849 ) ) ;
#151371=CARTESIAN_POINT ( 'NONE',  ( 3.386116603743833497, -0.3623624896987759914, -1.805063595765175499 ) ) ;
#151372=CARTESIAN_POINT ( 'NONE',  ( 0.1705643940957324023, 0.7724326726834315204, 1.859191304955130297 ) ) ;
#151373=CARTESIAN_POINT ( 'NONE',  ( 2.495865491978021211, 2.229134443137513966, 0.5594839687708874632 ) ) ;
#151375=CARTESIAN_POINT ( 'NONE',  ( 0.4966286816309881114, 0.3102001241638470685, 1.834739031104109408 ) ) ;
#151379=CARTESIAN_POINT ( 'NONE',  ( 5.027564050633359649, -0.2746679736120913318, 1.892429487827557599 ) ) ;
#151383=CARTESIAN_POINT ( 'NONE',  ( 4.142189164857057015, 0.5595570048471016911, 2.014385595549014418 ) ) ;
#151384=CARTESIAN_POINT ( 'NONE',  ( 2.483090063216564669, 1.711211315118581711, -0.7561169667836544761 ) ) ;
#151387=CARTESIAN_POINT ( 'NONE',  ( 3.227794649281841011, 1.698692639566254936, 0.3781252810216747529 ) ) ;
#151391=CARTESIAN_POINT ( 'NONE',  ( 3.949580097687496405, 0.5788178622721011912, -1.624998464860913705 ) ) ;
#151393=CARTESIAN_POINT ( 'NONE',  ( 3.737968522918270864, 2.181131050170285857, 0.2133239450496857148 ) ) ;
#151394=CARTESIAN_POINT ( 'NONE',  ( 6.147136880733683917, -1.866598994669689926, 1.177069016086537356 ) ) ;
#151396=CARTESIAN_POINT ( 'NONE',  ( 3.450208493196211812, -0.8844140035146315082, 1.982955601465713258 ) ) ;
#151397=CARTESIAN_POINT ( 'NONE',  ( 1.963248404482214049, 0.3131683437365209710, -1.798463397695612809 ) ) ;
#151399=CARTESIAN_POINT ( 'NONE',  ( 6.139883455347572294, 2.111525295599859575, -0.1581134299761654260 ) ) ;
#151401=CARTESIAN_POINT ( 'NONE',  ( 5.460555387939631800, -2.071112900911156185, -0.9828140750258400615 ) ) ;
#151404=CARTESIAN_POINT ( 'NONE',  ( 0.9969211937387794098, -2.069638562867767373, -0.4609060192823294932 ) ) ;
#151410=CARTESIAN_POINT ( 'NONE',  ( 1.120143885658178906, -0.5347273011463581360, 2.155877112962206965 ) ) ;
#151412=CARTESIAN_POINT ( 'NONE',  ( 6.557263107265463020, -1.238491779027944162, 1.591905563659588907 ) ) ;
#151414=CARTESIAN_POINT ( 'NONE',  ( 4.979373296276208727, -0.1066085398311214100, 2.059958923327874114 ) ) ;
#151420=CARTESIAN_POINT ( 'NONE',  ( 0.3399330434069799400, 2.085199349320911555, 0.1515528320938461238 ) ) ;
#151421=CARTESIAN_POINT ( 'NONE',  ( 4.676407821165474488, 1.496050514612049742, 1.352155788975975437 ) ) ;
#151422=CARTESIAN_POINT ( 'NONE',  ( 4.018977146631536712, -1.760761141180338774, 0.5383908109771737838 ) ) ;
#151424=CARTESIAN_POINT ( 'NONE',  ( 0.6567381767516925484, -1.453278249834984326, -0.9285724537800400524 ) ) ;
#151425=CARTESIAN_POINT ( 'NONE',  ( 0.4445464637146990250, -1.457232572767804379, 1.394089106691732693 ) ) ;
#151426=CARTESIAN_POINT ( 'NONE',  ( 1.214008909562364069, 2.217199183031343779, 0.6065299581617057401 ) ) ;
#151428=CARTESIAN_POINT ( 'NONE',  ( 1.071959817704574602, 2.180298862187507680, -0.6038346756046736319 ) ) ;
#151429=CARTESIAN_POINT ( 'NONE',  ( 3.317110013156245873, 1.904127318671836600, 0.9001942471269042123 ) ) ;
#151433=CARTESIAN_POINT ( 'NONE',  ( 0.000000000000000000, 4.569466175184296652, -2.600000000000000533 ) ) ;
#151439=CARTESIAN_POINT ( 'NONE',  ( 4.992532747203591192, -1.233408671777506349, 1.847344450390429937 ) ) ;
#151440=CARTESIAN_POINT ( 'NONE',  ( 3.556733441538503016, -1.932615445784117369, -1.033156731641969195 ) ) ;
#151443=CARTESIAN_POINT ( 'NONE',  ( 5.389097038490845648, 0.1425914310585977562, 1.956722230749983193 ) ) ;
#151445=CARTESIAN_POINT ( 'NONE',  ( 6.889999999999973035, 7.629137130509064946, 2.879999999999991456 ) ) ;
#151448=CARTESIAN_POINT ( 'NONE',  ( 4.922192346260840345, -2.110166376318895587, 0.2103620946037400852 ) ) ;
#151452=CARTESIAN_POINT ( 'NONE',  ( 6.684453901184132185, -2.118919246787358102, -0.4271090584619871566 ) ) ;
#151454=CARTESIAN_POINT ( 'NONE',  ( 5.636236351835953506, 0.3653394402399374741, 1.804471444190151930 ) ) ;
#151457=CARTESIAN_POINT ( 'NONE',  ( 1.083124124047912362, -0.7835505874942759741, 1.554128773191378432 ) ) ;
#151461=CARTESIAN_POINT ( 'NONE',  ( 5.823154874416164084, -0.05760400987671504547, 2.161107263091876618 ) ) ;
#151466=CARTESIAN_POINT ( 'NONE',  ( 4.487301133948972343, 1.932317252032596633, -0.9692046190768679459 ) ) ;
#151468=CARTESIAN_POINT ( 'NONE',  ( 4.587161778375014265, 1.762195453814468182, -0.8837856115832108950 ) ) ;
#151469=CARTESIAN_POINT ( 'NONE',  ( 4.376141123711778214, -0.2964218048276610618, 1.708115672221988346 ) ) ;
#151470=CARTESIAN_POINT ( 'NONE',  ( 1.118978350340808614, -0.04878210919301298465, 2.191179638975069732 ) ) ;
#151471=CARTESIAN_POINT ( 'NONE',  ( 2.186954941700581134, -2.263197366206463279, -0.4496495349725088686 ) ) ;
#151472=CARTESIAN_POINT ( 'NONE',  ( 4.798151449762615428, -2.060242214822493256, -0.05457638173838111340 ) ) ;
#151473=CARTESIAN_POINT ( 'NONE',  ( 0.3220787244772654323, 1.858110058275804111, 0.5644625801373166496 ) ) ;
#151479=CARTESIAN_POINT ( 'NONE',  ( 1.283827520628720187, 1.646837967535810021, -1.163270716046126196 ) ) ;
#151481=CARTESIAN_POINT ( 'NONE',  ( 3.399657359236216703, 1.738403758043248759, 1.359216269546263511 ) ) ;
#151483=CARTESIAN_POINT ( 'NONE',  ( 1.182201811662712210, 1.114302846955270709, -1.490276101724023583 ) ) ;
#151489=CARTESIAN_POINT ( 'NONE',  ( 6.667912628260062036, -1.128459271250933149, 1.455361883854713767 ) ) ;
#151491=CARTESIAN_POINT ( 'NONE',  ( 2.852473085487742477, 0.6931051061056427987, 1.940986274177344706 ) ) ;
#151494=CARTESIAN_POINT ( 'NONE',  ( 2.367837350726550660, 0.5366352218779540939, -1.947015567076612941 ) ) ;
#151497=CARTESIAN_POINT ( 'NONE',  ( 1.745067373267340960, -1.741593738584124695, 1.101550882630119244 ) ) ;
#151500=AXIS2_PLACEMENT_3D ( 'NONE', #108242, #174265, #158008 ) ;
#151501=CARTESIAN_POINT ( 'NONE',  ( -0.1408020194050328411, 7.629137130509059617, -2.700278568655100742 ) ) ;
#151502=CARTESIAN_POINT ( 'NONE',  ( 5.110101661328442901, -2.196521081226535443, 0.2136625748923453583 ) ) ;
#151504=CARTESIAN_POINT ( 'NONE',  ( 1.862795570070171713, -1.530026953448139659, 1.527182012981804560 ) ) ;
#151506=CARTESIAN_POINT ( 'NONE',  ( 2.184780103950241248, 1.616692242240840960, -1.205043568535242304 ) ) ;
#151509=CARTESIAN_POINT ( 'NONE',  ( 2.232162068744643069, -2.100961912546659871, -0.9323289839222002051 ) ) ;
#151513=CARTESIAN_POINT ( 'NONE',  ( 1.850267049257280139, 0.5840378008528935849, 1.777222254475477659 ) ) ;
#151514=CARTESIAN_POINT ( 'NONE',  ( 3.714077560468319827, 1.074663192196689376, -1.706111893292367343 ) ) ;
#151518=CARTESIAN_POINT ( 'NONE',  ( 5.444006973519509351, 0.8546016068469390881, -1.925070404590538242 ) ) ;
#151522=CARTESIAN_POINT ( 'NONE',  ( 5.326427914677607234, -0.9117507067677769195, -1.802394291917883473 ) ) ;
#151524=CARTESIAN_POINT ( 'NONE',  ( 1.305618366820593179, -1.623578218988607658, -1.271935013979957452 ) ) ;
#151532=CARTESIAN_POINT ( 'NONE',  ( 3.402935010178400166, 0.5245792999575286109, 2.106750930608875194 ) ) ;
#151535=CARTESIAN_POINT ( 'NONE',  ( 1.680954830071922812, 1.270413995023990106, 1.332975479855981416 ) ) ;
#151537=CARTESIAN_POINT ( 'NONE',  ( 4.599289333468261631, -0.5842463895667610041, 2.112197083089427885 ) ) ;
#151538=CARTESIAN_POINT ( 'NONE',  ( 6.883263157960403333, 6.034387817901857964, 2.748704107105720773 ) ) ;
#151539=CARTESIAN_POINT ( 'NONE',  ( 4.821284755203490313, -0.1158696699916968720, 2.259674544810440278 ) ) ;
#151547=CARTESIAN_POINT ( 'NONE',  ( 5.659369745216535463, 0.3440881560464129629, -1.735765479537496603 ) ) ;
#151549=CARTESIAN_POINT ( 'NONE',  ( 1.413257319143443658, 1.857191001717144685, 0.9929431703323916558 ) ) ;
#151552=CARTESIAN_POINT ( 'NONE',  ( 1.504289420374326447, 1.967163215448018088, 0.09980459116839916767 ) ) ;
#151556=CARTESIAN_POINT ( 'NONE',  ( 0.4495626703563436743, 1.451167377975391304, 1.320406988977901985 ) ) ;
#151557=CARTESIAN_POINT ( 'NONE',  ( 6.521734044569575062, -0.3839667898355834663, 1.776778520094610903 ) ) ;
#151562=CARTESIAN_POINT ( 'NONE',  ( 6.244977087980838171, -1.579202250953464670, 1.002420361074819688 ) ) ;
#151565=CARTESIAN_POINT ( 'NONE',  ( 5.366107254901441692, -2.060797467674013284, 0.1973761227843511823 ) ) ;
#151576=CARTESIAN_POINT ( 'NONE',  ( 5.301206097546149465, -1.683542251207278628, 1.007010407901312465 ) ) ;
#151578=CARTESIAN_POINT ( 'NONE',  ( 3.532577226125938274, 1.967586357134976094, -0.4389627639644277934 ) ) ;
#151579=CARTESIAN_POINT ( 'NONE',  ( 2.712013535993620383, 1.060242027361221862, -1.595356271853585195 ) ) ;
#151581=CARTESIAN_POINT ( 'NONE',  ( 0.7674258922165803076, 2.110627382301712540, -0.5898035449652740958 ) ) ;
#151582=CARTESIAN_POINT ( 'NONE',  ( 0.2335667940002502385, 6.947499997881678269, -2.748442024765639147 ) ) ;
#151583=CARTESIAN_POINT ( 'NONE',  ( 2.741296213614560440, -1.383352855433259698, -1.259238407996167153 ) ) ;
#151587=CARTESIAN_POINT ( 'NONE',  ( 4.253586407750776566, 2.053249321966661434, -0.5160394917872836995 ) ) ;
#151589=CARTESIAN_POINT ( 'NONE',  ( 6.285608408418759119, -1.950803066209889636, 0.6937918898708083093 ) ) ;
#151590=CARTESIAN_POINT ( 'NONE',  ( 1.364907732811880159, 0.1502005422731657047, -2.085395908040136526 ) ) ;
#151591=CARTESIAN_POINT ( 'NONE',  ( 6.720655732516676473, 3.678797444539682271, 2.787578482799071278 ) ) ;
#151592=CARTESIAN_POINT ( 'NONE',  ( 0.2172357734837098431, -1.693002290532450882, 0.3285655886510214230 ) ) ;
#151600=CARTESIAN_POINT ( 'NONE',  ( 0.02954414540562703972, -1.776926038569931254, 0.3510683431443075153 ) ) ;
#151608=CARTESIAN_POINT ( 'NONE',  ( 5.677361293727043901, 1.528752376640944100, 1.314985542479940817 ) ) ;
#151609=CARTESIAN_POINT ( 'NONE',  ( 0.3289748556246674394, 1.459166701075472750, -1.538843095060193233 ) ) ;
#151613=CARTESIAN_POINT ( 'NONE',  ( 0.1405533004714617507, 0.6596865332844923380, -2.358301179948574244 ) ) ;
#151617=CARTESIAN_POINT ( 'NONE',  ( 3.801571140118775727, -1.488283618643148287, -1.289908803443328145 ) ) ;
#151619=CARTESIAN_POINT ( 'NONE',  ( 1.594549238318817785, -1.131586138893545979, 1.793127659086241499 ) ) ;
#151623=CARTESIAN_POINT ( 'NONE',  ( 5.701184558104195332, -0.5354452791076976803, 2.124913622581547479 ) ) ;
#151625=CARTESIAN_POINT ( 'NONE',  ( 4.489231697071988769, 1.720940496173857470, -0.8657641181536148700 ) ) ;
#151628=CARTESIAN_POINT ( 'NONE',  ( -0.1294898018152357000, 1.363479816416721446, -2.179679775322340696 ) ) ;
#151629=CARTESIAN_POINT ( 'NONE',  ( 0.8739773845415177433, 2.125910683164092152, -0.5920798734769525673 ) ) ;
#151630=DIRECTION ( 'NONE',  ( -3.451266460341926649E-31, -5.200010849845536803E-32, 1.000000000000000000 ) ) ;
#151634=CARTESIAN_POINT ( 'NONE',  ( 5.787944378201490103, -1.246615054290018065, -1.524717904608218877 ) ) ;
#151635=CARTESIAN_POINT ( 'NONE',  ( 0.7670095293261131042, 1.871311197688549699, -0.5191222856946677844 ) ) ;
#151636=CARTESIAN_POINT ( 'NONE',  ( 6.028750418185333082, 2.265939813929934488, -0.3841603865788502103 ) ) ;
#151638=CARTESIAN_POINT ( 'NONE',  ( 4.065176880270331417, 1.594224420893322725, 0.9597675150698461444 ) ) ;
#151643=CARTESIAN_POINT ( 'NONE',  ( 0.7147126110796617748, 2.027027023440019171, 0.8336157706642086662 ) ) ;
#151648=CARTESIAN_POINT ( 'NONE',  ( 0.8733498553583609603, 1.760202786292342170, -0.4843115980177821744 ) ) ;
#151650=CARTESIAN_POINT ( 'NONE',  ( 2.953449220662739183, -1.603453536992532902, -0.6609773998737851208 ) ) ;
#151654=CARTESIAN_POINT ( 'NONE',  ( 5.531824841778981927, -1.161409778037244100, -1.408645805323349487 ) ) ;
#151655=CARTESIAN_POINT ( 'NONE',  ( 3.309375504473045293, -1.601080850277468937, -1.133301831143386007 ) ) ;
#151660=CARTESIAN_POINT ( 'NONE',  ( 4.723349490952149843, 1.845327050471495367, 1.044454997443218236 ) ) ;
#151663=CARTESIAN_POINT ( 'NONE',  ( 3.362232293424003426, -2.068089847843882279, 0.09686330349460009481 ) ) ;
#151667=CARTESIAN_POINT ( 'NONE',  ( 4.319114520555938697, 1.717138752081597719, -1.409087234901666763 ) ) ;
#151669=CARTESIAN_POINT ( 'NONE',  ( 3.428665021107531352, -1.741954984014550512, -1.499980572608774043 ) ) ;
#151676=CARTESIAN_POINT ( 'NONE',  ( 3.638835171272115421, 1.817485770107383436, 0.5952672491930725007 ) ) ;
#151678=CARTESIAN_POINT ( 'NONE',  ( 4.541862270049739969, 0.7358753100316551832, -1.560062421326340987 ) ) ;
#151679=CARTESIAN_POINT ( 'NONE',  ( 3.837125247982266174, -1.679222704393277921, -1.116210984008485507 ) ) ;
#151680=CARTESIAN_POINT ( 'NONE',  ( 3.762538640753902097, 2.164199696370266324, -0.7750164773838670307 ) ) ;
#151682=CARTESIAN_POINT ( 'NONE',  ( 6.164693330894345458, -1.490570670011469812, 1.488127047250583201 ) ) ;
#151685=CARTESIAN_POINT ( 'NONE',  ( 4.446413189832159496, 0.4709973186826624802, 1.705850592114676489 ) ) ;
#151687=CARTESIAN_POINT ( 'NONE',  ( 0.9027369068667027152, 1.732534852245724233, -1.501034128341944607 ) ) ;
#151688=CARTESIAN_POINT ( 'NONE',  ( 0.1634481287224815171, -1.141006008805772298, 1.314205411033820381 ) ) ;
#151691=CARTESIAN_POINT ( 'NONE',  ( 6.597619724345276104, -2.191060131252516641, 0.04951108399064289151 ) ) ;
#151696=CARTESIAN_POINT ( 'NONE',  ( 6.830528382861658088, -1.277203763263988101, 1.630111558092485868 ) ) ;
#151697=CARTESIAN_POINT ( 'NONE',  ( 1.235564962061060257, 0.5807501988173838781, -1.931125984888550473 ) ) ;
#151699=CARTESIAN_POINT ( 'NONE',  ( 5.936148346467474468, 0.9475192508551170123, -1.677314091114836980 ) ) ;
#151701=CARTESIAN_POINT ( 'NONE',  ( 1.178328164221422503, 2.187401300010451077, -0.3865082640040794493 ) ) ;
#151708=CARTESIAN_POINT ( 'NONE',  ( 0.02680830797223074380, 7.629137130509076492, -2.410890733638766825 ) ) ;
#151710=CARTESIAN_POINT ( 'NONE',  ( 4.845099162036492046, 0.5397016130457911176, -1.654733517006673482 ) ) ;
#151711=CARTESIAN_POINT ( 'NONE',  ( 1.978885927095444863, 1.829411362569667743, 0.7090815385668995940 ) ) ;
#151716=CARTESIAN_POINT ( 'NONE',  ( 6.848121815800094936, -0.8396676627679277027, 1.771385694100804375 ) ) ;
#151719=CARTESIAN_POINT ( 'NONE',  ( 1.147787885906520033, -1.784999543274916611, -1.390116309797536864 ) ) ;
#151722=CARTESIAN_POINT ( 'NONE',  ( 1.545950201917587696, 1.868165254341861647, 0.09716206808172561660 ) ) ;
#151723=CARTESIAN_POINT ( 'NONE',  ( 0.8087042982808723135, 1.034539495461658465, -1.391586887084266921 ) ) ;
#151724=CARTESIAN_POINT ( 'NONE',  ( 5.372676843235411503, -0.05303982195071360595, -2.191091664329389399 ) ) ;
#151725=CARTESIAN_POINT ( 'NONE',  ( 6.071339422564090427, 0.1780416842499404351, -2.300786051158403733 ) ) ;
#151726=CARTESIAN_POINT ( 'NONE',  ( 1.270465292308793126, -1.308197635955485216, 1.592426268366262665 ) ) ;
#151727=CARTESIAN_POINT ( 'NONE',  ( 3.415898659897542267, 1.231191954956109447, -1.501781470047100386 ) ) ;
#151729=CARTESIAN_POINT ( 'NONE',  ( 5.975831987570860981, 1.113884111790110820, 1.502598383168303409 ) ) ;
#151732=CARTESIAN_POINT ( 'NONE',  ( 6.591172692507557329, 1.163088239368128773, -1.646588791553056152 ) ) ;
#151735=CARTESIAN_POINT ( 'NONE',  ( 5.133435478496918947, 0.5880181904946503169, 1.928752423557971829 ) ) ;
#151738=CARTESIAN_POINT ( 'NONE',  ( 1.717148762710469789, -0.2249250470785572054, 1.811706739299999924 ) ) ;
#151747=CARTESIAN_POINT ( 'NONE',  ( 5.953772690328709594, -1.464304757327790973, -1.391265315224277099 ) ) ;
#151748=CARTESIAN_POINT ( 'NONE',  ( 0.3289748556246673838, 1.459166701075472750, -1.538843095060193233 ) ) ;
#151752=CARTESIAN_POINT ( 'NONE',  ( 5.032131441678504125, 1.061211460345131252, -1.766520746938464947 ) ) ;
#151753=CARTESIAN_POINT ( 'NONE',  ( 4.693982515131527755, 1.755768268644173791, 0.9914009648221073778 ) ) ;
#151763=CARTESIAN_POINT ( 'NONE',  ( 4.868517441940229951, -0.5404072756688071966, 1.942244311778835719 ) ) ;
#151764=CARTESIAN_POINT ( 'NONE',  ( 3.978315823851843014, -0.1823813840945518738, -1.832081410093854501 ) ) ;
#151766=CARTESIAN_POINT ( 'NONE',  ( 1.858496626375233163, 2.301273984257983241, -0.1728945724901974068 ) ) ;
#151768=CARTESIAN_POINT ( 'NONE',  ( 4.675171183009182663, 0.005162144975975196948, -2.161773191939574179 ) ) ;
#151770=CARTESIAN_POINT ( 'NONE',  ( 0.06387186515662347797, -1.267698835582967476, 1.471343342715900615 ) ) ;
#151774=CARTESIAN_POINT ( 'NONE',  ( 3.133525119713890472, -1.255248497922526463, -1.387151338369890574 ) ) ;
#151775=CARTESIAN_POINT ( 'NONE',  ( 6.666873957964818409, -1.802346848367493592, -0.7993007979140465125 ) ) ;
#151778=CARTESIAN_POINT ( 'NONE',  ( 1.577102763248950046, -2.096353118739826993, -0.6898709473643764856 ) ) ;
#151783=CARTESIAN_POINT ( 'NONE',  ( 6.719606758044225359, -1.912400718708512581, 0.4786219606899063117 ) ) ;
#151784=CARTESIAN_POINT ( 'NONE',  ( 6.235062949421072531, 0.2195253172713066969, 2.297251706954360095 ) ) ;
#151785=CARTESIAN_POINT ( 'NONE',  ( 6.795359140062033454, -1.661660808857531313, 0.8381669064597346841 ) ) ;
#151786=CARTESIAN_POINT ( 'NONE',  ( 3.889554661416291026, -1.907601829641421887, 0.7848441205193229520 ) ) ;
#151794=CARTESIAN_POINT ( 'NONE',  ( 6.812935010865087015, -1.682745870255862641, 1.371614790115786908 ) ) ;
#151796=CARTESIAN_POINT ( 'NONE',  ( 5.847170753249844033, 0.5281823367668266878, -1.763884204139199330 ) ) ;
#151799=CARTESIAN_POINT ( 'NONE',  ( 1.334983872447586650, -1.693447605269988276, 0.7947349781701129601 ) ) ;
#151806=CARTESIAN_POINT ( 'NONE',  ( 1.611815888142430264, -0.6431676737995162263, 1.801018335096972400 ) ) ;
#151807=CARTESIAN_POINT ( 'NONE',  ( 2.658786778619155022, -1.538754371767250495, -0.8742638447295988380 ) ) ;
#151808=CARTESIAN_POINT ( 'NONE',  ( 6.463545146426397991, -1.618288576614915764, -1.197193900782191234 ) ) ;
#151810=CARTESIAN_POINT ( 'NONE',  ( 4.060093344861609665, -1.099912525845229583, 1.568156085375242093 ) ) ;
#151812=CARTESIAN_POINT ( 'NONE',  ( 5.740667673349629574, -1.921128208576441843, -0.4332487841941043971 ) ) ;
#151813=CARTESIAN_POINT ( 'NONE',  ( 0.5805319366703353134, 1.050441701016215923, 1.842106252469346117 ) ) ;
#151815=CARTESIAN_POINT ( 'NONE',  ( 4.346470048663173102, 0.4987854378066917116, 1.802870001028591407 ) ) ;
#151816=CARTESIAN_POINT ( 'NONE',  ( 5.777914075412113881, 1.032862044635925569, 1.381300780159310460 ) ) ;
#151818=CARTESIAN_POINT ( 'NONE',  ( 3.932405576212230525, 1.181341412803040614, -1.863887651898883613 ) ) ;
#151821=CARTESIAN_POINT ( 'NONE',  ( 1.240767406152184282, -2.011986688465472906, -0.4537849334574247107 ) ) ;
#151829=CARTESIAN_POINT ( 'NONE',  ( 3.297389726143421740, -1.827171938055579536, 0.9735347560282039403 ) ) ;
#151833=CARTESIAN_POINT ( 'NONE',  ( 1.401042149647635071, -0.2984598639739938220, -1.997379878556293731 ) ) ;
#151835=CARTESIAN_POINT ( 'NONE',  ( 0.07479286986305369589, 4.095183424177953668, -2.410510762676120411 ) ) ;
#151837=CARTESIAN_POINT ( 'NONE',  ( 6.274767501101933043, -2.001204493855372579, 0.2439949869823473949 ) ) ;
#151838=CARTESIAN_POINT ( 'NONE',  ( 5.964071289222036221, -1.018598136897935547, 1.622275196354412419 ) ) ;
#151839=CARTESIAN_POINT ( 'NONE',  ( 4.300438532332786501, 1.693616701070689956, -1.390861761948622544 ) ) ;
#151841=CARTESIAN_POINT ( 'NONE',  ( 3.709155072767254424, 1.612916391665040194, -1.027221078234448859 ) ) ;
#151845=CARTESIAN_POINT ( 'NONE',  ( 0.4918148228068714989, -2.006445053647107013, 0.2004575690456936732 ) ) ;
#151848=CARTESIAN_POINT ( 'NONE',  ( 6.058177568126345669, -1.550975213528119623, 1.548612826651605712 ) ) ;
#151850=CARTESIAN_POINT ( 'NONE',  ( 4.172648073627690302, -1.609630772656017950, -0.6200716988599298540 ) ) ;
#151856=CARTESIAN_POINT ( 'NONE',  ( 1.469116868872882620, 1.728625619535430369, 0.9278086228877155950 ) ) ;
#151859=CARTESIAN_POINT ( 'NONE',  ( 0.1751657365761339624, 7.629137130509054288, -2.644001943226172102 ) ) ;
#151863=CARTESIAN_POINT ( 'NONE',  ( 3.896947601784990223, -0.1811674076915045506, -1.802394175579679958 ) ) ;
#151867=CARTESIAN_POINT ( 'NONE',  ( 5.408800935855493819, -0.4461688933581753336, -1.755527745762341718 ) ) ;
#151872=CARTESIAN_POINT ( 'NONE',  ( 4.633164157742322153, 0.0009153448507570947738, -1.861241882716960561 ) ) ;
#151874=CARTESIAN_POINT ( 'NONE',  ( 2.548326723280808892, -1.319200400300493570, 1.389225609306585119 ) ) ;
#151881=CARTESIAN_POINT ( 'NONE',  ( 0.5675189469334165349, 0.2105291993744831114, -2.151437729447757796 ) ) ;
#151884=CARTESIAN_POINT ( 'NONE',  ( 0.7447965706881398695, -1.568309060004613231, 0.9341869532639992535 ) ) ;
#151887=CARTESIAN_POINT ( 'NONE',  ( 2.362075219488588562, 0.7782009281872975803, 1.651537983114875763 ) ) ;
#151889=CARTESIAN_POINT ( 'NONE',  ( 3.139063269091638908, -0.1420806666206550495, -1.964468959564101613 ) ) ;
#151890=CARTESIAN_POINT ( 'NONE',  ( 3.755361975916061024, 1.927010760186953497, -0.2409419434407939486 ) ) ;
#151893=CARTESIAN_POINT ( 'NONE',  ( 4.517907016363444939, -0.5628432189327194912, 2.044499502628312371 ) ) ;
#151901=CARTESIAN_POINT ( 'NONE',  ( 4.230939532379584200, 0.09184734775685021724, 1.823503176236190626 ) ) ;
#151907=CARTESIAN_POINT ( 'NONE',  ( 4.768341783539651324, -1.221614081569386334, 1.416756073533788518 ) ) ;
#151909=CARTESIAN_POINT ( 'NONE',  ( 3.088414555603569145, -1.898068263532082245, -0.3288968790781700013 ) ) ;
#151910=CARTESIAN_POINT ( 'NONE',  ( 6.684431423333510480, 1.132142624513672091, -1.601896353945003071 ) ) ;
#151916=CARTESIAN_POINT ( 'NONE',  ( 1.722414120629287337, 2.094725599053618659, 0.3070382465363735158 ) ) ;
#151919=CARTESIAN_POINT ( 'NONE',  ( 6.157099584139436033, 1.695871835526874483, -1.187180358042688511 ) ) ;
#151920=CARTESIAN_POINT ( 'NONE',  ( 0.3449248370967008537, 0.5783895242766275979, -1.748133987124582012 ) ) ;
#151922=CARTESIAN_POINT ( 'NONE',  ( 5.942043047034061942, -1.969448396301001436, -1.185220976332189924 ) ) ;
#151925=CARTESIAN_POINT ( 'NONE',  ( 1.781587602986109742, 1.582980622272272653, 1.658122128702421261 ) ) ;
#151928=CARTESIAN_POINT ( 'NONE',  ( 5.648367429523982963, -1.529681991043756017, 1.196244224141077561 ) ) ;
#151930=CARTESIAN_POINT ( 'NONE',  ( 0.7912717950901988484, -0.05365516122857225123, -2.012662812414119706 ) ) ;
#151931=CARTESIAN_POINT ( 'NONE',  ( 6.350795928397162449, -1.845624747684541989, -0.8128223418941012968 ) ) ;
#151936=CARTESIAN_POINT ( 'NONE',  ( 2.765665077289869433, 1.118955468730401526, 1.765788254259098800 ) ) ;
#151937=CARTESIAN_POINT ( 'NONE',  ( 1.393014870165907526, 1.336991634843522236, 1.159753417114619545 ) ) ;
#151940=CARTESIAN_POINT ( 'NONE',  ( 4.593851424282248352, -2.291655481657675519, -0.05911330884650690953 ) ) ;
#151942=CARTESIAN_POINT ( 'NONE',  ( 3.169568575122613918, -1.035934168062458971, 1.398253053441183891 ) ) ;
#151946=CARTESIAN_POINT ( 'NONE',  ( 3.725721709451996322, -1.528540617003815383, -0.8183948105100163906 ) ) ;
#151947=CARTESIAN_POINT ( 'NONE',  ( 3.121698260611803999, 0.3212384671735257213, -2.147181447086630612 ) ) ;
#151950=CARTESIAN_POINT ( 'NONE',  ( 4.030482632556767975, 0.5424685788828055300, 1.942097399793737633 ) ) ;
#151951=CARTESIAN_POINT ( 'NONE',  ( 1.718750000000001554, -0.7852924748298989455, 1.895863743164124093 ) ) ;
#151953=CARTESIAN_POINT ( 'NONE',  ( 2.133698649363345190, -1.256510270340875035, -1.460289853754138445 ) ) ;
#151955=CARTESIAN_POINT ( 'NONE',  ( 4.307018013452124983, -0.4884699388765164074, -2.166881332863872522 ) ) ;
#151957=CARTESIAN_POINT ( 'NONE',  ( -0.1108833634137010582, 5.723767666350643601, -2.491012016648496363 ) ) ;
#151962=CARTESIAN_POINT ( 'NONE',  ( 0.8389114244844765311, 1.318684809372525857, -1.787403929136616165 ) ) ;
#151963=CARTESIAN_POINT ( 'NONE',  ( 6.109812101310618360, 0.5708666350849946891, -1.876949146916474298 ) ) ;
#151967=CARTESIAN_POINT ( 'NONE',  ( 6.731690493876715919, -1.469984723218084488, -1.719904613669322790 ) ) ;
#151970=CARTESIAN_POINT ( 'NONE',  ( 4.527816470857299436, 2.001556401900002058, -0.4979991880497411372 ) ) ;
#151974=CARTESIAN_POINT ( 'NONE',  ( 6.046149701670225696, 1.868418987705861234, 0.09211505606019491921 ) ) ;
#151975=CARTESIAN_POINT ( 'NONE',  ( 4.201623210320468260, 1.587898197979008774, 0.6974748919710629380 ) ) ;
#151976=CARTESIAN_POINT ( 'NONE',  ( 3.720004753662985664, 1.653986544816415494, 0.5419736716202552262 ) ) ;
#151977=CARTESIAN_POINT ( 'NONE',  ( 1.716775041481681585, 2.140780187006920077, 0.8202503203454788450 ) ) ;
#151979=CARTESIAN_POINT ( 'NONE',  ( 5.917543283689063571, -1.162172991910553010, -1.737764066907695915 ) ) ;
#151980=CARTESIAN_POINT ( 'NONE',  ( 6.404245030721173570, 1.437354257190478490, -1.306004427266238777 ) ) ;
#151983=CARTESIAN_POINT ( 'NONE',  ( 1.424454163599726320, -1.462446849824734274, -1.388484543128357229 ) ) ;
#151987=CARTESIAN_POINT ( 'NONE',  ( 2.948016456289838771, -1.425740979638410399, -1.569777838261996017 ) ) ;
#151989=CARTESIAN_POINT ( 'NONE',  ( 5.074738461036464088, -1.720261882950037124, -0.6118011564382742629 ) ) ;
#151996=CARTESIAN_POINT ( 'NONE',  ( 1.635027243301078848, 1.886126948880119780, 0.7230602950082564151 ) ) ;
#151997=CARTESIAN_POINT ( 'NONE',  ( 6.827182134110222123, -0.006956174471953178659, 2.188967759425272330 ) ) ;
#152000=CARTESIAN_POINT ( 'NONE',  ( 4.557361202124784683, 1.492679318236398878, 1.111055945242465093 ) ) ;
#152005=CARTESIAN_POINT ( 'NONE',  ( 5.408770660633122063, 1.379882519126625295, -1.195542987486551301 ) ) ;
#152009=CARTESIAN_POINT ( 'NONE',  ( 2.178627760304178818, -0.8125915806111455586, -1.531602080710131153 ) ) ;
#152010=CARTESIAN_POINT ( 'NONE',  ( 0.6205767395346533100, -1.653899685646512019, 0.5418069113267124370 ) ) ;
#152012=CARTESIAN_POINT ( 'NONE',  ( 5.321043329010971767, 2.130378997510178785, 0.8875623774946446165 ) ) ;
#152015=CARTESIAN_POINT ( 'NONE',  ( 1.528665837207894285, 1.985218273788964316, 0.5525772030575173410 ) ) ;
#152019=CARTESIAN_POINT ( 'NONE',  ( 6.854781963242574605, -0.9897500569795645298, 2.071502949204959254 ) ) ;
#152022=CARTESIAN_POINT ( 'NONE',  ( 6.819227946136852125, -0.1326586024288610444, 1.840611662119538749 ) ) ;
#152023=CARTESIAN_POINT ( 'NONE',  ( 3.304848191199673213, -0.3775801424153284458, -1.874573493127674961 ) ) ;
#152025=CARTESIAN_POINT ( 'NONE',  ( 4.670673364294657404, -1.443042178620690841, 1.669811033208345341 ) ) ;
#152030=CARTESIAN_POINT ( 'NONE',  ( 0.1881566102324930545, 1.164766123054150837, 1.649759867427439186 ) ) ;
#152031=CARTESIAN_POINT ( 'NONE',  ( 3.944573596103123414, 2.296136059628416604, 0.2296890760785547936 ) ) ;
#152032=CARTESIAN_POINT ( 'NONE',  ( 4.316819842036943911, -1.455217238560998272, 1.315978175897666080 ) ) ;
#152033=CARTESIAN_POINT ( 'NONE',  ( 0.4089400952669055567, -1.579117232646386704, 1.163831224039679979 ) ) ;
#152037=CARTESIAN_POINT ( 'NONE',  ( 6.298064597363540074, -0.9548514761729166578, -1.776169100128288658 ) ) ;
#152040=CARTESIAN_POINT ( 'NONE',  ( 3.063509990063197019, 1.831722579244631666, 1.165231348177008242 ) ) ;
#152042=CARTESIAN_POINT ( 'NONE',  ( 0.5453776912951785460, 0.1620316879334358084, 2.114494688702214020 ) ) ;
#152048=CARTESIAN_POINT ( 'NONE',  ( 1.686866501761717263, -0.2992900534812113489, -2.038785687196064789 ) ) ;
#152054=CARTESIAN_POINT ( 'NONE',  ( 4.336511155197938727, 1.173803677898217712, -1.509565991254034678 ) ) ;
#152058=CARTESIAN_POINT ( 'NONE',  ( 1.177659378823514791, 1.784474613499857032, -0.3112490768260189333 ) ) ;
#152060=CARTESIAN_POINT ( 'NONE',  ( 0.6728745832610707467, 1.688094080341449033, -0.9057684134900626516 ) ) ;
#152061=CARTESIAN_POINT ( 'NONE',  ( 2.471216696211364638, 1.848302923701108158, 0.9330170062570308787 ) ) ;
#152063=CARTESIAN_POINT ( 'NONE',  ( 0.7957029915596275371, -0.7116629262611442464, 1.838703523458279143 ) ) ;
#152064=CARTESIAN_POINT ( 'NONE',  ( 2.367563199519676420, 1.790531440309536926, -0.3556685536310541518 ) ) ;
#152065=CARTESIAN_POINT ( 'NONE',  ( 0.2589922964784003301, 0.8893095213439340396, 2.129655304206728328 ) ) ;
#152068=CARTESIAN_POINT ( 'NONE',  ( 4.176276986610152342, -1.057847390704643509, -1.770619276543743625 ) ) ;
#152073=CARTESIAN_POINT ( 'NONE',  ( 4.963951390035996170, 2.083465175373377498, -0.3060735771123861970 ) ) ;
#152075=CARTESIAN_POINT ( 'NONE',  ( 6.303194806757332458, -1.751150776259063457, 1.104182018118210262 ) ) ;
#152077=CARTESIAN_POINT ( 'NONE',  ( 4.358765367649009903, -1.604958417591015207, 1.448176592534822005 ) ) ;
#152078=CARTESIAN_POINT ( 'NONE',  ( 4.811197383834631580, 1.677940508811623710, -1.123774901704529317 ) ) ;
#152085=CARTESIAN_POINT ( 'NONE',  ( 2.395720570290179374, -1.993893129684479293, 0.3006499569925198956 ) ) ;
#152088=CARTESIAN_POINT ( 'NONE',  ( 6.620655732516651071, -0.002413161512292844035, 2.173887093218453082 ) ) ;
#152092=CARTESIAN_POINT ( 'NONE',  ( 4.517203946846011675, -1.842441744247227842, 0.8197884948388589610 ) ) ;
#152094=CARTESIAN_POINT ( 'NONE',  ( 1.013767525470328001, -0.7718518339048777710, -1.542633921862639701 ) ) ;
#152100=CARTESIAN_POINT ( 'NONE',  ( 5.641831084104285132, 0.7588036158820666843, -1.709917670604633066 ) ) ;
#152101=CARTESIAN_POINT ( 'NONE',  ( 6.398696026112846269, -1.975200287401058130, -0.3884956089365321774 ) ) ;
#152106=CARTESIAN_POINT ( 'NONE',  ( 0.7730648107450198703, 1.777001872080404166, -0.9530316558409924754 ) ) ;
#152107=CARTESIAN_POINT ( 'NONE',  ( 1.160107992948592237, 1.809582681877516697, 0.08717244660690416647 ) ) ;
#152109=CARTESIAN_POINT ( 'NONE',  ( 6.807524309086420367, -0.4794501827766698421, 2.115671360755105646 ) ) ;
#152114=CARTESIAN_POINT ( 'NONE',  ( 0.2158530320381162604, 0.9822752966809102926, -1.644539037099991718 ) ) ;
#152122=CARTESIAN_POINT ( 'NONE',  ( 4.469695567000064429, 2.097540297429688838, -0.5223010940857697459 ) ) ;
#152125=CARTESIAN_POINT ( 'NONE',  ( 0.5102161431939798986, -0.7575819503438313562, 1.980855387931411915 ) ) ;
#152127=CARTESIAN_POINT ( 'NONE',  ( 6.721730220878607831, -1.769880579078547012, 0.4471725050417332814 ) ) ;
#152128=CARTESIAN_POINT ( 'NONE',  ( 2.425019040235734558, -0.003784258722050458899, 1.971530340264670889 ) ) ;
#152129=CARTESIAN_POINT ( 'NONE',  ( 4.693567934957057375, 1.782326746607498791, -0.6936623114904352239 ) ) ;
#152133=CARTESIAN_POINT ( 'NONE',  ( 6.162556002056702731, -0.7074686763054702787, -1.838295890583282022 ) ) ;
#152134=CARTESIAN_POINT ( 'NONE',  ( 0.1287130127310652239, -1.775900012335431155, 0.7861216482863192523 ) ) ;
#152140=CARTESIAN_POINT ( 'NONE',  ( 5.127564033545165323, -0.2766344828325461580, 1.892035409188079997 ) ) ;
#152142=CARTESIAN_POINT ( 'NONE',  ( 3.545738602337618506, -1.670889076328873291, -1.441789439710974285 ) ) ;
#152143=CARTESIAN_POINT ( 'NONE',  ( 2.503190323335769740, 1.772782541628318720, -1.313999973512294694 ) ) ;
#152145=CARTESIAN_POINT ( 'NONE',  ( 0.7328884408557728714, 1.767063509844998492, 0.7314339715377634610 ) ) ;
#152146=CARTESIAN_POINT ( 'NONE',  ( -0.02338929933905826986, 0.006294950389555685130, -1.710968156697996401 ) ) ;
#152148=CARTESIAN_POINT ( 'NONE',  ( 2.875506610227479332, -0.2054619808779626633, 2.060159609288146232 ) ) ;
#152152=CARTESIAN_POINT ( 'NONE',  ( 0.8312129145573650124, 0.1600495679085281175, 2.155820468135719814 ) ) ;
#152153=CARTESIAN_POINT ( 'NONE',  ( 2.982162443640325566, -2.159563097825706990, -0.3721831821169723775 ) ) ;
#152160=CARTESIAN_POINT ( 'NONE',  ( 5.906827578720975858, -0.9711093913858243054, -1.436504219383877290 ) ) ;
#152161=EDGE_CURVE ( 'NONE', #12895, #106915, #82453, .T. ) ;
#152163=CARTESIAN_POINT ( 'NONE',  ( 3.274343992483694787, -1.016290647400164282, -1.803532422793553636 ) ) ;
#152164=CARTESIAN_POINT ( 'NONE',  ( 4.798512230019831293, 1.459014486584905956, -1.534486623482501644 ) ) ;
#152167=CARTESIAN_POINT ( 'NONE',  ( 3.274220328336883146, -0.9665011448860871823, -1.715865690870149285 ) ) ;
#152168=CARTESIAN_POINT ( 'NONE',  ( 0.8438408207818194340, -1.215224102361469161, -1.476598726422105656 ) ) ;
#152169=CARTESIAN_POINT ( 'NONE',  ( 4.910265066218413743, 1.583196867009181608, -1.657922308084827545 ) ) ;
#152170=CARTESIAN_POINT ( 'NONE',  ( 3.492628380820804956, -0.3572889717703279788, -1.790209119249221770 ) ) ;
#152174=CARTESIAN_POINT ( 'NONE',  ( 4.517842040498582179, -0.5326873650394120530, 1.941415848259191446 ) ) ;
#152175=CARTESIAN_POINT ( 'NONE',  ( 2.852341167582587378, -1.956174252073937359, -0.1491622203949396763 ) ) ;
#152178=CARTESIAN_POINT ( 'NONE',  ( 0.1751657365761521701, 1.361037063587458906, -2.300812366989886559 ) ) ;
#152179=CARTESIAN_POINT ( 'NONE',  ( 6.351524237630270520, 2.085149843271947301, -0.1523318108044656727 ) ) ;
#152180=CARTESIAN_POINT ( 'NONE',  ( 5.489024251479373895, 1.559478583775832261, -0.8368352093669585434 ) ) ;
#152182=CARTESIAN_POINT ( 'NONE',  ( 1.957222284144799929, 0.3726435881295561692, -2.159377063894574622 ) ) ;
#152183=CARTESIAN_POINT ( 'NONE',  ( 6.175711810462381379, -0.9247362235058408375, 1.474125693279482174 ) ) ;
#152185=CARTESIAN_POINT ( 'NONE',  ( 0.2335667940002502385, 6.947499997881678269, -2.748442024765639147 ) ) ;
#152186=CARTESIAN_POINT ( 'NONE',  ( 0.3106396986791125081, 1.498014557929911117, 0.8549171915634717900 ) ) ;
#152187=CARTESIAN_POINT ( 'NONE',  ( 1.177631936369994303, -1.035077938576201451, -2.052156377449709357 ) ) ;
#152188=CARTESIAN_POINT ( 'NONE',  ( 0.6971427418834205136, 1.794861059153027627, 1.257291590721874686 ) ) ;
#152189=CARTESIAN_POINT ( 'NONE',  ( 2.912931060594741162, 1.598032330669514778, -1.522282275181946032 ) ) ;
#152190=CARTESIAN_POINT ( 'NONE',  ( 6.491432910188612126, -0.4373703761123280964, 1.975813455233149218 ) ) ;
#152192=CARTESIAN_POINT ( 'NONE',  ( 0.4621001773846104554, -0.5802113591629636247, 2.092003544004197302 ) ) ;
#152194=ADVANCED_FACE ( 'NONE', ( #68440 ), #114097, .T. ) ;
#152195=CARTESIAN_POINT ( 'NONE',  ( 0.6556431738361043760, 2.038855430691276727, -0.5708433468438726122 ) ) ;
#152196=FACE_OUTER_BOUND ( 'NONE', #141514, .T. ) ;
#152197=CARTESIAN_POINT ( 'NONE',  ( 5.666998703487860389, -1.741597003894586937, -0.8236021136211798543 ) ) ;
#152199=CARTESIAN_POINT ( 'NONE',  ( 1.136728594277321980, 0.4534141614637792195, 2.246936901365268913 ) ) ;
#152203=CARTESIAN_POINT ( 'NONE',  ( 4.108218931252209494, -0.8498058027226679245, 2.052504409502105442 ) ) ;
#152208=CARTESIAN_POINT ( 'NONE',  ( 1.600232647554021392, -0.2440283035436350279, 2.001511509883910911 ) ) ;
#152210=CARTESIAN_POINT ( 'NONE',  ( 1.182570505923411952, 1.231668817017372408, -1.654277799056037335 ) ) ;
#152213=CARTESIAN_POINT ( 'NONE',  ( -0.1237769027084348328, -0.1346504581853508187, -1.811164470923332104 ) ) ;
#152216=CARTESIAN_POINT ( 'NONE',  ( 2.459888865612788855, 0.7521488021439284299, 1.602074255657309099 ) ) ;
#152217=CARTESIAN_POINT ( 'NONE',  ( 1.635388916632842360, 0.6352005984417673501, 1.913803229121699534 ) ) ;
#152218=CARTESIAN_POINT ( 'NONE',  ( -0.1121326479804653220, -0.4008509640632436088, -1.803546454093779561 ) ) ;
#152219=CARTESIAN_POINT ( 'NONE',  ( 5.144168085839278426, 0.6632553684719083575, 2.194301386939989218 ) ) ;
#152220=CARTESIAN_POINT ( 'NONE',  ( 3.240019139272034110, 0.4481936114588759845, 1.785621944311803100 ) ) ;
#152222=CARTESIAN_POINT ( 'NONE',  ( 4.383705365265609721, 1.192707349210776036, 1.382196219385352309 ) ) ;
#152223=CARTESIAN_POINT ( 'NONE',  ( 4.693982515131527755, 1.755768268644173791, 0.9914009648221073778 ) ) ;
#152225=CARTESIAN_POINT ( 'NONE',  ( 3.608526635699527141, -0.9147260449715814978, -2.069530211360113725 ) ) ;
#152227=CARTESIAN_POINT ( 'NONE',  ( 6.335009839202000670, 0.2025031609870796001, 2.096191850513532184 ) ) ;
#152229=CARTESIAN_POINT ( 'NONE',  ( 4.088381982606685838, 1.110138344689771239, -1.747393465062855533 ) ) ;
#152234=CARTESIAN_POINT ( 'NONE',  ( 2.473164231231731680, 0.09456843629558449316, -1.924295592635028029 ) ) ;
#152236=CARTESIAN_POINT ( 'NONE',  ( 6.983263157960363010, -0.003310164959547181717, 1.953544951557646403 ) ) ;
#152241=CARTESIAN_POINT ( 'NONE',  ( 0.5104038411899833871, -0.7921320118633947693, 2.075572886547627505 ) ) ;
#152242=CARTESIAN_POINT ( 'NONE',  ( 3.504997884693922483, 1.661208405451128245, -1.294291292614203170 ) ) ;
#152245=CARTESIAN_POINT ( 'NONE',  ( 0.2911520677349140884, -1.704046917483082346, 0.7485983125269514149 ) ) ;
#152250=CARTESIAN_POINT ( 'NONE',  ( 1.424255164902767934, -2.103954720533041556, 0.2648648325892372646 ) ) ;
#152253=CARTESIAN_POINT ( 'NONE',  ( 4.246505328441081417, -1.940195102956907336, -0.2900488188990399396 ) ) ;
#152254=CARTESIAN_POINT ( 'NONE',  ( 2.852577672069932735, 0.7271573612388192442, 2.035869728763760378 ) ) ;
#152255=CARTESIAN_POINT ( 'NONE',  ( 1.417261839328866513, -1.023339270300478221, -1.530466495063505628 ) ) ;
#152257=CARTESIAN_POINT ( 'NONE',  ( 4.171615353782907931, -0.9995084519054014960, 1.424469360818179986 ) ) ;
#152262=CARTESIAN_POINT ( 'NONE',  ( 1.481558191429487970, 1.997200094811113491, -0.8276061316847342919 ) ) ;
#152264=CARTESIAN_POINT ( 'NONE',  ( 2.847029653296664353, -1.038834691150035461, 1.727737368502464621 ) ) ;
#152266=CARTESIAN_POINT ( 'NONE',  ( 1.182749364907993206, -2.109161078630458430, -0.4729781282231394490 ) ) ;
#152268=CARTESIAN_POINT ( 'NONE',  ( 3.766447953776773883, -1.324889289065459774, 1.460063511008972137 ) ) ;
#152269=CARTESIAN_POINT ( 'NONE',  ( 6.609000000000038177, 2.443064466336189788, 2.382833824652215160 ) ) ;
#152270=CARTESIAN_POINT ( 'NONE',  ( 2.911592935152186090, -0.9596169164145462727, -1.688359700174842271 ) ) ;
#152279=CARTESIAN_POINT ( 'NONE',  ( 6.651428954171766605, -1.847749378774863560, -1.382155756676258784 ) ) ;
#152282=CARTESIAN_POINT ( 'NONE',  ( 3.766413727395605093, -0.7909564911158167844, -1.795405819223389488 ) ) ;
#152284=CARTESIAN_POINT ( 'NONE',  ( 1.213517774399593740, 1.944071949784083264, 0.5350861613380719639 ) ) ;
#152285=CARTESIAN_POINT ( 'NONE',  ( 3.837202554855035697, -1.762604653963547818, -1.172905022591600233 ) ) ;
#152289=CARTESIAN_POINT ( 'NONE',  ( 2.589598559577494186, -1.836209955096680613, -0.1354230481333124070 ) ) ;
#152293=CARTESIAN_POINT ( 'NONE',  ( 3.832379111121624327, -1.093062754469842579, -1.817066923117337751 ) ) ;
#152297=CARTESIAN_POINT ( 'NONE',  ( 5.887979924156289790, -0.9304241717780140641, 1.838884224927712419 ) ) ;
#152299=CARTESIAN_POINT ( 'NONE',  ( 2.401689157922583640, -0.7064633820979376866, -1.700523668893457296 ) ) ;
#152304=CARTESIAN_POINT ( 'NONE',  ( 2.086817400036289794, -2.164668306305051804, -0.4287355390964405211 ) ) ;
#152305=CARTESIAN_POINT ( 'NONE',  ( 3.690934243623856581, -0.4369955660583099699, -2.219648300357620396 ) ) ;
#152307=CARTESIAN_POINT ( 'NONE',  ( 4.306777863985831623, -0.4033372078124509708, -1.765930869088320865 ) ) ;
#152308=CARTESIAN_POINT ( 'NONE',  ( 4.223789564141206654, 0.8136391335250325874, -1.734469729061314913 ) ) ;
#152311=CARTESIAN_POINT ( 'NONE',  ( 3.397303563958519401, 1.553371746707431500, 1.213851982216722636 ) ) ;
#152312=CARTESIAN_POINT ( 'NONE',  ( 5.260568668178753349, -1.354309965608934352, 1.290672426560689035 ) ) ;
#152313=CARTESIAN_POINT ( 'NONE',  ( 4.879284944527097601, -0.09183316818502919310, 1.858928597182760711 ) ) ;
#152315=CARTESIAN_POINT ( 'NONE',  ( 0.4445464637146989695, -1.457232572767804379, 1.394089106691732693 ) ) ;
#152317=CARTESIAN_POINT ( 'NONE',  ( 2.069099208297279002, -1.926018337604347597, -0.8524663740339888385 ) ) ;
#152321=CARTESIAN_POINT ( 'NONE',  ( 2.830460552442021438, -1.048868820301660953, -1.842999677239331113 ) ) ;
#152323=CARTESIAN_POINT ( 'NONE',  ( 1.107682413490064022, 1.532168600112630230, 1.316196929287305473 ) ) ;
#152328=CARTESIAN_POINT ( 'NONE',  ( 2.302237272444170202, -2.161155982280529297, 0.05054500047013688047 ) ) ;
#152337=CARTESIAN_POINT ( 'NONE',  ( 6.567919234911265391, -1.285863816539883908, 1.649083965234589000 ) ) ;
#152339=CARTESIAN_POINT ( 'NONE',  ( 1.024742985469536016, 1.345695571256789513, -1.818664117639690714 ) ) ;
#152346=CARTESIAN_POINT ( 'NONE',  ( 4.301177763854931335, 1.387281528384849860, 1.024788870506128990 ) ) ;
#152348=CARTESIAN_POINT ( 'NONE',  ( 2.055556868256277259, 1.765410544359298894, -0.1243799924028898551 ) ) ;
#152349=( BOUNDED_SURFACE ( )  B_SPLINE_SURFACE ( 3, 3, ( 
 ( #27625, #176032, #190121, #41775, #59058, #77443, #62267, #157647, #209554, #127357 ),
 ( #25489, #91595, #143560, #61198, #9244, #125215, #29776, #193326, #177086, #28703 ),
 ( #194394, #94788, #112158, #166155, #18818, #115347, #117475, #114291, #100094, #51351 ),
 ( #84905, #148845, #147794, #131582, #35074, #418, #150992, #183467, #101144, #113221 ),
 ( #99040, #181338, #167232, #165095, #16687, #63332, #116402, #17742, #199705, #179226 ),
 ( #83830, #180289, #130544, #14558, #15623, #47106, #129492, #213812, #149922, #81713 ),
 ( #31912, #32965, #65432, #195474, #30851, #80656, #197584, #1491, #96929, #66489 ) ),
 .UNSPECIFIED., .T., .F., .T. ) 
 B_SPLINE_SURFACE_WITH_KNOTS ( ( 4, 3, 4 ),
 ( 4, 1, 1, 1, 1, 1, 1, 4 ),
 ( 0.000000000000000000, 0.5000000000000000000, 1.000000000000000000 ),
 ( 0.000000000000000000, 0.09090790722575105287, 0.1825853934691276381, 0.2551728700554835028, 0.3603391217242263855, 0.5205903519787860034, 0.7335386666926504429, 0.9999999999999998890 ),
 .UNSPECIFIED. ) 
 GEOMETRIC_REPRESENTATION_ITEM ( )  RATIONAL_B_SPLINE_SURFACE ( (
 ( 1.000000000000000222, 1.000000000000000222, 1.000000000000000222, 1.000000000000000222, 1.000000000000000222, 1.000000000000000444, 1.000000000000000222, 1.000000000000000222, 1.000000000000000222, 1.000000000000000222),
 ( 0.3333333333333334259, 0.3333333333333334259, 0.3333333333333334259, 0.3333333333333333148, 0.3333333333333334259, 0.3333333333333335369, 0.3333333333333334259, 0.3333333333333334814, 0.3333333333333334259, 0.3333333333333334259),
 ( 0.3333333333333334259, 0.3333333333333334259, 0.3333333333333334259, 0.3333333333333333148, 0.3333333333333334259, 0.3333333333333335369, 0.3333333333333334259, 0.3333333333333334814, 0.3333333333333334259, 0.3333333333333334259),
 ( 1.000000000000000222, 1.000000000000000222, 1.000000000000000222, 1.000000000000000222, 1.000000000000000222, 1.000000000000000444, 1.000000000000000222, 1.000000000000000222, 1.000000000000000222, 1.000000000000000222),
 ( 0.3333333333333334259, 0.3333333333333334259, 0.3333333333333334259, 0.3333333333333333148, 0.3333333333333334259, 0.3333333333333335369, 0.3333333333333334259, 0.3333333333333334814, 0.3333333333333334259, 0.3333333333333334259),
 ( 0.3333333333333334259, 0.3333333333333334259, 0.3333333333333334259, 0.3333333333333333148, 0.3333333333333334259, 0.3333333333333335369, 0.3333333333333334259, 0.3333333333333334814, 0.3333333333333334259, 0.3333333333333334259),
 ( 1.000000000000000222, 1.000000000000000222, 1.000000000000000222, 1.000000000000000222, 1.000000000000000222, 1.000000000000000444, 1.000000000000000222, 1.000000000000000222, 1.000000000000000222, 1.000000000000000222) ) ) 
 REPRESENTATION_ITEM ( '' )  SURFACE ( )  );
#152350=CARTESIAN_POINT ( 'NONE',  ( 2.666654630192913267, 0.6802043231916419241, 1.894807776549158218 ) ) ;
#152352=CARTESIAN_POINT ( 'NONE',  ( 4.946401613871811875, 2.200551846729232430, 0.1665617540023768828 ) ) ;
#152354=CARTESIAN_POINT ( 'NONE',  ( 3.920179414529322504, -2.014104250368133453, 0.1526392722818684933 ) ) ;
#152356=CARTESIAN_POINT ( 'NONE',  ( 4.987034407221377030, -1.996844880220369545, -0.7138980100366009163 ) ) ;
#152357=CARTESIAN_POINT ( 'NONE',  ( 4.376577478760902196, -0.4445230835841383898, -1.966641233467445016 ) ) ;
#152358=CARTESIAN_POINT ( 'NONE',  ( 4.254050669898622239, 0.7686244906546428890, -1.640568623306848606 ) ) ;
#152361=CARTESIAN_POINT ( 'NONE',  ( 1.551402291579254022, 0.5461136009352780540, -1.789155053659279071 ) ) ;
#152363=CARTESIAN_POINT ( 'NONE',  ( 1.634869402278725348, 1.785593253932623803, 0.6852637533772619749 ) ) ;
#152367=CARTESIAN_POINT ( 'NONE',  ( -0.1405747822309927342, -1.479430311965252542, -1.211566217618691210 ) ) ;
#152370=CARTESIAN_POINT ( 'NONE',  ( 1.310910670669521272, -1.548711629584406113, 1.204245502051364936 ) ) ;
#152373=CARTESIAN_POINT ( 'NONE',  ( 3.832379111121624327, -1.093062754469842579, -1.817066923117337751 ) ) ;
#152375=CARTESIAN_POINT ( 'NONE',  ( 5.483651708025924165, 1.321867191758316462, 1.462689542499737039 ) ) ;
#152377=CARTESIAN_POINT ( 'NONE',  ( 1.072522059793120652, 0.8197897455473095452, 1.838922316899212372 ) ) ;
#152379=CARTESIAN_POINT ( 'NONE',  ( 1.546650761107182914, -1.494491507556227505, 1.499968751290579494 ) ) ;
#152382=CARTESIAN_POINT ( 'NONE',  ( 2.910663983731573090, 0.6951178490613962868, 1.950330170896700022 ) ) ;
#152386=CARTESIAN_POINT ( 'NONE',  ( 5.191392108680514816, -0.7531529969884572795, 1.950447244483977993 ) ) ;
#152388=CARTESIAN_POINT ( 'NONE',  ( 3.030095697178539549, 1.015519584536026976, -1.516846343748608605 ) ) ;
#152389=CARTESIAN_POINT ( 'NONE',  ( 1.049118701917159946, -1.638035101892039602, 0.7738018112423280526 ) ) ;
#152394=CARTESIAN_POINT ( 'NONE',  ( 4.928867898441261275, 2.110505041808665716, 0.6446608841527908806 ) ) ;
#152396=ORIENTED_EDGE ( 'NONE', *, *, #106096, .T. ) ;
#152397=CARTESIAN_POINT ( 'NONE',  ( 4.371672787583542608, 0.4156390277068115480, -1.866406306929219605 ) ) ;
#152400=CARTESIAN_POINT ( 'NONE',  ( 6.531696417657103737, 1.982406992490031383, -0.5971068152322636102 ) ) ;
#152403=CARTESIAN_POINT ( 'NONE',  ( 5.829655996829377962, 1.081331853127937448, -1.906115348727636549 ) ) ;
#152408=CARTESIAN_POINT ( 'NONE',  ( 3.602682612693074660, 1.476495159181415939, -1.148357684351591912 ) ) ;
#152415=CARTESIAN_POINT ( 'NONE',  ( 0.4441182907778543631, -0.9332952320128800050, 1.734295555568473368 ) ) ;
#152416=CARTESIAN_POINT ( 'NONE',  ( 1.107046246104196552, -0.04665650516593074226, 2.016035445577879504 ) ) ;
#152420=CARTESIAN_POINT ( 'NONE',  ( 1.588088344156918907, -2.181139600106785092, -0.2122876309011075546 ) ) ;
#152421=CARTESIAN_POINT ( 'NONE',  ( 5.865807274569021068, 1.797851641234180287, -0.3166982042408575948 ) ) ;
#152428=CARTESIAN_POINT ( 'NONE',  ( 3.808014051635350672, 1.299385917162833692, -1.304790556973287163 ) ) ;
#152429=CARTESIAN_POINT ( 'NONE',  ( 1.102198380138383449, -0.9033151347564006839, 1.799099544393264472 ) ) ;
#152430=CARTESIAN_POINT ( 'NONE',  ( 1.652187889876779892, -0.3379717360396676806, -2.273286007567467237 ) ) ;
#152432=CARTESIAN_POINT ( 'NONE',  ( 1.164654898877310885, 1.413799132238046985, -1.210232755764220069 ) ) ;
#152436=CARTESIAN_POINT ( 'NONE',  ( 4.254103502353132171, 0.8128351696983120434, -1.731171583500931366 ) ) ;
#152440=CARTESIAN_POINT ( 'NONE',  ( 3.966417678127855950, -1.951510144350139919, -0.7507201541567410930 ) ) ;
#152441=CARTESIAN_POINT ( 'NONE',  ( 2.764352523130030548, -1.291370965961564421, 1.353630663414123969 ) ) ;
#152444=CARTESIAN_POINT ( 'NONE',  ( 3.421201824283449877, -1.039729455425863147, -1.395559870880677789 ) ) ;
#152448=CARTESIAN_POINT ( 'NONE',  ( 3.598037535421601429, -1.723020282968828809, -0.08274337828741322454 ) ) ;
#152449=CARTESIAN_POINT ( 'NONE',  ( 3.614928802375876771, -0.1595779646587774658, 2.185787688459623901 ) ) ;
#152450=CARTESIAN_POINT ( 'NONE',  ( 6.024089167411393220, -1.222679950896175205, -1.837027303407394507 ) ) ;
#152452=CARTESIAN_POINT ( 'NONE',  ( 3.977515510703835133, -0.1653560672004051324, 2.164858251032927061 ) ) ;
#152453=CARTESIAN_POINT ( 'NONE',  ( 1.787459277025660542, 1.258035843444211155, 1.323286951131589895 ) ) ;
#152455=CARTESIAN_POINT ( 'NONE',  ( 4.628176351164477786, 2.111873176223429738, 0.1524955421974716341 ) ) ;
#152457=CARTESIAN_POINT ( 'NONE',  ( 4.739906352223059116, 2.286097037578460611, 0.1700548269078107355 ) ) ;
#152459=CARTESIAN_POINT ( 'NONE',  ( 6.620655732516666170, 7.629137130509104026, 2.326260288887294969 ) ) ;
#152462=CARTESIAN_POINT ( 'NONE',  ( 0.5574859923395922845, -1.816599148028580579, 1.093606109393664427 ) ) ;
#152469=CARTESIAN_POINT ( 'NONE',  ( 5.695935454815424848, 1.779625283580280382, 0.9480427965274510482 ) ) ;
#152471=CARTESIAN_POINT ( 'NONE',  ( 4.311423628786446471, -1.712024382654028454, -1.150014069924868654 ) ) ;
#152476=CARTESIAN_POINT ( 'NONE',  ( 0.1331565106231363538, 2.033293680964400885, -2.362282156872722805 ) ) ;
#152477=CARTESIAN_POINT ( 'NONE',  ( 0.4805627621443783193, -0.2577823606141148027, -2.074612465628209890 ) ) ;
#152478=CARTESIAN_POINT ( 'NONE',  ( 4.869767617671093340, -0.2496050341583149201, -2.000857388266870984 ) ) ;
#152479=CARTESIAN_POINT ( 'NONE',  ( 4.405690278861111864, -0.7914791229979671883, -1.662609734262666894 ) ) ;
#152481=CARTESIAN_POINT ( 'NONE',  ( 0.7446035987349702845, -1.482829294443729351, 0.8806902949074472131 ) ) ;
#152482=PLANE ( 'NONE',  #13156 ) ;
#152483=CARTESIAN_POINT ( 'NONE',  ( 0.7218034001665899480, 2.265987065647384835, 0.3856900369042133292 ) ) ;
#152485=CARTESIAN_POINT ( 'NONE',  ( 0.7380304622728722785, -1.600708836854593198, -1.599060815671312641 ) ) ;
#152486=CARTESIAN_POINT ( 'NONE',  ( 3.404997959543601294, 1.660052132133410296, -1.295932331351705935 ) ) ;
#152494=CARTESIAN_POINT ( 'NONE',  ( 5.519863322019965324, -0.5397129975505778887, 2.154757917147765323 ) ) ;
#152495=CARTESIAN_POINT ( 'NONE',  ( 2.871223686158608679, 2.080653275041044026, -0.6881803712485771163 ) ) ;
#152498=CARTESIAN_POINT ( 'NONE',  ( 5.476992472119650124, 1.812042599547862176, 0.7524171098330989516 ) ) ;
#152500=FACE_OUTER_BOUND ( 'NONE', #99343, .T. ) ;
#152502=CARTESIAN_POINT ( 'NONE',  ( 4.834296457332984076, -1.136628438424293508, -1.790084250976264002 ) ) ;
#152506=CARTESIAN_POINT ( 'NONE',  ( 6.385629968321593353, 1.486944277142748572, 1.569300510047972219 ) ) ;
#152508=CARTESIAN_POINT ( 'NONE',  ( 5.267088776126935379, 1.772936381825638952, -0.4966186330585887210 ) ) ;
#152511=CARTESIAN_POINT ( 'NONE',  ( 1.065484398342542383, -1.105240684350906610, 1.344476687319878794 ) ) ;
#152516=CARTESIAN_POINT ( 'NONE',  ( 5.084929678302336775, -0.2608814864752464491, -2.145832476913120068 ) ) ;
#152519=CARTESIAN_POINT ( 'NONE',  ( 4.135729569369491543, -1.488772398488470872, -1.567562023322838671 ) ) ;
#152521=CARTESIAN_POINT ( 'NONE',  ( 5.202397865228217455, -0.6614073030348812665, -1.857238293531390916 ) ) ;
#152522=CARTESIAN_POINT ( 'NONE',  ( 4.393670956608656475, 0.08463240572039069931, 1.731882585348672343 ) ) ;
#152523=CARTESIAN_POINT ( 'NONE',  ( 0.4159077360078728969, -1.177411712353953588, -1.848246096435968600 ) ) ;
#152524=CARTESIAN_POINT ( 'NONE',  ( 1.782679935646735769, -1.233298141988391272, 1.950204222970158385 ) ) ;
#152525=CARTESIAN_POINT ( 'NONE',  ( 3.567699708620798216, 2.011335548252995764, -0.4479969848151729162 ) ) ;
#152526=CARTESIAN_POINT ( 'NONE',  ( 6.497608386930124880, -1.941524946301041554, 0.05238333795444527485 ) ) ;
#152532=CARTESIAN_POINT ( 'NONE',  ( 3.698430944683338328, -2.204125419102770600, -0.1106900096672913392 ) ) ;
#152534=CARTESIAN_POINT ( 'NONE',  ( 1.006444858994318681, 0.5332790290331288485, 1.782932314864177137 ) ) ;
#152536=CARTESIAN_POINT ( 'NONE',  ( -0.1290005225502641184, 1.996213967822700663, -2.587563282167547385 ) ) ;
#152539=CARTESIAN_POINT ( 'NONE',  ( 6.925078400183557470, 1.239878965558613322, 2.257517960274835200 ) ) ;
#152540=CARTESIAN_POINT ( 'NONE',  ( 6.703072984701052839, -0.3981723446819797063, 1.804146177254343009 ) ) ;
#152542=CARTESIAN_POINT ( 'NONE',  ( 2.993097573648812126, 1.768379194316849423, -1.058085006197813538 ) ) ;
#152545=CARTESIAN_POINT ( 'NONE',  ( 2.385421078170113507, 0.09676420124534937384, -2.017471438767451275 ) ) ;
#152548=CARTESIAN_POINT ( 'NONE',  ( 1.832957655136749908, 0.2007874442899897915, 2.051070037287055392 ) ) ;
#152553=CARTESIAN_POINT ( 'NONE',  ( 5.988949835885216011, -0.3198878037087344306, -2.183464699167809275 ) ) ;
#152554=CARTESIAN_POINT ( 'NONE',  ( 1.493687833870473325, 1.635750924671933282, 1.413141523588061776 ) ) ;
#152556=CARTESIAN_POINT ( 'NONE',  ( 0.4269707148552639997, -1.727061408318403712, 1.040797348915108111 ) ) ;
#152557=CARTESIAN_POINT ( 'NONE',  ( 1.845480572931688767, -1.229624162049542058, 1.941665159144045250 ) ) ;
#152560=PLANE ( 'NONE',  #134048 ) ;
#152562=CARTESIAN_POINT ( 'NONE',  ( 2.026040307571222332, 1.079255042350239391, -1.527726335390042767 ) ) ;
#152563=CARTESIAN_POINT ( 'NONE',  ( 3.485564796978508184, -0.5807542032013839339, 1.931124776463407189 ) ) ;
#152567=CARTESIAN_POINT ( 'NONE',  ( 5.602208710206744158, -2.106257355024013567, -0.001338375500582050358 ) ) ;
#152572=CARTESIAN_POINT ( 'NONE',  ( 5.185809364388858533, 1.945378451193703118, -0.5428193807620449451 ) ) ;
#152574=CARTESIAN_POINT ( 'NONE',  ( 0.3388347341246043531, -1.999784422754165458, -0.5045462532434812353 ) ) ;
#152576=CARTESIAN_POINT ( 'NONE',  ( 5.132170659515546518, 1.116069247042193124, -1.851066442873222639 ) ) ;
#152582=CARTESIAN_POINT ( 'NONE',  ( 2.770184829093131462, -2.147865496273542174, 0.3164581508635355145 ) ) ;
#152585=CARTESIAN_POINT ( 'NONE',  ( 2.085277916773973228, -0.7859315772556186852, 1.665205719185464561 ) ) ;
#152587=CARTESIAN_POINT ( 'NONE',  ( 4.581673536070863584, -1.032772929490553215, 1.932928240684625099 ) ) ;
#152588=CARTESIAN_POINT ( 'NONE',  ( 6.883263157960362477, -0.004191378316371896506, 2.053658919477070910 ) ) ;
#152589=CARTESIAN_POINT ( 'NONE',  ( 5.067353023127458833, 0.2270735253321141400, -2.251102950005756220 ) ) ;
#152597=CARTESIAN_POINT ( 'NONE',  ( 4.938602502702000407, 0.3022688342860947452, 1.743538433004296673 ) ) ;
#152600=CARTESIAN_POINT ( 'NONE',  ( 1.993330679213504153, 1.832751758872013914, -1.037179240317965823 ) ) ;
#152603=CARTESIAN_POINT ( 'NONE',  ( 2.312896453495900673, -1.524290774635113088, 1.247285826271822939 ) ) ;
#152605=CARTESIAN_POINT ( 'NONE',  ( 0.2210476084268316321, -1.750679471464357650, -0.8856473702157914296 ) ) ;
#152606=CARTESIAN_POINT ( 'NONE',  ( 5.871335974614770414, -1.558408318232169298, -0.9234296637983196998 ) ) ;
#152611=CARTESIAN_POINT ( 'NONE',  ( 6.209813078548920728, -1.856259414618817383, 0.2309603555875269776 ) ) ;
#152614=CARTESIAN_POINT ( 'NONE',  ( 5.647352632913819726, 1.828451368696734747, -0.9708816006866529680 ) ) ;
#152623=CARTESIAN_POINT ( 'NONE',  ( 5.547302793442128177, 1.730978599593002043, -0.9233319674036490898 ) ) ;
#152625=CARTESIAN_POINT ( 'NONE',  ( 3.690779688840303496, -1.198677090843719872, -1.620934038430859703 ) ) ;
#152626=CARTESIAN_POINT ( 'NONE',  ( 2.167068266397979670, 1.749796802513942318, -0.7803250849751103280 ) ) ;
#152627=CARTESIAN_POINT ( 'NONE',  ( -0.1108833634137010304, 0.2458664895051872190, -1.931623620491630611 ) ) ;
#152628=CARTESIAN_POINT ( 'NONE',  ( 0.01162390915069450026, -2.148011843722149372, 0.4338911918742721641 ) ) ;
#152630=CARTESIAN_POINT ( 'NONE',  ( 2.038157526861613889, 1.849479306444936411, 0.2792354855166642724 ) ) ;
#152632=CARTESIAN_POINT ( 'NONE',  ( 4.482685760555058074, -1.311686992106766203, 1.527362355471563182 ) ) ;
#152635=CARTESIAN_POINT ( 'NONE',  ( 4.745783977240443541, 2.094000167431044446, -0.3121058131653231538 ) ) ;
#152638=CARTESIAN_POINT ( 'NONE',  ( 6.514133371570012265, 2.065101995627930620, -0.1482383472809906122 ) ) ;
#152639=CARTESIAN_POINT ( 'NONE',  ( 1.523107970189445215, -1.967458627398379623, 0.7076814851830464104 ) ) ;
#152641=CARTESIAN_POINT ( 'NONE',  ( 6.141596500199405284, -1.324292569296809052, -1.256812384211228428 ) ) ;
#152642=EDGE_LOOP ( 'NONE', ( #173409, #20939, #37292, #151048 ) ) ;
#152651=CARTESIAN_POINT ( 'NONE',  ( 0.9963917123081984517, -1.767100618702711179, -0.3976972079893052459 ) ) ;
#152660=CARTESIAN_POINT ( 'NONE',  ( 6.222279831957801655, 1.994873610751910942, 0.2930524845206964879 ) ) ;
#152661=CARTESIAN_POINT ( 'NONE',  ( 0.2234921222181683598, 1.847112181986635626, 1.041312259928407702 ) ) ;
#152663=CARTESIAN_POINT ( 'NONE',  ( 0.1399997263886003374, 0.002789056014650820314, -1.999853399661279063 ) ) ;
#152667=CARTESIAN_POINT ( 'NONE',  ( 3.098452163322249042, 1.954020348291004794, 0.2456459092235723785 ) ) ;
#152668=CARTESIAN_POINT ( 'NONE',  ( 4.095327490859664188, -0.3419149367107060522, 1.987051255384481463 ) ) ;
#152672=CARTESIAN_POINT ( 'NONE',  ( 4.224703044441734612, 0.1064595904514322594, 2.188988589495489911 ) ) ;
#152674=CARTESIAN_POINT ( 'NONE',  ( 3.399358865922623263, 1.517880436307640579, 1.186064745714454638 ) ) ;
#152676=CARTESIAN_POINT ( 'NONE',  ( -0.02948999725178609935, 2.037268340021273882, -2.343334633859140315 ) ) ;
#152677=CARTESIAN_POINT ( 'NONE',  ( 0.1333542156527478262, 0.001576319744088505292, -2.046049510433409768 ) ) ;
#152682=CARTESIAN_POINT ( 'NONE',  ( 4.610180678033913182, 1.969109005737102347, -0.04407691609572064739 ) ) ;
#152683=CARTESIAN_POINT ( 'NONE',  ( 0.1693407553623625106, 1.118952433510589817, 1.587118285914286941 ) ) ;
#152684=CARTESIAN_POINT ( 'NONE',  ( 3.580729931658500398, -1.350255368601901651, 1.493277094049742182 ) ) ;
#152685=CARTESIAN_POINT ( 'NONE',  ( 4.938965133657190698, 1.317805461337580697, 1.882938791714399374 ) ) ;
#152687=CARTESIAN_POINT ( 'NONE',  ( 3.924516644892431572, -1.252765583397809079, 1.376256255023865283 ) ) ;
#152693=CARTESIAN_POINT ( 'NONE',  ( 0.1874131419884322858, 1.628132678060219884, 1.467219630700428157 ) ) ;
#152698=CARTESIAN_POINT ( 'NONE',  ( 0.1350027811974127134, -1.670744041527939094, 0.7364786222084362954 ) ) ;
#152700=CARTESIAN_POINT ( 'NONE',  ( 3.006226939181593227, -1.670314528538990873, 0.4657782236400943021 ) ) ;
#152704=CARTESIAN_POINT ( 'NONE',  ( 5.268108045213575785, 0.9031548532531764595, 1.586571422427636824 ) ) ;
#152705=CARTESIAN_POINT ( 'NONE',  ( 2.799599750139214471, -1.450362073461785473, -1.321114446766240347 ) ) ;
#152709=CARTESIAN_POINT ( 'NONE',  ( 4.283913115580790354, 2.056533504189705930, -0.5163123687341104606 ) ) ;
#152713=CARTESIAN_POINT ( 'NONE',  ( 1.991162705694597301, 0.1987741427678466066, 2.060657922996151914 ) ) ;
#152716=CARTESIAN_POINT ( 'NONE',  ( 4.969482899335432968, -1.875980303166164376, -1.189202907730102732 ) ) ;
#152718=CARTESIAN_POINT ( 'NONE',  ( 1.793957786719975633, 1.699999873817940044, -1.547402956443538313 ) ) ;
#152725=CARTESIAN_POINT ( 'NONE',  ( 3.041163856788456687, 0.05134138945498378792, 1.911883771832747048 ) ) ;
#152727=CARTESIAN_POINT ( 'NONE',  ( 4.119902764342167956, -0.8871895459346083035, -1.478924549062347049 ) ) ;
#152728=CARTESIAN_POINT ( 'NONE',  ( 3.309780021317248355, -1.205041885261768808, -1.616693488061982098 ) ) ;
#152729=CARTESIAN_POINT ( 'NONE',  ( 3.850415763719742479, 0.2810032917593773272, -2.281380581095279858 ) ) ;
#152731=CARTESIAN_POINT ( 'NONE',  ( 6.604139054488365801, -2.105657007711879469, 0.04960021190137350877 ) ) ;
#152734=CARTESIAN_POINT ( 'NONE',  ( 4.305725593384774896, -1.765090080884828661, 0.1286423764911871492 ) ) ;
#152736=CARTESIAN_POINT ( 'NONE',  ( 0.3579208530809056543, 2.266420720034970415, -0.3425275222256763397 ) ) ;
#152737=CARTESIAN_POINT ( 'NONE',  ( 6.333933918656591722, 1.821832875601756774, 0.2651207078676054429 ) ) ;
#152740=CARTESIAN_POINT ( 'NONE',  ( 6.087848540548081999, -2.180536604488235941, -0.2183335821156970336 ) ) ;
#152743=CARTESIAN_POINT ( 'NONE',  ( -0.1298852118744100725, 0.003815113116375076861, -1.726395881205538663 ) ) ;
#152744=CARTESIAN_POINT ( 'NONE',  ( 0.3796378701454300453, -0.1059898317679157376, 2.168723291021804833 ) ) ;
#152745=CARTESIAN_POINT ( 'NONE',  ( 1.692592581891849912, 1.490968054865527304, -1.357870634957742961 ) ) ;
#152747=CARTESIAN_POINT ( 'NONE',  ( 4.371652425709642742, 1.868346805267994570, -0.4693074334855638630 ) ) ;
#152749=CARTESIAN_POINT ( 'NONE',  ( 1.529832089473160517, -0.2657924667638748017, 2.205375646708715998 ) ) ;
#152758=CARTESIAN_POINT ( 'NONE',  ( 4.370479661831958573, -0.005723030808118654937, -1.740626722379432501 ) ) ;
#152760=CARTESIAN_POINT ( 'NONE',  ( 2.084357000244409175, 1.132115006494602394, -1.602057852124554316 ) ) ;
#152766=CARTESIAN_POINT ( 'NONE',  ( 0.2915633711191143451, -1.886499572934543956, 0.8344948317597818965 ) ) ;
#152769=CARTESIAN_POINT ( 'NONE',  ( 5.366422816783521732, -1.968444216653497003, -0.4370823996120917765 ) ) ;
#152770=CARTESIAN_POINT ( 'NONE',  ( 1.007111469781604596, 1.711705730394815106, -1.479659443445595413 ) ) ;
#152774=CARTESIAN_POINT ( 'NONE',  ( 1.247088714334358972, -1.471066981041386335, -1.155250539242147045 ) ) ;
#152775=CARTESIAN_POINT ( 'NONE',  ( 0.01762850287782054270, -1.587011929513387098, 0.6995264333442567928 ) ) ;
#152776=CARTESIAN_POINT ( 'NONE',  ( 3.861010967126535576, 0.2669419790740577558, -2.175157288012785184 ) ) ;
#152777=CARTESIAN_POINT ( 'NONE',  ( 5.825286519090714599, -0.06434016213947668650, 2.306860349555530654 ) ) ;
#152778=CARTESIAN_POINT ( 'NONE',  ( 0.7607050128039081205, -1.493160483426679841, 1.420726879377065988 ) ) ;
#152779=CARTESIAN_POINT ( 'NONE',  ( 3.908095550721983447, 1.372505747409875632, -1.374073360379985065 ) ) ;
#152782=CARTESIAN_POINT ( 'NONE',  ( 6.046149701670225696, 1.868418987705861234, 0.09211505606019490533 ) ) ;
#152785=CARTESIAN_POINT ( 'NONE',  ( 4.395157833011634096, -0.8647231026696032830, -1.821742675176166060 ) ) ;
#152789=CARTESIAN_POINT ( 'NONE',  ( 1.928079105319381314, 1.052063804484974385, -1.491885150056403431 ) ) ;
#152799=CARTESIAN_POINT ( 'NONE',  ( 5.777991907792089599, 1.989422559269612201, -0.3473161181037613954 ) ) ;
#152800=CARTESIAN_POINT ( 'NONE',  ( -0.1104750535120025967, -0.004616138082884357029, -2.103378236956429337 ) ) ;
#152804=CARTESIAN_POINT ( 'NONE',  ( 5.225487584538335284, -1.957599804553040945, 0.6444962787128440951 ) ) ;
#152805=CARTESIAN_POINT ( 'NONE',  ( 3.586564705785996843, -0.5826563296015655480, 1.930417576838711957 ) ) ;
#152814=CARTESIAN_POINT ( 'NONE',  ( 4.182970119252515495, -1.034007530860373336, -1.730600854597413640 ) ) ;
#152815=CARTESIAN_POINT ( 'NONE',  ( 3.380630241506640932, 1.664009615612583204, -0.7882418170854917916 ) ) ;
#152819=CARTESIAN_POINT ( 'NONE',  ( 1.612422076237954860, -2.289831013633353063, 0.2861181584819341706 ) ) ;
#152821=CARTESIAN_POINT ( 'NONE',  ( 4.815789973571149574, -2.120931333841672650, 0.4164600335647972162 ) ) ;
#152823=CARTESIAN_POINT ( 'NONE',  ( 6.614805131849967879, -0.1256686391097518729, 1.812046779126045726 ) ) ;
#152827=CARTESIAN_POINT ( 'NONE',  ( 1.815107966846595255, -0.2319292346777863389, 1.856160199827073587 ) ) ;
#152828=CARTESIAN_POINT ( 'NONE',  ( 6.719606758044225359, -1.912400718708512581, 0.4786219606899063117 ) ) ;
#152832=CARTESIAN_POINT ( 'NONE',  ( 1.137671262558290763, -1.993743905544292927, 0.9465009238469668240 ) ) ;
#152839=CARTESIAN_POINT ( 'NONE',  ( 6.385619905723967094, 1.359199996644964381, 1.428251207276862500 ) ) ;
#152841=CARTESIAN_POINT ( 'NONE',  ( 0.6402171227658737251, -1.634652429315278654, -1.629011242183490804 ) ) ;
#152842=CARTESIAN_POINT ( 'NONE',  ( 0.6253529088778920775, 0.1960189665039281104, -1.952063659030291998 ) ) ;
#152843=CARTESIAN_POINT ( 'NONE',  ( 4.645415531332927728, 1.844630620182326153, -0.9228673458712335353 ) ) ;
#152851=CARTESIAN_POINT ( 'NONE',  ( 6.408646267151912213, 0.6747503738608184864, 2.063755040143978370 ) ) ;
#152852=CARTESIAN_POINT ( 'NONE',  ( 4.845164456061270997, 0.5726227986864868003, -1.750029900461601340 ) ) ;
#152854=CARTESIAN_POINT ( 'NONE',  ( 0.3857445262360515437, -0.8876765639535091346, 1.646530163845527195 ) ) ;
#152858=CARTESIAN_POINT ( 'NONE',  ( 1.277824965264368728, 1.883817941867833134, -0.3277997056638781714 ) ) ;
#152859=CARTESIAN_POINT ( 'NONE',  ( 2.148939158097754376, -1.419410118233652485, -1.056944606630695560 ) ) ;
#152860=CARTESIAN_POINT ( 'NONE',  ( 6.375645430456404306, 0.3419251235410331602, -1.983688181122665650 ) ) ;
#152862=CARTESIAN_POINT ( 'NONE',  ( 4.657778235022878022, 1.106396155499450140, 1.563574394034000115 ) ) ;
#152864=CARTESIAN_POINT ( 'NONE',  ( 5.951603224533720038, 1.490215702738381331, 1.287855809377226102 ) ) ;
#152865=CARTESIAN_POINT ( 'NONE',  ( -0.06985027309261250539, -2.078401542846250116, 0.4200961532789050379 ) ) ;
#152867=CARTESIAN_POINT ( 'NONE',  ( 3.871829239884491791, 1.038646522470688671, 1.555605274479121114 ) ) ;
#152868=CARTESIAN_POINT ( 'NONE',  ( 6.041572768212772893, -1.254329016146822351, -1.184272192918204514 ) ) ;
#152870=CARTESIAN_POINT ( 'NONE',  ( 3.528125218122651230, -1.314342534882004809, -1.772652456903674567 ) ) ;
#152873=CARTESIAN_POINT ( 'NONE',  ( 0.7310139678005268538, -1.941628062548940381, -0.6965263486069167564 ) ) ;
#152880=CARTESIAN_POINT ( 'NONE',  ( 2.840353284027045344, -1.066491845456703835, 1.774417039089710935 ) ) ;
#152884=CARTESIAN_POINT ( 'NONE',  ( 1.084635305120797089, -1.279634344436600513, 1.562581769784775920 ) ) ;
#152886=CARTESIAN_POINT ( 'NONE',  ( 0.1749903794560749015, 6.948553613792602057, -2.550375946188668586 ) ) ;
#152888=CARTESIAN_POINT ( 'NONE',  ( 6.134138708105167481, 0.1511139231759016377, -2.010518800921741622 ) ) ;
#152889=CARTESIAN_POINT ( 'NONE',  ( 6.368375084315238688, -1.880202862833039834, -0.3662410793365057926 ) ) ;
#152891=CARTESIAN_POINT ( 'NONE',  ( 3.913774547416096095, -1.127657808996849198, -1.879056921112079115 ) ) ;
#152893=CARTESIAN_POINT ( 'NONE',  ( 2.900541297466651347, -1.884798985816903860, -0.3226963764228693576 ) ) ;
#152897=CARTESIAN_POINT ( 'NONE',  ( 1.089470510105726708, -0.4871801946146369078, 1.956568126268923846 ) ) ;
#152900=CARTESIAN_POINT ( 'NONE',  ( 6.374583145400191775, -0.1054333438532777389, -2.189162923280890904 ) ) ;
#152902=CARTESIAN_POINT ( 'NONE',  ( 3.451896303776471608, 1.724958192144626867, 0.0007732285732166971348 ) ) ;
#152909=CARTESIAN_POINT ( 'NONE',  ( 1.082386330805637398, 1.171445227557347923, -1.573568114121715933 ) ) ;
#152912=CARTESIAN_POINT ( 'NONE',  ( 0.07536363704233051131, 7.629137130509080045, -2.744199452819145790 ) ) ;
#152916=CARTESIAN_POINT ( 'NONE',  ( 3.545387212860445114, -1.672524232984048620, 0.6962571228125400413 ) ) ;
#152920=CARTESIAN_POINT ( 'NONE',  ( 5.443967095383744237, -1.154075521934978532, -1.396247737120015930 ) ) ;
#152924=CARTESIAN_POINT ( 'NONE',  ( 5.389040371011321717, 0.1367655989435011543, 1.856064314752596145 ) ) ;
#152926=CARTESIAN_POINT ( 'NONE',  ( 2.513182649960711945, -1.786459940013595205, 0.6919045257178286779 ) ) ;
#152934=CARTESIAN_POINT ( 'NONE',  ( 0.1456854043008250221, -1.672057201651616642, -1.369741535119282982 ) ) ;
#152936=CARTESIAN_POINT ( 'NONE',  ( 1.693425821628431471, -0.7032018978916483309, 1.968960419152628871 ) ) ;
#152938=CARTESIAN_POINT ( 'NONE',  ( 6.334985678650366658, 0.1896739171414266178, 1.917017188598265420 ) ) ;
#152941=CARTESIAN_POINT ( 'NONE',  ( 2.397230751819504402, 1.409552409829779140, 1.160114028286141075 ) ) ;
#152943=CARTESIAN_POINT ( 'NONE',  ( 1.828231037913151447, -0.9045423626323212396, -1.684975973026317408 ) ) ;
#152944=CARTESIAN_POINT ( 'NONE',  ( 1.223035424556912387, -1.779184897175438707, -0.8450996447877844320 ) ) ;
#152945=CARTESIAN_POINT ( 'NONE',  ( 4.089352007823720214, -0.7402336266850146895, 1.795645171352943770 ) ) ;
#152950=CARTESIAN_POINT ( 'NONE',  ( 3.955424862866574021, -1.843446357660895041, 1.048082435718917571 ) ) ;
#152958=CARTESIAN_POINT ( 'NONE',  ( 4.248545464119923842, 0.4890907236730773766, 1.758887239191930796 ) ) ;
#152964=CARTESIAN_POINT ( 'NONE',  ( 4.680451076648031616, -1.814532364864028136, -0.4542276060127621862 ) ) ;
#152967=CARTESIAN_POINT ( 'NONE',  ( 2.227063406323766870, -8.064668077616128736E-05, 1.926676517253867793 ) ) ;
#152975=CARTESIAN_POINT ( 'NONE',  ( 0.8435474745839615096, 0.4086855458026328880, -2.077256349191716200 ) ) ;
#152978=CARTESIAN_POINT ( 'NONE',  ( 5.858279169847476098, -2.070434559870216074, -0.005763162253501209233 ) ) ;
#152979=CARTESIAN_POINT ( 'NONE',  ( 0.4504185290156897947, -1.555054577268409899, -0.9855837367087336709 ) ) ;
#152981=CARTESIAN_POINT ( 'NONE',  ( 6.082725252809636274, -0.7780705872160005310, 2.163147651226764889 ) ) ;
#152985=CARTESIAN_POINT ( 'NONE',  ( 1.008267258593512183, -1.035053087846869335, -2.045343892876672065 ) ) ;
#152988=CARTESIAN_POINT ( 'NONE',  ( 6.140568862321206467, -1.639224632874112020, 1.040935801138809236 ) ) ;
#152992=CARTESIAN_POINT ( 'NONE',  ( -0.1228044941411730595, -1.800067586368118588, -0.9016598371343366169 ) ) ;
#152996=CARTESIAN_POINT ( 'NONE',  ( 3.240259679068544507, 0.5084995621511109176, 2.027717503869540749 ) ) ;
#152997=CARTESIAN_POINT ( 'NONE',  ( 1.287592460671227457, -0.8000790430911768336, 1.578758917787604021 ) ) ;
#152999=CARTESIAN_POINT ( 'NONE',  ( 4.330218815260163723, 2.247629863848239040, 0.4493651543184833397 ) ) ;
#153000=CARTESIAN_POINT ( 'NONE',  ( 3.538731034799988073, -1.318886434843706601, -1.135564254951209273 ) ) ;
#153004=CARTESIAN_POINT ( 'NONE',  ( 2.987300135396570688, 1.631410314640189929, 0.5874552976607245736 ) ) ;
#153005=CARTESIAN_POINT ( 'NONE',  ( 3.543588177981399134, 1.964110833604881812, -0.9256020844959752525 ) ) ;
#153007=CARTESIAN_POINT ( 'NONE',  ( 4.188685576152741064, 1.555700494002542067, -1.282988152656767911 ) ) ;
#153008=CARTESIAN_POINT ( 'NONE',  ( 2.062500000000001776, -1.451031289061204266, -1.451031289061035956 ) ) ;
#153011=CARTESIAN_POINT ( 'NONE',  ( 1.483290174073574441, 1.780938433730950621, -0.7347945396837353149 ) ) ;
#153013=CARTESIAN_POINT ( 'NONE',  ( 4.974942202162922378, -1.608427002576447995, 1.532403895573146491 ) ) ;
#153015=CARTESIAN_POINT ( 'NONE',  ( 6.883263157960373135, 2.058310207169287143, 2.252834201749584153 ) ) ;
#153021=CARTESIAN_POINT ( 'NONE',  ( 0.2413015266095243083, 2.127564327900688390, 0.6385326005407893080 ) ) ;
#153022=CARTESIAN_POINT ( 'NONE',  ( 6.268018250734934682, -1.947192974725008963, 0.2387856323943157166 ) ) ;
#153025=CARTESIAN_POINT ( 'NONE',  ( 0.4566077865506940059, 0.8268718848777978359, 1.997384878126715613 ) ) ;
#153029=CARTESIAN_POINT ( 'NONE',  ( 3.807127647779250168, -1.688003362470591684, 1.185206751978077788 ) ) ;
#153033=CARTESIAN_POINT ( 'NONE',  ( 4.692568346783878575, -0.4079999995015987091, -1.825350503840660110 ) ) ;
#153034=CARTESIAN_POINT ( 'NONE',  ( 4.131323472851686773, 0.4681366286901997853, 1.669664985128198831 ) ) ;
#153035=CARTESIAN_POINT ( 'NONE',  ( 3.843067196288481480, 0.5821562417002418277, -1.640339850388317089 ) ) ;
#153036=CARTESIAN_POINT ( 'NONE',  ( 0.6797070353673840826, 1.544897314466355143, 1.693757226825955753 ) ) ;
#153038=CARTESIAN_POINT ( 'NONE',  ( 4.511325128988150190, -2.050071535818901225, 0.4094859698564096706 ) ) ;
#153039=CARTESIAN_POINT ( 'NONE',  ( 0.4273693582952375891, 0.9489586001507933632, -1.577591209259328275 ) ) ;
#153042=CARTESIAN_POINT ( 'NONE',  ( 1.266250242576156815, 1.862016182229693673, -0.7743172429433076154 ) ) ;
#153047=CARTESIAN_POINT ( 'NONE',  ( 2.315225504062240702, 1.701464259299827919, -1.265282535349021575 ) ) ;
#153049=CARTESIAN_POINT ( 'NONE',  ( 5.936143289257818978, 0.8957264799932495025, -1.590785280889392528 ) ) ;
#153054=CARTESIAN_POINT ( 'NONE',  ( 1.916276942859599597, -2.019257470013501088, 0.05376132052286108215 ) ) ;
#153055=CARTESIAN_POINT ( 'NONE',  ( 0.07735805125222078305, -0.0005418671161615954465, -2.088975025666544472 ) ) ;
#153058=CARTESIAN_POINT ( 'NONE',  ( 4.117883143796479573, 1.847306362133010360, -0.2240370018555241372 ) ) ;
#153065=CARTESIAN_POINT ( 'NONE',  ( 4.969292227364340953, 0.1756445257206709631, -1.817221496977147854 ) ) ;
#153069=CARTESIAN_POINT ( 'NONE',  ( 1.668881318695322413, -0.6185640615885504845, -1.619952590838618312 ) ) ;
#153070=CARTESIAN_POINT ( 'NONE',  ( 0.6732859938517594678, -0.9703907760119870884, 1.444448127723398478 ) ) ;
#153071=CARTESIAN_POINT ( 'NONE',  ( 5.531924057230363623, -1.459877215294088204, -1.787231782134098168 ) ) ;
#153073=CARTESIAN_POINT ( 'NONE',  ( 1.440775599906311433, 0.3991536164789717955, 2.021572055866586837 ) ) ;
#153075=CARTESIAN_POINT ( 'NONE',  ( 0.5442957877539145173, 1.882187304385819493, -0.7230256762977352869 ) ) ;
#153078=CARTESIAN_POINT ( 'NONE',  ( 0.2156151883831447236, -1.933912933822299784, 0.3821239771369787097 ) ) ;
#153079=CARTESIAN_POINT ( 'NONE',  ( 3.463059065379545221, -1.560675823418774533, 1.104941681961457256 ) ) ;
#153082=CARTESIAN_POINT ( 'NONE',  ( 4.582781371344160526, -2.140174514510746029, -0.5380331057033281850 ) ) ;
#153087=CARTESIAN_POINT ( 'NONE',  ( 5.901066629635802308, -0.3109326959268610691, -2.097457242586676429 ) ) ;
#153090=CARTESIAN_POINT ( 'NONE',  ( 3.663348518144835086, -2.033753252616496532, -1.090341736564947484 ) ) ;
#153091=CARTESIAN_POINT ( 'NONE',  ( 4.211346380768822506, -1.629847038978438079, -1.091715234301626314 ) ) ;
#153093=CARTESIAN_POINT ( 'NONE',  ( 0.6550357524967264089, 1.634203043994170157, -1.084997510809107446 ) ) ;
#153097=CARTESIAN_POINT ( 'NONE',  ( 6.315638730379727228, -1.320822524126588515, -1.523799118890494020 ) ) ;
#153100=CARTESIAN_POINT ( 'NONE',  ( 3.274467656630496659, -1.066080149914239161, -1.891199154716957098 ) ) ;
#153102=CARTESIAN_POINT ( 'NONE',  ( 0.8266187642571948269, -0.9586779626098644869, -1.891633453305548773 ) ) ;
#153108=CARTESIAN_POINT ( 'NONE',  ( 0.7025034608351670151, -0.6919086601019829308, -1.941309234904058600 ) ) ;
#153114=CARTESIAN_POINT ( 'NONE',  ( 4.459560945705238311, -1.480416612418914646, -1.210464771850598975 ) ) ;
#153119=CARTESIAN_POINT ( 'NONE',  ( 0.1932431142802397694, 1.690279412936572134, -0.6521791651670250101 ) ) ;
#153121=CARTESIAN_POINT ( 'NONE',  ( 0.7256311455483875905, 0.7733690622436960593, -1.752846625659326696 ) ) ;
#153122=CARTESIAN_POINT ( 'NONE',  ( 1.592325325408463055, 1.022198633559557646, -1.800363622228560168 ) ) ;
#153124=CARTESIAN_POINT ( 'NONE',  ( 0.9539096209374531288, 1.969307747869667446, -0.09461285551524113713 ) ) ;
#153125=CARTESIAN_POINT ( 'NONE',  ( 3.281694405262673087, 1.158851912627656189, 1.410738560442346801 ) ) ;
#153126=CARTESIAN_POINT ( 'NONE',  ( 6.305322857734435793, 1.832379230283949667, 1.229636283518860118 ) ) ;
#153129=CARTESIAN_POINT ( 'NONE',  ( 4.281722439037777050, -1.974808133235542495, 0.5956899724020509046 ) ) ;
#153134=CARTESIAN_POINT ( 'NONE',  ( 5.227606396355295892, -2.000638224736817516, 0.6578950869102012655 ) ) ;
#153136=CARTESIAN_POINT ( 'NONE',  ( 6.250451049865752395, -2.060019788584551481, -0.2068627631737207651 ) ) ;
#153138=CARTESIAN_POINT ( 'NONE',  ( 3.585389192675687564, 1.955840111083558597, -0.9206723451176119788 ) ) ;
#153139=CARTESIAN_POINT ( 'NONE',  ( 4.670572394037289854, 0.7749771354828223213, 1.865277368486473630 ) ) ;
#153144=CARTESIAN_POINT ( 'NONE',  ( 2.606657977298726614, 1.900416011228076130, 0.6748465934659984011 ) ) ;
#153152=CARTESIAN_POINT ( 'NONE',  ( 4.359000025081374297, -0.002827702239943663542, -2.016598147179492262 ) ) ;
#153155=CARTESIAN_POINT ( 'NONE',  ( 6.159189016523521687, -1.482050057771692186, -0.8820200739605223994 ) ) ;
#153160=CARTESIAN_POINT ( 'NONE',  ( 5.975831987570860981, 1.113884111790110820, 1.502598383168303409 ) ) ;
#153161=CARTESIAN_POINT ( 'NONE',  ( -0.07552757677437360595, -0.8618087116909570744, -1.817275918844815541 ) ) ;
#153166=CARTESIAN_POINT ( 'NONE',  ( 0.8785300617164050196, -0.4926655378557908138, -1.955167820405806056 ) ) ;
#153173=CARTESIAN_POINT ( 'NONE',  ( 5.976186790766067958, -1.906884764771042517, -0.1824196792480689000 ) ) ;
#153181=CARTESIAN_POINT ( 'NONE',  ( 2.553791647773369089, 0.5774160426356907960, -2.083079400968433248 ) ) ;
#153184=CARTESIAN_POINT ( 'NONE',  ( 0.4047333657465709278, -2.105317319661216047, -0.2534319464195868843 ) ) ;
#153185=CARTESIAN_POINT ( 'NONE',  ( 5.596661130663158623, -0.4455768995972574364, -1.770251349769519367 ) ) ;
#153187=CARTESIAN_POINT ( 'NONE',  ( 1.897670943237000918, -0.6677869454260307869, 1.854917580456706183 ) ) ;
#153188=CARTESIAN_POINT ( 'NONE',  ( 4.799029005866479736, -0.2398712174674077491, -1.897248949554980024 ) ) ;
#153191=CARTESIAN_POINT ( 'NONE',  ( 5.441845355777640059, 1.321472782793672085, 1.460616519443626249 ) ) ;
#153192=CARTESIAN_POINT ( 'NONE',  ( 0.09355730106928944467, -1.941490229121365374, -0.04880333718709597285 ) ) ;
#153199=CARTESIAN_POINT ( 'NONE',  ( 5.443983014310386892, -1.216401775450553169, -1.475513148251464068 ) ) ;
#153203=CARTESIAN_POINT ( 'NONE',  ( 1.061882456046374434, 0.4290601450722114074, -2.164491299336705588 ) ) ;
#153205=CARTESIAN_POINT ( 'NONE',  ( 6.463545146426397991, -1.618288576614915764, -1.197193900782191234 ) ) ;
#153209=CARTESIAN_POINT ( 'NONE',  ( 2.928250347896840022, 1.105370970781336837, 1.750397071514836478 ) ) ;
#153213=CARTESIAN_POINT ( 'NONE',  ( 1.077287230265553397, -0.05381693868444264311, -2.161191418701657430 ) ) ;
#153218=CARTESIAN_POINT ( 'NONE',  ( 6.925078400183562799, 2.053856789352814793, 2.261525409452989965 ) ) ;
#153220=CARTESIAN_POINT ( 'NONE',  ( 5.959525138608227302, -1.649545596257080637, -0.5353374286216765476 ) ) ;
#153222=CARTESIAN_POINT ( 'NONE',  ( 3.151297481648129395, 1.777980080355131109, -1.060267355625019503 ) ) ;
#153223=CARTESIAN_POINT ( 'NONE',  ( 4.816069135992575134, 1.087346734782314472, -1.816536155142484121 ) ) ;
#153226=CARTESIAN_POINT ( 'NONE',  ( 2.360148646665951144, -1.969129416856093551, 0.04326586078102003657 ) ) ;
#153227=CARTESIAN_POINT ( 'NONE',  ( 1.142663480069527671, 1.843847066288730074, 0.5072560978593986247 ) ) ;
#153228=CARTESIAN_POINT ( 'NONE',  ( 4.453268702153020620, 0.5046191974597475927, -2.235886964606835559 ) ) ;
#153229=CARTESIAN_POINT ( 'NONE',  ( 2.297230901563730665, 1.410920830412419003, 1.158640757216542028 ) ) ;
#153233=CARTESIAN_POINT ( 'NONE',  ( 3.304942742240731590, -0.3968801077466362903, -1.973537420673168397 ) ) ;
#153234=CARTESIAN_POINT ( 'NONE',  ( 3.274216958324972726, -0.9628348462043828659, -1.709115330885315087 ) ) ;
#153237=CARTESIAN_POINT ( 'NONE',  ( 0.07536363704235825300, -0.001874865094115065866, -2.144269471569634433 ) ) ;
#153238=CARTESIAN_POINT ( 'NONE',  ( 6.685487044060022477, -0.8959250478542144513, 1.887356362924677233 ) ) ;
#153239=CARTESIAN_POINT ( 'NONE',  ( 4.926482082969720899, 1.694141084728201907, 0.5120089106541975132 ) ) ;
#153240=CARTESIAN_POINT ( 'NONE',  ( 0.6916816545035618935, -0.7852976098030055585, 2.046091368998310678 ) ) ;
#153241=CARTESIAN_POINT ( 'NONE',  ( 6.527322169609689695, -1.143008000885838760, -1.312471774050189444 ) ) ;
#153243=CARTESIAN_POINT ( 'NONE',  ( 0.1331715793776314105, 6.947497095909970000, -2.548608419791003055 ) ) ;
#153244=CARTESIAN_POINT ( 'NONE',  ( 1.159977488309314797, -0.5597072352675269702, -2.229110579909891143 ) ) ;
#153245=CARTESIAN_POINT ( 'NONE',  ( 0.8553300576445364012, 0.4222666777726029608, -2.150330908352434012 ) ) ;
#153246=CARTESIAN_POINT ( 'NONE',  ( 3.510573375967055654, -0.8941257848905452832, -2.017821460644920073 ) ) ;
#153248=CARTESIAN_POINT ( 'NONE',  ( 0.2393977111345606534, -0.1477851991248577135, -2.137246755706405210 ) ) ;
#153250=CARTESIAN_POINT ( 'NONE',  ( 1.218125882790439762, 1.038422275552937757, -1.845119264165562711 ) ) ;
#153251=CARTESIAN_POINT ( 'NONE',  ( 3.562500000000002665, -1.451031289061261109, -1.451031289060973561 ) ) ;
#153253=CARTESIAN_POINT ( 'NONE',  ( 5.174797004712035076, -1.813887718507047220, -0.6490126392820031453 ) ) ;
#153255=CARTESIAN_POINT ( 'NONE',  ( 1.505871038028598230, -2.274393761632488964, 0.2862045095256612326 ) ) ;
#153259=CARTESIAN_POINT ( 'NONE',  ( 3.405137934272496558, -0.4347481476216079055, -2.178183672434565565 ) ) ;
#153266=CARTESIAN_POINT ( 'NONE',  ( 1.459611520199757706, -1.915600648959712382, -0.6298732728240025169 ) ) ;
#153268=CARTESIAN_POINT ( 'NONE',  ( 6.619587925713169341, 0.3565228922877783924, -2.031493691534612012 ) ) ;
#153270=CARTESIAN_POINT ( 'NONE',  ( 6.093256065386793985, -0.5776499228958801302, 1.641946315008017576 ) ) ;
#153273=CARTESIAN_POINT ( 'NONE',  ( 1.194210174654856127, -0.4229520329555501723, -1.718335688698314101 ) ) ;
#153274=CARTESIAN_POINT ( 'NONE',  ( 1.494767762416524093, -2.000856930885573259, 0.2496086726550551249 ) ) ;
#153275=CARTESIAN_POINT ( 'NONE',  ( 0.2394788589213901198, 1.836227513651207177, 0.1364553164684492448 ) ) ;
#153276=CARTESIAN_POINT ( 'NONE',  ( 4.177453601039508690, 1.497175104222212783, 1.735980874517801587 ) ) ;
#153277=CARTESIAN_POINT ( 'NONE',  ( 3.433393508698717511, 0.8267853122289525736, -1.645126075773599039 ) ) ;
#153281=CARTESIAN_POINT ( 'NONE',  ( 4.594645031659345236, -0.4005623417570289280, -1.780931357837008733 ) ) ;
#153282=CARTESIAN_POINT ( 'NONE',  ( 4.957657809308734898, -1.899617967926207740, -0.6767155953601932117 ) ) ;
#153284=CARTESIAN_POINT ( 'NONE',  ( 2.958202477073975878, 2.251720482184274008, -0.2206431264100849887 ) ) ;
#153286=CARTESIAN_POINT ( 'NONE',  ( 6.001026715709635972, 1.723673884808615497, -1.209685691799726737 ) ) ;
#153288=CARTESIAN_POINT ( 'NONE',  ( 3.068866956829822801, 1.501395149897828851, -1.425812640530661479 ) ) ;
#153291=CARTESIAN_POINT ( 'NONE',  ( 5.901066629635801419, -0.3109326959268611246, -2.097457242586676429 ) ) ;
#153293=CARTESIAN_POINT ( 'NONE',  ( 2.227063406323766870, -8.064668077616128736E-05, 1.926676517253867793 ) ) ;
#153296=CARTESIAN_POINT ( 'NONE',  ( 6.385607329849364078, -1.855618941174362879, 0.6602924305801564087 ) ) ;
#153301=CARTESIAN_POINT ( 'NONE',  ( 0.8443251495477720470, -1.414827328263716266, -1.712562173056450643 ) ) ;
#153303=CARTESIAN_POINT ( 'NONE',  ( 3.487430266828908998, 1.904693919176775552, -0.8987260315082377105 ) ) ;
#153306=CARTESIAN_POINT ( 'NONE',  ( 0.7306206827372868640, -1.750454575335522067, -0.6323700682324316924 ) ) ;
#153312=CARTESIAN_POINT ( 'NONE',  ( 0.7387272492362946252, 1.258454933865692293, -1.706699550108881080 ) ) ;
#153315=CARTESIAN_POINT ( 'NONE',  ( 4.826587731031282580, -1.282962940432516907, 1.484285152025546672 ) ) ;
#153316=CARTESIAN_POINT ( 'NONE',  ( 2.413140945657660907, 1.930630709398067246, 0.9725960170764782475 ) ) ;
#153317=CARTESIAN_POINT ( 'NONE',  ( 1.557894219809667247, -1.301531972126177772, 1.302644501960325885 ) ) ;
#153320=CARTESIAN_POINT ( 'NONE',  ( 3.591523995615089948, -1.738451970352115961, -0.08344189160913899339 ) ) ;
#153324=CARTESIAN_POINT ( 'NONE',  ( 1.217891636700708435, -2.108894920778502602, 0.4742063263511315796 ) ) ;
#153326=CARTESIAN_POINT ( 'NONE',  ( 3.550157523342875709, 1.823840110401256931, -0.8594984857327039318 ) ) ;
#153328=CARTESIAN_POINT ( 'NONE',  ( 0.1808504484964272296, -2.097240537080494516, -0.5235256853268267507 ) ) ;
#153330=CARTESIAN_POINT ( 'NONE',  ( 3.080892710809614243, -0.1436740641204778401, -1.966277672030048107 ) ) ;
#153331=CARTESIAN_POINT ( 'NONE',  ( 6.609000000000036401, 7.629137130509092479, 2.600000000000000977 ) ) ;
#153332=CARTESIAN_POINT ( 'NONE',  ( 2.226030366740273880, 1.884328139559983573, 0.4695921692644353107 ) ) ;
#153338=CARTESIAN_POINT ( 'NONE',  ( -0.1108833634137010027, 1.377173795795206157, -2.152720132533674668 ) ) ;
#153344=CARTESIAN_POINT ( 'NONE',  ( 6.545943480548680249, 0.8917086005404940563, -2.128542236993334669 ) ) ;
#153345=CARTESIAN_POINT ( 'NONE',  ( 6.584431417889404337, 1.130572321132311098, -1.603143135845342515 ) ) ;
#153347=CARTESIAN_POINT ( 'NONE',  ( 3.836726278109466204, -1.889416792123297162, -0.5274722977551549175 ) ) ;
#153349=CARTESIAN_POINT ( 'NONE',  ( 1.635388916632842360, 0.6352005984417673501, 1.913803229121699534 ) ) ;
#153351=CARTESIAN_POINT ( 'NONE',  ( 2.448581487809509571, -1.456371601587917120, 1.537162028231451538 ) ) ;
#153355=CARTESIAN_POINT ( 'NONE',  ( 3.661895226921572100, -1.235415792305821103, 1.365283978338522441 ) ) ;
#153359=CARTESIAN_POINT ( 'NONE',  ( 3.849942018323779358, -1.464806807754112539, -1.533599281611098597 ) ) ;
#153362=CARTESIAN_POINT ( 'NONE',  ( 5.764934849280819229, -1.861221615537820728, -0.8850300128313455250 ) ) ;
#153364=CARTESIAN_POINT ( 'NONE',  ( 2.577489280727011778, -0.9446877197298314544, 1.580272903027237774 ) ) ;
#153370=CARTESIAN_POINT ( 'NONE',  ( 2.157103830005083100, -1.704838622333640030, 1.401371054633032909 ) ) ;
#153371=CARTESIAN_POINT ( 'NONE',  ( 3.866728509311831985, -1.522874988181441180, 1.673262526929709670 ) ) ;
#153373=CARTESIAN_POINT ( 'NONE',  ( 3.586021145937230870, 1.010873021915110748, 1.503094931805592394 ) ) ;
#153374=CARTESIAN_POINT ( 'NONE',  ( 4.645656780685024856, 1.893963204498310571, -0.2871864570129621375 ) ) ;
#153376=CARTESIAN_POINT ( 'NONE',  ( 4.434422825387909661, 1.933224968735423266, 0.3856102937377944295 ) ) ;
#153377=CARTESIAN_POINT ( 'NONE',  ( 1.043825456435763410, 0.7835056195745603302, -1.760039731681047215 ) ) ;
#153378=CARTESIAN_POINT ( 'NONE',  ( 4.926551758443064699, 1.790249073151507497, 0.5424879929923772659 ) ) ;
#153379=CARTESIAN_POINT ( 'NONE',  ( 3.739178398684524396, 0.3374720328367666888, 2.282779155512550062 ) ) ;
#153380=CARTESIAN_POINT ( 'NONE',  ( 4.615577964900333008, 0.4086796715298928184, -1.815441397462829398 ) ) ;
#153382=CARTESIAN_POINT ( 'NONE',  ( 0.5324358445358172709, 0.5899921999869184308, 1.928256190492839028 ) ) ;
#153384=CARTESIAN_POINT ( 'NONE',  ( 1.524195097446314318, -1.171203135327163913, -1.750160316008353201 ) ) ;
#153388=CARTESIAN_POINT ( 'NONE',  ( 6.573507624224045109, 2.070638407997299257, -0.6205318887850322929 ) ) ;
#153389=CARTESIAN_POINT ( 'NONE',  ( 3.269896953881154644, 0.5115095171020591636, -2.057881918134551125 ) ) ;
#153391=CARTESIAN_POINT ( 'NONE',  ( 1.019792603244329410, -0.4866989216864863188, 1.960159232486478498 ) ) ;
#153396=CARTESIAN_POINT ( 'NONE',  ( 1.792469030454997059, -2.151019407201111289, -0.2137723215496489249 ) ) ;
#153397=CARTESIAN_POINT ( 'NONE',  ( 6.610000000000026965, 7.052677709320480659, 2.598153670447616470 ) ) ;
#153399=CARTESIAN_POINT ( 'NONE',  ( 6.825078400183553384, 0.5907600490881077526, 1.908621492364571903 ) ) ;
#153402=CARTESIAN_POINT ( 'NONE',  ( 5.489470343000498076, -0.4852711138302409077, 1.957169415941109047 ) ) ;
#153406=CARTESIAN_POINT ( 'NONE',  ( 6.462449937854951365, -1.911777437574797345, -0.8467615847161328313 ) ) ;
#153408=CARTESIAN_POINT ( 'NONE',  ( 0.08136044664198981147, -0.1580758092474404408, -2.227059435111256924 ) ) ;
#153415=CARTESIAN_POINT ( 'NONE',  ( 3.633171361085251849, -1.593041208078986193, 0.6618793944016196917 ) ) ;
#153417=CARTESIAN_POINT ( 'NONE',  ( 1.510649146982666613, 1.557664219135522110, 0.8400682108315477015 ) ) ;
#153419=CARTESIAN_POINT ( 'NONE',  ( 2.895184040856535468, -0.1504547458161388240, -2.007539188286605825 ) ) ;
#153421=CARTESIAN_POINT ( 'NONE',  ( 5.333140672905051893, 0.1575165696711364749, 2.201206011701982934 ) ) ;
#153423=CARTESIAN_POINT ( 'NONE',  ( 4.306902303582704761, -0.4466378413249347257, -1.969604032634456825 ) ) ;
#153425=CARTESIAN_POINT ( 'NONE',  ( 4.266349992362879817, 2.119992548681798095, -0.05317809935000831351 ) ) ;
#153426=CARTESIAN_POINT ( 'NONE',  ( 3.761342352588430860, 1.897692735847063661, -0.6820134568972098243 ) ) ;
#153427=CARTESIAN_POINT ( 'NONE',  ( 4.482537919100934687, -1.178242479775050811, 1.376196796631526720 ) ) ;
#153431=CARTESIAN_POINT ( 'NONE',  ( 1.815107966846595255, -0.2319292346777863389, 1.856160199827073587 ) ) ;
#153434=CARTESIAN_POINT ( 'NONE',  ( 5.690068458729246714, 1.084374654971603569, 1.450890516563392518 ) ) ;
#153440=CARTESIAN_POINT ( 'NONE',  ( 0.5977379272000953314, 1.286164058678052946, 1.415416067018962387 ) ) ;
#153442=CARTESIAN_POINT ( 'NONE',  ( 1.820681965693775162, -1.389665069980907441, 1.385087887197037571 ) ) ;
#153445=CARTESIAN_POINT ( 'NONE',  ( 3.656581996618038843, 2.110704406498860486, 0.2042969539849878724 ) ) ;
#153446=CARTESIAN_POINT ( 'NONE',  ( -0.02948999725182511675, 6.948707995275583471, -2.521364601437687369 ) ) ;
#153447=CARTESIAN_POINT ( 'NONE',  ( 5.958271952116948711, 0.7966545185628256531, 1.803378638538119860 ) ) ;
#153449=CARTESIAN_POINT ( 'NONE',  ( 0.7561087546162044148, 0.8121304633340595824, -1.842289638184602341 ) ) ;
#153451=CARTESIAN_POINT ( 'NONE',  ( 0.8259615556985228091, 0.8540520341687988237, -1.937501654548081875 ) ) ;
#153453=CARTESIAN_POINT ( 'NONE',  ( 2.559107912120599071, 1.664280205102614429, -1.231313097332722872 ) ) ;
#153457=CARTESIAN_POINT ( 'NONE',  ( 4.751946794759532189, 0.7997392584290877737, 1.931828438813171456 ) ) ;
#153459=CARTESIAN_POINT ( 'NONE',  ( 2.643341535394112984, -1.351257319430071657, -1.227710988083303478 ) ) ;
#153460=CARTESIAN_POINT ( 'NONE',  ( 1.594102673003819248, -0.9688845198280521265, 1.530366366333405281 ) ) ;
#153462=CARTESIAN_POINT ( 'NONE',  ( 6.199877634063251541, -0.7475181258948644381, 2.076568058718592624 ) ) ;
#153464=CARTESIAN_POINT ( 'NONE',  ( 4.559734661428293201, 0.4870809927834463537, -2.152189095746533720 ) ) ;
#153467=CARTESIAN_POINT ( 'NONE',  ( 3.229067839489424330, 1.729836904712976686, 0.8154208365811002057 ) ) ;
#153470=CARTESIAN_POINT ( 'NONE',  ( 6.057099581687969803, 1.694805161836069107, -1.188877858866774107 ) ) ;
#153472=CARTESIAN_POINT ( 'NONE',  ( 5.899973326018037589, -0.7874313895239596350, -2.045375389432432467 ) ) ;
#153478=CARTESIAN_POINT ( 'NONE',  ( 4.024554299415397551, 1.775361691451295520, 0.5892213400080712482 ) ) ;
#153479=CARTESIAN_POINT ( 'NONE',  ( -0.02319159430949970652, 0.003959926571647092407, -1.810968101872318714 ) ) ;
#153485=CARTESIAN_POINT ( 'NONE',  ( 0.4265231311835169792, -1.290831556599820074, 1.487489745873808555 ) ) ;
#153486=CARTESIAN_POINT ( 'NONE',  ( 1.300407892936685572, 1.352140309104767013, -1.496066053310755262 ) ) ;
#153491=CARTESIAN_POINT ( 'NONE',  ( 1.746283639092637729, 0.6896231194409886411, 2.080178558289603963 ) ) ;
#153492=CARTESIAN_POINT ( 'NONE',  ( 5.777927443424748510, 1.091106472389313131, 1.463626628978510702 ) ) ;
#153500=CARTESIAN_POINT ( 'NONE',  ( 3.561895345837225779, -1.234009368583251387, 1.366721199326895952 ) ) ;
#153501=CARTESIAN_POINT ( 'NONE',  ( 1.014315213425314166, -2.013265974724808061, 0.002173784167216683862 ) ) ;
#153502=CARTESIAN_POINT ( 'NONE',  ( 1.880608668887576052, -0.2816854878555269392, 2.281025131504022863 ) ) ;
#153504=CARTESIAN_POINT ( 'NONE',  ( 6.455910365318025868, -0.6640748382394038307, 1.846044136633723243 ) ) ;
#153507=CARTESIAN_POINT ( 'NONE',  ( 4.095896644567202038, 1.253117935160457552, 1.444681106026260320 ) ) ;
#153512=CARTESIAN_POINT ( 'NONE',  ( 2.366838851271795718, 0.09958507307840713807, -2.088488507012337347 ) ) ;
#153513=CARTESIAN_POINT ( 'NONE',  ( 1.498681428038322050, 1.531199225506232553, -1.074333469806128427 ) ) ;
#153514=CARTESIAN_POINT ( 'NONE',  ( 2.407577179044288584, 0.4389615990625857500, 1.967586618684707522 ) ) ;
#153517=CARTESIAN_POINT ( 'NONE',  ( 2.788295088316892656, 1.491546084125561888, -0.8966509355741271170 ) ) ;
#153521=CARTESIAN_POINT ( 'NONE',  ( 3.457353000975535551, 0.4177302890290990889, -1.673392258113172382 ) ) ;
#153522=CARTESIAN_POINT ( 'NONE',  ( 3.474349307649237328, -2.112600797985896950, -0.5827812199917583591 ) ) ;
#153525=CARTESIAN_POINT ( 'NONE',  ( 3.836941170392699885, -2.090934008593826832, -0.5840943183372940828 ) ) ;
#153526=CARTESIAN_POINT ( 'NONE',  ( 1.945663734523142230, 0.6997465788082489757, -1.686465609443507763 ) ) ;
#153528=CARTESIAN_POINT ( 'NONE',  ( 5.032460059670339270, 0.6174496738353585368, 2.025276144886530627 ) ) ;
#153530=CARTESIAN_POINT ( 'NONE',  ( 5.021132725759672510, -2.177342503763429082, 0.7171727232720275236 ) ) ;
#153532=CARTESIAN_POINT ( 'NONE',  ( 6.720655732516684466, 7.052972427687314472, 2.524416814197846914 ) ) ;
#153534=CARTESIAN_POINT ( 'NONE',  ( 0.7508259783030580836, 2.089789393294994468, 0.3585813216958123606 ) ) ;
#153538=( BOUNDED_SURFACE ( )  B_SPLINE_SURFACE ( 3, 3, ( 
 ( #175650, #10979, #27237, #158332, #59746, #78124, #146361, #93344, #80262, #61883, #128048 ),
 ( #62941, #112834, #9926, #45652, #208118, #129109, #178850, #162593, #76000, #142105, #191863 ),
 ( #53893, #153532, #212374, #69043, #170839, #168702, #135160, #20306, #36558, #148474, #197201 ),
 ( #65057, #131213, #163660, #118955, #98653, #121115, #82383, #81329, #103717, #88540, #48840 ),
 ( #114954, #187080, #213434, #201179, #52817, #147408, #102646, #86391, #2975, #22430, #184934 ),
 ( #152459, #15242, #5101, #196155, #54963, #120028, #4039, #113909, #70108, #136221, #202241 ),
 ( #180954, #186004, #71177, #37639, #32577, #64015, #38713, #169768, #21358, #87464, #16298 ) ),
 .UNSPECIFIED., .T., .F., .T. ) 
 B_SPLINE_SURFACE_WITH_KNOTS ( ( 4, 3, 4 ),
 ( 4, 1, 1, 1, 1, 1, 1, 1, 4 ),
 ( 0.000000000000000000, 0.5000000000000000000, 1.000000000000000000 ),
 ( 0.000000000000000000, 0.2254494161556361009, 0.3971188491599597081, 0.5240836380151728813, 0.6154273167216615104, 0.6803253696226415626, 0.7282602231486813293, 0.7688932809586735972, 1.000000000000000000 ),
 .UNSPECIFIED. ) 
 GEOMETRIC_REPRESENTATION_ITEM ( )  RATIONAL_B_SPLINE_SURFACE ( (
 ( 1.000000000000000222, 1.000000000000000222, 0.9999999999999995559, 1.000000000000000666, 0.9999999999999997780, 0.9999999999999997780, 1.000000000000000000, 1.000000000000000000, 1.000000000000000000, 1.000000000000000000, 1.000000000000000000),
 ( 0.3333333333333334259, 0.3333333333333334259, 0.3333333333333332593, 0.3333333333333335369, 0.3333333333333333148, 0.3333333333333333148, 0.3333333333333334259, 0.3333333333333333703, 0.3333333333333333148, 0.3333333333333333703, 0.3333333333333333703),
 ( 0.3333333333333334259, 0.3333333333333334259, 0.3333333333333332593, 0.3333333333333335369, 0.3333333333333333148, 0.3333333333333333148, 0.3333333333333334259, 0.3333333333333333703, 0.3333333333333333148, 0.3333333333333333703, 0.3333333333333333703),
 ( 1.000000000000000222, 1.000000000000000222, 0.9999999999999995559, 1.000000000000000666, 0.9999999999999997780, 0.9999999999999997780, 1.000000000000000000, 1.000000000000000000, 1.000000000000000000, 1.000000000000000000, 1.000000000000000000),
 ( 0.3333333333333334259, 0.3333333333333334259, 0.3333333333333332593, 0.3333333333333335369, 0.3333333333333333148, 0.3333333333333333148, 0.3333333333333334259, 0.3333333333333333703, 0.3333333333333333148, 0.3333333333333333703, 0.3333333333333333703),
 ( 0.3333333333333334259, 0.3333333333333334259, 0.3333333333333332593, 0.3333333333333335369, 0.3333333333333333148, 0.3333333333333333148, 0.3333333333333334259, 0.3333333333333333703, 0.3333333333333333148, 0.3333333333333333703, 0.3333333333333333703),
 ( 1.000000000000000222, 1.000000000000000222, 0.9999999999999995559, 1.000000000000000666, 0.9999999999999997780, 0.9999999999999997780, 1.000000000000000000, 1.000000000000000000, 1.000000000000000000, 1.000000000000000000, 1.000000000000000000) ) ) 
 REPRESENTATION_ITEM ( '' )  SURFACE ( )  );
#153539=CARTESIAN_POINT ( 'NONE',  ( 6.883263157960365142, -0.001323150302089473379, 1.953658984494692330 ) ) ;
#153541=CARTESIAN_POINT ( 'NONE',  ( 5.133435478496918947, 0.5880181904946503169, 1.928752423557971829 ) ) ;
#153543=CARTESIAN_POINT ( 'NONE',  ( 3.151292761600641867, 1.771340389172958441, -1.056411398746412544 ) ) ;
#153545=CARTESIAN_POINT ( 'NONE',  ( -0.2411972340276023752, 5.722880186377757639, -2.494559970919587588 ) ) ;
#153549=CARTESIAN_POINT ( 'NONE',  ( 0.09384556119819162379, -2.090229486699231032, -0.04899896570133810414 ) ) ;
#153550=CARTESIAN_POINT ( 'NONE',  ( 4.307267641921147749, 1.238321930042911578, -1.591317616567271775 ) ) ;
#153551=CARTESIAN_POINT ( 'NONE',  ( 2.946635061770470632, -1.506786691049965432, -1.057933238436038925 ) ) ;
#153554=CARTESIAN_POINT ( 'NONE',  ( 1.254464346661397833, -1.363098773983735024, 1.056675342818178542 ) ) ;
#153556=CARTESIAN_POINT ( 'NONE',  ( 1.073308018423566823, -1.027821916426611581, 2.056166664744577321 ) ) ;
#153558=CARTESIAN_POINT ( 'NONE',  ( 0.4743659920835150978, 1.303974419552447639, 1.848657746038349092 ) ) ;
#153559=CARTESIAN_POINT ( 'NONE',  ( 2.965558217497352267, 0.3084109246280877237, -2.083234000326895430 ) ) ;
#153563=SURFACE_STYLE_FILL_AREA ( #135195 ) ;
#153569=CARTESIAN_POINT ( 'NONE',  ( 3.445754134864047025, -2.051236611594880799, 0.8531546545873994747 ) ) ;
#153570=CARTESIAN_POINT ( 'NONE',  ( 2.449409141518565036, 0.5832169002529237201, -2.112351429719904861 ) ) ;
#153573=CARTESIAN_POINT ( 'NONE',  ( 6.021922112293466967, 1.933069186966931863, -0.3339256516061983038 ) ) ;
#153578=CARTESIAN_POINT ( 'NONE',  ( 4.711248855110969913, 1.761570823303935551, -1.180294879073326308 ) ) ;
#153582=CARTESIAN_POINT ( 'NONE',  ( 5.541917325712655717, 0.8799508658935292216, -1.974686638939105343 ) ) ;
#153584=CARTESIAN_POINT ( 'NONE',  ( 5.108874002337426390, -0.2646564886703614006, 1.822002613180016883 ) ) ;
#153587=CARTESIAN_POINT ( 'NONE',  ( 0.4502399561126956273, -1.468881883692290113, -0.9332017962183251081 ) ) ;
#153591=CARTESIAN_POINT ( 'NONE',  ( 4.698204674003193304, -2.161138953124014161, -0.05634304724232848394 ) ) ;
#153595=B_SPLINE_CURVE_WITH_KNOTS ( 'NONE', 3,
 ( #153479, #54911, #119976, #202187, #136169, #185956, #74366, #53845, #171857, #189172 ),
 .UNSPECIFIED., .F., .F.,
 ( 4, 1, 1, 1, 1, 1, 1, 4 ),
 ( 0.000000000000000000, 0.09884949474608377418, 0.1930937302289311708, 0.2616037862002966730, 0.3630310524065313849, 0.5216543902990324888, 0.7338513509102306820, 0.9999999999999998890 ),
 .UNSPECIFIED. ) ;
#153596=CARTESIAN_POINT ( 'NONE',  ( 3.397504326804317909, 1.702965868850464082, 1.331369057855802174 ) ) ;
#153597=CARTESIAN_POINT ( 'NONE',  ( 5.325445421541009416, -1.872857986210634484, 0.6156230612282005410 ) ) ;
#153598=CARTESIAN_POINT ( 'NONE',  ( 3.971823236585111161, 1.486633142371917238, 0.8919779901093974894 ) ) ;
#153599=CARTESIAN_POINT ( 'NONE',  ( 1.206853476500208133, 1.935082376036290075, 1.028754739392373496 ) ) ;
#153600=CARTESIAN_POINT ( 'NONE',  ( 1.870602726103831381, 1.187374005633199836, 1.978520242944050711 ) ) ;
#153601=CARTESIAN_POINT ( 'NONE',  ( 3.374343653733542059, -1.230474546199412877, 1.652924668896506688 ) ) ;
#153602=CARTESIAN_POINT ( 'NONE',  ( 5.935097076209718381, -1.409686562828060152, -1.336055723097711256 ) ) ;
#153609=CARTESIAN_POINT ( 'NONE',  ( 3.628125149645112568, -1.312672481567092708, -1.773765351669121415 ) ) ;
#153611=ORIENTED_EDGE ( 'NONE', *, *, #122354, .T. ) ;
#153612=CARTESIAN_POINT ( 'NONE',  ( 0.8130640335680532349, -1.568041438259277554, -1.001899246494031948 ) ) ;
#153613=CARTESIAN_POINT ( 'NONE',  ( -0.02919842301645457147, 6.946858002156226064, -2.668856405631584217 ) ) ;
#153616=CARTESIAN_POINT ( 'NONE',  ( 6.925078400183597438, 7.629137130509070275, 2.744348168701661095 ) ) ;
#153617=CARTESIAN_POINT ( 'NONE',  ( 6.632757984263843554, -1.642112545546599023, 0.8327811610863435909 ) ) ;
#153619=CARTESIAN_POINT ( 'NONE',  ( 3.696211625926352440, -2.058462806815289259, -0.1027275840673105151 ) ) ;
#153625=CARTESIAN_POINT ( 'NONE',  ( 1.516555680085801994, 1.384881227076775190, -1.526387457142893256 ) ) ;
#153631=CARTESIAN_POINT ( 'NONE',  ( 5.461621781982892720, 0.4335984126433762853, -2.163701019753036192 ) ) ;
#153632=CARTESIAN_POINT ( 'NONE',  ( 0.3511320849261707622, -1.736299752564632204, 1.287366282644891724 ) ) ;
#153634=CARTESIAN_POINT ( 'NONE',  ( 0.2687680251878405424, -0.2516378192510167477, -2.000730910237565663 ) ) ;
#153636=CARTESIAN_POINT ( 'NONE',  ( 6.569012486276131213, -1.474873517498687336, 1.216900358440069052 ) ) ;
#153641=CARTESIAN_POINT ( 'NONE',  ( 1.481098450213329976, 1.729700800547562478, -0.7128637423776186255 ) ) ;
#153642=CARTESIAN_POINT ( 'NONE',  ( 3.169157936054858293, 1.820986098869777470, -0.8666075021629695563 ) ) ;
#153646=CARTESIAN_POINT ( 'NONE',  ( 4.951841757635310870, 0.6616352077237923623, -1.999514825752574332 ) ) ;
#153652=CARTESIAN_POINT ( 'NONE',  ( 4.078382194585396192, 0.9556978891391977315, 1.779404116599448082 ) ) ;
#153655=CARTESIAN_POINT ( 'NONE',  ( 0.5146022356567416800, 0.7859572577839054608, 1.907140732884365697 ) ) ;
#153657=CARTESIAN_POINT ( 'NONE',  ( 5.272814564875167420, -2.033366364591123521, -0.7337546567489708904 ) ) ;
#153663=CARTESIAN_POINT ( 'NONE',  ( 3.086559893568251223, 1.208301842568102247, -1.803703480758335642 ) ) ;
#153666=CARTESIAN_POINT ( 'NONE',  ( 2.313779677144182312, 1.201330555204615180, -1.395457044143719072 ) ) ;
#153668=CARTESIAN_POINT ( 'NONE',  ( 3.245827600587628758, 2.191739723504753101, -0.002129563554123526260 ) ) ;
#153670=CARTESIAN_POINT ( 'NONE',  ( 5.383742603502962965, 1.515107113446222398, 1.680479692888930288 ) ) ;
#153676=CARTESIAN_POINT ( 'NONE',  ( 5.940640833738206616, 0.3468769465994473444, 1.735210755170372376 ) ) ;
#153678=CARTESIAN_POINT ( 'NONE',  ( 1.378104160372157994, 1.254256560567709622, 1.691567388252762649 ) ) ;
#153681=CARTESIAN_POINT ( 'NONE',  ( 2.189847533163618465, -1.284324338361255258, -1.493307823759764341 ) ) ;
#153683=CARTESIAN_POINT ( 'NONE',  ( 0.2562055958934654210, -1.961350414083770977, -0.05204156388862594962 ) ) ;
#153684=CARTESIAN_POINT ( 'NONE',  ( 5.660388270892238616, 1.809938998256973575, 0.08008182766248285456 ) ) ;
#153688=CARTESIAN_POINT ( 'NONE',  ( 5.313307075269409374, -0.2735208697075517947, 1.850433306854900817 ) ) ;
#153690=CARTESIAN_POINT ( 'NONE',  ( 5.190316231837919680, 1.068962568377257671, -1.772817291931286787 ) ) ;
#153701=CARTESIAN_POINT ( 'NONE',  ( 4.756279191188107269, -1.961398630904508833, -0.05015466537350299348 ) ) ;
#153703=CARTESIAN_POINT ( 'NONE',  ( 2.266953675890924558, -2.015725231744563750, 0.04666741021024793656 ) ) ;
#153704=CARTESIAN_POINT ( 'NONE',  ( 2.536237933002471134, 0.6498936893539140058, 1.802224345963408192 ) ) ;
#153705=CARTESIAN_POINT ( 'NONE',  ( -0.1108833634137010027, 2.037774818562386514, -2.313487243312782216 ) ) ;
#153706=CARTESIAN_POINT ( 'NONE',  ( 0.4686481397476391364, -2.065551408369214137, -0.7328327568804984260 ) ) ;
#153708=CARTESIAN_POINT ( 'NONE',  ( 2.477632765499269141, 1.147360842229189437, 1.477270975257204411 ) ) ;
#153710=CARTESIAN_POINT ( 'NONE',  ( 4.166274970888473206, 2.012660793657996106, -0.05373556394885727755 ) ) ;
#153713=CARTESIAN_POINT ( 'NONE',  ( 4.271193901148872207, 1.890388351848461657, -0.9536453560208182356 ) ) ;
#153715=CARTESIAN_POINT ( 'NONE',  ( 5.951642636407409093, 1.565221049572671719, 1.355249363302114318 ) ) ;
#153716=CARTESIAN_POINT ( 'NONE',  ( 1.294599682487684422, 1.707161730183017534, -1.206694161613943272 ) ) ;
#153718=CARTESIAN_POINT ( 'NONE',  ( 5.930640623865813588, 1.760069778787749506, 0.4843501209313359479 ) ) ;
#153725=CARTESIAN_POINT ( 'NONE',  ( 0.06471810551328219252, -1.456173922333989790, 1.077237379209189827 ) ) ;
#153733=CARTESIAN_POINT ( 'NONE',  ( 5.642203898613793456, 0.8197873783117490820, 1.842442240159094080 ) ) ;
#153734=CARTESIAN_POINT ( 'NONE',  ( -0.004992717928550480244, -2.057963470346049650, -0.5107951590591561786 ) ) ;
#153736=CLOSED_SHELL ( 'NONE', ( #141403, #106232, #64576, #53084, #199942, #83275, #52579, #17967 ) ) ;
#153737=CARTESIAN_POINT ( 'NONE',  ( -0.1399997263889836974, 2.022132088033218533, -2.415689637818136948 ) ) ;
#153740=CARTESIAN_POINT ( 'NONE',  ( 3.959776185634265921, -0.5760637367184845425, 1.883274482577349973 ) ) ;
#153741=CARTESIAN_POINT ( 'NONE',  ( 4.446888776373093322, -1.802426293348384334, -0.9040943451460029534 ) ) ;
#153744=CARTESIAN_POINT ( 'NONE',  ( 4.505938053128990539, -0.9357023767473917619, -1.981784127816770935 ) ) ;
#153746=CARTESIAN_POINT ( 'NONE',  ( 3.663036927850862323, -1.698304795282145063, -0.9092769472496107230 ) ) ;
#153748=CARTESIAN_POINT ( 'NONE',  ( -0.1296875068447916890, 6.948706544289747988, -2.421546651465163347 ) ) ;
#153749=CARTESIAN_POINT ( 'NONE',  ( 0.2236267563471248943, -0.1037379595543522215, 2.204571545119632603 ) ) ;
#153753=CARTESIAN_POINT ( 'NONE',  ( 4.557443512217212778, 1.579177641033597368, 1.176567834677658908 ) ) ;
#153754=CARTESIAN_POINT ( 'NONE',  ( 0.04629046987890492182, -1.559278246393133838, 1.157480633202745635 ) ) ;
#153755=CARTESIAN_POINT ( 'NONE',  ( 3.703774327200870076, 1.459685083667804362, 1.386552827976398339 ) ) ;
#153756=CARTESIAN_POINT ( 'NONE',  ( 5.290469632519504195, -2.184888740097378879, 0.7135917202819259675 ) ) ;
#153758=CARTESIAN_POINT ( 'NONE',  ( 2.694024576921652425, 0.8818583146339260548, -1.638763372900291726 ) ) ;
#153765=CARTESIAN_POINT ( 'NONE',  ( 5.794497793856321799, 1.708647746284063684, -1.204582154990775811 ) ) ;
#153770=CARTESIAN_POINT ( 'NONE',  ( 0.6623940301842005107, -1.324425631624454036, 1.256838194884236204 ) ) ;
#153772=CARTESIAN_POINT ( 'NONE',  ( 2.883173651945786009, -0.5064310303744267161, -1.658517218374066848 ) ) ;
#153773=CARTESIAN_POINT ( 'NONE',  ( 6.509000000000033204, 1.287336644856639456, 2.017667062298739822 ) ) ;
#153776=CARTESIAN_POINT ( 'NONE',  ( 6.912935025559954205, -1.683935878860399971, 1.369999676949062550 ) ) ;
#153777=CARTESIAN_POINT ( 'NONE',  ( 5.338443970399977978, 1.799313579390570128, 0.3082849261525285600 ) ) ;
#153778=CARTESIAN_POINT ( 'NONE',  ( 3.239059677355364375, -0.1396402669299641186, -1.956817938210092089 ) ) ;
#153782=CARTESIAN_POINT ( 'NONE',  ( 3.809332071562030908, 1.790574611000576244, -1.135637872363919110 ) ) ;
#153783=CARTESIAN_POINT ( 'NONE',  ( 6.827182134110219458, 3.682144966263277919, 2.702925436647873880 ) ) ;
#153784=AXIS2_PLACEMENT_3D ( 'NONE', #87962, #138865, #120542 ) ;
#153786=CARTESIAN_POINT ( 'NONE',  ( 2.184514099445804547, 1.195434181571125132, -1.690031224328606196 ) ) ;
#153790=CARTESIAN_POINT ( 'NONE',  ( 4.653117599668723514, 0.3792583102804178985, 2.188544891856615049 ) ) ;
#153792=CARTESIAN_POINT ( 'NONE',  ( 1.776460590643181625, 1.997282851074515975, -1.137850514363091481 ) ) ;
#153797=CARTESIAN_POINT ( 'NONE',  ( 6.620655732516645742, 0.007553340620044741646, 1.826407896915737794 ) ) ;
#153799=CARTESIAN_POINT ( 'NONE',  ( 2.619282413590624525, 1.617716081779559278, 1.019604094833974628 ) ) ;
#153801=CARTESIAN_POINT ( 'NONE',  ( 3.733171248123872132, -1.593707704047672591, 0.6599822260907485250 ) ) ;
#153802=CARTESIAN_POINT ( 'NONE',  ( 2.307827663788959871, -1.164988201124015577, -1.645758576239789051 ) ) ;
#153804=CARTESIAN_POINT ( 'NONE',  ( 3.428665021107531352, -1.741954984014550512, -1.499980572608774043 ) ) ;
#153806=CARTESIAN_POINT ( 'NONE',  ( 3.304270634109522486, -2.259957100417890441, 0.1074057698594049759 ) ) ;
#153807=CARTESIAN_POINT ( 'NONE',  ( 6.551405291548149101, -1.690254494844857014, -1.256206543278805876 ) ) ;
#153810=CARTESIAN_POINT ( 'NONE',  ( 4.270580540438973394, -1.650736559713336771, -0.6384287733962620282 ) ) ;
#153812=CARTESIAN_POINT ( 'NONE',  ( 1.219134843238580235, -0.05193690637114551506, 2.291835786607650416 ) ) ;
#153814=CARTESIAN_POINT ( 'NONE',  ( 6.158133876658566486, -1.298579738958350660, 1.305440813956220136 ) ) ;
#153816=CARTESIAN_POINT ( 'NONE',  ( 5.876942531769461020, 2.026063101133714461, -0.8356547683932223913 ) ) ;
#153820=CARTESIAN_POINT ( 'NONE',  ( 6.197728532230423859, -1.496850047335227085, -1.430563974149069661 ) ) ;
#153821=CARTESIAN_POINT ( 'NONE',  ( 0.7433754753295095385, 0.3886281223182270761, -1.978556061772406505 ) ) ;
#153823=CARTESIAN_POINT ( 'NONE',  ( 4.828697303143684394, 1.844096510799615674, 0.5574245839122073942 ) ) ;
#153826=CARTESIAN_POINT ( 'NONE',  ( 1.231071286002645815, 1.486838745870424860, -1.650645422243676164 ) ) ;
#153835=CARTESIAN_POINT ( 'NONE',  ( 4.546296192243603151, -1.394137154979861570, 1.041651924218311986 ) ) ;
#153836=CARTESIAN_POINT ( 'NONE',  ( 2.488659587246493832, 1.902222718079676689, 0.4795239450603656084 ) ) ;
#153841=CARTESIAN_POINT ( 'NONE',  ( 0.1860857499333635756, -1.268064657576525978, -1.627672589050175089 ) ) ;
#153845=CARTESIAN_POINT ( 'NONE',  ( 0.8840797711214362087, 1.521441056815290516, 1.674750314396955542 ) ) ;
#153849=CARTESIAN_POINT ( 'NONE',  ( 1.352582913587907942, -1.478046865151939615, 1.146363905606573086 ) ) ;
#153850=CARTESIAN_POINT ( 'NONE',  ( 0.1934855802202296304, 1.507424494634423517, 0.8570536861387479943 ) ) ;
#153852=CARTESIAN_POINT ( 'NONE',  ( 3.808297599986898430, 1.548825491099754315, -1.550762550882843094 ) ) ;
#153853=CARTESIAN_POINT ( 'NONE',  ( 5.649573025266686699, -1.814708426832438048, -1.425321367006604056 ) ) ;
#153854=CARTESIAN_POINT ( 'NONE',  ( 6.907514182033759553, -0.4531076517439984186, 2.017496682098403937 ) ) ;
#153855=CARTESIAN_POINT ( 'NONE',  ( 2.923698373526161465, 1.078347508963822587, -1.614843327186490374 ) ) ;
#153861=CARTESIAN_POINT ( 'NONE',  ( 2.988907892087853568, -2.013985899409028946, 0.1017507309580278629 ) ) ;
#153865=CARTESIAN_POINT ( 'NONE',  ( 0.7502976729042536430, 0.5272139720400963459, 1.747899773703022408 ) ) ;
#153871=CARTESIAN_POINT ( 'NONE',  ( 0.3741789627117291239, 1.245922373857488274, 1.766349570875298758 ) ) ;
#153876=CARTESIAN_POINT ( 'NONE',  ( 6.147130067458792091, 0.1999419896685956377, 2.009763438563259008 ) ) ;
#153877=CARTESIAN_POINT ( 'NONE',  ( 5.637407045567618624, -0.05664847855723317838, 2.220727194027871665 ) ) ;
#153881=CARTESIAN_POINT ( 'NONE',  ( 5.295800851330623615, -0.7439313745516599186, 1.922114966912706224 ) ) ;
#153882=CARTESIAN_POINT ( 'NONE',  ( 3.533827422916273164, -1.646839391163470223, 1.163268690995450383 ) ) ;
#153889=CARTESIAN_POINT ( 'NONE',  ( 4.095077249698628741, 1.080899603560569799, -1.701687522498253946 ) ) ;
#153890=CARTESIAN_POINT ( 'NONE',  ( 3.116968920156853340, -1.774181764490849522, 0.4917334186493869108 ) ) ;
#153892=CARTESIAN_POINT ( 'NONE',  ( 2.210004991130873453, -0.5033687547432836862, 2.251983625769232500 ) ) ;
#153894=CARTESIAN_POINT ( 'NONE',  ( 3.919328646192806520, -0.1633067429045453600, 2.155504054270485970 ) ) ;
#153897=CARTESIAN_POINT ( 'NONE',  ( 3.761312542938214598, -2.295521343867617414, -0.1171695491895396041 ) ) ;
#153900=CARTESIAN_POINT ( 'NONE',  ( 2.342468781959532453, 0.4075140148256419792, 1.825566309089213579 ) ) ;
#153902=CARTESIAN_POINT ( 'NONE',  ( 6.578986288830292573, -0.09655258645749519031, -1.969210242046049331 ) ) ;
#153905=CARTESIAN_POINT ( 'NONE',  ( 1.893488989520499377, 1.919108310403025985, -1.089527612406354873 ) ) ;
#153911=CARTESIAN_POINT ( 'NONE',  ( 6.368046306259418365, 1.013251383440600284, 1.691012432383535602 ) ) ;
#153912=CARTESIAN_POINT ( 'NONE',  ( 5.444061505814771884, 0.9398705156117830306, -2.107803560374045038 ) ) ;
#153913=CARTESIAN_POINT ( 'NONE',  ( 0.7835587076311965049, -1.864072139945194717, 0.6119401183290391621 ) ) ;
#153914=CARTESIAN_POINT ( 'NONE',  ( 4.311423628786446471, -1.712024382654028454, -1.150014069924868654 ) ) ;
#153921=CARTESIAN_POINT ( 'NONE',  ( 6.197752310581432056, -1.568275824509495875, -1.501738253884659979 ) ) ;
#153924=CARTESIAN_POINT ( 'NONE',  ( 4.757273854911123756, 1.820453720981948242, -0.2752165127944474210 ) ) ;
#153928=CARTESIAN_POINT ( 'NONE',  ( 0.1923495491853322581, -0.4021996241703913455, -1.833441224692602844 ) ) ;
#153932=CARTESIAN_POINT ( 'NONE',  ( 0.5570965697654255422, -1.639946202723217450, 0.9833419947904219471 ) ) ;
#153933=CARTESIAN_POINT ( 'NONE',  ( 1.955557038561178240, 1.765385265556310701, -0.1263916157485909797 ) ) ;
#153934=CARTESIAN_POINT ( 'NONE',  ( 6.604166866988625095, -0.8575501651001187220, 1.819208590218702071 ) ) ;
#153936=CARTESIAN_POINT ( 'NONE',  ( 4.552287420941045326, -1.248256511182913364, 1.453175340101879875 ) ) ;
#153938=CARTESIAN_POINT ( 'NONE',  ( 5.635196759804959044, -0.04649108105550652653, -1.969165932527061402 ) ) ;
#153939=CARTESIAN_POINT ( 'NONE',  ( -0.1225938595818750754, -1.897163925677572305, -0.9476133185889324961 ) ) ;
#153941=CARTESIAN_POINT ( 'NONE',  ( 2.729206520949432946, -1.746158693253213379, 0.6715030345267187784 ) ) ;
#153942=CARTESIAN_POINT ( 'NONE',  ( -0.01727558406095473439, -0.1313277740116538805, -1.795991579427682616 ) ) ;
#153944=CARTESIAN_POINT ( 'NONE',  ( 3.457846583235091753, 0.5364296187198510646, -2.140574738106671759 ) ) ;
#153947=CARTESIAN_POINT ( 'NONE',  ( 1.135301032730736237, -0.04873925880971052838, -2.062252310772247910 ) ) ;
#153955=CARTESIAN_POINT ( 'NONE',  ( 2.928250347896840022, 1.105370970781336837, 1.750397071514836478 ) ) ;
#153960=CARTESIAN_POINT ( 'NONE',  ( 0.5397205009909338269, -1.917025550485540908, 0.6358503350361620621 ) ) ;
#153963=CARTESIAN_POINT ( 'NONE',  ( 0.1747926744264712562, 2.889263262932476817, -2.344248796821886138 ) ) ;
#153965=CARTESIAN_POINT ( 'NONE',  ( 6.063827332385394620, 1.649827434358666967, -1.158513616066357832 ) ) ;
#153966=CARTESIAN_POINT ( 'NONE',  ( 5.753135696777640362, 0.1336808224800915823, -1.911095040969860825 ) ) ;
#153967=CARTESIAN_POINT ( 'NONE',  ( 6.539320575229290000, 0.004092658091040673150, 2.003502637948690879 ) ) ;
#153968=CARTESIAN_POINT ( 'NONE',  ( 3.439196427729715566, -1.660734982795486481, -1.430121640581413889 ) ) ;
#153970=CARTESIAN_POINT ( 'NONE',  ( 2.918110517850933672, -1.910018876965378309, 0.09814724848770939314 ) ) ;
#153974=CARTESIAN_POINT ( 'NONE',  ( 0.6500178175347063325, 0.9963223104369984817, 1.753020061881370051 ) ) ;
#153976=CARTESIAN_POINT ( 'NONE',  ( 6.550331612656306035, -1.695486744446069727, 1.388264742925699569 ) ) ;
#153978=CARTESIAN_POINT ( 'NONE',  ( 3.399128784836574990, 1.359029604673635871, 1.061868196530877384 ) ) ;
#153983=CARTESIAN_POINT ( 'NONE',  ( 0.1507198084474276056, -0.4258245693303016610, -1.922078969575198526 ) ) ;
#153989=CARTESIAN_POINT ( 'NONE',  ( 3.914574264990647201, -0.5719694332564858597, -1.718857104472475861 ) ) ;
#153994=CARTESIAN_POINT ( 'NONE',  ( 4.863805359840983833, 0.5633507197577434233, -1.721726771216978369 ) ) ;
#153999=CARTESIAN_POINT ( 'NONE',  ( 5.037489322368606359, 1.736649509538616964, -0.6695082933049227858 ) ) ;
#154001=CARTESIAN_POINT ( 'NONE',  ( 2.565921762024740982, -0.9824477935329900546, 1.644319621262643638 ) ) ;
#154006=CARTESIAN_POINT ( 'NONE',  ( 6.925078400183556582, 1.239878965558613100, 2.257517960274834756 ) ) ;
#154011=CARTESIAN_POINT ( 'NONE',  ( 1.025464405625675646, -1.327728713622891688, -1.614889332886438655 ) ) ;
#154013=CARTESIAN_POINT ( 'NONE',  ( 6.370143239528382573, 0.9910226482379416169, 1.651782778771145432 ) ) ;
#154015=CARTESIAN_POINT ( 'NONE',  ( 2.836711209001481659, 0.2215568149019596367, 1.812007907362273018 ) ) ;
#154017=CARTESIAN_POINT ( 'NONE',  ( 1.775505761281343631, 0.3235837346332003372, -1.884644527778083001 ) ) ;
#154018=CARTESIAN_POINT ( 'NONE',  ( 1.609744333363828384, 0.5749553099084430130, -1.883740962975283706 ) ) ;
#154019=CARTESIAN_POINT ( 'NONE',  ( 3.474105628906531518, -1.872487600191057755, -0.5149888314514885490 ) ) ;
#154024=CARTESIAN_POINT ( 'NONE',  ( 4.394861267144759331, -2.057662932662501110, -0.5123870273424437904 ) ) ;
#154032=CARTESIAN_POINT ( 'NONE',  ( 3.545350327189537687, -1.383302465072188792, -1.191577590537174158 ) ) ;
#154037=CARTESIAN_POINT ( 'NONE',  ( 4.205816867194319464, -1.865656749788859647, 0.1373567816406878750 ) ) ;
#154039=CARTESIAN_POINT ( 'NONE',  ( 2.473164231231731680, 0.09456843629558449316, -1.924295592635028029 ) ) ;
#154041=CARTESIAN_POINT ( 'NONE',  ( 6.614115624646348834, 1.956711779489667125, -0.1410536379464824575 ) ) ;
#154046=CARTESIAN_POINT ( 'NONE',  ( 1.247838713208373029, 2.085211562554165621, -0.3660346322543471809 ) ) ;
#154050=CARTESIAN_POINT ( 'NONE',  ( 5.137584473783054051, 1.933663220787355419, -0.7400441640052906056 ) ) ;
#154051=CARTESIAN_POINT ( 'NONE',  ( 0.4152503475762688856, -0.9843521281015167324, -1.555853522519357934 ) ) ;
#154054=CARTESIAN_POINT ( 'NONE',  ( 5.520273603857641653, -2.079230528169520031, 0.9805040003046764374 ) ) ;
#154058=CARTESIAN_POINT ( 'NONE',  ( 1.728911070687192186, 0.2280534122649588435, 2.280891765651926750 ) ) ;
#154062=CARTESIAN_POINT ( 'NONE',  ( 5.560475942038150876, -1.756435177671934911, -0.8285927890409640062 ) ) ;
#154066=CARTESIAN_POINT ( 'NONE',  ( -0.1931356145602729502, -0.4479747710816587292, -1.970277229543435427 ) ) ;
#154067=CARTESIAN_POINT ( 'NONE',  ( 5.296111364736042937, -0.9110065213352031011, -1.799124599017036585 ) ) ;
#154071=CARTESIAN_POINT ( 'NONE',  ( 2.238330470135694750, 0.4590858415520538416, 2.039436070248427324 ) ) ;
#154072=CARTESIAN_POINT ( 'NONE',  ( 1.445802646165544880, 1.767618460842989014, 0.09138547110125286310 ) ) ;
#154074=CARTESIAN_POINT ( 'NONE',  ( 3.697495799125404492, -0.6661743112182354487, 2.193330854740268343 ) ) ;
#154075=CARTESIAN_POINT ( 'NONE',  ( 3.820004643325402238, 1.653240603489447569, 0.5438404159014453843 ) ) ;
#154078=CARTESIAN_POINT ( 'NONE',  ( 2.618122797784384836, 0.4666061159355525678, -1.669766330342295158 ) ) ;
#154079=CARTESIAN_POINT ( 'NONE',  ( 3.332658328316660423, -1.295540365661397297, 1.742140367482351238 ) ) ;
#154081=CARTESIAN_POINT ( 'NONE',  ( 4.434779938697545276, -1.616694733667634942, 1.205040202231235869 ) ) ;
#154082=CARTESIAN_POINT ( 'NONE',  ( 2.625000000000002665, -2.052068128417949833, 1.560916121760785068E-13 ) ) ;
#154084=CARTESIAN_POINT ( 'NONE',  ( 0.7449895426413064570, -1.653788825565579046, 0.9876836116205435223 ) ) ;
#154086=CARTESIAN_POINT ( 'NONE',  ( 4.482826657505923684, -1.449732756002309664, 1.683255901693592849 ) ) ;
#154088=FACE_OUTER_BOUND ( 'NONE', #210179, .T. ) ;
#154093=CARTESIAN_POINT ( 'NONE',  ( 0.6982527715983916083, 1.495984496936525021, 1.642170479989105480 ) ) ;
#154094=CARTESIAN_POINT ( 'NONE',  ( 5.740667459973674447, -1.913685094937540132, -0.4313615418530327150 ) ) ;
#154096=CARTESIAN_POINT ( 'NONE',  ( 0.4214394802095830506, -0.1064560406111268731, 2.159113264384164399 ) ) ;
#154099=CARTESIAN_POINT ( 'NONE',  ( 3.525881619439541037, 2.013048741316531220, -0.4491155694474731619 ) ) ;
#154104=CARTESIAN_POINT ( 'NONE',  ( 5.167206475355686557, 0.1846639555213614448, -1.861428779493356167 ) ) ;
#154105=CARTESIAN_POINT ( 'NONE',  ( 4.113671241589770489, 0.09026135180613574505, 1.731944212183807341 ) ) ;
#154106=CARTESIAN_POINT ( 'NONE',  ( 3.139928233896288390, 0.4259470162499751633, 1.687361108405739385 ) ) ;
#154107=CARTESIAN_POINT ( 'NONE',  ( 0.4863598079122740114, -2.275998871909711951, -0.2730087134108442615 ) ) ;
#154109=CARTESIAN_POINT ( 'NONE',  ( 4.968349523292523884, -1.969100025901071360, -0.7031758509000278767 ) ) ;
#154110=CARTESIAN_POINT ( 'NONE',  ( 0.5152501731416662123, -0.9825955030486509534, -1.556829690179861281 ) ) ;
#154112=EDGE_LOOP ( 'NONE', ( #113205, #209353 ) ) ;
#154113=CARTESIAN_POINT ( 'NONE',  ( 0.8619541869999207684, -0.05229984143813663777, -2.015912905633105101 ) ) ;
#154114=CARTESIAN_POINT ( 'NONE',  ( 1.143014088299774578, 2.045220145331683614, 0.5602274146137007360 ) ) ;
#154115=CARTESIAN_POINT ( 'NONE',  ( 6.825078400183547167, -0.008500281443135963844, 2.244262395727573356 ) ) ;
#154119=CARTESIAN_POINT ( 'NONE',  ( 2.508575005364023003, -2.114979441823850337, -0.1534387461676610942 ) ) ;
#154121=CARTESIAN_POINT ( 'NONE',  ( 4.424309136736732206, 1.121156565774838354, -1.440799707636587712 ) ) ;
#154128=CARTESIAN_POINT ( 'NONE',  ( 2.039325177177089721, 0.004250232316239943575, 2.019972748817438823 ) ) ;
#154129=CARTESIAN_POINT ( 'NONE',  ( 6.001041448284401447, 1.807427358944500684, -1.265864663738118345 ) ) ;
#154131=CARTESIAN_POINT ( 'NONE',  ( 4.205779932802704124, 0.6304169756579135475, -1.751020666094662337 ) ) ;
#154138=CARTESIAN_POINT ( 'NONE',  ( 5.145057536039753465, -1.563975785779356587, 0.9416349707431559413 ) ) ;
#154143=CARTESIAN_POINT ( 'NONE',  ( 0.4734851067992265627, 1.504414441068102404, 0.8618086654073161545 ) ) ;
#154144=CARTESIAN_POINT ( 'NONE',  ( 0.4798830478778244868, -0.2081801751476043960, -1.727770289196085329 ) ) ;
#154145=CARTESIAN_POINT ( 'NONE',  ( 5.637451635233869496, -2.088540497258955408, 0.9818693799023417990 ) ) ;
#154148=CARTESIAN_POINT ( 'NONE',  ( 0.9661734561289528900, 1.013198095218909245, 1.794397040888571437 ) ) ;
#154150=CARTESIAN_POINT ( 'NONE',  ( 0.4036724312478366938, 0.3418800534340654118, 1.986742826083332858 ) ) ;
#154153=CARTESIAN_POINT ( 'NONE',  ( 5.383624799460786647, 1.257121276536907750, 1.385457850027263182 ) ) ;
#154155=CARTESIAN_POINT ( 'NONE',  ( 3.287273477832891366, 0.04233216220104508987, -1.912079899511004433 ) ) ;
#154157=CARTESIAN_POINT ( 'NONE',  ( 5.496761087669068679, -0.5331231007881258588, -2.141394884921154151 ) ) ;
#154163=CARTESIAN_POINT ( 'NONE',  ( 6.217454246653871586, 1.762742247767977055, 1.178343227268910054 ) ) ;
#154165=CARTESIAN_POINT ( 'NONE',  ( 3.065757340968386035, 0.3400709678853690021, -2.282286004074239649 ) ) ;
#154166=CARTESIAN_POINT ( 'NONE',  ( 4.158614545834369736, -0.6132839004606009947, -1.863630207987923004 ) ) ;
#154167=CARTESIAN_POINT ( 'NONE',  ( 0.3034670832338138835, -1.512625156342655819, -1.248876549296701333 ) ) ;
#154171=CARTESIAN_POINT ( 'NONE',  ( 5.946499988598237252, -1.422611626450220434, 1.429444749906971790 ) ) ;
#154173=CARTESIAN_POINT ( 'NONE',  ( 0.1988192939417210425, -0.4940924592915455493, 1.773541111592655373 ) ) ;
#154174=CARTESIAN_POINT ( 'NONE',  ( 3.555704413576792788, 1.708454066091537493, 1.339533783212579099 ) ) ;
#154176=CARTESIAN_POINT ( 'NONE',  ( 0.2641366190093488164, 0.6592694798918593557, -2.015615888626711705 ) ) ;
#154181=CARTESIAN_POINT ( 'NONE',  ( 0.7200824656817590430, -1.100121004815158177, -1.742362558145001294 ) ) ;
#154187=CARTESIAN_POINT ( 'NONE',  ( 2.842330330863319876, 1.060513762474508015, -1.591057744338888913 ) ) ;
#154188=CARTESIAN_POINT ( 'NONE',  ( 5.805463146582474643, -0.4265672176911333713, 1.717519531449087866 ) ) ;
#154191=CARTESIAN_POINT ( 'NONE',  ( 0.1756362645438137582, 1.791864648875134636, -0.2657654445481233418 ) ) ;
#154193=CARTESIAN_POINT ( 'NONE',  ( 0.6377201071205064187, 1.913410132493647442, -0.09706281964840141052 ) ) ;
#154194=CARTESIAN_POINT ( 'NONE',  ( 2.084514231050747401, 1.193861083872927109, -1.691280048542340708 ) ) ;
#154196=CARTESIAN_POINT ( 'NONE',  ( 6.034044788248046132, 0.9204803733943857091, -1.628451883209979689 ) ) ;
#154197=CARTESIAN_POINT ( 'NONE',  ( 3.228933428962964758, 0.04559371896543929631, 1.825288036790246204 ) ) ;
#154199=CARTESIAN_POINT ( 'NONE',  ( 0.3644775225865644619, 2.281660525247240834, -0.3449698035877246105 ) ) ;
#154202=CARTESIAN_POINT ( 'NONE',  ( 4.123522620141695683, 0.2556129913668835907, -2.046733346555211330 ) ) ;
#154206=CARTESIAN_POINT ( 'NONE',  ( 0.3511320849261707622, -1.736299752564632204, 1.287366282644891724 ) ) ;
#154207=CARTESIAN_POINT ( 'NONE',  ( 6.742638474511262636, -2.029596885996234334, -0.4079607620106340260 ) ) ;
#154209=CARTESIAN_POINT ( 'NONE',  ( 4.183022562662654487, -0.2072598778708051315, -2.151613130492259440 ) ) ;
#154210=CARTESIAN_POINT ( 'NONE',  ( 4.283856624473350472, 1.958454427565621048, -0.4929297443572661641 ) ) ;
#154215=CARTESIAN_POINT ( 'NONE',  ( 2.993375309983861143, -0.3886322325962355273, 1.978555244300662874 ) ) ;
#154220=CARTESIAN_POINT ( 'NONE',  ( 6.310809538426106258, -0.5167911955388967415, -1.841158844219364044 ) ) ;
#154221=DIRECTION ( 'NONE',  ( 1.040834085586084257E-15, 1.000000000000000000, -4.622230424712076367E-32 ) ) ;
#154224=CARTESIAN_POINT ( 'NONE',  ( 4.675407748274028386, 1.496063595514389943, 1.352143027241403450 ) ) ;
#154227=CARTESIAN_POINT ( 'NONE',  ( 6.211878148792838061, -1.711051158068075839, 0.2163953478501578487 ) ) ;
#154232=CARTESIAN_POINT ( 'NONE',  ( 5.132044594934622062, 0.9627672477196843603, -1.603626212978970900 ) ) ;
#154234=CARTESIAN_POINT ( 'NONE',  ( 0.2584475630193752149, 2.007833436562710183, 0.1460894178599257687 ) ) ;
#154236=CARTESIAN_POINT ( 'NONE',  ( 1.991162705694597301, 0.1987741427678466344, 2.060657922996151914 ) ) ;
#154240=CARTESIAN_POINT ( 'NONE',  ( 0.7203276360899166786, 1.987051886588153682, 0.3419113104980234241 ) ) ;
#154241=CARTESIAN_POINT ( 'NONE',  ( 0.8436869049191192405, -1.150191864323051982, -1.399547552825676666 ) ) ;
#154249=CARTESIAN_POINT ( 'NONE',  ( 6.274997412412571585, 1.664062557780759066, -0.9488046768871650771 ) ) ;
#154258=CARTESIAN_POINT ( 'NONE',  ( 2.624079441566569582, -1.243859440641072123, -1.767801033134681843 ) ) ;
#154262=CARTESIAN_POINT ( 'NONE',  ( 1.353939357992512305, -1.539690173578952770, -1.458446627980537480 ) ) ;
#154263=CARTESIAN_POINT ( 'NONE',  ( 5.631824825758743991, -1.159798792365024145, -1.409841961918213427 ) ) ;
#154264=CARTESIAN_POINT ( 'NONE',  ( 2.372288100061814564, -1.215664946315485606, 1.551802774678180619 ) ) ;
#154265=CARTESIAN_POINT ( 'NONE',  ( 4.131050151015442928, 1.750605847248308145, 0.7702136748066327199 ) ) ;
#154268=CARTESIAN_POINT ( 'NONE',  ( 4.896905686981484429, 0.3346149513497528871, 1.940740247813901087 ) ) ;
#154269=CARTESIAN_POINT ( 'NONE',  ( 0.5505969416323712728, -1.640064848914600804, -1.039604180477508688 ) ) ;
#154275=CARTESIAN_POINT ( 'NONE',  ( 4.863870654145381778, 0.5962773724161560818, -1.817021391602848812 ) ) ;
#154277=CARTESIAN_POINT ( 'NONE',  ( 1.044295067165665669, 0.8929887407379887287, -2.018210024696056148 ) ) ;
#154279=CARTESIAN_POINT ( 'NONE',  ( 6.041657904462632622, -1.894779907254999118, 0.6802824325803021877 ) ) ;
#154280=CARTESIAN_POINT ( 'NONE',  ( -0.02338929933905046013, 4.099262448077650944, -2.266018688142543258 ) ) ;
#154283=CARTESIAN_POINT ( 'NONE',  ( 2.629418614236479712, 0.1040367438073786233, -2.067886086930009970 ) ) ;
#154287=CARTESIAN_POINT ( 'NONE',  ( 0.5148121308554790554, 1.489681748880047563, -1.566682057046255849 ) ) ;
#154291=CARTESIAN_POINT ( 'NONE',  ( 6.925078400183553029, 6.037155338232472523, 2.550556537725846340 ) ) ;
#154293=CARTESIAN_POINT ( 'NONE',  ( 4.271880269886525916, 1.546599990029189575, -0.7845881139060503218 ) ) ;
#154295=CARTESIAN_POINT ( 'NONE',  ( 2.096617048772158487, 2.047133997803842753, 0.3078910663548983795 ) ) ;
#154296=CARTESIAN_POINT ( 'NONE',  ( 5.027025340701954725, -1.815278874653761809, 1.089499710131608401 ) ) ;
#154300=CARTESIAN_POINT ( 'NONE',  ( 2.219528804134728528, 0.3415968887231227713, -1.939435228410562484 ) ) ;
#154301=CARTESIAN_POINT ( 'NONE',  ( 1.265713261412576562, 0.5522810963098608861, -1.830935845731461953 ) ) ;
#154302=CARTESIAN_POINT ( 'NONE',  ( 4.945436657225622312, 0.7223393070586077158, -2.175551854680431330 ) ) ;
#154303=CARTESIAN_POINT ( 'NONE',  ( 2.139018802738294589, -1.631172329757241801, 0.8201644002571031322 ) ) ;
#154309=CARTESIAN_POINT ( 'NONE',  ( 3.252200647028923974, 0.9015175226297014177, -1.800113812977667038 ) ) ;
#154310=CARTESIAN_POINT ( 'NONE',  ( 2.887496479553632422, -1.832211488775811414, 0.7015765724691159777 ) ) ;
#154314=CARTESIAN_POINT ( 'NONE',  ( 5.859345120547017949, 2.059885262428410968, -0.3562953063034664525 ) ) ;
#154315=CARTESIAN_POINT ( 'NONE',  ( 4.328786618740396719, 0.08755327933733339507, 1.767792532789840498 ) ) ;
#154317=CARTESIAN_POINT ( 'NONE',  ( 0.2874129202556953144, 1.626693421326959710, 1.468627725614686463 ) ) ;
#154318=CARTESIAN_POINT ( 'NONE',  ( -0.1298852118744100725, 0.003815113116375101580, -1.726395881205537330 ) ) ;
#154321=CARTESIAN_POINT ( 'NONE',  ( 5.713622356042774797, 2.214598200325838206, 0.6159738146167788031 ) ) ;
#154323=CARTESIAN_POINT ( 'NONE',  ( 6.274686883491842337, -1.720241393171379363, 0.2158021260532434760 ) ) ;
#154324=CARTESIAN_POINT ( 'NONE',  ( 2.297764732281985633, 1.706874461811638044, 1.398895601573101111 ) ) ;
#154325=CARTESIAN_POINT ( 'NONE',  ( 0.3038947965873342039, -1.677446906807459337, -1.377854473705003580 ) ) ;
#154327=CARTESIAN_POINT ( 'NONE',  ( 1.657563801924813784, 2.024516536105415820, -0.6199660602846206459 ) ) ;
#154328=CARTESIAN_POINT ( 'NONE',  ( 4.312500000000001776, 1.451031289061289531, 1.451031289060941587 ) ) ;
#154329=CARTESIAN_POINT ( 'NONE',  ( 6.727182134110200273, -0.004969159814478123736, 2.189081792362323586 ) ) ;
#154330=CARTESIAN_POINT ( 'NONE',  ( 4.401339437636656804, 1.546884307994823793, 1.147896415085915667 ) ) ;
#154332=CARTESIAN_POINT ( 'NONE',  ( 1.400361390298704656, -0.8304178796270310636, -2.136844513788013433 ) ) ;
#154336=CARTESIAN_POINT ( 'NONE',  ( 4.090652671443067767, -1.278631810133125546, 1.816222553172279319 ) ) ;
#154341=CARTESIAN_POINT ( 'NONE',  ( 1.740861508391436274, 2.010826320759526720, -0.1511413081683593562 ) ) ;
#154343=CARTESIAN_POINT ( 'NONE',  ( 6.461391904901197414, 1.712781507706350848, 1.149079448644703350 ) ) ;
#154346=CARTESIAN_POINT ( 'NONE',  ( 6.392160974223673797, -0.4739405955596608933, -1.674609590779071455 ) ) ;
#154349=CARTESIAN_POINT ( 'NONE',  ( 1.598528592787134883, 1.450519685958560512, -1.013601284844565908 ) ) ;
#154350=CARTESIAN_POINT ( 'NONE',  ( 6.604150274805285825, -0.1349072972122930258, 1.703313905121685456 ) ) ;
#154351=CARTESIAN_POINT ( 'NONE',  ( 6.269106929289325336, 1.662610211318481301, -0.5146825814001282362 ) ) ;
#154352=CARTESIAN_POINT ( 'NONE',  ( 3.966586032518903959, -2.139059804502403850, -0.8247178969851276520 ) ) ;
#154353=CARTESIAN_POINT ( 'NONE',  ( 3.327899939431624876, 1.796474422365784029, 0.4023406486387756664 ) ) ;
#154355=CARTESIAN_POINT ( 'NONE',  ( 3.909063277197013520, 1.565549990038747952, 0.9388121169797561949 ) ) ;
#154356=CARTESIAN_POINT ( 'NONE',  ( 5.379529795981254914, -0.4926393568372189335, -1.955173248319847845 ) ) ;
#154358=CARTESIAN_POINT ( 'NONE',  ( 3.098750496328426252, -0.6552482397011113457, -2.165565034296774272 ) ) ;
#154360=CARTESIAN_POINT ( 'NONE',  ( 4.911209521004105127, 1.831006069304096373, 1.040297942642433249 ) ) ;
#154362=CARTESIAN_POINT ( 'NONE',  ( 3.842288295254093100, -1.023014542950370975, 1.799900136785845817 ) ) ;
#154366=CARTESIAN_POINT ( 'NONE',  ( 5.408877457991549065, -0.5154355754800541423, -2.056752310636372982 ) ) ;
#154370=CARTESIAN_POINT ( 'NONE',  ( 2.420428029321282093, 1.258221797421785082, -1.458952285233440449 ) ) ;
#154372=CARTESIAN_POINT ( 'NONE',  ( 6.719592862238788378, 0.3399973502477529608, -1.939713583613829728 ) ) ;
#154377=CARTESIAN_POINT ( 'NONE',  ( 0.8091801829576624749, -0.5468400522714472745, -2.152931845550176249 ) ) ;
#154378=CARTESIAN_POINT ( 'NONE',  ( 2.485502531088045419, 1.925919180164997746, -0.8524081271456557252 ) ) ;
#154381=CARTESIAN_POINT ( 'NONE',  ( 0.3263015691194782741, -1.220318288589719913, 1.405194318597773329 ) ) ;
#154386=CARTESIAN_POINT ( 'NONE',  ( 1.143014088299774578, 2.045220145331683614, 0.5602274146137007360 ) ) ;
#154389=CARTESIAN_POINT ( 'NONE',  ( 3.824618516750320385, -1.319357783791510697, 1.452116237791359010 ) ) ;
#154390=CARTESIAN_POINT ( 'NONE',  ( 1.797963993548271411, -0.7283430984801853025, 2.035426966748521860 ) ) ;
#154391=CARTESIAN_POINT ( 'NONE',  ( 2.032514702046281485, -1.644074058028240692, 0.8291662819630771786 ) ) ;
#154394=CARTESIAN_POINT ( 'NONE',  ( 3.925522983587381276, 0.9287783018587884021, -1.471562914255954757 ) ) ;
#154397=CARTESIAN_POINT ( 'NONE',  ( 1.165152350680317195, -1.954565670758709128, -0.9236901323337529668 ) ) ;
#154399=CARTESIAN_POINT ( 'NONE',  ( 3.673203737196802710, -0.8145011343782401214, -1.844427810980188820 ) ) ;
#154401=CARTESIAN_POINT ( 'NONE',  ( 0.4796413896344040029, 2.016494124141111399, -0.7793912508547717888 ) ) ;
#154402=CARTESIAN_POINT ( 'NONE',  ( 2.623849442957484346, -1.133682707547468471, -1.612724008377570017 ) ) ;
#154404=CARTESIAN_POINT ( 'NONE',  ( 6.609000000000012420, 2.052634316153336691, 2.306727925381938604 ) ) ;
#154405=CARTESIAN_POINT ( 'NONE',  ( 2.173291266613562644, 1.196360937402714875, 1.529712666019187761 ) ) ;
#154409=CARTESIAN_POINT ( 'NONE',  ( -0.2106854629475426177, 0.2415373081153374957, -2.031805921504933554 ) ) ;
#154414=CARTESIAN_POINT ( 'NONE',  ( 6.422925328166578574, 2.149888460833260684, 0.8388895797235284002 ) ) ;
#154415=CARTESIAN_POINT ( 'NONE',  ( 6.725062055625550705, -1.793239977796506457, -0.7961783947641184467 ) ) ;
#154416=CARTESIAN_POINT ( 'NONE',  ( 4.293769791895286403, -1.349757117914761384, -1.423854091114319598 ) ) ;
#154419=CARTESIAN_POINT ( 'NONE',  ( 2.197888892816081796, 1.802417619043535701, 0.9041091288993635677 ) ) ;
#154421=CARTESIAN_POINT ( 'NONE',  ( 1.991562931776114542, -0.4585136385713373675, 2.066967827372573563 ) ) ;
#154425=CARTESIAN_POINT ( 'NONE',  ( 2.747807751077631977, 0.6205313035267927546, 1.733543155639664990 ) ) ;
#154430=CARTESIAN_POINT ( 'NONE',  ( 4.500305224345508393, -0.9970752094022590217, 1.871535012320741265 ) ) ;
#154431=CARTESIAN_POINT ( 'NONE',  ( -0.01213283819992416745, -0.3988646234997471618, -1.803908381610368261 ) ) ;
#154434=CARTESIAN_POINT ( 'NONE',  ( 4.024726114628586870, 1.955573890245201785, 0.6501785607586229032 ) ) ;
#154436=CARTESIAN_POINT ( 'NONE',  ( 1.012948470060770934, -1.796336717620912626, 0.4034172393945419377 ) ) ;
#154440=CIRCLE ( 'NONE', #47162, 0.04999999999999929501 ) ;
#154441=CARTESIAN_POINT ( 'NONE',  ( 1.436444770134176485, 1.085300811998829662, -1.921501399296850821 ) ) ;
#154442=CARTESIAN_POINT ( 'NONE',  ( 4.112777665030871610, 1.603588310063062794, -1.596181346845012117 ) ) ;
#154444=CARTESIAN_POINT ( 'NONE',  ( 3.041053801226344611, 0.04897401433806568977, 1.811106077260196345 ) ) ;
#154445=CARTESIAN_POINT ( 'NONE',  ( 4.206187189226945122, 1.174002167177927713, -1.513781418528682643 ) ) ;
#154447=CARTESIAN_POINT ( 'NONE',  ( 5.072747062355987602, 1.430223858385268665, -1.497173470029027120 ) ) ;
#154450=CARTESIAN_POINT ( 'NONE',  ( 3.924654207020538355, 1.871676352785199393, 0.6194476946735865130 ) ) ;
#154451=CARTESIAN_POINT ( 'NONE',  ( 1.307504913943892122, -0.4706295199745584301, 1.867897339068110618 ) ) ;
#154452=CARTESIAN_POINT ( 'NONE',  ( 4.188257260935820625, -1.850246793840780279, -0.2747695030091561463 ) ) ;
#154454=CARTESIAN_POINT ( 'NONE',  ( 3.440313875665978127, 1.038139129215289946, -2.061066213440334582 ) ) ;
#154455=CARTESIAN_POINT ( 'NONE',  ( 3.279601929513912939, -1.794223665640673593, 0.4940275889762090200 ) ) ;
#154458=CARTESIAN_POINT ( 'NONE',  ( 1.893330831959182836, 1.831869315246800189, -1.038985425167998633 ) ) ;
#154463=CARTESIAN_POINT ( 'NONE',  ( 3.252298345715322281, 0.9499829135306799843, -1.895951488860507128 ) ) ;
#154465=CARTESIAN_POINT ( 'NONE',  ( 1.213155585027906325, 1.648708085711389160, -1.166442415167892932 ) ) ;
#154471=CARTESIAN_POINT ( 'NONE',  ( 1.212450271513715094, -0.9707322288472041150, -1.931405299116681018 ) ) ;
#154472=CARTESIAN_POINT ( 'NONE',  ( 6.609999999999995879, 0.01081285896096205283, 1.720159828161060833 ) ) ;
#154474=DIRECTION ( 'NONE',  ( -1.000000000000000000, 0.000000000000000000, 0.000000000000000000 ) ) ;
#154477=CARTESIAN_POINT ( 'NONE',  ( 5.788296071918774821, -0.7303023681345042206, -1.879805717804765353 ) ) ;
#154479=CARTESIAN_POINT ( 'NONE',  ( 6.409723817861421757, -0.9859548438324974295, -1.843685114342674458 ) ) ;
#154481=CARTESIAN_POINT ( 'NONE',  ( 6.754756207809571755, -1.674487575904315406, 1.366813541845832924 ) ) ;
#154485=CARTESIAN_POINT ( 'NONE',  ( 0.7377199025260212650, 1.913388251642001103, -0.09504988074141537679 ) ) ;
#154489=CARTESIAN_POINT ( 'NONE',  ( 3.369487540355073030, 1.682505700701863338, -0.3791672619692722512 ) ) ;
#154491=CARTESIAN_POINT ( 'NONE',  ( 1.879799676208588899, -0.9517657123069392933, 1.491821474084076726 ) ) ;
#154492=CARTESIAN_POINT ( 'NONE',  ( 5.825267882404531861, -0.05969703229705652925, 2.206138628428089277 ) ) ;
#154494=CARTESIAN_POINT ( 'NONE',  ( 4.113539317574116616, 1.624649823752024824, 1.199838557982295217 ) ) ;
#154496=CARTESIAN_POINT ( 'NONE',  ( 4.072980787186268437, -1.570383936966279981, 1.425070900414181052 ) ) ;
#154497=CARTESIAN_POINT ( 'NONE',  ( 3.866814677988283044, -0.2004539179165897023, -2.006445418776988010 ) ) ;
#154498=CARTESIAN_POINT ( 'NONE',  ( 4.500164564109310206, -0.8477707339301239209, 1.600948808527142386 ) ) ;
#154502=CARTESIAN_POINT ( 'NONE',  ( 1.902992089709685031, 1.553661375375714471, 1.041555772207984676 ) ) ;
#154504=CARTESIAN_POINT ( 'NONE',  ( 5.848286676205444401, 0.8867688175292733899, -1.579494629471886791 ) ) ;
#154513=CARTESIAN_POINT ( 'NONE',  ( 4.465154236216789307, -1.701427117168831549, 1.265499569954648962 ) ) ;
#154514=CARTESIAN_POINT ( 'NONE',  ( -0.1296875068448125057, 7.629137130509072939, -2.426516348560475933 ) ) ;
#154516=CARTESIAN_POINT ( 'NONE',  ( 5.466080325957246799, 0.9693943247218398396, 1.716448534147915650 ) ) ;
#154518=CARTESIAN_POINT ( 'NONE',  ( 1.107682593029035711, 1.527310012579755183, 1.311747809748030846 ) ) ;
#154521=CARTESIAN_POINT ( 'NONE',  ( 0.4920138693931704887, -2.106576347024671225, 0.2123275358263312096 ) ) ;
#154523=CARTESIAN_POINT ( 'NONE',  ( 1.398975865466948632, 0.4019745351953528112, 2.030794141931663521 ) ) ;
#154527=CARTESIAN_POINT ( 'NONE',  ( 4.453126923439646667, 0.4583234712903122565, -2.039610397757870341 ) ) ;
#154529=CARTESIAN_POINT ( 'NONE',  ( 3.364083894888194592, 0.8197913233371353359, 1.631220078658943695 ) ) ;
#154530=CARTESIAN_POINT ( 'NONE',  ( 1.295247000857565167, 1.673883212702592660, -0.6929762496888560719 ) ) ;
#154532=CARTESIAN_POINT ( 'NONE',  ( 6.252570086353132162, 0.6882034672392455255, 2.096894461246688213 ) ) ;
#154533=CARTESIAN_POINT ( 'NONE',  ( 4.348781676370103710, 0.5853419563807431558, 2.127667884090424621 ) ) ;
#154537=CARTESIAN_POINT ( 'NONE',  ( 2.438023429326571456, -1.102505324871098757, -1.562262158393577405 ) ) ;
#154539=CARTESIAN_POINT ( 'NONE',  ( 6.760220206081136496, -2.069995208266177666, 0.04663682477341198757 ) ) ;
#154541=CARTESIAN_POINT ( 'NONE',  ( 5.460537066722415567, -1.980877156148381335, -0.9378266216248376530 ) ) ;
#154547=CARTESIAN_POINT ( 'NONE',  ( 3.725732288501612199, -1.111853074318921664, -1.504101509696729400 ) ) ;
#154554=CARTESIAN_POINT ( 'NONE',  ( 0.6023233765659050665, 1.963792105354182249, 0.1503755929508752975 ) ) ;
#154555=CARTESIAN_POINT ( 'NONE',  ( 1.687125285987755019, 1.678019391100945779, 1.117813378161469418 ) ) ;
#154560=CARTESIAN_POINT ( 'NONE',  ( 1.131117939106265569, -1.979831898266545487, 0.9398196729281658168 ) ) ;
#154561=CARTESIAN_POINT ( 'NONE',  ( 4.635264976507449397, -1.668059998867366778, 0.7425182445051290436 ) ) ;
#154570=CARTESIAN_POINT ( 'NONE',  ( 2.419273308677453826, -1.061688697878185206, -1.504126257600538974 ) ) ;
#154571=CARTESIAN_POINT ( 'NONE',  ( 0.01235793338260140865, -2.012684344489227062, -0.04732037452980299846 ) ) ;
#154572=CARTESIAN_POINT ( 'NONE',  ( 1.494008433901512278, 2.215370577347621328, 0.6118545706256629524 ) ) ;
#154574=CARTESIAN_POINT ( 'NONE',  ( 6.737165023268617325, -0.09304339776683606678, -1.959646862056351857 ) ) ;
#154577=CARTESIAN_POINT ( 'NONE',  ( 3.761887187967042134, 0.6396200178584460216, -1.802413552503052463 ) ) ;
#154581=CARTESIAN_POINT ( 'NONE',  ( 3.069954157378000925, -1.243473088950231675, 1.680628819622100423 ) ) ;
#154582=CARTESIAN_POINT ( 'NONE',  ( 1.076777757339364205, -0.04213119042271313425, -1.870346338061685154 ) ) ;
#154583=CARTESIAN_POINT ( 'NONE',  ( 1.722029606037442040, -1.727736752315935265, -1.038835718801443653 ) ) ;
#154586=CARTESIAN_POINT ( 'NONE',  ( 3.473892794100913672, -1.678317346756386108, -0.4606119698754263525 ) ) ;
#154589=CARTESIAN_POINT ( 'NONE',  ( 3.896855043588220546, 1.455827857355775246, -0.9247512240674607975 ) ) ;
#154590=CARTESIAN_POINT ( 'NONE',  ( 2.279091853667324141, 2.002311374866962979, -0.8913168663882904408 ) ) ;
#154591=CARTESIAN_POINT ( 'NONE',  ( 5.567066847960510323, -1.993696164035433371, -0.9465883713010987410 ) ) ;
#154594=CARTESIAN_POINT ( 'NONE',  ( 4.100555696908855019, 2.160072011501934064, 0.2185761814032516903 ) ) ;
#154595=CARTESIAN_POINT ( 'NONE',  ( 2.683998146737070378, -0.9385614705539682134, 1.565816405032012470 ) ) ;
#154597=CARTESIAN_POINT ( 'NONE',  ( 4.417270958439249107, -1.934380516720465959, 0.8614220525851381538 ) ) ;
#154598=CARTESIAN_POINT ( 'NONE',  ( 6.539320575229250920, 3.702490941164796379, 2.411252750440337156 ) ) ;
#154600=CARTESIAN_POINT ( 'NONE',  ( 4.564210359040954401, -1.498010274845029244, 1.735314277699088858 ) ) ;
#154602=CARTESIAN_POINT ( 'NONE',  ( 6.827182134110222123, -0.006956174471953178659, 2.188967759425272330 ) ) ;
#154604=CARTESIAN_POINT ( 'NONE',  ( 0.1356056236470788157, -0.09959319089659908475, 2.118264760961988458 ) ) ;
#154610=CARTESIAN_POINT ( 'NONE',  ( 5.326796142270829648, 0.8146286751641409474, -1.844708973168760924 ) ) ;
#154612=CARTESIAN_POINT ( 'NONE',  ( 3.766515156912704665, -0.8315086482118605460, -1.887695802070661344 ) ) ;
#154614=CARTESIAN_POINT ( 'NONE',  ( -0.1411974294642046046, 7.629137130509075604, -2.500278959528269063 ) ) ;
#154618=CARTESIAN_POINT ( 'NONE',  ( 6.035146784841348477, -1.584849238314169240, -1.513754250258770639 ) ) ;
#154619=CARTESIAN_POINT ( 'NONE',  ( 3.252577435111691617, 1.966644794889659043, -0.4445022851852917234 ) ) ;
#154620=CARTESIAN_POINT ( 'NONE',  ( 3.421284184235491743, -1.099380227797893905, -1.476844927387373163 ) ) ;
#154622=CARTESIAN_POINT ( 'NONE',  ( 0.1645217639845691082, -1.537023147574669402, -0.7826882907640534404 ) ) ;
#154624=CARTESIAN_POINT ( 'NONE',  ( 0.5812297525147345212, -0.8198687466959112546, 2.147686052911641497 ) ) ;
#154626=CARTESIAN_POINT ( 'NONE',  ( 0.6325467830279264403, 1.161941506187497364, -1.941124190868536603 ) ) ;
#154627=CARTESIAN_POINT ( 'NONE',  ( 2.824945763694948653, 1.983238121251710950, 0.7091105908984902673 ) ) ;
#154635=CARTESIAN_POINT ( 'NONE',  ( 2.197662576721173266, 1.936918166296027977, -0.8637449004969055544 ) ) ;
#154636=CARTESIAN_POINT ( 'NONE',  ( 4.236746486948286261, 1.365021424349493584, -1.752494286840690085 ) ) ;
#154637=CARTESIAN_POINT ( 'NONE',  ( 2.185716925580234449, -0.9354795820612994417, 1.981881815340847730 ) ) ;
#154640=CARTESIAN_POINT ( 'NONE',  ( 5.951606347324345236, 1.484592722905058393, 1.282605414028796353 ) ) ;
#154644=CARTESIAN_POINT ( 'NONE',  ( 4.306960158517386894, -0.4675538901007176285, -2.068242682749166672 ) ) ;
#154647=CARTESIAN_POINT ( 'NONE',  ( 5.137646372127643524, -1.526005641499485810, -1.531359247741073570 ) ) ;
#154649=CARTESIAN_POINT ( 'NONE',  ( 4.686955257832659427, 1.367739038236553295, 1.232883728221022990 ) ) ;
#154652=CARTESIAN_POINT ( 'NONE',  ( 0.4677839449492172674, -1.637930601595443125, -0.5889144675248291216 ) ) ;
#154653=CARTESIAN_POINT ( 'NONE',  ( 6.727182134110201162, 0.003007720480356981373, 1.910970182385363092 ) ) ;
#154656=CARTESIAN_POINT ( 'NONE',  ( 4.241217004700631676, -1.882188537963986219, 1.063020064016991117 ) ) ;
#154659=CARTESIAN_POINT ( 'NONE',  ( 3.924826023212550030, 2.051882857192890430, 0.6804245187241527715 ) ) ;
#154660=CARTESIAN_POINT ( 'NONE',  ( 4.428955518335824237, 0.09376622492938446740, 1.969227427985324352 ) ) ;
#154661=CARTESIAN_POINT ( 'NONE',  ( 3.514723022282209897, 1.734034291474368494, 0.002059465714070173124 ) ) ;
#154662=CARTESIAN_POINT ( 'NONE',  ( 0.4510473619779230003, -1.854578567552306767, -1.167393260480112493 ) ) ;
#154663=CARTESIAN_POINT ( 'NONE',  ( 1.009288123910282442, 1.745381235414251275, -1.509623180311530977 ) ) ;
#154664=CARTESIAN_POINT ( 'NONE',  ( 3.497389175668437211, 1.622225323665491326, 1.270757995044344391 ) ) ;
#154665=CARTESIAN_POINT ( 'NONE',  ( 5.970255158568685161, -1.845527328187264615, -0.6049325008806984982 ) ) ;
#154672=CARTESIAN_POINT ( 'NONE',  ( 3.311752114541001379, -0.4323003076652854881, 2.163846791405985570 ) ) ;
#154675=CARTESIAN_POINT ( 'NONE',  ( 0.4790722831046652641, -0.09921120595577682943, 1.858460205838560864 ) ) ;
#154676=CARTESIAN_POINT ( 'NONE',  ( -0.02900071798685524560, 2.860900941590225344, -2.661937258840251008 ) ) ;
#154680=CARTESIAN_POINT ( 'NONE',  ( 6.825078400183577365, 2.023440267519378999, 2.448151054272352578 ) ) ;
#154682=CARTESIAN_POINT ( 'NONE',  ( 6.474545096729184657, -0.09562278402284157819, -1.838781726270556582 ) ) ;
#154684=CARTESIAN_POINT ( 'NONE',  ( 2.008734545381769543, 1.527802914727709016, -1.383344190003793495 ) ) ;
#154691=CARTESIAN_POINT ( 'NONE',  ( 0.7079729303958534059, -2.051031625230379074, 0.2011725655505970656 ) ) ;
#154692=CARTESIAN_POINT ( 'NONE',  ( 6.620655732516651071, -0.002413161512292844035, 2.173887093218453082 ) ) ;
#154693=CARTESIAN_POINT ( 'NONE',  ( 4.722110844128335039, 1.763445737372179689, 0.5296355584529164329 ) ) ;
#154697=CARTESIAN_POINT ( 'NONE',  ( 5.444034239667132624, 0.8972360612293399651, -2.016436982482258333 ) ) ;
#154698=CARTESIAN_POINT ( 'NONE',  ( 0.5972264258897291844, 1.797487153981947916, -1.200333582630601637 ) ) ;
#154700=CARTESIAN_POINT ( 'NONE',  ( 0.5977379272000953314, 1.286164058678052946, 1.415416067018962165 ) ) ;
#154701=CARTESIAN_POINT ( 'NONE',  ( 1.323454262349360144, -1.463929862531298198, -1.387097294446784090 ) ) ;
#154704=CARTESIAN_POINT ( 'NONE',  ( 1.458857794315861156, 1.741214688395021470, 1.500301734068248294 ) ) ;
#154708=CARTESIAN_POINT ( 'NONE',  ( 1.410794581852807150, 1.648159533202856686, 0.8848386531258023435 ) ) ;
#154710=CARTESIAN_POINT ( 'NONE',  ( 2.782435679340321766, -0.5899881929209308540, -1.928257399728677601 ) ) ;
#154714=CARTESIAN_POINT ( 'NONE',  ( 5.057299757384343231, -1.778698004947255162, -1.127411927216742216 ) ) ;
#154719=CARTESIAN_POINT ( 'NONE',  ( 4.113539317574116616, 1.624649823752024824, 1.199838557982295217 ) ) ;
#154721=CARTESIAN_POINT ( 'NONE',  ( 6.883263157960402445, -0.003972766660574957552, 2.046037087719229319 ) ) ;
#154723=CARTESIAN_POINT ( 'NONE',  ( 4.991577004318280331, 1.598001195387260154, 1.455802845438579407 ) ) ;
#154729=CARTESIAN_POINT ( 'NONE',  ( 2.242849641980674491, -2.128998374728574117, -0.4250897845002408193 ) ) ;
#154732=CARTESIAN_POINT ( 'NONE',  ( 1.487592393518050837, -1.832424703912252317, -0.1798031890194173865 ) ) ;
#154734=CARTESIAN_POINT ( 'NONE',  ( 2.788834510562918645, 1.878274557074947948, -1.128960604485473862 ) ) ;
#154736=CARTESIAN_POINT ( 'NONE',  ( 3.327297708271567345, 0.05365531978675056046, 2.262033696468904065 ) ) ;
#154742=CARTESIAN_POINT ( 'NONE',  ( 5.149538872483485186, 0.5550977867328189541, -1.680460614999980340 ) ) ;
#154743=CARTESIAN_POINT ( 'NONE',  ( 3.580729931658500398, -1.350255368601901651, 1.493277094049742182 ) ) ;
#154745=CARTESIAN_POINT ( 'NONE',  ( 2.221831145078187575, -2.042928948074810069, 0.5108812299794410761 ) ) ;
#154748=CARTESIAN_POINT ( 'NONE',  ( 1.433975083751269697, 1.170624227716898780, 1.583764482814524088 ) ) ;
#154750=CARTESIAN_POINT ( 'NONE',  ( 0.3616705494772323726, -0.5269360983083425376, 1.889693748445469224 ) ) ;
#154751=CARTESIAN_POINT ( 'NONE',  ( 6.275650443109183740, 0.3000964294621047967, -1.786390703358155196 ) ) ;
#154755=CARTESIAN_POINT ( 'NONE',  ( 4.574985519202336981, -0.0001439422951596270033, -1.870836309977530920 ) ) ;
#154757=CARTESIAN_POINT ( 'NONE',  ( 5.155165671438199482, 1.724248240607465732, -1.145533019084030268 ) ) ;
#154768=CARTESIAN_POINT ( 'NONE',  ( 5.037533845850875380, 1.831247050742194515, -0.7043679133837479345 ) ) ;
#154770=CARTESIAN_POINT ( 'NONE',  ( 1.880232294074701604, -0.2495702131940503166, 2.000550610736756774 ) ) ;
#154773=CARTESIAN_POINT ( 'NONE',  ( 0.04676574305502100015, -1.756316032869180921, 1.310637071781264984 ) ) ;
#154775=CARTESIAN_POINT ( 'NONE',  ( 1.932664581101939838, 0.1784410483233467293, 1.861995071071875785 ) ) ;
#154777=CARTESIAN_POINT ( 'NONE',  ( 3.990493469460140830, -1.155612956054508977, 1.648335472937176194 ) ) ;
#154780=CARTESIAN_POINT ( 'NONE',  ( 3.198929712650464996, 1.915108447241938627, 0.9030302060772307238 ) ) ;
#154782=CARTESIAN_POINT ( 'NONE',  ( 5.002425025097493538, 2.064580399062130311, 0.1557331365308264881 ) ) ;
#154783=CARTESIAN_POINT ( 'NONE',  ( 0.9078953525096540300, -0.9432727566685695786, -1.865958795489220723 ) ) ;
#154784=CARTESIAN_POINT ( 'NONE',  ( 6.620655732516668834, 7.629137130509086262, 2.673739711112704143 ) ) ;
#154785=CARTESIAN_POINT ( 'NONE',  ( 6.299803673773761936, -0.6120917497752301761, 1.720027978493202436 ) ) ;
#154786=ORIENTED_EDGE ( 'NONE', *, *, #11231, .T. ) ;
#154791=CARTESIAN_POINT ( 'NONE',  ( 5.918603479541379109, -0.6925943527147163659, -1.782627650866043911 ) ) ;
#154799=CARTESIAN_POINT ( 'NONE',  ( 6.116814581292481456, 0.2004514801264325186, 2.006445662566976651 ) ) ;
#154802=CARTESIAN_POINT ( 'NONE',  ( -0.1405533004718313439, 1.431097497908106808, -1.984188993888830632 ) ) ;
#154806=CARTESIAN_POINT ( 'NONE',  ( 3.326963294591319009, -1.817917149290064982, -0.7580491890798303212 ) ) ;
#154807=CARTESIAN_POINT ( 'NONE',  ( 4.060172857048785389, -1.158672032380179573, 1.650094836768666084 ) ) ;
#154811=CARTESIAN_POINT ( 'NONE',  ( 4.646525747415945595, -1.761044916313101671, 1.304081410864160739 ) ) ;
#154813=CARTESIAN_POINT ( 'NONE',  ( 3.522408793619712153, 1.222923848883204156, -1.488421986030899591 ) ) ;
#154815=CARTESIAN_POINT ( 'NONE',  ( -0.1298852118743840378, 0.7651466308506644776, -1.811855282322960781 ) ) ;
#154816=CARTESIAN_POINT ( 'NONE',  ( 0.4521680116954321371, 0.6883007682146925488, -2.096869779678663281 ) ) ;
#154817=CARTESIAN_POINT ( 'NONE',  ( 0.07536363704235826688, -0.001874865094115066300, -2.144269471569634877 ) ) ;
#154823=CARTESIAN_POINT ( 'NONE',  ( -0.1119450412391852639, -0.4286113830911059130, -1.901434273657340412 ) ) ;
#154824=CARTESIAN_POINT ( 'NONE',  ( 2.772137614628172653, 2.003179168937582855, -0.1996775111661793500 ) ) ;
#154825=CARTESIAN_POINT ( 'NONE',  ( 5.202631756544580988, -1.620200680833181694, -1.630429044757361723 ) ) ;
#154827=CARTESIAN_POINT ( 'NONE',  ( 3.238934005158759621, -0.1320712000743811398, -1.856290971584534377 ) ) ;
#154831=CARTESIAN_POINT ( 'NONE',  ( 6.240485052285455581, 1.095381943021833449, -1.567431287326017664 ) ) ;
#154834=CARTESIAN_POINT ( 'NONE',  ( 5.741762370215764300, 2.088391581209507741, 0.1015199779932918489 ) ) ;
#154838=CARTESIAN_POINT ( 'NONE',  ( -0.02319159430949970999, 0.003959926571647092407, -1.810968101872318714 ) ) ;
#154840=CARTESIAN_POINT ( 'NONE',  ( 2.584235440824592001, -0.5423091454765850417, 1.647252552357024280 ) ) ;
#154846=CARTESIAN_POINT ( 'NONE',  ( 0.5321919801732944988, 1.189095644551215525, 1.694524325727378322 ) ) ;
#154847=CARTESIAN_POINT ( 'NONE',  ( 5.742758765878789085, 0.3605303665093100851, 1.789564367143759327 ) ) ;
#154848=CARTESIAN_POINT ( 'NONE',  ( 3.696105151714265347, 0.8860871710942277435, -1.750347149911928968 ) ) ;
#154852=CARTESIAN_POINT ( 'NONE',  ( 3.739029402251158984, 2.014021593674422572, 0.6637135986873595739 ) ) ;
#154857=CARTESIAN_POINT ( 'NONE',  ( 2.202089267374872872, 0.7962392033929905910, -1.911209141678638090 ) ) ;
#154859=CARTESIAN_POINT ( 'NONE',  ( 4.090652671443067767, -1.278631810133125546, 1.816222553172279319 ) ) ;
#154861=CARTESIAN_POINT ( 'NONE',  ( 2.057686432631794293, -1.410295276735703540, 1.815187820423395992 ) ) ;
#154863=CARTESIAN_POINT ( 'NONE',  ( 6.244999159755385776, -0.2970413431409227312, -2.040939473721150144 ) ) ;
#154867=CARTESIAN_POINT ( 'NONE',  ( 6.462460624273299814, -1.686435539877573220, -0.7394478613861471539 ) ) ;
#154869=CARTESIAN_POINT ( 'NONE',  ( 3.164218664783400747, 1.912571728330178855, -0.004505864839042527346 ) ) ;
#154870=CARTESIAN_POINT ( 'NONE',  ( -0.2106725631050202496, 0.2307243749109839093, -2.036935839376171842 ) ) ;
#154871=CARTESIAN_POINT ( 'NONE',  ( 3.961678648311004025, 1.711676862058534088, -0.2113787121680379411 ) ) ;
#154872=CARTESIAN_POINT ( 'NONE',  ( 1.956267901341804283, -1.236798062192035363, 1.592663274815858676 ) ) ;
#154873=CARTESIAN_POINT ( 'NONE',  ( 3.586856395851648394, -0.6656857563790157251, 2.200217309063193127 ) ) ;
#154874=CARTESIAN_POINT ( 'NONE',  ( 3.638171750181828035, 1.021205778115843010, -2.018914226005202206 ) ) ;
#154875=CARTESIAN_POINT ( 'NONE',  ( -0.01666059994226073634, -0.1612322585618740090, -2.171656592459796808 ) ) ;
#154878=CARTESIAN_POINT ( 'NONE',  ( 4.991328707773068807, 1.311207439723049317, 1.188721964340031301 ) ) ;
#154880=CARTESIAN_POINT ( 'NONE',  ( 0.6742756655733075366, -1.268823270132292791, 1.908895542103898890 ) ) ;
#154881=CARTESIAN_POINT ( 'NONE',  ( 5.578019757025042047, -1.797138167560994759, -0.3993771437491022702 ) ) ;
#154883=CARTESIAN_POINT ( 'NONE',  ( 6.158177532299373702, -1.552315630085840947, 1.547116483708823820 ) ) ;
#154887=CARTESIAN_POINT ( 'NONE',  ( 6.215297738502283842, -1.773692237561547147, -1.067698627785176768 ) ) ;
#154888=CARTESIAN_POINT ( 'NONE',  ( -0.1882626618336727398, -1.244567986390752390, -1.587255334073833790 ) ) ;
#154891=( BOUNDED_SURFACE ( )  B_SPLINE_SURFACE ( 3, 3, ( 
 ( #172867, #123139, #90549, #74288, #122053, #41809, #206402, #38584, #189097, #153399, #155541 ),
 ( #22293, #25520, #40730, #119900, #6052, #23376, #204244, #203188, #4970, #156613, #55896 ),
 ( #190154, #140383, #71048, #106836, #9278, #188017, #37510, #39645, #105753, #58027, #75349 ),
 ( #107922, #91628, #171780, #202107, #53767, #89486, #21228, #137164, #7120, #73193, #192272 ),
 ( #27657, #96959, #142512, #13537, #94817, #208521, #79607, #113253, #43933, #92688, #10329 ),
 ( #211726, #28732, #193357, #209583, #125250, #210669, #179258, #93753, #12462, #144654, #78537 ),
 ( #108982, #62297, #195500, #194424, #112186, #128456, #46065, #61229, #207471, #60156, #159791 ) ),
 .UNSPECIFIED., .T., .F., .F. ) 
 B_SPLINE_SURFACE_WITH_KNOTS ( ( 4, 3, 4 ),
 ( 4, 1, 1, 1, 1, 1, 1, 1, 4 ),
 ( 0.000000000000000000, 0.5000000000000000000, 1.000000000000000000 ),
 ( 0.000000000000000000, 0.2254179815473072723, 0.3971144120416517653, 0.5241699701252212629, 0.6156743509408303394, 0.6807935377546089351, 0.7289379548928518471, 0.7696256121123346006, 1.000000000000000000 ),
 .UNSPECIFIED. ) 
 GEOMETRIC_REPRESENTATION_ITEM ( )  RATIONAL_B_SPLINE_SURFACE ( (
 ( 1.000000000000000000, 1.000000000000000000, 1.000000000000000222, 0.9999999999999997780, 0.9999999999999997780, 1.000000000000000222, 0.9999999999999997780, 1.000000000000000222, 0.9999999999999992228, 1.000000000000000000, 1.000000000000000000),
 ( 0.3333333333333333703, 0.3333333333333334259, 0.3333333333333334259, 0.3333333333333332593, 0.3333333333333333703, 0.3333333333333334259, 0.3333333333333333703, 0.3333333333333334814, 0.3333333333333332038, 0.3333333333333333703, 0.3333333333333333703),
 ( 0.3333333333333333703, 0.3333333333333334259, 0.3333333333333334259, 0.3333333333333332593, 0.3333333333333333703, 0.3333333333333334259, 0.3333333333333333703, 0.3333333333333334814, 0.3333333333333332038, 0.3333333333333333703, 0.3333333333333333703),
 ( 1.000000000000000000, 1.000000000000000000, 1.000000000000000222, 0.9999999999999997780, 0.9999999999999997780, 1.000000000000000222, 0.9999999999999997780, 1.000000000000000222, 0.9999999999999992228, 1.000000000000000000, 1.000000000000000000),
 ( 0.3333333333333333703, 0.3333333333333334259, 0.3333333333333334259, 0.3333333333333332593, 0.3333333333333333703, 0.3333333333333334259, 0.3333333333333333703, 0.3333333333333334814, 0.3333333333333332038, 0.3333333333333333703, 0.3333333333333333703),
 ( 0.3333333333333333703, 0.3333333333333334259, 0.3333333333333334259, 0.3333333333333332593, 0.3333333333333333703, 0.3333333333333334259, 0.3333333333333333703, 0.3333333333333334814, 0.3333333333333332038, 0.3333333333333333703, 0.3333333333333333703),
 ( 1.000000000000000000, 1.000000000000000000, 1.000000000000000222, 0.9999999999999997780, 0.9999999999999997780, 1.000000000000000222, 0.9999999999999997780, 1.000000000000000222, 0.9999999999999992228, 1.000000000000000000, 1.000000000000000000) ) ) 
 REPRESENTATION_ITEM ( '' )  SURFACE ( )  );
#154893=CARTESIAN_POINT ( 'NONE',  ( 4.881433204766033818, 1.796953459403265674, -0.6949688560347905275 ) ) ;
#154895=CARTESIAN_POINT ( 'NONE',  ( 0.7037666293719077037, 1.955508453885120401, -1.053950084065604864 ) ) ;
#154905=CARTESIAN_POINT ( 'NONE',  ( 1.029656018189710309, 1.891699080040713410, -0.5197978237033786808 ) ) ;
#154908=CARTESIAN_POINT ( 'NONE',  ( 6.355910407107248083, -0.6622273607519140182, 1.846833223631501264 ) ) ;
#154911=CARTESIAN_POINT ( 'NONE',  ( 0.6380306694902828646, -1.602208245511031803, -1.597717328844779239 ) ) ;
#154915=CARTESIAN_POINT ( 'NONE',  ( 1.018573325691285003, 1.726041315240328444, 0.7214104187760682629 ) ) ;
#154916=CARTESIAN_POINT ( 'NONE',  ( 0.1055823559395060729, -0.08803060671099156853, 1.732021048141555220 ) ) ;
#154918=CARTESIAN_POINT ( 'NONE',  ( 4.247736854543925133, 2.191053489037126045, -0.05455935714590579716 ) ) ;
#154919=CARTESIAN_POINT ( 'NONE',  ( 4.594930786881223916, -0.5007672277346334466, -2.252456893713528530 ) ) ;
#154920=CARTESIAN_POINT ( 'NONE',  ( 6.661407821810922947, 0.3568556019579691707, -2.029490769664368255 ) ) ;
#154921=CARTESIAN_POINT ( 'NONE',  ( 2.343606807962240524, 1.941525774309307284, 0.04751797161560606525 ) ) ;
#154925=CARTESIAN_POINT ( 'NONE',  ( 3.727185537919291747, 2.006959858346604619, 0.1948421285040344286 ) ) ;
#154929=CARTESIAN_POINT ( 'NONE',  ( 1.383131112650197281, 1.687622997524572677, -0.6969523973551354779 ) ) ;
#154934=CARTESIAN_POINT ( 'NONE',  ( 5.225487584538335284, -1.957599804553040945, 0.6444962787128440951 ) ) ;
#154940=CARTESIAN_POINT ( 'NONE',  ( 5.707677564275420501, 1.530686452870811065, 1.317726828763097435 ) ) ;
#154941=CARTESIAN_POINT ( 'NONE',  ( 6.217462558288930019, 1.845152235743243052, 1.236491063047394201 ) ) ;
#154945=CARTESIAN_POINT ( 'NONE',  ( 4.504794318429003575, 1.594258339665870938, -1.305997064384886830 ) ) ;
#154946=CARTESIAN_POINT ( 'NONE',  ( 4.272111401563948085, 1.799923229630392640, -0.9091438646662284295 ) ) ;
#154953=CARTESIAN_POINT ( 'NONE',  ( 3.796249832574852601, -1.863883295361246084, 0.7690029265580224926 ) ) ;
#154954=CARTESIAN_POINT ( 'NONE',  ( 3.521284115754549582, -1.097709940230184200, -1.477957507169822104 ) ) ;
#154955=CARTESIAN_POINT ( 'NONE',  ( 2.016686958704193344, -1.090287029490369930, -2.033897785187769536 ) ) ;
#154957=CARTESIAN_POINT ( 'NONE',  ( 3.392016793147753617, -0.8794390384766533897, 1.974801309016629869 ) ) ;
#154962=CARTESIAN_POINT ( 'NONE',  ( 3.638291363623618047, 0.06041265439583366065, -2.297745614018332105 ) ) ;
#154964=CARTESIAN_POINT ( 'NONE',  ( 2.131529507118444133, -1.219933349377068099, -1.418231869465089057 ) ) ;
#154965=CARTESIAN_POINT ( 'NONE',  ( 0.2101411907093185261, -0.8379918008738492796, -1.782380744178988285 ) ) ;
#154969=CARTESIAN_POINT ( 'NONE',  ( 1.911028901235469313, 1.633884665098099598, -1.483674895440662667 ) ) ;
#154974=CARTESIAN_POINT ( 'NONE',  ( 6.543826718160733691, 0.7548084958455666404, -1.821436488709103019 ) ) ;
#154975=CARTESIAN_POINT ( 'NONE',  ( 5.268348002110199602, 1.133478272989609348, 2.010090980756351176 ) ) ;
#154976=CARTESIAN_POINT ( 'NONE',  ( 0.4144086874100678664, 0.7473079093508437909, 1.814158889769983185 ) ) ;
#154977=CARTESIAN_POINT ( 'NONE',  ( 2.711848548736516040, 0.5542824208455496837, -1.986605816314121808 ) ) ;
#154985=CARTESIAN_POINT ( 'NONE',  ( 5.775877569751362017, -2.119564319632438743, 0.4699819441058172842 ) ) ;
#154987=CARTESIAN_POINT ( 'NONE',  ( 5.741722636381445533, 1.839460222191912964, 0.08393339073512617876 ) ) ;
#154991=CARTESIAN_POINT ( 'NONE',  ( 6.807534431281101028, -0.5077146954460194372, 2.213219090469565664 ) ) ;
#154995=CARTESIAN_POINT ( 'NONE',  ( -0.04057498839846879202, -1.478066481919372510, -1.213044814162365981 ) ) ;
#154996=CARTESIAN_POINT ( 'NONE',  ( 1.393014870165907526, 1.336991634843522236, 1.159753417114619545 ) ) ;
#154998=CARTESIAN_POINT ( 'NONE',  ( 6.287749749268194854, 1.925770139592613450, -0.5864224512089585284 ) ) ;
#155000=CARTESIAN_POINT ( 'NONE',  ( 3.304201903042072175, 1.212927065539553206, -1.482701048864635496 ) ) ;
#155002=CARTESIAN_POINT ( 'NONE',  ( 4.123468233510577896, 0.2432657155154849538, -1.954413393957514788 ) ) ;
#155003=CARTESIAN_POINT ( 'NONE',  ( 6.521752737896459706, -0.4354215942184087584, 1.979412122172687694 ) ) ;
#155005=CARTESIAN_POINT ( 'NONE',  ( 2.940157781200231746, 1.856316385841882965, 0.2306766016651334850 ) ) ;
#155006=CARTESIAN_POINT ( 'NONE',  ( -0.005637892868452093476, -0.3948761927005627337, -1.788892068844874395 ) ) ;
#155008=CARTESIAN_POINT ( 'NONE',  ( 2.473496279428960776, 0.1070396533628548558, -2.204406164007084445 ) ) ;
#155011=CARTESIAN_POINT ( 'NONE',  ( 0.8892172652632176488, 0.1500229334146038762, 2.057259515242230830 ) ) ;
#155020=CARTESIAN_POINT ( 'NONE',  ( 2.611853368047814872, 0.5545374748289233491, -1.994631108499920646 ) ) ;
#155024=CARTESIAN_POINT ( 'NONE',  ( 1.365885014167470546, 0.5842608817006667010, -1.933330045775418116 ) ) ;
#155027=CARTESIAN_POINT ( 'NONE',  ( 0.1749903794560410675, 1.362372954287846882, -2.209288650253756536 ) ) ;
#155029=CARTESIAN_POINT ( 'NONE',  ( 4.938827285099913311, 1.158512636183751665, 1.649828125244500843 ) ) ;
#155030=CARTESIAN_POINT ( 'NONE',  ( 6.385945889491149607, -1.915137183225220197, 0.05458341080493907954 ) ) ;
#155031=CARTESIAN_POINT ( 'NONE',  ( 6.539320575229278454, 2.035006821797652687, 2.408631514295301645 ) ) ;
#155032=CARTESIAN_POINT ( 'NONE',  ( 3.790727848299980440, 1.850687065220711469, -1.173560875862532660 ) ) ;
#155034=CARTESIAN_POINT ( 'NONE',  ( 2.672007700615218528, 1.902801012812182169, -0.1915479950082218386 ) ) ;
#155038=CARTESIAN_POINT ( 'NONE',  ( 1.546500145565053108, -1.423948579484592747, 1.427951870166991544 ) ) ;
#155040=CARTESIAN_POINT ( 'NONE',  ( 5.882419586753742102, -0.3201050945752722532, -2.167950725039065052 ) ) ;
#155042=CARTESIAN_POINT ( 'NONE',  ( 3.240908261985251837, -1.521742930289736728, 0.8118271961824756744 ) ) ;
#155044=CARTESIAN_POINT ( 'NONE',  ( 6.064709079624690524, 0.6667526090060638122, 2.013086243192941716 ) ) ;
#155048=CARTESIAN_POINT ( 'NONE',  ( 0.3089402658475807195, -1.578002999302514642, 1.165503548361209063 ) ) ;
#155053=AXIS2_PLACEMENT_3D ( 'NONE', #181676, #48512, #100443 ) ;
#155055=CARTESIAN_POINT ( 'NONE',  ( 2.367557981294612812, 0.4819373766774863177, -1.746117998840409191 ) ) ;
#155059=CARTESIAN_POINT ( 'NONE',  ( 3.826654739275455519, 1.278450958818643901, -1.283618901898140985 ) ) ;
#155064=CARTESIAN_POINT ( 'NONE',  ( 5.336322170104328855, -1.033901835001526104, 1.547212704913742520 ) ) ;
#155066=CARTESIAN_POINT ( 'NONE',  ( 2.583477129321013255, -0.5985834622587657972, 1.819768813671450935 ) ) ;
#155076=CARTESIAN_POINT ( 'NONE',  ( 0.9903105584966699348, -0.5097506344743455431, -2.027405242695742515 ) ) ;
#155078=CARTESIAN_POINT ( 'NONE',  ( 6.616243401494351417, -0.9090183210780745648, -1.698415751782512695 ) ) ;
#155080=CARTESIAN_POINT ( 'NONE',  ( 2.080808903162992607, -0.08653491207171599975, -1.823647505904809174 ) ) ;
#155082=CARTESIAN_POINT ( 'NONE',  ( 1.511816067030671729, -0.6413169068853613597, 1.801808535584384252 ) ) ;
#155085=CARTESIAN_POINT ( 'NONE',  ( 1.398812336859527550, 0.3809602064741451355, 1.932172009363951837 ) ) ;
#155086=CARTESIAN_POINT ( 'NONE',  ( 3.808095655114822176, 1.371164123868431117, -1.375570907105559293 ) ) ;
#155090=CARTESIAN_POINT ( 'NONE',  ( 0.2208628207966298607, -1.659654761427356240, -0.8422171645118268213 ) ) ;
#155101=CARTESIAN_POINT ( 'NONE',  ( 3.650846181029033133, -1.491723252493650564, 1.052289205326197852 ) ) ;
#155102=CARTESIAN_POINT ( 'NONE',  ( 5.858611323429600226, -1.916351766245901977, -0.6279953093112633500 ) ) ;
#155107=CARTESIAN_POINT ( 'NONE',  ( 4.592568387165754551, -0.4099775813008778025, -1.825014511474598589 ) ) ;
#155109=CARTESIAN_POINT ( 'NONE',  ( 2.561056213344356181, -1.676160556340213992, -0.9495491084439124929 ) ) ;
#155110=CARTESIAN_POINT ( 'NONE',  ( 6.543807102324334934, 1.350441955444921849, 1.423202910149905298 ) ) ;
#155117=CARTESIAN_POINT ( 'NONE',  ( 0.1052747227462194346, -0.09900681772390507174, 2.115024835901352596 ) ) ;
#155120=CARTESIAN_POINT ( 'NONE',  ( 5.330949937734919430, -1.947458545883517189, -0.7027056652011903770 ) ) ;
#155121=CARTESIAN_POINT ( 'NONE',  ( 0.08126746489400815676, -0.8690269180096841239, 1.623235155968821841 ) ) ;
#155123=CARTESIAN_POINT ( 'NONE',  ( 4.940191063930403637, -1.940984743010031544, -1.231243198015237628 ) ) ;
#155127=CARTESIAN_POINT ( 'NONE',  ( 0.8148889116572692881, 2.119938092393148565, 0.8724386107587696060 ) ) ;
#155130=CARTESIAN_POINT ( 'NONE',  ( 5.244061567092353826, 0.5653492691648214219, 1.857832877570769314 ) ) ;
#155134=CARTESIAN_POINT ( 'NONE',  ( 5.801015586618943232, -0.2871438832755985326, -1.890612906794430614 ) ) ;
#155135=CARTESIAN_POINT ( 'NONE',  ( 6.210172754313918908, 1.157103754073171675, -1.651340222398114843 ) ) ;
#155139=CARTESIAN_POINT ( 'NONE',  ( 3.152369405254138446, -1.582674238129866184, 1.366072548952133259 ) ) ;
#155140=CARTESIAN_POINT ( 'NONE',  ( 1.691920373447815207, -1.760920987957525385, -0.1775098275408875104 ) ) ;
#155141=CARTESIAN_POINT ( 'NONE',  ( 6.604150280000163242, -0.1430408514614608939, 1.983920101186954721 ) ) ;
#155142=CARTESIAN_POINT ( 'NONE',  ( 4.312625044126452423, 2.094834666918590216, 0.9310453638207391025 ) ) ;
#155143=CARTESIAN_POINT ( 'NONE',  ( 1.710509606392306647, -0.2150479285965025134, 1.726905287013901225 ) ) ;
#155146=CARTESIAN_POINT ( 'NONE',  ( 2.459901920361181826, 1.337243170739129239, 1.103576756174700746 ) ) ;
#155148=CARTESIAN_POINT ( 'NONE',  ( 1.468971578825052804, 1.639158939101122758, 0.8813203298513817563 ) ) ;
#155149=CARTESIAN_POINT ( 'NONE',  ( 2.910768570555821277, 0.7291657262279130913, 2.045214924614814578 ) ) ;
#155151=CARTESIAN_POINT ( 'NONE',  ( 4.505092375653735992, -0.09411930587044713137, 2.014432893821124004 ) ) ;
#155152=CARTESIAN_POINT ( 'NONE',  ( 2.843750000000001332, 1.895863743164146298, 0.7852924748298368840 ) ) ;
#155155=CARTESIAN_POINT ( 'NONE',  ( 1.114139429068806919, -0.8636777455973219109, -1.721994443286285259 ) ) ;
#155157=CARTESIAN_POINT ( 'NONE',  ( 4.992532747203591192, -1.233408671777506349, 1.847344450390429937 ) ) ;
#155162=CARTESIAN_POINT ( 'NONE',  ( 0.9091800373960364778, -0.5448693228766487984, -2.153321320651789161 ) ) ;
#155163=CARTESIAN_POINT ( 'NONE',  ( 6.285602425426498385, -1.847771260692541162, 0.6596951833430020340 ) ) ;
#155166=CARTESIAN_POINT ( 'NONE',  ( 5.800151253372650473, -2.262578822528161560, -0.008439264561578212892 ) ) ;
#155169=CARTESIAN_POINT ( 'NONE',  ( 3.771981659335025938, -2.032644659601599457, 0.3498187521492699403 ) ) ;
#155173=CARTESIAN_POINT ( 'NONE',  ( 4.727732462671866642, -1.149354582003499159, -1.475719300151681512 ) ) ;
#155174=CARTESIAN_POINT ( 'NONE',  ( 3.990606130280470509, -1.729166733334456030, 0.1323968765898491939 ) ) ;
#155175=CARTESIAN_POINT ( 'NONE',  ( 3.614586527008158523, -0.1238012486478034802, 1.736083139875769676 ) ) ;
#155176=CARTESIAN_POINT ( 'NONE',  ( 0.7148891103036036920, 2.120809155261915713, 0.8706237914077943341 ) ) ;
#155178=CARTESIAN_POINT ( 'NONE',  ( 5.003505698738024421, -2.080571448108500476, 0.2061593518874194064 ) ) ;
#155179=CARTESIAN_POINT ( 'NONE',  ( 5.244061567092353826, 0.5653492691648214219, 1.857832877570769314 ) ) ;
#155183=CARTESIAN_POINT ( 'NONE',  ( 0.9850002542920628379, -2.016597020373378513, 0.002813405579435435122 ) ) ;
#155184=CARTESIAN_POINT ( 'NONE',  ( 1.266058358664986949, 0.6103625328083387425, -2.030891291126469600 ) ) ;
#155188=CARTESIAN_POINT ( 'NONE',  ( 2.051582899450168362, -1.892833867889589960, 0.9560217657286762538 ) ) ;
#155190=CARTESIAN_POINT ( 'NONE',  ( 4.037589748876240670, -1.260430739550026269, -1.321009972365666307 ) ) ;
#155196=CARTESIAN_POINT ( 'NONE',  ( 2.566670905829854021, 0.6845714803544473703, 1.900350667086497580 ) ) ;
#155197=CARTESIAN_POINT ( 'NONE',  ( 5.860442804830619856, 0.8892231252738895808, 2.019869304780027353 ) ) ;
#155199=CARTESIAN_POINT ( 'NONE',  ( 3.168646232094144199, 1.351176984073151788, -1.279899388936973192 ) ) ;
#155205=CARTESIAN_POINT ( 'NONE',  ( 5.074738461036464088, -1.720261882950037124, -0.6118011564382742629 ) ) ;
#155209=CARTESIAN_POINT ( 'NONE',  ( 1.018380972650875460, 1.732250818821230443, -0.07729615888975129023 ) ) ;
#155210=CARTESIAN_POINT ( 'NONE',  ( -0.01232043299871990460, -0.3711077647031227333, -1.706071622908360119 ) ) ;
#155211=CARTESIAN_POINT ( 'NONE',  ( 5.654963871297442601, -1.822634436652656342, 1.415334302069543027 ) ) ;
#155213=CARTESIAN_POINT ( 'NONE',  ( 0.2982115315293157320, -2.060280707965747027, -0.05303618902755858483 ) ) ;
#155216=CARTESIAN_POINT ( 'NONE',  ( 5.729893540575130118, -2.074111880986319711, -0.9905765078317919636 ) ) ;
#155219=CARTESIAN_POINT ( 'NONE',  ( 5.805500895539822181, -0.4530025297027094888, 1.814837910242727226 ) ) ;
#155220=CARTESIAN_POINT ( 'NONE',  ( 3.814637755342592307, -0.6046605605216844870, -1.814329123173196834 ) ) ;
#155222=CARTESIAN_POINT ( 'NONE',  ( 4.881566871873391555, 2.059980941486462047, -0.7921658822237286346 ) ) ;
#155223=CARTESIAN_POINT ( 'NONE',  ( 5.014918053075636095, 0.1589874617720990202, 2.111459674661147368 ) ) ;
#155228=CARTESIAN_POINT ( 'NONE',  ( 5.461630201184114242, -1.671734486004393450, -1.304435072541964447 ) ) ;
#155229=CARTESIAN_POINT ( 'NONE',  ( 2.239721530183640841, -2.061013379209011287, 1.037980457044695992 ) ) ;
#155230=CARTESIAN_POINT ( 'NONE',  ( 3.350005920730843911, -0.7974703105717847462, 1.792663495558038056 ) ) ;
#155232=CARTESIAN_POINT ( 'NONE',  ( 6.930530977065029852, -1.274000060550171787, 1.622871787371343855 ) ) ;
#155236=CARTESIAN_POINT ( 'NONE',  ( 5.489470343000498076, -0.4852711138302409077, 1.957169415941109047 ) ) ;
#155239=CARTESIAN_POINT ( 'NONE',  ( 2.993230899678362089, 0.2615320595270088644, 2.155169926569647565 ) ) ;
#155241=CARTESIAN_POINT ( 'NONE',  ( 0.2465380642357860586, 1.084720387836759725, -1.822023332652397354 ) ) ;
#155247=CARTESIAN_POINT ( 'NONE',  ( 1.528665837207894285, 1.985218273788964316, 0.5525772030575173410 ) ) ;
#155253=CARTESIAN_POINT ( 'NONE',  ( 3.897043152223302886, -0.1904361752127527174, -1.902785305300330743 ) ) ;
#155254=CARTESIAN_POINT ( 'NONE',  ( 5.155052684544634722, -1.496415494590461748, -0.9447146595812674352 ) ) ;
#155257=CARTESIAN_POINT ( 'NONE',  ( 0.5447927104418804900, 0.1337802856970966847, 1.806726864048732173 ) ) ;
#155259=CARTESIAN_POINT ( 'NONE',  ( 0.7080363470168028472, 1.138615994813133359, -1.540489816406021673 ) ) ;
#155261=CARTESIAN_POINT ( 'NONE',  ( 2.172408243068229439, -0.9739482337229148357, -1.826950231780352762 ) ) ;
#155263=CARTESIAN_POINT ( 'NONE',  ( 6.016445890116215445, 1.255022122864515310, -1.387330985440645037 ) ) ;
#155264=CARTESIAN_POINT ( 'NONE',  ( 2.473051018021198200, 0.08991741065280876855, -1.823594477012622228 ) ) ;
#155265=CARTESIAN_POINT ( 'NONE',  ( 5.391335350415090488, 1.947751002805158560, -1.037606470750504828 ) ) ;
#155268=CARTESIAN_POINT ( 'NONE',  ( 3.613784930257180950, 0.5038104997578238820, -2.000076687661219044 ) ) ;
#155272=CARTESIAN_POINT ( 'NONE',  ( 0.3687372981288695728, -1.412185959430117821, 1.636573055046482983 ) ) ;
#155274=CARTESIAN_POINT ( 'NONE',  ( 6.092251258522619395, 1.023830597077223903, -1.799436568697235783 ) ) ;
#155276=CARTESIAN_POINT ( 'NONE',  ( 3.796290242343594024, -2.158924006851222988, -0.1102321833298808840 ) ) ;
#155277=CARTESIAN_POINT ( 'NONE',  ( 3.738929604108613969, 1.918458267904774806, 0.6316034170958833016 ) ) ;
#155278=CARTESIAN_POINT ( 'NONE',  ( 2.365611650783586040, -0.4327418640146083462, 1.913375882425945917 ) ) ;
#155284=CARTESIAN_POINT ( 'NONE',  ( 2.061732777098632230, 1.244387006429502396, 1.586668050434843158 ) ) ;
#155287=CARTESIAN_POINT ( 'NONE',  ( 5.959226163113887864, -1.611951592244726950, 1.028742869173946861 ) ) ;
#155291=CARTESIAN_POINT ( 'NONE',  ( 3.919546125582054508, -1.392558991000433011, -1.458545569310132350 ) ) ;
#155294=CARTESIAN_POINT ( 'NONE',  ( 6.616207624681263333, -0.8185094323158810248, -1.518158226148608625 ) ) ;
#155298=CARTESIAN_POINT ( 'NONE',  ( 4.042156614576187579, 1.861303109871172312, 0.1859210194900539903 ) ) ;
#155300=CARTESIAN_POINT ( 'NONE',  ( 1.832961912758425349, -1.964510197511709189, -0.6532998099852762586 ) ) ;
#155305=CARTESIAN_POINT ( 'NONE',  ( 0.3160300859305562593, 1.034144755472726995, -1.730879882831819705 ) ) ;
#155306=CARTESIAN_POINT ( 'NONE',  ( 1.687489445765244289, 1.732788098368071461, -0.5283295289823899399 ) ) ;
#155312=CARTESIAN_POINT ( 'NONE',  ( 5.800374965758359203, 1.282846238547242557, -1.422814914302351852 ) ) ;
#155319=CARTESIAN_POINT ( 'NONE',  ( 3.221700144506876917, -2.083771231579465866, 0.5749860669421111847 ) ) ;
#155322=CARTESIAN_POINT ( 'NONE',  ( 1.301209403646291118, -0.3165094942152619772, -2.096747597609450953 ) ) ;
#155323=CARTESIAN_POINT ( 'NONE',  ( 5.737271026523679041, -1.649412122839075234, 0.7826820710771440481 ) ) ;
#155324=CARTESIAN_POINT ( 'NONE',  ( 1.686731049638652502, -0.2853660037422758866, -1.950466449893713428 ) ) ;
#155325=CARTESIAN_POINT ( 'NONE',  ( 4.605663860560767375, 1.420894170025093439, 1.280184534114735095 ) ) ;
#155328=CARTESIAN_POINT ( 'NONE',  ( 5.424252406547988237, 0.9690106866696795995, 1.714583495817107783 ) ) ;
#155329=CARTESIAN_POINT ( 'NONE',  ( 0.005655660794708254786, -0.8285957215397036224, -1.754384556632330838 ) ) ;
#155333=MANIFOLD_SOLID_BREP ( 'Sweep1[2]', #39627 ) ;
#155336=CARTESIAN_POINT ( 'NONE',  ( 4.688094572372190960, 1.103980140559155831, 1.561224650464939190 ) ) ;
#155338=CARTESIAN_POINT ( 'NONE',  ( 0.6048602812970468312, -0.7454967350204609877, -2.077179305122120123 ) ) ;
#155341=CARTESIAN_POINT ( 'NONE',  ( 6.006499477249034769, -2.003593090125683762, -0.1951834861853833925 ) ) ;
#155344=CARTESIAN_POINT ( 'NONE',  ( 5.753138727196851043, 0.1435251449807967150, -2.011451301405759118 ) ) ;
#155345=CARTESIAN_POINT ( 'NONE',  ( 1.891162872569674080, 0.2007839719405466183, 2.060584128686280714 ) ) ;
#155348=CARTESIAN_POINT ( 'NONE',  ( 0.5851287433712646369, -0.2658872486876809327, -2.145209338178376335 ) ) ;
#155354=CARTESIAN_POINT ( 'NONE',  ( 4.553154410594215662, -1.128159591824983377, 1.317121951208845454 ) ) ;
#155356=CARTESIAN_POINT ( 'NONE',  ( 2.518496159030516601, 0.8812310945605882351, 1.873447404777649261 ) ) ;
#155357=CARTESIAN_POINT ( 'NONE',  ( 4.728176305778284849, 2.111628383735635328, 0.1544883665849701437 ) ) ;
#155360=CARTESIAN_POINT ( 'NONE',  ( 2.114047118560181016, 1.964524245714272643, -0.1396653253868378186 ) ) ;
#155363=CARTESIAN_POINT ( 'NONE',  ( 4.330218815260163723, 2.247629863848239040, 0.4493651543184833397 ) ) ;
#155364=CARTESIAN_POINT ( 'NONE',  ( 1.629252094361890890, -1.719607636260962025, 0.6136192449261099746 ) ) ;
#155368=CARTESIAN_POINT ( 'NONE',  ( 2.619392002094393490, 1.702953528017937090, 1.073460467912157101 ) ) ;
#155369=CARTESIAN_POINT ( 'NONE',  ( 3.713678095275750657, 0.4809820416172749802, -1.901733992618503066 ) ) ;
#155373=CARTESIAN_POINT ( 'NONE',  ( 6.404249610866886044, 1.549990571320001731, -1.403138301853884773 ) ) ;
#155374=CARTESIAN_POINT ( 'NONE',  ( 4.258513496744737559, -1.310932089386746879, 1.189237179687177015 ) ) ;
#155376=CARTESIAN_POINT ( 'NONE',  ( 0.8498829323080080433, 2.188760582993890313, -0.1110106097068005726 ) ) ;
#155377=CARTESIAN_POINT ( 'NONE',  ( 5.876847675788273939, 1.605460876287589045, -0.6722632963065499068 ) ) ;
#155381=CARTESIAN_POINT ( 'NONE',  ( 6.135373049470649320, 0.7166818055565070678, 2.184152129457237912 ) ) ;
#155383=CARTESIAN_POINT ( 'NONE',  ( 5.501237755103592697, 1.708535605516453115, 0.2940088878824585472 ) ) ;
#155384=CARTESIAN_POINT ( 'NONE',  ( 2.350463684150871035, 2.206416367115513477, 0.05273732197710182673 ) ) ;
#155386=CARTESIAN_POINT ( 'NONE',  ( 5.406739488685087025, 0.6250254011054052761, 2.079287783280135304 ) ) ;
#155388=CARTESIAN_POINT ( 'NONE',  ( 0.6732554233833996093, 1.864234297354839143, -1.003953180072956419 ) ) ;
#155389=CARTESIAN_POINT ( 'NONE',  ( 4.187500000000002665, -1.451031289060945584, 1.451031289061284646 ) ) ;
#155391=CARTESIAN_POINT ( 'NONE',  ( 4.594702886556338406, -0.4214696541114425488, -1.879573207023744974 ) ) ;
#155392=CARTESIAN_POINT ( 'NONE',  ( 1.541950133533489975, -2.090104109921666620, 0.7524221467923494222 ) ) ;
#155398=CARTESIAN_POINT ( 'NONE',  ( 3.510577332121900707, -2.218788133798971884, -0.1078075537720973032 ) ) ;
#155404=CARTESIAN_POINT ( 'NONE',  ( 1.969375177810539945, -1.978050944945686673, -0.3905967402937361443 ) ) ;
#155406=CARTESIAN_POINT ( 'NONE',  ( 6.162562474744170515, -0.7388518307863629619, -1.925989236560563977 ) ) ;
#155409=CARTESIAN_POINT ( 'NONE',  ( 6.614805129994690169, -0.1227637983064084892, 1.711830280531308812 ) ) ;
#155412=CARTESIAN_POINT ( 'NONE',  ( 1.897346677678591442, -0.6019946308016431713, 1.664328231202655273 ) ) ;
#155413=CARTESIAN_POINT ( 'NONE',  ( 0.5807041986926939625, -0.7231374404764076003, 1.882475062126743204 ) ) ;
#155414=CARTESIAN_POINT ( 'NONE',  ( 6.321804186586025942, 0.9940233051523542640, -1.428469917405380318 ) ) ;
#155415=CARTESIAN_POINT ( 'NONE',  ( 4.335649905164426166, 0.9806507323757740480, -2.072138663387664614 ) ) ;
#155416=CARTESIAN_POINT ( 'NONE',  ( 3.415785861374909249, 1.167101634185686576, -1.423959568491977912 ) ) ;
#155419=CARTESIAN_POINT ( 'NONE',  ( 3.117977517195897441, -0.8984765085307615529, -1.589086709143338272 ) ) ;
#155420=CARTESIAN_POINT ( 'NONE',  ( 3.621720349255663773, 0.2986264320336135536, 1.994071497604548382 ) ) ;
#155422=CARTESIAN_POINT ( 'NONE',  ( 3.696369045748033155, -2.259781416529721643, -0.1137371904085457408 ) ) ;
#155424=CARTESIAN_POINT ( 'NONE',  ( 5.210040546657988436, -2.096114648464560748, 0.2032773619186321323 ) ) ;
#155426=CARTESIAN_POINT ( 'NONE',  ( 3.543477799061961253, 1.872898848466747479, -0.8826743078152868849 ) ) ;
#155429=CARTESIAN_POINT ( 'NONE',  ( 6.006510593949522026, -2.110231943656666331, -0.2080817731764383061 ) ) ;
#155431=CARTESIAN_POINT ( 'NONE',  ( 0.7680398806059639538, 0.9487340639210088966, 1.676631345724951982 ) ) ;
#155439=CARTESIAN_POINT ( 'NONE',  ( 0.6861347341944658007, 2.138861475627896080, -0.5996866306409093239 ) ) ;
#155440=CARTESIAN_POINT ( 'NONE',  ( 2.696425475562960195, -2.100245048574858497, -0.1560501473716560672 ) ) ;
#155443=CARTESIAN_POINT ( 'NONE',  ( 6.754761327113334879, -0.4959639348531270642, -1.793591138363290316 ) ) ;
#155449=CARTESIAN_POINT ( 'NONE',  ( 0.5805319366703353134, 1.050441701016215923, 1.842106252469346117 ) ) ;
#155452=CARTESIAN_POINT ( 'NONE',  ( 3.033595934319989418, 1.863777508880835487, -0.6128360024686765328 ) ) ;
#155453=CARTESIAN_POINT ( 'NONE',  ( 2.044033295145482043, 0.8276103948961744949, -1.997198329219296742 ) ) ;
#155454=CARTESIAN_POINT ( 'NONE',  ( 1.048114208743459619, -1.451426956872736262, 1.132798186660122441 ) ) ;
#155458=CARTESIAN_POINT ( 'NONE',  ( 3.784860527941535491, 1.262060850391345523, 1.198560274591720098 ) ) ;
#155461=CARTESIAN_POINT ( 'NONE',  ( 0.4620835240300471547, 2.137967531602209981, -0.3185850937674692407 ) ) ;
#155463=CARTESIAN_POINT ( 'NONE',  ( 2.548203688163702463, 1.844428314090811538, -0.8144999995377337765 ) ) ;
#155465=CARTESIAN_POINT ( 'NONE',  ( 2.553542074257345362, 0.5272840835596946940, -1.899572117879143596 ) ) ;
#155467=CARTESIAN_POINT ( 'NONE',  ( 6.509000000000012776, 0.5843741663743782233, 2.053293374786519188 ) ) ;
#155472=CARTESIAN_POINT ( 'NONE',  ( -0.1110810684433168327, 2.049790377237853178, -2.213868588080004418 ) ) ;
#155478=CARTESIAN_POINT ( 'NONE',  ( 5.350698970897345141, 0.6634653876971875475, 2.210164229930264845 ) ) ;
#155479=CARTESIAN_POINT ( 'NONE',  ( 6.672321430365630412, -0.9237476215336395402, -1.730755693189582667 ) ) ;
#155480=CARTESIAN_POINT ( 'NONE',  ( 3.608209768781400761, 1.961936380018937331, 0.004537341891153179319 ) ) ;
#155482=CARTESIAN_POINT ( 'NONE',  ( 0.5279704824466545654, -1.728000714500482982, 1.038995864524896895 ) ) ;
#155484=CARTESIAN_POINT ( 'NONE',  ( 2.395853177668628931, -2.093565527891564582, 0.3158384217898829727 ) ) ;
#155488=CARTESIAN_POINT ( 'NONE',  ( 3.697050842446505392, -0.5329721798031424873, 1.762307204009383454 ) ) ;
#155492=CARTESIAN_POINT ( 'NONE',  ( 3.603867943843573673, 1.538443694073919898, 1.459757404076333698 ) ) ;
#155493=CARTESIAN_POINT ( 'NONE',  ( 0.05820987927622478519, -1.643049995186950829, -0.8308948761173093889 ) ) ;
#155497=CARTESIAN_POINT ( 'NONE',  ( 4.042301887969748542, 2.050516515953205055, 0.2056252831919377910 ) ) ;
#155500=CARTESIAN_POINT ( 'NONE',  ( 1.557894219809667247, -1.301531972126177772, 1.302644501960325885 ) ) ;
#155506=CARTESIAN_POINT ( 'NONE',  ( 0.7509353727821498348, 0.6442623716619542140, 2.110749664216593047 ) ) ;
#155507=CARTESIAN_POINT ( 'NONE',  ( 3.515140014801207524, 2.043520737213794458, 0.9711500472536734874 ) ) ;
#155509=CARTESIAN_POINT ( 'NONE',  ( 3.533306822026711647, -0.1277962806783480842, 1.807111865170844656 ) ) ;
#155511=CARTESIAN_POINT ( 'NONE',  ( 3.749167220118687638, 0.2288279286139145163, -1.901904479094515210 ) ) ;
#155512=CARTESIAN_POINT ( 'NONE',  ( 5.301260566756325510, -1.777534899005998481, 1.061244097098137606 ) ) ;
#155514=CARTESIAN_POINT ( 'NONE',  ( 2.799638878761875116, -0.6198165829789729075, 1.871555056500016745 ) ) ;
#155515=CARTESIAN_POINT ( 'NONE',  ( 0.8856179577424825311, 1.291390466942985649, 1.429610664621896898 ) ) ;
#155516=CARTESIAN_POINT ( 'NONE',  ( 3.819104250046548632, -0.1383300533824398659, 1.865606469731183825 ) ) ;
#155518=CARTESIAN_POINT ( 'NONE',  ( 3.475486094516122115, 0.05728489528775136674, -2.307140494302026390 ) ) ;
#155519=CARTESIAN_POINT ( 'NONE',  ( 3.894834723524211118, 0.2711828204805393772, 1.841042229387960472 ) ) ;
#155524=CARTESIAN_POINT ( 'NONE',  ( 0.9792911203426227784, -0.05348914117170092131, -2.105562491362684252 ) ) ;
#155530=CARTESIAN_POINT ( 'NONE',  ( 1.758217466200185042, 0.8068918862002281145, -1.961288232260410380 ) ) ;
#155532=CARTESIAN_POINT ( 'NONE',  ( 1.002220075199202309, -0.9041908160717628817, 1.806139134770538002 ) ) ;
#155535=EDGE_CURVE ( 'NONE', #70481, #176125, #89756, .T. ) ;
#155538=CARTESIAN_POINT ( 'NONE',  ( 0.6499751493908960676, 0.6786997614584532323, -2.052318101833712660 ) ) ;
#155539=CARTESIAN_POINT ( 'NONE',  ( 6.610000000000006537, 2.052567036419289614, 2.306714106643445561 ) ) ;
#155541=CARTESIAN_POINT ( 'NONE',  ( 6.825078400183573812, 0.002648415797040087893, 1.855566311045192540 ) ) ;
#155544=CARTESIAN_POINT ( 'NONE',  ( 5.419157771004846857, -1.820987890746316173, 0.8666037247077316152 ) ) ;
#155546=CARTESIAN_POINT ( 'NONE',  ( -0.005964567173097347699, -2.191213315851054944, -0.04726126812268362232 ) ) ;
#155548=CARTESIAN_POINT ( 'NONE',  ( 0.8137758769373629741, -0.3292158159766758185, 2.238336236828967429 ) ) ;
#155552=CARTESIAN_POINT ( 'NONE',  ( 1.018978518071847583, -1.731272710380473923, 0.8202338080745846804 ) ) ;
#155556=CARTESIAN_POINT ( 'NONE',  ( 2.420142186669431705, 1.127438667474765621, -1.305497878543178336 ) ) ;
#155558=CARTESIAN_POINT ( 'NONE',  ( 1.668863397688532091, 0.1364744985549205814, -1.764554890378322805 ) ) ;
#155559=CARTESIAN_POINT ( 'NONE',  ( 1.858066033337543832, 0.7684160352657551929, -1.860855044080988785 ) ) ;
#155560=CARTESIAN_POINT ( 'NONE',  ( 4.454274341225270994, 2.206355006892012138, -0.05062909709598743119 ) ) ;
#155562=CARTESIAN_POINT ( 'NONE',  ( 3.990493710177836828, -1.159536886187025440, 1.653596977174769833 ) ) ;
#155564=CARTESIAN_POINT ( 'NONE',  ( 4.108145954595856075, -0.8103754143699601897, 1.959725966023172727 ) ) ;
#155565=CARTESIAN_POINT ( 'NONE',  ( 3.620720401301917857, 0.2986476686686300175, 1.994069442355271615 ) ) ;
#155566=CARTESIAN_POINT ( 'NONE',  ( 3.972783152890049241, -1.338232477621086547, 1.221218810135711541 ) ) ;
#155569=ORIENTED_EDGE ( 'NONE', *, *, #15404, .T. ) ;
#155570=CARTESIAN_POINT ( 'NONE',  ( 1.586564105604048480, -0.2713065988851799393, -1.850747533123621391 ) ) ;
#155581=CARTESIAN_POINT ( 'NONE',  ( 4.605793411009856619, 1.573235607984494688, 1.422142093439874522 ) ) ;
#155583=CARTESIAN_POINT ( 'NONE',  ( 5.237557467868056094, -1.392094792763297617, -1.396070155715684269 ) ) ;
#155585=CARTESIAN_POINT ( 'NONE',  ( 0.8615886222705991804, -1.589730513765170938, -1.235154978249096036 ) ) ;
#155587=CARTESIAN_POINT ( 'NONE',  ( 6.262923198102183342, -0.1061305018058098515, -2.114825283700927372 ) ) ;
#155589=CARTESIAN_POINT ( 'NONE',  ( 2.084514231050747401, 1.193861083872927109, -1.691280048542340708 ) ) ;
#155592=CARTESIAN_POINT ( 'NONE',  ( 3.152369405254138446, -1.582674238129866184, 1.366072548952133259 ) ) ;
#155595=CARTESIAN_POINT ( 'NONE',  ( 2.625780896952558674, -1.049238153381076177, -1.493741879923994542 ) ) ;
#155596=CARTESIAN_POINT ( 'NONE',  ( 1.928074960669722504, -0.8543848903827315766, -1.597334059258429972 ) ) ;
#155598=CARTESIAN_POINT ( 'NONE',  ( 5.760442859251142522, 0.8911043219209063837, 2.019162844794204048 ) ) ;
#155600=CARTESIAN_POINT ( 'NONE',  ( 4.630015379333586978, -1.354682855507854278, -1.741961856448564161 ) ) ;
#155603=CARTESIAN_POINT ( 'NONE',  ( 3.281800106729782840, 1.865104756965057620, -0.4213900744019505318 ) ) ;
#155606=CARTESIAN_POINT ( 'NONE',  ( 6.566853775770633561, 1.536883091774071453, -1.387433097640700774 ) ) ;
#155608=CARTESIAN_POINT ( 'NONE',  ( 5.689076433642084041, 1.658752129386225516, 1.432425853890168188 ) ) ;
#155618=CARTESIAN_POINT ( 'NONE',  ( 5.330949937734919430, -1.947458545883517189, -0.7027056652011903770 ) ) ;
#155619=CARTESIAN_POINT ( 'NONE',  ( 3.967344596728016093, 0.2348649212099394590, -1.912067515532820838 ) ) ;
#155620=CARTESIAN_POINT ( 'NONE',  ( 1.388296234047466049, -0.7283980888908546669, -1.880428666220852696 ) ) ;
#155624=CARTESIAN_POINT ( 'NONE',  ( 1.025618320672251560, -1.392776288830662512, -1.691927514038966907 ) ) ;
#155625=CARTESIAN_POINT ( 'NONE',  ( 5.303274670167754223, 1.494737065598228165, 1.048009559513597866 ) ) ;
#155632=CARTESIAN_POINT ( 'NONE',  ( 2.401689157922583640, -0.7064633820979376866, -1.700523668893457296 ) ) ;
#155633=CARTESIAN_POINT ( 'NONE',  ( 0.08268127059449237315, -1.313209137626596634, 1.525886470183013044 ) ) ;
#155634=CARTESIAN_POINT ( 'NONE',  ( 2.267358445155386981, -2.297842707097216053, 0.05573287391750710029 ) ) ;
#155635=CARTESIAN_POINT ( 'NONE',  ( 6.789906393989944888, -1.279003670332454989, -1.487618534420580119 ) ) ;
#155638=CARTESIAN_POINT ( 'NONE',  ( 3.058751851047710080, 0.4689117840017149041, 1.853869267190631831 ) ) ;
#155640=CARTESIAN_POINT ( 'NONE',  ( 0.9771079587245214970, 1.912259438035465386, 0.7939916666956441382 ) ) ;
#155642=CARTESIAN_POINT ( 'NONE',  ( 2.085595224044423102, -0.8910886986466991511, 1.891471387866516585 ) ) ;
#155643=CARTESIAN_POINT ( 'NONE',  ( 1.024039198018782626, 1.117340804906666873, -1.500143343703803422 ) ) ;
#155644=CARTESIAN_POINT ( 'NONE',  ( 1.932970024460831882, 1.034005469613193062, 1.730602090182407959 ) ) ;
#155648=CARTESIAN_POINT ( 'NONE',  ( 2.243362625160577384, 1.740107689937436808, 0.04144568419049177860 ) ) ;
#155653=CARTESIAN_POINT ( 'NONE',  ( 2.771755371404661439, 0.9226176164769549493, 1.457180633135872094 ) ) ;
#155654=CARTESIAN_POINT ( 'NONE',  ( 2.718528139169604341, 2.064530135181973591, 0.7356957861901700646 ) ) ;
#155655=CARTESIAN_POINT ( 'NONE',  ( 5.180388087185870738, -1.228261608319089149, 1.833297759731546073 ) ) ;
#155657=CARTESIAN_POINT ( 'NONE',  ( 2.079201016916156330, 2.024566655493876155, 0.7844037353602287821 ) ) ;
#155658=CARTESIAN_POINT ( 'NONE',  ( 2.103868193876055503, -1.825329726703457833, 0.04394198290156441783 ) ) ;
#155660=CARTESIAN_POINT ( 'NONE',  ( 5.050072346573388771, 1.046394516673061270, 1.840669678815173960 ) ) ;
#155661=CARTESIAN_POINT ( 'NONE',  ( 6.639320575229294086, 0.5800432152290584398, 2.049144803211971233 ) ) ;
#155663=CARTESIAN_POINT ( 'NONE',  ( 5.337530604160453329, 0.9314408107504292822, -2.094771667654048208 ) ) ;
#155667=CARTESIAN_POINT ( 'NONE',  ( 0.4520119014386895229, -1.502510013782244025, -1.496567369470555020 ) ) ;
#155675=CARTESIAN_POINT ( 'NONE',  ( 5.485000066852382616, -2.016597020608828839, 0.002808655738886777897 ) ) ;
#155677=CARTESIAN_POINT ( 'NONE',  ( 2.993094585481168579, 0.2480512885563341541, 2.047511573040517341 ) ) ;
#155679=CARTESIAN_POINT ( 'NONE',  ( -0.1408020194049965368, 5.721120576699901150, -2.694324532632543345 ) ) ;
#155683=CARTESIAN_POINT ( 'NONE',  ( 5.982419568921026887, -0.3181065885738461607, -2.168126298386578110 ) ) ;
#155684=CARTESIAN_POINT ( 'NONE',  ( 3.973279856364997809, -1.994869694282218386, -0.2930714778977619450 ) ) ;
#155685=CARTESIAN_POINT ( 'NONE',  ( 3.438839575862782549, -1.396446551253815782, -1.200180114512699792 ) ) ;
#155687=CARTESIAN_POINT ( 'NONE',  ( 6.405291383686446238, 1.519602032305459538, 1.011395407323860907 ) ) ;
#155690=CARTESIAN_POINT ( 'NONE',  ( 6.754744673581316583, -1.754229693457433736, 1.428470910521584036 ) ) ;
#155691=CARTESIAN_POINT ( 'NONE',  ( 2.367922061077184726, 2.065251240347278472, -0.4117205849265455075 ) ) ;
#155701=CARTESIAN_POINT ( 'NONE',  ( 2.267978396857213585, 0.5610993688725562922, -2.044979925899123252 ) ) ;
#155702=CARTESIAN_POINT ( 'NONE',  ( 3.885193193976806292, -2.073655658835142024, -0.7971110592776513570 ) ) ;
#155703=CARTESIAN_POINT ( 'NONE',  ( 2.115410589380119610, -2.125216164159982046, 0.5342070311455533460 ) ) ;
#155705=CARTESIAN_POINT ( 'NONE',  ( 6.883263157960391787, -0.001104538646235289417, 1.946037152736757925 ) ) ;
#155707=CARTESIAN_POINT ( 'NONE',  ( 5.723093114104088386, -1.772945450647535948, -0.8403097561825512152 ) ) ;
#155710=CARTESIAN_POINT ( 'NONE',  ( 6.610000000000030518, 1.266345627986571021, 2.115470293623383569 ) ) ;
#155712=CARTESIAN_POINT ( 'NONE',  ( 3.621431001533811589, 1.820626359085864454, 1.087046460333654485 ) ) ;
#155714=CARTESIAN_POINT ( 'NONE',  ( 5.664953204072169513, -1.952404353424816774, -0.9282482345986733385 ) ) ;
#155716=CARTESIAN_POINT ( 'NONE',  ( 5.565905774130330386, -1.163279849954502287, 1.427249551226833502 ) ) ;
#155719=CARTESIAN_POINT ( 'NONE',  ( 0.04591871184063747030, -1.399829139283098822, 1.033961902999945170 ) ) ;
#155720=CARTESIAN_POINT ( 'NONE',  ( 6.827182134110227452, 2.468179810210658687, 2.195371296381436022 ) ) ;
#155724=CARTESIAN_POINT ( 'NONE',  ( 4.311504812833309330, -0.3723461477018601973, 2.129241309423899775 ) ) ;
#155726=CARTESIAN_POINT ( 'NONE',  ( 0.3504316985127345907, -0.8248687954017698276, 1.525068808560197109 ) ) ;
#155728=CARTESIAN_POINT ( 'NONE',  ( 3.731458613173586514, -1.998165266068991253, 0.8252760040215676440 ) ) ;
#155729=CARTESIAN_POINT ( 'NONE',  ( 4.815676612163926507, -1.933897303736350270, 0.3816649536505806184 ) ) ;
#155730=CARTESIAN_POINT ( 'NONE',  ( 3.743219424636199832, -1.670416500854546626, -0.4642454339297346078 ) ) ;
#155731=CARTESIAN_POINT ( 'NONE',  ( 1.365048776756357940, 0.1565470504056795942, -2.186014887712848243 ) ) ;
#155732=CARTESIAN_POINT ( 'NONE',  ( 1.396046310939329738, 1.748920304266964543, 1.505474166573782968 ) ) ;
#155733=CARTESIAN_POINT ( 'NONE',  ( 3.198563317047153465, -0.5950029230564283234, -1.973035911149529698 ) ) ;
#155734=CARTESIAN_POINT ( 'NONE',  ( 5.513211315966105808, -1.893842782867664054, 0.4293952855863486517 ) ) ;
#155742=CARTESIAN_POINT ( 'NONE',  ( 2.696532018272995490, -2.200798769047443759, -0.1632673417703081331 ) ) ;
#155745=CARTESIAN_POINT ( 'NONE',  ( 1.076741303291447460, 1.716668495539741324, 0.7189669686299257068 ) ) ;
#155746=CARTESIAN_POINT ( 'NONE',  ( -0.02900071798685177615, 6.946858727649162901, -2.768864135414349281 ) ) ;
#155752=ORIENTED_EDGE ( 'NONE', *, *, #17772, .T. ) ;
#155753=CARTESIAN_POINT ( 'NONE',  ( 2.729428266803469061, -1.923432490405907247, 0.7405405203823824944 ) ) ;
#155759=CARTESIAN_POINT ( 'NONE',  ( 1.147419824990800752, -1.624031055642958243, -1.268641727334917313 ) ) ;
#155762=CARTESIAN_POINT ( 'NONE',  ( 4.968220237687512864, -1.735557695065930606, -0.6152675618510683453 ) ) ;
#155766=CARTESIAN_POINT ( 'NONE',  ( 4.512475528931441104, -0.9420208833846724916, -1.995868093903986118 ) ) ;
#155767=CARTESIAN_POINT ( 'NONE',  ( 6.749321564901560322, -1.811022791033944257, -1.355814775124731808 ) ) ;
#155769=CARTESIAN_POINT ( 'NONE',  ( -0.03509584499547176162, -1.534781374734139670, 1.140672443274578729 ) ) ;
#155770=CARTESIAN_POINT ( 'NONE',  ( 1.288296401830712368, -0.7303101666344159471, -1.879802715551846859 ) ) ;
#155772=CARTESIAN_POINT ( 'NONE',  ( 1.652187889876779892, -0.3379717360396676806, -2.273286007567467237 ) ) ;
#155774=CARTESIAN_POINT ( 'NONE',  ( 6.604189988765333474, -0.8127675640051763573, 1.729262449380222444 ) ) ;
#155776=CARTESIAN_POINT ( 'NONE',  ( 1.955717210371358483, 1.865846021326333926, -0.1348392221205765851 ) ) ;
#155777=CARTESIAN_POINT ( 'NONE',  ( 2.589077643123653072, 1.706113014995232380, 1.074661422923957055 ) ) ;
#155781=CARTESIAN_POINT ( 'NONE',  ( 3.668672709498523865, -1.414518211590541252, 1.560516469030509334 ) ) ;
#155782=EDGE_CURVE ( 'NONE', #60268, #89693, #53663, .T. ) ;
#155786=CARTESIAN_POINT ( 'NONE',  ( 3.885024839820313325, -1.886105071096555230, -0.7231171000243222791 ) ) ;
#155789=CARTESIAN_POINT ( 'NONE',  ( 6.865701141133224716, -0.4594653659172152071, 2.018469443450424894 ) ) ;
#155791=CARTESIAN_POINT ( 'NONE',  ( 4.780646861661003832, -2.095393720161139228, -0.5303334973314683953 ) ) ;
#155797=CARTESIAN_POINT ( 'NONE',  ( 2.102231420249685456, 0.8322404413585123839, -2.005527090382641653 ) ) ;
#155800=CARTESIAN_POINT ( 'NONE',  ( 1.645803748337611783, 0.5784278848013635344, 1.748079663633335334 ) ) ;
#155803=CARTESIAN_POINT ( 'NONE',  ( 3.070069520051089906, -1.303570237086741024, 1.761582097007891923 ) ) ;
#155805=CARTESIAN_POINT ( 'NONE',  ( 3.661208364039827856, -1.994111792441630726, -1.068896079077549910 ) ) ;
#155811=CARTESIAN_POINT ( 'NONE',  ( 5.026482010321593030, 1.693441115147217291, 0.5138918105389718161 ) ) ;
#155813=CARTESIAN_POINT ( 'NONE',  ( 2.309725134170067307, -0.4624151122551781179, 2.054391039957529586 ) ) ;
#155816=CARTESIAN_POINT ( 'NONE',  ( 1.152721088564850671, -0.4753370964276568134, -1.911210599630641882 ) ) ;
#155819=CARTESIAN_POINT ( 'NONE',  ( 5.502179438505619302, -0.8068474266363240277, 1.622048611428918319 ) ) ;
#155822=CARTESIAN_POINT ( 'NONE',  ( 4.733189744967194024, -1.710186631362722309, 0.7584244158565583982 ) ) ;
#155825=CARTESIAN_POINT ( 'NONE',  ( 4.416890754593222113, -1.537527071031305814, 1.386575359339572877 ) ) ;
#155835=CARTESIAN_POINT ( 'NONE',  ( 3.420314466093795414, 0.8798059112791326575, 1.753580237611163994 ) ) ;
#155837=CARTESIAN_POINT ( 'NONE',  ( 2.056017322730230301, 1.755501262438976751, -0.9912458455646618871 ) ) ;
#155841=CARTESIAN_POINT ( 'NONE',  ( 1.950266909631480861, 0.5821006739541793040, 1.777759251391328732 ) ) ;
#155845=CARTESIAN_POINT ( 'NONE',  ( 3.796581652666820350, 1.495729193744433028, -1.498731062137735437 ) ) ;
#155846=CARTESIAN_POINT ( 'NONE',  ( 5.107906530550561541, 0.6527686194882609261, -1.964817160181751010 ) ) ;
#155848=CARTESIAN_POINT ( 'NONE',  ( 1.118821681092090126, -0.04763362108583040627, 2.090370170816723494 ) ) ;
#155849=CARTESIAN_POINT ( 'NONE',  ( 6.720655732516647163, -0.007268404184145297979, 2.273772995263834140 ) ) ;
#155850=CARTESIAN_POINT ( 'NONE',  ( 6.370122744524995717, 0.9412729668686821149, 1.564051812004362940 ) ) ;
#155859=CARTESIAN_POINT ( 'NONE',  ( 6.024064539286675846, -1.897261554996135802, 0.2387622092476364699 ) ) ;
#155867=CARTESIAN_POINT ( 'NONE',  ( 6.485953897545715385, -2.015913262743720402, 0.05231248585663844652 ) ) ;
#155870=CARTESIAN_POINT ( 'NONE',  ( 0.1399997263886003374, 7.629137130509076492, -2.599723212958489516 ) ) ;
#155874=CARTESIAN_POINT ( 'NONE',  ( 2.817198160248539196, -1.711224680871022086, -0.9748066430285988737 ) ) ;
#155875=CARTESIAN_POINT ( 'NONE',  ( 4.007435537932837910, -1.928747227692016564, 0.5880391185724976877 ) ) ;
#155878=CARTESIAN_POINT ( 'NONE',  ( 5.191441776010862874, -0.7909675746368143301, 2.043907961996515699 ) ) ;
#155880=CARTESIAN_POINT ( 'NONE',  ( 3.118101180835719521, -0.9482820236139007930, -1.676744857821835355 ) ) ;
#155882=CARTESIAN_POINT ( 'NONE',  ( -0.1298852118744100725, 6.948705093303869873, -2.321530996463050389 ) ) ;
#155883=CARTESIAN_POINT ( 'NONE',  ( 0.1331565106231571705, 4.092041177288479048, -2.500854978060399691 ) ) ;
#155890=CARTESIAN_POINT ( 'NONE',  ( 5.776868925826902590, 1.698781319366513998, -0.7106697882480541573 ) ) ;
#155891=CARTESIAN_POINT ( 'NONE',  ( 3.000642180831034622, -1.983674057915509881, -0.3420062109290455954 ) ) ;
#155892=CARTESIAN_POINT ( 'NONE',  ( 4.851052417537679240, -1.089491736270932432, 2.023782222440795753 ) ) ;
#155893=FACE_OUTER_BOUND ( 'NONE', #150756, .T. ) ;
#155894=CARTESIAN_POINT ( 'NONE',  ( 2.922522432510234136, -1.287038294151692241, 1.344341647096161996 ) ) ;
#155900=CARTESIAN_POINT ( 'NONE',  ( 6.550343146927733784, -1.615745695573450824, 1.326605865911892002 ) ) ;
#155906=CARTESIAN_POINT ( 'NONE',  ( 6.129511981615775262, -1.621618681806114459, 0.5882815792577487102 ) ) ;
#155908=CARTESIAN_POINT ( 'NONE',  ( 1.353744004007218615, 0.1277301157788513497, -1.729473920685227428 ) ) ;
#155913=CARTESIAN_POINT ( 'NONE',  ( 0.3564121386029559524, -2.069725681613205470, -0.05427943458365809548 ) ) ;
#155914=CARTESIAN_POINT ( 'NONE',  ( 5.637271085457097541, -1.648663388651723460, 0.7845467231081537651 ) ) ;
#155915=CARTESIAN_POINT ( 'NONE',  ( 3.801568999928582659, -1.482573837031101016, -1.284759613706359271 ) ) ;
#155920=CARTESIAN_POINT ( 'NONE',  ( 3.668700845920089826, 0.7647225481513253431, 1.977962425194310203 ) ) ;
#155924=CARTESIAN_POINT ( 'NONE',  ( 1.674760025662187735, 1.393346669028448392, -1.531324272915953744 ) ) ;
#155927=CARTESIAN_POINT ( 'NONE',  ( 3.370003599138057471, 0.5381768412672756074, -2.155016279732512974 ) ) ;
#155929=CARTESIAN_POINT ( 'NONE',  ( 1.811588643561705680, 1.319210623403826110, -1.882327697243087350 ) ) ;
#155931=CARTESIAN_POINT ( 'NONE',  ( 6.649293052619501765, 1.797374026962361482, -1.011582863395175114 ) ) ;
#155935=CARTESIAN_POINT ( 'NONE',  ( 6.128435733830499998, 0.1874100934057248424, 1.831705376836203936 ) ) ;
#155937=CARTESIAN_POINT ( 'NONE',  ( 3.129067941553372645, 1.730785544086024696, 0.8136490247460312908 ) ) ;
#155938=CARTESIAN_POINT ( 'NONE',  ( -0.2102771530458276972, 0.6786276403282426317, -2.283427277113641019 ) ) ;
#155939=CARTESIAN_POINT ( 'NONE',  ( 4.032037319687285404, 0.9221689259152658913, -1.457338292308225869 ) ) ;
#155940=CARTESIAN_POINT ( 'NONE',  ( 2.096888995370162156, 1.803417055948232983, 0.9023429676050932491 ) ) ;
#155941=CARTESIAN_POINT ( 'NONE',  ( 3.885566394551481562, -0.7213347477983514944, -2.182621754721993490 ) ) ;
#155942=CARTESIAN_POINT ( 'NONE',  ( 3.146068640573984165, 0.8174054641026907708, -2.109740015476600838 ) ) ;
#155943=CARTESIAN_POINT ( 'NONE',  ( 5.162764661449575243, -1.526107291725445236, 1.451632374922463553 ) ) ;
#155946=CARTESIAN_POINT ( 'NONE',  ( 4.762845401903825326, -1.580659612885275012, -0.7961057336023872333 ) ) ;
#155948=CARTESIAN_POINT ( 'NONE',  ( 1.201600019185744994, -0.5526092242729553350, 2.224544611104557035 ) ) ;
#155949=CARTESIAN_POINT ( 'NONE',  ( 5.718664505737725001, -0.04093049815006092468, 1.840854889930729765 ) ) ;
#155952=CARTESIAN_POINT ( 'NONE',  ( 5.912113082354765403, 1.474260358680115290, -1.621598248542432064 ) ) ;
#155955=CARTESIAN_POINT ( 'NONE',  ( 5.916483165358986440, 0.8355632440216669288, 1.894440869009452300 ) ) ;
#155956=CARTESIAN_POINT ( 'NONE',  ( 0.2687680251878405424, -0.2516378192510167477, -2.000730910237565663 ) ) ;
#155958=CARTESIAN_POINT ( 'NONE',  ( 4.723225685987796574, -0.09301374627979085152, 1.924373785979951013 ) ) ;
#155961=CARTESIAN_POINT ( 'NONE',  ( 1.389269710167878369, -2.111442789942123088, -0.6905784607170639688 ) ) ;
#155971=CARTESIAN_POINT ( 'NONE',  ( 1.223018651738450480, -1.772137153356953432, -0.8420139538000551704 ) ) ;
#155973=CARTESIAN_POINT ( 'NONE',  ( 6.144970055084349347, -0.2864424343173576082, -1.940704187532462210 ) ) ;
#155976=CARTESIAN_POINT ( 'NONE',  ( 0.3392369075362114961, 0.3904986559340599128, 2.228413801644222758 ) ) ;
#155980=CARTESIAN_POINT ( 'NONE',  ( 0.9306671693925671063, 0.1315677519515070781, 1.865966016356377821 ) ) ;
#155981=CARTESIAN_POINT ( 'NONE',  ( 0.5801786448705691379, -0.6264061342569470225, 1.617264071341844245 ) ) ;
#155983=CARTESIAN_POINT ( 'NONE',  ( 3.984055765753656164, -2.167877601896048390, -0.3204034371554059235 ) ) ;
#155984=CARTESIAN_POINT ( 'NONE',  ( 3.979734726549417623, 2.174020839304124042, -0.7740601867209749853 ) ) ;
#155985=CARTESIAN_POINT ( 'NONE',  ( 6.925078400183531713, -0.004750840071900476122, 2.044148492825672569 ) ) ;
#155986=CARTESIAN_POINT ( 'NONE',  ( 2.431497994139957264, 0.9153433635570235039, -1.712687122320022626 ) ) ;
#155990=CARTESIAN_POINT ( 'NONE',  ( 5.467072749063267345, -1.670387955228332277, 1.306269166133757986 ) ) ;
#155992=CARTESIAN_POINT ( 'NONE',  ( 3.498672800139957406, -1.986100699840901651, 0.3474671148789992836 ) ) ;
#155996=CARTESIAN_POINT ( 'NONE',  ( 0.5041868517345666767, -0.6120625888205477594, -1.720162557568189809 ) ) ;
#156001=CARTESIAN_POINT ( 'NONE',  ( 5.735248378139378822, -1.864208485850331609, 0.8789154904798938128 ) ) ;
#156006=CARTESIAN_POINT ( 'NONE',  ( 4.951822102061871789, -1.429791030739693047, -1.426725901824247078 ) ) ;
#156007=CARTESIAN_POINT ( 'NONE',  ( 5.531947820799793192, -2.167606221786242848, 0.4847573843902542312 ) ) ;
#156012=CARTESIAN_POINT ( 'NONE',  ( 4.680574674004650326, -1.998471466470305602, -0.5028169189831372954 ) ) ;
#156013=CARTESIAN_POINT ( 'NONE',  ( 3.955704058034177351, -1.882473782773282700, -0.7231407674024927790 ) ) ;
#156020=CARTESIAN_POINT ( 'NONE',  ( 3.708361104356564297, -1.524809962200252444, -1.319026932540816599 ) ) ;
#156021=CARTESIAN_POINT ( 'NONE',  ( 3.134520880496123318, -1.623366475481220261, 0.8686021547102340534 ) ) ;
#156023=CARTESIAN_POINT ( 'NONE',  ( 0.6280632297508845774, -2.189494644770412890, 0.7293192972532935858 ) ) ;
#156025=CARTESIAN_POINT ( 'NONE',  ( 3.813887338145681927, -2.130327034543195275, 0.3653767458386343314 ) ) ;
#156028=CARTESIAN_POINT ( 'NONE',  ( 1.973319494866377699, 1.790917844098998124, -0.5403536831049270406 ) ) ;
#156029=CARTESIAN_POINT ( 'NONE',  ( 0.5441301207207068780, 1.965759916638841309, 0.1495998195316684265 ) ) ;
#156033=CARTESIAN_POINT ( 'NONE',  ( 1.875870136999336246, 2.111227540014638304, -0.6426800678154330759 ) ) ;
#156039=CARTESIAN_POINT ( 'NONE',  ( 5.647334207030327846, -1.553848685622709835, -1.213239188487026166 ) ) ;
#156040=CARTESIAN_POINT ( 'NONE',  ( 5.865930957382810895, 2.274600175340906638, -0.3886535673101945143 ) ) ;
#156041=CARTESIAN_POINT ( 'NONE',  ( 0.8187140321147531319, -1.423520202335259999, 1.350257566363553208 ) ) ;
#156043=CARTESIAN_POINT ( 'NONE',  ( 2.500897397093455155, 0.4475292293845704594, 2.013297154094250807 ) ) ;
#156050=CARTESIAN_POINT ( 'NONE',  ( 5.178266966923749770, -1.157238278732542369, -1.836894593069735793 ) ) ;
#156052=CARTESIAN_POINT ( 'NONE',  ( 4.897927690869709139, -0.6253142351902387652, -1.731941863025769246 ) ) ;
#156056=CARTESIAN_POINT ( 'NONE',  ( 6.620655732516644854, 4.701125524277991907, 2.388986273831222640 ) ) ;
#156057=CARTESIAN_POINT ( 'NONE',  ( 6.720655732516647163, -0.007268404184145290173, 2.273772995263834584 ) ) ;
#156058=CARTESIAN_POINT ( 'NONE',  ( 0.5791066246769066561, 1.747692025923882841, -0.6672336632058752937 ) ) ;
#156059=CARTESIAN_POINT ( 'NONE',  ( 0.6150082408139592172, 1.559066714514239393, -1.639647465354547196 ) ) ;
#156065=CARTESIAN_POINT ( 'NONE',  ( 6.159198499077391808, -1.652456008184695735, -0.9899348748576908275 ) ) ;
#156066=CARTESIAN_POINT ( 'NONE',  ( 2.166550811918485753, -1.616863761265506794, -0.7202261968358366628 ) ) ;
#156068=CARTESIAN_POINT ( 'NONE',  ( 6.182294962360654900, 1.036951722903585837, 1.725357817989848996 ) ) ;
#156070=CARTESIAN_POINT ( 'NONE',  ( 3.585460515032745210, -0.5529844701629010872, 1.834067302312661241 ) ) ;
#156073=CARTESIAN_POINT ( 'NONE',  ( 4.035575377323636026, 1.855309441653162139, -0.6614512482757756162 ) ) ;
#156074=CARTESIAN_POINT ( 'NONE',  ( 6.451426753955883164, -1.802380967894920527, 0.9117540809469369956 ) ) ;
#156076=CARTESIAN_POINT ( 'NONE',  ( 2.500682550815761740, 1.503739811390795378, -1.112508705057350999 ) ) ;
#156077=CARTESIAN_POINT ( 'NONE',  ( 6.252575197229738535, 0.5485693247098271108, 1.635415954441843844 ) ) ;
#156078=ORIENTED_EDGE ( 'NONE', *, *, #142903, .T. ) ;
#156079=CARTESIAN_POINT ( 'NONE',  ( 1.998912159191484905, -0.5904864226158462737, -2.126349760018491963 ) ) ;
#156082=CARTESIAN_POINT ( 'NONE',  ( 6.566857081534598350, 1.454584517406570132, -1.316677807353151097 ) ) ;
#156086=CARTESIAN_POINT ( 'NONE',  ( 0.1747926744264451659, 0.2546335194838904581, -1.890750172325323275 ) ) ;
#156091=CARTESIAN_POINT ( 'NONE',  ( 2.189971326302230903, -1.350648006375281929, -1.569233719104834890 ) ) ;
#156095=CARTESIAN_POINT ( 'NONE',  ( 6.340501840829311675, 1.221348521443364366, -1.733245716811770309 ) ) ;
#156098=CARTESIAN_POINT ( 'NONE',  ( 0.07479286986305369589, 1.387406912293275729, -2.112587013352088317 ) ) ;
#156100=CARTESIAN_POINT ( 'NONE',  ( 5.571638683613604037, 1.528505562557905595, -1.314797328242120367 ) ) ;
#156101=CARTESIAN_POINT ( 'NONE',  ( 6.280494692369203769, -0.5183099952858164494, -1.844178102243919870 ) ) ;
#156102=CARTESIAN_POINT ( 'NONE',  ( 6.539320575229223387, 6.036367980355456631, 2.598156967962389263 ) ) ;
#156103=CARTESIAN_POINT ( 'NONE',  ( 3.386445149735781257, -0.4294187885149694517, -2.148908265708626697 ) ) ;
#156106=CARTESIAN_POINT ( 'NONE',  ( 2.865378420500460432, -1.565876230000915470, -1.097592462808501645 ) ) ;
#156110=CARTESIAN_POINT ( 'NONE',  ( 6.925078400183515726, -0.002206826874838823185, 1.955452213090567160 ) ) ;
#156111=CARTESIAN_POINT ( 'NONE',  ( 6.591443028821331040, -0.4675721919094841250, 2.072835713318227135 ) ) ;
#156114=CARTESIAN_POINT ( 'NONE',  ( 6.093348126157794198, -0.7399906200981146709, 2.062998119606203939 ) ) ;
#156116=CARTESIAN_POINT ( 'NONE',  ( 3.100334465813825435, -0.4993057154734497072, -1.650917527159057707 ) ) ;
#156118=CARTESIAN_POINT ( 'NONE',  ( 6.398696098476772676, -2.079943653215409416, -0.4123558718646391785 ) ) ;
#156122=CARTESIAN_POINT ( 'NONE',  ( 0.1858947801188018389, -1.204007190563995078, -1.549573762531175625 ) ) ;
#156130=CARTESIAN_POINT ( 'NONE',  ( 2.965264322261091934, -1.482184020574893069, -1.041122702216127571 ) ) ;
#156134=CARTESIAN_POINT ( 'NONE',  ( 3.580526426040127941, -1.214262702978758712, 1.344428254631929276 ) ) ;
#156138=CARTESIAN_POINT ( 'NONE',  ( 4.896841239116665356, 0.3175000240179836619, 1.833586397851859839 ) ) ;
#156140=CARTESIAN_POINT ( 'NONE',  ( 2.794441263998331149, 1.385543030692138133, -1.323043162562879349 ) ) ;
#156141=CARTESIAN_POINT ( 'NONE',  ( 0.9908991873810431006, 1.612194894691898250, -0.8564790819722142290 ) ) ;
#156152=CARTESIAN_POINT ( 'NONE',  ( 1.728581982081365265, 0.2060769881795926906, 2.080452860985905428 ) ) ;
#156153=CARTESIAN_POINT ( 'NONE',  ( 6.211935731971203190, -1.911736917912661537, 0.2365620046330171311 ) ) ;
#156155=CARTESIAN_POINT ( 'NONE',  ( 2.186296784933777992, -1.789763940591000191, -0.3589617604915079085 ) ) ;
#156156=CARTESIAN_POINT ( 'NONE',  ( 3.422699507934780616, 1.400174360247144589, -1.705827624971032686 ) ) ;
#156159=CARTESIAN_POINT ( 'NONE',  ( 1.476665317443916603, -1.350161712199383413, 1.354623164920423450 ) ) ;
#156160=CARTESIAN_POINT ( 'NONE',  ( 1.785543415971390102, -1.855581397249297382, 0.6606886831301524987 ) ) ;
#156161=CARTESIAN_POINT ( 'NONE',  ( 2.876435298317912004, -0.1456031558026495976, -1.936675272211895837 ) ) ;
#156165=CARTESIAN_POINT ( 'NONE',  ( 6.385601346537729484, -1.752585461374029929, 0.6262014864842447848 ) ) ;
#156170=CARTESIAN_POINT ( 'NONE',  ( 2.683357600500847262, 1.551837136583393839, 1.547750905674146971 ) ) ;
#156176=CARTESIAN_POINT ( 'NONE',  ( 4.072732355924274295, -1.704239406772959153, -0.6552279023967976235 ) ) ;
#156183=CARTESIAN_POINT ( 'NONE',  ( 2.420428029321282093, 1.258221797421785082, -1.458952285233440449 ) ) ;
#156184=CARTESIAN_POINT ( 'NONE',  ( 6.526224699197019419, 1.005635830909179074, 1.684226478273798788 ) ) ;
#156190=CARTESIAN_POINT ( 'NONE',  ( -0.1232448511370512201, -0.4725888426768353190, -2.071762565325820038 ) ) ;
#156193=CARTESIAN_POINT ( 'NONE',  ( 5.032118066406459533, 1.187563481491529460, 1.695602288408842417 ) ) ;
#156194=CARTESIAN_POINT ( 'NONE',  ( 0.1164230846485321547, -0.09151219166612066525, 1.839079034809627755 ) ) ;
#156197=CARTESIAN_POINT ( 'NONE',  ( 5.326872488440856479, 0.9340183262317149904, -2.100526973934746522 ) ) ;
#156201=CARTESIAN_POINT ( 'NONE',  ( 0.3754557147975129960, 2.136610487456944263, -0.8307393200860619942 ) ) ;
#156204=CARTESIAN_POINT ( 'NONE',  ( 4.558499613049934673, -1.735246752265024561, -0.8719658702049468690 ) ) ;
#156209=CARTESIAN_POINT ( 'NONE',  ( 6.363533315466952445, -1.540175188624912650, -1.133462061071670579 ) ) ;
#156210=CARTESIAN_POINT ( 'NONE',  ( 0.2402810872906081530, 0.2891477966728701610, 1.700304936625576024 ) ) ;
#156211=CARTESIAN_POINT ( 'NONE',  ( 6.227749967195367553, 0.7672974224810540367, -1.865044430435198519 ) ) ;
#156215=CARTESIAN_POINT ( 'NONE',  ( 2.976600611693449139, -0.1542612496043833104, -2.085005227243463821 ) ) ;
#156216=CARTESIAN_POINT ( 'NONE',  ( 0.6898892245524823608, -1.755727311204742680, -0.2225690630779184609 ) ) ;
#156219=CARTESIAN_POINT ( 'NONE',  ( 3.943561162899355654, 0.7735357226616009774, -2.157932208606289759 ) ) ;
#156220=CARTESIAN_POINT ( 'NONE',  ( 2.448798285840974476, 0.4648185774855151942, -1.677030037339591217 ) ) ;
#156223=CARTESIAN_POINT ( 'NONE',  ( 1.651252135258261422, -0.2480751513778757522, -1.715843305285965403 ) ) ;
#156225=CARTESIAN_POINT ( 'NONE',  ( 1.855673809551155795, -0.6311025070286357952, 1.750906552266822569 ) ) ;
#156226=CARTESIAN_POINT ( 'NONE',  ( 2.611994278460927799, 0.5808993838645438723, -2.091943403374715515 ) ) ;
#156228=CARTESIAN_POINT ( 'NONE',  ( 3.661342437515973547, 1.897110692972364454, -0.6839366698164971448 ) ) ;
#156229=CARTESIAN_POINT ( 'NONE',  ( 1.843750000000001332, 1.895863743164127868, 0.7852924748298895086 ) ) ;
#156231=CARTESIAN_POINT ( 'NONE',  ( 0.8856179577424825311, 1.291390466942985649, 1.429610664621896898 ) ) ;
#156233=CARTESIAN_POINT ( 'NONE',  ( 4.957398421247804166, -1.904820672624758515, 1.142771788014641743 ) ) ;
#156239=CARTESIAN_POINT ( 'NONE',  ( 5.748318879583719010, 1.095320496750437966, -1.932492775422405717 ) ) ;
#156240=CARTESIAN_POINT ( 'NONE',  ( 4.545333077707183200, 1.753367681936630840, -0.8802267832125689750 ) ) ;
#156243=CARTESIAN_POINT ( 'NONE',  ( 5.255258077898470326, -1.907309223944063437, -1.216589440439620695 ) ) ;
#156245=CARTESIAN_POINT ( 'NONE',  ( 3.104023224481029519, 0.7448178976848550681, -1.923671348419103921 ) ) ;
#156249=CARTESIAN_POINT ( 'NONE',  ( 5.008994926481016741, 1.626754543590884561, 0.9232732976792232815 ) ) ;
#156250=CARTESIAN_POINT ( 'NONE',  ( 4.043420308529748652, -1.281227996783333989, 1.168826672502675912 ) ) ;
#156251=CARTESIAN_POINT ( 'NONE',  ( 2.858654643706417975, 0.2527927160936989659, -1.721832920378673748 ) ) ;
#156252=CARTESIAN_POINT ( 'NONE',  ( 0.6445460132639491135, 0.6724220840489106843, 2.191533042908066165 ) ) ;
#156253=CARTESIAN_POINT ( 'NONE',  ( 0.8685540286928781217, 1.089157903960279672, 1.919174906450902274 ) ) ;
#156254=CARTESIAN_POINT ( 'NONE',  ( 4.370703248089922610, -0.001752428395085294443, -2.090933975693793911 ) ) ;
#156255=CARTESIAN_POINT ( 'NONE',  ( 5.542900022196344700, -1.532237948119744342, -1.192973588722973100 ) ) ;
#156258=CARTESIAN_POINT ( 'NONE',  ( 0.3697678102792775756, -0.2496098759999023087, -2.000856779379902139 ) ) ;
#156261=CARTESIAN_POINT ( 'NONE',  ( 6.522112240665402183, -1.799906897009293738, 0.9091900463213120620 ) ) ;
#156265=CARTESIAN_POINT ( 'NONE',  ( 3.879382553896340013, 1.718498013671100777, -0.6167319420108534622 ) ) ;
#156271=CARTESIAN_POINT ( 'NONE',  ( 2.426041109754235592, -1.997208190617974166, 0.3004318525065238776 ) ) ;
#156273=CARTESIAN_POINT ( 'NONE',  ( 3.432308073483012922, -1.112138214925220803, 1.491878268611693814 ) ) ;
#156279=CARTESIAN_POINT ( 'NONE',  ( 5.338443970399977978, 1.799313579390570128, 0.3082849261525285600 ) ) ;
#156283=CARTESIAN_POINT ( 'NONE',  ( 0.6317059331818836165, 0.1778517408326604765, -1.724704385026996079 ) ) ;
#156284=CARTESIAN_POINT ( 'NONE',  ( 6.703072984701052839, -0.3981723446819797063, 1.804146177254343009 ) ) ;
#156285=CARTESIAN_POINT ( 'NONE',  ( 5.198025161738785371, -0.8347013672818380803, 2.151627338387426036 ) ) ;
#156287=CARTESIAN_POINT ( 'NONE',  ( 0.3157904346527000139, -2.021491663516309156, 0.3995350904514202162 ) ) ;
#156289=CARTESIAN_POINT ( 'NONE',  ( 5.800273438847154850, -2.081326394616866970, 0.9752826944557994038 ) ) ;
#156292=CARTESIAN_POINT ( 'NONE',  ( 5.260568668178753349, -1.354309965608934352, 1.290672426560689035 ) ) ;
#156294=CARTESIAN_POINT ( 'NONE',  ( 3.515784362865181478, -0.5505564139345071606, 1.831456330389509501 ) ) ;
#156296=CARTESIAN_POINT ( 'NONE',  ( 4.846401659255799466, 2.200796399388889935, 0.1645688927329121420 ) ) ;
#156297=CARTESIAN_POINT ( 'NONE',  ( 4.329393036353162749, -1.639139883998712799, -1.340335314225228780 ) ) ;
#156300=CARTESIAN_POINT ( 'NONE',  ( 6.983263157960404754, 0.5693283498368858497, 2.097578288773850552 ) ) ;
#156303=CARTESIAN_POINT ( 'NONE',  ( 5.391314312714450274, -0.05227466736787074464, -2.120015263102632552 ) ) ;
#156304=CARTESIAN_POINT ( 'NONE',  ( 2.063905019644726835, 0.3937302209732340685, -2.273608288252434662 ) ) ;
#156305=CARTESIAN_POINT ( 'NONE',  ( 3.631260574587381829, 0.05062604155347744800, -1.961386756325018021 ) ) ;
#156306=CARTESIAN_POINT ( 'NONE',  ( 6.977413162628444354, -0.1478290182607009950, 2.029965231729473185 ) ) ;
#156310=CARTESIAN_POINT ( 'NONE',  ( 5.331267653506235327, -1.592659417495114083, -1.236803018183525449 ) ) ;
#156313=CARTESIAN_POINT ( 'NONE',  ( -0.2408018239684095729, -0.007136184528808943960, -2.100252307185761058 ) ) ;
#156314=CARTESIAN_POINT ( 'NONE',  ( 1.604584692665763423, 2.168457688117795712, 0.1093331725631509210 ) ) ;
#156321=CARTESIAN_POINT ( 'NONE',  ( 1.071639231386111391, 1.986785141929363618, -0.5470796107636519690 ) ) ;
#156324=CARTESIAN_POINT ( 'NONE',  ( 6.727182134110196721, 2.084960209934753284, 2.120171393779949565 ) ) ;
#156328=CARTESIAN_POINT ( 'NONE',  ( 3.299369280271017946, 1.727720890571235124, -0.8199460011262191816 ) ) ;
#156329=CARTESIAN_POINT ( 'NONE',  ( 5.436323762753620947, 1.744125921451036065, 0.2996227856876289564 ) ) ;
#156332=CARTESIAN_POINT ( 'NONE',  ( 0.03503794071320948805, -0.08894543905034424380, 1.809493548878613023 ) ) ;
#156333=CARTESIAN_POINT ( 'NONE',  ( 6.274997412412571585, 1.664062557780759066, -0.9488046768871650771 ) ) ;
#156335=CARTESIAN_POINT ( 'NONE',  ( 0.5552397518338060278, 1.722184604005328357, -1.148819969904082861 ) ) ;
#156338=CARTESIAN_POINT ( 'NONE',  ( 5.735183426005796115, -1.690533149647139410, 0.8011652756413772947 ) ) ;
#156339=CARTESIAN_POINT ( 'NONE',  ( 3.017977635683791071, -0.9002817137206723386, -1.588204215665294461 ) ) ;
#156340=CARTESIAN_POINT ( 'NONE',  ( 6.111994396789379280, -2.190734547077430872, 0.2660306753756238041 ) ) ;
#156343=CARTESIAN_POINT ( 'NONE',  ( 2.945816691342293847, 1.456820166381930015, 1.460492231956188824 ) ) ;
#156349=CARTESIAN_POINT ( 'NONE',  ( 6.619590326553026038, 0.3579758704960536719, -2.039031579972025554 ) ) ;
#156351=CARTESIAN_POINT ( 'NONE',  ( 3.901784996602038813, -0.6316019492740264640, 2.067237329103743804 ) ) ;
#156352=CARTESIAN_POINT ( 'NONE',  ( 4.195966715351859833, 1.320990344651201021, 1.527833845825769643 ) ) ;
#156353=CARTESIAN_POINT ( 'NONE',  ( 2.348037267531626338, -0.8415878996531295231, 1.772339229757218471 ) ) ;
#156354=CARTESIAN_POINT ( 'NONE',  ( 6.620655732516668834, 6.034240673559561507, 2.768629221164942145 ) ) ;
#156359=CARTESIAN_POINT ( 'NONE',  ( 2.518767860054324625, 0.2516336668320385828, 2.000731427934741902 ) ) ;
#156362=DIRECTION ( 'NONE',  ( -1.000000000000000000, 0.000000000000000000, 0.000000000000000000 ) ) ;
#156363=CARTESIAN_POINT ( 'NONE',  ( 5.572493885891085519, 0.7809320506734825917, 1.745880147543739325 ) ) ;
#156367=CARTESIAN_POINT ( 'NONE',  ( 3.444935562074178392, -1.779636981393231565, -0.9480232565319337557 ) ) ;
#156370=CARTESIAN_POINT ( 'NONE',  ( 5.948237010872538200, 1.723075781188963207, 0.07969437682242562493 ) ) ;
#156374=CARTESIAN_POINT ( 'NONE',  ( 4.622238261848357510, 1.152259890254858421, -1.473394524551620011 ) ) ;
#156376=CARTESIAN_POINT ( 'NONE',  ( 2.254815949590884827, -0.5480598642870064818, -1.996355599893632649 ) ) ;
#156383=CARTESIAN_POINT ( 'NONE',  ( 0.1932431142802397694, 1.690279412936572134, -0.6521791651670250101 ) ) ;
#156388=CARTESIAN_POINT ( 'NONE',  ( 5.607027416250175200, -0.04201266709560196738, 1.915314589656505362 ) ) ;
#156395=CARTESIAN_POINT ( 'NONE',  ( 3.450221060135277629, 2.161883445724331665, 0.001893877739161941697 ) ) ;
#156399=CARTESIAN_POINT ( 'NONE',  ( 5.719710266082651096, -1.780569991979109590, 0.4021758204828808081 ) ) ;
#156401=CARTESIAN_POINT ( 'NONE',  ( 1.106637804720354668, 1.495658270405418877, -1.284366697391533529 ) ) ;
#156402=CARTESIAN_POINT ( 'NONE',  ( 3.568532368641282648, 0.6928216322696268969, 1.782650395559831180 ) ) ;
#156405=CARTESIAN_POINT ( 'NONE',  ( 5.055114266443681004, 1.638575763527612583, -1.092465951337840524 ) ) ;
#156406=CARTESIAN_POINT ( 'NONE',  ( 0.9373250018651816395, 0.7876268737729983371, -1.775224631529322306 ) ) ;
#156410=CARTESIAN_POINT ( 'NONE',  ( 6.363548717301088509, -1.704009271243651868, -1.262090224194649446 ) ) ;
#156412=CARTESIAN_POINT ( 'NONE',  ( 3.914637684252043393, -0.6027250981219151038, -1.814865640613130271 ) ) ;
#156414=CARTESIAN_POINT ( 'NONE',  ( 1.272829778695073299, -1.399090282553701270, 1.706552004499435560 ) ) ;
#156417=CARTESIAN_POINT ( 'NONE',  ( 6.287749749268194854, 1.925770139592613450, -0.5864224512089585284 ) ) ;
#156418=CARTESIAN_POINT ( 'NONE',  ( 0.2331563151865486683, 0.005903526429595904942, -1.945944850731482934 ) ) ;
#156420=CARTESIAN_POINT ( 'NONE',  ( 5.700407750362016301, 1.350738941191354625, -1.497498989668680114 ) ) ;
#156422=CARTESIAN_POINT ( 'NONE',  ( 1.908725956546155178, 0.6474277305483535638, 1.966616875269424192 ) ) ;
#156433=CARTESIAN_POINT ( 'NONE',  ( 6.925078400183553917, 6.038071034253152725, 2.450556290382682523 ) ) ;
#156435=CARTESIAN_POINT ( 'NONE',  ( 4.904772540272760217, -0.9336124152922348207, -1.461164293347013921 ) ) ;
#156439=CARTESIAN_POINT ( 'NONE',  ( 2.465759480183654428, -0.4578044685884518072, 2.018832516862689275 ) ) ;
#156440=CARTESIAN_POINT ( 'NONE',  ( 4.007494584968971374, -2.025512140874039524, 0.6163414799803969002 ) ) ;
#156443=CARTESIAN_POINT ( 'NONE',  ( 1.639439270303972851, 1.821716124042528584, -0.7488776562727271768 ) ) ;
#156446=CARTESIAN_POINT ( 'NONE',  ( -0.08783152977152529350, -1.912005390248720627, -0.04503566501021933483 ) ) ;
#156447=CARTESIAN_POINT ( 'NONE',  ( 3.433774379101984575, 1.031038968642459475, -2.047360584804863493 ) ) ;
#156448=CARTESIAN_POINT ( 'NONE',  ( 1.963248404482214049, 0.3131683437365209710, -1.798463397695612809 ) ) ;
#156452=CARTESIAN_POINT ( 'NONE',  ( 3.146742683403806140, 1.965092980649842502, 0.4368759242464967940 ) ) ;
#156453=CARTESIAN_POINT ( 'NONE',  ( 2.940231979924610162, -1.012623612260230566, 1.680088604585870060 ) ) ;
#156457=CARTESIAN_POINT ( 'NONE',  ( 6.298786922650962516, 1.737427944715240091, 1.162477542130130548 ) ) ;
#156458=CARTESIAN_POINT ( 'NONE',  ( 4.873781607783202574, 1.020544065373253817, 1.445763320596996193 ) ) ;
#156460=CARTESIAN_POINT ( 'NONE',  ( 1.131117939106265569, -1.979831898266545487, 0.9398196729281658168 ) ) ;
#156461=CARTESIAN_POINT ( 'NONE',  ( 6.105355155539634815, -1.726289741429184899, 0.2200517785161565654 ) ) ;
#156465=CARTESIAN_POINT ( 'NONE',  ( 0.2460673368967214447, -2.230335335914147343, -0.5547215216719133535 ) ) ;
#156467=CARTESIAN_POINT ( 'NONE',  ( 5.729790939124476346, -1.568816369837353619, -0.7386035493782086014 ) ) ;
#156468=CARTESIAN_POINT ( 'NONE',  ( 1.594636444620714633, -2.196503929104542951, -0.2137616909994101977 ) ) ;
#156469=CARTESIAN_POINT ( 'NONE',  ( 5.354042097475935513, -0.7863316197885154013, 2.023950393233854061 ) ) ;
#156471=CARTESIAN_POINT ( 'NONE',  ( 0.5325983862809284819, 0.6208049431430485710, 2.024263306480874380 ) ) ;
#156472=CARTESIAN_POINT ( 'NONE',  ( 3.750000000000002665, 2.137871159508210026E-13, 2.052068128417945836 ) ) ;
#156474=CARTESIAN_POINT ( 'NONE',  ( 4.084924167595121780, -0.1881231333150361895, -1.917172266129524294 ) ) ;
#156476=CARTESIAN_POINT ( 'NONE',  ( 1.208037074693757651, 1.685330760668615646, 1.447128815913247379 ) ) ;
#156477=EDGE_LOOP ( 'NONE', ( #167880, #134426, #58761, #209248 ) ) ;
#156481=CARTESIAN_POINT ( 'NONE',  ( 4.160924129468469346, 0.5925846814045959698, 2.140718581676650079 ) ) ;
#156487=CARTESIAN_POINT ( 'NONE',  ( 0.8092204703840089053, 1.198858234535697065, -1.621184076614573533 ) ) ;
#156489=CARTESIAN_POINT ( 'NONE',  ( 6.725054104113727504, -1.884248279909329638, -0.8396177084525523471 ) ) ;
#156492=CARTESIAN_POINT ( 'NONE',  ( -0.07694640568740516995, -1.131669979810394633, -1.452919414246391261 ) ) ;
#156495=CARTESIAN_POINT ( 'NONE',  ( 1.862210123611393708, -1.255811410660602867, 1.247235970127296811 ) ) ;
#156496=CARTESIAN_POINT ( 'NONE',  ( 0.5631252389872200004, -1.117830369828230808, 1.678006741548984770 ) ) ;
#156497=CARTESIAN_POINT ( 'NONE',  ( 6.567905868640212752, -1.062476624526029312, 1.378933096211315101 ) ) ;
#156498=CARTESIAN_POINT ( 'NONE',  ( 4.546573649138107243, -1.841725595444974939, 1.364713657601625885 ) ) ;
#156500=CARTESIAN_POINT ( 'NONE',  ( 2.413779523973126118, 1.202770565240804279, -1.394052804434331216 ) ) ;
#156503=CARTESIAN_POINT ( 'NONE',  ( 3.205874166558682514, -1.823564452915670042, 0.08818595847179949709 ) ) ;
#156504=CARTESIAN_POINT ( 'NONE',  ( 3.551407868487792552, -1.352154898762620849, 1.496051317864899088 ) ) ;
#156506=CARTESIAN_POINT ( 'NONE',  ( 3.362467959171450360, 1.015586399080644187, 2.021831916694483144 ) ) ;
#156508=CARTESIAN_POINT ( 'NONE',  ( 5.772525194315006658, -1.338739070262290110, 1.625669279078660878 ) ) ;
#156510=CARTESIAN_POINT ( 'NONE',  ( 2.102089431743926706, 0.7944251937819692966, -1.912079865474418439 ) ) ;
#156513=CARTESIAN_POINT ( 'NONE',  ( 6.358074577831472673, 0.8120454629646983724, -1.959034198684066697 ) ) ;
#156515=CARTESIAN_POINT ( 'NONE',  ( 0.6801461905075457670, -1.071176224578209935, 1.601055298966150842 ) ) ;
#156522=CARTESIAN_POINT ( 'NONE',  ( 0.2994921435493704820, -0.2801620449621230469, -2.203647339609093869 ) ) ;
#156523=CARTESIAN_POINT ( 'NONE',  ( 2.626118769021787536, -1.211593817910999293, -1.722331309457482362 ) ) ;
#156526=CARTESIAN_POINT ( 'NONE',  ( 6.420743829754993470, -1.316656903452334992, 1.315380689086578236 ) ) ;
#156528=CARTESIAN_POINT ( 'NONE',  ( 0.07680821025393690105, 0.005952109439256307241, -1.810863387344714193 ) ) ;
#156532=CARTESIAN_POINT ( 'NONE',  ( 0.03560581989598374242, -0.09759080014098624190, 2.118463022953632091 ) ) ;
#156535=CARTESIAN_POINT ( 'NONE',  ( 2.805073129645048624, -1.632656238785214597, 1.087510969322850629 ) ) ;
#156536=CARTESIAN_POINT ( 'NONE',  ( 2.237400686453533183, -1.931180590798301955, 0.9714560045831142077 ) ) ;
#156541=CARTESIAN_POINT ( 'NONE',  ( 3.486021976759791308, -0.3410757193606011040, -1.706382030880509104 ) ) ;
#156544=CARTESIAN_POINT ( 'NONE',  ( 2.530624857006387618, 1.977747929495787371, -0.3905373530270899174 ) ) ;
#156546=CARTESIAN_POINT ( 'NONE',  ( 0.2511322555047851290, -1.735185354305257110, 1.289038484408123963 ) ) ;
#156547=CARTESIAN_POINT ( 'NONE',  ( 2.184392200726268829, -1.933073530578834465, -0.3863716293817393566 ) ) ;
#156554=CARTESIAN_POINT ( 'NONE',  ( 2.860025901456241471, 0.7249204854099660089, -1.885284610270787642 ) ) ;
#156556=CARTESIAN_POINT ( 'NONE',  ( 5.631924041214952936, -1.458266564992457104, -1.788428398515107043 ) ) ;
#156558=CARTESIAN_POINT ( 'NONE',  ( 2.641395077882053410, 1.795597516233004232, -0.7905247784146393064 ) ) ;
#156560=CARTESIAN_POINT ( 'NONE',  ( 0.5631252389872200004, -1.117830369828230808, 1.678006741548984770 ) ) ;
#156561=ORIENTED_EDGE ( 'NONE', *, *, #79408, .T. ) ;
#156562=CARTESIAN_POINT ( 'NONE',  ( 2.184896953550282461, 1.697450634274371595, -1.265404921814163641 ) ) ;
#156565=CARTESIAN_POINT ( 'NONE',  ( 2.554438963407625884, -1.601868926591401232, -0.9074879233003440016 ) ) ;
#156569=CARTESIAN_POINT ( 'NONE',  ( 4.517907016363444939, -0.5628432189327194912, 2.044499502628312371 ) ) ;
#156571=CARTESIAN_POINT ( 'NONE',  ( 0.5152501731416662123, -0.9825955030486509534, -1.556829690179861281 ) ) ;
#156575=CARTESIAN_POINT ( 'NONE',  ( 4.200502791967850591, -0.6429285697095908914, -1.958015678616845445 ) ) ;
#156578=CARTESIAN_POINT ( 'NONE',  ( 1.540310226958538475, -1.555040833713853710, 0.9856339240054690087 ) ) ;
#156581=CARTESIAN_POINT ( 'NONE',  ( 6.509000000000037645, 7.629137130509070275, 2.600000000000001421 ) ) ;
#156582=CARTESIAN_POINT ( 'NONE',  ( 1.647397727484143592, -1.863059487452220386, 1.182652941231487453 ) ) ;
#156583=CARTESIAN_POINT ( 'NONE',  ( 3.620660229735796154, 1.438486863682734818, -1.746180642158390084 ) ) ;
#156585=CARTESIAN_POINT ( 'NONE',  ( 3.972783152890049241, -1.338232477621086547, 1.221218810135711541 ) ) ;
#156586=CARTESIAN_POINT ( 'NONE',  ( 2.624132809847005365, 1.901796678110598382, 0.2296932149444090299 ) ) ;
#156587=CARTESIAN_POINT ( 'NONE',  ( 3.824723168590526523, -1.392635068473629500, 1.532133406949770960 ) ) ;
#156589=CARTESIAN_POINT ( 'NONE',  ( 2.465646028844501902, 1.933766160897397057, -0.3828895411656701997 ) ) ;
#156590=CARTESIAN_POINT ( 'NONE',  ( 0.5692023642799119987, 0.1922812221162081003, -1.916781067358761748 ) ) ;
#156591=CARTESIAN_POINT ( 'NONE',  ( 4.223419137798128276, -1.790188510885984297, 0.5427707113358354318 ) ) ;
#156592=CARTESIAN_POINT ( 'NONE',  ( 2.631810907782325071, -2.152760894471450914, 0.8317484501371147365 ) ) ;
#156593=CARTESIAN_POINT ( 'NONE',  ( 4.123391753781197266, 0.2291962677869363585, -1.846827494033479455 ) ) ;
#156601=CARTESIAN_POINT ( 'NONE',  ( 0.3992258182855871196, 1.749727718737997373, -1.171850562161039777 ) ) ;
#156605=CARTESIAN_POINT ( 'NONE',  ( 6.837200347746460238, -1.934230338078479550, 0.9651617863762136373 ) ) ;
#156606=CARTESIAN_POINT ( 'NONE',  ( 1.670341986359990205, 2.114562342887704283, -0.1611296783964668855 ) ) ;
#156607=CARTESIAN_POINT ( 'NONE',  ( 0.3166733070498818359, -0.6846287639105748113, -1.900330225253379801 ) ) ;
#156611=CARTESIAN_POINT ( 'NONE',  ( 1.001511639980020130, 1.766541945284912263, 1.245431700958275600 ) ) ;
#156613=CARTESIAN_POINT ( 'NONE',  ( 6.825078400183516081, 0.5802287360496224400, 2.007770452540482697 ) ) ;
#156616=CARTESIAN_POINT ( 'NONE',  ( 5.682827415814322158, 1.645762192317705486, -1.164983060713747909 ) ) ;
#156620=CARTESIAN_POINT ( 'NONE',  ( 0.5853300251711880398, -0.2802842603415867107, -2.245014038439311577 ) ) ;
#156624=CARTESIAN_POINT ( 'NONE',  ( 1.423292265346193464, -1.388624197914482883, -1.319832876491247697 ) ) ;
#156629=CARTESIAN_POINT ( 'NONE',  ( 2.525662786804376836, -0.9926222177696201188, -1.410421675411769993 ) ) ;
#156632=CARTESIAN_POINT ( 'NONE',  ( 0.7371257246046484246, -1.245724469572104587, -1.257322912719664787 ) ) ;
#156633=CARTESIAN_POINT ( 'NONE',  ( 1.471341131262299706, -1.727646810417843959, -1.033094421854539036 ) ) ;
#156634=CARTESIAN_POINT ( 'NONE',  ( 3.716033540554028125, -2.174548934981130444, 0.3748234698989146851 ) ) ;
#156638=CARTESIAN_POINT ( 'NONE',  ( 4.055424778641623540, -1.844328037693225397, 1.046277804987456372 ) ) ;
#156639=CARTESIAN_POINT ( 'NONE',  ( 4.534779904478015489, -1.617806963314952773, 1.203370736114671269 ) ) ;
#156640=CARTESIAN_POINT ( 'NONE',  ( 3.673895663291579350, 1.797233291820631962, -0.2271657407440821064 ) ) ;
#156644=CARTESIAN_POINT ( 'NONE',  ( 1.094370286708164386, -0.4508366001288487968, -1.815394955969009461 ) ) ;
#156645=CARTESIAN_POINT ( 'NONE',  ( 5.760330229460346452, 0.7440287100829169331, 1.667389206893993725 ) ) ;
#156654=CARTESIAN_POINT ( 'NONE',  ( 4.096021571020786567, 1.387573888390711385, 1.603661410755026440 ) ) ;
#156655=CARTESIAN_POINT ( 'NONE',  ( -0.02968770228140016343, 1.391517546076680434, -2.083419219542380407 ) ) ;
#156658=CARTESIAN_POINT ( 'NONE',  ( 3.954335293022055886, 0.7064427249091516092, 1.840614667007954841 ) ) ;
#156660=CARTESIAN_POINT ( 'NONE',  ( 6.486579876843341808, -1.171037552013409089, 1.512559164390047783 ) ) ;
#156662=CARTESIAN_POINT ( 'NONE',  ( 0.2634788376212302552, 1.973769265480609381, -0.7665230665306818070 ) ) ;
#156664=CARTESIAN_POINT ( 'NONE',  ( 0.9946828900261883710, 2.039433816042154124, 0.3556643922909968891 ) ) ;
#156668=CARTESIAN_POINT ( 'NONE',  ( 3.960945476642624641, 0.2557261242597759776, -2.074860007841982767 ) ) ;
#156671=CARTESIAN_POINT ( 'NONE',  ( 1.781981981289095796, -0.9795585948506604357, 1.540336029244721461 ) ) ;
#156672=CARTESIAN_POINT ( 'NONE',  ( 1.189788175852508845, 1.078664940389061577, 1.455116354534333079 ) ) ;
#156673=CARTESIAN_POINT ( 'NONE',  ( 6.076841795016812320, -2.094286673724785164, -0.6961510500591641115 ) ) ;
#156675=CARTESIAN_POINT ( 'NONE',  ( 4.032405518703926717, 1.182977813604596973, -1.862726815517960821 ) ) ;
#156678=CARTESIAN_POINT ( 'NONE',  ( 2.420441844550869526, -0.7335502799032425081, -1.766186906296034698 ) ) ;
#156681=CARTESIAN_POINT ( 'NONE',  ( 4.844224204019831781, -0.9789346907586125024, 1.824324395707350943 ) ) ;
#156685=CARTESIAN_POINT ( 'NONE',  ( 6.269083535738129598, 2.097726667780253074, -0.6343229546324488100 ) ) ;
#156696=CARTESIAN_POINT ( 'NONE',  ( 5.577033793921920335, 1.910671465402475677, 0.7975372692515869666 ) ) ;
#156697=CARTESIAN_POINT ( 'NONE',  ( 4.600175520841607302, -1.926116679539988885, -0.04579137001822254638 ) ) ;
#156698=CARTESIAN_POINT ( 'NONE',  ( 0.1050925082292548940, -0.09611335402343046397, 2.014234898253919326 ) ) ;
#156702=CARTESIAN_POINT ( 'NONE',  ( 6.597627758599571735, -2.291905675289906519, 0.04924309260747637695 ) ) ;
#156703=CARTESIAN_POINT ( 'NONE',  ( 5.057177669875371429, -1.544152220135000420, -0.9737345633797565014 ) ) ;
#156711=CARTESIAN_POINT ( 'NONE',  ( 2.981803241483144351, -1.814435276338403735, -0.3121031562058202424 ) ) ;
#156712=CARTESIAN_POINT ( 'NONE',  ( -0.05795285570054254515, -1.240470478354677164, -1.586248892985191006 ) ) ;
#156713=CARTESIAN_POINT ( 'NONE',  ( 0.8085102987360716087, -1.969961327451934086, 1.183767188307288221 ) ) ;
#156714=CARTESIAN_POINT ( 'NONE',  ( 6.543807102324334934, 1.350441955444921849, 1.423202910149905298 ) ) ;
#156718=CARTESIAN_POINT ( 'NONE',  ( 0.3442982867475213871, -0.9772804826688463731, 1.825211318103404867 ) ) ;
#156720=CARTESIAN_POINT ( 'NONE',  ( 2.577772492168933116, -1.072305133946813260, 1.794659622045821079 ) ) ;
#156721=CARTESIAN_POINT ( 'NONE',  ( 1.252583056964752029, -1.476889893665521925, 1.148006582770304096 ) ) ;
#156722=CARTESIAN_POINT ( 'NONE',  ( 1.493517298738750609, 1.942243344100362590, 0.5404107738020345053 ) ) ;
#156726=CARTESIAN_POINT ( 'NONE',  ( 1.997219015684068344, -1.740079325084613604, 0.04332556902747128347 ) ) ;
#156731=CARTESIAN_POINT ( 'NONE',  ( 3.316762602600237475, 1.559927958434914608, 0.7363868292221543710 ) ) ;
#156732=CARTESIAN_POINT ( 'NONE',  ( 3.175498511859841333, 1.392037702009111033, 1.692654053968026151 ) ) ;
#156733=CARTESIAN_POINT ( 'NONE',  ( 4.864015066594513215, 2.183220759563545776, -0.3215228633955333759 ) ) ;
#156735=CARTESIAN_POINT ( 'NONE',  ( 2.747136105846450516, -0.3671824478193272956, -2.139636267262314373 ) ) ;
#156736=CARTESIAN_POINT ( 'NONE',  ( 0.9085097582094739943, 1.384192474337717194, -1.190531929384466281 ) ) ;
#156737=CARTESIAN_POINT ( 'NONE',  ( 4.944582029040364368, -1.531444570474638667, 1.462332997386527556 ) ) ;
#156741=CARTESIAN_POINT ( 'NONE',  ( 4.915721525821019178, -1.224934246408443839, -1.937497040551818150 ) ) ;
#156745=CARTESIAN_POINT ( 'NONE',  ( 0.8387270772249322270, 1.259995426201226953, -1.705408266269872630 ) ) ;
#156753=CARTESIAN_POINT ( 'NONE',  ( 5.520157785563180930, -1.821743191724470634, 0.8647220171385738841 ) ) ;
#156755=CARTESIAN_POINT ( 'NONE',  ( 3.432538798476657327, -1.232314722524804562, 1.653799735942045990 ) ) ;
#156757=CARTESIAN_POINT ( 'NONE',  ( -0.1409997244346088141, 2.874455162768466909, -2.488748179275114492 ) ) ;
#156761=CARTESIAN_POINT ( 'NONE',  ( 6.369083545433415594, 2.098215621258665564, -0.6323776016037768732 ) ) ;
#156762=CARTESIAN_POINT ( 'NONE',  ( 3.674454069786535548, 1.462445212485608437, 1.388486266691544957 ) ) ;
#156763=CARTESIAN_POINT ( 'NONE',  ( 3.104851637799400876, -0.3563606998662186554, 1.806257425991746546 ) ) ;
#156767=CARTESIAN_POINT ( 'NONE',  ( 0.1293586867831516274, -1.054425554818343880, -1.365251215659948558 ) ) ;
#156770=CARTESIAN_POINT ( 'NONE',  ( 6.473497647428577473, 2.167417048064937291, -0.6491153028224846411 ) ) ;
#156771=CARTESIAN_POINT ( 'NONE',  ( 1.735132801782751200, 0.2076089413485527335, 2.095809512812545350 ) ) ;
#156781=CARTESIAN_POINT ( 'NONE',  ( 4.008219027074312990, -0.8479933951243652235, 2.053374474559205520 ) ) ;
#156782=CARTESIAN_POINT ( 'NONE',  ( 2.326364362698669641, 2.126017103801054464, 0.5310240739047759062 ) ) ;
#156783=CARTESIAN_POINT ( 'NONE',  ( 0.4873205249028254027, -0.2742316277877173691, -2.189713876267186166 ) ) ;
#156785=CARTESIAN_POINT ( 'NONE',  ( 4.562918044398325712, 1.517878595006398212, -1.242988302126393441 ) ) ;
#156789=CARTESIAN_POINT ( 'NONE',  ( 6.610000000000006537, 2.052567036419289614, 2.306714106643445561 ) ) ;
#156792=CARTESIAN_POINT ( 'NONE',  ( 3.023802379225454473, -0.4096935937694180518, 2.080477853870852378 ) ) ;
#156794=CARTESIAN_POINT ( 'NONE',  ( 4.979442225389012933, 2.018306902694905425, -0.7746836383674888804 ) ) ;
#156795=CARTESIAN_POINT ( 'NONE',  ( 4.124425300631988200, 0.09459923933386081563, 1.838956108544815171 ) ) ;
#156798=CARTESIAN_POINT ( 'NONE',  ( 6.703062861115646420, -0.3699031437116198084, 1.706546720392573491 ) ) ;
#156799=CARTESIAN_POINT ( 'NONE',  ( 6.827182134110164391, 0.6048993162116442779, 1.764860727632423076 ) ) ;
#156802=CARTESIAN_POINT ( 'NONE',  ( 3.801785103514757846, -0.6297183656660889639, 2.067937956787009757 ) ) ;
#156804=CARTESIAN_POINT ( 'NONE',  ( 5.114611164699836010, 0.6351010243071940620, -1.913510948406547563 ) ) ;
#156806=CARTESIAN_POINT ( 'NONE',  ( 3.749029689823797806, -1.768526636652943296, 1.242828150824742961 ) ) ;
#156807=CARTESIAN_POINT ( 'NONE',  ( 4.147701676541888816, 0.6670536769024897339, -1.855179015784082619 ) ) ;
#156809=CARTESIAN_POINT ( 'NONE',  ( 0.6402171227658737251, -1.634652429315278654, -1.629011242183490804 ) ) ;
#156810=CARTESIAN_POINT ( 'NONE',  ( 4.147771190963340793, 0.6980094919085011451, -1.939086781881957933 ) ) ;
#156811=CARTESIAN_POINT ( 'NONE',  ( 6.163619218806376310, 1.002299704222510357, 1.663313343435903091 ) ) ;
#156818=CARTESIAN_POINT ( 'NONE',  ( 2.608667852368121043, -0.8438080161984360394, -2.039271889284439254 ) ) ;
#156821=CARTESIAN_POINT ( 'NONE',  ( 6.350445966956749899, -1.952004966925089624, -0.1956573963535559180 ) ) ;
#156822=CARTESIAN_POINT ( 'NONE',  ( -0.02900071798682749002, 0.2267074960015900975, -2.207170277039482986 ) ) ;
#156827=CARTESIAN_POINT ( 'NONE',  ( 5.665905727187005247, -1.164751086281138770, 1.425882759469448979 ) ) ;
#156829=CARTESIAN_POINT ( 'NONE',  ( 2.289980725320222010, -0.8822103741390595610, 1.862666789336121509 ) ) ;
#156835=CARTESIAN_POINT ( 'NONE',  ( 0.5849274615713345726, -0.2514902370338990001, -2.045404637917444646 ) ) ;
#156837=CARTESIAN_POINT ( 'NONE',  ( 4.915489835137424102, -0.9894786724786635013, -1.552603174752004600 ) ) ;
#156844=CARTESIAN_POINT ( 'NONE',  ( 4.090592613104036879, -2.182713160620152859, -0.3248913242878055385 ) ) ;
#156845=CARTESIAN_POINT ( 'NONE',  ( 0.4038910500440278106, -0.5768866637368921246, 2.083095904058133385 ) ) ;
#156847=CARTESIAN_POINT ( 'NONE',  ( 0.4922593472763935329, -1.060406550076501642, 1.591262010887870115 ) ) ;
#156848=CARTESIAN_POINT ( 'NONE',  ( 0.5675926644314840397, 1.357872185771633156, 1.490966652548594285 ) ) ;
#156853=CARTESIAN_POINT ( 'NONE',  ( 0.2329894512427649333, -1.712236961970284632, 0.7538099095961707796 ) ) ;
#156854=CARTESIAN_POINT ( 'NONE',  ( 2.466030083290056130, -1.032479112849067793, 1.731996155473938259 ) ) ;
#156858=CARTESIAN_POINT ( 'NONE',  ( 3.510471945985794928, -0.8535800194418289299, -1.925527614133336840 ) ) ;
#156863=CARTESIAN_POINT ( 'NONE',  ( 4.254169105220822367, 0.8597269205913078416, -1.827796444439087287 ) ) ;
#156866=CARTESIAN_POINT ( 'NONE',  ( 4.464260128311710041, 1.014592192358022338, 1.908665273222116543 ) ) ;
#156872=CARTESIAN_POINT ( 'NONE',  ( 1.627621631281210179, 0.1606834768266463820, -2.165304058017766486 ) ) ;
#156875=CARTESIAN_POINT ( 'NONE',  ( 0.7844012160764175512, 1.623964078452419857, -0.8677550623670119423 ) ) ;
#156877=CARTESIAN_POINT ( 'NONE',  ( 3.228257827484398490, 2.138632370135685523, 0.4780590757816546854 ) ) ;
#156879=CARTESIAN_POINT ( 'NONE',  ( 4.118261297349164352, -1.160217402330826042, -1.942256231939092137 ) ) ;
#156885=CARTESIAN_POINT ( 'NONE',  ( 4.516719421352251906, 1.617689212748760985, 0.7181139158070405371 ) ) ;
#156887=CARTESIAN_POINT ( 'NONE',  ( 1.167171324275569466, -1.903845421566036311, -0.9005605707013781824 ) ) ;
#156890=CARTESIAN_POINT ( 'NONE',  ( 0.5550503504515170716, 1.639475800691666985, -1.091118944626153331 ) ) ;
#156893=CARTESIAN_POINT ( 'NONE',  ( 5.185751641416406876, 1.743707907788614619, -0.4909320375018846883 ) ) ;
#156898=CARTESIAN_POINT ( 'NONE',  ( 4.838664814796108438, 0.3202261158844340039, 1.842872994462002145 ) ) ;
#156900=CARTESIAN_POINT ( 'NONE',  ( 4.873920291170623642, -2.031351322358550870, 0.3986081187722507746 ) ) ;
#156911=CARTESIAN_POINT ( 'NONE',  ( 4.228923158279327410, -1.829750178516520442, -0.7082015076659909925 ) ) ;
#156912=CARTESIAN_POINT ( 'NONE',  ( 2.302111043707856020, -1.802142186715177674, 0.9039695891032775155 ) ) ;
#156917=CARTESIAN_POINT ( 'NONE',  ( 1.616246341788161622, 1.260175398906153266, -1.382505567627971388 ) ) ;
#156919=CARTESIAN_POINT ( 'NONE',  ( 3.972906070543721579, -1.488974544083881746, 1.355118003239277336 ) ) ;
#156921=CARTESIAN_POINT ( 'NONE',  ( 3.620818518838536004, 0.3129716219542731936, 2.093870907184330221 ) ) ;
#156923=CARTESIAN_POINT ( 'NONE',  ( 5.143061708805018561, -0.2499388813127951525, -2.055141626981969338 ) ) ;
#156925=CARTESIAN_POINT ( 'NONE',  ( 6.650343161644081569, -1.616936162011050948, 1.324992778059615128 ) ) ;
#156927=CARTESIAN_POINT ( 'NONE',  ( 5.684540951402929920, -1.781552174421060064, -0.3977488440568625605 ) ) ;
#156934=CARTESIAN_POINT ( 'NONE',  ( 6.621744163077868173, -0.4141588628726756149, 1.873750786029332316 ) ) ;
#156942=CARTESIAN_POINT ( 'NONE',  ( 5.273064617572334356, 1.777004185780726386, -0.9530273427700783895 ) ) ;
#156947=CARTESIAN_POINT ( 'NONE',  ( 2.782036810173736718, -1.130008284276774022, -1.612816519099938173 ) ) ;
#156948=CARTESIAN_POINT ( 'NONE',  ( 3.427361390312729572, -1.528753972193249933, -1.314983687342549556 ) ) ;
#156950=CARTESIAN_POINT ( 'NONE',  ( 6.727182134110219813, 2.036943547479725058, 2.394510323907019345 ) ) ;
#156951=CARTESIAN_POINT ( 'NONE',  ( 3.961010909407122860, 0.2689195440248594027, -2.174814543647784593 ) ) ;
#156953=CARTESIAN_POINT ( 'NONE',  ( 3.047785661706010174, 0.6947733606382737737, -1.796906316042534923 ) ) ;
#156965=CARTESIAN_POINT ( 'NONE',  ( 5.759284750224211713, 1.812880138157666465, -0.3211251414683007899 ) ) ;
#156966=CARTESIAN_POINT ( 'NONE',  ( 2.385404357411140541, 0.09669159202466531822, -2.010876702762071311 ) ) ;
#156967=CARTESIAN_POINT ( 'NONE',  ( 5.396019846235262207, 0.1618137187183350256, 2.292739235009821908 ) ) ;
#156969=CARTESIAN_POINT ( 'NONE',  ( 2.781907013001069906, -1.067198605185412763, -1.524341717138616215 ) ) ;
#156976=CARTESIAN_POINT ( 'NONE',  ( 6.497611715980437630, -2.090283427287362272, 0.05178676472679385329 ) ) ;
#156982=CARTESIAN_POINT ( 'NONE',  ( 5.830603237517035353, 1.664100180626144398, 0.4535787370015566533 ) ) ;
#156985=CARTESIAN_POINT ( 'NONE',  ( 1.705275228087951955, 1.618143048327233435, 0.6241232001420042863 ) ) ;
#156989=CARTESIAN_POINT ( 'NONE',  ( 6.192256317468841864, 1.077302059837774273, -1.884901478735945046 ) ) ;
#156991=CARTESIAN_POINT ( 'NONE',  ( 4.758326833623739205, 0.7015320795021735556, 1.685726030614169924 ) ) ;
#156992=CARTESIAN_POINT ( 'NONE',  ( 1.990992145637654698, 0.1870960246039363450, 1.952785824368876932 ) ) ;
#156996=CARTESIAN_POINT ( 'NONE',  ( 3.194099758881031814, 1.346771490053525033, 1.637864368873870990 ) ) ;
#157000=CARTESIAN_POINT ( 'NONE',  ( 1.463825199929311260, -0.5068179562870354093, 2.007114080642191656 ) ) ;
#157003=CARTESIAN_POINT ( 'NONE',  ( 3.633611385093922674, -0.1624337102359394436, 2.215399726503309630 ) ) ;
#157005=CARTESIAN_POINT ( 'NONE',  ( 1.337049673779285852, 0.6609975811289883207, -2.201632501652720286 ) ) ;
#157007=CARTESIAN_POINT ( 'NONE',  ( 6.262562444065095768, -0.7369429887811511648, -1.926613908347002413 ) ) ;
#157015=CARTESIAN_POINT ( 'NONE',  ( -0.1102773484824119132, 0.6802821481026833927, -2.283667859588431881 ) ) ;
#157016=CARTESIAN_POINT ( 'NONE',  ( 2.678358392608829686, -1.649718294651691730, -0.5031959223205755283 ) ) ;
#157017=CARTESIAN_POINT ( 'NONE',  ( 2.325407997918966796, -1.497503195670712328, -1.350734289967000512 ) ) ;
#157018=CARTESIAN_POINT ( 'NONE',  ( 3.954570948191834745, 0.8096313216635497856, 2.112761250790657908 ) ) ;
#157019=CARTESIAN_POINT ( 'NONE',  ( 5.830723289215218763, 2.029276893092274658, 0.5632808350878695247 ) ) ;
#157021=CARTESIAN_POINT ( 'NONE',  ( 4.042088942692352305, 1.761052656288846663, 0.1752445044498444349 ) ) ;
#157023=CARTESIAN_POINT ( 'NONE',  ( 6.181209693220585777, 1.577568176048673720, 1.663411239723869173 ) ) ;
#157025=CARTESIAN_POINT ( 'NONE',  ( 5.244037021109955177, 0.5378974813256987009, 1.760811445753920346 ) ) ;
#157028=CARTESIAN_POINT ( 'NONE',  ( 5.929655999079198381, 1.083026401007038952, -1.905042663481799403 ) ) ;
#157030=CARTESIAN_POINT ( 'NONE',  ( 5.512195382060368409, 2.068158883198469855, -0.09793725168850964113 ) ) ;
#157033=CARTESIAN_POINT ( 'NONE',  ( 3.914609504329464418, 1.361597497701543480, -1.363134563274936761 ) ) ;
#157036=CARTESIAN_POINT ( 'NONE',  ( -0.08724509969064601911, -2.221098688967707790, -0.04574986941241648841 ) ) ;
#157046=CARTESIAN_POINT ( 'NONE',  ( 1.627322669196319849, 0.1476378700930695564, -1.956383933670035713 ) ) ;
#157050=CARTESIAN_POINT ( 'NONE',  ( 5.424254290899477304, 0.9654600744411747648, 1.707767180430696641 ) ) ;
#157053=CARTESIAN_POINT ( 'NONE',  ( 0.4798239446817476606, 2.109833986122396254, -0.8175194613929820386 ) ) ;
#157054=CARTESIAN_POINT ( 'NONE',  ( -0.2106725631049838343, 0.7236243445625335502, -2.087119268998542942 ) ) ;
#157057=CARTESIAN_POINT ( 'NONE',  ( 0.5966796567213605851, 1.558732183387041781, -1.033768272189788950 ) ) ;
#157058=CARTESIAN_POINT ( 'NONE',  ( 0.4395775532227184090, -1.463650450414313520, -0.9296597220836488873 ) ) ;
#157061=CARTESIAN_POINT ( 'NONE',  ( 3.333693798916517625, 0.9835563995168915552, -1.958507884819527867 ) ) ;
#157062=CARTESIAN_POINT ( 'NONE',  ( 5.016800025512162975, 1.595470874386342608, -1.667385368739245255 ) ) ;
#157063=CARTESIAN_POINT ( 'NONE',  ( 0.5321925127804688627, 1.059884587108523402, -1.767317575122410167 ) ) ;
#157064=CARTESIAN_POINT ( 'NONE',  ( 2.220557385006210804, 0.0001418518128949025625, 1.942124712491780869 ) ) ;
#157067=CARTESIAN_POINT ( 'NONE',  ( 5.097945154717048233, 1.425953928781589886, 1.569717048080176314 ) ) ;
#157069=CARTESIAN_POINT ( 'NONE',  ( 3.973279856364997809, -1.994869694282218386, -0.2930714778977619450 ) ) ;
#157073=CARTESIAN_POINT ( 'NONE',  ( 1.101864800459760207, -1.825872481749410525, -0.002338443969775172437 ) ) ;
#157078=CARTESIAN_POINT ( 'NONE',  ( 5.383688703920392449, 1.382483038487541283, 1.528581890270568122 ) ) ;
#157083=CARTESIAN_POINT ( 'NONE',  ( 4.934242777533356161, -1.082215927170935954, -1.705062858592779174 ) ) ;
#157084=CARTESIAN_POINT ( 'NONE',  ( 5.408899451717416262, -0.5379699361975317506, -2.155043070319954790 ) ) ;
#157088=CARTESIAN_POINT ( 'NONE',  ( 3.696211625926352440, -2.058462806815289259, -0.1027275840673105151 ) ) ;
#157089=CARTESIAN_POINT ( 'NONE',  ( 3.938125092175647879, -1.678004675797317713, -1.117833462672225497 ) ) ;
#157096=CARTESIAN_POINT ( 'NONE',  ( 3.479842141819572632, 1.821463063354014533, 0.8645922719773959653 ) ) ;
#157097=CARTESIAN_POINT ( 'NONE',  ( 2.396224210035051261, 1.478860665732561586, -1.096489538662905217 ) ) ;
#157098=CARTESIAN_POINT ( 'NONE',  ( 1.208152727780729130, -0.5562822606778123902, 2.239534654701015981 ) ) ;
#157100=CARTESIAN_POINT ( 'NONE',  ( 3.585389192675687564, 1.955840111083558597, -0.9206723451176119788 ) ) ;
#157102=CARTESIAN_POINT ( 'NONE',  ( 3.673487740190139572, -0.9280425899400122081, -2.102842487114229275 ) ) ;
#157104=CARTESIAN_POINT ( 'NONE',  ( -0.02244404828157658613, -0.004869073801674199918, -2.189079685368473527 ) ) ;
#157105=CARTESIAN_POINT ( 'NONE',  ( 1.885419139999934934, 1.287927767047767125, 1.356919574424742203 ) ) ;
#157107=CARTESIAN_POINT ( 'NONE',  ( 5.717641559312711230, -1.923570962979544330, 0.4312651734501466994 ) ) ;
#157112=CARTESIAN_POINT ( 'NONE',  ( 0.8388348947251201837, 2.174866457552121268, 0.3736606161612308630 ) ) ;
#157117=CARTESIAN_POINT ( 'NONE',  ( 6.596557512146871360, -0.5253642993188823995, -1.900122941938019450 ) ) ;
#157118=CARTESIAN_POINT ( 'NONE',  ( 5.391387774523593635, 2.037479383949382772, -1.083606018200606869 ) ) ;
#157119=CARTESIAN_POINT ( 'NONE',  ( 6.303157624210896870, -1.571610030290017557, 0.9964359807085266807 ) ) ;
#157120=CARTESIAN_POINT ( 'NONE',  ( 3.168856051829985532, 1.497182195067780386, -1.418930203433153903 ) ) ;
#157127=CARTESIAN_POINT ( 'NONE',  ( 5.072805357664615045, 1.500764584350265718, -1.569201701505947844 ) ) ;
#157130=CARTESIAN_POINT ( 'NONE',  ( 4.599059095968327071, -0.4863373063577690059, 1.775805238918099382 ) ) ;
#157132=CARTESIAN_POINT ( 'NONE',  ( 6.720655732516610747, 3.700489942686377098, 2.440724243369211788 ) ) ;
#157135=CARTESIAN_POINT ( 'NONE',  ( 0.8610526709191126393, -1.638059776709074322, 1.560773681941391100 ) ) ;
#157140=CARTESIAN_POINT ( 'NONE',  ( 0.3461628310420067356, 0.9829124436787043395, -1.640176041098049264 ) ) ;
#157141=CARTESIAN_POINT ( 'NONE',  ( 1.973191454406374890, 1.694654629526294087, -0.5103889506637182549 ) ) ;
#157142=CARTESIAN_POINT ( 'NONE',  ( 5.057293878089731187, -1.725371964895198840, 1.036928162195766889 ) ) ;
#157144=CARTESIAN_POINT ( 'NONE',  ( 4.137795317726181032, -1.450671198928995098, -1.526879382678330010 ) ) ;
#157146=CARTESIAN_POINT ( 'NONE',  ( 3.075699878008768096, -0.7735687425090407299, 1.752645402151173926 ) ) ;
#157148=CARTESIAN_POINT ( 'NONE',  ( 3.771889708208826075, -1.940809680921409486, 0.3342159591338197400 ) ) ;
#157149=CARTESIAN_POINT ( 'NONE',  ( 0.05319811239242258627, 0.3688592364489845510, 2.088132107045739705 ) ) ;
#157150=EDGE_CURVE ( 'NONE', #202900, #41604, #50979, .T. ) ;
#157151=CARTESIAN_POINT ( 'NONE',  ( 2.869827659178546764, 0.9992216309704025079, 1.581230272166146644 ) ) ;
#157152=CARTESIAN_POINT ( 'NONE',  ( 4.863727610707407223, 1.705404662657764137, -0.2575704655415639310 ) ) ;
#157154=CARTESIAN_POINT ( 'NONE',  ( 2.877765823869771644, 2.095344539500657799, -0.6929138170133213315 ) ) ;
#157157=CARTESIAN_POINT ( 'NONE',  ( 6.848121815800094936, -0.8396676627679277027, 1.771385694100804375 ) ) ;
#157162=CARTESIAN_POINT ( 'NONE',  ( 0.1747926744264660381, 0.006858446013176254172, -1.855468577918440776 ) ) ;
#157165=CARTESIAN_POINT ( 'NONE',  ( 1.715371797147913435, -1.774658612622433296, -1.066089629202723765 ) ) ;
#157169=CARTESIAN_POINT ( 'NONE',  ( 6.621762855810419346, -0.4656160214656123175, 2.076383538966434017 ) ) ;
#157172=CARTESIAN_POINT ( 'NONE',  ( 5.325545996062735377, -1.462220743079494012, 1.388274341532859335 ) ) ;
#157173=CARTESIAN_POINT ( 'NONE',  ( 4.751152363292252545, 0.1813030634821456710, -1.907091066879146757 ) ) ;
#157175=CARTESIAN_POINT ( 'NONE',  ( 2.648187065138879692, 0.7411268365287644322, 2.062558662443473523 ) ) ;
#157177=CARTESIAN_POINT ( 'NONE',  ( 2.970861089138315592, -1.445268511421276214, 1.252435071843561731 ) ) ;
#157179=CARTESIAN_POINT ( 'NONE',  ( 0.2457205463545810431, 1.994068899247893434, -0.2986513045247774500 ) ) ;
#157181=CARTESIAN_POINT ( 'NONE',  ( 3.579701903670178709, -1.028438467219190411, 1.820211688285853446 ) ) ;
#157183=CARTESIAN_POINT ( 'NONE',  ( 2.625662686473359653, -0.9909224867145174365, -1.411489731159983219 ) ) ;
#157194=CARTESIAN_POINT ( 'NONE',  ( 3.053145041208281452, -1.596494782498259157, 0.8559496646718143253 ) ) ;
#157198=CARTESIAN_POINT ( 'NONE',  ( 3.879414023784663712, 0.2179053609261162039, -1.798230022952992613 ) ) ;
#157199=CARTESIAN_POINT ( 'NONE',  ( 6.539320575229256249, 6.037491965140660000, 2.591644950450102680 ) ) ;
#157202=CARTESIAN_POINT ( 'NONE',  ( 4.263987252221818736, -1.856165113571141445, 0.1354236832897796894 ) ) ;
#157204=CARTESIAN_POINT ( 'NONE',  ( 1.880356884260485195, -0.5129869988758984922, -1.845544782535366801 ) ) ;
#157205=CARTESIAN_POINT ( 'NONE',  ( 1.201864610381056853, -1.825762228264395048, -0.004348209057210283834 ) ) ;
#157206=CIRCLE ( 'NONE', #184833, 0.05000000000000109912 ) ;
#157213=AXIS2_PLACEMENT_3D ( 'NONE', #180106, #97803, #14375 ) ;
#157215=CARTESIAN_POINT ( 'NONE',  ( 6.244967536942622743, -0.2852903188887367936, -1.948516424197583197 ) ) ;
#157217=CARTESIAN_POINT ( 'NONE',  ( 0.1105426557568081891, -0.9253945370547181914, -1.951590883024490353 ) ) ;
#157218=CARTESIAN_POINT ( 'NONE',  ( 1.377023180242874068, 1.931088066391934976, -0.8015266744223081830 ) ) ;
#157219=CARTESIAN_POINT ( 'NONE',  ( 6.633821588623410648, -1.258873362295178655, -1.458256629947017879 ) ) ;
#157221=CARTESIAN_POINT ( 'NONE',  ( 1.043660158496478196, 0.7440559408637310579, -1.667260813828251642 ) ) ;
#157222=CARTESIAN_POINT ( 'NONE',  ( 3.510573375967055654, -0.8941257848905452832, -2.017821460644920073 ) ) ;
#157225=CARTESIAN_POINT ( 'NONE',  ( 0.5625819312903357350, 0.5574351770905332515, 1.829310545699929458 ) ) ;
#157228=CARTESIAN_POINT ( 'NONE',  ( 1.521857752106166695, 1.940948540861246352, -0.3334180107718246466 ) ) ;
#157229=CARTESIAN_POINT ( 'NONE',  ( 2.665492718168083641, 1.041058713608807418, 1.639284265488485381 ) ) ;
#157233=CARTESIAN_POINT ( 'NONE',  ( 6.209776894639321476, 0.5414253987558427239, -1.780396208465367280 ) ) ;
#157238=CARTESIAN_POINT ( 'NONE',  ( 2.085717061910817183, -0.9337068281064246911, 1.982830571388309204 ) ) ;
#157242=CARTESIAN_POINT ( 'NONE',  ( 2.736711336054332921, 0.2235625380298221498, 1.811883384933578256 ) ) ;
#157248=CARTESIAN_POINT ( 'NONE',  ( 1.910648867733771850, 1.427813452364127045, -1.293523827780170166 ) ) ;
#157249=CARTESIAN_POINT ( 'NONE',  ( 5.524254240939322713, 0.9636562883742012531, 1.708648623189083393 ) ) ;
#157257=CARTESIAN_POINT ( 'NONE',  ( 5.172746982222708567, 1.431596967658786745, -1.495705434250683918 ) ) ;
#157262=CARTESIAN_POINT ( 'NONE',  ( 5.080843078579284189, -0.8290085517158821693, 2.144167039965215071 ) ) ;
#157266=CARTESIAN_POINT ( 'NONE',  ( 0.2172540613933468812, -0.1060665143617581102, 2.289936275665432674 ) ) ;
#157270=CARTESIAN_POINT ( 'NONE',  ( 4.417874594837376101, 1.193482090904834925, -1.531842204047480616 ) ) ;
#157275=CARTESIAN_POINT ( 'NONE',  ( 6.275647926998929371, 0.3200337115364471074, -1.885262484646982095 ) ) ;
#157276=CARTESIAN_POINT ( 'NONE',  ( -0.005825499538506145533, -0.3671160670182890273, -1.691004160741523155 ) ) ;
#157277=CARTESIAN_POINT ( 'NONE',  ( 5.384000029850495750, -2.016708404008683786, 0.004832792792668073358 ) ) ;
#157281=CARTESIAN_POINT ( 'NONE',  ( 2.168024591681999791, -1.285456077792548335, 1.648657952768191715 ) ) ;
#157282=CARTESIAN_POINT ( 'NONE',  ( 0.1096998152198442600, -0.7512755041745984297, -1.601369504124000587 ) ) ;
#157283=CARTESIAN_POINT ( 'NONE',  ( 6.188124994278807023, 1.678003296889327034, 1.117835524071027598 ) ) ;
#157285=CARTESIAN_POINT ( 'NONE',  ( 2.783473570837506017, 1.621738419858234304, 1.620254553110695772 ) ) ;
#157286=CARTESIAN_POINT ( 'NONE',  ( 2.044474178175458068, -1.396829902048246197, -1.037857226380611619 ) ) ;
#157288=CARTESIAN_POINT ( 'NONE',  ( 2.336848640490073237, -1.070562806433389857, 1.363724479458855443 ) ) ;
#157290=CARTESIAN_POINT ( 'NONE',  ( 1.240418688720058560, -1.814558931778247119, -0.4126190233522536444 ) ) ;
#157291=CARTESIAN_POINT ( 'NONE',  ( 2.348295082997472250, -0.9299805079447539535, 1.962071136543291683 ) ) ;
#157292=CARTESIAN_POINT ( 'NONE',  ( 3.573454097414618946, 1.463926983822515293, 1.387100322000796027 ) ) ;
#157293=CARTESIAN_POINT ( 'NONE',  ( 5.062500000000005329, -1.451031289061317064, -1.451031289060909168 ) ) ;
#157295=CARTESIAN_POINT ( 'NONE',  ( 0.6395170938602061650, -1.359983930408629194, -1.364592209491755082 ) ) ;
#157297=CARTESIAN_POINT ( 'NONE',  ( 3.797323596237450971, -0.2205154750010793197, -2.210469098741683514 ) ) ;
#157299=CARTESIAN_POINT ( 'NONE',  ( -0.2108831679771167866, 1.375689764684871808, -2.152500126786048185 ) ) ;
#157303=CARTESIAN_POINT ( 'NONE',  ( 5.801095770108652516, -0.3255204119565913157, -2.197341616521626406 ) ) ;
#157304=CARTESIAN_POINT ( 'NONE',  ( 4.914483161888778540, 0.7490505147796694407, 1.813437088826752142 ) ) ;
#157308=CARTESIAN_POINT ( 'NONE',  ( 6.011039796215681186, 1.991063742206979459, 1.074381780396720165 ) ) ;
#157310=CARTESIAN_POINT ( 'NONE',  ( 2.295447401932719345, -1.843475527790199964, 0.9254330757148797604 ) ) ;
#157315=CARTESIAN_POINT ( 'NONE',  ( 4.376139848268215893, -1.078761963904120602, 1.527931137620001989 ) ) ;
#157316=CARTESIAN_POINT ( 'NONE',  ( 3.269848819717678712, 1.566352396371019973, -0.7445194440909275180 ) ) ;
#157317=CARTESIAN_POINT ( 'NONE',  ( 2.577381053492054264, -0.8929794387350452611, 1.493718712549793715 ) ) ;
#157318=CARTESIAN_POINT ( 'NONE',  ( 0.7675861853312654359, 2.207383698986573162, -0.6181827981695892094 ) ) ;
#157319=CARTESIAN_POINT ( 'NONE',  ( 1.571597221169357628, 0.1616201177277211132, -2.200922231076734459 ) ) ;
#157320=CARTESIAN_POINT ( 'NONE',  ( 4.546477914129923192, -1.678139501482888152, 1.246787890680167710 ) ) ;
#157321=CARTESIAN_POINT ( 'NONE',  ( 5.964781414698055784, 0.1407378593174268555, -1.936906258807554071 ) ) ;
#157323=CARTESIAN_POINT ( 'NONE',  ( 0.2994542103806375200, 1.388483683912977495, -1.462447666687356485 ) ) ;
#157330=CARTESIAN_POINT ( 'NONE',  ( 4.740742070742828496, 0.3150700179065483719, 1.798135100120237251 ) ) ;
#157332=CARTESIAN_POINT ( 'NONE',  ( 1.852830919558448697, 0.6925466627333074499, 2.095365425716289032 ) ) ;
#157340=CARTESIAN_POINT ( 'NONE',  ( 1.019792603244329410, -0.4866989216864863188, 1.960159232486478498 ) ) ;
#157343=CARTESIAN_POINT ( 'NONE',  ( 3.203785720953303606, 0.6742969627455961401, -1.734658892920079243 ) ) ;
#157350=CARTESIAN_POINT ( 'NONE',  ( 4.002439121739418404, -0.5745171773131328985, -1.733004836422600725 ) ) ;
#157354=CARTESIAN_POINT ( 'NONE',  ( 6.890000000000050306, -0.002781820520068867264, 1.999840353888074240 ) ) ;
#157355=CARTESIAN_POINT ( 'NONE',  ( 5.665905727187005247, -1.164751086281138770, 1.425882759469448979 ) ) ;
#157356=CARTESIAN_POINT ( 'NONE',  ( 4.530063604893081575, -1.417328398590127714, -1.821081770091488083 ) ) ;
#157358=CARTESIAN_POINT ( 'NONE',  ( 0.6321923500852930644, 1.061553894661429576, -1.766199267744901658 ) ) ;
#157359=CARTESIAN_POINT ( 'NONE',  ( 5.360842878201462547, -0.8341330746063200241, 2.141841041818067559 ) ) ;
#157363=CARTESIAN_POINT ( 'NONE',  ( 5.787941465827733722, -0.8397648285632768328, 1.671655200917811168 ) ) ;
#157364=CARTESIAN_POINT ( 'NONE',  ( 2.056764645581514728, 0.4224895836346024280, 1.864965418913032913 ) ) ;
#157366=CARTESIAN_POINT ( 'NONE',  ( 3.668774463136436736, -1.482526648764719734, 1.634931011441637771 ) ) ;
#157367=CARTESIAN_POINT ( 'NONE',  ( 4.610634390349757084, 2.027228601534016406, 0.6112464051817678712 ) ) ;
#157369=CARTESIAN_POINT ( 'NONE',  ( 6.883263157960370471, 7.052343128562386987, 2.644342559190917541 ) ) ;
#157370=CARTESIAN_POINT ( 'NONE',  ( -0.2110808730066961458, 1.402160971018800995, -2.056005932258188285 ) ) ;
#157373=CARTESIAN_POINT ( 'NONE',  ( 1.782679935646735769, -1.233298141988391272, 1.950204222970158385 ) ) ;
#157374=CARTESIAN_POINT ( 'NONE',  ( 3.244534624505683418, -1.932379277470747558, -0.3379807920969243873 ) ) ;
#157377=CARTESIAN_POINT ( 'NONE',  ( 6.789892339975323488, -1.342670783288713698, -1.565829586757736758 ) ) ;
#157381=CARTESIAN_POINT ( 'NONE',  ( 4.276577519141481432, -0.4465006364167342645, -1.966305148836451577 ) ) ;
#157388=CARTESIAN_POINT ( 'NONE',  ( 2.167058194802372828, 1.611091607626200961, -1.455523108145313937 ) ) ;
#157391=CARTESIAN_POINT ( 'NONE',  ( 0.7728169288007546989, -1.939476032597256872, -0.6969182633713083552 ) ) ;
#157392=CARTESIAN_POINT ( 'NONE',  ( 0.07755575628183572490, 2.860544851022389867, -2.677061994759164065 ) ) ;
#157395=PLANE ( 'NONE',  #128483 ) ;
#157398=CARTESIAN_POINT ( 'NONE',  ( 3.527896108305649037, -1.883508717751972705, 0.3295761852530054159 ) ) ;
#157399=CARTESIAN_POINT ( 'NONE',  ( 5.260532772634206822, -1.280100971201453497, 1.222426461919926322 ) ) ;
#157404=CARTESIAN_POINT ( 'NONE',  ( 6.081633583971849610, -0.6405020660514448849, 1.805506905929341821 ) ) ;
#157406=CARTESIAN_POINT ( 'NONE',  ( 1.117730493923989599, 0.4056601665377962407, -2.030061024271647252 ) ) ;
#157409=CARTESIAN_POINT ( 'NONE',  ( 6.438356904408193415, 1.850619875698428674, 0.2722718653145329015 ) ) ;
#157410=CARTESIAN_POINT ( 'NONE',  ( 1.998415063578623085, -0.4859047700337820741, -1.759764234465097221 ) ) ;
#157411=CARTESIAN_POINT ( 'NONE',  ( 5.584669497696876483, -2.152379054646291756, -0.4867646435422824935 ) ) ;
#157414=CARTESIAN_POINT ( 'NONE',  ( 3.420431513525914902, 0.9250737872015384333, 1.843656989716379035 ) ) ;
#157418=CARTESIAN_POINT ( 'NONE',  ( 0.5620833348847533717, 2.138143771118843350, -0.3165822943479515983 ) ) ;
#157420=CARTESIAN_POINT ( 'NONE',  ( 4.932118098221458524, 1.189261692661430114, 1.694535115018414917 ) ) ;
#157422=CARTESIAN_POINT ( 'NONE',  ( 3.304151629394710632, -2.159270932758147854, 0.1024373671053082913 ) ) ;
#157424=CARTESIAN_POINT ( 'NONE',  ( 3.088540408894335787, -1.201353318763114020, 1.623377594596470352 ) ) ;
#157425=CARTESIAN_POINT ( 'NONE',  ( 2.558977423257744022, 1.577441344615847951, -1.166261179026031325 ) ) ;
#157426=CARTESIAN_POINT ( 'NONE',  ( 6.720655732516665815, 6.034026441762381232, 2.768628153821062199 ) ) ;
#157432=CARTESIAN_POINT ( 'NONE',  ( 1.692592581891849912, 1.490968054865527304, -1.357870634957742961 ) ) ;
#157434=CARTESIAN_POINT ( 'NONE',  ( 6.356982542327763497, 0.3766756592470664744, -2.158781491689326426 ) ) ;
#157436=CARTESIAN_POINT ( 'NONE',  ( 5.431871263539022721, -1.864374737420209760, 0.4251265778823994368 ) ) ;
#157440=CARTESIAN_POINT ( 'NONE',  ( 3.304314702139679039, 1.277028363417181289, -1.560513873864778578 ) ) ;
#157443=CARTESIAN_POINT ( 'NONE',  ( 6.247054435025749086, -1.454095476552646593, 0.9272665607438534963 ) ) ;
#157447=CARTESIAN_POINT ( 'NONE',  ( 4.323419078940895943, -1.790677508454678657, 0.5408235849187342792 ) ) ;
#157449=CARTESIAN_POINT ( 'NONE',  ( 2.395452669547156077, -1.851176756146424074, 0.9269567275110508486 ) ) ;
#157455=CARTESIAN_POINT ( 'NONE',  ( 0.2459857770662046417, 0.9310377468562742731, -1.553837941864342875 ) ) ;
#157460=CARTESIAN_POINT ( 'NONE',  ( 1.996468121258226924, 1.940055844723225009, 0.2909814450420752929 ) ) ;
#157462=CARTESIAN_POINT ( 'NONE',  ( 6.310162246266422414, 1.098484216484491904, -1.569160930707512502 ) ) ;
#157469=CARTESIAN_POINT ( 'NONE',  ( 2.659225025413253007, -1.880336703546074073, -1.066323988048664795 ) ) ;
#157473=CARTESIAN_POINT ( 'NONE',  ( 5.561492448144861989, 0.3540975402388062410, -1.790731494587729067 ) ) ;
#157476=CARTESIAN_POINT ( 'NONE',  ( 0.9660189047021714437, 0.9680410686894457273, 1.717217487461615955 ) ) ;
#157477=CARTESIAN_POINT ( 'NONE',  ( 3.814637755342592307, -0.6046605605216844870, -1.814329123173196834 ) ) ;
#157480=CARTESIAN_POINT ( 'NONE',  ( 5.476995390384709061, 1.819097369218507732, 0.7554879866787550524 ) ) ;
#157482=CARTESIAN_POINT ( 'NONE',  ( 5.917518263527802524, -1.082453682572570797, -1.612232301441741233 ) ) ;
#157489=CARTESIAN_POINT ( 'NONE',  ( 4.477155480220369910, -1.709698060584059043, -0.8567103784868701499 ) ) ;
#157491=CARTESIAN_POINT ( 'NONE',  ( 0.4291286860223575972, 2.112415399404877547, 0.6383354507134838540 ) ) ;
#157493=CARTESIAN_POINT ( 'NONE',  ( 6.569000952640477564, -1.554625895936670554, 1.278542242695315689 ) ) ;
#157495=CARTESIAN_POINT ( 'NONE',  ( 6.692070433991195166, -0.7751425012093198230, 1.651373049820707317 ) ) ;
#157496=CARTESIAN_POINT ( 'NONE',  ( 2.119664376568120012, 0.3561266789769075292, -2.039353370234835872 ) ) ;
#157500=CARTESIAN_POINT ( 'NONE',  ( 6.491075539335432687, 1.626419376453295706, -0.9240138038444989377 ) ) ;
#157505=CARTESIAN_POINT ( 'NONE',  ( 6.925078400183578786, 2.094238355957972253, 2.065574651578235610 ) ) ;
#157508=CARTESIAN_POINT ( 'NONE',  ( 5.027816288645148290, -1.483603310789272323, 0.8976219912088311270 ) ) ;
#157510=CARTESIAN_POINT ( 'NONE',  ( 2.289971195246335078, -1.349064171463711936, -1.570471239911851669 ) ) ;
#157511=CARTESIAN_POINT ( 'NONE',  ( 3.251669871774115705, 2.065089526129770814, -0.4662906127247400945 ) ) ;
#157514=CARTESIAN_POINT ( 'NONE',  ( 2.008593398387849671, 0.6130636034600014383, 1.871695086544410636 ) ) ;
#157517=CARTESIAN_POINT ( 'NONE',  ( 0.2285749388857594433, 1.317234250586714284, -1.386657971642536014 ) ) ;
#157518=CARTESIAN_POINT ( 'NONE',  ( 3.890815911290066875, 1.937189890886330756, -1.225201777657213498 ) ) ;
#157519=CARTESIAN_POINT ( 'NONE',  ( 1.717148762710469789, -0.2249250470785572054, 1.811706739299999924 ) ) ;
#157524=CARTESIAN_POINT ( 'NONE',  ( 2.830340462983381489, -0.9960867002655849900, -1.749474899777081704 ) ) ;
#157525=CARTESIAN_POINT ( 'NONE',  ( 1.850371385673426294, -1.951817131159512719, -0.1975377159662907445 ) ) ;
#157530=CARTESIAN_POINT ( 'NONE',  ( 5.349593081218750434, 2.088290806564324420, -0.1017214290881287009 ) ) ;
#157531=CARTESIAN_POINT ( 'NONE',  ( 4.856192259477753126, 0.6790438925599675546, 1.634599669825251178 ) ) ;
#157533=CARTESIAN_POINT ( 'NONE',  ( 1.166276502169643070, -1.387892208999995436, 1.695937554688830451 ) ) ;
#157534=CARTESIAN_POINT ( 'NONE',  ( 5.560439297528310121, -1.575983010118024774, -0.7385839837668640717 ) ) ;
#157536=CARTESIAN_POINT ( 'NONE',  ( 0.1331715793776782342, 4.090830978607494117, -2.508370148267160538 ) ) ;
#157537=CARTESIAN_POINT ( 'NONE',  ( 6.100222456320119058, -0.2858642287353658218, 2.280774976835740819 ) ) ;
#157538=CARTESIAN_POINT ( 'NONE',  ( 6.081315976822482483, 1.162057296412899676, -1.286934115659829736 ) ) ;
#157539=CARTESIAN_POINT ( 'NONE',  ( 5.512245374570181156, 2.168932156859445737, -0.1011643165890318136 ) ) ;
#157541=CARTESIAN_POINT ( 'NONE',  ( 0.2513570338038995100, 0.2008850299538050832, -2.107768975555255331 ) ) ;
#157542=CARTESIAN_POINT ( 'NONE',  ( 3.937500000000001776, 1.451031289060957574, -1.451031289061275320 ) ) ;
#157545=CARTESIAN_POINT ( 'NONE',  ( 4.928697230495170167, 1.843396615675118699, 0.5593075106890015302 ) ) ;
#157547=CARTESIAN_POINT ( 'NONE',  ( 0.6630925397578091296, 0.6502370396846578471, 2.123993688044391259 ) ) ;
#157552=CARTESIAN_POINT ( 'NONE',  ( 2.438390712420679396, -1.281362850324974989, -1.814285216940268342 ) ) ;
#157559=CARTESIAN_POINT ( 'NONE',  ( 0.7213275451133926985, 1.987047012402185731, 0.3419330716275259530 ) ) ;
#157561=CARTESIAN_POINT ( 'NONE',  ( 0.3739784900498700493, -2.023488180542520887, 0.3987778971655773219 ) ) ;
#157566=CARTESIAN_POINT ( 'NONE',  ( 1.844620604044054035, -1.498293487275937697, 0.9415191625909284934 ) ) ;
#157567=CARTESIAN_POINT ( 'NONE',  ( 0.7389079861009685279, 2.013985778099684154, -0.1017531103126300962 ) ) ;
#157568=CARTESIAN_POINT ( 'NONE',  ( 5.530708837500646347, -1.570004293196942013, 0.7514903552788397834 ) ) ;
#157569=CARTESIAN_POINT ( 'NONE',  ( 3.720531229262864947, 2.177046216224611364, 0.7181995365407625176 ) ) ;
#157571=CARTESIAN_POINT ( 'NONE',  ( 2.765369989423609454, 0.9851603262180377296, 1.555203531693909680 ) ) ;
#157574=CARTESIAN_POINT ( 'NONE',  ( 2.819161699164650869, -0.1809198688003388622, 1.816599095187728219 ) ) ;
#157575=CARTESIAN_POINT ( 'NONE',  ( 3.533827422916273164, -1.646839391163470223, 1.163268690995450383 ) ) ;
#157577=CARTESIAN_POINT ( 'NONE',  ( 2.466018556964240549, 2.218949015226141963, -0.4410763869808070337 ) ) ;
#157579=CARTESIAN_POINT ( 'NONE',  ( 5.719784389160836646, -2.055351168476500234, 0.4581721925015455610 ) ) ;
#157581=CARTESIAN_POINT ( 'NONE',  ( 2.453653613718423276, 1.598880132357576755, 1.315258840600006085 ) ) ;
#157584=CARTESIAN_POINT ( 'NONE',  ( 4.406960118137589255, -0.4655763551070742912, -2.068578822641816473 ) ) ;
#157587=CARTESIAN_POINT ( 'NONE',  ( 1.400868510093127073, 1.575373640256217733, -1.108617158386180357 ) ) ;
#157594=CARTESIAN_POINT ( 'NONE',  ( -0.08724509969064601911, -2.221098688967707790, -0.04574986941241648841 ) ) ;
#157595=CARTESIAN_POINT ( 'NONE',  ( 2.678859613419749763, -2.014854250346362008, -0.6126693332187698182 ) ) ;
#157598=CARTESIAN_POINT ( 'NONE',  ( 6.684420909863875160, 1.071953792136259187, -1.520962823361602601 ) ) ;
#157603=CARTESIAN_POINT ( 'NONE',  ( 0.4047333657465709278, -2.105317319661216047, -0.2534319464195868843 ) ) ;
#157605=CARTESIAN_POINT ( 'NONE',  ( 3.842202535371820993, -0.9690557767615382012, 1.705768119890891610 ) ) ;
#157606=CARTESIAN_POINT ( 'NONE',  ( 2.202237438260604030, -2.161223104231101644, 0.05255616829508147347 ) ) ;
#157610=CARTESIAN_POINT ( 'NONE',  ( 3.028976774107559944, -1.169381637243168903, -1.289075744332576878 ) ) ;
#157614=CARTESIAN_POINT ( 'NONE',  ( 1.897814322125553010, 0.1948091626960517242, 2.006652841580962132 ) ) ;
#157615=CARTESIAN_POINT ( 'NONE',  ( 6.825078400183579141, 1.241995729952071637, 2.258014901253778461 ) ) ;
#157617=CARTESIAN_POINT ( 'NONE',  ( 2.711746521272298871, -1.950232680175187250, 0.2877518621813393018 ) ) ;
#157618=CARTESIAN_POINT ( 'NONE',  ( 5.572493885891085519, 0.7809320506734825917, 1.745880147543739325 ) ) ;
#157623=CARTESIAN_POINT ( 'NONE',  ( 2.279949990775688384, 1.980252038983502993, -0.3961774098769352825 ) ) ;
#157625=CARTESIAN_POINT ( 'NONE',  ( 5.948310197725324322, 2.304532173486303570, 0.1212388396696506970 ) ) ;
#157626=CARTESIAN_POINT ( 'NONE',  ( 6.689906388054261299, -1.280585065398877731, -1.486383542710856043 ) ) ;
#157627=CARTESIAN_POINT ( 'NONE',  ( 2.448037131198562921, -0.8433605282326918084, 1.771390271482737200 ) ) ;
#157629=CARTESIAN_POINT ( 'NONE',  ( 0.8092204703840089053, 1.198858234535697065, -1.621184076614573533 ) ) ;
#157631=CARTESIAN_POINT ( 'NONE',  ( 2.852857698155007782, -1.958159313504294730, -0.8059144277542380497 ) ) ;
#157634=CARTESIAN_POINT ( 'NONE',  ( 2.238008233095424515, 0.4029187984595939409, 1.796341404040911804 ) ) ;
#157638=CARTESIAN_POINT ( 'NONE',  ( 2.795306286867365486, -0.1602278063087131110, -2.114629986603839829 ) ) ;
#157639=CARTESIAN_POINT ( 'NONE',  ( 0.7437973067255730930, 0.5320827018340993364, 1.762565881533173950 ) ) ;
#157643=CARTESIAN_POINT ( 'NONE',  ( 4.182927011504236070, -0.1980092267137799622, -2.051220347156012647 ) ) ;
#157645=CARTESIAN_POINT ( 'NONE',  ( 1.804012939494209267, 1.363607186100148638, -1.237405090928713092 ) ) ;
#157647=CARTESIAN_POINT ( 'NONE',  ( -0.02244404828157658613, 5.719765766439059540, -2.783169749654360814 ) ) ;
#157650=CARTESIAN_POINT ( 'NONE',  ( 1.295869073816724226, 1.673045085319382119, 1.439284050222865652 ) ) ;
#157651=CARTESIAN_POINT ( 'NONE',  ( 2.776973401877864234, -2.164208356635976216, -0.6592219059844570683 ) ) ;
#157653=CARTESIAN_POINT ( 'NONE',  ( 3.603588835282888869, 1.315886683649561295, 1.245372468285299128 ) ) ;
#157654=CARTESIAN_POINT ( 'NONE',  ( 3.204202018521628226, 1.211454676919420326, -1.484069150048252350 ) ) ;
#157655=CARTESIAN_POINT ( 'NONE',  ( 4.650872726564402981, -0.4503784926754761386, -2.020631409805350387 ) ) ;
#157658=CARTESIAN_POINT ( 'NONE',  ( 2.307442625383813617, -0.4335913300187159702, 1.923040929009907973 ) ) ;
#157659=CARTESIAN_POINT ( 'NONE',  ( 0.6570953225405625764, -1.625623130003026606, -1.033337472089399078 ) ) ;
#157660=CARTESIAN_POINT ( 'NONE',  ( 3.924554409752772699, 1.776107677202539925, 0.5873546117282567591 ) ) ;
#157661=CARTESIAN_POINT ( 'NONE',  ( 2.210004991130873453, -0.5033687547432836862, 2.251983625769232500 ) ) ;
#157662=CARTESIAN_POINT ( 'NONE',  ( 3.560865204049929122, 1.468383728701172064, -1.143307097947023010 ) ) ;
#157667=CARTESIAN_POINT ( 'NONE',  ( 0.9617104568129207776, 0.4090027284681818642, -2.065791855309044411 ) ) ;
#157672=CARTESIAN_POINT ( 'NONE',  ( 2.408575119285644384, -2.115224228095522907, -0.1514441693673748146 ) ) ;
#157673=CARTESIAN_POINT ( 'NONE',  ( 6.393224328948585722, -0.1011241736039915490, -2.017280362314947340 ) ) ;
#157677=CARTESIAN_POINT ( 'NONE',  ( 1.019082891775088484, 1.996809913787592095, 0.8282600050937348746 ) ) ;
#157683=CARTESIAN_POINT ( 'NONE',  ( 5.823453932400854960, -1.463924103857511039, -1.387103351090559711 ) ) ;
#157687=CARTESIAN_POINT ( 'NONE',  ( 0.09312846265441956928, -0.5046389715205062965, -2.214118724221309620 ) ) ;
#157691=CARTESIAN_POINT ( 'NONE',  ( 6.556263154800559434, -1.238474754573845038, 1.591913907798309991 ) ) ;
#157695=DIRECTION ( 'NONE',  ( -1.000000000000000000, 1.016547956922408957E-15, 1.479114432388267300E-31 ) ) ;
#157696=CARTESIAN_POINT ( 'NONE',  ( 3.211258912624019857, -0.3355696072399985685, 1.691725950409156631 ) ) ;
#157699=CARTESIAN_POINT ( 'NONE',  ( 0.7195362622018970367, -0.9397137143956849625, -1.499438161327722341 ) ) ;
#157700=CARTESIAN_POINT ( 'NONE',  ( 1.401040355039730345, -0.2976371227399738917, -1.990864243493442709 ) ) ;
#157702=CARTESIAN_POINT ( 'NONE',  ( 3.997267248050282884, 1.865803599355109421, -1.178106810156675843 ) ) ;
#157706=CARTESIAN_POINT ( 'NONE',  ( 4.283913115580790354, 2.056533504189705930, -0.5163123687341104606 ) ) ;
#157707=CARTESIAN_POINT ( 'NONE',  ( 2.864861414439429321, -0.1511590275467006583, -2.010826137130202529 ) ) ;
#157708=CARTESIAN_POINT ( 'NONE',  ( 3.796947700133224135, -0.1831754980210500150, -1.802320314001674806 ) ) ;
#157709=VERTEX_POINT ( 'NONE', #122435 ) ;
#157712=CARTESIAN_POINT ( 'NONE',  ( 0.7603692911175019553, -1.357789551990191246, 1.287012767582619510 ) ) ;
#157714=CARTESIAN_POINT ( 'NONE',  ( 6.164658409365947556, -1.287482145768016339, 1.294691480910937775 ) ) ;
#157717=CARTESIAN_POINT ( 'NONE',  ( 2.413182783470344983, -1.785834301256707723, 0.6938157933340273198 ) ) ;
#157727=CARTESIAN_POINT ( 'NONE',  ( 3.428091063814618700, -2.088597262255381448, 0.3661859999234198249 ) ) ;
#157728=CARTESIAN_POINT ( 'NONE',  ( -0.1296875068448125057, 1.390030859318210688, -2.083197486262199138 ) ) ;
#157730=CARTESIAN_POINT ( 'NONE',  ( 4.903572647403447782, -0.5284346980384787562, 1.899126047080600621 ) ) ;
#157731=CARTESIAN_POINT ( 'NONE',  ( 0.2287712656204986261, 1.385237311202421662, -1.461098210751586857 ) ) ;
#157733=CARTESIAN_POINT ( 'NONE',  ( 6.350787976822619640, -1.936633936377421206, -0.8562603515115329023 ) ) ;
#157735=CARTESIAN_POINT ( 'NONE',  ( 1.961466609329724164, 1.720096886549182136, 1.151944459977225055 ) ) ;
#157736=CARTESIAN_POINT ( 'NONE',  ( 3.046748965309022505, -1.587984067068026528, -1.117546226756223726 ) ) ;
#157739=CARTESIAN_POINT ( 'NONE',  ( 3.433613042289254569, 0.9395709039844526433, -1.867677030932006765 ) ) ;
#157742=CARTESIAN_POINT ( 'NONE',  ( 1.013979471798792886, -1.811656969585205612, -0.0007847632289004204901 ) ) ;
#157744=CARTESIAN_POINT ( 'NONE',  ( 5.549527019956425278, -1.737703232767298545, -1.360318885177333570 ) ) ;
#157746=CARTESIAN_POINT ( 'NONE',  ( 3.786314268594536347, -1.089870966172037825, 1.918795532666245363 ) ) ;
#157749=CARTESIAN_POINT ( 'NONE',  ( 3.053266463924544372, -1.685387242695039811, 0.9035085923766730254 ) ) ;
#157751=CARTESIAN_POINT ( 'NONE',  ( 5.336411075974297979, -1.153114810915600641, 1.719314882265559286 ) ) ;
#157753=CARTESIAN_POINT ( 'NONE',  ( 2.975616057669258741, 2.053088362031017855, -0.6768339029224537118 ) ) ;
#157754=CARTESIAN_POINT ( 'NONE',  ( 4.300438532332786501, 1.693616701070689956, -1.390861761948622766 ) ) ;
#157762=CARTESIAN_POINT ( 'NONE',  ( 6.262565978045822490, -0.7396069823457154246, -1.933831554736538338 ) ) ;
#157763=CARTESIAN_POINT ( 'NONE',  ( 4.793539397740587127, 1.428753304119126266, 1.292492988728560999 ) ) ;
#157764=CARTESIAN_POINT ( 'NONE',  ( 0.5621253344089729431, -1.117812357707391069, 1.678020072846800659 ) ) ;
#157768=CARTESIAN_POINT ( 'NONE',  ( 4.856285946018928712, -1.968934436971051305, -0.05237921274019693985 ) ) ;
#157770=CARTESIAN_POINT ( 'NONE',  ( 0.4807640440005828131, -0.2721776580492247799, -2.174417363000572756 ) ) ;
#157771=CARTESIAN_POINT ( 'NONE',  ( 5.373610676068619973, 1.758448663713826132, -0.4906839848310071139 ) ) ;
#157777=ORIENTED_EDGE ( 'NONE', *, *, #135974, .F. ) ;
#157778=CARTESIAN_POINT ( 'NONE',  ( 3.016969003575611818, -1.773741936391802332, 0.4936923545346691977 ) ) ;
#157779=CARTESIAN_POINT ( 'NONE',  ( -0.1106856583841060310, -0.002128758811529348188, -1.996853503091333470 ) ) ;
#157780=CARTESIAN_POINT ( 'NONE',  ( 1.072081722297711259, 1.739511735661619429, -1.502347287396257114 ) ) ;
#157781=CARTESIAN_POINT ( 'NONE',  ( 6.244970037249994554, -0.2844439363869250004, -1.940879991452467479 ) ) ;
#157789=CARTESIAN_POINT ( 'NONE',  ( 2.226223261843117918, 2.028672367434441792, 0.5052007718874002018 ) ) ;
#157790=CARTESIAN_POINT ( 'NONE',  ( 0.7076149179639171782, -1.862046558926268913, 0.1791945732521060819 ) ) ;
#157791=CARTESIAN_POINT ( 'NONE',  ( 1.528672481244568448, 1.986742605292156405, -0.3418812301651391605 ) ) ;
#157794=CARTESIAN_POINT ( 'NONE',  ( 2.102700294964424454, -0.3804589880251930123, 1.698169956227519872 ) ) ;
#157798=CARTESIAN_POINT ( 'NONE',  ( 2.596001052779199014, -1.720239769356088688, -0.1272231981628013098 ) ) ;
#157799=CARTESIAN_POINT ( 'NONE',  ( 2.736070936638954176, 2.175344985778558726, 0.2654339622269741295 ) ) ;
#157800=CARTESIAN_POINT ( 'NONE',  ( 5.461621781982892720, 0.4335984126433762853, -2.163701019753036192 ) ) ;
#157802=CARTESIAN_POINT ( 'NONE',  ( 3.010768451359053355, 0.7272417100659108735, 2.045797318486474836 ) ) ;
#157803=CARTESIAN_POINT ( 'NONE',  ( 1.383131112650197281, 1.687622997524572677, -0.6969523973551354779 ) ) ;
#157804=CARTESIAN_POINT ( 'NONE',  ( 3.415340404243884187, -1.954662906411578804, 0.8143554997327147049 ) ) ;
#157805=CARTESIAN_POINT ( 'NONE',  ( 6.539320575229270460, 2.052047842581938841, 2.303245992296603983 ) ) ;
#157807=CARTESIAN_POINT ( 'NONE',  ( 3.896227223837216869, -0.7194467914123764407, -2.176594258899899437 ) ) ;
#157811=CARTESIAN_POINT ( 'NONE',  ( 5.514381189547274076, -2.221473413594120760, -0.001881066846495804690 ) ) ;
#157819=ORIENTED_EDGE ( 'NONE', *, *, #199481, .F. ) ;
#157820=CARTESIAN_POINT ( 'NONE',  ( 4.377577386359387646, -0.4445010797573499817, -1.966645064109616481 ) ) ;
#157822=CARTESIAN_POINT ( 'NONE',  ( 2.817292378285217502, -1.792290562959488742, -1.020665671854523060 ) ) ;
#157827=CARTESIAN_POINT ( 'NONE',  ( 6.070311387754347088, -2.079788119406985825, -0.6908379657195938828 ) ) ;
#157828=CARTESIAN_POINT ( 'NONE',  ( 3.428361437285933455, -1.528740797599713153, -1.314997250469025936 ) ) ;
#157829=CARTESIAN_POINT ( 'NONE',  ( 2.841158510722852970, 0.6603703904487292498, -1.718939526767604420 ) ) ;
#157832=CARTESIAN_POINT ( 'NONE',  ( 6.141596500199405284, -1.324292569296809052, -1.256812384211228428 ) ) ;
#157834=CARTESIAN_POINT ( 'NONE',  ( 0.1931282604852417040, -0.5026490872193057902, -2.214429643963564232 ) ) ;
#157835=CARTESIAN_POINT ( 'NONE',  ( 2.315183273126443009, 1.881732686034083724, 0.9459776246590365645 ) ) ;
#157845=CARTESIAN_POINT ( 'NONE',  ( 2.074623746436579985, 0.9110886696130392481, 1.915067268644244702 ) ) ;
#157846=CARTESIAN_POINT ( 'NONE',  ( 4.060924178622978609, 0.5945426864985210447, 2.140278595106285042 ) ) ;
#157847=CARTESIAN_POINT ( 'NONE',  ( 1.148660753082946240, -1.725648174752218100, 1.350667304935410318 ) ) ;
#157848=CARTESIAN_POINT ( 'NONE',  ( 0.1709339574563934483, -1.438030690398562239, 1.674123062825278563 ) ) ;
#157851=CARTESIAN_POINT ( 'NONE',  ( 4.387127823891323608, 0.09410986116351567621, 1.959716250186482434 ) ) ;
#157856=CARTESIAN_POINT ( 'NONE',  ( 6.610000000000011866, 2.967812824040619191, 2.453181572820534395 ) ) ;
#157860=CARTESIAN_POINT ( 'NONE',  ( 3.797228045176269440, -0.2112621354826669517, -2.110076569278092062 ) ) ;
#157862=CARTESIAN_POINT ( 'NONE',  ( 5.612251347527116963, -0.9680786960581324596, -1.932885698521320528 ) ) ;
#157863=CARTESIAN_POINT ( 'NONE',  ( 4.001369526190221571, -1.836035423186295201, 0.1395379388276704880 ) ) ;
#157864=CARTESIAN_POINT ( 'NONE',  ( 5.348842313791752900, -1.825074749614737701, -0.8578464102408298597 ) ) ;
#157867=CARTESIAN_POINT ( 'NONE',  ( 0.3798832434597871344, -0.2101876225509922147, -1.727645577085941353 ) ) ;
#157872=CARTESIAN_POINT ( 'NONE',  ( 3.678741886385179072, -2.082744454470350615, -0.5786317199799119182 ) ) ;
#157873=CARTESIAN_POINT ( 'NONE',  ( 5.694685421800770087, -1.276849089899323886, -1.560260200769040706 ) ) ;
#157875=CARTESIAN_POINT ( 'NONE',  ( 3.485389320157119997, 1.955090977548096687, -0.9225387301767663528 ) ) ;
#157876=CARTESIAN_POINT ( 'NONE',  ( 3.725814648419359720, -1.171505211990100159, -1.585385422309880887 ) ) ;
#157877=CARTESIAN_POINT ( 'NONE',  ( -0.1232117409455633916, -0.1621322592461546530, -2.156395338765437764 ) ) ;
#157878=CARTESIAN_POINT ( 'NONE',  ( 1.624504772527136875, -1.283422126333678692, -1.917570747650028551 ) ) ;
#157879=CARTESIAN_POINT ( 'NONE',  ( 2.513025655421320170, 1.839406356194466463, 0.9293899518807801075 ) ) ;
#157880=CARTESIAN_POINT ( 'NONE',  ( 5.319850173407331795, 1.153525655430783337, -1.562239502177962480 ) ) ;
#157890=CARTESIAN_POINT ( 'NONE',  ( 2.098912041516465266, -0.5885267676426220174, -2.126790307141281033 ) ) ;
#157892=CARTESIAN_POINT ( 'NONE',  ( 6.069191303861535935, 1.728486752094375190, 0.9278679456784575397 ) ) ;
#157893=CARTESIAN_POINT ( 'NONE',  ( -0.1290005225502641184, 1.996213967822700663, -2.587563282167547385 ) ) ;
#157897=CARTESIAN_POINT ( 'NONE',  ( 5.490138966579363178, -0.4511402564183407127, -1.784887083484905768 ) ) ;
#157899=CARTESIAN_POINT ( 'NONE',  ( 2.395450018592326646, 1.592181132671898869, 1.308497088967359723 ) ) ;
#157906=CARTESIAN_POINT ( 'NONE',  ( 0.4443025167278572551, 2.055347410954794451, 0.1520637142833832778 ) ) ;
#157908=CARTESIAN_POINT ( 'NONE',  ( 4.405690278861111864, -0.7914791229979671883, -1.662609734262666894 ) ) ;
#157914=CARTESIAN_POINT ( 'NONE',  ( 4.196070124731249074, -0.8457972711899945928, 2.038567251995755836 ) ) ;
#157915=CARTESIAN_POINT ( 'NONE',  ( 6.679017863784723730, -0.1010099541198590523, -2.260277599329813647 ) ) ;
#157917=CARTESIAN_POINT ( 'NONE',  ( 0.1758378621803426134, 1.891278220088285833, -0.2826890867150752551 ) ) ;
#157918=CARTESIAN_POINT ( 'NONE',  ( -0.1706859984542466180, -1.561801110730935971, -1.275320528755889526 ) ) ;
#157922=CARTESIAN_POINT ( 'NONE',  ( 5.883449979803575758, 0.1360998956825946737, -1.907488392096804874 ) ) ;
#157924=CARTESIAN_POINT ( 'NONE',  ( 0.3911966820569385828, 1.383097094795827209, 1.259704262696823118 ) ) ;
#157925=CARTESIAN_POINT ( 'NONE',  ( 2.360564879530482330, -1.931125380751706810, -0.5807522007576990664 ) ) ;
#157928=CARTESIAN_POINT ( 'NONE',  ( 3.897179185067170870, 1.779300596213341690, -1.126466309965125756 ) ) ;
#157933=CARTESIAN_POINT ( 'NONE',  ( 4.271743411778946786, 0.4384756098019436665, -1.971458303354764352 ) ) ;
#157936=CARTESIAN_POINT ( 'NONE',  ( 4.429101881081805914, 0.1011787780425543737, 2.159334005894457231 ) ) ;
#157942=CARTESIAN_POINT ( 'NONE',  ( 2.014367633873125563, 2.165423841567072127, -0.1585431616079237827 ) ) ;
#157945=CARTESIAN_POINT ( 'NONE',  ( 0.6789530235665336422, 1.236279375446739603, 1.364625092910062953 ) ) ;
#157948=CARTESIAN_POINT ( 'NONE',  ( 2.841561854484982774, 0.7863008361240211297, -2.045831095052422555 ) ) ;
#157950=CARTESIAN_POINT ( 'NONE',  ( 3.801889278938491934, -0.6593813483589389124, 2.164292034026161549 ) ) ;
#157956=CARTESIAN_POINT ( 'NONE',  ( 4.235448325177215700, -1.219352424245947253, -1.282881785660697771 ) ) ;
#157958=CARTESIAN_POINT ( 'NONE',  ( 0.8859290024384089968, 1.414438444053778055, 1.560449103131421156 ) ) ;
#157962=CARTESIAN_POINT ( 'NONE',  ( 0.8363043462186695587, -1.097040784323728424, 1.635518954194992824 ) ) ;
#157964=CARTESIAN_POINT ( 'NONE',  ( 6.292592244351721043, 1.492246071875057645, -1.356311808412967723 ) ) ;
#157969=CARTESIAN_POINT ( 'NONE',  ( 4.258574955689950592, -1.386304660245713860, 1.256184814050688603 ) ) ;
#157970=CARTESIAN_POINT ( 'NONE',  ( 4.575093719746353038, 1.890691655113156289, 0.8438020912069632562 ) ) ;
#157980=CARTESIAN_POINT ( 'NONE',  ( -0.02968770228140016343, 0.003472272166151618711, -1.826291111852257343 ) ) ;
#157982=CARTESIAN_POINT ( 'NONE',  ( 3.947668504265917644, 1.419370528949075005, 1.354593381527373186 ) ) ;
#157983=CARTESIAN_POINT ( 'NONE',  ( 2.337267334706777611, -1.242538083881424615, 1.587593183769491656 ) ) ;
#157986=CARTESIAN_POINT ( 'NONE',  ( 1.018573325691285003, 1.726041315240328444, 0.7214104187760682629 ) ) ;
#157988=CARTESIAN_POINT ( 'NONE',  ( 3.199479786217104493, 1.818179288054132536, -0.8647478076822049387 ) ) ;
#157990=CARTESIAN_POINT ( 'NONE',  ( 3.814152603263697650, 1.130891212129871093, -1.789721717560237790 ) ) ;
#157991=CARTESIAN_POINT ( 'NONE',  ( 6.825078400183551608, 4.689370880799383912, 2.706890346843467299 ) ) ;
#157992=CARTESIAN_POINT ( 'NONE',  ( 5.389151899530504330, 0.1487064154041470299, 2.065066873896327593 ) ) ;
#157994=CARTESIAN_POINT ( 'NONE',  ( -0.1291982275798781443, -0.004298614154785855221, -2.073875112923003083 ) ) ;
#157995=CARTESIAN_POINT ( 'NONE',  ( 6.720655732516672920, 1.239197277384354035, 2.287559680360019332 ) ) ;
#157996=CARTESIAN_POINT ( 'NONE',  ( 5.438443955714742373, 1.798867289239113987, 0.3102399082220568816 ) ) ;
#157999=CARTESIAN_POINT ( 'NONE',  ( 6.539320575229296217, -0.001643797937642094186, 2.203502507913539077 ) ) ;
#158003=CARTESIAN_POINT ( 'NONE',  ( 6.533860241792342372, -1.853627334332415888, 0.4695604596292660138 ) ) ;
#158008=DIRECTION ( 'NONE',  ( -1.000000000000000000, 1.014813233446432150E-15, 1.972152263052529514E-31 ) ) ;
#158013=CARTESIAN_POINT ( 'NONE',  ( 5.308220328704632784, 1.198845711980157214, -1.621194722098241003 ) ) ;
#158015=( NAMED_UNIT ( * ) SI_UNIT ( $, .STERADIAN. ) SOLID_ANGLE_UNIT ( ) );
#158019=CARTESIAN_POINT ( 'NONE',  ( 2.940244962816233265, -1.016462931258435010, 1.686739332702111405 ) ) ;
#158020=CARTESIAN_POINT ( 'NONE',  ( 3.708611378246814638, 1.915606880664010747, 0.6298579873919087913 ) ) ;
#158022=CARTESIAN_POINT ( 'NONE',  ( 6.727182134110234024, 0.5746707207614526469, 2.142055518182262475 ) ) ;
#158023=CARTESIAN_POINT ( 'NONE',  ( 4.189532503254236318, -0.8396404696654431454, 2.024412170900617092 ) ) ;
#158024=CARTESIAN_POINT ( 'NONE',  ( 2.116120358982703120, -0.9062717621706478655, -1.699889088518308222 ) ) ;
#158027=CARTESIAN_POINT ( 'NONE',  ( 0.2331563151865486128, 1.372759770070256291, -2.202161770551560149 ) ) ;
#158034=CARTESIAN_POINT ( 'NONE',  ( 6.146043377905669125, 0.5841948715668408010, 1.746183665442810007 ) ) ;
#158035=CARTESIAN_POINT ( 'NONE',  ( 2.824860481609407614, 1.456601328488495106, -1.389772560336500318 ) ) ;
#158036=CARTESIAN_POINT ( 'NONE',  ( 4.569826555773855326, 1.780639694173843823, -1.453273832002010213 ) ) ;
#158037=CARTESIAN_POINT ( 'NONE',  ( -0.02919842301646497981, 5.720960850909259321, -2.667883601355185430 ) ) ;
#158038=CARTESIAN_POINT ( 'NONE',  ( 2.658860470891976302, 1.497794124733292431, -1.104231377384189861 ) ) ;
#158045=CARTESIAN_POINT ( 'NONE',  ( 6.409723817861421757, -0.9859548438324974295, -1.843685114342674458 ) ) ;
#158050=CARTESIAN_POINT ( 'NONE',  ( 6.357991264096761519, 1.719682601729131566, -0.1347253291539267650 ) ) ;
#158053=CARTESIAN_POINT ( 'NONE',  ( 1.406441466896314996, -0.9629721463089849776, -1.441941353469172293 ) ) ;
#158057=CARTESIAN_POINT ( 'NONE',  ( 5.787976215063657115, -1.371286462501415837, -1.683233787797025371 ) ) ;
#158058=CARTESIAN_POINT ( 'NONE',  ( 4.178209475066913647, -1.049361115903378883, 1.493786327181771068 ) ) ;
#158059=CARTESIAN_POINT ( 'NONE',  ( 2.711707638535421960, 0.5279276851305572116, -1.889291386287835550 ) ) ;
#158063=CARTESIAN_POINT ( 'NONE',  ( 3.475340844119988226, -1.870931441966826148, -0.9980012987173056960 ) ) ;
#158067=CARTESIAN_POINT ( 'NONE',  ( 0.9189038144036645317, -1.502058968113138437, 1.424965263859011122 ) ) ;
#158070=CARTESIAN_POINT ( 'NONE',  ( 3.493049024619375054, -2.141166226970441233, -0.5910787634417090652 ) ) ;
#158071=EDGE_LOOP ( 'NONE', ( #68412, #155569, #31742, #58520 ) ) ;
#158072=CARTESIAN_POINT ( 'NONE',  ( 0.7218034001665899480, 2.265987065647384835, 0.3856900369042133292 ) ) ;
#158074=CARTESIAN_POINT ( 'NONE',  ( 6.895384927792009400, -1.844987169530726723, 0.9222207602926129066 ) ) ;
#158081=CARTESIAN_POINT ( 'NONE',  ( -0.2102771530458094895, 1.993718876163485421, -2.617492801249762913 ) ) ;
#158082=CARTESIAN_POINT ( 'NONE',  ( 2.801416971846592219, -0.5432927088015163664, 1.637025921142007956 ) ) ;
#158083=CARTESIAN_POINT ( 'NONE',  ( 1.165250339122084533, 1.861343190080061660, -0.7762330495894868010 ) ) ;
#158084=CARTESIAN_POINT ( 'NONE',  ( 3.972163192483857408, 1.252710246566196783, 1.883753103390993777 ) ) ;
#158085=CARTESIAN_POINT ( 'NONE',  ( 4.776057437618447921, 1.212020014983648863, 1.722159047642721541 ) ) ;
#158087=CARTESIAN_POINT ( 'NONE',  ( 3.672906134817868651, 0.04599029964666952880, -1.769319831623831663 ) ) ;
#158090=CARTESIAN_POINT ( 'NONE',  ( 6.444901331192640193, -1.838261776244881185, -1.369441068571846554 ) ) ;
#158091=CARTESIAN_POINT ( 'NONE',  ( 5.771403949166884040, 1.100151190403714452, 1.476150860297696932 ) ) ;
#158095=CARTESIAN_POINT ( 'NONE',  ( 5.033237522093748417, -1.548190877955179179, -1.551241237171486098 ) ) ;
#158098=CARTESIAN_POINT ( 'NONE',  ( 5.406714943436663035, 0.5975561702324573288, 1.982271326387271770 ) ) ;
#158099=CARTESIAN_POINT ( 'NONE',  ( 0.09298292169932984019, 1.756857073293972116, 0.9896806593640145033 ) ) ;
#158101=CARTESIAN_POINT ( 'NONE',  ( 2.824735624865559735, 1.814154213653540237, 0.6486305857245775464 ) ) ;
#158104=CARTESIAN_POINT ( 'NONE',  ( 6.539320575229233157, 0.001224430076711413356, 2.103502572931112091 ) ) ;
#158112=CARTESIAN_POINT ( 'NONE',  ( 1.767943819387544968, -1.947426213878332035, 0.2369139692007388165 ) ) ;
#158115=CARTESIAN_POINT ( 'NONE',  ( 5.705508943770692731, -1.545575431542939970, -1.208212526538715137 ) ) ;
#158119=CARTESIAN_POINT ( 'NONE',  ( 6.631704542599726082, -1.407888343591977121, -1.640466528430361670 ) ) ;
#158123=CARTESIAN_POINT ( 'NONE',  ( 0.2978465640060874997, -1.869987984933557890, -0.05268733258671080832 ) ) ;
#158124=CARTESIAN_POINT ( 'NONE',  ( 6.520799197568460492, 1.728869810328565793, -0.1316537485448170952 ) ) ;
#158126=CARTESIAN_POINT ( 'NONE',  ( 3.368858348882136422, 0.05182064297618373117, -2.191103300807801801 ) ) ;
#158127=CARTESIAN_POINT ( 'NONE',  ( 4.313705703444643547, -0.3987071732099633503, 2.272742389722400169 ) ) ;
#158128=CARTESIAN_POINT ( 'NONE',  ( 6.749297902460969389, -1.652236475679531580, -1.231405567270830170 ) ) ;
#158129=CARTESIAN_POINT ( 'NONE',  ( 1.886567394283003907, 1.689560458097194795, -0.9572515956587694941 ) ) ;
#158132=CARTESIAN_POINT ( 'NONE',  ( 4.799148092389167175, -0.2621723519393297508, -2.104289960152181393 ) ) ;
#158134=CARTESIAN_POINT ( 'NONE',  ( 3.111954093273407107, 0.05229746705895028935, 2.015912966248374349 ) ) ;
#158138=CARTESIAN_POINT ( 'NONE',  ( 1.523764310407935030, -1.012771255265769943, -1.518815351243132383 ) ) ;
#158143=CARTESIAN_POINT ( 'NONE',  ( 5.401267763076613271, 1.683455835520174526, 1.188505893847252581 ) ) ;
#158147=CARTESIAN_POINT ( 'NONE',  ( 4.424476369979273294, -0.8654530498428643082, -1.825003331238822746 ) ) ;
#158148=CARTESIAN_POINT ( 'NONE',  ( 5.830790380266278383, 1.493519825859883854, -1.644436761705171612 ) ) ;
#158153=CARTESIAN_POINT ( 'NONE',  ( 4.329017481302106063, 0.09909362218092979124, 2.058626247020868494 ) ) ;
#158154=CARTESIAN_POINT ( 'NONE',  ( 3.340470361411255418, 0.4872029778183217252, -1.956561305313428978 ) ) ;
#158162=CARTESIAN_POINT ( 'NONE',  ( 2.530624857006387618, 1.977747929495787371, -0.3905373530270899174 ) ) ;
#158163=CARTESIAN_POINT ( 'NONE',  ( 2.870863542623874221, 1.748142402769039760, -0.5779331317549916136 ) ) ;
#158164=CARTESIAN_POINT ( 'NONE',  ( 1.454236823263599376, 0.6660240913333862478, -2.209497540817098038 ) ) ;
#158167=CARTESIAN_POINT ( 'NONE',  ( 3.233815116076131257, -1.449111151313630996, -1.604113057997895053 ) ) ;
#158172=CARTESIAN_POINT ( 'NONE',  ( 1.428351348257720588, 1.801920623737063520, 0.5021531274154652502 ) ) ;
#158173=CARTESIAN_POINT ( 'NONE',  ( 6.016478623866945874, 1.324313071814016141, -1.460584582105582285 ) ) ;
#158177=CARTESIAN_POINT ( 'NONE',  ( 0.1709339574563934483, -1.438030690398562239, 1.674123062825278563 ) ) ;
#158182=CARTESIAN_POINT ( 'NONE',  ( 6.539320575229247368, 1.232987345766973775, 2.316458022558224972 ) ) ;
#158183=CARTESIAN_POINT ( 'NONE',  ( 4.645367602377043603, -1.523440194387800650, -1.251305281888495102 ) ) ;
#158184=CARTESIAN_POINT ( 'NONE',  ( 5.830798129077900072, 2.222503408945066816, 0.6210771851366378993 ) ) ;
#158185=CARTESIAN_POINT ( 'NONE',  ( 6.391040216397121831, 0.1834577666269270046, 1.851959058998996710 ) ) ;
#158187=CARTESIAN_POINT ( 'NONE',  ( 2.623947407551871169, 2.023649216642096960, -0.3979924315659318923 ) ) ;
#158194=CARTESIAN_POINT ( 'NONE',  ( 4.879425774075326849, -0.1113562312203674326, 2.168454086520410495 ) ) ;
#158196=CARTESIAN_POINT ( 'NONE',  ( 4.177188522404684079, 1.205947341878073287, 1.391433828303423326 ) ) ;
#158197=MANIFOLD_SOLID_BREP ( 'Sweep1[3]', #140154 ) ;
#158199=CARTESIAN_POINT ( 'NONE',  ( 6.620655732516649294, 4.698502813744664941, 2.488957606609870421 ) ) ;
#158200=CARTESIAN_POINT ( 'NONE',  ( 6.198795224570643470, 1.821041368708445907, 1.219022265761634971 ) ) ;
#158202=CARTESIAN_POINT ( 'NONE',  ( 0.3161853103110903729, -2.218393710063219615, 0.4432750438988151687 ) ) ;
#158207=CARTESIAN_POINT ( 'NONE',  ( 0.04731519813723151363, -1.748418646119804354, 0.7749314921376223575 ) ) ;
#158208=CARTESIAN_POINT ( 'NONE',  ( 0.5140565032336151807, 1.225199188247323878, -1.277449566202024656 ) ) ;
#158209=CARTESIAN_POINT ( 'NONE',  ( 5.830732115328919996, 1.350214353519451960, -1.493314199452821178 ) ) ;
#158211=CARTESIAN_POINT ( 'NONE',  ( 4.348724867337580235, 0.5594899878812797933, 2.030215228624824952 ) ) ;
#158212=CARTESIAN_POINT ( 'NONE',  ( 3.708511580433976107, 1.820041504565768742, 0.5977543794245043784 ) ) ;
#158214=CARTESIAN_POINT ( 'NONE',  ( 4.685976223243822680, -1.210123887884282601, -1.553869430650482997 ) ) ;
#158215=CARTESIAN_POINT ( 'NONE',  ( 6.064714679231743233, 0.6376439298158544933, 1.916535431269225098 ) ) ;
#158216=CARTESIAN_POINT ( 'NONE',  ( 3.256579335763456040, -1.417408692332474462, 1.220890361658559575 ) ) ;
#158217=CARTESIAN_POINT ( 'NONE',  ( 4.740679804603589176, 0.2991043602584910199, 1.698571524128352994 ) ) ;
#158218=CARTESIAN_POINT ( 'NONE',  ( 1.406358598101828283, -1.903450966454448334, -0.1843715739238485363 ) ) ;
#158220=CARTESIAN_POINT ( 'NONE',  ( 1.981372325807278623, -0.1102420082176903682, -2.204251428397439483 ) ) ;
#158223=CARTESIAN_POINT ( 'NONE',  ( 6.725062055625550705, -1.793239977796506457, -0.7961783947641184467 ) ) ;
#158229=CARTESIAN_POINT ( 'NONE',  ( 2.365759603224312446, -0.4558734232973959966, 2.019384234097781228 ) ) ;
#158234=CARTESIAN_POINT ( 'NONE',  ( 6.481110812017948142, -1.938455339442773706, -0.8599551062365148324 ) ) ;
#158241=CARTESIAN_POINT ( 'NONE',  ( 5.079453798366286854, 1.392331892589277142, -1.458333960840517696 ) ) ;
#158242=CARTESIAN_POINT ( 'NONE',  ( 4.839036869973236676, -1.621808105726432414, -1.019334933273335242 ) ) ;
#158243=CARTESIAN_POINT ( 'NONE',  ( 2.138457411672203712, 0.4836887423533155483, 2.137355272389021899 ) ) ;
#158248=CARTESIAN_POINT ( 'NONE',  ( 5.291276029577359985, -0.05376236717486576611, -2.012660120947160181 ) ) ;
#158249=CARTESIAN_POINT ( 'NONE',  ( 1.546972149855216250, 0.1906517044060058452, 1.902890584052991718 ) ) ;
#158252=CARTESIAN_POINT ( 'NONE',  ( 0.4039230143318903177, -1.081087622585241714, -1.701935196855845822 ) ) ;
#158254=CARTESIAN_POINT ( 'NONE',  ( 3.983990651536262195, -2.068283627568163308, -0.3046923749255076586 ) ) ;
#158256=CARTESIAN_POINT ( 'NONE',  ( 2.115808521728879565, -0.8096002590626363293, -1.522937571937353241 ) ) ;
#158258=CARTESIAN_POINT ( 'NONE',  ( 6.504144398916748671, -0.9053081408615070158, 1.915699539216948688 ) ) ;
#158266=CARTESIAN_POINT ( 'NONE',  ( 2.719172733320520674, 1.531317187073286901, 0.9673847807401686483 ) ) ;
#158270=CARTESIAN_POINT ( 'NONE',  ( 3.562975276761202181, -1.478990456472810910, 1.045639718295880094 ) ) ;
#158274=CARTESIAN_POINT ( 'NONE',  ( 4.457361271359429722, 1.493968932455931542, 1.109517434556703597 ) ) ;
#158275=CARTESIAN_POINT ( 'NONE',  ( 1.458442676765151269, -1.819496111524568027, -0.5994125798251969117 ) ) ;
#158276=CARTESIAN_POINT ( 'NONE',  ( 0.6393319655835437709, -1.287349573739982933, -1.294668131371433661 ) ) ;
#158284=CARTESIAN_POINT ( 'NONE',  ( 5.225436369306192930, 0.1968503305618974075, -1.959608170402066696 ) ) ;
#158287=CARTESIAN_POINT ( 'NONE',  ( 0.4805627621443783193, -0.2577823606141148027, -2.074612465628209890 ) ) ;
#158289=CARTESIAN_POINT ( 'NONE',  ( 5.772470297455748245, -1.221717764600898981, 1.489408783192472052 ) ) ;
#158291=CARTESIAN_POINT ( 'NONE',  ( 1.113953379265147925, -0.8168401028521531382, -1.632710947565917170 ) ) ;
#158292=CARTESIAN_POINT ( 'NONE',  ( 1.682535984017709874, -1.178549783888741320, 1.865657194899547733 ) ) ;
#158294=CARTESIAN_POINT ( 'NONE',  ( 1.459083999156213451, -1.613880964290700160, 1.025699646091532857 ) ) ;
#158295=CARTESIAN_POINT ( 'NONE',  ( 6.948121156015312216, -0.8458062566301125518, 1.777170381402736865 ) ) ;
#158296=CARTESIAN_POINT ( 'NONE',  ( 2.173291266613562644, 1.196360937402714875, 1.529712666019187761 ) ) ;
#158297=CARTESIAN_POINT ( 'NONE',  ( 0.7728142736522191081, -2.006652962095498260, 0.1948079406639269262 ) ) ;
#158299=CARTESIAN_POINT ( 'NONE',  ( 6.315283160355378733, -1.595611397598785564, -0.9574585435550940771 ) ) ;
#158305=CARTESIAN_POINT ( 'NONE',  ( 2.542740116143254792, -1.820367712357463974, 1.220030464664762393 ) ) ;
#158309=CARTESIAN_POINT ( 'NONE',  ( 2.596107596775329540, -1.820790993511243849, -0.1344670722737417168 ) ) ;
#158312=CIRCLE ( 'NONE', #109974, 0.05000000000000057176 ) ;
#158316=CARTESIAN_POINT ( 'NONE',  ( 1.295397306693826467, 1.458444760659328265, 1.258811869801695682 ) ) ;
#158317=CARTESIAN_POINT ( 'NONE',  ( 6.139501739389007007, 1.813922436357641388, -0.7475906808915923074 ) ) ;
#158318=AXIS2_PLACEMENT_3D ( 'NONE', #107617, #73984, #7896 ) ;
#158322=CARTESIAN_POINT ( 'NONE',  ( 5.460537066722415567, -1.980877156148381335, -0.9378266216248376530 ) ) ;
#158324=CARTESIAN_POINT ( 'NONE',  ( 4.909070852169226562, -1.665950775781706028, 1.228889460859562854 ) ) ;
#158328=CARTESIAN_POINT ( 'NONE',  ( 4.676596114989339803, 1.702786692269612212, 1.544373632959222586 ) ) ;
#158331=CARTESIAN_POINT ( 'NONE',  ( 0.6215105264332577706, -2.174887359234744633, 0.7243307227927602288 ) ) ;
#158332=CARTESIAN_POINT ( 'NONE',  ( 6.620655732516644854, 4.701125524277991907, 2.388986273831222640 ) ) ;
#158334=CARTESIAN_POINT ( 'NONE',  ( 5.085854714555574141, -1.927481041573789744, -0.2360958376807794079 ) ) ;
#158338=CARTESIAN_POINT ( 'NONE',  ( 5.273660385517703553, 0.3669835118517566497, -1.876681294024808988 ) ) ;
#158339=CARTESIAN_POINT ( 'NONE',  ( 6.756889588843246308, -1.328954913838266361, 1.099249449767102593 ) ) ;
#158340=CARTESIAN_POINT ( 'NONE',  ( 5.260953973667149342, -0.05432152012316109058, -2.015980820358989511 ) ) ;
#158344=CARTESIAN_POINT ( 'NONE',  ( 1.710996362105126511, -0.2544465352872951613, 2.075019263894110733 ) ) ;
#158345=CARTESIAN_POINT ( 'NONE',  ( 0.08049558579637566824, -0.1306036352819762714, -1.740669940395103366 ) ) ;
#158346=CARTESIAN_POINT ( 'NONE',  ( 6.117814597332064785, 0.2004318333163370436, 2.006446488866588496 ) ) ;
#158348=CARTESIAN_POINT ( 'NONE',  ( 3.328363117612358479, 2.236410206915816268, 0.5022841181492423424 ) ) ;
#158349=CARTESIAN_POINT ( 'NONE',  ( 2.237881400472482962, 0.3803048411740033719, 1.698081864755231374 ) ) ;
#158350=CARTESIAN_POINT ( 'NONE',  ( 2.935903058640790597, -2.042584291827519660, 0.5695675404085094318 ) ) ;
#158351=DIRECTION ( 'NONE',  ( -1.000000000000000000, 0.000000000000000000, 0.000000000000000000 ) ) ;
#158352=CARTESIAN_POINT ( 'NONE',  ( 1.879855919261735675, -0.2174549385326445539, 1.720076089969482469 ) ) ;
#158354=CARTESIAN_POINT ( 'NONE',  ( 2.031498134000471190, 1.782053568523461751, -0.5365169527500669444 ) ) ;
#158355=CARTESIAN_POINT ( 'NONE',  ( 2.752568609338637895, -2.165203543660359387, -0.1620229588487445971 ) ) ;
#158356=CARTESIAN_POINT ( 'NONE',  ( 3.151577601795185757, 1.966304690962265234, -0.4465026806126579095 ) ) ;
#158357=CARTESIAN_POINT ( 'NONE',  ( 3.687500000000002665, -1.451031289060967788, 1.451031289061265550 ) ) ;
#158359=CARTESIAN_POINT ( 'NONE',  ( 6.551400848983751857, -1.549099897634421685, -1.145107510758677893 ) ) ;
#158361=CARTESIAN_POINT ( 'NONE',  ( 3.111816671419795011, 1.753586859115576324, 1.363618078755132634 ) ) ;
#158367=CARTESIAN_POINT ( 'NONE',  ( 0.01275469579824477576, -2.220946917248843189, -0.04775700320917666830 ) ) ;
#158368=CARTESIAN_POINT ( 'NONE',  ( 4.422284181769401634, 0.9229163912191931107, 1.731201473044992944 ) ) ;
#158373=CARTESIAN_POINT ( 'NONE',  ( 5.624405936800197736, 1.354097840178031475, -1.812292894430814094 ) ) ;
#158374=CARTESIAN_POINT ( 'NONE',  ( 2.365751517750969146, -0.4541778970535991777, 2.011898661289913903 ) ) ;
#158378=CARTESIAN_POINT ( 'NONE',  ( 4.165207536865437099, 0.2314014899743311315, -1.856129391651973215 ) ) ;
#158379=CARTESIAN_POINT ( 'NONE',  ( 2.900671442982618142, -0.8568821622233543378, -1.507568437789049032 ) ) ;
#158380=CARTESIAN_POINT ( 'NONE',  ( 6.550331612656306035, -1.695486744446069727, 1.388264742925699569 ) ) ;
#158381=CARTESIAN_POINT ( 'NONE',  ( 0.4994150495197279271, 1.833458848295946186, -1.227822027206025179 ) ) ;
#158382=CARTESIAN_POINT ( 'NONE',  ( 5.999939506776140519, -0.7010436009657755596, -1.811167765765375526 ) ) ;
#158384=CARTESIAN_POINT ( 'NONE',  ( 0.6861729220449981348, 1.650083401500940239, 1.158686392676591570 ) ) ;
#158385=CARTESIAN_POINT ( 'NONE',  ( 0.1586465271753433603, 2.115359532055087310, 0.1496401998123952359 ) ) ;
#158386=CARTESIAN_POINT ( 'NONE',  ( 6.557263107265463020, -1.238491779027944162, 1.591905563659588907 ) ) ;
#158389=CARTESIAN_POINT ( 'NONE',  ( 4.564971734551386717, -1.632036996880025903, -0.8184370388232551363 ) ) ;
#158390=CARTESIAN_POINT ( 'NONE',  ( 2.380145745526092593, 1.357289424207007489, 1.739932290444376584 ) ) ;
#158395=CARTESIAN_POINT ( 'NONE',  ( 0.9494800659552645739, -1.824215446917340389, 0.8674010940010259407 ) ) ;
#158399=CARTESIAN_POINT ( 'NONE',  ( 2.834617457269935414, -1.779228943046967437, -0.5452927797432933765 ) ) ;
#158404=CARTESIAN_POINT ( 'NONE',  ( 4.072732355924274295, -1.704239406772959153, -0.6552279023967976235 ) ) ;
#158408=CARTESIAN_POINT ( 'NONE',  ( 0.7547592729708142434, -1.719773315039843986, -0.2198852240756724863 ) ) ;
#158409=CARTESIAN_POINT ( 'NONE',  ( 5.490138966579363178, -0.4511402564183407127, -1.784887083484905768 ) ) ;
#158410=CARTESIAN_POINT ( 'NONE',  ( 4.143447727350758392, -2.008842960899869912, 1.135675674892607345 ) ) ;
#158412=CARTESIAN_POINT ( 'NONE',  ( 0.5618817370758311114, 2.038728707766800596, -0.2996719410968719521 ) ) ;
#158413=CARTESIAN_POINT ( 'NONE',  ( 2.032666248472639214, -1.733752323498815029, 0.8752225562490000277 ) ) ;
#158414=CARTESIAN_POINT ( 'NONE',  ( 6.028750418185333082, 2.265939813929934488, -0.3841603865788502103 ) ) ;
#158417=CARTESIAN_POINT ( 'NONE',  ( 5.612129163471575310, -0.8422657237196762292, -1.670366365510121742 ) ) ;
#158421=CARTESIAN_POINT ( 'NONE',  ( 2.953266587970606150, -1.684550232849800544, 0.9053361341156559439 ) ) ;
#158423=CARTESIAN_POINT ( 'NONE',  ( 3.844505992619148937, 2.196175933995975438, 0.2170506636963928093 ) ) ;
#158428=CARTESIAN_POINT ( 'NONE',  ( 2.081525663035548757, -0.1140690627178981842, -2.304871973535598251 ) ) ;
#158429=CARTESIAN_POINT ( 'NONE',  ( 2.400770673373255448, 0.4268909467371252431, 1.914702609522442867 ) ) ;
#158432=CARTESIAN_POINT ( 'NONE',  ( 6.315292642669888323, -1.766025379077978741, -1.065358839237473099 ) ) ;
#158434=CARTESIAN_POINT ( 'NONE',  ( 3.837125247982266174, -1.679222704393277921, -1.116210984008485507 ) ) ;
#158437=CARTESIAN_POINT ( 'NONE',  ( 4.364470425680367249, -1.957169923074707274, -0.4852690807995581057 ) ) ;
#158442=CARTESIAN_POINT ( 'NONE',  ( 2.465899347143265086, -0.4792435138091205027, 2.117354166282244599 ) ) ;
#158446=CARTESIAN_POINT ( 'NONE',  ( 2.108475139129362574, 1.389272611029747750, -1.252756881873963168 ) ) ;
#158447=CARTESIAN_POINT ( 'NONE',  ( 0.2279051764371925748, -1.265926261136205211, -1.626655886597817124 ) ) ;
#158448=CARTESIAN_POINT ( 'NONE',  ( 0.07775346131141079586, 1.298946786380944074, -2.537735853881052162 ) ) ;
#158452=CARTESIAN_POINT ( 'NONE',  ( 2.877492880751183257, 0.2784179829431778219, -1.891769048003589138 ) ) ;
#158454=CARTESIAN_POINT ( 'NONE',  ( 4.680378828550276538, -1.717002404052007325, -0.4286406472287905278 ) ) ;
#158455=CARTESIAN_POINT ( 'NONE',  ( 1.400873256076972329, -0.2815782128867699852, -1.891321520182134286 ) ) ;
#158457=CARTESIAN_POINT ( 'NONE',  ( 6.485945863600712791, -1.915068438110486770, 0.05257573307166327897 ) ) ;
#158459=CARTESIAN_POINT ( 'NONE',  ( 0.6255436495894195481, 0.2045281481408110225, -2.060252820462626477 ) ) ;
#158462=CARTESIAN_POINT ( 'NONE',  ( 5.700035372616791385, -1.870836310086241294, 0.001406584917262864625 ) ) ;
#158463=CARTESIAN_POINT ( 'NONE',  ( 1.330379832379691818, 1.758967509726565792, 0.4888242021733391618 ) ) ;
#158464=CARTESIAN_POINT ( 'NONE',  ( 5.725267921653402148, -0.05769419298589681389, 2.206291853148376170 ) ) ;
#158467=CARTESIAN_POINT ( 'NONE',  ( 2.576693429754982390, 1.349077690114818040, -1.560390594356737104 ) ) ;
#158471=CARTESIAN_POINT ( 'NONE',  ( 0.2105424042340813540, -0.9235240298187572527, -1.952328634516012684 ) ) ;
#158474=CARTESIAN_POINT ( 'NONE',  ( 5.353992430378140099, -0.7485205528568983357, 1.930488744064068785 ) ) ;
#158476=CARTESIAN_POINT ( 'NONE',  ( 2.970174626046933053, 1.153603175066318931, 1.827835936144058371 ) ) ;
#158478=CARTESIAN_POINT ( 'NONE',  ( 3.281903422188407138, 1.969933747823931380, -0.4446889725447465413 ) ) ;
#158479=CARTESIAN_POINT ( 'NONE',  ( 2.383191274269541360, -0.003000794896521400724, 1.962046632024143866 ) ) ;
#158481=CARTESIAN_POINT ( 'NONE',  ( 6.720655732516644498, 4.691561721546229968, 2.636312907496433322 ) ) ;
#158487=CARTESIAN_POINT ( 'NONE',  ( 1.182827746461931229, 1.645757370610765102, -1.164989914844760444 ) ) ;
#158489=CARTESIAN_POINT ( 'NONE',  ( 6.146043800834426918, 0.6857851511376764631, 2.081541312870714311 ) ) ;
#158490=DIRECTION ( 'NONE',  ( 1.039099362110107450E-15, 1.000000000000000000, -4.583713267641621330E-32 ) ) ;
#158491=CARTESIAN_POINT ( 'NONE',  ( 5.097880177178074845, 1.288836597028759634, 1.412999258680311510 ) ) ;
#158495=CARTESIAN_POINT ( 'NONE',  ( 2.882435586221145485, -0.5880402899147363360, -1.928746874286999979 ) ) ;
#158497=CARTESIAN_POINT ( 'NONE',  ( 4.911038474854160896, 1.501934305467259145, 0.8478258478515336982 ) ) ;
#158501=CARTESIAN_POINT ( 'NONE',  ( 4.798043669735932326, -1.870115615568968881, -0.04763329477865811679 ) ) ;
#158503=CARTESIAN_POINT ( 'NONE',  ( 0.5673436759025469733, 1.799520464221905369, 1.023488823764052480 ) ) ;
#158506=CARTESIAN_POINT ( 'NONE',  ( 6.569024019911770651, -1.395121139060730542, 1.155258474184825745 ) ) ;
#158509=CARTESIAN_POINT ( 'NONE',  ( 0.7206316775285178666, 1.371080193274256676, -1.184091668402836639 ) ) ;
#158515=CARTESIAN_POINT ( 'NONE',  ( 0.3968290921660848070, 0.3316028935436679537, 1.933473477243151439 ) ) ;
#158517=CARTESIAN_POINT ( 'NONE',  ( 4.745656728581866268, 1.894139079640380086, -0.2851870984255585051 ) ) ;
#158518=CARTESIAN_POINT ( 'NONE',  ( 0.1747926744264660381, 0.006858446013176254172, -1.855468577918440776 ) ) ;
#158524=CARTESIAN_POINT ( 'NONE',  ( 2.026462046419864826, 1.244889377058140845, -1.767065586814352773 ) ) ;
#158528=CARTESIAN_POINT ( 'NONE',  ( 5.174738384962677351, -1.719472664011096219, -0.6136495084824307167 ) ) ;
#158530=CARTESIAN_POINT ( 'NONE',  ( 0.7902269029948695289, -1.955937164205447054, -0.2457751801602201802 ) ) ;
#158531=CARTESIAN_POINT ( 'NONE',  ( 3.375170810042011915, -1.688748480992762868, -0.8973671847329609541 ) ) ;
#158534=CARTESIAN_POINT ( 'NONE',  ( 4.035575377323636026, 1.855309441653162139, -0.6614512482757756162 ) ) ;
#158536=CARTESIAN_POINT ( 'NONE',  ( 5.759312517635055251, 1.912593682650292060, -0.3362288579709416525 ) ) ;
#158540=CARTESIAN_POINT ( 'NONE',  ( 6.064709079624690524, 0.6667526090060638122, 2.013086243192941716 ) ) ;
#158542=CARTESIAN_POINT ( 'NONE',  ( 4.354103434560454566, 0.8146061972254794448, -1.730223316255767196 ) ) ;
#158546=CARTESIAN_POINT ( 'NONE',  ( 4.635406539864527886, -0.09663638271006223801, 2.010879464324326626 ) ) ;
#158548=CARTESIAN_POINT ( 'NONE',  ( 5.742758765878789085, 0.3605303665093100851, 1.789564367143759327 ) ) ;
#158550=CARTESIAN_POINT ( 'NONE',  ( 1.486871883557450591, 1.994755712061954123, 0.5540851298423480342 ) ) ;
#158555=CARTESIAN_POINT ( 'NONE',  ( 6.807498166657679484, -0.4075194142965676836, 1.832415718333743282 ) ) ;
#158564=CARTESIAN_POINT ( 'NONE',  ( 5.080564943346563389, -0.6172752100359213401, 1.620779670503540659 ) ) ;
#158567=CARTESIAN_POINT ( 'NONE',  ( 2.623957243734816647, 2.031168598393529034, -0.3995267358143372860 ) ) ;
#158568=CARTESIAN_POINT ( 'NONE',  ( 3.972345043000875098, -2.094467101900459483, -0.3087697250930310222 ) ) ;
#158571=CARTESIAN_POINT ( 'NONE',  ( 2.166797266485945617, 1.462705959888461971, -1.319016900598804831 ) ) ;
#158576=CARTESIAN_POINT ( 'NONE',  ( 4.189605479905995189, -0.8790709274306067744, 2.117190895528203498 ) ) ;
#158577=CARTESIAN_POINT ( 'NONE',  ( 0.4162703231485806454, 1.261427835099769634, -1.320066674804179385 ) ) ;
#158581=CARTESIAN_POINT ( 'NONE',  ( 1.916272853804147136, -2.012662139290276819, 0.05368196500972129831 ) ) ;
#158582=CARTESIAN_POINT ( 'NONE',  ( 2.518345088137901477, 0.8342845254802437882, 1.775630740545742992 ) ) ;
#158586=CARTESIAN_POINT ( 'NONE',  ( 4.998031443873323099, -0.7039345487453112504, -1.968691415026160962 ) ) ;
#158587=CARTESIAN_POINT ( 'NONE',  ( 3.731107905939319735, -1.635417248454105854, 0.6770700851450436319 ) ) ;
#158589=CARTESIAN_POINT ( 'NONE',  ( 6.052705554163346768, -1.962971892542137553, -1.183510860282228405 ) ) ;
#158590=CARTESIAN_POINT ( 'NONE',  ( 5.911982399937937949, 1.163873415549965262, -1.294066288734674997 ) ) ;
#158593=CARTESIAN_POINT ( 'NONE',  ( 6.047535252586548893, -1.628406021067085874, 1.622660289872903006 ) ) ;
#158595=CARTESIAN_POINT ( 'NONE',  ( 5.219963594993116018, -1.465640877661518626, -0.9259742478883812300 ) ) ;
#158596=CARTESIAN_POINT ( 'NONE',  ( 5.863789056686759871, -0.5331677977272324398, 2.104577851170267078 ) ) ;
#158598=CARTESIAN_POINT ( 'NONE',  ( 0.1107727185766090999, 2.028241449780379568, 0.6078911015285259900 ) ) ;
#158599=CARTESIAN_POINT ( 'NONE',  ( 5.812500000000003553, 1.451031289061346818, 1.451031289060879637 ) ) ;
#158601=CARTESIAN_POINT ( 'NONE',  ( 3.856402372034730686, 0.6923319331257683507, 1.797858303039111982 ) ) ;
#158603=CARTESIAN_POINT ( 'NONE',  ( 0.4697634657386277612, -1.879787550458272394, -1.183196895768683365 ) ) ;
#158610=CARTESIAN_POINT ( 'NONE',  ( 2.526306204038858194, -2.196730012672935661, 0.3287970392919815632 ) ) ;
#158616=CARTESIAN_POINT ( 'NONE',  ( 1.072888940501380839, -0.9041080511620370741, 1.802418165037560138 ) ) ;
#158618=CARTESIAN_POINT ( 'NONE',  ( 5.512196432965448700, 2.060465348046951917, -0.09781390707789237859 ) ) ;
#158624=CARTESIAN_POINT ( 'NONE',  ( 0.2625039974461966241, -1.576774366707566433, -0.8037556782162450508 ) ) ;
#158625=CARTESIAN_POINT ( 'NONE',  ( 5.871638708485903635, -0.2633594344273459398, -1.713904792762838136 ) ) ;
#158626=CARTESIAN_POINT ( 'NONE',  ( 6.075711799444424521, -0.9231013878284710650, 1.475285791177717076 ) ) ;
#158627=CARTESIAN_POINT ( 'NONE',  ( 3.562334897874219308, -1.538608923441080689, 1.699488912218325654 ) ) ;
#158629=CARTESIAN_POINT ( 'NONE',  ( 1.780954670855667388, 1.268887097626215876, 1.334285251370644021 ) ) ;
#158632=CARTESIAN_POINT ( 'NONE',  ( 2.783998052563033010, -0.9402290988879957734, 1.564698673013890984 ) ) ;
#158633=CARTESIAN_POINT ( 'NONE',  ( 3.428361437285933455, -1.528740797599713153, -1.314997250469025936 ) ) ;
#158636=CARTESIAN_POINT ( 'NONE',  ( 5.104563850188495344, -0.7068653695375884949, -1.983929190867816494 ) ) ;
#158638=CARTESIAN_POINT ( 'NONE',  ( 2.893098739488662030, 0.2508700648995808025, 2.055025655848155886 ) ) ;
#158641=CARTESIAN_POINT ( 'NONE',  ( 4.723349490952149843, 1.845327050471495367, 1.044454997443218236 ) ) ;
#158642=CARTESIAN_POINT ( 'NONE',  ( 1.207505077391484161, -0.4687122323817956571, 1.868500445134027466 ) ) ;
#158649=CARTESIAN_POINT ( 'NONE',  ( 6.433838290133602200, -2.056603270127650429, 0.5165238393732355382 ) ) ;
#158650=CARTESIAN_POINT ( 'NONE',  ( 1.817543918834242378, -0.2582919827684154179, 2.089997942319920199 ) ) ;
#158653=CARTESIAN_POINT ( 'NONE',  ( 6.666864641256595725, 1.379314998728842445, -1.249469950728621326 ) ) ;
#158659=CARTESIAN_POINT ( 'NONE',  ( 0.5629301599625028407, 0.6213668382478373386, 2.027498709647377773 ) ) ;
#158662=CARTESIAN_POINT ( 'NONE',  ( 3.683996026499200660, -1.166640140252427793, -1.577160851978461009 ) ) ;
#158663=CARTESIAN_POINT ( 'NONE',  ( 1.305796196612364124, -0.5247483525172502716, 2.096912610238470975 ) ) ;
#158667=CARTESIAN_POINT ( 'NONE',  ( 2.888294976258547475, 1.492474662269949182, -0.8948698564717886272 ) ) ;
#158671=CARTESIAN_POINT ( 'NONE',  ( 2.495470048217228065, 1.954872899240958972, 0.4925676099705801891 ) ) ;
#158672=CARTESIAN_POINT ( 'NONE',  ( 6.825078400183555161, 2.003297025668087983, 2.546134486959560572 ) ) ;
#158674=CARTESIAN_POINT ( 'NONE',  ( 2.852367248507085229, 0.6625980423298013511, 1.856917580869015039 ) ) ;
#158675=CARTESIAN_POINT ( 'NONE',  ( 5.906500813101932756, -1.903809282439900219, -0.1807861040028224398 ) ) ;
#158680=CARTESIAN_POINT ( 'NONE',  ( 1.717450570094357865, 1.680397536943441406, 1.120097702336475987 ) ) ;
#158682=CARTESIAN_POINT ( 'NONE',  ( 5.684705870536221894, -2.249774798156725986, -0.5126945500162644054 ) ) ;
#158683=CARTESIAN_POINT ( 'NONE',  ( 5.881297811770386907, -0.04968318840743202180, 1.961410508136133712 ) ) ;
#158685=CARTESIAN_POINT ( 'NONE',  ( 3.502741298630154709, 0.4721981695934416856, 1.903977903881831191 ) ) ;
#158687=CARTESIAN_POINT ( 'NONE',  ( 0.8619541869999207684, -0.05229984143813663777, -2.015912905633105101 ) ) ;
#158689=CARTESIAN_POINT ( 'NONE',  ( 1.235738130824210357, 0.6087300624019938988, -2.027988197625143929 ) ) ;
#158692=CARTESIAN_POINT ( 'NONE',  ( 1.605144257462550517, -1.827384369528777031, 0.2241066044648756805 ) ) ;
#158695=CARTESIAN_POINT ( 'NONE',  ( 2.900754761704402274, -2.089926006748676457, -0.3584049868644647585 ) ) ;
#158699=CARTESIAN_POINT ( 'NONE',  ( 2.794271844819782302, -2.055044804604218456, -0.1548302833056774130 ) ) ;
#158701=CARTESIAN_POINT ( 'NONE',  ( 1.434833617064284805, -1.334073193498284793, -1.269287082821937362 ) ) ;
#158707=CARTESIAN_POINT ( 'NONE',  ( 0.9618826090718561872, 0.4271145061440981272, -2.164990749644220447 ) ) ;
#158708=CARTESIAN_POINT ( 'NONE',  ( 2.144175119285938180, 0.8672398327666650530, -2.089775168228876545 ) ) ;
#158710=CARTESIAN_POINT ( 'NONE',  ( 2.707043852439145581, 1.551706383644942289, -0.9346757785875584590 ) ) ;
#158711=CARTESIAN_POINT ( 'NONE',  ( 3.098755142807321672, 1.734096097442457518, 0.8144269386064789673 ) ) ;
#158712=CARTESIAN_POINT ( 'NONE',  ( 4.721179655770254335, -1.847879960204744432, -0.9338546512941485744 ) ) ;
#158714=CARTESIAN_POINT ( 'NONE',  ( 2.764479830724082543, -1.360639549628063882, 1.426867346614549836 ) ) ;
#158715=CARTESIAN_POINT ( 'NONE',  ( 0.2703664580724125521, -1.260843473572888396, 1.456531361591931972 ) ) ;
#158716=CARTESIAN_POINT ( 'NONE',  ( 4.047608660086319254, 0.6306619223146043840, -1.761260876548931709 ) ) ;
#158717=CARTESIAN_POINT ( 'NONE',  ( 1.875998176474055423, 2.207483416130914478, -0.6726682516732527262 ) ) ;
#158719=CARTESIAN_POINT ( 'NONE',  ( 3.332308176975990577, -1.110599006344037853, 1.493168399320473627 ) ) ;
#158725=CARTESIAN_POINT ( 'NONE',  ( 0.3289212212809545788, 2.016005455721520345, 0.6092940615431781115 ) ) ;
#158727=CARTESIAN_POINT ( 'NONE',  ( 6.309879873373573922, -2.146112031266556919, 0.2576265230809087758 ) ) ;
#158728=CARTESIAN_POINT ( 'NONE',  ( 0.1057309665696047341, 1.499486454312322525, 1.353398366655131246 ) ) ;
#158737=CARTESIAN_POINT ( 'NONE',  ( 4.505092375653735992, -0.09411930587044713137, 2.014432893821124004 ) ) ;
#158741=CARTESIAN_POINT ( 'NONE',  ( 6.227428301493934448, -2.037140905555033576, 0.7235935974677574212 ) ) ;
#158745=CARTESIAN_POINT ( 'NONE',  ( 6.169546029190325243, 1.392557221580101423, 1.458547251757099650 ) ) ;
#158749=CARTESIAN_POINT ( 'NONE',  ( 1.295042460130943152, 1.303850460046240833, 1.129354085073847491 ) ) ;
#158754=CARTESIAN_POINT ( 'NONE',  ( 0.8074156707096367125, -1.761990802586909766, 0.1653023320123351292 ) ) ;
#158755=CARTESIAN_POINT ( 'NONE',  ( 2.192043262494451916, 1.240095455230303401, 1.585687145212981042 ) ) ;
#158757=CARTESIAN_POINT ( 'NONE',  ( 4.120313900606538127, -1.131812998600056241, -1.894281110011143632 ) ) ;
#158758=CARTESIAN_POINT ( 'NONE',  ( 5.682552277248558603, 1.299237613850280360, -1.739252610423980938 ) ) ;
#158762=CARTESIAN_POINT ( 'NONE',  ( 3.545663791850160784, -1.958584582392399742, 0.8131309587096480218 ) ) ;
#158763=CARTESIAN_POINT ( 'NONE',  ( 2.355092412869797869, 0.09611577090188135053, -2.014234804981252847 ) ) ;
#158764=CARTESIAN_POINT ( 'NONE',  ( 3.375094514129430845, -1.600109896321648462, -0.8493348278759412784 ) ) ;
#158768=CARTESIAN_POINT ( 'NONE',  ( 0.2154177506630133854, -1.835460468737951878, 0.3602540799089171131 ) ) ;
#158770=CARTESIAN_POINT ( 'NONE',  ( 5.690036971771410101, -0.8169618954828453683, 1.632782195682795257 ) ) ;
#158772=CARTESIAN_POINT ( 'NONE',  ( 1.112342557844925750, 1.847186106069747646, 0.5076494344821417259 ) ) ;
#158779=CARTESIAN_POINT ( 'NONE',  ( 3.340189922722580196, -1.266226476691566738, -1.700888996046201029 ) ) ;
#158780=CARTESIAN_POINT ( 'NONE',  ( -0.1298852118744100725, 0.003815113116375101580, -1.726395881205537330 ) ) ;
#158782=CARTESIAN_POINT ( 'NONE',  ( 4.727780648284140241, -1.210341919374293473, -1.556009220651358715 ) ) ;
#158783=CARTESIAN_POINT ( 'NONE',  ( 6.099862406061942188, 1.323743610676546334, 1.380425988546908567 ) ) ;
#158785=CARTESIAN_POINT ( 'NONE',  ( 0.3162073025194310771, 1.084344979787469354, -1.818339158833045976 ) ) ;
#158787=CARTESIAN_POINT ( 'NONE',  ( 1.100149375694438714, 0.8407228983892693908, -1.892171374333020406 ) ) ;
#158788=CARTESIAN_POINT ( 'NONE',  ( 3.011592816664434569, -0.9578117005206161494, -1.689242170645321339 ) ) ;
#158792=CARTESIAN_POINT ( 'NONE',  ( 3.222686667372671732, 0.05170946606813638102, 2.090169120961588245 ) ) ;
#158795=CARTESIAN_POINT ( 'NONE',  ( 0.6624192275643402406, 0.5246805835648783445, 1.733790746550630146 ) ) ;
#158797=CARTESIAN_POINT ( 'NONE',  ( 5.180388087185870738, -1.228261608319089149, 1.833297759731546073 ) ) ;
#158800=CARTESIAN_POINT ( 'NONE',  ( 3.294164632606086940, -0.8960083017303889230, 2.016869484631748310 ) ) ;
#158803=CARTESIAN_POINT ( 'NONE',  ( 1.787617358713189386, 1.829539840090635749, -0.5563488465884156575 ) ) ;
#158805=CARTESIAN_POINT ( 'NONE',  ( 4.967269779104159788, 1.799668380515654142, 1.023422521214325309 ) ) ;
#158808=CARTESIAN_POINT ( 'NONE',  ( 3.063507763784904192, 0.3185916186679502715, -2.137983152197140413 ) ) ;
#158809=CARTESIAN_POINT ( 'NONE',  ( 4.722331747100577459, 2.097238624054961864, 0.6360808509995665716 ) ) ;
#158820=CARTESIAN_POINT ( 'NONE',  ( 6.332887962430945983, -1.963924782908726296, -0.6550794379977520343 ) ) ;
#158821=CARTESIAN_POINT ( 'NONE',  ( 4.828697303143684394, 1.844096510799615674, 0.5574245839122073942 ) ) ;
#158822=CARTESIAN_POINT ( 'NONE',  ( 6.380470236391142080, -0.5646626916907444560, -2.040458243955853401 ) ) ;
#158826=CARTESIAN_POINT ( 'NONE',  ( 4.996905641018499544, 0.3326216897534995387, 1.940969171785451364 ) ) ;
#158827=CARTESIAN_POINT ( 'NONE',  ( 0.2346725361867564585, 0.3788711812165134196, 2.158297013397599162 ) ) ;
#158828=CARTESIAN_POINT ( 'NONE',  ( 4.846238042176662653, 1.821038859956089606, 0.1311717439725426648 ) ) ;
#158834=CARTESIAN_POINT ( 'NONE',  ( 2.647807870277216757, 0.6224553824519338807, 1.732961026760751366 ) ) ;
#158835=CARTESIAN_POINT ( 'NONE',  ( 5.818613517226002507, -0.7285450932710479943, -1.876915101588324974 ) ) ;
#158836=CARTESIAN_POINT ( 'NONE',  ( 1.265469760322552206, -2.298542322993640141, 0.001328286606278733300 ) ) ;
#158837=CARTESIAN_POINT ( 'NONE',  ( 5.366048076001885825, -1.952644961629325548, 0.1885061251027941032 ) ) ;
#158841=CARTESIAN_POINT ( 'NONE',  ( 0.7134375191242479097, -1.748147108003229810, -1.108949491591210146 ) ) ;
#158843=CARTESIAN_POINT ( 'NONE',  ( 1.189138979623612480, 1.585436599910443611, 1.363068659274695893 ) ) ;
#158844=CARTESIAN_POINT ( 'NONE',  ( 6.649276393164253562, -1.424495517243940856, -1.050074490644896441 ) ) ;
#158847=CARTESIAN_POINT ( 'NONE',  ( 1.610509732637079638, -0.2130687159686726062, 1.727248725346673952 ) ) ;
#158851=CARTESIAN_POINT ( 'NONE',  ( 2.314726122855132129, 1.540323329518531903, 0.7764098835694576151 ) ) ;
#158852=CARTESIAN_POINT ( 'NONE',  ( 2.437293137456029157, -1.626093413141915134, -1.469474007205706645 ) ) ;
#158853=CARTESIAN_POINT ( 'NONE',  ( 5.303435803989668074, 1.802500012205746183, 1.273053691228965389 ) ) ;
#158856=CARTESIAN_POINT ( 'NONE',  ( 2.922911270491454161, -1.500192211782652718, 1.569583652781519012 ) ) ;
#158857=CARTESIAN_POINT ( 'NONE',  ( 1.330379832379691818, 1.758967509726565792, 0.4888242021733391618 ) ) ;
#158858=CARTESIAN_POINT ( 'NONE',  ( 3.450509668567053545, -1.418736885945747428, 1.571922360790501738 ) ) ;
#158861=CARTESIAN_POINT ( 'NONE',  ( 3.878722286802076535, -0.2252994024176681598, -2.281293266731793778 ) ) ;
#158866=CARTESIAN_POINT ( 'NONE',  ( 6.270221287042929248, 2.215581787426896376, -0.1604564985231044516 ) ) ;
#158872=CARTESIAN_POINT ( 'NONE',  ( 3.990861413484114273, -2.010826503599131065, 0.1511389102963680842 ) ) ;
#158874=CARTESIAN_POINT ( 'NONE',  ( 2.096602096640389767, 2.039512422605322950, 0.3069443246750125365 ) ) ;
#158879=CARTESIAN_POINT ( 'NONE',  ( 5.103566685217446164, -2.181124530238859993, 0.2125310249164805709 ) ) ;
#158880=CARTESIAN_POINT ( 'NONE',  ( 3.832657856672664565, 0.6767144645295587457, -1.899618369658891748 ) ) ;
#158881=CARTESIAN_POINT ( 'NONE',  ( 2.261056740009634414, 1.805359621025553363, -0.3608742708730780513 ) ) ;
#158885=CARTESIAN_POINT ( 'NONE',  ( 6.159193757800505153, -1.567253032978152660, -0.9359774744091067245 ) ) ;
#158887=CARTESIAN_POINT ( 'NONE',  ( 6.157125652023562878, -1.936745554134344349, -1.169425401991762259 ) ) ;
#158889=CARTESIAN_POINT ( 'NONE',  ( 1.963634227113943087, 0.3588053174017143965, -2.075111507017588064 ) ) ;
#158893=( NAMED_UNIT ( * ) SI_UNIT ( $, .STERADIAN. ) SOLID_ANGLE_UNIT ( ) );
#158894=MANIFOLD_SOLID_BREP ( 'Sweep1[6]', #63736 ) ;
#158900=CARTESIAN_POINT ( 'NONE',  ( 2.725082634249659463, 1.605975871135911559, -1.534981474645187971 ) ) ;
#158901=CARTESIAN_POINT ( 'NONE',  ( -0.01666059994226073634, -0.1612322585618740090, -2.171656592459796808 ) ) ;
#158905=CARTESIAN_POINT ( 'NONE',  ( 4.351973852746993110, -0.7528527933186466292, 1.811862133468461922 ) ) ;
#158913=CARTESIAN_POINT ( 'NONE',  ( 3.269896953881154644, 0.5115095171020591636, -2.057881918134551125 ) ) ;
#158915=CARTESIAN_POINT ( 'NONE',  ( 4.715790015261832835, -2.120648752638915724, 0.4184459369844309440 ) ) ;
#158916=CARTESIAN_POINT ( 'NONE',  ( 4.405690278861111864, -0.7914791229979671883, -1.662609734262666894 ) ) ;
#158919=CARTESIAN_POINT ( 'NONE',  ( 6.210887288261135453, -0.2055507460125911567, 1.728089712739445671 ) ) ;
#158920=CARTESIAN_POINT ( 'NONE',  ( 6.727182134110200273, 2.469373133786161745, 2.195552656936059055 ) ) ;
#158923=CARTESIAN_POINT ( 'NONE',  ( 2.501032641837992454, 1.736685530831501456, -1.287010829427559289 ) ) ;
#158925=CARTESIAN_POINT ( 'NONE',  ( 6.011092252151500226, 2.013677719867816851, 0.1017325769363253418 ) ) ;
#158927=CARTESIAN_POINT ( 'NONE',  ( 2.008865009297224447, 1.601992838228694316, -1.451600824242594845 ) ) ;
#158928=CARTESIAN_POINT ( 'NONE',  ( 4.024654096683129900, 1.870930367033913688, 0.6213144229534044438 ) ) ;
#158930=CARTESIAN_POINT ( 'NONE',  ( 1.378406844460399405, 1.376398589878137013, 1.852031911770692263 ) ) ;
#158931=CARTESIAN_POINT ( 'NONE',  ( 3.966302600639686204, -1.813262256789631266, -0.6959421042645166366 ) ) ;
#158940=CARTESIAN_POINT ( 'NONE',  ( 2.345003271878861373, 0.4830727525354863716, 2.153096645625157457 ) ) ;
#158943=CARTESIAN_POINT ( 'NONE',  ( 6.244970037249994554, -0.2844439363869250004, -1.940879991452467479 ) ) ;
#158947=CARTESIAN_POINT ( 'NONE',  ( 0.1749903794560566661, 7.629137130509112907, -2.555305779167945435 ) ) ;
#158949=CARTESIAN_POINT ( 'NONE',  ( 5.173706384855800700, -1.019854773079221344, 1.532662130498331887 ) ) ;
#158957=CARTESIAN_POINT ( 'NONE',  ( 0.7607050128039081205, -1.493160483426679841, 1.420726879377065988 ) ) ;
#158959=CARTESIAN_POINT ( 'NONE',  ( 2.207255083745041979, -1.492367883816644314, -1.111680554738720073 ) ) ;
#158960=CARTESIAN_POINT ( 'NONE',  ( 5.196754805642953556, 1.508532920973480795, 1.055450849767838317 ) ) ;
#158967=CARTESIAN_POINT ( 'NONE',  ( 4.828867971087246858, 2.111205472107956282, 0.6427781511747706622 ) ) ;
#158968=CARTESIAN_POINT ( 'NONE',  ( 6.538354595224527444, 2.236366790538524718, 0.3417416818044561877 ) ) ;
#158970=CARTESIAN_POINT ( 'NONE',  ( 5.941655795435678122, -1.702662506596404279, 0.6190658298997688824 ) ) ;
#158971=CARTESIAN_POINT ( 'NONE',  ( 0.05782782957228919940, 1.164991625563294386, 1.645756161228327130 ) ) ;
#158974=CARTESIAN_POINT ( 'NONE',  ( 5.584596538761582352, -1.209766832763665034, 1.480987728393488023 ) ) ;
#158975=CARTESIAN_POINT ( 'NONE',  ( 0.9361565222895779081, 1.842281575443193375, 0.3236747858033904302 ) ) ;
#158976=CARTESIAN_POINT ( 'NONE',  ( 2.817592499383800853, -1.357869084745389809, -1.490969456672403881 ) ) ;
#158978=CARTESIAN_POINT ( 'NONE',  ( 3.826872495277617414, 1.999758222635793947, 0.6608955202877621060 ) ) ;
#158983=CARTESIAN_POINT ( 'NONE',  ( 3.146744605306639908, 1.971464920705681800, 0.4384460897248109723 ) ) ;
#158987=CARTESIAN_POINT ( 'NONE',  ( 3.954491917119377753, 0.7739500986865335275, 2.018479124525011770 ) ) ;
#158994=CARTESIAN_POINT ( 'NONE',  ( 1.750661792711872611, -2.160631921778751519, -0.2139166996905516871 ) ) ;
#158997=CARTESIAN_POINT ( 'NONE',  ( 0.5734669319550633748, -1.023298125840161887, 1.530493987491374330 ) ) ;
#159000=CARTESIAN_POINT ( 'NONE',  ( 1.945129482973105839, -1.762486321751283835, -1.302348873264857820 ) ) ;
#159001=CARTESIAN_POINT ( 'NONE',  ( 6.883263157960367806, 6.035304072343574688, 2.648703854151325032 ) ) ;
#159002=CARTESIAN_POINT ( 'NONE',  ( 2.589068414660402606, -0.3862909535316555454, -2.229145898733439157 ) ) ;
#159008=CARTESIAN_POINT ( 'NONE',  ( 4.411239408862893008, -0.3036837672792407905, 1.743313046103856179 ) ) ;
#159010=CARTESIAN_POINT ( 'NONE',  ( 0.5519644926167607268, 0.6605455615449079554, -1.999741160550670527 ) ) ;
#159014=CARTESIAN_POINT ( 'NONE',  ( 6.257435441360899908, 1.928747933193178721, -0.5880367767025842518 ) ) ;
#159015=CARTESIAN_POINT ( 'NONE',  ( 5.256058454422637638, 0.7267480909730811289, -1.659609831382781397 ) ) ;
#159018=CARTESIAN_POINT ( 'NONE',  ( 3.256579335763456040, -1.417408692332474462, 1.220890361658559575 ) ) ;
#159019=CARTESIAN_POINT ( 'NONE',  ( 3.889561532384703924, -1.914723906051108315, 0.7877538119766480662 ) ) ;
#159028=CARTESIAN_POINT ( 'NONE',  ( 3.930091730393743710, 1.087902980620155891, 1.632394305395828304 ) ) ;
#159029=CARTESIAN_POINT ( 'NONE',  ( 1.054064285791616262, 1.779355684154381834, -0.9478921834336280217 ) ) ;
#159032=CARTESIAN_POINT ( 'NONE',  ( 0.4384654110765589530, 0.3132546388123040870, 1.843968665737522050 ) ) ;
#159034=CARTESIAN_POINT ( 'NONE',  ( 3.252200647028923974, 0.9015175226297014177, -1.800113812977667038 ) ) ;
#159036=CARTESIAN_POINT ( 'NONE',  ( 2.988026824963069927, -2.114671507216555391, 0.1067447620008883935 ) ) ;
#159037=CARTESIAN_POINT ( 'NONE',  ( 6.825078400183555161, 2.951006455646577820, 2.596623860847916188 ) ) ;
#159038=CARTESIAN_POINT ( 'NONE',  ( 4.879381568908511824, -0.1049739508458477355, 2.067839077007492143 ) ) ;
#159040=CARTESIAN_POINT ( 'NONE',  ( 0.1696251593464107033, 1.207222248521317765, 1.706790159955206887 ) ) ;
#159042=CARTESIAN_POINT ( 'NONE',  ( 5.754876975610782708, -1.437719105923901841, 1.124948175183659638 ) ) ;
#159048=CARTESIAN_POINT ( 'NONE',  ( 6.791986947960565679, -0.9495855537378706801, 1.990061496475347802 ) ) ;
#159050=CARTESIAN_POINT ( 'NONE',  ( 6.633470332280523074, -0.1331818211787652029, 1.881796397474523541 ) ) ;
#159058=CARTESIAN_POINT ( 'NONE',  ( 0.07700591528349286230, 5.724620991219308230, -2.504819247423330175 ) ) ;
#159061=( NAMED_UNIT ( * ) PLANE_ANGLE_UNIT ( ) SI_UNIT ( $, .RADIAN. ) );
#159062=CARTESIAN_POINT ( 'NONE',  ( 0.1394461523056772234, 0.2496508530322391062, -1.754170159799403717 ) ) ;
#159065=CARTESIAN_POINT ( 'NONE',  ( 1.850388327615314799, -1.959487253598888312, -0.1980615517182797158 ) ) ;
#159066=CARTESIAN_POINT ( 'NONE',  ( 3.655875201264874974, 1.122517324909186653, 1.674876314423722423 ) ) ;
#159068=CARTESIAN_POINT ( 'NONE',  ( 6.827182134110222123, -0.006956174471953178659, 2.188967759425272330 ) ) ;
#159069=CARTESIAN_POINT ( 'NONE',  ( 3.855584222106961612, 2.174980185927982923, -0.2676557845137442215 ) ) ;
#159071=CARTESIAN_POINT ( 'NONE',  ( 1.764547866544708521, -1.364041108321904616, 1.360535031132574568 ) ) ;
#159074=CARTESIAN_POINT ( 'NONE',  ( 0.2331563151865486683, 2.034376611827843906, -2.362208330281903024 ) ) ;
#159081=CARTESIAN_POINT ( 'NONE',  ( 5.882333747326812023, -0.2767177626767613474, -1.820229446528654371 ) ) ;
#159082=CARTESIAN_POINT ( 'NONE',  ( 2.578773234406753101, -1.386572882437474341, 1.459666011457598556 ) ) ;
#159083=CARTESIAN_POINT ( 'NONE',  ( 4.165566195501821056, -0.7159155550505342802, -2.184124419653421523 ) ) ;
#159084=CARTESIAN_POINT ( 'NONE',  ( -0.02900071798685177615, 6.946858727649162901, -2.768864135414349281 ) ) ;
#159085=CARTESIAN_POINT ( 'NONE',  ( 2.289708051090312058, -1.211253549455925338, -1.412920978024762908 ) ) ;
#159090=CARTESIAN_POINT ( 'NONE',  ( 4.898031494525131535, -0.7058569028579181337, -1.968109489924846356 ) ) ;
#159091=CARTESIAN_POINT ( 'NONE',  ( 4.364026845288040413, 0.8817440624687390427, 1.649792572839225091 ) ) ;
#159094=CARTESIAN_POINT ( 'NONE',  ( 6.656889574143706412, -1.327764893807031221, 1.100862838992909598 ) ) ;
#159096=CARTESIAN_POINT ( 'NONE',  ( 1.371252568922965098, -0.2536805693413109464, -1.715349781374966742 ) ) ;
#159100=CARTESIAN_POINT ( 'NONE',  ( 6.227409518260961896, 0.1680337313966096258, -2.164657318592048352 ) ) ;
#159101=CARTESIAN_POINT ( 'NONE',  ( 4.951681858558426796, 0.5695450498939165218, -1.734646904759745700 ) ) ;
#159102=CARTESIAN_POINT ( 'NONE',  ( 1.709737484509077143, 0.5745576563440238926, -1.875703277996950469 ) ) ;
#159109=CARTESIAN_POINT ( 'NONE',  ( 2.438272501909013901, -1.223040458498025673, -1.732039452853536776 ) ) ;
#159113=CARTESIAN_POINT ( 'NONE',  ( 0.4618902312403838639, -0.5555351291045197426, 1.994226918997483500 ) ) ;
#159116=CARTESIAN_POINT ( 'NONE',  ( 3.159039748919801216, 0.5414197367904579616, 2.154182169225922205 ) ) ;
#159118=CARTESIAN_POINT ( 'NONE',  ( 0.5987520574620349700, -0.3298207119002970478, 2.274815185769126114 ) ) ;
#159120=CARTESIAN_POINT ( 'NONE',  ( 6.842638575262629530, -2.021612500624434539, -0.4081942145969327251 ) ) ;
#159123=CARTESIAN_POINT ( 'NONE',  ( 0.1331565106231571705, 4.092041177288479048, -2.500854978060399691 ) ) ;
#159124=CARTESIAN_POINT ( 'NONE',  ( 5.952668924537682038, -1.582617586749142102, -0.9407850039931386910 ) ) ;
#159126=CARTESIAN_POINT ( 'NONE',  ( -0.1104750535120043037, 1.338503269012698116, -2.356272470560859755 ) ) ;
#159127=CARTESIAN_POINT ( 'NONE',  ( 3.293694421395336303, -0.6999868571894217739, 1.576533365092074757 ) ) ;
#159128=CARTESIAN_POINT ( 'NONE',  ( 1.358611653602972869, -1.916354379050893009, -0.6279873632355145174 ) ) ;
#159129=CARTESIAN_POINT ( 'NONE',  ( 3.340769233699531604, 0.5564940052410914939, -2.230230389815818892 ) ) ;
#159130=CARTESIAN_POINT ( 'NONE',  ( 2.601149388587006950, 1.818552668380982951, -1.345706882341807242 ) ) ;
#159131=CARTESIAN_POINT ( 'NONE',  ( 4.846364118386396136, 2.100373345016784743, 0.1556085008114059531 ) ) ;
#159133=CARTESIAN_POINT ( 'NONE',  ( 3.321328847770131709, -1.706417891748934546, 0.4689366942724793041 ) ) ;
#159135=CARTESIAN_POINT ( 'NONE',  ( 6.603114554492313104, -0.5110835225830052675, 2.243201349117603716 ) ) ;
#159136=CARTESIAN_POINT ( 'NONE',  ( 4.910013284106277354, 1.267360923890372693, -1.335742228452965863 ) ) ;
#159140=CARTESIAN_POINT ( 'NONE',  ( 4.347736757272717689, 2.190986304709115373, -0.05254992341368477232 ) ) ;
#159143=CARTESIAN_POINT ( 'NONE',  ( 4.387213907293201487, 0.09840592021137170575, 2.068135374880715638 ) ) ;
#159144=CARTESIAN_POINT ( 'NONE',  ( -0.03006412033006514162, -0.9462945741195265548, 1.780671068589256834 ) ) ;
#159147=CARTESIAN_POINT ( 'NONE',  ( 3.633351821168579132, -1.779675539450284560, 0.7381315413402672609 ) ) ;
#159150=CARTESIAN_POINT ( 'NONE',  ( 0.4752230700786713169, -1.603524673181003779, 1.537559121520514660 ) ) ;
#159159=CARTESIAN_POINT ( 'NONE',  ( 1.820681965693775162, -1.389665069980907663, 1.385087887197037571 ) ) ;
#159162=CARTESIAN_POINT ( 'NONE',  ( 5.055110333045015558, 1.632132345252810035, -1.088295032039228172 ) ) ;
#159165=CARTESIAN_POINT ( 'NONE',  ( 6.614160618316515361, -1.014195557614630205, -1.909021090911746654 ) ) ;
#159166=CARTESIAN_POINT ( 'NONE',  ( -0.1106727585416019261, 7.629137130509112907, -2.603481208547548054 ) ) ;
#159169=CARTESIAN_POINT ( 'NONE',  ( 0.7021627906659900775, -0.6242572379067250488, -1.763460184394528341 ) ) ;
#159170=CARTESIAN_POINT ( 'NONE',  ( 6.538463365017005202, 1.657764536579940495, -0.5080105315169358704 ) ) ;
#159172=CARTESIAN_POINT ( 'NONE',  ( 2.841561854484982774, 0.7863008361240211297, -2.045831095052422555 ) ) ;
#159173=CARTESIAN_POINT ( 'NONE',  ( 4.120403395486138542, -1.183043222452788257, -1.981120964393435768 ) ) ;
#159174=CARTESIAN_POINT ( 'NONE',  ( 5.589157960464589792, 1.819533713976368094, -0.9674792931896135650 ) ) ;
#159175=CARTESIAN_POINT ( 'NONE',  ( 2.273291157499750526, 1.194718917728957885, 1.530869066462538619 ) ) ;
#159177=CARTESIAN_POINT ( 'NONE',  ( 4.922192346260840345, -2.110166376318895587, 0.2103620946037400852 ) ) ;
#159178=CARTESIAN_POINT ( 'NONE',  ( 2.777970385693105726, 1.728001979019553325, -1.038993764437286416 ) ) ;
#159180=CARTESIAN_POINT ( 'NONE',  ( 5.297975422827020608, -0.7987165953184969247, 2.057335881587420534 ) ) ;
#159183=CARTESIAN_POINT ( 'NONE',  ( 0.1877650043593872553, -0.8638833939697135866, 1.608357707688967242 ) ) ;
#159189=CARTESIAN_POINT ( 'NONE',  ( 5.330957127283824981, 0.1492067265368417217, 2.055538663769764796 ) ) ;
#159195=CARTESIAN_POINT ( 'NONE',  ( 4.266274442087925500, 2.019191850312745284, -0.05169103710895606163 ) ) ;
#159200=CARTESIAN_POINT ( 'NONE',  ( 4.047771301309529335, 0.6961604498142616171, -1.939876652229477028 ) ) ;
#159201=CARTESIAN_POINT ( 'NONE',  ( 2.303361484738715159, 1.314996338066702242, -1.528741580717301263 ) ) ;
#159202=ORIENTED_EDGE ( 'NONE', *, *, #113502, .T. ) ;
#159207=CARTESIAN_POINT ( 'NONE',  ( 3.391953724946984661, 0.04666865176591524639, 2.015725201127672506 ) ) ;
#159208=CARTESIAN_POINT ( 'NONE',  ( 1.939159035295745959, 0.7054217538491479589, -1.700835786604155242 ) ) ;
#159209=CARTESIAN_POINT ( 'NONE',  ( 0.4875218067809834466, -0.2886260216827610803, -2.289518885299694606 ) ) ;
#159211=CARTESIAN_POINT ( 'NONE',  ( 2.636181727411972098, 1.021492356387411427, -1.905029093917938399 ) ) ;
#159213=CARTESIAN_POINT ( 'NONE',  ( 2.900137762625193183, 0.2794712830477152354, 2.281260185934708140 ) ) ;
#159216=CARTESIAN_POINT ( 'NONE',  ( 1.076777757339364205, -0.04213119042271313425, -1.870346338061685154 ) ) ;
#159218=CARTESIAN_POINT ( 'NONE',  ( 6.157099186568592231, -1.690597638883487797, -1.013973547023840460 ) ) ;
#159222=CARTESIAN_POINT ( 'NONE',  ( 0.7157882511714327434, -0.3199875008889854766, 2.183444778895065941 ) ) ;
#159225=DIRECTION ( 'NONE',  ( -1.000000000000000000, 0.000000000000000000, 0.000000000000000000 ) ) ;
#159226=CARTESIAN_POINT ( 'NONE',  ( 4.873880070992254510, 1.134317645522317175, 1.612277344948910285 ) ) ;
#159227=CARTESIAN_POINT ( 'NONE',  ( 6.258070668236964451, 0.7691888804484037223, -1.867794269369964066 ) ) ;
#159228=CARTESIAN_POINT ( 'NONE',  ( 4.002764008144163554, -0.7221186334790052896, -2.191863981390995253 ) ) ;
#159229=CARTESIAN_POINT ( 'NONE',  ( 2.588800687925230992, 1.999571085336487641, 0.5053362289856622169 ) ) ;
#159236=CARTESIAN_POINT ( 'NONE',  ( 5.617690636765501289, 0.4290425436993560715, -2.128212118068722347 ) ) ;
#159238=CARTESIAN_POINT ( 'NONE',  ( 4.440845869443198701, -1.426288408191313639, -1.164454570719307469 ) ) ;
#159241=CARTESIAN_POINT ( 'NONE',  ( 6.720655732516650716, 2.984497329163855461, 2.280179935440066252 ) ) ;
#159242=CARTESIAN_POINT ( 'NONE',  ( 5.126606437771586755, 0.1607948393855564151, 2.185736094377451089 ) ) ;
#159244=CARTESIAN_POINT ( 'NONE',  ( 0.1931282604852417040, -0.5026490872193057902, -2.214429643963564232 ) ) ;
#159250=CARTESIAN_POINT ( 'NONE',  ( 1.322737547172361472, -0.04825712817433693014, 1.769365563168373345 ) ) ;
#159251=CARTESIAN_POINT ( 'NONE',  ( 5.619794420184654804, -0.4867899507037063422, 1.953244479579784976 ) ) ;
#159253=CARTESIAN_POINT ( 'NONE',  ( 4.506922906144382956, 1.629430921360131679, -1.334182900473983135 ) ) ;
#159254=CARTESIAN_POINT ( 'NONE',  ( 3.462411278976515128, -1.846996576941996482, -0.5078680121572733963 ) ) ;
#159256=CARTESIAN_POINT ( 'NONE',  ( 4.281674416708352027, -1.885371899234816739, 0.5696992939150746782 ) ) ;
#159257=CARTESIAN_POINT ( 'NONE',  ( 5.414321571020942692, -2.019972751022606872, 0.004158903309840755735 ) ) ;
#159258=CARTESIAN_POINT ( 'NONE',  ( 1.516246529245099284, 1.258767711876613848, -1.383943980506313398 ) ) ;
#159259=CARTESIAN_POINT ( 'NONE',  ( 5.320820994898000755, 1.595919931443249951, 0.6549295409969541071 ) ) ;
#159260=CARTESIAN_POINT ( 'NONE',  ( 1.300873410958070409, -0.2835801433653042380, -1.891145142470892715 ) ) ;
#159262=CARTESIAN_POINT ( 'NONE',  ( 2.016531038934398445, -1.041976349804032420, -1.945408382319254503 ) ) ;
#159266=CARTESIAN_POINT ( 'NONE',  ( 6.285602425426498385, -1.847771260692541162, 0.6596951833430019230 ) ) ;
#159274=CARTESIAN_POINT ( 'NONE',  ( 2.383334800519558705, -0.002349189141126820958, 2.070544812199434315 ) ) ;
#159279=CARTESIAN_POINT ( 'NONE',  ( 6.410795937096152919, -0.5649949523399040441, -2.043744576961013859 ) ) ;
#159284=CARTESIAN_POINT ( 'NONE',  ( 5.290388671387995068, -1.915306256023458831, 0.6297802918850337051 ) ) ;
#159285=CARTESIAN_POINT ( 'NONE',  ( 4.294081978838642399, -0.8244651323695743050, -1.729401801750865442 ) ) ;
#159287=CARTESIAN_POINT ( 'NONE',  ( 2.911879292414457865, -1.082406496695037301, -1.905547650945007554 ) ) ;
#159288=CARTESIAN_POINT ( 'NONE',  ( 0.1335669894368292088, 2.005130876877735613, -2.568368839946821414 ) ) ;
#159290=CARTESIAN_POINT ( 'NONE',  ( 5.449481901252090310, -1.818156339564154012, 0.8647962134734816786 ) ) ;
#159291=CARTESIAN_POINT ( 'NONE',  ( 1.828231037913151447, -0.9045423626323212396, -1.684975973026317408 ) ) ;
#159294=CARTESIAN_POINT ( 'NONE',  ( -0.07068620461728526705, -1.560437159073333468, -1.276799021846956705 ) ) ;
#159296=CARTESIAN_POINT ( 'NONE',  ( 3.298458272841266137, 1.646618950329106434, -1.288217307904614639 ) ) ;
#159298=CARTESIAN_POINT ( 'NONE',  ( 2.309205411980755240, -0.3811568730716380915, 1.681943839628738058 ) ) ;
#159300=CARTESIAN_POINT ( 'NONE',  ( 6.381110825713084189, -1.939362502171553482, -0.8581636585355472135 ) ) ;
#159310=CARTESIAN_POINT ( 'NONE',  ( 2.385177931559249398, 0.08740048966574034961, -1.809473338476126569 ) ) ;
#159316=CARTESIAN_POINT ( 'NONE',  ( 4.266123773889715309, 1.810994338341217480, -0.04873877536224096446 ) ) ;
#159317=CARTESIAN_POINT ( 'NONE',  ( 6.639320575229290533, 2.050619746573784763, 2.302922995531462291 ) ) ;
#159321=CARTESIAN_POINT ( 'NONE',  ( 3.965176940185519250, 1.595341564286660629, 0.9581005465538834365 ) ) ;
#159322=CARTESIAN_POINT ( 'NONE',  ( 1.405720392582618938, -1.065544983005232371, -1.591680324291492310 ) ) ;
#159323=CARTESIAN_POINT ( 'NONE',  ( 1.395219695971817941, 1.379742824092672349, 1.195523663710513995 ) ) ;
#159331=CARTESIAN_POINT ( 'NONE',  ( 5.541845313694261144, 1.319919544752303331, 1.461889559981154108 ) ) ;
#159334=CARTESIAN_POINT ( 'NONE',  ( 0.3047781727255130524, 1.820093451774043691, 1.028452505696121344 ) ) ;
#159336=CARTESIAN_POINT ( 'NONE',  ( 5.315425438393720725, -0.2827910679824903184, 1.905415604636887750 ) ) ;
#159338=CARTESIAN_POINT ( 'NONE',  ( 1.324926479183065497, -0.04897172810776688479, 1.825096452545173609 ) ) ;
#159339=CARTESIAN_POINT ( 'NONE',  ( 1.928631425534212074, 1.268998755960360603, -1.805353087401928569 ) ) ;
#159340=CARTESIAN_POINT ( 'NONE',  ( 0.8965662283535699162, -1.866366896104875162, -0.4163465257057268332 ) ) ;
#159342=CARTESIAN_POINT ( 'NONE',  ( 6.860212146170862724, -1.969081375482661267, 0.04489377202578949400 ) ) ;
#159343=CARTESIAN_POINT ( 'NONE',  ( 3.069799403425711226, -1.154559939549955949, 1.561474065217777207 ) ) ;
#159345=CARTESIAN_POINT ( 'NONE',  ( 1.106795812180675798, 0.8196504822069600182, -1.842164015508622521 ) ) ;
#159347=CARTESIAN_POINT ( 'NONE',  ( 6.473497990634856869, -0.2285008921534004422, 1.846817554525240990 ) ) ;
#159353=CARTESIAN_POINT ( 'NONE',  ( 3.087623348389135547, -0.8860277256741244667, 2.004638750299721828 ) ) ;
#159357=CARTESIAN_POINT ( 'NONE',  ( 2.314841291766779108, 1.630546960418734148, 0.8213866120303781049 ) ) ;
#159361=CARTESIAN_POINT ( 'NONE',  ( -0.02968770228137588424, 5.725071598255107475, -2.420367217772397606 ) ) ;
#159363=CARTESIAN_POINT ( 'NONE',  ( 1.488762753728092969, -0.2822029396061729867, -1.905608977972670370 ) ) ;
#159364=CARTESIAN_POINT ( 'NONE',  ( 5.506681978947471912, 0.5658967987182733639, 1.878394690154854496 ) ) ;
#159368=ADVANCED_FACE ( 'NONE', ( #91675 ), #32330, .F. ) ;
#159369=CARTESIAN_POINT ( 'NONE',  ( 5.390230798962840630, -0.5317533105795355652, -2.125930911514521959 ) ) ;
#159372=CARTESIAN_POINT ( 'NONE',  ( 3.573154620739454224, 1.869565233029608198, 0.8895530118792621677 ) ) ;
#159376=CARTESIAN_POINT ( 'NONE',  ( 4.465672607755381662, -2.229637596627360718, -0.5588700134179708234 ) ) ;
#159382=CARTESIAN_POINT ( 'NONE',  ( 3.978411374042570170, -0.1916562231945718731, -1.932471992628071789 ) ) ;
#159385=ADVANCED_FACE ( 'NONE', ( #45052 ), #93804, .T. ) ;
#159387=CARTESIAN_POINT ( 'NONE',  ( 5.431871263539022721, -1.864374737420209760, 0.4251265778823994368 ) ) ;
#159388=CARTESIAN_POINT ( 'NONE',  ( 6.792093547228882144, -0.7321312287554645470, 1.560492760358098918 ) ) ;
#159389=CARTESIAN_POINT ( 'NONE',  ( 4.839077477813122918, -1.706110771555340744, -1.074664961451990308 ) ) ;
#159393=CARTESIAN_POINT ( 'NONE',  ( 1.218821504741087969, -0.04963993015681333193, 2.090216850290891326 ) ) ;
#159394=CARTESIAN_POINT ( 'NONE',  ( 6.889980056308100842, -0.7542815031014777905, 1.599730008835710482 ) ) ;
#159395=CARTESIAN_POINT ( 'NONE',  ( 5.889296118903345700, -0.7283762112263308941, -1.880435897373772258 ) ) ;
#159397=CARTESIAN_POINT ( 'NONE',  ( 3.609589514692018053, -2.258491968568816066, 0.3911977494595666460 ) ) ;
#159398=CARTESIAN_POINT ( 'NONE',  ( 0.6908507670086707630, -0.6304954947415147837, 1.622297741125192427 ) ) ;
#159399=CARTESIAN_POINT ( 'NONE',  ( 3.164422831683691761, 2.120778211551369807, -0.003951117757632071313 ) ) ;
#159401=CARTESIAN_POINT ( 'NONE',  ( 0.5437846328400409712, 1.620832503561630666, -0.6162787013818531445 ) ) ;
#159403=CARTESIAN_POINT ( 'NONE',  ( 1.275590745840638363, -1.816738662498600165, 0.4029602180237248366 ) ) ;
#159404=CARTESIAN_POINT ( 'NONE',  ( 0.7839114044838908502, -2.061656150924387365, 0.6811309647984428173 ) ) ;
#159405=CARTESIAN_POINT ( 'NONE',  ( 2.993375309983861143, -0.3886322325962355273, 1.978555244300662874 ) ) ;
#159406=CARTESIAN_POINT ( 'NONE',  ( 4.187500000000002665, -1.451031289060945584, 1.451031289061284646 ) ) ;
#159408=CARTESIAN_POINT ( 'NONE',  ( 6.639296574806412110, -1.719437650081551139, 0.8690664522189944785 ) ) ;
#159410=CARTESIAN_POINT ( 'NONE',  ( 2.918465973627711652, -2.218669909917521998, 0.1131645065166643205 ) ) ;
#159416=CARTESIAN_POINT ( 'NONE',  ( 6.398696371038459674, -2.178289998122169280, -0.4347530419120289036 ) ) ;
#159417=MECHANICAL_DESIGN_GEOMETRIC_PRESENTATION_REPRESENTATION('',(#45191),#197441);
#159418=CARTESIAN_POINT ( 'NONE',  ( 4.967221142815226642, 1.706001049663580460, 0.9686458024478412643 ) ) ;
#159421=DIRECTION ( 'NONE',  ( 1.039099362110107450E-15, 1.000000000000000000, -4.583713267641621330E-32 ) ) ;
#159422=CARTESIAN_POINT ( 'NONE',  ( 6.186863813140405455, -0.3229369685709322924, -2.239133911541963506 ) ) ;
#159423=CARTESIAN_POINT ( 'NONE',  ( 2.277848244636628827, -2.001361501815647870, 0.4987805053587587856 ) ) ;
#159428=CARTESIAN_POINT ( 'NONE',  ( 3.268673085221412311, -1.727008210369033847, -0.7190761260571986169 ) ) ;
#159429=CARTESIAN_POINT ( 'NONE',  ( 2.338123177510130102, 0.4612838472501363252, -1.671594290515050041 ) ) ;
#159430=CARTESIAN_POINT ( 'NONE',  ( 0.1524363970008953684, 0.8851206712186098224, 2.114804356544320640 ) ) ;
#159431=CARTESIAN_POINT ( 'NONE',  ( 1.079469989902905214, -0.05558308599296066244, -2.206230565744627281 ) ) ;
#159432=CARTESIAN_POINT ( 'NONE',  ( 3.520547545725543515, 1.372905562624787024, -1.669742455111824286 ) ) ;
#159433=CARTESIAN_POINT ( 'NONE',  ( 5.437426780092255996, 0.7852709207246920675, -1.776270868113111856 ) ) ;
#159436=CARTESIAN_POINT ( 'NONE',  ( 0.03128095451081137207, -0.7860540964617872550, -1.895863743164089676 ) ) ;
#159437=CARTESIAN_POINT ( 'NONE',  ( -0.1399997263889594112, -0.002789056014654289761, -2.000146600338557956 ) ) ;
#159444=CARTESIAN_POINT ( 'NONE',  ( 3.580510235063854019, -1.759844519496515325, -0.4856381957471164745 ) ) ;
#159445=CARTESIAN_POINT ( 'NONE',  ( 2.485638465518677176, 2.017858404210779888, -0.8937526715337427152 ) ) ;
#159451=CARTESIAN_POINT ( 'NONE',  ( 0.7561249178302269502, 0.8145892717734238841, -1.848413388458100215 ) ) ;
#159452=CARTESIAN_POINT ( 'NONE',  ( 1.418772191123615078, -0.7664089246972278779, -1.977313068770427229 ) ) ;
#159455=CARTESIAN_POINT ( 'NONE',  ( 3.502650316321722634, 0.4479755722775873861, 1.806107967122023927 ) ) ;
#159457=CARTESIAN_POINT ( 'NONE',  ( 0.6378455412261313517, -1.529572671500577297, -1.527792216034072670 ) ) ;
#159458=CARTESIAN_POINT ( 'NONE',  ( 5.731092321990707283, 2.014232586630093191, 0.09613807139101374077 ) ) ;
#159460=CARTESIAN_POINT ( 'NONE',  ( -0.01814341541641998484, -1.915199053885572988, -0.04638162876333290496 ) ) ;
#159462=CARTESIAN_POINT ( 'NONE',  ( 4.160648861918358143, -1.351394993475165673, 1.227733137840483879 ) ) ;
#159467=CARTESIAN_POINT ( 'NONE',  ( 6.591172692507557329, 1.163088239368128773, -1.646588791553056152 ) ) ;
#159468=CARTESIAN_POINT ( 'NONE',  ( 5.507694354943953208, -0.8313836724207699369, -1.642813217252625524 ) ) ;
#159471=CARTESIAN_POINT ( 'NONE',  ( 4.371882800840491967, 2.239072524489620353, -0.5581132647194796403 ) ) ;
#159473=CARTESIAN_POINT ( 'NONE',  ( 0.2630567961459496784, -1.839733103847444928, -0.9287307787974752316 ) ) ;
#159475=CARTESIAN_POINT ( 'NONE',  ( 1.856878829904203165, 0.3300924852138227283, -1.913646475244117795 ) ) ;
#159476=CARTESIAN_POINT ( 'NONE',  ( 5.694729993868760332, -1.451380474000956156, -1.782189233907914838 ) ) ;
#159479=CARTESIAN_POINT ( 'NONE',  ( 4.047608660086319254, 0.6306619223146043840, -1.761260876548931709 ) ) ;
#159481=CARTESIAN_POINT ( 'NONE',  ( 2.127084423382288314, 1.709874882824816478, 0.8565708355050825062 ) ) ;
#159484=CARTESIAN_POINT ( 'NONE',  ( 3.616033620774202983, -2.174319932014677548, 0.3768175846284789743 ) ) ;
#159486=CARTESIAN_POINT ( 'NONE',  ( 6.883263157960391787, 1.249388486322531078, 2.158948101847418144 ) ) ;
#159489=CARTESIAN_POINT ( 'NONE',  ( 1.440630571055816489, 0.3805203625029949799, 1.934124978983255527 ) ) ;
#159490=CARTESIAN_POINT ( 'NONE',  ( 1.624504772527136875, -1.283422126333678692, -1.917570747650028551 ) ) ;
#159491=CARTESIAN_POINT ( 'NONE',  ( 2.488659587246494276, 1.902222718079676689, 0.4795239450603656084 ) ) ;
#159492=FACE_OUTER_BOUND ( 'NONE', #174431, .T. ) ;
#159493=CARTESIAN_POINT ( 'NONE',  ( 6.614137777011339203, 2.057435194276434842, -0.1460075293888435377 ) ) ;
#159495=CARTESIAN_POINT ( 'NONE',  ( 4.012907874177486178, 0.1037781579101039742, 2.014008197856680393 ) ) ;
#159502=CARTESIAN_POINT ( 'NONE',  ( 1.833130710876787584, -2.060620742141227701, -0.6837463184809766670 ) ) ;
#159506=CARTESIAN_POINT ( 'NONE',  ( 1.950266909631480861, 0.5821006739541793040, 1.777759251391328510 ) ) ;
#159507=CARTESIAN_POINT ( 'NONE',  ( 6.186834690482100108, -0.3103498281695793448, -2.139073744226393181 ) ) ;
#159508=CARTESIAN_POINT ( 'NONE',  ( 0.07775346131144718342, 5.719027203068962173, -2.882954358279002260 ) ) ;
#159509=CARTESIAN_POINT ( 'NONE',  ( 6.827182134110219458, 2.993868409037139688, 2.165198344177218903 ) ) ;
#159512=CARTESIAN_POINT ( 'NONE',  ( 2.279812546382542493, 1.875032136476075584, -0.3747091278499328770 ) ) ;
#159513=CARTESIAN_POINT ( 'NONE',  ( 4.029968384200533826, 0.9465192177370416182, -1.495271383057869441 ) ) ;
#159514=CARTESIAN_POINT ( 'NONE',  ( 1.910667195161031007, -0.5113573046386342691, -1.842555643073694238 ) ) ;
#159517=CARTESIAN_POINT ( 'NONE',  ( -0.06540554862877968889, -1.536972603800386361, 1.143280314369120587 ) ) ;
#159519=CARTESIAN_POINT ( 'NONE',  ( 1.047426762419433777, 1.826728496382063582, -0.9743617655595809834 ) ) ;
#159521=CARTESIAN_POINT ( 'NONE',  ( 5.014452206985246185, 1.289541220462528504, -1.355370375751355105 ) ) ;
#159522=CARTESIAN_POINT ( 'NONE',  ( 1.664397423953474009, -1.292156093668932693, 1.290017532847971271 ) ) ;
#159523=CARTESIAN_POINT ( 'NONE',  ( 5.549527019956425278, -1.737703232767298545, -1.360318885177333570 ) ) ;
#159526=CARTESIAN_POINT ( 'NONE',  ( 3.227062719040986405, -1.904794013395166186, -0.7919108894221676964 ) ) ;
#159535=CARTESIAN_POINT ( 'NONE',  ( 5.705552448923417508, -1.629793913574303588, -1.276656259598766940 ) ) ;
#159537=CARTESIAN_POINT ( 'NONE',  ( 2.319794969891198821, -2.097318901067245722, 0.5227781780692899449 ) ) ;
#159539=CARTESIAN_POINT ( 'NONE',  ( 3.053383268589305644, -1.780226508164801213, 0.9538969713841909392 ) ) ;
#159540=CARTESIAN_POINT ( 'NONE',  ( 6.620655732516651071, -0.002413161512292844035, 2.173887093218453082 ) ) ;
#159546=CARTESIAN_POINT ( 'NONE',  ( 1.815639016007553730, -1.320828798922760949, -1.523793687088881299 ) ) ;
#159548=CARTESIAN_POINT ( 'NONE',  ( 6.567925981381852907, -1.350348970527824211, 1.726830949945204363 ) ) ;
#159550=CARTESIAN_POINT ( 'NONE',  ( 4.218947473185084007, 1.474887410857337100, -1.217315437338606365 ) ) ;
#159554=CARTESIAN_POINT ( 'NONE',  ( 3.849232595480827079, 0.2440098934328518987, -2.001514877671112025 ) ) ;
#159557=CARTESIAN_POINT ( 'NONE',  ( 5.051616488536272875, 0.5384910649316194675, -1.638604462054549238 ) ) ;
#159562=CARTESIAN_POINT ( 'NONE',  ( 3.848780967690920374, -1.530814235938406931, 1.074699354247290017 ) ) ;
#159563=ORIENTED_EDGE ( 'NONE', *, *, #94249, .F. ) ;
#159564=CARTESIAN_POINT ( 'NONE',  ( 1.446235060908855008, -0.9343481645287862181, 1.847524432027500385 ) ) ;
#159566=ORIENTED_EDGE ( 'NONE', *, *, #6025, .T. ) ;
#159567=CARTESIAN_POINT ( 'NONE',  ( 5.918593472536316291, -0.6585524616501952089, -1.687715565691887187 ) ) ;
#159570=CARTESIAN_POINT ( 'NONE',  ( 0.4042039562905282435, -1.797914468929398879, -0.2212116797051487393 ) ) ;
#159576=CARTESIAN_POINT ( 'NONE',  ( 0.6780837441340243910, -1.046368970337024473, -1.659334490400856454 ) ) ;
#159578=CARTESIAN_POINT ( 'NONE',  ( 4.728101222851567975, 1.910784947378706855, 0.1365434035073622987 ) ) ;
#159585=CARTESIAN_POINT ( 'NONE',  ( 1.833122199354455972, 0.2117775504973731793, 2.151289291301178075 ) ) ;
#159589=CARTESIAN_POINT ( 'NONE',  ( 4.682524874021861017, -1.770931954651306262, -0.4427778663074270482 ) ) ;
#159591=CARTESIAN_POINT ( 'NONE',  ( 1.510939727685528311, 1.736590689682067756, 0.9330581202648262629 ) ) ;
#159592=CARTESIAN_POINT ( 'NONE',  ( 3.181800181368432678, 1.864768544494728175, -0.4233684943922080834 ) ) ;
#159595=CARTESIAN_POINT ( 'NONE',  ( 4.246515029176777034, -1.947796394531702280, -0.2911330189915450339 ) ) ;
#159597=CARTESIAN_POINT ( 'NONE',  ( 5.513211315966105808, -1.893842782867664054, 0.4293952855863486517 ) ) ;
#159601=CARTESIAN_POINT ( 'NONE',  ( 5.924112389714110805, -2.104401743431310923, 0.2612745606217213856 ) ) ;
#159603=CARTESIAN_POINT ( 'NONE',  ( 4.002528454542265024, -1.891902218777557598, -0.2775262981309714605 ) ) ;
#159607=CARTESIAN_POINT ( 'NONE',  ( 0.2331563151865486683, 0.005903526429595904942, -1.945944850731482934 ) ) ;
#159609=SURFACE_STYLE_FILL_AREA ( #175876 ) ;
#159610=CARTESIAN_POINT ( 'NONE',  ( 5.461592787958983841, -1.588467041389821421, -1.236575366846304647 ) ) ;
#159612=CARTESIAN_POINT ( 'NONE',  ( 6.498675964634617941, -0.4922777150685350156, -1.758009983081544991 ) ) ;
#159613=CARTESIAN_POINT ( 'NONE',  ( 2.137250951388528275, -0.09934309608320913976, -2.068088366144354318 ) ) ;
#159618=CARTESIAN_POINT ( 'NONE',  ( 6.526239545637954720, 1.075124705556152138, -1.530631868311462362 ) ) ;
#159629=CARTESIAN_POINT ( 'NONE',  ( 3.867547151669390448, -0.1745043776680033631, -1.725349009328189576 ) ) ;
#159631=CARTESIAN_POINT ( 'NONE',  ( 1.498975721005956219, 0.3999860688887920679, 2.031077231357696355 ) ) ;
#159632=CARTESIAN_POINT ( 'NONE',  ( 3.234098929720787385, 2.117403153491578927, -0.002560228748609005411 ) ) ;
#159635=CARTESIAN_POINT ( 'NONE',  ( 0.3210686601547476093, -1.756690599571947065, -0.8905566435374636658 ) ) ;
#159639=CARTESIAN_POINT ( 'NONE',  ( -0.03509584499547176162, -1.534781374734139670, 1.140672443274578729 ) ) ;
#159640=CARTESIAN_POINT ( 'NONE',  ( 3.328363117612358479, 2.236410206915816268, 0.5022841181492423424 ) ) ;
#159641=CARTESIAN_POINT ( 'NONE',  ( 1.049113529465800054, -1.437755431736492673, -1.125068434497819680 ) ) ;
#159642=CARTESIAN_POINT ( 'NONE',  ( 3.375170810042011915, -1.688748480992762868, -0.8973671847329609541 ) ) ;
#159647=CARTESIAN_POINT ( 'NONE',  ( 2.127199591969671122, 1.800101769773830185, 0.9015413830680671925 ) ) ;
#159648=CARTESIAN_POINT ( 'NONE',  ( 2.289831844592318255, -1.277571413231039399, -1.488851726829776068 ) ) ;
#159652=CARTESIAN_POINT ( 'NONE',  ( 5.490208796768200727, -0.5072484191241812823, -2.028029781992314096 ) ) ;
#159653=CARTESIAN_POINT ( 'NONE',  ( 2.957584522866180343, 1.761491525812574510, -0.1715649573520404425 ) ) ;
#159655=CARTESIAN_POINT ( 'NONE',  ( 6.158190107012026182, -1.625331280325162053, 1.616661686624631944 ) ) ;
#159656=CARTESIAN_POINT ( 'NONE',  ( 5.068161541800582093, -1.640353732806285825, -0.5817517365288951137 ) ) ;
#159658=CARTESIAN_POINT ( 'NONE',  ( 4.358545522520183013, -0.6637924119957930857, 1.601953373104019418 ) ) ;
#159659=CARTESIAN_POINT ( 'NONE',  ( 5.494640824104591204, 2.138133990741352353, 0.3765844856341519775 ) ) ;
#159660=CARTESIAN_POINT ( 'NONE',  ( 0.5853561509586381328, 1.734793994416533369, 1.213709793590052932 ) ) ;
#159661=CARTESIAN_POINT ( 'NONE',  ( 5.468750000000003553, 0.7852924748297082091, -1.895863743164194704 ) ) ;
#159662=CARTESIAN_POINT ( 'NONE',  ( -0.1909996267163149852, 7.629137130509101361, -2.600377616606447617 ) ) ;
#159663=CARTESIAN_POINT ( 'NONE',  ( 3.452094016638465490, 1.926566264197142830, 0.001310335549949831480 ) ) ;
#159665=CARTESIAN_POINT ( 'NONE',  ( 0.06548277170575435291, -1.780103896928236118, 1.328506668625312859 ) ) ;
#159669=CARTESIAN_POINT ( 'NONE',  ( 2.051734446849303506, -1.982521776546506853, 1.002060208660388474 ) ) ;
#159674=CARTESIAN_POINT ( 'NONE',  ( 1.266250242576156815, 1.862016182229693673, -0.7743172429433076154 ) ) ;
#159676=CARTESIAN_POINT ( 'NONE',  ( 5.406706549104464798, 0.5953045380993631230, 1.974924460807401028 ) ) ;
#159682=CARTESIAN_POINT ( 'NONE',  ( 0.5613125002107671735, 1.751697300359332798, -0.2511290008074765212 ) ) ;
#159683=CARTESIAN_POINT ( 'NONE',  ( 5.748594953515238082, 1.706903099953221759, -0.3051902176867369865 ) ) ;
#159684=CARTESIAN_POINT ( 'NONE',  ( 5.372502291033079302, -0.05049805449116586548, -1.739898325138872215 ) ) ;
#159685=CARTESIAN_POINT ( 'NONE',  ( 3.491970780479057179, -2.289775125716007054, -0.1112369151145074092 ) ) ;
#159687=CARTESIAN_POINT ( 'NONE',  ( 2.730204174461122069, 0.2256132759956077649, 1.827196471909063202 ) ) ;
#159691=CARTESIAN_POINT ( 'NONE',  ( 2.696107482849848580, -1.820545782403935720, -0.1364615833806467338 ) ) ;
#159692=CARTESIAN_POINT ( 'NONE',  ( 4.342422763466713853, 0.4390309838058319425, -1.967887491402267486 ) ) ;
#159695=CARTESIAN_POINT ( 'NONE',  ( 4.506922906144382956, 1.629430921360131679, -1.334182900473983135 ) ) ;
#159698=CARTESIAN_POINT ( 'NONE',  ( 2.647004975520852454, -0.3514972095969396970, -2.040143077068845123 ) ) ;
#159701=CARTESIAN_POINT ( 'NONE',  ( 4.319064098534145302, 1.638436671179326787, -1.346072318137331969 ) ) ;
#159702=CARTESIAN_POINT ( 'NONE',  ( 6.727182134110220701, 0.005875948494733078051, 1.810970247402940103 ) ) ;
#159710=CARTESIAN_POINT ( 'NONE',  ( 6.187751663909415001, 2.028806014889028120, -0.6170373231123224000 ) ) ;
#159711=CARTESIAN_POINT ( 'NONE',  ( 1.307801118376609839, -0.5120802815330603996, 2.042612192628911139 ) ) ;
#159715=CARTESIAN_POINT ( 'NONE',  ( 6.209776894639321476, 0.5414253987558427239, -1.780396208465367280 ) ) ;
#159720=CARTESIAN_POINT ( 'NONE',  ( 0.5980879788009090259, 1.428637019467562830, 1.567290143595565066 ) ) ;
#159723=CARTESIAN_POINT ( 'NONE',  ( 2.295295855072278624, -1.753792786583353580, 0.8793850528211948347 ) ) ;
#159724=CARTESIAN_POINT ( 'NONE',  ( 1.569428280142046717, 0.1587979871724466974, -2.155937297210829495 ) ) ;
#159728=CARTESIAN_POINT ( 'NONE',  ( 3.215853349543820183, -1.415750056632815168, -1.000566135699741066 ) ) ;
#159729=CARTESIAN_POINT ( 'NONE',  ( 2.150002804924430411, -1.345968700644652349, 1.103203096369822056 ) ) ;
#159733=CARTESIAN_POINT ( 'NONE',  ( 2.600935288962639369, 0.9528664403582010056, -1.776738882381201812 ) ) ;
#159734=CARTESIAN_POINT ( 'NONE',  ( 6.825078400183546279, 2.419143596098617621, 2.525240329153962904 ) ) ;
#159736=CARTESIAN_POINT ( 'NONE',  ( 1.323050886902911616, -0.05057411593789931659, 1.970981584096524575 ) ) ;
#159737=CARTESIAN_POINT ( 'NONE',  ( 5.256085721135645095, 0.7693902824621422498, -1.750971482026221437 ) ) ;
#159742=CARTESIAN_POINT ( 'NONE',  ( 1.348313414878389294, 0.9933643222376374871, -1.758399455230485575 ) ) ;
#159744=CARTESIAN_POINT ( 'NONE',  ( 5.614422408412740317, -1.031215703586242149, -2.064428503307714546 ) ) ;
#159745=CARTESIAN_POINT ( 'NONE',  ( 6.074655751228532630, 1.318658252384183438, -1.452748870126779890 ) ) ;
#159746=CARTESIAN_POINT ( 'NONE',  ( 3.063279882407277999, 1.654721480355027863, 1.053479689057647217 ) ) ;
#159748=CARTESIAN_POINT ( 'NONE',  ( 0.2818752512256904597, 1.674885806461807958, -1.122501178855893400 ) ) ;
#159751=CARTESIAN_POINT ( 'NONE',  ( 1.516979485257620608, 0.2134662686405098542, 2.106589464619255558 ) ) ;
#159754=CARTESIAN_POINT ( 'NONE',  ( 1.569984571489828173, -1.747861548559765721, -0.5788160320587890650 ) ) ;
#159757=CARTESIAN_POINT ( 'NONE',  ( 2.637105894733019262, 1.998242115483703341, 0.7103459930332192140 ) ) ;
#159760=CARTESIAN_POINT ( 'NONE',  ( 2.829428133295128323, -1.924058217741884125, 0.7386292696346643538 ) ) ;
#159762=CARTESIAN_POINT ( 'NONE',  ( -0.1121326479804653220, -0.4008509640632436088, -1.803546454093779561 ) ) ;
#159767=CARTESIAN_POINT ( 'NONE',  ( 0.03028722099337673168, -1.361824662662258767, -1.737358624739212543 ) ) ;
#159768=CARTESIAN_POINT ( 'NONE',  ( 3.075713870353123713, 2.149355976742998831, -0.7065000242163150812 ) ) ;
#159770=CARTESIAN_POINT ( 'NONE',  ( 2.865264419611464941, -1.483432276133073380, -1.039550242524535539 ) ) ;
#159771=CARTESIAN_POINT ( 'NONE',  ( 3.186650014752292925, 1.506923149468800682, -1.182699731353755501 ) ) ;
#159772=CARTESIAN_POINT ( 'NONE',  ( 4.193848433072798088, -1.425472641756184489, -1.501718461524886195 ) ) ;
#159774=CARTESIAN_POINT ( 'NONE',  ( 2.201972163173575137, -1.971069923813788982, 0.04663598398449429056 ) ) ;
#159775=CARTESIAN_POINT ( 'NONE',  ( 6.498663727319215155, -0.5164181641097148612, -1.855934172746701583 ) ) ;
#159776=CARTESIAN_POINT ( 'NONE',  ( 3.045614982896325262, 0.6747646648952825288, -1.744891315567910439 ) ) ;
#159777=CARTESIAN_POINT ( 'NONE',  ( 2.754834555525199846, 0.7783630933865728352, 2.172589714749242784 ) ) ;
#159779=CARTESIAN_POINT ( 'NONE',  ( 2.541259301162884121, 1.702954558545258346, -0.7510573925902948034 ) ) ;
#159781=CARTESIAN_POINT ( 'NONE',  ( 6.566849514013569866, 1.531126396248701171, -1.382332999690039754 ) ) ;
#159784=CARTESIAN_POINT ( 'NONE',  ( 0.7859291816119529095, 1.415994179718871759, 1.559173624910270783 ) ) ;
#159786=CARTESIAN_POINT ( 'NONE',  ( 5.641917277892137150, 0.8817427965214555963, -1.973778517010720490 ) ) ;
#159787=CARTESIAN_POINT ( 'NONE',  ( 6.533853655515883041, -1.958494339806987394, 0.4928751659435038901 ) ) ;
#159791=CARTESIAN_POINT ( 'NONE',  ( 6.825078400183573812, 0.002648415797040087893, 1.855566311045192540 ) ) ;
#159794=CARTESIAN_POINT ( 'NONE',  ( 4.294157853547872605, -0.8666056138363428252, -1.820986994602634024 ) ) ;
#159799=CARTESIAN_POINT ( 'NONE',  ( 6.526263005029544928, 1.249015235541932167, -1.764162671312206498 ) ) ;
#159804=CARTESIAN_POINT ( 'NONE',  ( 6.187125092307005580, 1.678016663812756937, 1.117817459622950649 ) ) ;
#159809=CARTESIAN_POINT ( 'NONE',  ( 2.103723633838894713, -1.724574586359624906, 0.04069764719066489012 ) ) ;
#159813=CARTESIAN_POINT ( 'NONE',  ( 1.141466271755723794, 0.7239738643088615699, -1.615086939138086652 ) ) ;
#159814=CARTESIAN_POINT ( 'NONE',  ( 1.945949197151348509, -1.316483196816301549, -1.523026451717986784 ) ) ;
#159816=CARTESIAN_POINT ( 'NONE',  ( 4.190592561755676293, -2.182319254149690302, -0.3268587364041104504 ) ) ;
#159817=CARTESIAN_POINT ( 'NONE',  ( 4.944265959323273840, -1.029449158807031361, 1.911525048081736955 ) ) ;
#159821=CARTESIAN_POINT ( 'NONE',  ( 3.035902975225315714, -2.043024508941180706, 0.5676086983019896781 ) ) ;
#159822=CARTESIAN_POINT ( 'NONE',  ( 3.110954007106698338, 0.05231540665236523308, 2.015913653835194719 ) ) ;
#159823=CARTESIAN_POINT ( 'NONE',  ( 3.287185820011778947, 0.03942761580559561718, -1.811315726287704431 ) ) ;
#159828=CARTESIAN_POINT ( 'NONE',  ( 0.6900581440293825919, -1.856003987442723657, -0.2331820809091043056 ) ) ;
#159832=CARTESIAN_POINT ( 'NONE',  ( 6.481070005604858686, -0.09514881109910081070, -1.823337098959529001 ) ) ;
#159834=CARTESIAN_POINT ( 'NONE',  ( 1.762754532109143124, -0.09793373165993285445, -1.913366418544469205 ) ) ;
#159840=CARTESIAN_POINT ( 'NONE',  ( 5.190363053866647647, -2.144918610114197488, -0.2683968819863768451 ) ) ;
#159843=CARTESIAN_POINT ( 'NONE',  ( 2.584367824843319283, 1.138156186954141003, 1.789115803205274080 ) ) ;
#159844=CARTESIAN_POINT ( 'NONE',  ( -0.1296875068448125334, 4.095146142119266308, -2.381513845672214913 ) ) ;
#159846=CARTESIAN_POINT ( 'NONE',  ( 4.147701676541888816, 0.6670536769024897339, -1.855179015784082619 ) ) ;
#159847=CARTESIAN_POINT ( 'NONE',  ( 6.433860211133586304, -1.853236450885078712, 0.4715264990977630077 ) ) ;
#159848=ORIENTED_EDGE ( 'NONE', *, *, #50413, .F. ) ;
#159849=CARTESIAN_POINT ( 'NONE',  ( 5.173117096678320870, 1.865890646727845326, -1.000864459693462383 ) ) ;
#159851=CARTESIAN_POINT ( 'NONE',  ( 6.760212172060996672, -1.969150147884619173, 0.04690145372830689663 ) ) ;
#159852=CARTESIAN_POINT ( 'NONE',  ( 2.994010707676255212, -0.5641155714235489560, -1.858205125314008832 ) ) ;
#159856=CARTESIAN_POINT ( 'NONE',  ( 3.328152359787967640, 2.039751367458849884, 0.4576943786474896858 ) ) ;
#159859=CARTESIAN_POINT ( 'NONE',  ( 0.1701768659465550948, 0.6913354060617262764, 1.674562877054022625 ) ) ;
#159861=CARTESIAN_POINT ( 'NONE',  ( 5.584669497696876483, -2.152379054646291756, -0.4867646435422824935 ) ) ;
#159864=CARTESIAN_POINT ( 'NONE',  ( 2.555956245031346885, 0.5892994983645870599, -2.126554282292691500 ) ) ;
#159867=CARTESIAN_POINT ( 'NONE',  ( 1.295406243800485635, 1.766531960031037407, -0.7327172462580702206 ) ) ;
#159869=CARTESIAN_POINT ( 'NONE',  ( 5.670397268163976712, -0.9275489576153757021, -1.851018422006404096 ) ) ;
#159871=CARTESIAN_POINT ( 'NONE',  ( 2.870174731959000525, 1.155358403710282866, 1.826860881501219280 ) ) ;
#159872=CARTESIAN_POINT ( 'NONE',  ( 4.493798347139664529, -2.191065130646638437, -0.05333993539427539510 ) ) ;
#159879=CARTESIAN_POINT ( 'NONE',  ( 0.6685925339881376717, 1.356301626434471164, 1.492253803477984642 ) ) ;
#159882=CARTESIAN_POINT ( 'NONE',  ( 5.401260523219934662, -1.778462342247935979, 1.059464396209061521 ) ) ;
#159883=CARTESIAN_POINT ( 'NONE',  ( 4.178288987252887665, -1.108116244417625573, 1.575729328202896573 ) ) ;
#159884=CARTESIAN_POINT ( 'NONE',  ( 6.275037739279882842, 1.841983620878117733, -1.043829292874172143 ) ) ;
#159887=CARTESIAN_POINT ( 'NONE',  ( 4.276189508915988036, -1.008629908464111269, -1.691384299763159182 ) ) ;
#159888=CARTESIAN_POINT ( 'NONE',  ( 0.3577192552456122665, 2.167005522336755696, -0.3256184645209562190 ) ) ;
#159889=CARTESIAN_POINT ( 'NONE',  ( 3.773894676421325034, 1.015518775504126614, 1.516979517045339287 ) ) ;
#159892=EDGE_CURVE ( 'NONE', #113025, #11785, #35208, .T. ) ;
#159895=ORIENTED_EDGE ( 'NONE', *, *, #155782, .T. ) ;
#159896=CARTESIAN_POINT ( 'NONE',  ( 1.276629239279066574, 1.701104413791530767, -0.7050613402737049284 ) ) ;
#159897=CARTESIAN_POINT ( 'NONE',  ( 5.502202757749218520, -0.9014697883563610459, 1.800137906301606305 ) ) ;
#159898=CARTESIAN_POINT ( 'NONE',  ( 1.300659708833833861, -2.077133573725042037, 0.9841232947556498578 ) ) ;
#159899=CARTESIAN_POINT ( 'NONE',  ( 5.436364959771895045, -1.092926877770916017, 1.628904810760459121 ) ) ;
#159903=CARTESIAN_POINT ( 'NONE',  ( 0.8013346216862862192, -1.776568573310655985, 1.062853015585236482 ) ) ;
#159905=CARTESIAN_POINT ( 'NONE',  ( 1.909825778081200909, -0.9882315549833411428, -1.842464674945838654 ) ) ;
#159906=CARTESIAN_POINT ( 'NONE',  ( 6.789980064821725669, -0.7525070324889830964, 1.600651327395278711 ) ) ;
#159909=CARTESIAN_POINT ( 'NONE',  ( -0.2102771530458277249, 4.081134801423261571, -2.758393064927369576 ) ) ;
#159910=CARTESIAN_POINT ( 'NONE',  ( 2.313636755748917473, 1.135937956827288042, -1.318730690005095241 ) ) ;
#159914=CARTESIAN_POINT ( 'NONE',  ( 3.140908386031955324, -1.520905784971425589, 0.8136546746303519040 ) ) ;
#159915=( BOUNDED_CURVE ( )  B_SPLINE_CURVE ( 3, ( #22821, #156057, #88936, #39105 ),
 .UNSPECIFIED., .F., .T. ) 
 B_SPLINE_CURVE_WITH_KNOTS ( ( 4, 4 ),
 ( 0.5000000000000018874, 1.000000000000000000 ),
 .UNSPECIFIED. ) 
 CURVE ( )  GEOMETRIC_REPRESENTATION_ITEM ( )  RATIONAL_B_SPLINE_CURVE ( ( 0.9999999999999974465, 0.3333333333333333703, 0.3333333333333358683, 1.000000000000000000 ) ) 
 REPRESENTATION_ITEM ( '' )  );
#159916=CARTESIAN_POINT ( 'NONE',  ( 1.083813775577105565, -0.9808430935620198188, 1.959877696171570927 ) ) ;
#159918=CARTESIAN_POINT ( 'NONE',  ( 3.967548030458594166, 0.2710504330169676845, -2.190103208553782821 ) ) ;
#159921=CARTESIAN_POINT ( 'NONE',  ( 2.325261487346420797, -1.983500291700568852, -0.8831872222036639686 ) ) ;
#159922=CARTESIAN_POINT ( 'NONE',  ( 0.8381832108898427114, 1.798179982845280467, 0.3147962740308178353 ) ) ;
#159923=CARTESIAN_POINT ( 'NONE',  ( 2.975892561826110505, -0.8538584053617600533, 1.937700190512989362 ) ) ;
#159925=CARTESIAN_POINT ( 'NONE',  ( 6.539320575229274013, 7.053493080409727334, 2.394893457813539683 ) ) ;
#159927=CARTESIAN_POINT ( 'NONE',  ( 4.124787647867947271, 0.1125639427311639490, 2.289740828591101174 ) ) ;
#159931=CARTESIAN_POINT ( 'NONE',  ( 6.024141157665446222, -2.204869988984262896, 0.2693334978098835264 ) ) ;
#159937=CARTESIAN_POINT ( 'NONE',  ( 4.236954046275762664, 2.015912997090345549, -0.05229627655192746472 ) ) ;
#159939=CARTESIAN_POINT ( 'NONE',  ( 2.166912933460037660, 1.531321095959611966, -1.381971985785889423 ) ) ;
#159945=CARTESIAN_POINT ( 'NONE',  ( 4.752002516643937469, 0.8370584164609263800, 2.025481692006773748 ) ) ;
#159946=CARTESIAN_POINT ( 'NONE',  ( 2.479138880926802901, -2.011204309026824344, -0.1455328587063598189 ) ) ;
#159947=CARTESIAN_POINT ( 'NONE',  ( 2.559893532628489954, -1.268187297466142338, 1.335118840784771166 ) ) ;
#159948=EDGE_CURVE ( 'NONE', #137219, #205352, #163924, .T. ) ;
#159951=CARTESIAN_POINT ( 'NONE',  ( 5.913091143547532624, 1.611232972626057247, 0.8583240166551919792 ) ) ;
#159953=CARTESIAN_POINT ( 'NONE',  ( 5.559536883401111851, 0.4474127746876849221, -2.217688626266269392 ) ) ;
#159955=CARTESIAN_POINT ( 'NONE',  ( 1.981218818260335413, -0.1044028718686483975, -2.103608768903475035 ) ) ;
#159964=CARTESIAN_POINT ( 'NONE',  ( 2.707538781118669302, 1.902989223989959067, -1.145821276547890122 ) ) ;
#159966=CARTESIAN_POINT ( 'NONE',  ( 6.883263157960371359, 7.052674735402435502, 2.544342468817725855 ) ) ;
#159969=CARTESIAN_POINT ( 'NONE',  ( 4.035565188342554954, 1.848088059160474694, -0.6588067414724924076 ) ) ;
#159978=CARTESIAN_POINT ( 'NONE',  ( 2.988655875014298857, -1.259908772670719657, 1.705623289672608678 ) ) ;
#159980=CARTESIAN_POINT ( 'NONE',  ( 4.926735330553584369, 2.067573386176469796, 0.6309256262674377558 ) ) ;
#159981=CARTESIAN_POINT ( 'NONE',  ( 3.473999211503727036, -1.775402473473717935, -0.4878004006634574230 ) ) ;
#159984=CARTESIAN_POINT ( 'NONE',  ( 5.331890987662370129, 1.715487909331077310, 0.2919898797263379975 ) ) ;
#159985=CARTESIAN_POINT ( 'NONE',  ( 6.727182134110201162, 0.6069527724139511804, 1.765151538780465712 ) ) ;
#159988=CARTESIAN_POINT ( 'NONE',  ( 3.274459119871219848, -1.289031633699176949, 1.735169069618908821 ) ) ;
#159990=CARTESIAN_POINT ( 'NONE',  ( 5.413435409655408925, 0.5825687168248098180, 1.930121546480124461 ) ) ;
#159992=CARTESIAN_POINT ( 'NONE',  ( 2.413140945657660907, 1.930630709398067246, 0.9725960170764782475 ) ) ;
#159993=CARTESIAN_POINT ( 'NONE',  ( 3.743400255998735382, -1.490684086824107357, -1.290067496309046158 ) ) ;
#159994=CARTESIAN_POINT ( 'NONE',  ( -0.005964567173097347699, -2.191213315851054944, -0.04726126812268362232 ) ) ;
#159995=CARTESIAN_POINT ( 'NONE',  ( 4.300292543067584461, 1.499173285595749583, -1.234514081855079048 ) ) ;
#160004=CARTESIAN_POINT ( 'NONE',  ( 2.327434156339613924, -0.0004056629378437063877, 2.206952907597827362 ) ) ;
#160006=CARTESIAN_POINT ( 'NONE',  ( 6.227397112613878960, 0.1477489091250457076, -1.956280406615627854 ) ) ;
#160012=CARTESIAN_POINT ( 'NONE',  ( 5.630750141678076304, -1.662707896839428434, 0.7909858098210584831 ) ) ;
#160018=CARTESIAN_POINT ( 'NONE',  ( 6.064709079624690524, 0.6667526090060638122, 2.013086243192941716 ) ) ;
#160022=CARTESIAN_POINT ( 'NONE',  ( 0.1103218441215253337, -0.8811044119183660817, -1.861458889230242164 ) ) ;
#160024=CARTESIAN_POINT ( 'NONE',  ( 2.277597300015369086, -1.806044765408962194, 0.4486390909646633118 ) ) ;
#160025=CARTESIAN_POINT ( 'NONE',  ( 3.895923546780861724, -0.5813109859279729230, -1.747131793041277970 ) ) ;
#160030=CARTESIAN_POINT ( 'NONE',  ( 4.354274438496381627, 2.206422198305586058, -0.05263853172451230661 ) ) ;
#160031=CARTESIAN_POINT ( 'NONE',  ( 6.415309710857563630, -0.2865549832780675543, 2.244158528320794765 ) ) ;
#160033=CARTESIAN_POINT ( 'NONE',  ( 5.660388270892238616, 1.809938998256973575, 0.08008182766248285456 ) ) ;
#160034=CARTESIAN_POINT ( 'NONE',  ( 0.005092704479254389627, -0.09411098085002241043, 2.014433268766747887 ) ) ;
#160036=CARTESIAN_POINT ( 'NONE',  ( 6.526239545637954720, 1.075124705556152138, -1.530631868311462362 ) ) ;
#160037=CARTESIAN_POINT ( 'NONE',  ( 5.127564033545165323, -0.2766344828325461025, 1.892035409188079997 ) ) ;
#160039=CARTESIAN_POINT ( 'NONE',  ( 1.024039198018782626, 1.117340804906666873, -1.500143343703803422 ) ) ;
#160040=CARTESIAN_POINT ( 'NONE',  ( 0.7433754753295095385, 0.3886281223182270761, -1.978556061772406505 ) ) ;
#160042=CARTESIAN_POINT ( 'NONE',  ( 3.686240278715931851, -1.037925599752804739, 1.832463683143903399 ) ) ;
#160047=CARTESIAN_POINT ( 'NONE',  ( 3.392836290029502155, -1.947660480455270404, -0.5347636834307776255 ) ) ;
#160050=CARTESIAN_POINT ( 'NONE',  ( 3.866626755795209203, -1.454868229745639008, 1.598846606682593929 ) ) ;
#160056=CARTESIAN_POINT ( 'NONE',  ( 1.153041021216383299, -0.5271860560512993121, -2.106100485105724562 ) ) ;
#160060=CARTESIAN_POINT ( 'NONE',  ( 1.892365914234435120, -0.5883382831698009685, -2.111031122750434808 ) ) ;
#160062=CARTESIAN_POINT ( 'NONE',  ( 2.606633135955916725, -0.8653751708443763180, -2.090666874703292599 ) ) ;
#160068=CARTESIAN_POINT ( 'NONE',  ( 3.954177229731909549, 0.6350985098286399122, 1.652046152411037694 ) ) ;
#160071=CARTESIAN_POINT ( 'NONE',  ( 0.9035134896902213830, 1.721610636892715984, 1.212602220121623775 ) ) ;
#160076=CARTESIAN_POINT ( 'NONE',  ( 6.468375372808552903, -1.978050569928070379, -0.3905794195708453542 ) ) ;
#160080=CARTESIAN_POINT ( 'NONE',  ( 3.801501934187266230, -0.5436965770258190833, 1.789884385262895616 ) ) ;
#160081=CARTESIAN_POINT ( 'NONE',  ( 4.715722526854881913, 0.4587184135333640111, -2.018627749927892179 ) ) ;
#160089=CARTESIAN_POINT ( 'NONE',  ( 3.560947883890089649, 1.548132398191165882, -1.204989647596923508 ) ) ;
#160090=CARTESIAN_POINT ( 'NONE',  ( 1.300157425512000087, -1.823841169980220167, 0.8594962466553014435 ) ) ;
#160091=ADVANCED_FACE ( 'NONE', ( #167864 ), #165169, .F. ) ;
#160095=CARTESIAN_POINT ( 'NONE',  ( 1.317418832401914930, -1.826178791559311509, 0.4043020138455517554 ) ) ;
#160097=CARTESIAN_POINT ( 'NONE',  ( 3.129155277828885140, 1.821763076032786977, 0.8570700399232934474 ) ) ;
#160099=CARTESIAN_POINT ( 'NONE',  ( 1.968512934334982978, -2.077085554295199810, -0.4095441970272342136 ) ) ;
#160101=CARTESIAN_POINT ( 'NONE',  ( 3.824723168590526523, -1.392635068473629500, 1.532133406949770960 ) ) ;
#160103=CARTESIAN_POINT ( 'NONE',  ( -0.04130929284668418550, -1.869521504948624235, -0.9361258523304989421 ) ) ;
#160105=CARTESIAN_POINT ( 'NONE',  ( 5.790036952090301448, -0.8187086143041850672, 1.631793460665122986 ) ) ;
#160111=CARTESIAN_POINT ( 'NONE',  ( 5.983472182158235064, 2.041168445429199618, -0.8392293214988936212 ) ) ;
#160113=CARTESIAN_POINT ( 'NONE',  ( 4.652931681422667332, 0.3304644650514582116, 1.883354098946861344 ) ) ;
#160122=FACE_OUTER_BOUND ( 'NONE', #201631, .T. ) ;
#160130=CARTESIAN_POINT ( 'NONE',  ( 2.834760172256750810, -1.883157219239324887, -0.5764521555583942414 ) ) ;
#160131=CARTESIAN_POINT ( 'NONE',  ( 3.480092364642515701, -2.014234743589532695, -0.09611699103692641910 ) ) ;
#160134=CARTESIAN_POINT ( 'NONE',  ( 6.727182134110199385, 1.257034414284210921, 2.204727292504021108 ) ) ;
#160135=CARTESIAN_POINT ( 'NONE',  ( 4.013774469618203611, -1.125877316280783358, -1.879984707117538845 ) ) ;
#160137=CARTESIAN_POINT ( 'NONE',  ( 1.659075543930859764, -1.650851203806924294, -0.9926060514057006845 ) ) ;
#160139=CARTESIAN_POINT ( 'NONE',  ( -0.1296875068448125334, 2.048176110289974261, -2.243787855586779401 ) ) ;
#160140=CARTESIAN_POINT ( 'NONE',  ( 0.1329588055935396196, 0.006246367379872731426, -1.846049620084761367 ) ) ;
#160149=CARTESIAN_POINT ( 'NONE',  ( 6.550350952284553330, -1.418464805562440922, 1.173678288350611609 ) ) ;
#160150=CARTESIAN_POINT ( 'NONE',  ( 2.244791168117025837, 1.953224514136771006, 0.4868699220301163089 ) ) ;
#160151=CARTESIAN_POINT ( 'NONE',  ( 4.306267096541755990, -2.002170989124392175, 1.128539623919281754 ) ) ;
#160152=CARTESIAN_POINT ( 'NONE',  ( -0.1290005225502675879, 5.719648796287211567, -2.768066027128403217 ) ) ;
#160153=CARTESIAN_POINT ( 'NONE',  ( 2.219380450391433168, 0.3239122733160957890, -1.832380290584040505 ) ) ;
#160155=CARTESIAN_POINT ( 'NONE',  ( -0.1290005225502675879, 2.860092606084875033, -2.662085506130333457 ) ) ;
#160156=CARTESIAN_POINT ( 'NONE',  ( 5.836178160628028522, -1.067892152678026951, -1.586260290404594597 ) ) ;
#160159=CARTESIAN_POINT ( 'NONE',  ( 4.616787868375789472, -0.1008748965102136408, 2.088423895528898733 ) ) ;
#160160=CARTESIAN_POINT ( 'NONE',  ( 3.537841792810627606, 0.8420186812403904764, -1.670516725672297031 ) ) ;
#160163=CARTESIAN_POINT ( 'NONE',  ( 6.463511695382619493, 0.2867160277617316622, -1.700725516685620553 ) ) ;
#160165=CARTESIAN_POINT ( 'NONE',  ( 1.547078507373225165, -1.226440487959565173, 1.226290910655163380 ) ) ;
#160168=B_SPLINE_CURVE_WITH_KNOTS ( 'NONE', 3,
 ( #93925, #159966, #11571, #143763, #56070, #122226, #105929, #171953, #23542, #89651, #155705 ),
 .UNSPECIFIED., .F., .F.,
 ( 4, 1, 1, 1, 1, 1, 1, 1, 4 ),
 ( 0.000000000000000000, 0.2254704865597413344, 0.3973194950497592193, 0.5246576192285303808, 0.6166070239209043846, 0.6823180413592140336, 0.7309932997181896042, 0.7717238569598857678, 1.000000000000000000 ),
 .UNSPECIFIED. ) ;
#160169=CARTESIAN_POINT ( 'NONE',  ( 6.209878556409044847, 0.6379485578581347571, -2.075210184031409888 ) ) ;
#160170=CARTESIAN_POINT ( 'NONE',  ( 3.932112477472641920, 0.9751300899686901058, -1.543267412809447681 ) ) ;
#160171=CARTESIAN_POINT ( 'NONE',  ( 1.920681792755132067, -1.391007931628859939, 1.383589105726056756 ) ) ;
#160172=CARTESIAN_POINT ( 'NONE',  ( 0.07011551774125344971, -0.9937341303020963412, 1.869520526064169408 ) ) ;
#160176=CARTESIAN_POINT ( 'NONE',  ( 2.684367718930933844, 1.136400967617630986, 1.790090880730066392 ) ) ;
#160180=CARTESIAN_POINT ( 'NONE',  ( 0.9892257793299992219, 0.1485654903058269416, 2.064951490685583924 ) ) ;
#160183=CARTESIAN_POINT ( 'NONE',  ( 2.983289111093189394, -2.053184633062016484, -0.8481636011889515103 ) ) ;
#160185=CARTESIAN_POINT ( 'NONE',  ( 0.5812297525147345212, -0.8198687466959112546, 2.147686052911641497 ) ) ;
#160187=CARTESIAN_POINT ( 'NONE',  ( 5.155161738035724639, 1.717805270433828246, -1.141362358335789251 ) ) ;
#160191=CARTESIAN_POINT ( 'NONE',  ( 0.2333540202161506205, 0.2466631755442013352, -2.080888922837381916 ) ) ;
#160192=CARTESIAN_POINT ( 'NONE',  ( 5.196754805642953556, 1.508532920973480795, 1.055450849767838317 ) ) ;
#160194=CARTESIAN_POINT ( 'NONE',  ( 3.117853853556023846, -0.8486709934477435491, -1.501428560464845630 ) ) ;
#160195=CARTESIAN_POINT ( 'NONE',  ( 1.094935803221647186, 1.780670018850015079, 0.9462964651613046119 ) ) ;
#160196=CARTESIAN_POINT ( 'NONE',  ( 3.305630555216050759, 1.456526447221625276, -1.778376517212407748 ) ) ;
#160197=CARTESIAN_POINT ( 'NONE',  ( 2.319920442056855325, -2.194974118250800021, 0.5478587534586392138 ) ) ;
#160198=CARTESIAN_POINT ( 'NONE',  ( 5.707678396406405064, -0.5131847548165735518, 2.042461488563215966 ) ) ;
#160200=CARTESIAN_POINT ( 'NONE',  ( 4.182668740906975380, -0.1716826142807558186, -1.761352938113736277 ) ) ;
#160204=CARTESIAN_POINT ( 'NONE',  ( 6.233931918547526152, 2.266764885754421144, 0.3408509611897111991 ) ) ;
#160205=CARTESIAN_POINT ( 'NONE',  ( 4.892441406782115365, 1.528958278715689234, -1.025397978904031060 ) ) ;
#160210=CARTESIAN_POINT ( 'NONE',  ( 4.207102436150745639, -0.3756362130699179014, 2.158856393654845274 ) ) ;
#160215=CARTESIAN_POINT ( 'NONE',  ( 3.088414555603569145, -1.898068263532082245, -0.3288968790781700013 ) ) ;
#160218=CARTESIAN_POINT ( 'NONE',  ( -0.1224090711158704881, -1.988194106603015987, -0.9910323345065151779 ) ) ;
#160228=CARTESIAN_POINT ( 'NONE',  ( 0.1683002474503410839, -0.8351952195557799108, -1.773497582445908938 ) ) ;
#160230=CARTESIAN_POINT ( 'NONE',  ( 6.508665849870632236, 1.605377118863276387, -1.447859449074364591 ) ) ;
#160231=CARTESIAN_POINT ( 'NONE',  ( 5.441838459065293065, 1.316327937319297758, 1.454900926449454124 ) ) ;
#160234=CARTESIAN_POINT ( 'NONE',  ( 5.401312781148373432, 1.764888628567516049, 1.247983453017486699 ) ) ;
#160235=CARTESIAN_POINT ( 'NONE',  ( -0.1106727585415863135, 6.947232144882324434, -2.598525652753637782 ) ) ;
#160238=CARTESIAN_POINT ( 'NONE',  ( 0.6494046996203367561, 0.5928216254872006319, -1.774177939146783345 ) ) ;
#160239=CARTESIAN_POINT ( 'NONE',  ( 5.993412714446900047, 1.671717086469927560, 0.4595231857335341785 ) ) ;
#160241=CARTESIAN_POINT ( 'NONE',  ( 3.351304529449970371, 0.5305821810032870234, -2.126252377916526992 ) ) ;
#160242=CARTESIAN_POINT ( 'NONE',  ( 3.276728144386112263, -1.376063543960687641, 1.852258789692583507 ) ) ;
#160243=CARTESIAN_POINT ( 'NONE',  ( 5.483688661837972766, 1.380929853543419128, 1.529855004671219820 ) ) ;
#160244=CARTESIAN_POINT ( 'NONE',  ( 1.324054681829215818, 1.871493247920783753, 0.5181311518769672331 ) ) ;
#160247=CARTESIAN_POINT ( 'NONE',  ( 5.010073305087408002, -0.7609581946756528437, 1.979555329295646260 ) ) ;
#160249=CARTESIAN_POINT ( 'NONE',  ( 2.531875153343257523, -1.674887184936912909, 1.122499117612890673 ) ) ;
#160251=CARTESIAN_POINT ( 'NONE',  ( 6.194375513154499302, -2.195555142843173879, -0.2223249613259313806 ) ) ;
#160260=CARTESIAN_POINT ( 'NONE',  ( 3.924726224964281140, 1.956320258297845172, 0.6483119717206936583 ) ) ;
#160262=CARTESIAN_POINT ( 'NONE',  ( 0.2329586101569872392, 0.008238550247445528343, -1.845944905557160398 ) ) ;
#160265=CARTESIAN_POINT ( 'NONE',  ( 4.582678730018482582, -1.317704446820912700, 1.530705718492784362 ) ) ;
#160270=CARTESIAN_POINT ( 'NONE',  ( 3.133719265644947960, -1.383057153600345535, -1.528062560492246202 ) ) ;
#160271=CARTESIAN_POINT ( 'NONE',  ( 2.936172824561167349, -1.650081981912490336, -1.158688413653415239 ) ) ;
#160278=CARTESIAN_POINT ( 'NONE',  ( 2.829453700430568652, -1.392333688140505510, 1.458332250898628057 ) ) ;
#160279=CARTESIAN_POINT ( 'NONE',  ( 2.958754162918544761, 0.2696264243384552950, -1.821159755858774654 ) ) ;
#160280=CARTESIAN_POINT ( 'NONE',  ( 1.155362744787872931, -1.816424715318950112, 1.423309470994944537 ) ) ;
#160282=CARTESIAN_POINT ( 'NONE',  ( 2.477987356985793088, 1.327747062846416526, 1.705691702009938915 ) ) ;
#160287=CARTESIAN_POINT ( 'NONE',  ( 1.604156678829884886, -0.6703249191640224813, -1.746612230856612769 ) ) ;
#160289=CARTESIAN_POINT ( 'NONE',  ( 5.366080375918201639, 0.9711980517450971018, 1.715566965677978173 ) ) ;
#160293=CARTESIAN_POINT ( 'NONE',  ( 0.5927436934281338221, -2.190715567557582677, -0.2661302102612560505 ) ) ;
#160294=CARTESIAN_POINT ( 'NONE',  ( 6.408651866624735405, 0.6456447432892989946, 1.967203394946090977 ) ) ;
#160297=CARTESIAN_POINT ( 'NONE',  ( 6.639320575229248789, 2.413637632230402286, 2.584074196137386092 ) ) ;
#160298=CARTESIAN_POINT ( 'NONE',  ( 4.592626242060598329, -0.4308863251132522554, -1.923655822462609466 ) ) ;
#160299=CARTESIAN_POINT ( 'NONE',  ( 0.05319811239242258627, 0.3688592364489845510, 2.088132107045739705 ) ) ;
#160301=CARTESIAN_POINT ( 'NONE',  ( 4.899205829341429563, 1.920759858200033587, -1.278847778945918279 ) ) ;
#160302=CARTESIAN_POINT ( 'NONE',  ( 2.096602096640389767, 2.039512422605322950, 0.3069443246750125365 ) ) ;
#160310=CARTESIAN_POINT ( 'NONE',  ( 4.141221389272289777, -0.2091070545618961274, -2.161069556037761519 ) ) ;
#160313=CARTESIAN_POINT ( 'NONE',  ( 4.476008884455379366, -1.787108923542475525, -0.4427587100873929815 ) ) ;
#160315=CARTESIAN_POINT ( 'NONE',  ( 6.620655732516652847, 2.468432086671234149, 2.210906647470804565 ) ) ;
#160316=CARTESIAN_POINT ( 'NONE',  ( 5.337503337980974649, 0.8888059580158399475, -2.003405333693850654 ) ) ;
#160318=CARTESIAN_POINT ( 'NONE',  ( 6.280173827431851485, -1.216757814587710929, 1.907326054681435235 ) ) ;
#160325=CARTESIAN_POINT ( 'NONE',  ( 1.111743784240331712, -0.7909239834335696218, -1.583357840528883287 ) ) ;
#160326=CARTESIAN_POINT ( 'NONE',  ( 4.916656812733911863, -0.6802563888389367985, -1.894789199515679146 ) ) ;
#160328=CARTESIAN_POINT ( 'NONE',  ( 3.926872384942071914, 1.999011803875171189, 0.6627620907858290389 ) ) ;
#160329=CARTESIAN_POINT ( 'NONE',  ( 1.757307594529472272, 1.832486779838927937, -0.5580655975847663708 ) ) ;
#160331=CARTESIAN_POINT ( 'NONE',  ( 3.103910798422233608, 0.7114650421483189602, -1.836736179910645195 ) ) ;
#160332=CARTESIAN_POINT ( 'NONE',  ( 5.308855472784884455, -0.4948685743355190070, -1.958072916474236314 ) ) ;
#160333=CARTESIAN_POINT ( 'NONE',  ( 1.850267049257280139, 0.5840378008528935849, 1.777222254475477659 ) ) ;
#160334=CARTESIAN_POINT ( 'NONE',  ( 5.232891500378062943, 0.1322050776780703540, 1.719872175869048947 ) ) ;
#160335=CARTESIAN_POINT ( 'NONE',  ( 1.546972149855216472, 0.1906517044060058730, 1.902890584052991940 ) ) ;
#160337=CARTESIAN_POINT ( 'NONE',  ( 1.049787907720298286, -1.741764784136769162, -1.355102641770723704 ) ) ;
#160347=CARTESIAN_POINT ( 'NONE',  ( 2.418496320782090869, 0.8830982243829659240, 1.872697815963566992 ) ) ;
#160352=CARTESIAN_POINT ( 'NONE',  ( 6.111998723603361938, -0.7147493727725148238, 1.996541221815250733 ) ) ;
#160357=CARTESIAN_POINT ( 'NONE',  ( 4.007185349139028574, 2.006139037694018690, 0.2004037502189442987 ) ) ;
#160358=CARTESIAN_POINT ( 'NONE',  ( 4.399565145148922163, -1.877536364458038065, 0.3796658851462595408 ) ) ;
#160360=CARTESIAN_POINT ( 'NONE',  ( 3.070069520051089906, -1.303570237086741024, 1.761582097007891923 ) ) ;
#160361=CARTESIAN_POINT ( 'NONE',  ( 0.2335667940002476017, 0.2385907455819072931, -2.187945659632169804 ) ) ;
#160363=CARTESIAN_POINT ( 'NONE',  ( 5.133069374350656133, 1.861756548879553996, 0.7665277172332859434 ) ) ;
#160366=CARTESIAN_POINT ( 'NONE',  ( 6.310183273250552283, 1.218863855842572175, -1.731025912240143017 ) ) ;
#160369=CARTESIAN_POINT ( 'NONE',  ( 3.157844376090960026, 0.9421199074126384021, 1.866540799821286845 ) ) ;
#160371=CARTESIAN_POINT ( 'NONE',  ( 2.238867094643140376, -1.542287835237671212, 0.7722583484809567578 ) ) ;
#160373=CARTESIAN_POINT ( 'NONE',  ( 5.097945154717048233, 1.425953928781589886, 1.569717048080176314 ) ) ;
#160382=CARTESIAN_POINT ( 'NONE',  ( 1.172180985828397581, 0.7336035429467204771, 1.656470807091579900 ) ) ;
#160388=CARTESIAN_POINT ( 'NONE',  ( 2.613665174717228368, -0.5667244042059360609, 1.720617414772870335 ) ) ;
#160391=CARTESIAN_POINT ( 'NONE',  ( 3.525696930263744200, 1.816150354290571034, -0.4055864600542318232 ) ) ;
#160392=CARTESIAN_POINT ( 'NONE',  ( 1.634256478289298320, 0.6027960111968011514, 1.818337931642779903 ) ) ;
#160393=CARTESIAN_POINT ( 'NONE',  ( 0.7447965706881398695, -1.568309060004613231, 0.9341869532639992535 ) ) ;
#160401=CARTESIAN_POINT ( 'NONE',  ( 5.805506361076694155, -1.550124894993635261, -1.214668715896784379 ) ) ;
#160404=CARTESIAN_POINT ( 'NONE',  ( 0.2696249905001372182, 1.205521239366886821, 1.707859383111657747 ) ) ;
#160406=CARTESIAN_POINT ( 'NONE',  ( 4.875960570263176308, 1.108828003875685475, 1.575097709652195643 ) ) ;
#160408=CARTESIAN_POINT ( 'NONE',  ( 1.623764174509664038, -1.011042645414115038, -1.519837739365454521 ) ) ;
#160409=CARTESIAN_POINT ( 'NONE',  ( 2.508667999599442755, -0.8457060194008919618, -2.038605049697986615 ) ) ;
#160411=CARTESIAN_POINT ( 'NONE',  ( 0.8538788329778913555, -0.7122206123622039087, 1.836445260119154543 ) ) ;
#160412=CARTESIAN_POINT ( 'NONE',  ( 2.542442122522000414, -1.613304532933591995, 1.080848972723145618 ) ) ;
#160414=CARTESIAN_POINT ( 'NONE',  ( 1.282577132041575529, -1.967586879516727061, 0.4389604359977539172 ) ) ;
#160416=CARTESIAN_POINT ( 'NONE',  ( 5.067181549875774849, 1.617961714123143047, 0.9193176493522186021 ) ) ;
#160422=CARTESIAN_POINT ( 'NONE',  ( 1.716621854089026344, 2.046377219401524616, 0.7848826361863747714 ) ) ;
#160426=CARTESIAN_POINT ( 'NONE',  ( 2.244514701088017539, 0.3993153960501935051, 1.781317584591130432 ) ) ;
#160432=CARTESIAN_POINT ( 'NONE',  ( 1.418447215319606602, 1.294224929256732493, -1.427187236927564440 ) ) ;
#160433=CARTESIAN_POINT ( 'NONE',  ( 5.928557400228100072, -1.247251702497784942, 1.514172074262534418 ) ) ;
#160436=CARTESIAN_POINT ( 'NONE',  ( 4.985950990042907094, -2.174969566330759996, -0.2684501861200879747 ) ) ;
#160440=CARTESIAN_POINT ( 'NONE',  ( 3.801679563076823420, -1.564429233171928058, -1.355977067927462754 ) ) ;
#160444=CARTESIAN_POINT ( 'NONE',  ( 3.938341551375645011, -1.911473949098478897, -1.276577049080502624 ) ) ;
#160451=CARTESIAN_POINT ( 'NONE',  ( 3.521366475706534160, -1.157360712602263808, -1.559242563676524584 ) ) ;
#160455=CARTESIAN_POINT ( 'NONE',  ( 5.203337695038355193, 1.683698669361912259, -0.9069238330124268499 ) ) ;
#160456=CARTESIAN_POINT ( 'NONE',  ( 5.860297766850644408, 0.7031890092840873407, 1.575098903243739024 ) ) ;
#160457=CARTESIAN_POINT ( 'NONE',  ( 4.557827498477605488, 1.164984774316142113, 1.645760986912048862 ) ) ;
#160459=CARTESIAN_POINT ( 'NONE',  ( 2.192262590105994668, -0.9421081357594159877, 1.995820444975453745 ) ) ;
#160462=CARTESIAN_POINT ( 'NONE',  ( 1.781308773403101231, 1.442672104170627190, 1.513329462076596243 ) ) ;
#160463=CARTESIAN_POINT ( 'NONE',  ( 0.4261447845913856614, 1.691672268694037307, 0.5201907349937917591 ) ) ;
#160464=CARTESIAN_POINT ( 'NONE',  ( 5.467422714486909641, -1.967887220244109558, -0.4390321945699494632 ) ) ;
#160467=CARTESIAN_POINT ( 'NONE',  ( 2.906493132324819761, 1.659771084382713369, -1.581246672503307638 ) ) ;
#160468=CARTESIAN_POINT ( 'NONE',  ( 1.587455592251562297, -1.731706956562387711, -0.1728515053983879501 ) ) ;
#160469=CARTESIAN_POINT ( 'NONE',  ( 2.971057270251746818, -1.603071526910588629, 1.388259434452358665 ) ) ;
#160471=CARTESIAN_POINT ( 'NONE',  ( 1.036033436886945047, 1.672847207165208072, -0.4555716438836182602 ) ) ;
#160474=CARTESIAN_POINT ( 'NONE',  ( 1.856167715545921748, -0.7324389044234179691, 2.044012385327702575 ) ) ;
#160475=CARTESIAN_POINT ( 'NONE',  ( 3.344935638061694139, -1.780668040901035143, -0.9463001528628791625 ) ) ;
#160476=CARTESIAN_POINT ( 'NONE',  ( 3.750000000000002665, 2.137871159508210026E-13, 2.052068128417945836 ) ) ;
#160478=CARTESIAN_POINT ( 'NONE',  ( 0.1121488755844394364, -0.8197171475488943537, -1.741376145853351431 ) ) ;
#160480=CARTESIAN_POINT ( 'NONE',  ( 3.674281580191523400, 2.204306621758029383, -0.2748671541705596799 ) ) ;
#160486=CARTESIAN_POINT ( 'NONE',  ( 5.284588373313929388, 1.531378566088846371, -0.8270805780791794515 ) ) ;
#160487=CARTESIAN_POINT ( 'NONE',  ( 5.019951445752288244, 1.940773837913706057, -0.2859759768028962146 ) ) ;
#160491=CARTESIAN_POINT ( 'NONE',  ( 5.184992917819648994, -0.2698046931138863846, -2.246192962944548732 ) ) ;
#160492=CARTESIAN_POINT ( 'NONE',  ( 1.943872066224684669, 1.420748078972498440, 1.495595626624636409 ) ) ;
#160494=( BOUNDED_CURVE ( )  B_SPLINE_CURVE ( 3, ( #154602, #106970, #44061, #125374 ),
 .UNSPECIFIED., .F., .T. ) 
 B_SPLINE_CURVE_WITH_KNOTS ( ( 4, 4 ),
 ( 0.5000000000000003331, 1.000000000000000000 ),
 .UNSPECIFIED. ) 
 CURVE ( )  GEOMETRIC_REPRESENTATION_ITEM ( )  RATIONAL_B_SPLINE_CURVE ( ( 0.9999999999999997780, 0.3333333333333334259, 0.3333333333333338699, 1.000000000000000222 ) ) 
 REPRESENTATION_ITEM ( '' )  );
#160498=CARTESIAN_POINT ( 'NONE',  ( 3.883945074633635031, -0.9243716352356041721, 1.626130415258054018 ) ) ;
#160499=CARTESIAN_POINT ( 'NONE',  ( 2.707300540323886562, 1.633622375412818073, 0.5822755513817943207 ) ) ;
#160500=CARTESIAN_POINT ( 'NONE',  ( 0.1699995558098127968, 1.326729642492694872, 1.869266897796989291 ) ) ;
#160501=CARTESIAN_POINT ( 'NONE',  ( 0.7278961316968115547, -2.094849050945537972, 0.6941159686642893734 ) ) ;
#160502=CARTESIAN_POINT ( 'NONE',  ( 3.502937704049163159, 1.705309618848281472, -1.328393843302433153 ) ) ;
#160503=CARTESIAN_POINT ( 'NONE',  ( 4.716706857919571227, -0.09384406936703558466, 1.939798966779549882 ) ) ;
#160510=CARTESIAN_POINT ( 'NONE',  ( 5.959611329766300258, -1.915599147091971544, -0.6298778581111733610 ) ) ;
#160514=CARTESIAN_POINT ( 'NONE',  ( 2.912524513316586461, 1.322148455168963510, -1.259233298254287536 ) ) ;
#160515=CARTESIAN_POINT ( 'NONE',  ( 2.221956617217385244, -2.140583525707707935, 0.5359638216213060691 ) ) ;
#160516=EDGE_LOOP ( 'NONE', ( #144136, #177971, #5810, #127175 ) ) ;
#160520=CARTESIAN_POINT ( 'NONE',  ( 0.5979230068290807276, 1.359733756741304811, 1.493685216911154967 ) ) ;
#160521=CARTESIAN_POINT ( 'NONE',  ( 1.436355765274465623, -1.180822252328097344, -1.761085815303937929 ) ) ;
#160524=CARTESIAN_POINT ( 'NONE',  ( 1.779899486625190264, -1.028416011161866983, -1.550745576289275895 ) ) ;
#160526=CARTESIAN_POINT ( 'NONE',  ( 0.2687375195599971400, -1.410744835756465365, 1.637978619736128127 ) ) ;
#160527=CARTESIAN_POINT ( 'NONE',  ( 6.610000000000006537, 0.002781820520842553934, 2.000159646111852929 ) ) ;
#160531=CARTESIAN_POINT ( 'NONE',  ( 3.527797039230845311, -1.088449851438414218, -1.465592618984489670 ) ) ;
#160535=CARTESIAN_POINT ( 'NONE',  ( 6.415388720371407949, 0.6297814698452592896, 1.915305867393565897 ) ) ;
#160536=CARTESIAN_POINT ( 'NONE',  ( 5.894452933195245770, 1.502573388107550034, -1.063714819228026132 ) ) ;
#160537=CARTESIAN_POINT ( 'NONE',  ( 0.07700591528353968596, 0.003617085621422307627, -1.910863332519038282 ) ) ;
#160538=CARTESIAN_POINT ( 'NONE',  ( 4.108297157686680912, -2.301651690510425841, 0.1678553853470560464 ) ) ;
#160540=CARTESIAN_POINT ( 'NONE',  ( 6.116527240895272222, 1.456737685447502262, -1.597155580871166602 ) ) ;
#160542=CARTESIAN_POINT ( 'NONE',  ( 1.733828471206948496, 1.921180395534723528, 0.2831599317468564969 ) ) ;
#160544=CARTESIAN_POINT ( 'NONE',  ( 5.132278277959533064, 0.2326997901972542582, -2.286600633956968220 ) ) ;
#160547=CARTESIAN_POINT ( 'NONE',  ( 4.170664822833985319, -1.745344833062393075, -0.6735866001992969476 ) ) ;
#160549=CARTESIAN_POINT ( 'NONE',  ( 2.742330423940505302, 1.058908597569432120, -1.592262909973440888 ) ) ;
#160552=CARTESIAN_POINT ( 'NONE',  ( 4.125739685719872263, -2.112183141943014153, 0.6395159525410462065 ) ) ;
#160557=CARTESIAN_POINT ( 'NONE',  ( 1.563680990848853591, 1.942865793614118930, -0.3330471066002506642 ) ) ;
#160558=CARTESIAN_POINT ( 'NONE',  ( 1.167484012262551607, -2.087313454887162578, -0.9842159052040798661 ) ) ;
#160559=CARTESIAN_POINT ( 'NONE',  ( 2.594135478747404022, 0.9273930874063830432, -1.728848471177657942 ) ) ;
#160561=CARTESIAN_POINT ( 'NONE',  ( 5.541865367331380909, 1.381078337155069224, 1.532129260548445782 ) ) ;
#160568=CARTESIAN_POINT ( 'NONE',  ( 2.553800759094803308, 1.675875371511101886, 1.380159786156359258 ) ) ;
#160572=CARTESIAN_POINT ( 'NONE',  ( 2.407302635362520427, -0.4140892318466664612, 1.823965488845371574 ) ) ;
#160573=CARTESIAN_POINT ( 'NONE',  ( 6.520800673124607982, 2.014292100380775885, 0.7847517145297827623 ) ) ;
#160578=CARTESIAN_POINT ( 'NONE',  ( 2.736851483355093873, 1.801321139115559244, 0.6423184003811268639 ) ) ;
#160580=CARTESIAN_POINT ( 'NONE',  ( 4.100303288188038131, -0.5556836211836749806, -1.680424235071773742 ) ) ;
#160581=CARTESIAN_POINT ( 'NONE',  ( 1.646971982979035909, 0.1886418863925183320, 1.902964618272011021 ) ) ;
#160584=CARTESIAN_POINT ( 'NONE',  ( -0.1884536309573183466, -1.180508991428173671, -1.509157985239983679 ) ) ;
#160586=CARTESIAN_POINT ( 'NONE',  ( 0.3794556558127279988, -0.1030994254981997954, 2.067933115924729837 ) ) ;
#160589=CARTESIAN_POINT ( 'NONE',  ( 5.383624799460786647, 1.257121276536907750, 1.385457850027263182 ) ) ;
#160590=CARTESIAN_POINT ( 'NONE',  ( 2.262075381241589245, 0.7800679334904643270, 1.650788133108482825 ) ) ;
#160591=CARTESIAN_POINT ( 'NONE',  ( 4.899154391205060577, 1.836108854712194649, -1.224054507610386366 ) ) ;
#160595=CARTESIAN_POINT ( 'NONE',  ( 2.893094712532847890, 0.2500570216604477980, 2.047387263510790145 ) ) ;
#160604=CARTESIAN_POINT ( 'NONE',  ( 5.652806998763869828, -0.4994405740583847675, -2.009109930559597856 ) ) ;
#160607=CARTESIAN_POINT ( 'NONE',  ( 3.145949958485740883, 0.7812230816454240889, -2.015650884352723882 ) ) ;
#160609=CARTESIAN_POINT ( 'NONE',  ( 3.211586479193883292, 1.593432852337670624, 1.240894322269629813 ) ) ;
#160616=CARTESIAN_POINT ( 'NONE',  ( 1.094935803221647186, 1.780670018850015079, 0.9462964651613046119 ) ) ;
#160617=CARTESIAN_POINT ( 'NONE',  ( 5.741772062182810998, 2.188963553168365994, 0.1087695542012837302 ) ) ;
#160619=CARTESIAN_POINT ( 'NONE',  ( 4.992401499097729456, -1.057410677138232780, 1.593263788312593743 ) ) ;
#160623=CARTESIAN_POINT ( 'NONE',  ( 3.497672881252233967, -1.986097994744703721, 0.3474890017408845955 ) ) ;
#160626=CARTESIAN_POINT ( 'NONE',  ( 5.157137038817142916, -1.458691705945897032, -0.9200343150467110709 ) ) ;
#160631=CARTESIAN_POINT ( 'NONE',  ( 0.6200890622066607127, 2.048230590617374336, -0.3001980380039070972 ) ) ;
#160632=CARTESIAN_POINT ( 'NONE',  ( 6.865700769154306826, -0.4580177224273937475, 2.026514595051785772 ) ) ;
#160634=CARTESIAN_POINT ( 'NONE',  ( 5.813115421323210796, 1.476946679544950847, -1.048544953227096288 ) ) ;
#160638=CARTESIAN_POINT ( 'NONE',  ( 6.217428747564047065, 1.510149904227086504, 1.000116013982331076 ) ) ;
#160641=CARTESIAN_POINT ( 'NONE',  ( 3.486445073788289051, -0.4274320362823453290, -2.149191018322317515 ) ) ;
#160643=CARTESIAN_POINT ( 'NONE',  ( 0.4144086874100678664, 0.7473079093508437909, 1.814158889769983185 ) ) ;
#160645=CARTESIAN_POINT ( 'NONE',  ( 5.483970141128155618, -1.915793143390194242, 0.004843307671191510178 ) ) ;
#160655=CARTESIAN_POINT ( 'NONE',  ( 2.008865009297224447, 1.601992838228694316, -1.451600824242594845 ) ) ;
#160656=ADVANCED_FACE ( 'NONE', ( #146046 ), #54480, .F. ) ;
#160660=CARTESIAN_POINT ( 'NONE',  ( 2.362075219488588562, 0.7782009281872975803, 1.651537983114875763 ) ) ;
#160662=CARTESIAN_POINT ( 'NONE',  ( 5.051681782491273864, 0.5714109786712183725, -1.733901259708306331 ) ) ;
#160664=CARTESIAN_POINT ( 'NONE',  ( 3.058751851047710080, 0.4689117840017149041, 1.853869267190631831 ) ) ;
#160666=CARTESIAN_POINT ( 'NONE',  ( 3.965261034597372891, 1.688065314258681893, 1.014448032605998584 ) ) ;
#160668=CARTESIAN_POINT ( 'NONE',  ( 6.409718653046240000, -0.9196952807892575521, -1.710506293091022201 ) ) ;
#160669=EDGE_LOOP ( 'NONE', ( #199102, #183274, #56915, #22505 ) ) ;
#160672=CARTESIAN_POINT ( 'NONE',  ( 5.976833544478475702, -1.498421880457675215, 1.500811427713820478 ) ) ;
#160674=CARTESIAN_POINT ( 'NONE',  ( 3.563058999304801411, -1.561743426874351970, 1.103242700682869781 ) ) ;
#160679=CARTESIAN_POINT ( 'NONE',  ( 4.881498389339896882, 0.1952109149471596417, -2.003590356478464507 ) ) ;
#160681=CARTESIAN_POINT ( 'NONE',  ( 5.602125774977974260, -1.825872481414937853, 0.004271240736861136277 ) ) ;
#160682=CARTESIAN_POINT ( 'NONE',  ( 0.9595327444568906294, 1.691550050060253829, 1.193477315110213599 ) ) ;
#160689=CARTESIAN_POINT ( 'NONE',  ( 0.2333690889706682703, 0.003390530909083006028, -2.053566628440507635 ) ) ;
#160694=CARTESIAN_POINT ( 'NONE',  ( 3.937908632975633871, -1.444535402496229137, -0.9590898762639500363 ) ) ;
#160696=CARTESIAN_POINT ( 'NONE',  ( 1.323191598296684646, -1.869966582492128548, -0.8887066864657000576 ) ) ;
#160697=CARTESIAN_POINT ( 'NONE',  ( 2.829822700998831486, 0.7593016614581545864, -1.976571788296621834 ) ) ;
#160701=CARTESIAN_POINT ( 'NONE',  ( 0.9538786243144499188, -0.7140540310214549269, 1.835613268467409576 ) ) ;
#160706=CARTESIAN_POINT ( 'NONE',  ( 3.029517917392979598, -1.539792254791607862, -1.698243321706040421 ) ) ;
#160707=CARTESIAN_POINT ( 'NONE',  ( 1.242498012622397674, 0.3540479964400863877, 1.790853789395550955 ) ) ;
#160708=CARTESIAN_POINT ( 'NONE',  ( 3.041163856788456687, 0.05134138945498378792, 1.911883771832747048 ) ) ;
#160712=CARTESIAN_POINT ( 'NONE',  ( 1.898691433116481031, -1.975183796067316866, -0.3886032139628642912 ) ) ;
#160713=CARTESIAN_POINT ( 'NONE',  ( 1.727322521004183598, 0.1496332796787832875, -1.956138870750294023 ) ) ;
#160717=CARTESIAN_POINT ( 'NONE',  ( 5.332010518800971433, 2.059573894497103819, 0.3580650863252275440 ) ) ;
#160718=CARTESIAN_POINT ( 'NONE',  ( 3.063107849133941851, 0.2611542325122416797, -1.750338901227658894 ) ) ;
#160722=CARTESIAN_POINT ( 'NONE',  ( 0.04132284026489921325, -1.696808583893465894, -1.386471574116483696 ) ) ;
#160723=CARTESIAN_POINT ( 'NONE',  ( 4.400191647014492169, 1.342938829013840207, -1.106906270395467295 ) ) ;
#160726=CARTESIAN_POINT ( 'NONE',  ( 4.727759377455642564, -1.549208768551156190, -0.7787371415562751586 ) ) ;
#160727=CARTESIAN_POINT ( 'NONE',  ( 4.229095133649480864, -2.024433085375398900, -0.7850780064641171840 ) ) ;
#160729=CARTESIAN_POINT ( 'NONE',  ( 6.385953923436008317, -2.015982004707029596, 0.05432014494890363698 ) ) ;
#160730=CARTESIAN_POINT ( 'NONE',  ( 6.156250000000002665, -1.895863743163982207, 0.7852924748303072855 ) ) ;
#160732=CARTESIAN_POINT ( 'NONE',  ( 2.819263867200746176, -0.1907306445340165024, 1.916936124417574661 ) ) ;
#160734=CARTESIAN_POINT ( 'NONE',  ( 0.03034698492793227315, -2.177136498186870384, 0.4399771670399817425 ) ) ;
#160735=VERTEX_POINT ( 'NONE', #23188 ) ;
#160736=CARTESIAN_POINT ( 'NONE',  ( 6.983263157960372780, 7.052928845687945980, 2.444341994195888379 ) ) ;
#160739=CARTESIAN_POINT ( 'NONE',  ( 2.262617597476920039, 2.220861250988148683, 0.05131716197829398751 ) ) ;
#160744=CARTESIAN_POINT ( 'NONE',  ( 0.2291389764034670318, 2.011204493129043591, 0.1455304468792120720 ) ) ;
#160746=CARTESIAN_POINT ( 'NONE',  ( 5.125460521936802571, 0.2056810312900352600, -2.052415479088207650 ) ) ;
#160751=CARTESIAN_POINT ( 'NONE',  ( 6.889956934492897034, -0.7990643998789861424, 1.689675875712663755 ) ) ;
#160752=CARTESIAN_POINT ( 'NONE',  ( 6.135404405475363809, 0.5537102809010217008, 1.643457313873160741 ) ) ;
#160753=CARTESIAN_POINT ( 'NONE',  ( 5.653775904655955920, 0.7130309894091393375, 1.587888939141286038 ) ) ;
#160754=CARTESIAN_POINT ( 'NONE',  ( 2.894357049080374278, -0.6678387144627718763, -2.192917219349885816 ) ) ;
#160756=CARTESIAN_POINT ( 'NONE',  ( 2.290725937607818175, 1.422998120520948984, 1.168276728405498455 ) ) ;
#160760=CARTESIAN_POINT ( 'NONE',  ( 2.115964440355810439, -0.8579360106165806465, -1.611413330227830176 ) ) ;
#160761=CARTESIAN_POINT ( 'NONE',  ( 2.197888892816081796, 1.802417619043535701, 0.9041091288993635677 ) ) ;
#160764=CARTESIAN_POINT ( 'NONE',  ( 4.155375932019107488, -1.749630165425161143, -1.171798067238625229 ) ) ;
#160769=CARTESIAN_POINT ( 'NONE',  ( 2.752462066230080495, -2.064650614848703825, -0.1547973748374023295 ) ) ;
#160772=CARTESIAN_POINT ( 'NONE',  ( 4.881546266219149999, 0.2071824046101199135, -2.110321684233848583 ) ) ;
#160774=CARTESIAN_POINT ( 'NONE',  ( 6.586557105272873969, -1.791547847876047594, -0.3505316570680468979 ) ) ;
#160781=CARTESIAN_POINT ( 'NONE',  ( 6.486587849989844834, -1.303813291173651301, 1.673118453357678392 ) ) ;
#160782=CARTESIAN_POINT ( 'NONE',  ( 1.465998146299499094, 2.074868464730471374, -0.3595401751291906756 ) ) ;
#160785=CARTESIAN_POINT ( 'NONE',  ( 4.768306509995578146, -0.7929947328253506011, -1.683642203456004127 ) ) ;
#160794=CARTESIAN_POINT ( 'NONE',  ( 2.207404936347991065, -1.573848641742966459, -1.171066219227391070 ) ) ;
#160795=CARTESIAN_POINT ( 'NONE',  ( 1.446389902895691693, 2.159248346720197276, 0.1057134262518744372 ) ) ;
#160800=CARTESIAN_POINT ( 'NONE',  ( 3.233448856393176474, -1.601016440221241455, -0.6660543662743572124 ) ) ;
#160801=CARTESIAN_POINT ( 'NONE',  ( 1.868729199028572596, 1.665863247900209121, -0.5035742270650641617 ) ) ;
#160805=CARTESIAN_POINT ( 'NONE',  ( 0.8607036144342284922, -0.7282710370301350711, 1.880145570116364073 ) ) ;
#160806=CARTESIAN_POINT ( 'NONE',  ( 6.925078400183590333, 2.001873123210990535, 2.545813127278444998 ) ) ;
#160808=CARTESIAN_POINT ( 'NONE',  ( 1.621884544099384096, -1.093522035911981050, -1.640203223306810232 ) ) ;
#160809=CARTESIAN_POINT ( 'NONE',  ( 5.695548698317931091, 1.764485844685494742, -0.7379451211212140205 ) ) ;
#160815=CARTESIAN_POINT ( 'NONE',  ( 1.453777360798803819, -1.464386276593489189, -1.391179603160071387 ) ) ;
#160816=CARTESIAN_POINT ( 'NONE',  ( 4.032480619008128819, 1.237564890788948269, -1.947499633988438061 ) ) ;
#160817=CARTESIAN_POINT ( 'NONE',  ( 6.338335788673861160, -1.050647824335379399, 1.656640365463659670 ) ) ;
#160818=CARTESIAN_POINT ( 'NONE',  ( 3.151168776707893748, 1.684956273983062580, -1.004420888743910334 ) ) ;
#160822=CARTESIAN_POINT ( 'NONE',  ( 1.007203092032255665, -0.04580389244966718426, 2.116997601370627091 ) ) ;
#160825=CARTESIAN_POINT ( 'NONE',  ( 2.185277780439310202, -0.7877041259056734024, 1.664256631099890971 ) ) ;
#160828=CARTESIAN_POINT ( 'NONE',  ( 3.445663904809421307, -1.957918079443463855, 0.8150281543025169606 ) ) ;
#160833=CARTESIAN_POINT ( 'NONE',  ( 3.761055697714862589, -1.815786459315921642, -0.9745866149870155981 ) ) ;
#160835=CARTESIAN_POINT ( 'NONE',  ( 0.2746299231596514012, 1.718356743839201561, -0.6618312839273902126 ) ) ;
#160839=CARTESIAN_POINT ( 'NONE',  ( -0.01666059994226073634, -0.1612322585618740090, -2.171656592459796808 ) ) ;
#160840=CARTESIAN_POINT ( 'NONE',  ( 3.023041696300738934, 2.129209760986842781, 0.7651156340112361676 ) ) ;
#160842=CARTESIAN_POINT ( 'NONE',  ( 2.636723998446516948, 1.707110652976281839, 0.6067464242315090406 ) ) ;
#160844=CARTESIAN_POINT ( 'NONE',  ( 2.905391412282500863, -1.844872930762898600, 0.5157873856561823178 ) ) ;
#160845=CARTESIAN_POINT ( 'NONE',  ( 4.334477209444560053, -1.194628513295314942, 1.690740121169509447 ) ) ;
#160847=CARTESIAN_POINT ( 'NONE',  ( 1.586731204520151151, -0.2873679327500404668, -1.950290023627434755 ) ) ;
#160848=CARTESIAN_POINT ( 'NONE',  ( 0.3934162593667543950, 1.425226140442600098, 1.296210752655905463 ) ) ;
#160849=CARTESIAN_POINT ( 'NONE',  ( 2.694054421766533203, -1.865511834602461949, -0.1395888279770511053 ) ) ;
#160850=CARTESIAN_POINT ( 'NONE',  ( 2.174872218848258765, -1.417835807431093276, 1.820694940605925849 ) ) ;
#160852=CARTESIAN_POINT ( 'NONE',  ( 2.664321193032999524, -0.7092454343347885937, -1.720814620647417303 ) ) ;
#160855=CARTESIAN_POINT ( 'NONE',  ( 6.127400154304522673, 0.1556050751826357770, -2.056880999590751991 ) ) ;
#160860=CARTESIAN_POINT ( 'NONE',  ( 6.387733883603046614, 1.449543625446013673, 1.527951702703828074 ) ) ;
#160862=CARTESIAN_POINT ( 'NONE',  ( 6.538358481810655043, 2.137031053877674225, 0.3242996077847115632 ) ) ;
#160863=CARTESIAN_POINT ( 'NONE',  ( 6.164714676696682716, 0.6357101859572679148, 1.917071687811313652 ) ) ;
#160871=CARTESIAN_POINT ( 'NONE',  ( 4.891814693739657827, -2.006371927678828104, 0.2024599332275459629 ) ) ;
#160876=CARTESIAN_POINT ( 'NONE',  ( 6.579002408576895000, -0.1006694238701970334, -2.159482418181729813 ) ) ;
#160881=CARTESIAN_POINT ( 'NONE',  ( 6.485953897545715385, -2.015913262743720402, 0.05231248585663844652 ) ) ;
#160884=CARTESIAN_POINT ( 'NONE',  ( 1.840065157383737438, 1.705764225012149859, 0.2551292777918309773 ) ) ;
#160888=CARTESIAN_POINT ( 'NONE',  ( 0.9656335942268097217, 0.8653965441102560163, 1.543625204253181948 ) ) ;
#160889=CARTESIAN_POINT ( 'NONE',  ( 1.014315213425314166, -2.013265974724808061, 0.002173784167216683862 ) ) ;
#160891=CARTESIAN_POINT ( 'NONE',  ( 3.258999418838660400, -1.672185875938383859, 1.440126295696932068 ) ) ;
#160892=CARTESIAN_POINT ( 'NONE',  ( 5.084931552659712750, 2.075598280349931546, 0.6366630897998347693 ) ) ;
#160896=CARTESIAN_POINT ( 'NONE',  ( 3.598385148150527346, -1.043669326629501848, 1.845773325594574077 ) ) ;
#160897=CARTESIAN_POINT ( 'NONE',  ( 2.829704019156009220, 0.7231233381281774175, -1.882481713119791067 ) ) ;
#160898=CARTESIAN_POINT ( 'NONE',  ( 3.709066938097814514, 1.527391393591450486, -0.9738182928965555263 ) ) ;
#160902=CARTESIAN_POINT ( 'NONE',  ( 0.3384655940862451029, 0.3152513238553408814, 1.843739016257638141 ) ) ;
#160905=CARTESIAN_POINT ( 'NONE',  ( 1.358442855636652791, -1.820242846481026078, -0.5975442777857197241 ) ) ;
#160914=CARTESIAN_POINT ( 'NONE',  ( 5.383715653711652394, 1.448795075966866852, 1.604530791579752425 ) ) ;
#160918=CARTESIAN_POINT ( 'NONE',  ( 3.181995841446764839, 2.068044944583770306, -0.4684364081647199307 ) ) ;
#160919=CARTESIAN_POINT ( 'NONE',  ( -0.1296875068448159474, 0.7431874094961619104, -1.910093690679348200 ) ) ;
#160921=CARTESIAN_POINT ( 'NONE',  ( 4.499269426148129192, 1.581550893178500727, 1.176622024725955784 ) ) ;
#160922=CARTESIAN_POINT ( 'NONE',  ( 0.03540237040386850359, -0.09474447662855033092, 2.011072404829179483 ) ) ;
#160924=CARTESIAN_POINT ( 'NONE',  ( 5.594942764039734229, 1.868482245966827326, 0.9958698414167986845 ) ) ;
#160925=CARTESIAN_POINT ( 'NONE',  ( 0.9067890187421032699, 0.5993529260880943177, 1.981728858978973218 ) ) ;
#160926=CARTESIAN_POINT ( 'NONE',  ( 2.343606807962240524, 1.941525774309307284, 0.04751797161560606525 ) ) ;
#160930=CARTESIAN_POINT ( 'NONE',  ( 2.642619598058312036, -1.737709898662170183, 1.162055570667380300 ) ) ;
#160933=CARTESIAN_POINT ( 'NONE',  ( -0.05833479489262324152, -1.112358503097829576, -1.430056051773327841 ) ) ;
#160935=CARTESIAN_POINT ( 'NONE',  ( 4.143358556170802842, -1.920740624720223666, 1.086653567583625746 ) ) ;
#160937=CARTESIAN_POINT ( 'NONE',  ( 3.487540646120320442, 1.995909124301387116, -0.9416478298167814120 ) ) ;
#160940=CARTESIAN_POINT ( 'NONE',  ( 1.242663310189826564, 1.843194135250892707, 0.5091577964371830634 ) ) ;
#160942=CARTESIAN_POINT ( 'NONE',  ( 5.512195382060368409, 2.068158883198469855, -0.09793725168850964113 ) ) ;
#160944=CARTESIAN_POINT ( 'NONE',  ( 2.694378501574711926, -2.155843008138720762, -0.1600555415394027403 ) ) ;
#160945=CARTESIAN_POINT ( 'NONE',  ( 5.003566749295822014, -2.181051155298455058, 0.2145382695054529609 ) ) ;
#160952=CARTESIAN_POINT ( 'NONE',  ( 0.2291389764034670318, 2.011204493129043591, 0.1455304468792120720 ) ) ;
#160956=CARTESIAN_POINT ( 'NONE',  ( 5.120015143727554729, 2.048507142264085701, -0.2983452141967629645 ) ) ;
#160957=CARTESIAN_POINT ( 'NONE',  ( 3.018101299323606046, -0.9500872288037317537, -1.675862364343786215 ) ) ;
#160958=CARTESIAN_POINT ( 'NONE',  ( -0.1058464554703278104, -0.8645191204341062807, -1.819937883007181512 ) ) ;
#160961=CARTESIAN_POINT ( 'NONE',  ( 3.731269929808676000, 0.05278475387572807015, -1.968924232409387409 ) ) ;
#160962=CARTESIAN_POINT ( 'NONE',  ( 0.4456111923471539615, 0.6836232613432814409, -2.082162021007263331 ) ) ;
#160963=CARTESIAN_POINT ( 'NONE',  ( 4.160648861918358143, -1.351394993475165673, 1.227733137840483879 ) ) ;
#160970=CARTESIAN_POINT ( 'NONE',  ( 1.909461114401575843, -0.8690924446688346183, -1.623246667998109682 ) ) ;
#160971=CARTESIAN_POINT ( 'NONE',  ( 5.590095194574172588, 1.202541018705102660, 1.614423701025817115 ) ) ;
#160972=CARTESIAN_POINT ( 'NONE',  ( 0.4393512522801552023, 1.325809523182071237, 1.877307722886724317 ) ) ;
#160973=CARTESIAN_POINT ( 'NONE',  ( 5.453941704850034711, -0.7095916301838971485, 1.829088932523432964 ) ) ;
#160979=CARTESIAN_POINT ( 'NONE',  ( 1.505537475160537264, -2.074567991729712180, 0.2591490344204059881 ) ) ;
#160980=CARTESIAN_POINT ( 'NONE',  ( 0.1802491246630563426, -1.813337052076903877, -0.4591185353455888296 ) ) ;
#160982=CARTESIAN_POINT ( 'NONE',  ( -0.1104750535120043037, 1.338503269012698116, -2.356272470560859755 ) ) ;
#160983=CARTESIAN_POINT ( 'NONE',  ( 0.5029371931441508625, -1.732330776274123796, 0.1679752909130062255 ) ) ;
#160986=CARTESIAN_POINT ( 'NONE',  ( 1.787319861506628804, 1.187891131197996497, 1.250883549239764081 ) ) ;
#160987=CARTESIAN_POINT ( 'NONE',  ( 1.488088480104592826, -2.181432686776756391, -0.2102995727721947705 ) ) ;
#160988=CARTESIAN_POINT ( 'NONE',  ( 3.668774463136436736, -1.482526648764719734, 1.634931011441637771 ) ) ;
#160990=CARTESIAN_POINT ( 'NONE',  ( 1.587047119190465594, 2.091647000433814352, 0.5815059253076891865 ) ) ;
#160991=CARTESIAN_POINT ( 'NONE',  ( 1.031563979315492485, -1.156294252604734396, -1.412831148817683680 ) ) ;
#160992=CARTESIAN_POINT ( 'NONE',  ( 2.905574018005254722, -2.039320757748352086, 0.5691538075108558692 ) ) ;
#160993=CARTESIAN_POINT ( 'NONE',  ( 6.539320575229256249, 2.979067782826943844, 2.350490835693248126 ) ) ;
#160995=CARTESIAN_POINT ( 'NONE',  ( 3.527152830493656577, -2.117552691746289018, 0.8784855890422419433 ) ) ;
#160999=CARTESIAN_POINT ( 'NONE',  ( 6.006509256357773552, -2.210310773855695743, -0.2204792344780072411 ) ) ;
#161005=CARTESIAN_POINT ( 'NONE',  ( 4.272111401563948085, 1.799923229630392640, -0.9091438646662284295 ) ) ;
#161007=CARTESIAN_POINT ( 'NONE',  ( 1.780209297579591565, -1.142364670758776013, -1.717135550327288485 ) ) ;
#161012=CARTESIAN_POINT ( 'NONE',  ( 5.261759291836726860, 1.077959533075742993, 1.907929976554381124 ) ) ;
#161013=CARTESIAN_POINT ( 'NONE',  ( 1.881482635453747720, -0.5404922439061732309, -1.942541187959702764 ) ) ;
#161014=CARTESIAN_POINT ( 'NONE',  ( 2.489598673502769977, -1.836455140896048999, -0.1334285330320400531 ) ) ;
#161017=CARTESIAN_POINT ( 'NONE',  ( 5.332948099851452461, 0.1360325894329272867, 1.820554394434070744 ) ) ;
#161018=CARTESIAN_POINT ( 'NONE',  ( 5.836564609439236939, 0.5826586670559866787, -1.930416874340326938 ) ) ;
#161020=CARTESIAN_POINT ( 'NONE',  ( 5.471622919743277969, 2.182126815565027300, -0.5975609995224858695 ) ) ;
#161022=CARTESIAN_POINT ( 'NONE',  ( 0.2234445423696731770, -0.1008541980360810469, 2.103780803345968398 ) ) ;
#161027=MANIFOLD_SOLID_BREP ( 'Sweep1[8]', #70675 ) ;
#161033=CARTESIAN_POINT ( 'NONE',  ( 1.353939357992512305, -1.539690173578952770, -1.458446627980537480 ) ) ;
#161034=CARTESIAN_POINT ( 'NONE',  ( 3.111816671419795011, 1.753586859115576324, 1.363618078755132634 ) ) ;
#161038=CARTESIAN_POINT ( 'NONE',  ( 3.842202535371820993, -0.9690557767615382012, 1.705768119890891610 ) ) ;
#161044=ORIENTED_EDGE ( 'NONE', *, *, #118594, .T. ) ;
#161045=CARTESIAN_POINT ( 'NONE',  ( 2.391022662813433453, -2.030629854096975606, -0.6112283555373964061 ) ) ;
#161047=CARTESIAN_POINT ( 'NONE',  ( 4.118171802502921253, -1.108985364570359566, -1.855417305202881506 ) ) ;
#161048=CARTESIAN_POINT ( 'NONE',  ( 3.948646536499214932, -1.533023199436277961, -1.019512891124202403 ) ) ;
#161051=CARTESIAN_POINT ( 'NONE',  ( 5.226372699876832506, 0.1332071266631333351, 1.735289576922446786 ) ) ;
#161052=CARTESIAN_POINT ( 'NONE',  ( 6.727182134110222478, 3.706444386917655986, 2.325533714637216143 ) ) ;
#161056=CARTESIAN_POINT ( 'NONE',  ( 3.450221060135277629, 2.161883445724331665, 0.001893877739161941697 ) ) ;
#161059=CARTESIAN_POINT ( 'NONE',  ( 5.923203835008548523, 0.8145033986626595279, 1.844426808122232142 ) ) ;
#161061=CARTESIAN_POINT ( 'NONE',  ( 2.922914210685311431, 2.035003303901411265, 0.7295308445595325431 ) ) ;
#161062=CARTESIAN_POINT ( 'NONE',  ( 4.200430055897656167, -0.6152532741215356316, -1.872979577440760046 ) ) ;
#161065=CARTESIAN_POINT ( 'NONE',  ( 5.073749223668181152, -1.075672608635285687, 1.616763269924810231 ) ) ;
#161074=CARTESIAN_POINT ( 'NONE',  ( 0.6400319944965120467, -1.562016764346199960, -1.559085968200937256 ) ) ;
#161076=CARTESIAN_POINT ( 'NONE',  ( 6.297705697576845729, -1.418553083497756884, -1.355282376159852475 ) ) ;
#161080=CARTESIAN_POINT ( 'NONE',  ( 0.07479286986305544449, 6.948552162806721277, -2.450557996216149892 ) ) ;
#161081=CARTESIAN_POINT ( 'NONE',  ( 5.015489797737916255, -0.9877249803392705862, -1.553577481828890106 ) ) ;
#161086=CARTESIAN_POINT ( 'NONE',  ( 5.836213162209912930, -1.179542664122106510, -1.762073437084572314 ) ) ;
#161089=CARTESIAN_POINT ( 'NONE',  ( 0.1806374041631699234, -1.998871265498179506, -0.5013196448642556202 ) ) ;
#161090=EDGE_CURVE ( 'NONE', #57811, #103946, #114351, .T. ) ;
#161092=CARTESIAN_POINT ( 'NONE',  ( 2.172091045797384989, -0.8737597001905510474, -1.643165899227620796 ) ) ;
#161093=CARTESIAN_POINT ( 'NONE',  ( 3.632213977189250098, 0.2737156317273430894, 1.820677940640710979 ) ) ;
#161097=CARTESIAN_POINT ( 'NONE',  ( 6.610000000000012754, 2.967812824040618302, 2.453181572820533951 ) ) ;
#161098=EDGE_LOOP ( 'NONE', ( #77797, #191973, #159895, #6816 ) ) ;
#161100=CARTESIAN_POINT ( 'NONE',  ( 3.844505992619148937, 2.196175933995975438, 0.2170506636963928093 ) ) ;
#161101=CARTESIAN_POINT ( 'NONE',  ( 5.659536867407776839, 0.4493550105662181271, -2.217189852095033942 ) ) ;
#161103=CARTESIAN_POINT ( 'NONE',  ( 5.343967111402722736, -1.155686419774919704, -1.395051459885946699 ) ) ;
#161104=CARTESIAN_POINT ( 'NONE',  ( 6.087116770962817114, 1.596809997336025022, 1.058066368194489959 ) ) ;
#161106=CARTESIAN_POINT ( 'NONE',  ( 6.508674657442179878, 1.384610780642284711, -1.258058027910214927 ) ) ;
#161107=CARTESIAN_POINT ( 'NONE',  ( 5.479139036522528983, -1.730609802697373079, -0.8137914003483390779 ) ) ;
#161109=CARTESIAN_POINT ( 'NONE',  ( 5.893352214189693683, 1.342564598491655437, 1.153274331617970550 ) ) ;
#161111=CARTESIAN_POINT ( 'NONE',  ( 1.833220611596135363, -1.622487599052296670, -1.197302888167578683 ) ) ;
#161113=CARTESIAN_POINT ( 'NONE',  ( 3.211649026191341072, -0.4105298382788050704, 2.065488094592916823 ) ) ;
#161118=CARTESIAN_POINT ( 'NONE',  ( 2.654562054903885304, 2.005031730908119147, 0.2428967267811207309 ) ) ;
#161122=CARTESIAN_POINT ( 'NONE',  ( 3.093221446634909721, 1.855696356685032633, -1.108285163885482039 ) ) ;
#161128=CARTESIAN_POINT ( 'NONE',  ( 1.311231623020674419, -1.711955697424736744, 1.335301017299495685 ) ) ;
#161132=CARTESIAN_POINT ( 'NONE',  ( 2.384552795368581890, -0.3778730364575392797, -2.158588602542845347 ) ) ;
#161133=CARTESIAN_POINT ( 'NONE',  ( 6.883263157960330503, 7.629137130509037412, 2.553810918356711479 ) ) ;
#161134=CARTESIAN_POINT ( 'NONE',  ( 2.887862062735581326, 1.599188571496454658, 1.600737006856695288 ) ) ;
#161141=EDGE_CURVE ( 'NONE', #117162, #167392, #149998, .T. ) ;
#161142=CARTESIAN_POINT ( 'NONE',  ( 4.006921011573481906, 1.516870794648169873, 0.9113941657561406284 ) ) ;
#161144=CARTESIAN_POINT ( 'NONE',  ( 0.7628874492277806230, -1.525271245827728661, 1.452362197770618923 ) ) ;
#161147=CARTESIAN_POINT ( 'NONE',  ( 6.239861269555550649, 2.010826412442122013, -0.1511553674920090573 ) ) ;
#161150=CARTESIAN_POINT ( 'NONE',  ( 3.274138816734498025, -1.115311402298941656, 1.501645261301733481 ) ) ;
#161151=CARTESIAN_POINT ( 'NONE',  ( 3.133707330959301096, 1.967300496787489639, -0.6450458050009516553 ) ) ;
#161156=PLANE ( 'NONE',  #204357 ) ;
#161157=CARTESIAN_POINT ( 'NONE',  ( 6.508665849870631348, 1.605377118863276165, -1.447859449074364591 ) ) ;
#161160=CARTESIAN_POINT ( 'NONE',  ( 2.629291921057617554, 0.09916324773191761976, -1.959495597191794225 ) ) ;
#161162=CARTESIAN_POINT ( 'NONE',  ( 0.9837497097957871306, 1.861730512597782550, 0.7742002051285418185 ) ) ;
#161166=CARTESIAN_POINT ( 'NONE',  ( 1.036156370570060270, 1.841834720703208639, 0.3256331921374157057 ) ) ;
#161168=CARTESIAN_POINT ( 'NONE',  ( 3.234638274129162827, 1.273785088661258058, -1.559031609643942717 ) ) ;
#161170=CARTESIAN_POINT ( 'NONE',  ( 1.915762678288157383, -1.385565726045881130, -1.600959455242874974 ) ) ;
#161172=CARTESIAN_POINT ( 'NONE',  ( 4.229010956685672618, -1.930657356216297860, -0.7480826485904977785 ) ) ;
#161174=CARTESIAN_POINT ( 'NONE',  ( 0.3454080995960371325, 0.6521308015206389586, -1.986527616087286452 ) ) ;
#161176=CARTESIAN_POINT ( 'NONE',  ( 4.963791182761823961, 1.805510465697376610, -0.2690417022049585438 ) ) ;
#161181=CARTESIAN_POINT ( 'NONE',  ( 6.774453055690137226, -1.363307072557031985, 1.735998097611628710 ) ) ;
#161184=CARTESIAN_POINT ( 'NONE',  ( 4.916621234345090130, -0.6478637630910142331, -1.799314785492410529 ) ) ;
#161192=CARTESIAN_POINT ( 'NONE',  ( 4.815616550699190590, -1.834762568278673900, 0.3632225495420540184 ) ) ;
#161201=CARTESIAN_POINT ( 'NONE',  ( 1.780066195911081284, -1.089727156841081346, -1.640273131265007844 ) ) ;
#161202=CARTESIAN_POINT ( 'NONE',  ( 3.726185550002871771, 2.006962945745351945, 0.1948219989877792990 ) ) ;
#161206=CARTESIAN_POINT ( 'NONE',  ( 3.908297495596550597, 1.550167135825938569, -1.549264980215167231 ) ) ;
#161208=CARTESIAN_POINT ( 'NONE',  ( 2.555585810550043302, 0.5154765373659023764, -1.856070933656640332 ) ) ;
#161210=CARTESIAN_POINT ( 'NONE',  ( 0.1331565106231571705, 6.948071080078889850, -2.540993614958915181 ) ) ;
#161217=CARTESIAN_POINT ( 'NONE',  ( 4.950658015114751009, -1.558304906039936988, -0.9804572199803849308 ) ) ;
#161218=CARTESIAN_POINT ( 'NONE',  ( 1.893228294049788207, -0.1010902060475794423, -2.010683160356161014 ) ) ;
#161219=CARTESIAN_POINT ( 'NONE',  ( 4.815913765717094286, -1.849969270989433534, 1.363755144342413850 ) ) ;
#161220=CARTESIAN_POINT ( 'NONE',  ( -0.1290005225502433017, 7.629137130509076492, -2.773995091683974401 ) ) ;
#161221=CARTESIAN_POINT ( 'NONE',  ( 1.990827601993300666, 0.1760917813397035736, 1.852568099299256366 ) ) ;
#161224=CARTESIAN_POINT ( 'NONE',  ( 5.976807594091997800, -1.347613670528555740, 1.357171208065083512 ) ) ;
#161227=CARTESIAN_POINT ( 'NONE',  ( 4.405862271158119903, -0.8954353465763136288, -1.889446048457727789 ) ) ;
#161228=CARTESIAN_POINT ( 'NONE',  ( 2.992876365407059147, 1.605230647100181596, -0.9602576221170722182 ) ) ;
#161232=CARTESIAN_POINT ( 'NONE',  ( 4.793404903408416295, 1.281069664470562142, 1.155212482600373125 ) ) ;
#161236=CARTESIAN_POINT ( 'NONE',  ( 6.262907710099243630, -0.1037740067610822270, -2.014008436551452785 ) ) ;
#161239=CARTESIAN_POINT ( 'NONE',  ( 6.385609454247954453, -2.047150228866960298, 0.7234482234039444348 ) ) ;
#161240=CARTESIAN_POINT ( 'NONE',  ( 4.863791234866603475, 1.805334366393744450, -0.2710410529033688842 ) ) ;
#161241=CARTESIAN_POINT ( 'NONE',  ( 1.323018481131872370, -1.771187822987334570, -0.8437873667686208723 ) ) ;
#161242=CARTESIAN_POINT ( 'NONE',  ( 0.4568545718052554050, -1.995212666551810399, -0.7087754862673681933 ) ) ;
#161247=CARTESIAN_POINT ( 'NONE',  ( 2.244932509249154329, 2.057497683098849617, 0.5125483897536405875 ) ) ;
#161251=CARTESIAN_POINT ( 'NONE',  ( 0.7255434793691470929, 0.2065170452952343472, -2.059959488672699290 ) ) ;
#161252=CARTESIAN_POINT ( 'NONE',  ( 6.883263157960364254, 3.685033293952295175, 2.667793810733168236 ) ) ;
#161254=CARTESIAN_POINT ( 'NONE',  ( 2.297798353768167434, 2.029563722251678026, -0.9032078376340900716 ) ) ;
#161255=ORIENTED_EDGE ( 'NONE', *, *, #203422, .T. ) ;
#161256=CARTESIAN_POINT ( 'NONE',  ( 0.3175262209036809891, 1.174723722100686762, -1.975753589677962552 ) ) ;
#161258=CARTESIAN_POINT ( 'NONE',  ( 6.086800983681886379, 1.986285820840045124, 0.5554444937589071429 ) ) ;
#161262=CARTESIAN_POINT ( 'NONE',  ( 0.1333542156527295908, 5.722835866173135777, -2.639957043922738666 ) ) ;
#161263=CARTESIAN_POINT ( 'NONE',  ( 6.040549724581927293, -1.551790349881351450, 0.9907606852931831742 ) ) ;
#161266=DIRECTION ( 'NONE',  ( 1.000000000000000000, 0.000000000000000000, 0.000000000000000000 ) ) ;
#161267=CARTESIAN_POINT ( 'NONE',  ( 3.258550815082728036, -1.306766610546957530, 1.125807055032159054 ) ) ;
#161268=CARTESIAN_POINT ( 'NONE',  ( 1.692592581891849912, 1.490968054865527082, -1.357870634957742961 ) ) ;
#161269=CARTESIAN_POINT ( 'NONE',  ( 2.795839995030196423, 1.662961046791612940, -1.587192879829945946 ) ) ;
#161271=CARTESIAN_POINT ( 'NONE',  ( 2.355063576532693936, -1.750152493129919717, 1.433722681173225100 ) ) ;
#161272=CARTESIAN_POINT ( 'NONE',  ( 4.406922956430887162, 1.628233754946675882, -1.335794222675233511 ) ) ;
#161274=CARTESIAN_POINT ( 'NONE',  ( 3.725649928583890436, -1.052200936647734286, -1.422817597083583241 ) ) ;
#161277=CARTESIAN_POINT ( 'NONE',  ( 5.935170609274059039, -1.657740282732190096, -1.583558971889464706 ) ) ;
#161278=CARTESIAN_POINT ( 'NONE',  ( 4.927609005033061429, 0.9437523325564222132, -1.580719041474540010 ) ) ;
#161283=CARTESIAN_POINT ( 'NONE',  ( 4.734432829848630675, 0.3728853646711489112, 2.159338447334692823 ) ) ;
#161288=CARTESIAN_POINT ( 'NONE',  ( 3.176308805823165660, -1.146983237646619580, 1.547710939905672989 ) ) ;
#161291=CARTESIAN_POINT ( 'NONE',  ( 0.4400545237335662940, -2.106857831338632359, 0.7043091553551988904 ) ) ;
#161301=CARTESIAN_POINT ( 'NONE',  ( 2.278492620635372390, 1.590801041788017178, -0.7064735415249421280 ) ) ;
#161303=CARTESIAN_POINT ( 'NONE',  ( 0.6780837441340243910, -1.046368970337024473, -1.659334490400856676 ) ) ;
#161307=CARTESIAN_POINT ( 'NONE',  ( 6.702040708066513197, -2.161345696851162845, 0.04751196314212167288 ) ) ;
#161310=CARTESIAN_POINT ( 'NONE',  ( 5.823154874416164084, -0.05760400987671504547, 2.161107263091876618 ) ) ;
#161313=CARTESIAN_POINT ( 'NONE',  ( 6.591095686763909001, 1.716256228956919871, -0.9697327587238188107 ) ) ;
#161314=CARTESIAN_POINT ( 'NONE',  ( 6.380242484794338864, -0.2077342984398328762, 1.721287130621736772 ) ) ;
#161316=CARTESIAN_POINT ( 'NONE',  ( 3.404031855413204966, -0.8899279105200922357, -2.002928011436304612 ) ) ;
#161317=CARTESIAN_POINT ( 'NONE',  ( 2.802171680323842118, -0.7245931359087741663, 2.190924829087222303 ) ) ;
#161318=CARTESIAN_POINT ( 'NONE',  ( 6.134070664438048048, 1.019536383099900245, -1.790854842558225801 ) ) ;
#161319=CARTESIAN_POINT ( 'NONE',  ( 1.165847801482827517, -1.232189268765693235, 1.500965459471349961 ) ) ;
#161324=CARTESIAN_POINT ( 'NONE',  ( 3.586284538990120119, 1.181046903802231984, 1.761068336431830472 ) ) ;
#161326=CARTESIAN_POINT ( 'NONE',  ( 2.637342451166882373, 0.6819965276749391236, 1.897697610567940174 ) ) ;
#161328=CARTESIAN_POINT ( 'NONE',  ( 5.719807747550186505, -2.154180246964752410, 0.4782370604126117142 ) ) ;
#161338=CARTESIAN_POINT ( 'NONE',  ( 4.592684518728709975, -0.4495978358524716501, -2.011083796685923630 ) ) ;
#161344=CARTESIAN_POINT ( 'NONE',  ( 3.738929604108613969, 1.918458267904774806, 0.6316034170958833016 ) ) ;
#161349=CARTESIAN_POINT ( 'NONE',  ( 2.623961231070126132, -1.185536401616044566, -1.685555923420704039 ) ) ;
#161350=CARTESIAN_POINT ( 'NONE',  ( 2.619767714365705658, 0.2496074646863334634, 2.000857082853441327 ) ) ;
#161356=CARTESIAN_POINT ( 'NONE',  ( 2.653672528425448540, -0.3418824089525332455, -1.986742401007553172 ) ) ;
#161357=CARTESIAN_POINT ( 'NONE',  ( 2.976309490518674217, -0.1360139883382974202, -1.836174483004118674 ) ) ;
#161358=CARTESIAN_POINT ( 'NONE',  ( 6.393228082638676923, 1.922373441260841087, -1.083778638264052852 ) ) ;
#161360=CARTESIAN_POINT ( 'NONE',  ( 2.390102426918311540, -0.9266024157483061519, 1.953076554623616401 ) ) ;
#161362=CARTESIAN_POINT ( 'NONE',  ( 4.188735998470741073, 1.634407174013367214, -1.345997343221926545 ) ) ;
#161363=CARTESIAN_POINT ( 'NONE',  ( 2.583761237542493205, 1.502156065388253081, -1.739619357585840520 ) ) ;
#161367=CARTESIAN_POINT ( 'NONE',  ( 1.656895194024514906, -1.602792776363659133, -0.9643473572949823325 ) ) ;
#161368=CARTESIAN_POINT ( 'NONE',  ( 6.104366069677094053, -0.7090783117675543146, -1.839710284007533225 ) ) ;
#161373=CARTESIAN_POINT ( 'NONE',  ( 0.3642759247451561322, 2.182245240920151375, -0.3280614795862640820 ) ) ;
#161374=CARTESIAN_POINT ( 'NONE',  ( 6.320769956279724155, -1.466918727022302971, 1.461273828345016845 ) ) ;
#161377=CARTESIAN_POINT ( 'NONE',  ( 6.539320575229297106, 0.5644099559201658511, 2.255290358406045303 ) ) ;
#161378=CARTESIAN_POINT ( 'NONE',  ( 5.453970954872065846, 1.969229766360120149, -0.09616449669870225092 ) ) ;
#161379=CARTESIAN_POINT ( 'NONE',  ( -0.1401555495076401980, -1.643345231473653190, -1.339971704266910812 ) ) ;
#161381=CARTESIAN_POINT ( 'NONE',  ( 4.248838534556359292, 0.6131519058680062750, 2.224680453567278171 ) ) ;
#161382=CARTESIAN_POINT ( 'NONE',  ( 2.043871907009750633, 1.419221230981766668, 1.496905473486829230 ) ) ;
#161391=CARTESIAN_POINT ( 'NONE',  ( 4.352125359537689420, -0.8347222424532302343, 2.004499096949263759 ) ) ;
#161393=CARTESIAN_POINT ( 'NONE',  ( 4.106863108761789505, -0.3106082297497716471, 1.814695527881895476 ) ) ;
#161395=CARTESIAN_POINT ( 'NONE',  ( 6.620655732516649294, 4.703748234811334861, 2.289014941052476715 ) ) ;
#161396=CARTESIAN_POINT ( 'NONE',  ( 5.653911837654605144, 0.8871495062587383407, 2.004161502255866090 ) ) ;
#161398=CARTESIAN_POINT ( 'NONE',  ( 5.823173511171203742, -0.06224829877122214916, 2.261828766561886361 ) ) ;
#161404=CARTESIAN_POINT ( 'NONE',  ( 0.7953275966026486232, -0.6425790844533132429, 1.649264876520744272 ) ) ;
#161405=CARTESIAN_POINT ( 'NONE',  ( 5.338544149128367167, 1.197215095128815632, -1.618272059301849586 ) ) ;
#161407=CARTESIAN_POINT ( 'NONE',  ( 4.032330418399681093, 1.128390736420165519, -1.777953997047557744 ) ) ;
#161408=CARTESIAN_POINT ( 'NONE',  ( 1.862754361789496160, -0.09592165986596230820, -1.913344494172765753 ) ) ;
#161410=CARTESIAN_POINT ( 'NONE',  ( 2.717198260794476017, -1.712298780928861008, -0.9731099088599747260 ) ) ;
#161411=CARTESIAN_POINT ( 'NONE',  ( 4.992447118679333329, -1.118567257517719460, 1.681552772592603384 ) ) ;
#161412=CARTESIAN_POINT ( 'NONE',  ( 1.129532124359374334, -1.183843481993757774, -1.448407549327054955 ) ) ;
#161413=CARTESIAN_POINT ( 'NONE',  ( 5.443894040360703457, 0.6935754108010495633, -1.579493244201269908 ) ) ;
#161414=CARTESIAN_POINT ( 'NONE',  ( 1.072351618572921605, 0.7776387867773439933, 1.747342548420704800 ) ) ;
#161416=CARTESIAN_POINT ( 'NONE',  ( 1.418904949497600487, 1.480075412272121582, -1.637148382315711359 ) ) ;
#161424=CARTESIAN_POINT ( 'NONE',  ( 6.332887962430945983, -1.963924782908726296, -0.6550794379977520343 ) ) ;
#161425=CARTESIAN_POINT ( 'NONE',  ( 0.9595327444568906294, 1.691550050060253829, 1.193477315110213599 ) ) ;
#161430=CARTESIAN_POINT ( 'NONE',  ( 5.110073233524446756, -0.7627883623938614965, 1.978724553277847464 ) ) ;
#161438=CARTESIAN_POINT ( 'NONE',  ( 3.884138610457484653, -0.1511163893381066714, 2.010518618204664154 ) ) ;
#161439=CARTESIAN_POINT ( 'NONE',  ( 5.155460239800898847, 1.844409812803897264, -0.5174689040137578910 ) ) ;
#161441=CARTESIAN_POINT ( 'NONE',  ( 2.314256413632868714, 1.428969747754246233, -1.661726224907192684 ) ) ;
#161444=CARTESIAN_POINT ( 'NONE',  ( 5.097907127711155617, 1.355137859109056819, 1.488956579698009763 ) ) ;
#161448=CARTESIAN_POINT ( 'NONE',  ( 5.888306048034124274, -0.7624388358357903073, -1.975341773770035614 ) ) ;
#161450=CARTESIAN_POINT ( 'NONE',  ( 3.052369502041663019, -1.581437162565798804, 1.367655637459828544 ) ) ;
#161452=CARTESIAN_POINT ( 'NONE',  ( 1.377515174558477273, 1.023066641755419282, 1.388426169202553018 ) ) ;
#161453=ORIENTED_EDGE ( 'NONE', *, *, #47479, .T. ) ;
#161454=CARTESIAN_POINT ( 'NONE',  ( 5.467072749063267345, -1.670387955228332277, 1.306269166133758208 ) ) ;
#161463=CARTESIAN_POINT ( 'NONE',  ( 1.963241191952873388, -1.455257657876586341, -1.078514734469406600 ) ) ;
#161469=CARTESIAN_POINT ( 'NONE',  ( 2.350024359177401490, 0.8526225883829393615, -1.598239438867412820 ) ) ;
#161470=CARTESIAN_POINT ( 'NONE',  ( 6.539320575229228716, 1.281788455817688188, 2.013036689384885225 ) ) ;
#161475=CARTESIAN_POINT ( 'NONE',  ( 3.754231824312683763, -1.858861104869345082, -0.09317703841194531489 ) ) ;
#161476=CARTESIAN_POINT ( 'NONE',  ( 1.071739250477701466, -0.8599075215434035524, 1.711803488807943197 ) ) ;
#161477=CARTESIAN_POINT ( 'NONE',  ( 6.071306304379397112, 0.1413743337459697769, -1.921272325444240980 ) ) ;
#161480=EDGE_CURVE ( 'NONE', #99811, #193311, #186930, .T. ) ;
#161485=CARTESIAN_POINT ( 'NONE',  ( 5.910992199152527604, -1.554775717584104378, 1.208803697826433599 ) ) ;
#161488=CARTESIAN_POINT ( 'NONE',  ( 0.3399330434069799400, 2.085199349320911555, 0.1515528320938461238 ) ) ;
#161489=CARTESIAN_POINT ( 'NONE',  ( 5.790048612033079856, -0.8660258810785811390, 1.720834695440204509 ) ) ;
#161491=CARTESIAN_POINT ( 'NONE',  ( 1.149113351018778539, -1.436424422225426767, -1.126575773451453433 ) ) ;
#161492=CARTESIAN_POINT ( 'NONE',  ( 1.770444396619451632, 1.136427050704125419, 1.891651738277564831 ) ) ;
#161494=CARTESIAN_POINT ( 'NONE',  ( 0.1231139863388103495, 1.664874722635242277, 0.9407772870168448209 ) ) ;
#161496=CARTESIAN_POINT ( 'NONE',  ( 0.9593497616274889728, 1.608103478905052119, 1.136861374779022604 ) ) ;
#161497=CARTESIAN_POINT ( 'NONE',  ( 1.294366139777222369, 1.586748096885544745, -1.119478687268110173 ) ) ;
#161499=CARTESIAN_POINT ( 'NONE',  ( 0.3333609138582178111, -1.319029705771988858, 1.524807370920200356 ) ) ;
#161501=CARTESIAN_POINT ( 'NONE',  ( 5.049569799528213387, 1.377159375265882391, 1.251766951177714526 ) ) ;
#161507=CARTESIAN_POINT ( 'NONE',  ( 1.523247060345904291, -2.062048068855956373, 0.7425582295156886170 ) ) ;
#161511=CARTESIAN_POINT ( 'NONE',  ( 1.576486190600217663, -1.733098801405801304, -0.5742540608338757568 ) ) ;
#161515=CARTESIAN_POINT ( 'NONE',  ( 6.509000000000034092, 7.052765612591089806, 2.598154238703707541 ) ) ;
#161517=CARTESIAN_POINT ( 'NONE',  ( 0.7680398806059639538, 0.9487340639210088966, 1.676631345724951982 ) ) ;
#161518=CARTESIAN_POINT ( 'NONE',  ( 5.260583753728677259, -0.6573284944802314511, -1.848511375219172415 ) ) ;
#161521=CARTESIAN_POINT ( 'NONE',  ( 4.669572502782517454, 1.262004115398765780, 1.791526714441132873 ) ) ;
#161524=CARTESIAN_POINT ( 'NONE',  ( 3.889561532384704368, -1.914723906051108537, 0.7877538119766481772 ) ) ;
#161528=CARTESIAN_POINT ( 'NONE',  ( 4.008600857689972763, -2.199693827605917917, 0.6672659128543911855 ) ) ;
#161533=CARTESIAN_POINT ( 'NONE',  ( 4.312401332534675724, 1.776009277829879718, 0.7858599780834804038 ) ) ;
#161537=CARTESIAN_POINT ( 'NONE',  ( 5.133030909251353968, 1.769313487831367659, 0.7262901588861517821 ) ) ;
#161539=CARTESIAN_POINT ( 'NONE',  ( 6.774431772926147843, -1.055741295204252195, 1.364281925921766447 ) ) ;
#161540=CARTESIAN_POINT ( 'NONE',  ( 4.206267736153862735, 1.236801365491456028, -1.592660703826812352 ) ) ;
#161542=CARTESIAN_POINT ( 'NONE',  ( 1.295869073816724226, 1.673045085319382119, 1.439284050222865652 ) ) ;
#161545=CARTESIAN_POINT ( 'NONE',  ( 1.341864181646670540, 2.088322648670298598, 0.1009416716012418447 ) ) ;
#161546=CARTESIAN_POINT ( 'NONE',  ( 6.450471989241519211, 0.5578098333037047052, 1.679625245746432016 ) ) ;
#161547=CARTESIAN_POINT ( 'NONE',  ( 5.678361341766085424, 1.528739221709461082, 1.314999087022615587 ) ) ;
#161549=CARTESIAN_POINT ( 'NONE',  ( 2.572590238467100665, -2.194022629849821104, -0.6638836622538509813 ) ) ;
#161550=CARTESIAN_POINT ( 'NONE',  ( 0.7963321702096434196, 1.420339700582837539, 1.005379078535458159 ) ) ;
#161552=CARTESIAN_POINT ( 'NONE',  ( 0.9832555119714074809, 1.599142458273569600, 0.6705785602827417646 ) ) ;
#161555=CARTESIAN_POINT ( 'NONE',  ( 1.803425971091272340, -1.834736872252432649, 1.160642024321426380 ) ) ;
#161556=CARTESIAN_POINT ( 'NONE',  ( 2.747280062631300535, 0.2910806042949847239, -1.995268371848608835 ) ) ;
#161557=CARTESIAN_POINT ( 'NONE',  ( 4.812500000000003553, 1.451031289061308183, 1.451031289060921159 ) ) ;
#161560=CARTESIAN_POINT ( 'NONE',  ( 6.111935756226617222, -1.911612718183410387, 0.2385651428990897549 ) ) ;
#161562=CARTESIAN_POINT ( 'NONE',  ( 3.375417215397161552, -1.960608319544883793, -1.044296844735680185 ) ) ;
#161568=CARTESIAN_POINT ( 'NONE',  ( 5.952664183270127474, -1.497414089959566930, -0.8868285315999470120 ) ) ;
#161570=CARTESIAN_POINT ( 'NONE',  ( 3.894932841003693191, 0.2855096342280309396, 1.940843471192068792 ) ) ;
#161575=CARTESIAN_POINT ( 'NONE',  ( 4.200629628819559258, -0.7044727654359562719, -2.150022973637927048 ) ) ;
#161576=CARTESIAN_POINT ( 'NONE',  ( 1.732955346664406537, -1.957976925384408817, -0.6489628464096306448 ) ) ;
#161578=CARTESIAN_POINT ( 'NONE',  ( 2.061739773175938595, 0.3863463398323406794, -2.229145236428681454 ) ) ;
#161581=CARTESIAN_POINT ( 'NONE',  ( 3.743291833738107144, -1.414529149469236691, -1.224010458943748603 ) ) ;
#161582=CARTESIAN_POINT ( 'NONE',  ( 2.267823513004694647, 1.585025364652093760, -0.7039959249812016706 ) ) ;
#161583=CARTESIAN_POINT ( 'NONE',  ( 6.462441986028243157, -2.002789442531027309, -0.8901952361822995652 ) ) ;
#161584=CARTESIAN_POINT ( 'NONE',  ( 0.3939699847536023980, 1.636818068892214040, 1.480257586202008646 ) ) ;
#161585=CARTESIAN_POINT ( 'NONE',  ( 4.083022661009271914, -0.2092679848491978134, -2.151539631373246220 ) ) ;
#161586=CARTESIAN_POINT ( 'NONE',  ( 5.068278781427039803, -1.829183178514147690, -0.6524800764661740082 ) ) ;
#161589=CARTESIAN_POINT ( 'NONE',  ( 6.872336254976083580, -1.150436037642876608, 1.475500831757702747 ) ) ;
#161594=CARTESIAN_POINT ( 'NONE',  ( 5.238907797441370029, 2.013986022392059816, -0.1017483359899013229 ) ) ;
#161598=CARTESIAN_POINT ( 'NONE',  ( 2.701551412915685457, -0.5726843992823158480, 1.733614832724015731 ) ) ;
#161599=CARTESIAN_POINT ( 'NONE',  ( 1.923171073188837843, 2.059116738528983692, 0.7940920450543451636 ) ) ;
#161605=CARTESIAN_POINT ( 'NONE',  ( 1.265885189609064376, 0.5823756177252036315, -1.934031124627869414 ) ) ;
#161606=CARTESIAN_POINT ( 'NONE',  ( 1.576976220782677185, -1.497206391897941913, 1.501870991332490135 ) ) ;
#161608=CARTESIAN_POINT ( 'NONE',  ( 1.604125426503384411, 1.858527726531463697, 0.09786615749988146484 ) ) ;
#161610=CARTESIAN_POINT ( 'NONE',  ( 6.614142728931415860, -0.9689641062460941923, -1.818880834187324824 ) ) ;
#161611=CARTESIAN_POINT ( 'NONE',  ( 6.451795992440088057, -1.844709169062180409, -0.8146298745319994206 ) ) ;
#161615=CARTESIAN_POINT ( 'NONE',  ( 4.019992336727182369, -0.9402185374879183932, -1.564826772493657536 ) ) ;
#161619=CARTESIAN_POINT ( 'NONE',  ( 6.432970213454214381, 1.034009579150240610, 1.730599625746793935 ) ) ;
#161620=CARTESIAN_POINT ( 'NONE',  ( 5.472543265827003012, -0.04911201564661467345, -1.840652735559132669 ) ) ;
#161621=CARTESIAN_POINT ( 'NONE',  ( 0.07680821025393690105, 0.005952109439256307241, -1.810863387344714193 ) ) ;
#161622=CARTESIAN_POINT ( 'NONE',  ( 3.510674805948321264, -0.9346715503392712954, -2.110115307156499753 ) ) ;
#161624=CARTESIAN_POINT ( 'NONE',  ( 5.800121417639972243, -2.161773191644947634, -0.006422599366645573467 ) ) ;
#161626=CARTESIAN_POINT ( 'NONE',  ( 1.153739077726954498, 0.7885942357991974072, 1.774928408438203098 ) ) ;
#161628=CARTESIAN_POINT ( 'NONE',  ( 4.183220704542046420, -1.177475575078859027, -1.973740397952013836 ) ) ;
#161631=CARTESIAN_POINT ( 'NONE',  ( 4.680451076648031616, -1.814532364864028136, -0.4542276060127621862 ) ) ;
#161633=CARTESIAN_POINT ( 'NONE',  ( 2.162237915172473546, 1.912057200688283665, 0.04323261116381121871 ) ) ;
#161636=CARTESIAN_POINT ( 'NONE',  ( 4.266400587755204477, 1.039063272370500668, 1.946970035688735390 ) ) ;
#161637=CARTESIAN_POINT ( 'NONE',  ( 6.983263157960410972, 2.978556228996271482, 2.299637001123565838 ) ) ;
#161642=CARTESIAN_POINT ( 'NONE',  ( 2.073447407941295673, 1.887670557785134928, -0.5683696268203948243 ) ) ;
#161643=CARTESIAN_POINT ( 'NONE',  ( 0.9038794553481295235, 1.888499008566895787, 1.325839279686758632 ) ) ;
#161644=CARTESIAN_POINT ( 'NONE',  ( 2.752341281506097470, -1.956419249932477955, -0.1471676765215298721 ) ) ;
#161646=CARTESIAN_POINT ( 'NONE',  ( 5.471554536677815328, -0.3081364425130261320, 2.039334399838355960 ) ) ;
#161653=CARTESIAN_POINT ( 'NONE',  ( 0.7960475122521799562, -1.534068779871503363, -1.536527999751842621 ) ) ;
#161658=CARTESIAN_POINT ( 'NONE',  ( 2.196370303256788503, -0.4943915968025693330, -1.803980227719769847 ) ) ;
#161659=CARTESIAN_POINT ( 'NONE',  ( 0.3861014259941424887, -0.9735654513510684227, 1.816333823429964411 ) ) ;
#161661=CARTESIAN_POINT ( 'NONE',  ( 6.727182134110231360, 2.105158487175392334, 2.022197281440795358 ) ) ;
#161663=CARTESIAN_POINT ( 'NONE',  ( 2.807167725247063483, 1.639017566557477990, -0.9848878580655600068 ) ) ;
#161665=CARTESIAN_POINT ( 'NONE',  ( 3.871743310845751296, 0.9831255770079703193, 1.471438590500689925 ) ) ;
#161666=CARTESIAN_POINT ( 'NONE',  ( 1.805181101471531546, 1.663141274854248230, -0.9436981260437929953 ) ) ;
#161669=CARTESIAN_POINT ( 'NONE',  ( 5.378507874412199463, -0.4701315380702688618, -1.856876755957288516 ) ) ;
#161671=CARTESIAN_POINT ( 'NONE',  ( 6.250452387334210158, -1.959941389959872549, -0.1944618805250642457 ) ) ;
#161673=CARTESIAN_POINT ( 'NONE',  ( 2.004293344102888508, -0.9022931611136343344, 1.919180038594799687 ) ) ;
#161674=CARTESIAN_POINT ( 'NONE',  ( 4.873830839387755631, 1.077430855447782942, 1.529020332772989210 ) ) ;
#161675=CARTESIAN_POINT ( 'NONE',  ( 1.207329354700342305, -0.4456725867950651621, 1.770335049871730071 ) ) ;
#161677=CARTESIAN_POINT ( 'NONE',  ( 4.301547675229603129, 1.771612934706376707, 1.315755017190944676 ) ) ;
#161680=CARTESIAN_POINT ( 'NONE',  ( 1.398963405728241183, 0.4003750237208941742, 2.023287731994154015 ) ) ;
#161689=CARTESIAN_POINT ( 'NONE',  ( 4.598136200040512378, 0.8882050449813773119, -1.870312673664726644 ) ) ;
#161691=CARTESIAN_POINT ( 'NONE',  ( 2.179201376995115513, -0.1036959380565916772, -2.159207860300814463 ) ) ;
#161693=CARTESIAN_POINT ( 'NONE',  ( 2.719404001658455527, 1.707403962800517316, 1.078498517531191858 ) ) ;
#161694=CARTESIAN_POINT ( 'NONE',  ( 6.620655732516615544, 2.958939621373418483, 2.526443930770333246 ) ) ;
#161700=CARTESIAN_POINT ( 'NONE',  ( 1.604704241733472037, 1.883313803065278513, 0.7212895827233902768 ) ) ;
#161701=CARTESIAN_POINT ( 'NONE',  ( 5.706613541269077494, 1.932210019790636224, 1.034112652976440394 ) ) ;
#161703=CARTESIAN_POINT ( 'NONE',  ( 4.359561026920276916, -1.481784043772149451, -1.208992945495937610 ) ) ;
#161708=CARTESIAN_POINT ( 'NONE',  ( 2.161732667986946410, 1.242745142284812365, 1.587824664567152766 ) ) ;
#161711=CARTESIAN_POINT ( 'NONE',  ( 5.174679765213248572, -1.625057609515182078, -0.5782863776828560676 ) ) ;
#161712=CARTESIAN_POINT ( 'NONE',  ( -0.1399997263889559695, 7.629137130509076492, -2.600276787041354343 ) ) ;
#161717=CARTESIAN_POINT ( 'NONE',  ( 0.8485890540621650047, -2.054197865963180547, -0.2570499307305574299 ) ) ;
#161719=CARTESIAN_POINT ( 'NONE',  ( 5.004484103855499910, -1.798449698946352537, -0.2161431223286890690 ) ) ;
#161722=CARTESIAN_POINT ( 'NONE',  ( 6.445981706654077215, -1.189238676736432465, -1.366527308926633211 ) ) ;
#161725=CARTESIAN_POINT ( 'NONE',  ( 3.345827479060593301, 2.191629467292684819, -0.0001215010576177677764 ) ) ;
#161728=CARTESIAN_POINT ( 'NONE',  ( 0.1858947801188018389, -1.204007190563995078, -1.549573762531175625 ) ) ;
#161730=CARTESIAN_POINT ( 'NONE',  ( 4.446842608676645270, -1.712983832262956696, -0.8575701973691277624 ) ) ;
#161737=CARTESIAN_POINT ( 'NONE',  ( 1.657319961134783748, -1.854130675604428902, -1.111159678259740602 ) ) ;
#161740=CARTESIAN_POINT ( 'NONE',  ( 2.028078973712159172, 1.053637016394028292, -1.490636434207486261 ) ) ;
#161742=CARTESIAN_POINT ( 'NONE',  ( 5.139593076133684768, -1.292025762983130877, -1.289991942498528443 ) ) ;
#161744=CARTESIAN_POINT ( 'NONE',  ( 2.935702856749936362, -1.841876368404654629, 0.5141854427313449216 ) ) ;
#161746=CARTESIAN_POINT ( 'NONE',  ( 3.332427603156477680, -1.175354876789212799, 1.580226413267592500 ) ) ;
#161748=CARTESIAN_POINT ( 'NONE',  ( 5.548367435846999207, -1.528527190574509032, 1.197884188273186323 ) ) ;
#161752=CARTESIAN_POINT ( 'NONE',  ( 4.939744792934912532, -2.012803497507458683, 0.6676120485993168874 ) ) ;
#161754=CARTESIAN_POINT ( 'NONE',  ( 2.930216680654484041, -0.9444820207657660394, -1.662695861641521278 ) ) ;
#161759=CARTESIAN_POINT ( 'NONE',  ( 5.338544149128367167, 1.197215095128815632, -1.618272059301849586 ) ) ;
#161761=CARTESIAN_POINT ( 'NONE',  ( 6.094357461763901362, -1.817385979143220309, -0.1739998769475574192 ) ) ;
#161762=CARTESIAN_POINT ( 'NONE',  ( 0.7485892145711987578, -2.054541080789675789, -0.2550698046258002005 ) ) ;
#161767=CARTESIAN_POINT ( 'NONE',  ( 6.819227946136852125, -0.1326586024288610444, 1.840611662119538749 ) ) ;
#161773=CARTESIAN_POINT ( 'NONE',  ( 3.375360373764887179, -0.3420621250952958214, -1.699858368971490563 ) ) ;
#161775=CARTESIAN_POINT ( 'NONE',  ( 1.850524992189076290, -2.059912964915584954, -0.2069831422613493399 ) ) ;
#161777=CARTESIAN_POINT ( 'NONE',  ( 2.197004041102487371, 1.892657838527435299, 0.9490559450526787622 ) ) ;
#161781=CARTESIAN_POINT ( 'NONE',  ( 0.5671661303022774714, 1.710823773062917219, 0.9755123711343968163 ) ) ;
#161786=CARTESIAN_POINT ( 'NONE',  ( 2.344040366607359704, 2.291775683190785173, 0.05432913299479279201 ) ) ;
#161787=CARTESIAN_POINT ( 'NONE',  ( 0.4338677482375961070, 0.9413943332680120291, -1.564114433284753636 ) ) ;
#161788=CARTESIAN_POINT ( 'NONE',  ( 3.287273477832891366, 0.04233216220104508987, -1.912079899511004433 ) ) ;
#161791=CARTESIAN_POINT ( 'NONE',  ( 1.494390954318410625, -1.073482900754536784, 1.702939308294330489 ) ) ;
#161792=CARTESIAN_POINT ( 'NONE',  ( 1.586688997538304058, 1.889165970957426444, 0.5283831072378852856 ) ) ;
#161796=CARTESIAN_POINT ( 'NONE',  ( 4.980460981504991835, -0.2552229379441274815, -2.074931007936396288 ) ) ;
#161797=CARTESIAN_POINT ( 'NONE',  ( 3.467426238747231881, 1.726840169280913662, -0.3869839817904097701 ) ) ;
#161800=CARTESIAN_POINT ( 'NONE',  ( 0.1467655724766807612, -1.757430454515636509, 1.308964887167405111 ) ) ;
#161801=CARTESIAN_POINT ( 'NONE',  ( 4.101278252482940978, -1.735469017763660027, 0.1308211784099410635 ) ) ;
#161804=CARTESIAN_POINT ( 'NONE',  ( 4.815645707022956579, -1.391897370064384631, 1.033600972745553070 ) ) ;
#161805=CARTESIAN_POINT ( 'NONE',  ( 5.178266966923749770, -1.157238278732542369, -1.836894593069735793 ) ) ;
#161807=CARTESIAN_POINT ( 'NONE',  ( 5.999232488047272049, -0.2420365156972601739, 2.001857322483958423 ) ) ;
#161808=CARTESIAN_POINT ( 'NONE',  ( 5.781250000000004441, 0.7852924748302878566, 1.895863743163952453 ) ) ;
#161811=CARTESIAN_POINT ( 'NONE',  ( 3.399358865922623263, 1.517880436307640579, 1.186064745714454638 ) ) ;
#161813=CARTESIAN_POINT ( 'NONE',  ( -0.004779673669230537214, -2.156333359934967220, -0.5329991086745686779 ) ) ;
#161815=CARTESIAN_POINT ( 'NONE',  ( 6.983263157960371892, 7.629137130509070275, 2.546189081643289942 ) ) ;
#161819=CARTESIAN_POINT ( 'NONE',  ( 2.561440534034305827, -1.845267710029829145, 1.236318238231758571 ) ) ;
#161820=CARTESIAN_POINT ( 'NONE',  ( 6.443807124430430910, 1.351966286592180211, 1.421895456074427688 ) ) ;
#161829=CARTESIAN_POINT ( 'NONE',  ( 5.635237469726069648, -0.04712981909091130961, -2.062292871413499373 ) ) ;
#161833=CARTESIAN_POINT ( 'NONE',  ( 0.6316679966703161453, 0.9168908782757211329, -1.513568585016269452 ) ) ;
#161834=CARTESIAN_POINT ( 'NONE',  ( 6.346334349054894908, 0.2861236430486256421, -1.710204530248355059 ) ) ;
#161835=CARTESIAN_POINT ( 'NONE',  ( 5.267066465580821699, 1.675244640197434798, -0.4716337365339871579 ) ) ;
#161837=CARTESIAN_POINT ( 'NONE',  ( 3.281108521976669135, 2.071599159226782838, -0.9818635949487266590 ) ) ;
#161839=CARTESIAN_POINT ( 'NONE',  ( 0.7437973067255730930, 0.5320827018340993364, 1.762565881533173950 ) ) ;
#161842=CARTESIAN_POINT ( 'NONE',  ( 2.203868028057700990, -1.825262823911228072, 0.04193083753635528516 ) ) ;
#161843=CARTESIAN_POINT ( 'NONE',  ( 2.953750172290268150, -1.864168560446223033, -0.7691209412190866956 ) ) ;
#161844=CARTESIAN_POINT ( 'NONE',  ( 0.6740948890744530297, -1.214310170130480593, 1.824057261183717582 ) ) ;
#161846=CARTESIAN_POINT ( 'NONE',  ( 4.577239374156605756, 0.002566705667105330900, -2.106147099847696325 ) ) ;
#161849=CARTESIAN_POINT ( 'NONE',  ( 1.082579992370054311, 1.234693400583252609, -1.661741702728709802 ) ) ;
#161852=CARTESIAN_POINT ( 'NONE',  ( 4.916704032076687270, -0.7149955815140829340, -1.996424279390257572 ) ) ;
#161853=CARTESIAN_POINT ( 'NONE',  ( 0.1879448220486016896, -0.9096115147686645308, 1.698232400582524670 ) ) ;
#161854=ORIENTED_EDGE ( 'NONE', *, *, #185415, .F. ) ;
#161860=CARTESIAN_POINT ( 'NONE',  ( 6.258074605086497932, 0.8102346573028992305, -1.959903593942226685 ) ) ;
#161861=CARTESIAN_POINT ( 'NONE',  ( 1.641775563537830829, -1.524941811188656127, -1.452692102197229884 ) ) ;
#161864=CARTESIAN_POINT ( 'NONE',  ( 5.225394145299861570, 0.1845887361094991075, -1.851793659149820082 ) ) ;
#161872=CARTESIAN_POINT ( 'NONE',  ( 1.996468121258226924, 1.940055844723225009, 0.2909814450420752929 ) ) ;
#161873=CARTESIAN_POINT ( 'NONE',  ( 0.9190830904215805397, 1.997680973563022544, 0.8264451868333838602 ) ) ;
#161874=CARTESIAN_POINT ( 'NONE',  ( 3.292204118033771110, -0.8216723425069611952, -1.841733987974409237 ) ) ;
#161878=CARTESIAN_POINT ( 'NONE',  ( 3.374086008222790589, -0.3405263371191130095, 1.699849027820112823 ) ) ;
#161879=CARTESIAN_POINT ( 'NONE',  ( 2.237881400472482962, 0.3803048411740033719, 1.698081864755231374 ) ) ;
#161882=CARTESIAN_POINT ( 'NONE',  ( 3.093097461593071973, 1.769307450888421673, -1.056303779743078985 ) ) ;
#161883=CARTESIAN_POINT ( 'NONE',  ( 1.159529582462547781, -0.4871260124716703110, -1.956262300040665814 ) ) ;
#161884=CARTESIAN_POINT ( 'NONE',  ( 6.925078400183550364, -0.007619068086212391067, 2.144148427808051594 ) ) ;
#161886=CARTESIAN_POINT ( 'NONE',  ( 1.463681139585114588, 1.942636298559533792, -0.3350429378523085977 ) ) ;
#161888=CARTESIAN_POINT ( 'NONE',  ( 6.205323455156911194, 1.660478276859885582, -0.9486371710855368011 ) ) ;
#161893=CARTESIAN_POINT ( 'NONE',  ( 1.524088222275731486, -2.004166515738073695, 0.2493262195080257204 ) ) ;
#161895=CARTESIAN_POINT ( 'NONE',  ( 4.401628477801726724, 1.850755835686506590, 1.378093606121533199 ) ) ;
#161896=CARTESIAN_POINT ( 'NONE',  ( 6.443807124430430910, 1.351966286592180211, 1.421895456074427688 ) ) ;
#161897=CARTESIAN_POINT ( 'NONE',  ( 2.272246806564695021, -0.9202570425024100276, -1.732484491337261456 ) ) ;
#161899=CARTESIAN_POINT ( 'NONE',  ( 0.03578008775950020093, -1.617816776142148250, 1.203357013023528932 ) ) ;
#161901=CARTESIAN_POINT ( 'NONE',  ( 1.358780451569325365, -2.012465911620679115, -0.6584304486853159721 ) ) ;
#161904=CARTESIAN_POINT ( 'NONE',  ( 1.446930991382020748, 0.5358794165791405106, -1.761430032344503349 ) ) ;
#161906=CARTESIAN_POINT ( 'NONE',  ( 4.241221290925122567, -0.2070989531138747453, -2.161143177887809852 ) ) ;
#161908=CARTESIAN_POINT ( 'NONE',  ( 3.322626870553476941, -0.8629183168706102691, -1.937285153019531414 ) ) ;
#161912=CARTESIAN_POINT ( 'NONE',  ( 3.585278813505449858, 1.864625933638365485, -0.8777486340088790362 ) ) ;
#161914=CARTESIAN_POINT ( 'NONE',  ( 0.2922019606856861018, 1.531309713818730822, -1.022077305420886040 ) ) ;
#161918=CARTESIAN_POINT ( 'NONE',  ( 0.2236267563471248943, -0.1037379595543522215, 2.204571545119632603 ) ) ;
#161919=CARTESIAN_POINT ( 'NONE',  ( 2.319920442056855325, -2.194974118250800021, 0.5478587534586392138 ) ) ;
#161921=CARTESIAN_POINT ( 'NONE',  ( 2.566445574732978407, 0.6140501124722294035, 1.704450811836472734 ) ) ;
#161922=CARTESIAN_POINT ( 'NONE',  ( 2.026450851813020648, 0.4238854151232730461, 1.868046764376835922 ) ) ;
#161924=CARTESIAN_POINT ( 'NONE',  ( 3.631357695093720750, 0.05367941694835526995, -2.069842578854002468 ) ) ;
#161926=CARTESIAN_POINT ( 'NONE',  ( 1.692193703850993103, -1.961769708113933808, -0.1953840112930530781 ) ) ;
#161927=CARTESIAN_POINT ( 'NONE',  ( 6.147092719882727430, -1.626042154682215468, 1.032876571686857536 ) ) ;
#161928=CARTESIAN_POINT ( 'NONE',  ( 3.063207453921251489, 0.2760179531714930246, -1.850060308400132358 ) ) ;
#161929=CARTESIAN_POINT ( 'NONE',  ( 1.489377799468382113, -0.3424701664414407931, -2.282033458877083199 ) ) ;
#161931=CARTESIAN_POINT ( 'NONE',  ( 2.453354322281832811, 1.436274109216955752, 1.183453651933939588 ) ) ;
#161933=CARTESIAN_POINT ( 'NONE',  ( 5.213357787468869020, -1.740689653174596563, -1.106377904087485486 ) ) ;
#161937=CARTESIAN_POINT ( 'NONE',  ( 5.877981411467888329, 1.251756350581848309, 1.693418440539447234 ) ) ;
#161939=CARTESIAN_POINT ( 'NONE',  ( 5.887991582945823588, -0.9777203880148609416, 1.927937229880334113 ) ) ;
#161941=CARTESIAN_POINT ( 'NONE',  ( 6.129558478109055741, -0.2449627755865962375, 2.004677898944156489 ) ) ;
#161948=CARTESIAN_POINT ( 'NONE',  ( 4.522672878804367969, 0.3494810548456111499, 1.985869246038343583 ) ) ;
#161953=CARTESIAN_POINT ( 'NONE',  ( 6.420800710400103917, 2.015122584031241004, 0.7829223626853940576 ) ) ;
#161958=CARTESIAN_POINT ( 'NONE',  ( 0.3861688966736884776, -0.6463253627202453222, -1.803393044390422029 ) ) ;
#161960=CARTESIAN_POINT ( 'NONE',  ( 1.453258822912409043, 0.5037300415833938505, -1.649688963556243282 ) ) ;
#161965=CARTESIAN_POINT ( 'NONE',  ( 6.766881895623299670, -1.710433013466134744, -0.7576501205904457859 ) ) ;
#161966=CARTESIAN_POINT ( 'NONE',  ( 0.5748582965167781111, -1.456639466575420538, 1.389732462146851200 ) ) ;
#161968=CARTESIAN_POINT ( 'NONE',  ( 3.364504783244476993, 0.9904720576699842516, 1.972067388187691339 ) ) ;
#161970=CARTESIAN_POINT ( 'NONE',  ( 5.770445249457275771, -0.9694031614774318850, -1.942678356158732855 ) ) ;
#161974=CARTESIAN_POINT ( 'NONE',  ( 3.264422710156249963, 2.120667954687505574, -0.001943060928578931989 ) ) ;
#161975=CARTESIAN_POINT ( 'NONE',  ( 2.337517745082304810, 0.5350678814987767096, -1.944078148028174136 ) ) ;
#161976=CARTESIAN_POINT ( 'NONE',  ( 1.775370306292364031, 0.3070917902865456517, -1.785173024263370101 ) ) ;
#161982=CARTESIAN_POINT ( 'NONE',  ( 0.9189787140968961321, -1.730522700298501304, 0.8221016984403562988 ) ) ;
#161990=CARTESIAN_POINT ( 'NONE',  ( 5.770447993230207295, -1.374857387916775364, 1.668144713590607120 ) ) ;
#161993=CARTESIAN_POINT ( 'NONE',  ( 2.531617689938488791, -0.2033970545941807817, 2.110794199748195599 ) ) ;
#161994=CARTESIAN_POINT ( 'NONE',  ( -0.02988540731099428513, 6.948706544289728448, -2.321349141872154132 ) ) ;
#161996=CARTESIAN_POINT ( 'NONE',  ( 3.760970446608974171, -1.736958583363076736, -0.9323722252271587907 ) ) ;
#161997=CARTESIAN_POINT ( 'NONE',  ( 5.238497809344139000, 1.134185964801931679, -1.539638564045166857 ) ) ;
#162000=CARTESIAN_POINT ( 'NONE',  ( 0.3970419974134197783, 0.3524218036512065111, 2.039982198586967943 ) ) ;
#162001=CARTESIAN_POINT ( 'NONE',  ( 2.853385946047338084, 1.932536089888321040, -0.1910151464093560736 ) ) ;
#162006=CARTESIAN_POINT ( 'NONE',  ( 2.115285117227220901, -2.027561382914280674, 0.5091250600777631474 ) ) ;
#162009=CARTESIAN_POINT ( 'NONE',  ( -0.02317427319796245069, -1.617030479356797334, -0.8165419217573687272 ) ) ;
#162011=CARTESIAN_POINT ( 'NONE',  ( 3.932405576212230525, 1.181341412803040614, -1.863887651898883613 ) ) ;
#162012=CARTESIAN_POINT ( 'NONE',  ( 3.065657736429776570, 0.3252250816505456998, -2.182562984848686938 ) ) ;
#162015=CARTESIAN_POINT ( 'NONE',  ( 1.348149404638066873, 0.9416913409402676294, -1.664245089135652389 ) ) ;
#162017=CARTESIAN_POINT ( 'NONE',  ( 4.176279081494421952, -1.061646348645030713, -1.777293304589353085 ) ) ;
#162019=CARTESIAN_POINT ( 'NONE',  ( 3.028364643526501698, 1.202066397148596977, -1.796461956351296019 ) ) ;
#162020=CARTESIAN_POINT ( 'NONE',  ( 4.950807510372833065, -1.851323926424643274, -1.172527737679923465 ) ) ;
#162027=CARTESIAN_POINT ( 'NONE',  ( 0.6861729220449981348, 1.650083401500940239, 1.158686392676591570 ) ) ;
#162029=CARTESIAN_POINT ( 'NONE',  ( 4.996967907133109676, 0.3485794866864948549, 2.040532872733556768 ) ) ;
#162030=CARTESIAN_POINT ( 'NONE',  ( 3.510301166856438115, -0.7815644168660453861, -1.761018089871415393 ) ) ;
#162031=CARTESIAN_POINT ( 'NONE',  ( 5.554358401905552967, -1.342484540487314026, 1.637217851860258699 ) ) ;
#162034=CARTESIAN_POINT ( 'NONE',  ( 4.258625426654465862, -0.6138343748593175775, -1.871441549783653180 ) ) ;
#162035=CARTESIAN_POINT ( 'NONE',  ( 6.369073578265099123, 2.195482680428318290, -0.6590174882785122534 ) ) ;
#162036=CARTESIAN_POINT ( 'NONE',  ( 3.738726038629454074, 0.2694068579384527595, 1.805578518607708016 ) ) ;
#162043=CARTESIAN_POINT ( 'NONE',  ( 1.417261839328866513, -1.023339270300478221, -1.530466495063505628 ) ) ;
#162044=CARTESIAN_POINT ( 'NONE',  ( 5.396744779746093457, -1.965104602953187563, -0.4368240711251635822 ) ) ;
#162045=CARTESIAN_POINT ( 'NONE',  ( 5.854147224351119227, 0.1731004610599009841, -2.292201554650086237 ) ) ;
#162046=CARTESIAN_POINT ( 'NONE',  ( 5.612146373276853950, 1.959670608579218376, -0.09257137562097839112 ) ) ;
#162051=CARTESIAN_POINT ( 'NONE',  ( 1.523107970189445215, -1.967458627398379623, 0.7076814851830464104 ) ) ;
#162052=CARTESIAN_POINT ( 'NONE',  ( 6.315310819269446263, -0.2119676446582714757, 1.757049200028695690 ) ) ;
#162054=CARTESIAN_POINT ( 'NONE',  ( -0.1106727585416201337, 1.364743060583981649, -2.259751816641343058 ) ) ;
#162055=CARTESIAN_POINT ( 'NONE',  ( 0.7842107965865081631, 1.535900883440274090, -0.8186502264825399333 ) ) ;
#162060=CARTESIAN_POINT ( 'NONE',  ( 1.664246808422519486, -1.221613929703774915, 1.218001262086549907 ) ) ;
#162061=CARTESIAN_POINT ( 'NONE',  ( 1.962683346935737205, -2.005255389829229351, -0.8846387633431598285 ) ) ;
#162062=CARTESIAN_POINT ( 'NONE',  ( 4.617920694193921705, -2.164688156338661962, 0.4286357439418769788 ) ) ;
#162064=CARTESIAN_POINT ( 'NONE',  ( 1.639757756142570244, 2.007014814066264474, -0.8283606533975582664 ) ) ;
#162065=CARTESIAN_POINT ( 'NONE',  ( 0.5041868517345666767, -0.6120625888205477594, -1.720162557568189809 ) ) ;
#162066=CARTESIAN_POINT ( 'NONE',  ( 3.819616621146375568, -1.462967937902563964, -1.530840818714680029 ) ) ;
#162070=CARTESIAN_POINT ( 'NONE',  ( 3.158078472442786833, 1.032628797542353816, 2.046708512074166819 ) ) ;
#162073=CARTESIAN_POINT ( 'NONE',  ( 5.602238577124374785, -1.000643217919431116, 1.983199510308247815 ) ) ;
#162080=CARTESIAN_POINT ( 'NONE',  ( 3.744767666119628746, 2.000857235306313875, -0.2496062519145719194 ) ) ;
#162082=CARTESIAN_POINT ( 'NONE',  ( 2.606363979242664719, 2.062007909489747881, 0.05513178878350195877 ) ) ;
#162088=CARTESIAN_POINT ( 'NONE',  ( 5.472676780243426187, -0.05103125619924236966, -2.191024458042860168 ) ) ;
#162089=CARTESIAN_POINT ( 'NONE',  ( 2.901017702322743919, -0.9963018188003970321, -1.753030416019534021 ) ) ;
#162090=CARTESIAN_POINT ( 'NONE',  ( 1.663359199420410883, 0.9473472845980964729, 1.578708189602283873 ) ) ;
#162094=CARTESIAN_POINT ( 'NONE',  ( 5.807590115592688562, -0.4411735188285180187, 1.771332044933016547 ) ) ;
#162095=CARTESIAN_POINT ( 'NONE',  ( 5.713517581197447015, 1.944070655204039433, 0.5350908816983344085 ) ) ;
#162097=CARTESIAN_POINT ( 'NONE',  ( 5.331070463540595661, 0.1608317336210095816, 2.256856606938316023 ) ) ;
#162099=CARTESIAN_POINT ( 'NONE',  ( 0.9968619785027620361, -0.5136065205212798634, -2.042351051948914531 ) ) ;
#162104=MANIFOLD_SOLID_BREP ( 'Sweep1[12]', #1556 ) ;
#162109=CARTESIAN_POINT ( 'NONE',  ( 2.531719857061366152, -0.2131849592692437734, 2.211133432850121761 ) ) ;
#162113=CARTESIAN_POINT ( 'NONE',  ( 3.262109210011232108, -1.959739898415867154, 0.09363895518171151677 ) ) ;
#162120=CARTESIAN_POINT ( 'NONE',  ( 2.039458538997685366, 0.004855507148140979744, 2.120778211687989856 ) ) ;
#162122=CARTESIAN_POINT ( 'NONE',  ( 4.487301133948972343, 1.932317252032596633, -0.9692046190768679459 ) ) ;
#162123=CARTESIAN_POINT ( 'NONE',  ( 3.175182228840720544, 1.170341537027960843, 1.421418621496411294 ) ) ;
#162127=CARTESIAN_POINT ( 'NONE',  ( 5.525286087770139964, -1.108758243214434724, -1.341423578285575235 ) ) ;
#162131=CARTESIAN_POINT ( 'NONE',  ( 2.993221558690632556, 1.854768100113469265, -1.110066390340218367 ) ) ;
#162132=CARTESIAN_POINT ( 'NONE',  ( 4.218124927476913477, -1.674631575811252215, -1.122325875776951420 ) ) ;
#162135=CARTESIAN_POINT ( 'NONE',  ( 2.395597313961893349, 1.670541196947441520, 1.371929806955954012 ) ) ;
#162136=CARTESIAN_POINT ( 'NONE',  ( 2.759003776822867238, -1.713332664616385781, -0.9749793123631170788 ) ) ;
#162138=CARTESIAN_POINT ( 'NONE',  ( 6.509000000000013664, 7.052434016701248254, 2.698154332336550887 ) ) ;
#162139=CARTESIAN_POINT ( 'NONE',  ( 4.810071659083087425, 1.336522264689719686, -1.409242981738271894 ) ) ;
#162149=CARTESIAN_POINT ( 'NONE',  ( 0.9739772326014315418, 2.126351460888118883, -0.5901193814053447007 ) ) ;
#162151=CARTESIAN_POINT ( 'NONE',  ( 5.067221110791254368, 1.704927679941736329, 0.9703409489375602881 ) ) ;
#162156=CARTESIAN_POINT ( 'NONE',  ( 4.576008823784957436, -1.786506429242448624, -0.4446734633927542091 ) ) ;
#162161=CARTESIAN_POINT ( 'NONE',  ( 6.152600690169603759, 2.097733681304454034, 0.3095894981632040244 ) ) ;
#162164=CARTESIAN_POINT ( 'NONE',  ( 6.661407821810922947, 0.3568556019579691707, -2.029490769664368255 ) ) ;
#162167=CARTESIAN_POINT ( 'NONE',  ( 1.785388869275974955, -1.753811856250932610, 0.6230531623785877660 ) ) ;
#162168=CARTESIAN_POINT ( 'NONE',  ( 3.298233973420101606, 1.449563003725433896, -1.135193286699177628 ) ) ;
#162173=CARTESIAN_POINT ( 'NONE',  ( 2.842613246588860942, 2.190307313262893185, 0.2694104812042824038 ) ) ;
#162174=CARTESIAN_POINT ( 'NONE',  ( 5.800151253372650473, -2.262578822528161560, -0.008439264561578212892 ) ) ;
#162176=CARTESIAN_POINT ( 'NONE',  ( 6.258062559271784231, 0.6844122130202813237, -1.677549884021255933 ) ) ;
#162177=CARTESIAN_POINT ( 'NONE',  ( 5.542171544414384421, 0.7827158775690710169, 1.748735243013665785 ) ) ;
#162179=CARTESIAN_POINT ( 'NONE',  ( 6.157094445334826638, -1.605393284960114242, -0.9600186418455139981 ) ) ;
#162181=CARTESIAN_POINT ( 'NONE',  ( 5.916418678859147740, 0.7547467877644217227, 1.701316312257817875 ) ) ;
#162183=CARTESIAN_POINT ( 'NONE',  ( 5.998865924308096176, 1.444533723251522073, -1.022291996631684574 ) ) ;
#162184=CARTESIAN_POINT ( 'NONE',  ( 0.9191581010105540628, -1.820984308097562954, 0.8666112775468015617 ) ) ;
#162186=CARTESIAN_POINT ( 'NONE',  ( 2.895255201988570892, 1.806112693971681615, -1.083030686944158161 ) ) ;
#162191=CARTESIAN_POINT ( 'NONE',  ( 3.322525440707891242, -0.8223705904544276191, -1.844992516297422780 ) ) ;
#162194=CARTESIAN_POINT ( 'NONE',  ( 3.585389192675687564, 1.955840111083558597, -0.9206723451176119788 ) ) ;
#162199=CARTESIAN_POINT ( 'NONE',  ( 1.082764339582122481, 1.293380948865870073, -1.743738868014677035 ) ) ;
#162203=CARTESIAN_POINT ( 'NONE',  ( 2.085717061910817183, -0.9337068281064246911, 1.982830571388309204 ) ) ;
#162205=CARTESIAN_POINT ( 'NONE',  ( 3.081239027650189310, -0.1650901621712965450, -2.256537306257479614 ) ) ;
#162214=CARTESIAN_POINT ( 'NONE',  ( 3.321328847770131709, -1.706417891748934546, 0.4689366942724793041 ) ) ;
#162216=CARTESIAN_POINT ( 'NONE',  ( 5.930760676324511316, 2.125237774816424619, 0.5940772278362898007 ) ) ;
#162220=CARTESIAN_POINT ( 'NONE',  ( 5.782827418265350516, 1.646828846085298448, -1.163285542026312847 ) ) ;
#162223=CARTESIAN_POINT ( 'NONE',  ( 3.449935675575486638, 1.870836310073907827, 0.001118452434160921221 ) ) ;
#162224=CARTESIAN_POINT ( 'NONE',  ( 3.379797469122407083, -1.996479967689598789, 0.5476083754193948883 ) ) ;
#162230=CARTESIAN_POINT ( 'NONE',  ( 3.244534624505683418, -1.932379277470747558, -0.3379807920969243873 ) ) ;
#162231=CARTESIAN_POINT ( 'NONE',  ( 1.458361007166041112, 1.524808354686446599, 1.319028796778199508 ) ) ;
#162235=CARTESIAN_POINT ( 'NONE',  ( 0.5263522483448194178, 1.788089326329355577, 0.5492086291003297482 ) ) ;
#162237=CARTESIAN_POINT ( 'NONE',  ( 2.215092046557234795, 1.614471179978003823, -1.202476892717120105 ) ) ;
#162239=CARTESIAN_POINT ( 'NONE',  ( 2.759486767256282391, 2.009531813720342175, -0.6668115938158604150 ) ) ;
#162241=CARTESIAN_POINT ( 'NONE',  ( 3.771986465066007099, -2.040223509676724500, 0.3510349978646867264 ) ) ;
#162243=CARTESIAN_POINT ( 'NONE',  ( 6.333939708931282553, 2.067699390258682879, 0.3079354192142729763 ) ) ;
#162244=CARTESIAN_POINT ( 'NONE',  ( 4.401258566127845384, 1.466438172381477445, 1.087111955044787859 ) ) ;
#162251=CARTESIAN_POINT ( 'NONE',  ( 5.654919265238161685, 0.3773621422162172223, 1.874504418562010999 ) ) ;
#162258=CARTESIAN_POINT ( 'NONE',  ( 0.8547319020580852467, 0.3593373433725781108, -1.805665335529122784 ) ) ;
#162259=EDGE_LOOP ( 'NONE', ( #111595, #135538, #166785, #24799 ) ) ;
#162262=CARTESIAN_POINT ( 'NONE',  ( 4.270664716992385479, -1.744513905240049567, -0.6754176267826096369 ) ) ;
#162263=CARTESIAN_POINT ( 'NONE',  ( -0.02319159430947541692, 2.051704324979522820, -2.228571760951563618 ) ) ;
#162269=CARTESIAN_POINT ( 'NONE',  ( 0.8132587859420150611, -1.660809389245621492, -1.058212622827129357 ) ) ;
#162270=CARTESIAN_POINT ( 'NONE',  ( 2.495720449669075247, -1.994069261235394741, 0.2986488809556055446 ) ) ;
#162274=CARTESIAN_POINT ( 'NONE',  ( 2.466951935624495551, 0.1062163371072753354, -2.188993582743845590 ) ) ;
#162284=CARTESIAN_POINT ( 'NONE',  ( 5.284640796330934087, 1.621094592300664328, -0.8731043043393662550 ) ) ;
#162285=CARTESIAN_POINT ( 'NONE',  ( 2.086589530005359183, -1.236640506920426263, 1.588416314350507674 ) ) ;
#162286=CARTESIAN_POINT ( 'NONE',  ( 3.726148964702048705, -2.024938297411133625, -1.087335920097615594 ) ) ;
#162287=CARTESIAN_POINT ( 'NONE',  ( -0.02919842301645457147, -0.002306431287177941429, -2.073770398395402115 ) ) ;
#162288=CARTESIAN_POINT ( 'NONE',  ( 2.254548712976621516, -0.4907705908011159579, -1.795021142807408543 ) ) ;
#162291=CARTESIAN_POINT ( 'NONE',  ( 5.888906298306328502, -1.818048641159516476, -0.5935555146628914702 ) ) ;
#162294=CARTESIAN_POINT ( 'NONE',  ( 5.390208805286830440, -0.5092157624977285968, -2.027641083400610000 ) ) ;
#162295=CARTESIAN_POINT ( 'NONE',  ( 3.678450976403758066, -1.802590750232490491, -0.4997190347926713794 ) ) ;
#162298=CARTESIAN_POINT ( 'NONE',  ( 5.372543328820884589, -0.05112055865702340440, -1.840719716649619198 ) ) ;
#162302=CARTESIAN_POINT ( 'NONE',  ( 5.355954780876127863, 1.722648150766812103, -0.09025627888907016005 ) ) ;
#162304=CARTESIAN_POINT ( 'NONE',  ( 0.7208516900601771304, 1.708106959156988847, 0.2981761063507569198 ) ) ;
#162307=CARTESIAN_POINT ( 'NONE',  ( 4.645498245716852992, 1.942073188235559522, -0.9706016350095565404 ) ) ;
#162308=CARTESIAN_POINT ( 'NONE',  ( 3.351995281737112364, 1.825872481133209879, -0.0009662468829912954560 ) ) ;
#162309=CARTESIAN_POINT ( 'NONE',  ( 1.041763817972749750, 1.313373124611896703, 1.457441342770829262 ) ) ;
#162310=CARTESIAN_POINT ( 'NONE',  ( 0.5623061109219238407, -1.172325791230070857, 1.762859051686527012 ) ) ;
#162311=CARTESIAN_POINT ( 'NONE',  ( 0.1294186239076781653, -2.093018298938463140, 0.9351526010841960668 ) ) ;
#162315=CARTESIAN_POINT ( 'NONE',  ( 3.088655771522513582, -1.261447869382603004, 1.704333039148818507 ) ) ;
#162320=CARTESIAN_POINT ( 'NONE',  ( 0.3915760470782835845, -1.894197279051227811, 0.8358220917567968922 ) ) ;
#162321=CARTESIAN_POINT ( 'NONE',  ( 6.983263157960365675, -0.006178392973848687020, 2.053544886540019210 ) ) ;
#162323=CARTESIAN_POINT ( 'NONE',  ( 2.174768466102798836, 0.9529365794415098900, 2.006655600372597714 ) ) ;
#162325=CARTESIAN_POINT ( 'NONE',  ( 0.3000039258060793745, 1.578900123410318823, -1.670874907869798864 ) ) ;
#162327=CARTESIAN_POINT ( 'NONE',  ( 5.858276910504900847, -2.062741130177087268, -0.005609060510954055022 ) ) ;
#162331=CARTESIAN_POINT ( 'NONE',  ( 0.2331563151865486683, 2.034376611827843906, -2.362208330281903024 ) ) ;
#162332=CARTESIAN_POINT ( 'NONE',  ( 5.847170753249844033, 0.5281823367668266878, -1.763884204139199330 ) ) ;
#162335=ORIENTED_EDGE ( 'NONE', *, *, #32928, .F. ) ;
#162336=CARTESIAN_POINT ( 'NONE',  ( -0.2104748580754426390, 2.865278511227668634, -2.591885361450113834 ) ) ;
#162337=CARTESIAN_POINT ( 'NONE',  ( 1.922448523189672853, 1.607815062812420370, 0.6247884732281087095 ) ) ;
#162338=CARTESIAN_POINT ( 'NONE',  ( 1.639861632979456418, 2.010800986640928656, -0.1531718788195315928 ) ) ;
#162339=CARTESIAN_POINT ( 'NONE',  ( 1.846706770127172881, 0.3881029198684777803, -2.265567138619323018 ) ) ;
#162341=CARTESIAN_POINT ( 'NONE',  ( 2.073834635255236147, 2.165437736866062224, -0.6553434645707820749 ) ) ;
#162342=CARTESIAN_POINT ( 'NONE',  ( 4.442079272866404693, 0.9008978453017953969, -1.903793715863113523 ) ) ;
#162344=CARTESIAN_POINT ( 'NONE',  ( 3.057584390254026729, 1.761565543986362670, -0.1695560061622681525 ) ) ;
#162347=CARTESIAN_POINT ( 'NONE',  ( 4.845436733290686249, 0.7204735554154987343, -2.176297985750157427 ) ) ;
#162353=CARTESIAN_POINT ( 'NONE',  ( 4.488337453930180132, -0.4787454259813396229, -2.138356021698713416 ) ) ;
#162359=CARTESIAN_POINT ( 'NONE',  ( 3.527879399192564325, -1.148099800794393444, -1.546878348965428973 ) ) ;
#162362=CARTESIAN_POINT ( 'NONE',  ( 6.135037582782754129, 1.979230198018981701, 0.7618025574447004900 ) ) ;
#162367=CARTESIAN_POINT ( 'NONE',  ( 6.356982874815331641, 0.3076174260261410054, -1.815216213958574132 ) ) ;
#162371=CARTESIAN_POINT ( 'NONE',  ( 2.366429680491717313, 0.08383053003592833008, -1.738530308508005273 ) ) ;
#162377=CARTESIAN_POINT ( 'NONE',  ( 6.719591497160966931, -2.098179372288328182, 0.5198544864785522579 ) ) ;
#162380=CARTESIAN_POINT ( 'NONE',  ( 6.051685545382852638, 0.6321331830463626789, -2.067208725892249799 ) ) ;
#162384=CARTESIAN_POINT ( 'NONE',  ( 6.081318999601531772, 1.822420489394786625, -0.7521447986948930353 ) ) ;
#162385=CARTESIAN_POINT ( 'NONE',  ( 4.868316058674494684, -0.4618845756635507893, 1.671066720262862182 ) ) ;
#162388=CARTESIAN_POINT ( 'NONE',  ( 1.488088480104592826, -2.181432686776756391, -0.2102995727721947705 ) ) ;
#162389=CARTESIAN_POINT ( 'NONE',  ( 3.505163243484223479, 1.820685690116738531, -1.417681053453226703 ) ) ;
#162390=CARTESIAN_POINT ( 'NONE',  ( 5.606733736089553055, 1.563247385715782700, -1.342922781998987736 ) ) ;
#162391=CARTESIAN_POINT ( 'NONE',  ( 1.376788300709189450, 1.794419955772775355, -0.7429034522522351969 ) ) ;
#162396=CARTESIAN_POINT ( 'NONE',  ( 4.078469121099765005, 1.002472831208834680, 1.868716877859360137 ) ) ;
#162397=CARTESIAN_POINT ( 'NONE',  ( 2.865861461037176205, -0.1511401116795624278, -2.010826411938296143 ) ) ;
#162399=CARTESIAN_POINT ( 'NONE',  ( 4.383934217864794647, 1.438874268414831015, 1.673263306058408340 ) ) ;
#162408=CARTESIAN_POINT ( 'NONE',  ( 3.995036845513312951, 1.742007986889832161, -1.100897373992800299 ) ) ;
#162413=CARTESIAN_POINT ( 'NONE',  ( 3.457679895445249674, -1.530724978927421986, -1.317682070945853656 ) ) ;
#162418=CARTESIAN_POINT ( 'NONE',  ( 3.432544477427549534, 2.010279954523132240, 0.4531449079418439774 ) ) ;
#162419=CARTESIAN_POINT ( 'NONE',  ( 2.461564753630896440, -1.930417925741171103, -0.5826551686555283549 ) ) ;
#162423=CARTESIAN_POINT ( 'NONE',  ( 0.9547317490294878750, 0.3612830171869831353, -1.805165878648997690 ) ) ;
#162424=CARTESIAN_POINT ( 'NONE',  ( 6.322910218073367616, 2.057572540570989261, 0.7984293639632376038 ) ) ;
#162426=CARTESIAN_POINT ( 'NONE',  ( 2.618638089201937635, 1.414096770131420877, -1.634928933042498755 ) ) ;
#162428=CARTESIAN_POINT ( 'NONE',  ( 4.100857973768299303, 1.937344669444723166, 0.8546590867991187279 ) ) ;
#162429=CARTESIAN_POINT ( 'NONE',  ( 2.812212034788389214, -1.912053501320301718, 1.275153900055803646 ) ) ;
#162431=CARTESIAN_POINT ( 'NONE',  ( 1.129532124359374334, -1.183843481993757774, -1.448407549327054955 ) ) ;
#162432=CARTESIAN_POINT ( 'NONE',  ( 4.996930482532231821, 1.639556309048403770, -1.094490209086243171 ) ) ;
#162433=CARTESIAN_POINT ( 'NONE',  ( 4.698454014923811428, 1.387101836239763131, -1.463925544105355803 ) ) ;
#162437=CARTESIAN_POINT ( 'NONE',  ( 5.936178820057578243, 1.039279821879979693, -1.831694563109196316 ) ) ;
#162438=CARTESIAN_POINT ( 'NONE',  ( 6.619590326553026038, 0.3579758704960536719, -2.039031579972025554 ) ) ;
#162442=CARTESIAN_POINT ( 'NONE',  ( 4.680523324745738734, -1.912062325676016306, -0.4798145647967356764 ) ) ;
#162443=CARTESIAN_POINT ( 'NONE',  ( 5.941667304196568189, -1.900381328601069342, 0.6844855596733252501 ) ) ;
#162445=CARTESIAN_POINT ( 'NONE',  ( 4.565214137342485934, -2.059927483508086965, -1.040394749072820701 ) ) ;
#162446=CARTESIAN_POINT ( 'NONE',  ( 2.149356475496758456, 1.796580072245733462, -1.012980232677022974 ) ) ;
#162453=CARTESIAN_POINT ( 'NONE',  ( 4.510331875626576448, 2.170777084992558059, -0.04906379945510477847 ) ) ;
#162456=CARTESIAN_POINT ( 'NONE',  ( 2.753256032281672372, 1.832158412346639453, -0.1828795585285883096 ) ) ;
#162458=CARTESIAN_POINT ( 'NONE',  ( 6.620655732516647518, 0.01042156863438310939, 1.726407961933309920 ) ) ;
#162459=CARTESIAN_POINT ( 'NONE',  ( 5.108995794240286159, -0.3219066699026683631, 2.167653318578148358 ) ) ;
#162461=CARTESIAN_POINT ( 'NONE',  ( 5.506774338047922157, 1.717276559928378132, -1.473185486808053835 ) ) ;
#162468=CARTESIAN_POINT ( 'NONE',  ( 0.9886869571070689977, 1.563518247070281086, -0.8293041508813036033 ) ) ;
#162469=CARTESIAN_POINT ( 'NONE',  ( 4.529943747908701468, -1.973814829549960237, 0.3949202218342766080 ) ) ;
#162472=CARTESIAN_POINT ( 'NONE',  ( 3.575310672209235374, 0.05349853608750848588, -2.105455972502618955 ) ) ;
#162473=CARTESIAN_POINT ( 'NONE',  ( 2.548326723280808892, -1.319200400300493570, 1.389225609306585119 ) ) ;
#162475=CARTESIAN_POINT ( 'NONE',  ( 3.226963424687212090, -1.818787540941589009, -0.7562359814760648558 ) ) ;
#162476=CARTESIAN_POINT ( 'NONE',  ( 5.818619510638624703, -0.7308962487734929070, -1.883076464014792117 ) ) ;
#162477=CARTESIAN_POINT ( 'NONE',  ( 1.709613803025863188, -1.856884215550944850, 0.2259493607114013147 ) ) ;
#162478=CARTESIAN_POINT ( 'NONE',  ( 1.697631272820496307, -1.418720726069604865, -1.355276769646639901 ) ) ;
#162479=CARTESIAN_POINT ( 'NONE',  ( 3.826516835200497457, 1.638561065401537897, 0.5390252620694930830 ) ) ;
#162480=CARTESIAN_POINT ( 'NONE',  ( 1.336036003918249948, -1.064896177285217016, -1.588262137521757822 ) ) ;
#162482=CARTESIAN_POINT ( 'NONE',  ( 0.8564375766340023288, 2.204168734417511821, -0.1118928034387969561 ) ) ;
#162492=CARTESIAN_POINT ( 'NONE',  ( 1.434126425884488354, 1.231690216755284562, 1.664001042209894088 ) ) ;
#162497=CARTESIAN_POINT ( 'NONE',  ( 5.672555391165950311, 0.8593836824349295744, 1.938725756316476589 ) ) ;
#162502=CARTESIAN_POINT ( 'NONE',  ( 6.514115657861259123, 1.956686900881845714, -0.1430618042221123987 ) ) ;
#162504=CARTESIAN_POINT ( 'NONE',  ( 4.218124927476913477, -1.674631575811252215, -1.122325875776951420 ) ) ;
#162505=CARTESIAN_POINT ( 'NONE',  ( 3.696418550083080401, 1.350829783741511969, -1.358666786172907592 ) ) ;
#162507=CARTESIAN_POINT ( 'NONE',  ( 1.699035084177059174, 1.824418957995146195, 1.213967346723361596 ) ) ;
#162509=CARTESIAN_POINT ( 'NONE',  ( 4.781498422495529255, 0.1932255103699429266, -2.003883580701450562 ) ) ;
#162512=CARTESIAN_POINT ( 'NONE',  ( 6.064083512088704886, -1.132370213454384045, 1.788784107109566701 ) ) ;
#162513=CARTESIAN_POINT ( 'NONE',  ( 2.771125873548622831, 1.984386128312282116, -0.6585125772022564217 ) ) ;
#162515=CARTESIAN_POINT ( 'NONE',  ( 0.4633286609967076086, 1.707074611214503435, -0.2455724507211871910 ) ) ;
#162518=EDGE_CURVE ( 'NONE', #8341, #112905, #166819, .T. ) ;
#162526=CARTESIAN_POINT ( 'NONE',  ( 1.295247000857565167, 1.673883212702592660, -0.6929762496888560719 ) ) ;
#162531=CARTESIAN_POINT ( 'NONE',  ( 2.156637704053586901, 0.3978940469637832766, 1.767043172555267772 ) ) ;
#162532=CARTESIAN_POINT ( 'NONE',  ( 6.639320575229251453, 0.008029245381881154262, 1.796863947021019481 ) ) ;
#162538=CARTESIAN_POINT ( 'NONE',  ( 2.506119797010537997, 1.860588423725167306, 0.04906839929019050223 ) ) ;
#162540=CARTESIAN_POINT ( 'NONE',  ( 0.1049102937123137097, -0.09321989032292328503, 1.913444960606479395 ) ) ;
#162541=CARTESIAN_POINT ( 'NONE',  ( 0.1471128783409255958, -1.407412912164500263, -1.162481699956314785 ) ) ;
#162547=CARTESIAN_POINT ( 'NONE',  ( 4.258625426654465862, -0.6138343748593175775, -1.871441549783653180 ) ) ;
#162550=CARTESIAN_POINT ( 'NONE',  ( 6.580031370938625557, -2.148343778048496411, -0.4316624935760752790 ) ) ;
#162552=CARTESIAN_POINT ( 'NONE',  ( 5.508790920392054424, 1.458765576344657866, -1.258282468310659707 ) ) ;
#162555=CARTESIAN_POINT ( 'NONE',  ( 2.649284799151204073, -1.834272514977531632, 1.226802785254533346 ) ) ;
#162557=CARTESIAN_POINT ( 'NONE',  ( 0.07037084582631887575, 0.7337836260858082715, 1.766209603411242668 ) ) ;
#162560=CARTESIAN_POINT ( 'NONE',  ( 0.1331715793776600265, 0.003733371859311259821, -1.953671397793784070 ) ) ;
#162561=CARTESIAN_POINT ( 'NONE',  ( 1.804143404396211681, 1.437808690349717589, -1.305647666910898730 ) ) ;
#162562=CARTESIAN_POINT ( 'NONE',  ( 0.7376574009502723239, -1.897405874265755354, -0.6818954202830117550 ) ) ;
#162564=CARTESIAN_POINT ( 'NONE',  ( 4.944130858096120740, -0.8794851946119870423, 1.640036094180880477 ) ) ;
#162566=CARTESIAN_POINT ( 'NONE',  ( 6.509000000000037645, 7.629137130509070275, 2.600000000000001421 ) ) ;
#162569=CARTESIAN_POINT ( 'NONE',  ( 1.312353134292881141, 1.468346937154514364, -1.627112938194043235 ) ) ;
#162573=CARTESIAN_POINT ( 'NONE',  ( 2.033574986395149775, -1.191784744093337123, -1.383114941912518159 ) ) ;
#162577=CARTESIAN_POINT ( 'NONE',  ( 6.509000000000011887, 3.696273625755361447, 2.514342382328867753 ) ) ;
#162579=CARTESIAN_POINT ( 'NONE',  ( 6.305291373979138747, 1.520805759102667132, 1.009792402853857407 ) ) ;
#162580=CARTESIAN_POINT ( 'NONE',  ( 4.645332984504850771, 1.754159843842403976, -0.8783796436172899291 ) ) ;
#162583=CARTESIAN_POINT ( 'NONE',  ( 4.528971853086540378, -2.003544689622422936, 0.8885388601788182239 ) ) ;
#162585=CARTESIAN_POINT ( 'NONE',  ( 3.766520095694513959, -0.8345382577515870759, -1.894767260282135712 ) ) ;
#162589=CARTESIAN_POINT ( 'NONE',  ( 3.797728626882245884, 1.624942816722572125, -1.626123495085467496 ) ) ;
#162593=CARTESIAN_POINT ( 'NONE',  ( 6.620655732516631531, 2.063554893983750027, 2.233578047529918287 ) ) ;
#162595=CARTESIAN_POINT ( 'NONE',  ( 3.749888610702892144, 0.6998405808875374223, 1.811630882863373149 ) ) ;
#162599=CARTESIAN_POINT ( 'NONE',  ( 5.484596585704371918, -1.208295678440996390, 1.482354609825987435 ) ) ;
#162600=CARTESIAN_POINT ( 'NONE',  ( 5.016472913109910614, 1.187476848380929928, -1.251119849200056366 ) ) ;
#162601=CARTESIAN_POINT ( 'NONE',  ( 5.102750050473856547, 1.865045247124358818, 0.7672954931761332142 ) ) ;
#162602=CARTESIAN_POINT ( 'NONE',  ( 4.992985585870878928, -2.287786813913486039, 0.2239274308311194894 ) ) ;
#162604=CARTESIAN_POINT ( 'NONE',  ( 0.7157882511714327434, -0.3199875008889854766, 2.183444778895065941 ) ) ;
#162607=CARTESIAN_POINT ( 'NONE',  ( 6.169200886764430791, 0.1279487620423936933, -1.765195888111121159 ) ) ;
#162608=CARTESIAN_POINT ( 'NONE',  ( 4.553361389630797618, -1.314998166741452090, 1.528740011303417745 ) ) ;
#162610=CARTESIAN_POINT ( 'NONE',  ( 2.256202855815407915, 0.9821592622454662358, 2.071323110799852873 ) ) ;
#162611=CARTESIAN_POINT ( 'NONE',  ( 1.464397578914914400, 0.1305661322733233098, -1.735479185401978208 ) ) ;
#162613=CARTESIAN_POINT ( 'NONE',  ( 1.141452232654313059, -0.03515412242651934360, -1.733669386235114906 ) ) ;
#162617=CARTESIAN_POINT ( 'NONE',  ( 1.574930973106080545, 1.458645925580204006, -1.608354241196547685 ) ) ;
#162618=CARTESIAN_POINT ( 'NONE',  ( 2.764861550476094276, -0.1531697945360478985, -2.010801143277194392 ) ) ;
#162620=CARTESIAN_POINT ( 'NONE',  ( 6.041620323887018529, -1.397190737843529540, -1.326607404314980254 ) ) ;
#162622=CARTESIAN_POINT ( 'NONE',  ( 2.232967058637932656, 1.447036570497368446, -1.685575845266892747 ) ) ;
#162629=CARTESIAN_POINT ( 'NONE',  ( 5.688919983501732780, 1.323409507385058914, 1.130498143038612513 ) ) ;
#162630=CARTESIAN_POINT ( 'NONE',  ( 3.314850587115983238, -1.487306837207631016, 1.279512770686676904 ) ) ;
#162635=CARTESIAN_POINT ( 'NONE',  ( 4.341306091576823789, -1.971171287362062818, 1.110239852968941232 ) ) ;
#162636=CARTESIAN_POINT ( 'NONE',  ( 0.9946673667629982729, 2.031838985545178389, 0.3545390999590279368 ) ) ;
#162638=CARTESIAN_POINT ( 'NONE',  ( 2.096875702627752691, -0.6037365238656807742, -2.180425337281781673 ) ) ;
#162641=CARTESIAN_POINT ( 'NONE',  ( 3.479631686803522417, 1.184185218286455621, 1.448006030947253331 ) ) ;
#162642=CARTESIAN_POINT ( 'NONE',  ( 2.918323747256291956, -1.167012588333454781, -1.282868673017246941 ) ) ;
#162644=CARTESIAN_POINT ( 'NONE',  ( 5.987848539424092564, -2.180829346447300310, -0.2163489798085171945 ) ) ;
#162645=CARTESIAN_POINT ( 'NONE',  ( 6.616287922300326585, -1.079552588663035051, -2.039509185488725951 ) ) ;
#162646=CARTESIAN_POINT ( 'NONE',  ( 3.784175263432405956, -1.067420458145739826, 1.879713924940962677 ) ) ;
#162647=CARTESIAN_POINT ( 'NONE',  ( 4.628815217244971691, -1.774851831708891714, 0.7884768782448601243 ) ) ;
#162649=CARTESIAN_POINT ( 'NONE',  ( 6.766881895623299670, -1.710433013466134744, -0.7576501205904457859 ) ) ;
#162650=( NAMED_UNIT ( * ) SI_UNIT ( $, .STERADIAN. ) SOLID_ANGLE_UNIT ( ) );
#162656=CARTESIAN_POINT ( 'NONE',  ( 5.678361341766085424, 1.528739221709461082, 1.314999087022615587 ) ) ;
#162662=CARTESIAN_POINT ( 'NONE',  ( 2.965264444195826243, 0.2674972279559268973, -1.805858685475017378 ) ) ;
#162669=CARTESIAN_POINT ( 'NONE',  ( 6.498695841808301843, -1.981098178724240322, -0.3918999010058578092 ) ) ;
#162670=CARTESIAN_POINT ( 'NONE',  ( 1.383610671357866639, 0.1525377206293351273, -2.115047022047947589 ) ) ;
#162673=CARTESIAN_POINT ( 'NONE',  ( 2.201794467188260995, 0.7177229581568910222, -1.717183780122087056 ) ) ;
#162675=CARTESIAN_POINT ( 'NONE',  ( 6.684453628662900826, -2.020573120193806638, -0.4047117086388977714 ) ) ;
#162676=CARTESIAN_POINT ( 'NONE',  ( 6.205703963786828758, 1.882472927010571118, 0.7231429968634556227 ) ) ;
#162682=CARTESIAN_POINT ( 'NONE',  ( 0.07680821025394034274, 2.052785608010514018, -2.228496998325917744 ) ) ;
#162684=CARTESIAN_POINT ( 'NONE',  ( 6.257185446134499784, -2.006139278912861368, -0.2004013049526700285 ) ) ;
#162685=CARTESIAN_POINT ( 'NONE',  ( 4.558453444723221892, -1.645810703501834560, -0.8254300276653583346 ) ) ;
#162687=CARTESIAN_POINT ( 'NONE',  ( 3.844573663522454332, 2.296428955072826295, 0.2277027427845106922 ) ) ;
#162689=CARTESIAN_POINT ( 'NONE',  ( 5.431013727915853906, 0.1530101862373678123, 2.156222312673663488 ) ) ;
#162691=CARTESIAN_POINT ( 'NONE',  ( 1.347104335016526599, 0.5619601930287048130, -1.858996895088180556 ) ) ;
#162695=COLOUR_RGB ( '', 0.08235294, 0.09019608, 0.10196078) ;
#162696=CARTESIAN_POINT ( 'NONE',  ( 5.114793989753786185, 0.7273159113986256141, -2.180329384352611033 ) ) ;
#162699=CARTESIAN_POINT ( 'NONE',  ( 4.768341783539651324, -1.221614081569386334, 1.416756073533788518 ) ) ;
#162700=CARTESIAN_POINT ( 'NONE',  ( 1.300873410958070409, -0.2835801433653042380, -1.891145142470892715 ) ) ;
#162703=CARTESIAN_POINT ( 'NONE',  ( 2.895379187063460424, 1.892502543702856865, -1.135010264495312837 ) ) ;
#162704=CARTESIAN_POINT ( 'NONE',  ( 6.883263157960373135, 2.058310207169287143, 2.252834201749584153 ) ) ;
#162709=CARTESIAN_POINT ( 'NONE',  ( 1.335163258876404857, -1.783904897583366012, 0.8392522581757311251 ) ) ;
#162710=CARTESIAN_POINT ( 'NONE',  ( 0.7457024085506950284, -1.977219658456253359, 1.189539768987533330 ) ) ;
#162711=CARTESIAN_POINT ( 'NONE',  ( 2.734756269166933151, -1.876540383875524576, -0.5722209215143353456 ) ) ;
#162712=CARTESIAN_POINT ( 'NONE',  ( 5.120015017920454881, 2.040880116263335431, -0.2974388374509198685 ) ) ;
#162719=CARTESIAN_POINT ( 'NONE',  ( 1.446384731406271218, -0.9785283779201507937, 1.938150590114567473 ) ) ;
#162725=CARTESIAN_POINT ( 'NONE',  ( 2.213927045526514537, -0.8776910013945339317, -1.651823421649289081 ) ) ;
#162726=CARTESIAN_POINT ( 'NONE',  ( 6.292270065666691892, -2.150519007954437622, -0.2187886337903441336 ) ) ;
#162729=CARTESIAN_POINT ( 'NONE',  ( 6.727182134110193168, 4.701113012587437190, 2.373661997258198486 ) ) ;
#162731=CARTESIAN_POINT ( 'NONE',  ( 2.174333686202088334, 0.8191313854410250395, 1.728107290330855639 ) ) ;
#162732=CARTESIAN_POINT ( 'NONE',  ( 3.713518252986651724, -1.743675808792734205, 0.3021571867034832382 ) ) ;
#162733=CARTESIAN_POINT ( 'NONE',  ( 2.121601645288184290, -0.4173985973947492711, 1.866012167355892704 ) ) ;
#162736=CARTESIAN_POINT ( 'NONE',  ( 5.607027416250175200, -0.04201266709560196738, 1.915314589656505362 ) ) ;
#162737=CARTESIAN_POINT ( 'NONE',  ( 6.707475516188797116, -1.580950341439198992, -1.174378316608926331 ) ) ;
#162739=CARTESIAN_POINT ( 'NONE',  ( 2.601940685209406467, 1.502730264585940168, 1.496503045097858919 ) ) ;
#162741=CARTESIAN_POINT ( 'NONE',  ( 4.803500792215161574, -0.4985019455652460740, 1.802925825644098534 ) ) ;
#162742=CARTESIAN_POINT ( 'NONE',  ( 0.7854531640391904102, 1.224056292049885419, 1.354719642434290439 ) ) ;
#162744=CARTESIAN_POINT ( 'NONE',  ( 4.160898416275903067, -1.636102012888400292, 1.481223685352812680 ) ) ;
#162747=CARTESIAN_POINT ( 'NONE',  ( 2.172402883950707686, -0.9704110660942105726, -1.820128386451558500 ) ) ;
#162757=CARTESIAN_POINT ( 'NONE',  ( 4.545415791725802457, 1.850806902094417783, -0.9279678557222792445 ) ) ;
#162759=CARTESIAN_POINT ( 'NONE',  ( 2.899875653925917174, -0.6810940995312758650, 2.051530325002319799 ) ) ;
#162761=CARTESIAN_POINT ( 'NONE',  ( 1.805337931753002501, 1.756199045189226204, -0.9973023101699033388 ) ) ;
#162763=CARTESIAN_POINT ( 'NONE',  ( 0.07479286986305369589, 0.2526433113205875935, -1.890777245541554574 ) ) ;
#162766=CARTESIAN_POINT ( 'NONE',  ( -0.1531117392989979065, -1.803405091603600185, -0.9023890051431044945 ) ) ;
#162767=CARTESIAN_POINT ( 'NONE',  ( 5.144143540903125533, 0.6357783856077160456, 2.097287126430439130 ) ) ;
#162769=CARTESIAN_POINT ( 'NONE',  ( 4.148624843374196125, 1.876505540506741010, 0.3678670841067503416 ) ) ;
#162773=CARTESIAN_POINT ( 'NONE',  ( 2.442982655898734645, -1.755780842375562312, -0.9913809985205720432 ) ) ;
#162776=CARTESIAN_POINT ( 'NONE',  ( 5.104412161113025093, -0.5839786719442441321, -1.623048794067801781 ) ) ;
#162777=CARTESIAN_POINT ( 'NONE',  ( 0.1405533004714799583, 1.991423289015941345, -2.694406653617386294 ) ) ;
#162783=CARTESIAN_POINT ( 'NONE',  ( 0.2861044793709514589, -1.271156181823060560, -1.634742764404631066 ) ) ;
#162785=CARTESIAN_POINT ( 'NONE',  ( 4.986864056229866726, -1.707513420791425540, -0.6052512474536574372 ) ) ;
#162788=CARTESIAN_POINT ( 'NONE',  ( 5.725234622465176670, 1.600757532941178063, 0.8479277756611166561 ) ) ;
#162791=CARTESIAN_POINT ( 'NONE',  ( 2.800927341068761844, 1.851789894747071008, 1.171597702228709181 ) ) ;
#162794=CARTESIAN_POINT ( 'NONE',  ( 6.865680895677650497, -0.4029405758906497437, 1.823372528724865438 ) ) ;
#162796=CARTESIAN_POINT ( 'NONE',  ( 4.622610566699385082, 0.3315282304991398754, 1.886534565956134335 ) ) ;
#162802=CARTESIAN_POINT ( 'NONE',  ( 1.938557520917514987, 2.138169252768943984, 0.3173444169591658204 ) ) ;
#162805=CARTESIAN_POINT ( 'NONE',  ( 2.467563089314188662, 1.790814366166630034, -0.3536809140580049471 ) ) ;
#162807=CARTESIAN_POINT ( 'NONE',  ( 4.752862199841776381, -1.465721779273346570, 1.088108411805274622 ) ) ;
#162810=CARTESIAN_POINT ( 'NONE',  ( 2.531394148431935776, -0.1834752923718513118, 1.903540536635806912 ) ) ;
#162812=CARTESIAN_POINT ( 'NONE',  ( 3.367590298639517421, -0.3867537717311599343, 1.931019599036578160 ) ) ;
#162814=CARTESIAN_POINT ( 'NONE',  ( 4.985854738014197984, -1.927824157794202353, -0.2341192097771953584 ) ) ;
#162818=CARTESIAN_POINT ( 'NONE',  ( 4.799148092389167175, -0.2621723519393297508, -2.104289960152181393 ) ) ;
#162819=MANIFOLD_SOLID_BREP ( 'Sweep1[10]', #191758 ) ;
#162821=CARTESIAN_POINT ( 'NONE',  ( 2.613799471529183460, -0.5979904443059110841, 1.816458080996792068 ) ) ;
#162823=CARTESIAN_POINT ( 'NONE',  ( 6.983263157960366563, 2.446371134953594151, 2.328889586965996905 ) ) ;
#162826=CARTESIAN_POINT ( 'NONE',  ( 4.793612393603923216, 1.877549684267119101, -0.7266104139797191497 ) ) ;
#162828=CARTESIAN_POINT ( 'NONE',  ( 4.705575438601840688, -0.4840451379145363497, 1.760283039881085809 ) ) ;
#162829=CARTESIAN_POINT ( 'NONE',  ( 1.082579992370054311, 1.234693400583252609, -1.661741702728709802 ) ) ;
#162833=CARTESIAN_POINT ( 'NONE',  ( 5.524238439434661530, 1.113281918156138639, -1.503147240406087271 ) ) ;
#162842=CARTESIAN_POINT ( 'NONE',  ( 1.780221101387355009, -1.146701191353172611, -1.723467693327894068 ) ) ;
#162843=CARTESIAN_POINT ( 'NONE',  ( 2.161849840330143824, 1.305120488479810659, 1.667033946717882742 ) ) ;
#162846=CARTESIAN_POINT ( 'NONE',  ( 1.041781249306489965, 1.318715992218882693, 1.462978117936466926 ) ) ;
#162851=CARTESIAN_POINT ( 'NONE',  ( 3.099882009726143917, -2.289598904869084350, 0.1129434519280565069 ) ) ;
#162852=CARTESIAN_POINT ( 'NONE',  ( 1.207329354700342305, -0.4456725867950651621, 1.770335049871730071 ) ) ;
#162853=CARTESIAN_POINT ( 'NONE',  ( 1.951281838316549777, -1.706683157587106425, 0.8630329916254894096 ) ) ;
#162857=CARTESIAN_POINT ( 'NONE',  ( 1.424089148264463089, -1.997494042244374768, 0.2507359931839692191 ) ) ;
#162858=CARTESIAN_POINT ( 'NONE',  ( 1.428482823135175606, -1.248714028858177283, 1.512975372890807524 ) ) ;
#162862=CARTESIAN_POINT ( 'NONE',  ( 4.242189115703227209, 0.5575990197337198362, 2.014825664747122769 ) ) ;
#162863=CARTESIAN_POINT ( 'NONE',  ( 3.379546851323252721, 1.122120933264129539, 1.368648242959294992 ) ) ;
#162865=CARTESIAN_POINT ( 'NONE',  ( 6.509759575370489770, -1.074588918421373940, -2.024802758542126213 ) ) ;
#162866=CARTESIAN_POINT ( 'NONE',  ( 4.435344831996881787, 0.7407458870649418214, -1.574957418989342939 ) ) ;
#162869=CARTESIAN_POINT ( 'NONE',  ( 4.850818353276647343, -0.8162368348260983231, 1.529697846671844941 ) ) ;
#162870=CARTESIAN_POINT ( 'NONE',  ( 5.090355501040885855, 1.120491699331874536, -1.859593947532897973 ) ) ;
#162872=CARTESIAN_POINT ( 'NONE',  ( 5.348842313791752900, -1.825074749614737701, -0.8578464102408298597 ) ) ;
#162873=CARTESIAN_POINT ( 'NONE',  ( 6.500000003069670740, 7.552736074387352678E-08, -2.052068128417939175 ) ) ;
#162875=CARTESIAN_POINT ( 'NONE',  ( 3.293886989636186868, -0.7820812614263569218, 1.760672275598859748 ) ) ;
#162877=CARTESIAN_POINT ( 'NONE',  ( 0.2061412868327249515, 1.650399489264813502, 1.486927644236696766 ) ) ;
#162879=CARTESIAN_POINT ( 'NONE',  ( 6.983263157960365675, 7.629137130509066722, 2.646189081643287810 ) ) ;
#162883=CARTESIAN_POINT ( 'NONE',  ( 1.489269531296941507, -2.110695925841240772, -0.6924467157797905559 ) ) ;
#162889=CARTESIAN_POINT ( 'NONE',  ( 5.810998785189021909, -1.628375694745004321, 1.266036720739783128 ) ) ;
#162893=CARTESIAN_POINT ( 'NONE',  ( 6.573518820989787237, 1.789947451694915204, -0.5432430119688207437 ) ) ;
#162894=CARTESIAN_POINT ( 'NONE',  ( 5.414640894582111841, -1.106827951885097638, -1.334981224695269475 ) ) ;
#162895=CARTESIAN_POINT ( 'NONE',  ( 4.300191697305631777, 1.341742100086223743, -1.108517911846224502 ) ) ;
#162898=CARTESIAN_POINT ( 'NONE',  ( 3.386539700769741312, -0.4487184517108309123, -2.247870937536749381 ) ) ;
#162900=CARTESIAN_POINT ( 'NONE',  ( 1.394213304513430174, 1.506067903837378097, -1.058747118707924262 ) ) ;
#162903=CARTESIAN_POINT ( 'NONE',  ( 1.834698128333624112, 0.1755570873784827179, 1.817110820650599923 ) ) ;
#162904=CARTESIAN_POINT ( 'NONE',  ( 2.725232599228684993, 2.001511357256777313, 0.2440295182731533341 ) ) ;
#162905=CARTESIAN_POINT ( 'NONE',  ( 1.201424296212102893, -0.5295503721958020327, 2.126384922054704862 ) ) ;
#162907=CARTESIAN_POINT ( 'NONE',  ( 4.454198790814194453, 2.105553956100237656, -0.04914431425445846269 ) ) ;
#162910=CARTESIAN_POINT ( 'NONE',  ( 1.434126425884488354, 1.231690216755284562, 1.664001042209894088 ) ) ;
#162913=CARTESIAN_POINT ( 'NONE',  ( 4.072980787186268437, -1.570383936966279981, 1.425070900414181052 ) ) ;
#162915=CARTESIAN_POINT ( 'NONE',  ( -0.02299388927988389730, 0.001624902753813092359, -1.910968047046639251 ) ) ;
#162923=CARTESIAN_POINT ( 'NONE',  ( 3.199477664157297063, 1.824241505505564964, -0.8673461216518009165 ) ) ;
#162924=CARTESIAN_POINT ( 'NONE',  ( 0.7277292075377658209, -1.999665741513008799, 0.6608504825312794262 ) ) ;
#162927=CARTESIAN_POINT ( 'NONE',  ( 4.979284885303652430, -0.09383206328643842187, 1.858730327737258436 ) ) ;
#162933=CARTESIAN_POINT ( 'NONE',  ( 1.855835942623608181, -0.6640040153468586004, 1.846199708051485811 ) ) ;
#162934=CARTESIAN_POINT ( 'NONE',  ( 0.5675189469334164238, 0.2105291993744831114, -2.151437729447757796 ) ) ;
#162938=CARTESIAN_POINT ( 'NONE',  ( 3.180671111220879865, -0.8518272437034493105, -1.510038686645834183 ) ) ;
#162939=CARTESIAN_POINT ( 'NONE',  ( 2.325747778006927557, 1.687818050649522617, 0.4237310505307323449 ) ) ;
#162940=CARTESIAN_POINT ( 'NONE',  ( 6.164718480307596060, -1.636601974411681981, 1.627217620858178337 ) ) ;
#162943=CARTESIAN_POINT ( 'NONE',  ( 2.548181945144313953, 2.060261615984103400, 0.05380422017278729124 ) ) ;
#162945=CARTESIAN_POINT ( 'NONE',  ( 1.704453651327157537, -1.458331393932917885, -1.392334588655015803 ) ) ;
#162946=CARTESIAN_POINT ( 'NONE',  ( 6.925078400183531713, -0.004750840071900476122, 2.044148492825672569 ) ) ;
#162950=CARTESIAN_POINT ( 'NONE',  ( 0.9890677962714401472, 1.739647146885098694, -0.9275093368027197416 ) ) ;
#162951=CARTESIAN_POINT ( 'NONE',  ( 4.377155534175989793, -1.710687068321177007, -0.8549628122409487219 ) ) ;
#162956=CARTESIAN_POINT ( 'NONE',  ( 1.119792439799172978, -0.4886160933238526405, 1.959555815251372568 ) ) ;
#162958=CARTESIAN_POINT ( 'NONE',  ( 4.208297055918253093, -2.301676378859803584, 0.1658454734064350733 ) ) ;
#162959=CARTESIAN_POINT ( 'NONE',  ( 5.863715402168388380, -0.4781514528688200483, 1.902565108626976809 ) ) ;
#162960=CARTESIAN_POINT ( 'NONE',  ( 2.149198318390078910, 1.709348667602617722, -0.9624241554767107854 ) ) ;
#162962=CARTESIAN_POINT ( 'NONE',  ( -0.01695367945527340853, -2.016028864686558730, -0.04667425414178057869 ) ) ;
#162964=CARTESIAN_POINT ( 'NONE',  ( 1.059931528796464129, 1.266109226500349960, 1.696929307225014449 ) ) ;
#162967=CARTESIAN_POINT ( 'NONE',  ( 1.130510352786683326, -1.665311210022573540, 0.7854980884962546872 ) ) ;
#162969=CARTESIAN_POINT ( 'NONE',  ( 4.416952212917071741, -1.612892420192946652, 1.453532087098859504 ) ) ;
#162971=CARTESIAN_POINT ( 'NONE',  ( 1.916421503514931679, -2.120014230100770725, 0.05699577502370903326 ) ) ;
#162975=CARTESIAN_POINT ( 'NONE',  ( 2.882161881593125585, -1.062215874558822826, 1.765801728998709352 ) ) ;
#162978=CARTESIAN_POINT ( 'NONE',  ( 0.3976880421775743635, -0.6195963491163231085, -1.733980255833282191 ) ) ;
#162982=CARTESIAN_POINT ( 'NONE',  ( 1.318052817733056825, -2.207296558944459974, 0.4957021660386366491 ) ) ;
#162984=CARTESIAN_POINT ( 'NONE',  ( 2.917991513842286277, -1.809334129394428947, 0.09316547460730231767 ) ) ;
#162985=CARTESIAN_POINT ( 'NONE',  ( 1.727608309356289729, 0.7294743340424666433, -1.771600730223451547 ) ) ;
#162986=CARTESIAN_POINT ( 'NONE',  ( 3.666520218671379450, -0.8364210039109070127, -1.894060025281426807 ) ) ;
#162989=CARTESIAN_POINT ( 'NONE',  ( 1.270321628189803542, -1.252206795699914332, 1.522702518494284396 ) ) ;
#162990=CARTESIAN_POINT ( 'NONE',  ( 0.3406813593837527687, 0.3259726575214479394, 1.898462188649749249 ) ) ;
#162991=CARTESIAN_POINT ( 'NONE',  ( 3.238977024203249400, -1.650389259550872456, 0.8806316622528218563 ) ) ;
#162992=CARTESIAN_POINT ( 'NONE',  ( 1.137850649969934347, -2.084210194689451789, 0.9910022104400189047 ) ) ;
#162994=CARTESIAN_POINT ( 'NONE',  ( 2.259996020855909116, -1.860750554326926487, 0.04185779618384557338 ) ) ;
#162996=CARTESIAN_POINT ( 'NONE',  ( 5.740703853076708718, -2.011634581743710903, -0.4553567745326501104 ) ) ;
#162999=CARTESIAN_POINT ( 'NONE',  ( 6.458053290436937210, 2.100604981398071835, -0.1509308302805877633 ) ) ;
#163001=CARTESIAN_POINT ( 'NONE',  ( 5.606754022945427351, 1.640879930231559758, -1.407263238018638507 ) ) ;
#163002=CARTESIAN_POINT ( 'NONE',  ( 1.048114208743459619, -1.451426956872736262, 1.132798186660122441 ) ) ;
#163003=CARTESIAN_POINT ( 'NONE',  ( 5.936196224836090884, -1.123750473735840361, -1.677956830082157236 ) ) ;
#163010=CARTESIAN_POINT ( 'NONE',  ( 4.100796195634116792, 1.845626398921360822, 0.8128187495666516771 ) ) ;
#163015=CARTESIAN_POINT ( 'NONE',  ( 6.086834708314957432, -0.3123483334277510348, -2.138898144987111838 ) ) ;
#163020=CARTESIAN_POINT ( 'NONE',  ( 5.677361293727043901, 1.528752376640944100, 1.314985542479940817 ) ) ;
#163022=CARTESIAN_POINT ( 'NONE',  ( 2.156509779666794024, -1.334175267976490664, 1.093223185313265899 ) ) ;
#163027=CARTESIAN_POINT ( 'NONE',  ( 0.3679306741783492929, -1.162814898748459225, 1.334192561405376676 ) ) ;
#163029=CARTESIAN_POINT ( 'NONE',  ( 0.3287710483851979393, 1.386612999538240576, -1.459627859818838802 ) ) ;
#163031=CARTESIAN_POINT ( 'NONE',  ( 3.505080564089088746, 1.740947047783932611, -1.355986173033681075 ) ) ;
#163033=CARTESIAN_POINT ( 'NONE',  ( 5.014598762909163732, 0.8246402433861481640, 2.008555861535677778 ) ) ;
#163038=CARTESIAN_POINT ( 'NONE',  ( 2.649219347560148208, 0.2619616101627724736, 2.104190563435456518 ) ) ;
#163039=CARTESIAN_POINT ( 'NONE',  ( 1.476185646619165404, -2.006963189339417308, -0.1948195631672477446 ) ) ;
#163040=CARTESIAN_POINT ( 'NONE',  ( 2.812559491778331200, -0.5300286150072616165, -1.732275345909091380 ) ) ;
#163047=CARTESIAN_POINT ( 'NONE',  ( 1.674859764755828095, 1.664904793830531027, -0.9475745862929999541 ) ) ;
#163050=( BOUNDED_SURFACE ( )  B_SPLINE_SURFACE ( 3, 3, ( 
 ( #113748, #97445, #11897, #209016, #114802, #77971, #127896, #110547, #95325, #30301, #10823, #176549, #180801, #163501, #32427, #194921, #162438, #80100, #28159, #212220, #63855, #130011, #126815, #193847, #46558, #94255, #197049, #210089, #160294, #47636, #144094, #196002, #178688, #161374, #76897, #12957, #31369, #112678, #61728, #15085, #143021, #213286, #179752, #81175, #45497, #111613, #147254, #64912, #131061, #177625, #48687, #29233, #79035, #145150, #211156, #62780, #100617, #122027, #182930, #116931, #2018, #65949, #187994, #123113, #199158, #34546, #73166, #133157, #18283, #104636, #68087, #203164, #22270, #164557, #166692, #6027, #89459, #88379, #84369, #955, #23349, #139272, #54809, #150457, #83287, #137136, #120957, #205302, #16142, #186928, #49737, #155512, #198107, #82227, #132098, #38560, #55871, #50803, #17211, #148318, #72096, #56941, #149372, #170683, #154447, #67021, #138206, #204218, #214317, #99558, #39619, #189071, #105723, #171753, #98493, #7093, #165623, #115864, #181849, #33486, #76383, #190129, #142492, #143569, #158712, #177095, #78516, #111088, #157655, #93732, #193334, #40706, #108959, #210648, #208499, #174979, #60134, #126291, #191185, #25497, #62274, #107898, #173924, #206376, #10309, #141441, #160845, #125227, #124167, #209561, #128435, #91605, #44980, #192250, #159772, #28710, #41784, #26561, #9253, #43912, #61206, #127364, #94796, #75324, #90525, #106810, #207447, #59066, #58003, #42852, #110026, #172840, #74265, #24411, #12437, #156587, #176040, #27632, #11371, #140358, #77451, #144633, #8181, #92668, #162986, #164055, #161924, #17752, #30859, #195480, #82781, #211704, #165104, #113230, #131591, #99049, #15634, #16696, #13514, #145705, #181346, #129499, #63340, #47113, #179235, #114298, #148854, #116411, #213822, #64408, #81721, #96936, #180296, #427, #50292, #79586, #65440, #198644, #182401, #112165, #14567, #80663, #66499, #34031, #196544, #130552, #146754, #32973, #178168, #83842, #149931, #100104, #166164, #212772, #97997, #197592, #132638, #1500, #67566, #48187, #194402, #95868, #31919, #46044, #29784, #147803, #49236, #115355, #117485, #23092, #89207, #119619, #152061, #105467, #186675, #20952, #88124, #69709, #185603, #183476, #39370, #68641, #22014, #121773, #38302, #35083, #120700, #102233, #170427, #155261, #3631, #135813, #104380, #103306, #154194, #101155, #133709, #85986, #171500, #5762, #71842, #201836, #202909, #55618, #137951, #53481, #203971, #168304, #19901, #6842, #37234, #2569, #187742, #199715, #52423, #51362, #87049, #167241, #18829, #134764, #169367, #200772, #153122, #4693, #70768, #84913, #136882, #151001, #54553, #118549, #184531, #36154, #127111, #191997, #76136, #188820, #24164, #109778, #208251, #59885, #90267, #92420, #143314, #142239, #74006, #139025, #44728, #75073, #93480, #157406, #91345, #190935, #40454, #159519, #94548, #173670, #8998, #110836, #107638, #207196, #126034, #42599, #174734, #43662, #205049, #141186, #175787, #60954, #27379, #58821, #189884, #209307, #176841, #26306, #124974, #57756, #108705, #158459, #28454, #56692, #10060, #156335, #193076, #172585, #122859, #106556, #11118, #77194, #25245, #206126, #7921, #160586, #72920, #123916, #140099, #41526, #211451, #112975, #129255, #128185, #13264, #14309, #99855, #63085, #195225, #182146, #46862 ),
 ( #82520, #178987, #65191, #164849, #12193, #80404, #33776, #180043, #146501, #31665, #47936, #162737, #30601, #78264, #79337, #145454, #177915, #130302, #62030, #144388, #96690, #212518, #29529, #64160, #97742, #210388, #45794, #194146, #16441, #111915, #196290, #163801, #81471, #95620, #213570, #15377, #131345, #161671, #114050, #147548, #197340, #50035, #48982, #115100, #181097, #32713, #98795, #148607, #176, #66244, #132392, #198394, #116160, #117226, #152864, #100904, #183224, #34830, #18584, #85726, #54303, #87866, #185349, #35906, #201584, #166993, #151812, #186415, #21758, #51101, #36971, #170170, #153938, #83590, #199459, #84662, #202654, #5507, #168050, #101981, #150751, #4442, #149672, #55364, #121517, #71587, #137696, #2312, #69455, #103054, #120441, #203716, #187488, #19652, #104124, #67311, #3385, #70512, #39118, #165917, #135560, #53231, #1253, #17502, #133454, #119361, #184280, #68389, #136627, #169107, #38052, #20704, #86798, #134518, #200522, #52168, #118294, #93224, #9803, #88948, #92161, #73743, #141985, #209051, #123661, #41272, #158214, #74822, #207999, #6587, #105201, #57502, #143056, #75878, #59625, #189624, #174473, #27118, #125782, #107381, #191744, #139839, #43399, #109521, #175528, #172322, #171238, #138764, #126851, #159256, #192808, #140922, #42338, #26048, #204781, #10857, #190679, #76930, #155002, #205868, #206936, #72666, #60687, #156073, #106300, #22834, #122594, #56435, #23912, #108453, #188557, #58565, #40188, #90016, #7659, #173404, #24985, #91088, #157148, #8741, #124719, #147288, #180834, #63890, #128979, #80136, #210124, #178724, #64943, #114836, #144131, #130045, #48721, #32459, #176585, #78007, #177660, #81209, #98530, #46594, #194958, #61765, #31405, #28197, #148353, #214352, #164590, #16176, #111648, #162475, #196038, #213320, #82260, #65982, #112712, #197084, #160331, #96424, #97479, #132133, #44467, #30339, #14048, #94291, #110583, #11935, #146240, #62819, #127933, #163535, #212256, #131095, #47672, #113783, #193886, #45534, #29268, #95360, #161410, #15121, #12994, #79069, #145187, #211193, #179785, #2051, #134259, #36708, #167792, #86538, #99592, #198140, #150492, #21502, #102794, #168851, #68123, #52964, #120181, #4189, #200265, #152603, #18321, #70259, #136373, #202392, #50841, #33520, #153681, #116967, #166730, #149409, #51916, #69191, #20454, #118039, #119102, #186157, #54044, #184026, #37791, #84404, #103865, #169915, #87610, #182965, #165658, #5250, #34580, #35642, #991, #101721, #135312, #49772, #17245, #71326, #115898, #181884, #19387, #201326, #185084, #83321, #67055, #133191, #199192, #100652, #85466, #151552, #3122, #91905, #204527, #154748, #74565, #22582, #8478, #138504, #41011, #140664, #205608, #206679, #104943, #88688, #24725, #6331, #170983, #72404, #56176, #155816, #58310, #108197, #189369, #106043, #57245, #122338, #7400, #124466, #190425, #188295, #107121, #42082, #174221, #203457, #38860, #39935, #25796, #157962, #23659, #172066, #89770, #90828, #55112, #9554, #75629, #141739, #137441, #73481, #123405, #173144, #121258, #187230, #139581, #156890, #54730, #17937, #168479, #103486, #104563, #138132, #102411, #36333, #100280, #5949, #72019, #20077, #134941, #88308, #169547, #3808, #70951, #52596, #86166, #166346, #22195, #51543, #4872, #170608, #21128 ),
 ( #152236, #101341, #118724, #167422, #2749, #19014, #84023, #117667, #184709, #204141, #85094, #151179, #116590, #68819, #183660, #203086, #154372, #182584, #69881, #35264, #135992, #137061, #202006, #38486, #34207, #186855, #200947, #87232, #120881, #150113, #53666, #1686, #119797, #185777, #37410, #153296, #67740, #133890, #199896, #111719, #93295, #142052, #77003, #157215, #125855, #12003, #61834, #91159, #10927, #210198, #128000, #123731, #25057, #124789, #28267, #193954, #208067, #59692, #8811, #192880, #189693, #95432, #161485, #45602, #177727, #58636, #109594, #143129, #160401, #29339, #13063, #191812, #144202, #107453, #43476, #44535, #79142, #205941, #175599, #27189, #41344, #57573, #173480, #159331, #9874, #74889, #110653, #209125, #78077, #60762, #126922, #140997, #207005, #190749, #94359, #42413, #176654, #108518, #174547, #26122, #92233, #158284, #75950, #81281, #198205, #114905, #33584, #46665, #145259, #97551, #183031, #49840, #115967, #15190, #76424, #67124, #165726, #147357, #99657, #179853, #17314, #83392, #149476, #212323, #195031, #100717, #63961, #113858, #96497, #213384, #16244, #1059, #112786, #197151, #132198, #133257, #166794, #131160, #65008, #129057, #34647, #18388, #48788, #163608, #117036, #181956, #32525, #199263, #180902, #98601, #178797, #50908, #80208, #211264, #62888, #30413, #162547, #14117, #31476, #146309, #130116, #164662, #82330, #196106, #148422, #47742, #66054, #84465, #36771, #122397, #203518, #137501, #168913, #153740, #6392, #105003, #20516, #187292, #119161, #171042, #38919, #22641, #151617, #134324, #39995, #3184, #53028, #35709, #86601, #169974, #150557, #118105, #106103, #88749, #172125, #54107, #21562, #5308, #184090, #71389, #87668, #55172, #200330, #185147, #120242, #51980, #188355, #135372, #85528, #154806, #101786, #121317, #69255, #72465, #138565, #186220, #204586, #167854, #19452, #56237, #201390, #102857, #152667, #4251, #70320, #2117, #68191, #37851, #136437, #202453, #103929, #158019, #44261, #94091, #123467, #43209, #27994, #160130, #155874, #57304, #156947, #60486, #11729, #25850, #174275, #189430, #10661, #7463, #127725, #193684, #77805, #143926, #90888, #141794, #109325, #192609, #61559, #45328, #91959, #175332, #41072, #9607, #110384, #209921, #107179, #26915, #111447, #23719, #73542, #173205, #8538, #126644, #89826, #75684, #207798, #24785, #76733, #139644, #205666, #74620, #140725, #206738, #58369, #59426, #93024, #176389, #124523, #190480, #125584, #42139, #108254, #191544, #142851, #159065, #208855, #163334, #97280, #161201, #66847, #132991, #14914, #195829, #149205, #15978, #64750, #131932, #113582, #81008, #12787, #83125, #112507, #65782, #165451, #82063, #78861, #164395, #146038, #214156, #198991, #47467, #179584, #148155, #147096, #197942, #144982, #177452, #129846, #780, #49570, #115694, #31206, #32261, #99398, #181687, #213120, #33317, #212052, #17046, #50638, #29066, #30129, #210986, #95149, #96218, #63692, #128776, #130892, #48524, #62614, #194753, #46390, #178519, #162269, #196886, #114644, #98329, #13856, #79932, #180637, #169722, #166525, #85271, #86343, #84203, #154554, #167594, #117844, #5056, #134064, #87419, #35445, #53850, #21312, #152415, #153485, #150292, #67919, #103674, #51722, #200073, #183836, #101524, #36514, #71131, #22383, #3994, #52770 ),
 ( #204325, #19193, #151357, #72202, #2926, #68999, #203269, #104745, #182761, #70063, #135116, #136175, #137249, #20259, #38666, #6133, #187033, #201132, #54915, #121066, #116764, #184890, #138310, #202194, #102600, #119983, #185960, #118906, #168655, #34379, #37592, #18116, #170792, #88493, #100452, #1859, #140473, #139379, #158820, #143682, #189179, #60240, #157762, #175085, #44017, #205411, #41891, #57051, #9362, #75434, #206485, #77559, #58115, #142598, #141546, #7203, #126399, #39731, #110136, #26672, #59172, #171863, #73276, #92776, #191294, #42960, #123215, #207552, #192359, #125331, #40816, #122135, #27748, #124274, #76488, #190232, #74371, #174029, #23457, #208608, #55982, #156696, #108002, #93844, #90636, #25600, #109069, #91713, #10416, #176148, #188100, #159882, #11487, #105836, #89569, #155618, #172948, #106924, #24527, #8286, #47223, #194507, #211813, #13620, #33080, #127478, #179346, #160956, #131692, #94905, #61318, #177206, #163096, #164155, #162029, #128541, #193449, #14676, #65547, #212882, #210756, #45093, #181449, #63450, #15741, #79693, #145806, #113341, #28820, #81826, #16798, #95977, #129603, #99155, #29891, #195589, #64513, #30968, #97043, #130658, #111202, #80773, #114400, #197698, #196648, #146860, #112268, #49340, #165208, #48288, #180398, #46155, #32019, #98104, #82882, #12546, #147909, #78621, #115459, #144745, #62377, #178282, #213924, #209674, #101262, #67665, #132744, #119722, #38405, #199823, #20003, #134867, #133809, #35186, #51464, #50394, #150035, #151107, #22115, #117588, #183579, #104487, #167346, #1605, #21054, #136985, #531, #184637, #83944, #36254, #37335, #52519, #70870, #186778, #4792, #18932, #201931, #87151, #148959, #2673, #170530, #102334, #68745, #168406, #86087, #85018, #200874, #66598, #118651, #198746, #185701, #53587, #152163, #54654, #3732, #17861, #103408, #116514, #69807, #153222, #135913, #169469, #203012, #120802, #182504, #34134, #100203, #166269, #24265, #109883, #90370, #174837, #41634, #39469, #92527, #71943, #142349, #207301, #91449, #204066, #105567, #125083, #9105, #75181, #171600, #23192, #191041, #175896, #6941, #158567, #189982, #58924, #76240, #89309, #74113, #155356, #107748, #173774, #156439, #88226, #8022, #26415, #25349, #73022, #10166, #138053, #208359, #42706, #157510, #55718, #139120, #108814, #141293, #59989, #205147, #126143, #192104, #43770, #56790, #154295, #5870, #140208, #121872, #172687, #106661, #206228, #187843, #122958, #188918, #40556, #57855, #124017, #62133, #161775, #30710, #145559, #129356, #162842, #93587, #45901, #146606, #15486, #14420, #178020, #144490, #163910, #213673, #195334, #79442, #12289, #29638, #112019, #65298, #159631, #211557, #193188, #81573, #127219, #11227, #209414, #46965, #196398, #194255, #160696, #77307, #212625, #131444, #78370, #113082, #13368, #210498, #128293, #95723, #143419, #28565, #63192, #115208, #179087, #96793, #197447, #80510, #94652, #114156, #147657, #61060, #64266, #176948, #130410, #48042, #180149, #49088, #27487, #97847, #31775, #44836, #110942, #181198, #37890, #139684, #137540, #103968, #203557, #5346, #117336, #166024, #205706, #170010, #16547, #154846, #88788, #67419, #89863, #51212, #71428, #138603, #186255, #21598, #82629, #155913, #116266, #72504, #172166, #6430, #164955, #171080, #149783, #204626 ),
 ( #22676, #87703, #38960, #106142, #56277, #153776, #122436, #1357, #188394, #40030, #23758, #33882, #148714, #57341, #99960, #133561, #132501, #55210, #121356, #32826, #283, #98902, #7498, #66355, #187331, #105043, #73582, #198499, #50144, #182257, #17609, #83694, #199568, #93061, #90924, #161239, #174313, #124561, #11769, #140761, #94130, #42177, #60525, #28035, #159100, #160169, #156989, #74657, #110423, #58407, #206773, #190520, #108292, #43243, #77842, #29105, #10702, #59464, #208894, #25887, #109362, #143965, #193724, #8577, #142894, #127768, #45368, #41111, #91997, #158057, #209959, #111484, #125623, #191581, #9643, #176426, #107220, #12825, #78900, #177492, #95188, #75719, #26954, #126686, #61598, #145022, #211026, #175371, #123504, #24822, #76771, #189469, #173244, #141833, #192648, #44301, #207838, #166568, #18156, #48562, #81047, #34420, #115735, #194791, #84244, #150330, #199030, #66890, #129884, #180675, #82102, #17086, #100493, #62651, #130932, #820, #178556, #114682, #49610, #50678, #128810, #32300, #196925, #46428, #112546, #30166, #98367, #147132, #96254, #181725, #164430, #83164, #213158, #16016, #162307, #182803, #212089, #165492, #116803, #33356, #13892, #99437, #31242, #149247, #79973, #64788, #148195, #133030, #214195, #146077, #63725, #195868, #14950, #47507, #113619, #179622, #65824, #131972, #97319, #163375, #197982, #104785, #36551, #22422, #170831, #154594, #69036, #51761, #171904, #135154, #184927, #167631, #152452, #87457, #67957, #35486, #23500, #6172, #89607, #185996, #153525, #71169, #101564, #203305, #5094, #54954, #117881, #102638, #37631, #183874, #39774, #52810, #2967, #88532, #19232, #187072, #201171, #137287, #121106, #103710, #38705, #85312, #151396, #72241, #118948, #168694, #20299, #86384, #136214, #138348, #122176, #169761, #4031, #204365, #70100, #202234, #56022, #188141, #53886, #21350, #105879, #1897, #134101, #120021, #200110, #192398, #143718, #157802, #91749, #189217, #142638, #60278, #158856, #57087, #106963, #44054, #76526, #208647, #172987, #175123, #11525, #10453, #156735, #7239, #127514, #9400, #176184, #25637, #174065, #59209, #123252, #27784, #177242, #41928, #75470, #193486, #190271, #141583, #126435, #125366, #42995, #110173, #73316, #207590, #93882, #209710, #159921, #191330, #58153, #77595, #45128, #109108, #26710, #140510, #92812, #61355, #111238, #139419, #28855, #24567, #155657, #40856, #205454, #90673, #8326, #74410, #108040, #206522, #124312, #65576, #198776, #145842, #180431, #80804, #79726, #195626, #211848, #210790, #96012, #97076, #182536, #63485, #129640, #50425, #47261, #162064, #181479, #82913, #160990, #130692, #29928, #196682, #197728, #212914, #16830, #132773, #165237, #113375, #147942, #33109, #94942, #163129, #116544, #48321, #14712, #114432, #32048, #31002, #179381, #12582, #146894, #144782, #131723, #213955, #64548, #561, #98136, #178320, #49368, #78654, #13654, #99186, #164186, #115486, #148986, #15772, #81858, #66627, #62413, #128577, #194542, #46188, #112304, #120831, #201961, #199853, #38435, #17891, #88256, #71972, #102364, #186807, #150065, #86119, #21080, #22142, #55747, #20033, #168434, #83978, #138081, #204095, #152192, #52550, #5899, #87183, #135945, #203040, #184666, #3760, #1636, #154325, #183612, #137013, #121903, #153248, #67695 ),
 ( #18964, #36286, #118681, #34163, #166302, #69835, #51494, #170559, #133842, #100234, #117621, #53617, #54681, #200901, #167375, #35219, #4823, #101295, #85048, #119750, #185729, #151136, #134895, #2702, #68776, #37363, #103437, #169498, #70902, #104515, #143449, #8057, #188947, #60020, #175924, #39499, #9136, #122989, #75210, #76270, #91479, #109913, #11259, #43800, #90399, #26447, #126172, #187871, #41665, #209446, #141321, #107776, #207334, #58956, #124047, #172717, #61091, #173801, #23226, #158596, #92556, #74144, #93616, #57884, #56820, #142378, #105598, #106692, #192135, #125111, #10195, #27517, #40587, #25379, #24295, #191069, #42735, #190013, #171630, #157539, #159659, #108841, #139149, #77336, #89338, #155386, #208387, #174867, #156469, #140237, #206259, #6969, #73050, #205178, #313, #178051, #29669, #82660, #161805, #128324, #213703, #115239, #193221, #162870, #62165, #14450, #15516, #30740, #49121, #164987, #197477, #95753, #180181, #65327, #127250, #195364, #148744, #80541, #46995, #146638, #212653, #63222, #112051, #44867, #113112, #176979, #97880, #31804, #13396, #32857, #211586, #210531, #81601, #110973, #45932, #131474, #64294, #163941, #181229, #194287, #179117, #79472, #130440, #196427, #129385, #28597, #96821, #98932, #48072, #78401, #16577, #94685, #160727, #147686, #114183, #12320, #144521, #145590, #201726, #53367, #17641, #85870, #136766, #84800, #200657, #50176, #170310, #21898, #52306, #150888, #38192, #119502, #168189, #20840, #2450, #118436, #116296, #186564, #1388, #169254, #54444, #185487, #182287, #37113, #34969, #103191, #88008, #68525, #134654, #86939, #36040, #153005, #33913, #66384, #18716, #104264, #4582, #70656, #184423, #135700, #202794, #120586, #102120, #154079, #101041, #132532, #198529, #99989, #133594, #166055, #83726, #199599, #167131, #149817, #19788, #151947, #3518, #67449, #117368, #183365, #51242, #69590, #6731, #92312, #208140, #71727, #41417, #155149, #107524, #108592, #123805, #142127, #43549, #76024, #122741, #58709, #158355, #5646, #73896, #175672, #173555, #139989, #25128, #91231, #156226, #204931, #27260, #206010, #55506, #190822, #124858, #106446, #125929, #90160, #89096, #174620, #93368, #138911, #9948, #157291, #42483, #59770, #72810, #57645, #56582, #8881, #74960, #7803, #137839, #189765, #191887, #141070, #171386, #109670, #203861, #121660, #26196, #207077, #187628, #22977, #39255, #105349, #188704, #40340, #172469, #24057, #79220, #160474, #11003, #131234, #161555, #179927, #29417, #177800, #62963, #126999, #31550, #180978, #45678, #95508, #197223, #194028, #145338, #162617, #129133, #46745, #80285, #77080, #13144, #64040, #147432, #146384, #211339, #61910, #81352, #48863, #112858, #195109, #144278, #178874, #30485, #114978, #143208, #96569, #110726, #213456, #44610, #209198, #192958, #14193, #113931, #111795, #78148, #60838, #130185, #32600, #210272, #212398, #196178, #128072, #47820, #97625, #176726, #12081, #28339, #163683, #15265, #65080, #159404, #94435, #182028, #201464, #186297, #17387, #102931, #200404, #3264, #86677, #33656, #84542, #99731, #52052, #118179, #34717, #120321, #100788, #185224, #184166, #49919, #168992, #82405, #152744, #69332, #101863, #62, #116040, #135443, #19531, #85607, #20591, #36848, #4325, #18464, #165802, #164731, #70395, #166871 ),
 ( #150632, #167931, #2193, #35787, #151696, #16320, #117107, #53108, #136513, #119241, #68269, #1135, #202532, #54181, #98675, #134402, #83470, #148494, #183108, #66126, #132269, #198278, #149550, #67198, #133335, #199339, #50985, #205747, #206814, #204667, #171124, #21636, #8617, #141872, #88832, #123543, #23798, #22718, #138646, #154887, #153820, #39001, #40072, #125661, #6471, #72547, #207881, #56316, #105086, #124602, #25933, #104007, #73624, #187371, #139724, #140803, #155955, #174355, #75764, #108334, #122477, #90967, #190562, #37933, #106184, #59504, #57379, #172208, #189507, #41153, #188438, #89903, #170051, #7541, #107262, #173282, #5391, #87744, #24864, #157030, #58448, #55252, #74699, #42218, #92041, #158098, #9686, #71468, #137581, #203599, #121399, #126730, #142935, #60571, #44344, #114469, #82951, #100273, #81894, #130726, #65610, #208936, #180470, #600, #50463, #76816, #213990, #198817, #116582, #109406, #10745, #110466, #16870, #182577, #196717, #48358, #192690, #181517, #175412, #84015, #150106, #34199, #166339, #176466, #98173, #131760, #149025, #17930, #1678, #32085, #132813, #93102, #164221, #197765, #191623, #14749, #212948, #15808, #26995, #67732, #43286, #147980, #64585, #159143, #33146, #49403, #66666, #115522, #99226, #31038, #97112, #163164, #80841, #146931, #165276, #117660, #120872, #102403, #170599, #23265, #152229, #69874, #186846, #103476, #22186, #35257, #133882, #86158, #171668, #38478, #104555, #3800, #203078, #55787, #154362, #135983, #88301, #168471, #5941, #72012, #138125, #200940, #183652, #89377, #52589, #20069, #85087, #201997, #4864, #199889, #167415, #155426, #204134, #7012, #169538, #70942, #54723, #19006, #121944, #137053, #187910, #101333, #39540, #53656, #36325, #105641, #51535, #87224, #185769, #118716, #119788, #37402, #151171, #2742, #21118, #68812, #134934, #184703, #153288, #40629, #26486, #27559, #25417, #206301, #56860, #43838, #177020, #124090, #158638, #58995, #57925, #173840, #190053, #188985, #74189, #75249, #160769, #41705, #107815, #28637, #91523, #140281, #159698, #61129, #139188, #108885, #8099, #174908, #175965, #191110, #209488, #111015, #143492, #157581, #126216, #11297, #73087, #141362, #94724, #92596, #207375, #10235, #76310, #9174, #125151, #205218, #42777, #123034, #109954, #192177, #142417, #193260, #208426, #156510, #93655, #106732, #60060, #77376, #127289, #44907, #172759, #24334, #90442, #29711, #212696, #130479, #113154, #16618, #179159, #213742, #64337, #112092, #131512, #144561, #115276, #97920, #48111, #62205, #178094, #15553, #180221, #31843, #197515, #65365, #49159, #96862, #95792, #12362, #32894, #30783, #181268, #162910, #47038, #80582, #194329, #98972, #82700, #195409, #14492, #165024, #63263, #146680, #114223, #196469, #163978, #81640, #210571, #147725, #78441, #128362, #45971, #161849, #13437, #79514, #145632, #211628, #129425, #155640, #176169, #74393, #11510, #44038, #175108, #39756, #42982, #24549, #92796, #159903, #140495, #206505, #109092, #25622, #158841, #171887, #56006, #8309, #93865, #26694, #10438, #58136, #125351, #192384, #76510, #124295, #142621, #90656, #208630, #60263, #126420, #123236, #105861, #77581, #189201, #156718, #7224, #190254, #141567, #122157, #89591, #143704, #110156, #188125, #91734, #207575, #191314, #73300, #27769 ) ),
 .UNSPECIFIED., .T., .F., .T. ) 
 B_SPLINE_SURFACE_WITH_KNOTS ( ( 4, 3, 4 ),
 ( 4, 1, 1, 1, 1, 1, 1, 1, 1, 1, 1, 1, 1, 1, 1, 1, 1, 1, 1, 1, 1, 1, 1, 1, 1, 1, 1, 1, 1, 1, 1, 1, 1, 1, 1, 1, 1, 1, 1, 1, 1, 1, 1, 1, 1, 1, 1, 1, 1, 1, 1, 1, 1, 1, 1, 1, 1, 1, 1, 1, 1, 1, 1, 1, 1, 1, 1, 1, 1, 1, 1, 1, 1, 1, 1, 1, 1, 1, 1, 1, 1, 1, 1, 1, 1, 1, 1, 1, 1, 1, 1, 1, 1, 1, 1, 1, 1, 1, 1, 1, 1, 1, 1, 1, 1, 1, 1, 1, 1, 1, 1, 1, 1, 1, 1, 1, 1, 1, 1, 1, 1, 1, 1, 1, 1, 1, 1, 1, 1, 1, 1, 1, 1, 1, 1, 1, 1, 1, 1, 1, 1, 1, 1, 1, 1, 1, 1, 1, 1, 1, 1, 1, 1, 1, 1, 1, 1, 1, 1, 1, 1, 1, 1, 1, 1, 1, 1, 1, 1, 1, 1, 1, 1, 1, 1, 1, 1, 1, 1, 1, 1, 1, 1, 1, 1, 1, 1, 1, 1, 1, 1, 1, 1, 1, 1, 1, 1, 1, 1, 1, 1, 1, 1, 1, 1, 1, 1, 1, 1, 1, 1, 1, 1, 1, 1, 1, 1, 1, 1, 1, 1, 1, 1, 1, 1, 1, 1, 1, 1, 1, 1, 1, 1, 1, 1, 1, 1, 1, 1, 1, 1, 1, 1, 1, 1, 1, 1, 1, 1, 1, 1, 1, 1, 1, 1, 1, 1, 1, 1, 1, 1, 1, 1, 1, 1, 1, 1, 1, 1, 1, 1, 1, 1, 1, 1, 1, 1, 1, 1, 1, 1, 1, 1, 1, 1, 1, 1, 1, 1, 1, 1, 1, 1, 1, 1, 1, 1, 1, 1, 1, 1, 1, 1, 1, 1, 1, 1, 1, 1, 1, 1, 1, 1, 1, 1, 1, 1, 1, 1, 1, 1, 1, 1, 1, 1, 1, 1, 1, 1, 1, 1, 1, 1, 1, 1, 1, 1, 1, 1, 1, 1, 1, 1, 1, 1, 1, 1, 1, 1, 1, 1, 1, 1, 1, 1, 1, 1, 1, 1, 1, 1, 1, 1, 1, 1, 1, 1, 1, 1, 1, 1, 1, 1, 1, 1, 1, 1, 1, 1, 1, 1, 1, 1, 1, 4 ),
 ( 0.000000000000000000, 0.5000000000000000000, 1.000000000000000000 ),
 ( 0.000000000000000000, 0.002599974731368114196, 0.005208790931971673047, 0.007813145979665977320, 0.01041652777592116073, 0.01302061325022423749, 0.01562498222773845216, 0.01822909327250534645, 0.02083329118620782031, 0.02343750764584028035, 0.02604160881127103033, 0.02864587273906003470, 0.03124992668191499748, 0.03385418289307650513, 0.03645825757725845717, 0.03906249379052053466, 0.04166666320740203266, 0.04427081823557592333, 0.04687506849204003262, 0.04947913642841410276, 0.05208339700068515682, 0.05468745344639398126, 0.05729170333903113588, 0.05989581325979084075, 0.06250002080062810883, 0.06510424464624173235, 0.06770834408375023261, 0.07031260355790951155, 0.07291665769283758869, 0.07552091454841564078, 0.07812498837240108851, 0.08072922377910608793, 0.08333339284475561881, 0.08593754734057650058, 0.08854179710653446722, 0.09114586450482109470, 0.09375012458370637902, 0.09635418052565795921, 0.09895842987840544613, 0.1015625393267825388, 0.1041667463075427041, 0.1067709697059155277, 0.1093750686050062593, 0.1119793276133541904, 0.1145833812402851093, 0.1171876375884709082, 0.1197917109360151500, 0.1223959458003068407, 0.1250001144218755300, 0.1276042683764700425, 0.1302085177025434359, 0.1328125845892443313, 0.1354168441945610146, 0.1380208996559441903, 0.1406251484930516882, 0.1432292574929059925, 0.1458334639374244401, 0.1484376869122458475, 0.1510417852965526830, 0.1536460438630466996, 0.1562500970055218374, 0.1588543528702505148, 0.1614584257649260002, 0.1640626601106844606, 0.1666668283118819260, 0.1692709817489688462, 0.1718752306590244638, 0.1744792970577103974, 0.1770835562133957763, 0.1796876112177483997, 0.1822918595631332073, 0.1848959681380851483, 0.1875001740701665309, 0.1901043966452301559, 0.1927084945383780445, 0.1953127526869259389, 0.1979168053684795814, 0.2005210607736844508, 0.2031251332390507092, 0.2057293670901427229, 0.2083335348946688259, 0.2109376878379560227, 0.2135419363558502259, 0.2161460022900811573, 0.2187502610200618980, 0.2213543155909112325, 0.2239585634684796434, 0.2265626716421396125, 0.2291668770855771753, 0.2317710992846666596, 0.2343751967102698508, 0.2369794544647692847, 0.2395835067089256143, 0.2421877616785296505, 0.2447918337381362330, 0.2473960671184182170, 0.2500002345499632850, 0.2526043870231480248, 0.2552086351727278490, 0.2578127006660536624, 0.2604169589942467167, 0.2630210131551104502, 0.2656252605887587936, 0.2682293683847277177, 0.2708335733633049913, 0.2734377952101950116, 0.2760418921918580404, 0.2786461495761977103, 0.2812502014064713896, 0.2838544559643880194, 0.2864585276417753179, 0.2890627605750938911, 0.2916669276573394809, 0.2942710796841097043, 0.2968753274892133587, 0.2994793925651746958, 0.3020836505154881335, 0.3046877042898750165, 0.3072919513034905736, 0.3098960587453611915, 0.3125002632828523530, 0.3151044848013095923, 0.3177085813626279731, 0.3203128384006882490, 0.3229168898405855304, 0.3255211440107198539, 0.3281252153294201834, 0.3307294478396133885, 0.3333336145962333963, 0.3359377662002681064, 0.3385420136847264727, 0.3411460783668558427, 0.3437503359631899347, 0.3463543893746011126, 0.3489586359920627823, 0.3515627431034201722, 0.3541669472235909888, 0.3567711684373747749, 0.3593752646019360286, 0.3619795213175900916, 0.3645835723906095116, 0.3671878261968588575, 0.3697918971803975663, 0.3723961292912953969, 0.3750002957459567798, 0.3776044469509276524, 0.3802086941385645069, 0.3828127584503868142, 0.3854170157166348365, 0.3880210687885642384, 0.3906253150337437030, 0.3932294218381663375, 0.3958336255647753599, 0.3984378464976386924, 0.4010419422890235119, 0.4036461987061379930, 0.4062502494357712601, 0.4088545029020263510, 0.4114585735739221262, 0.4140628053093475813, 0.4166669714857112461, 0.4192711223152827404, 0.4218753692299160307, 0.4244794331949501842, 0.4270836901549991405, 0.4296877429109347002, 0.4322919888076972583, 0.4348960953287579478, 0.4375002986855570652, 0.4401045193612476147, 0.4427086148030301427, 0.4453128709454660106, 0.4479169213551993378, 0.4505211745053449013, 0.4531252448891109341, 0.4557294762728811288, 0.4583336421946030970, 0.4609377926724337327, 0.4635420393378766879, 0.4661461029796354349, 0.4687503596573671660, 0.4713544121207915438, 0.4739586576929967765, 0.4765627639542633909, 0.4791669669649988861, 0.4817711874072597711, 0.4843752825230089321, 0.4869795384146229367, 0.4895835885279371524, 0.4921878413858530310, 0.4947919115049980165, 0.4973961425609249032, 0.5000003082516567554, 0.5026044584014001115, 0.5052087048414615200, 0.5078127681834534446, 0.5104170246027455171, 0.5130210767971369323, 0.5156253220686399796, 0.5182294280936764475, 0.5208336307820899957, 0.5234378510146604491, 0.5260419458279406157, 0.5286462014925853437, 0.5312502513329574461, 0.5338545039225196520, 0.5364585738005485105, 0.5390628045524396006, 0.5416669700358295314, 0.5442711198811350792, 0.5468753661196208427, 0.5494794291853500878, 0.5520836853700766822, 0.5546877373189100791, 0.5572919823135623618, 0.5598960881259297251, 0.5625002905157588939, 0.5651045105623757614, 0.5677086050967478092, 0.5703128605582734600, 0.5729169101491768945, 0.5755211624942581095, 0.5781252321546730411, 0.5807294626263322934, 0.5833336279260263879, 0.5859377774905402125, 0.5885420235512536236, 0.5911460863642216124, 0.5937503423382545220, 0.5963543940650019026, 0.5989586388066517886, 0.6015627444299086468, 0.6041669465448881171, 0.6067711664292861906, 0.6093752607083083861, 0.6119795159905627724, 0.6145835653554690969, 0.6171878174799397820, 0.6197918869462408775, 0.6223961171614702526, 0.6250002823011129305, 0.6276044316084782304, 0.6302086775152213605, 0.6328127400989277396, 0.6354169958861367595, 0.6380210474142689048, 0.6406252919267632073, 0.6432293973844667168, 0.6458335992483292820, 0.6484378189942425763, 0.6510419130414711875, 0.6536461681683013447, 0.6562502173306804520, 0.6588544692584096252, 0.6614585385540960871, 0.6640627685366956579, 0.6666669335399304508, 0.6692710826137896474, 0.6718753283903641238, 0.6744793907683068745, 0.6770836463925611337, 0.6796876977455479363, 0.6822919420527318035, 0.6848960473684391204, 0.6875002490049163528, 0.6901044686360783276, 0.6927085624750688453, 0.6953128174703216979, 0.6979168664536427036, 0.7005211182084990496, 0.7031251873570698585, 0.7057294171308388098, 0.7083335820213095824, 0.7109377308853042088, 0.7135419765555117699, 0.7161460387511890957, 0.7187502942363581671, 0.7213543454376690756, 0.7239585895633880996, 0.7265626947606567132, 0.7291668961934797411, 0.7317711157336249661, 0.7343752093879328813, 0.7369794642754557978, 0.7395835131031885945, 0.7421877647090413532, 0.7447918337339959338, 0.7473960633227341166, 0.7500002281240860658, 0.7526043768018576552, 0.7552086223895014827, 0.7578126844264116979, 0.7604169397963658206, 0.7630209908694718379, 0.7656252348375721661, 0.7682293399399604539, 0.7708335411928610714, 0.7734377606657260040, 0.7760418541589074737, 0.7786461089625497101, 0.7812501576581653007, 0.7838544091388848223, 0.7864584780637244865, 0.7890627074912324179, 0.7916668722271122949, 0.7942710207423038238, 0.7968752662711893198, 0.7994793281728324041, 0.8020835834514440377, 0.8046876344198176101, 0.8072918782541467220, 0.8098959832852158369, 0.8125001843819276148, 0.8151044038112509327, 0.8177084971668638902, 0.8203127519104773668, 0.8229168004974481976, 0.8255210518769072747, 0.8281251207251358881, 0.8307293500152160837, 0.8333335147092740813, 0.8359376630855301915, 0.8385419085794658667, 0.8411459703693440204, 0.8437502255804886220, 0.8463542764676049712, 0.8489585201920134550, 0.8515626251753276588, 0.8541668261395859441, 0.8567710455491102106, 0.8593751387907155870, 0.8619793934981552219, 0.8645834419999574028, 0.8671876933020320477, 0.8697917620971562513, 0.8723959912736143352, 0.8750001559495040881, 0.8776043042104727521, 0.8802085496932706699, 0.8828126113948897569, 0.8854168665624462253, 0.8880209173917842369, 0.8906251610301256783, 0.8932292659892527853, 0.8958334668447968108, 0.8984376862582688084, 0.9010417794094305322, 0.9036460341045560174, 0.9062500825446693220, 0.9088543337932389887, 0.9114584025587700866, 0.9140626316454156797, 0.9166667963267953745, 0.9192709444961273402, 0.9218751899916067805, 0.9244792516284782158, 0.9270835067763207871, 0.9296875575713596795, 0.9322918011475309630, 0.9348959061060417852, 0.9375001068764983181, 0.9401043263176916964, 0.9427084194022110619, 0.9453126741091559815, 0.9479167225106870376, 0.9505209737258253355, 0.9531250424882484751, 0.9557292715345466760, 0.9583334362123939743, 0.9609375841976093291, 0.9635418299546441023, 0.9661458919105455623, 0.9687501459642621215, 0.9713541960184646218, 0.9739584433044384815, 0.9765625494917742344, 0.9791667425299969141, 0.9817709508269629737, 0.9843750450459556323, 0.9869794226472197174, 0.9895834977571079660, 0.9921868632736227100, 0.9947912224625704569, 0.9974000159472320437, 1.000000000000000000 ),
 .UNSPECIFIED. ) 
 GEOMETRIC_REPRESENTATION_ITEM ( )  RATIONAL_B_SPLINE_SURFACE ( (
 ( 1.000000000000000000, 1.000000000000000000, 1.000000000000000000, 1.000000000000000222, 0.9999999999999997780, 1.000000000000000444, 0.9999999999999997780, 1.000000000000000222, 0.9999999999999996669, 1.000000000000000000, 1.000000000000000000, 1.000000000000000222, 1.000000000000000000, 1.000000000000000000, 0.9999999999999997780, 1.000000000000000000, 1.000000000000000000, 1.000000000000000000, 0.9999999999999997780, 1.000000000000000444, 0.9999999999999997780, 1.000000000000000222, 1.000000000000000000, 0.9999999999999997780, 1.000000000000000000, 1.000000000000000222, 0.9999999999999997780, 1.000000000000000222, 0.9999999999999997780, 1.000000000000000222, 1.000000000000000000, 0.9999999999999997780, 1.000000000000000444, 0.9999999999999997780, 1.000000000000000222, 0.9999999999999997780, 1.000000000000000444, 1.000000000000000000, 1.000000000000000000, 1.000000000000000000, 1.000000000000000000, 1.000000000000000000, 1.000000000000000000, 0.9999999999999997780, 1.000000000000000222, 0.9999999999999996669, 1.000000000000000444, 0.9999999999999994449, 1.000000000000000222, 1.000000000000000000, 1.000000000000000000, 1.000000000000000000, 1.000000000000000000, 1.000000000000000000, 0.9999999999999996669, 1.000000000000000444, 0.9999999999999997780, 1.000000000000000222, 0.9999999999999996669, 1.000000000000000000, 1.000000000000000000, 1.000000000000000222, 0.9999999999999997780, 1.000000000000000000, 1.000000000000000222, 0.9999999999999997780, 1.000000000000000000, 0.9999999999999997780, 1.000000000000000222, 0.9999999999999997780, 1.000000000000000444, 0.9999999999999994449, 1.000000000000000444, 0.9999999999999997780, 0.9999999999999997780, 1.000000000000000444, 0.9999999999999996669, 1.000000000000000000, 1.000000000000000000, 1.000000000000000000, 1.000000000000000000, 1.000000000000000222, 1.000000000000000000, 1.000000000000000000, 0.9999999999999996669, 1.000000000000000222, 1.000000000000000000, 0.9999999999999997780, 0.9999999999999997780, 0.9999999999999997780, 1.000000000000000000, 1.000000000000000222, 0.9999999999999997780, 1.000000000000000222, 0.9999999999999996669, 1.000000000000000444, 0.9999999999999997780, 1.000000000000000222, 1.000000000000000222, 0.9999999999999997780, 1.000000000000000222, 1.000000000000000000, 0.9999999999999997780, 1.000000000000000444, 1.000000000000000000, 1.000000000000000000, 1.000000000000000222, 1.000000000000000000, 1.000000000000000000, 1.000000000000000222, 0.9999999999999993339, 1.000000000000000444, 1.000000000000000222, 0.9999999999999997780, 1.000000000000000000, 1.000000000000000222, 1.000000000000000444, 1.000000000000000000, 1.000000000000000222, 0.9999999999999997780, 1.000000000000000222, 0.9999999999999997780, 1.000000000000000222, 1.000000000000000000, 0.9999999999999997780, 0.9999999999999996669, 1.000000000000000444, 0.9999999999999997780, 1.000000000000000444, 0.9999999999999997780, 1.000000000000000222, 1.000000000000000222, 1.000000000000000000, 0.9999999999999997780, 1.000000000000000222, 0.9999999999999997780, 1.000000000000000000, 1.000000000000000000, 1.000000000000000000, 0.9999999999999997780, 1.000000000000000222, 1.000000000000000000, 1.000000000000000000, 1.000000000000000000, 1.000000000000000222, 1.000000000000000222, 0.9999999999999994449, 1.000000000000000222, 1.000000000000000000, 0.9999999999999994449, 1.000000000000000444, 0.9999999999999997780, 1.000000000000000222, 0.9999999999999996669, 1.000000000000000444, 1.000000000000000000, 0.9999999999999996669, 1.000000000000000444, 0.9999999999999997780, 1.000000000000000000, 1.000000000000000444, 1.000000000000000000, 1.000000000000000222, 0.9999999999999996669, 1.000000000000000000, 0.9999999999999997780, 0.9999999999999997780, 1.000000000000000222, 1.000000000000000000, 1.000000000000000444, 0.9999999999999996669, 1.000000000000000222, 0.9999999999999997780, 0.9999999999999997780, 1.000000000000000444, 0.9999999999999997780, 1.000000000000000444, 0.9999999999999996669, 1.000000000000000222, 0.9999999999999996669, 1.000000000000000222, 0.9999999999999997780, 1.000000000000000444, 1.000000000000000222, 0.9999999999999996669, 1.000000000000000444, 0.9999999999999996669, 1.000000000000000000, 0.9999999999999997780, 1.000000000000000000, 1.000000000000000000, 1.000000000000000222, 0.9999999999999994449, 1.000000000000000444, 0.9999999999999993339, 1.000000000000000666, 0.9999999999999994449, 1.000000000000000222, 1.000000000000000222, 1.000000000000000000, 1.000000000000000000, 0.9999999999999997780, 1.000000000000000222, 0.9999999999999996669, 1.000000000000000222, 0.9999999999999996669, 1.000000000000000222, 1.000000000000000000, 1.000000000000000222, 0.9999999999999997780, 1.000000000000000222, 1.000000000000000222, 1.000000000000000000, 0.9999999999999997780, 1.000000000000000222, 1.000000000000000222, 1.000000000000000000, 1.000000000000000000, 1.000000000000000222, 0.9999999999999997780, 1.000000000000000000, 1.000000000000000222, 0.9999999999999996669, 0.9999999999999997780, 1.000000000000000222, 0.9999999999999997780, 1.000000000000000000, 0.9999999999999997780, 0.9999999999999997780, 1.000000000000000222, 1.000000000000000000, 1.000000000000000000, 1.000000000000000222, 0.9999999999999996669, 1.000000000000000444, 1.000000000000000000, 1.000000000000000222, 0.9999999999999997780, 1.000000000000000222, 0.9999999999999997780, 1.000000000000000444, 0.9999999999999997780, 1.000000000000000222, 0.9999999999999997780, 1.000000000000000222, 0.9999999999999997780, 1.000000000000000222, 1.000000000000000000, 1.000000000000000222, 1.000000000000000000, 1.000000000000000000, 1.000000000000000222, 1.000000000000000000, 1.000000000000000000, 0.9999999999999997780, 1.000000000000000000, 1.000000000000000444, 0.9999999999999996669, 1.000000000000000222, 0.9999999999999997780, 1.000000000000000000, 0.9999999999999997780, 1.000000000000000222, 1.000000000000000222, 1.000000000000000000, 1.000000000000000000, 0.9999999999999996669, 1.000000000000000444, 0.9999999999999997780, 1.000000000000000000, 1.000000000000000222, 0.9999999999999996669, 1.000000000000000444, 1.000000000000000000, 0.9999999999999997780, 1.000000000000000222, 0.9999999999999997780, 1.000000000000000000, 1.000000000000000000, 1.000000000000000000, 1.000000000000000000, 1.000000000000000000, 1.000000000000000222, 1.000000000000000444, 0.9999999999999997780, 1.000000000000000222, 1.000000000000000000, 1.000000000000000444, 0.9999999999999997780, 1.000000000000000222, 0.9999999999999997780, 1.000000000000000222, 0.9999999999999997780, 1.000000000000000222, 1.000000000000000000, 1.000000000000000222, 1.000000000000000222, 1.000000000000000222, 0.9999999999999997780, 1.000000000000000222, 0.9999999999999997780, 1.000000000000000222, 0.9999999999999997780, 1.000000000000000444, 0.9999999999999996669, 1.000000000000000444, 1.000000000000000000, 1.000000000000000000, 0.9999999999999997780, 1.000000000000000222, 1.000000000000000000, 0.9999999999999997780, 1.000000000000000000, 0.9999999999999997780, 1.000000000000000222, 1.000000000000000000, 1.000000000000000000, 1.000000000000000222, 0.9999999999999997780, 1.000000000000000444, 0.9999999999999996669, 1.000000000000000222, 1.000000000000000222, 0.9999999999999997780, 1.000000000000000000, 0.9999999999999997780, 1.000000000000000000, 0.9999999999999996669, 1.000000000000000444, 0.9999999999999997780, 1.000000000000000222, 1.000000000000000000, 1.000000000000000000, 1.000000000000000000, 0.9999999999999997780, 0.9999999999999997780, 1.000000000000000000, 0.9999999999999997780, 1.000000000000000444, 0.9999999999999996669, 1.000000000000000222, 1.000000000000000000, 1.000000000000000444, 1.000000000000000222, 1.000000000000000000, 0.9999999999999997780, 1.000000000000000222, 1.000000000000000444, 0.9999999999999997780, 1.000000000000000222, 0.9999999999999997780, 1.000000000000000000, 1.000000000000000000, 1.000000000000000222, 0.9999999999999997780, 1.000000000000000222, 1.000000000000000000, 1.000000000000000222, 0.9999999999999997780, 1.000000000000000000, 1.000000000000000222, 1.000000000000000000, 1.000000000000000222, 1.000000000000000000, 1.000000000000000000, 0.9999999999999997780, 1.000000000000000444, 0.9999999999999997780, 1.000000000000000000, 1.000000000000000000, 1.000000000000000444, 0.9999999999999996669, 1.000000000000000222, 1.000000000000000000, 0.9999999999999996669, 1.000000000000000444, 0.9999999999999996669, 1.000000000000000444, 0.9999999999999997780, 1.000000000000000222, 0.9999999999999997780, 1.000000000000000222, 1.000000000000000222, 1.000000000000000222, 1.000000000000000000, 1.000000000000000000, 1.000000000000000000),
 ( 0.3333333333333333703, 0.3333333333333333703, 0.3333333333333334259, 0.3333333333333334259, 0.3333333333333333703, 0.3333333333333334259, 0.3333333333333333148, 0.3333333333333333703, 0.3333333333333333148, 0.3333333333333333703, 0.3333333333333333703, 0.3333333333333334259, 0.3333333333333333703, 0.3333333333333333703, 0.3333333333333333703, 0.3333333333333333703, 0.3333333333333333703, 0.3333333333333333148, 0.3333333333333333703, 0.3333333333333334814, 0.3333333333333333148, 0.3333333333333334259, 0.3333333333333333148, 0.3333333333333334259, 0.3333333333333332593, 0.3333333333333335369, 0.3333333333333333703, 0.3333333333333333703, 0.3333333333333333703, 0.3333333333333333703, 0.3333333333333333703, 0.3333333333333333703, 0.3333333333333334259, 0.3333333333333333703, 0.3333333333333333703, 0.3333333333333333703, 0.3333333333333334814, 0.3333333333333333703, 0.3333333333333333703, 0.3333333333333333703, 0.3333333333333334259, 0.3333333333333332593, 0.3333333333333334814, 0.3333333333333332593, 0.3333333333333334259, 0.3333333333333332038, 0.3333333333333335369, 0.3333333333333332593, 0.3333333333333334814, 0.3333333333333333703, 0.3333333333333333148, 0.3333333333333333703, 0.3333333333333333703, 0.3333333333333333148, 0.3333333333333333148, 0.3333333333333334814, 0.3333333333333332593, 0.3333333333333334259, 0.3333333333333332593, 0.3333333333333333703, 0.3333333333333333703, 0.3333333333333334259, 0.3333333333333333148, 0.3333333333333333148, 0.3333333333333334259, 0.3333333333333333703, 0.3333333333333333703, 0.3333333333333333703, 0.3333333333333334814, 0.3333333333333332038, 0.3333333333333335924, 0.3333333333333332593, 0.3333333333333335369, 0.3333333333333333148, 0.3333333333333332593, 0.3333333333333335924, 0.3333333333333332038, 0.3333333333333333703, 0.3333333333333333703, 0.3333333333333334259, 0.3333333333333333148, 0.3333333333333334259, 0.3333333333333333703, 0.3333333333333334259, 0.3333333333333332038, 0.3333333333333333703, 0.3333333333333333703, 0.3333333333333333703, 0.3333333333333332593, 0.3333333333333333703, 0.3333333333333333148, 0.3333333333333334259, 0.3333333333333333148, 0.3333333333333334259, 0.3333333333333333148, 0.3333333333333334814, 0.3333333333333333703, 0.3333333333333334259, 0.3333333333333333703, 0.3333333333333333148, 0.3333333333333333703, 0.3333333333333334259, 0.3333333333333333148, 0.3333333333333334814, 0.3333333333333334259, 0.3333333333333333703, 0.3333333333333334259, 0.3333333333333333703, 0.3333333333333334259, 0.3333333333333334814, 0.3333333333333332038, 0.3333333333333334259, 0.3333333333333334259, 0.3333333333333333703, 0.3333333333333333148, 0.3333333333333334259, 0.3333333333333334259, 0.3333333333333334259, 0.3333333333333333703, 0.3333333333333333148, 0.3333333333333334259, 0.3333333333333333703, 0.3333333333333334259, 0.3333333333333333703, 0.3333333333333333148, 0.3333333333333332593, 0.3333333333333334259, 0.3333333333333333148, 0.3333333333333335369, 0.3333333333333332593, 0.3333333333333334814, 0.3333333333333334259, 0.3333333333333334259, 0.3333333333333333148, 0.3333333333333334259, 0.3333333333333333148, 0.3333333333333333148, 0.3333333333333333703, 0.3333333333333333703, 0.3333333333333332593, 0.3333333333333334259, 0.3333333333333333148, 0.3333333333333333703, 0.3333333333333334259, 0.3333333333333333148, 0.3333333333333334814, 0.3333333333333332593, 0.3333333333333333703, 0.3333333333333334259, 0.3333333333333332038, 0.3333333333333335369, 0.3333333333333333703, 0.3333333333333333703, 0.3333333333333333148, 0.3333333333333334259, 0.3333333333333333703, 0.3333333333333332593, 0.3333333333333335369, 0.3333333333333332593, 0.3333333333333333703, 0.3333333333333334814, 0.3333333333333333703, 0.3333333333333334259, 0.3333333333333332593, 0.3333333333333334259, 0.3333333333333332593, 0.3333333333333333703, 0.3333333333333334259, 0.3333333333333333703, 0.3333333333333334814, 0.3333333333333332593, 0.3333333333333333703, 0.3333333333333333703, 0.3333333333333333703, 0.3333333333333334259, 0.3333333333333333148, 0.3333333333333334259, 0.3333333333333332593, 0.3333333333333333703, 0.3333333333333332593, 0.3333333333333334814, 0.3333333333333333703, 0.3333333333333334259, 0.3333333333333334259, 0.3333333333333332593, 0.3333333333333334814, 0.3333333333333333148, 0.3333333333333333148, 0.3333333333333333148, 0.3333333333333333703, 0.3333333333333333703, 0.3333333333333334259, 0.3333333333333332593, 0.3333333333333335369, 0.3333333333333332038, 0.3333333333333335924, 0.3333333333333332593, 0.3333333333333334814, 0.3333333333333333703, 0.3333333333333333703, 0.3333333333333333703, 0.3333333333333333148, 0.3333333333333334259, 0.3333333333333333703, 0.3333333333333333703, 0.3333333333333333148, 0.3333333333333333703, 0.3333333333333333148, 0.3333333333333333703, 0.3333333333333332593, 0.3333333333333334259, 0.3333333333333333703, 0.3333333333333334259, 0.3333333333333333148, 0.3333333333333334259, 0.3333333333333333703, 0.3333333333333334259, 0.3333333333333334259, 0.3333333333333334259, 0.3333333333333332593, 0.3333333333333334259, 0.3333333333333333703, 0.3333333333333333148, 0.3333333333333333148, 0.3333333333333335369, 0.3333333333333332593, 0.3333333333333333148, 0.3333333333333333703, 0.3333333333333333148, 0.3333333333333334814, 0.3333333333333333703, 0.3333333333333334814, 0.3333333333333333703, 0.3333333333333332593, 0.3333333333333334259, 0.3333333333333333703, 0.3333333333333335369, 0.3333333333333333148, 0.3333333333333334259, 0.3333333333333333148, 0.3333333333333335924, 0.3333333333333332593, 0.3333333333333334259, 0.3333333333333334259, 0.3333333333333333703, 0.3333333333333333703, 0.3333333333333334259, 0.3333333333333334259, 0.3333333333333334259, 0.3333333333333333703, 0.3333333333333333703, 0.3333333333333334259, 0.3333333333333333148, 0.3333333333333333703, 0.3333333333333332038, 0.3333333333333334259, 0.3333333333333334814, 0.3333333333333332593, 0.3333333333333333703, 0.3333333333333333148, 0.3333333333333334814, 0.3333333333333332593, 0.3333333333333334259, 0.3333333333333333703, 0.3333333333333333703, 0.3333333333333333703, 0.3333333333333333148, 0.3333333333333334259, 0.3333333333333333703, 0.3333333333333333148, 0.3333333333333334259, 0.3333333333333332038, 0.3333333333333334259, 0.3333333333333333703, 0.3333333333333333703, 0.3333333333333333703, 0.3333333333333334259, 0.3333333333333333148, 0.3333333333333333703, 0.3333333333333333703, 0.3333333333333333703, 0.3333333333333333703, 0.3333333333333334259, 0.3333333333333334814, 0.3333333333333332593, 0.3333333333333333703, 0.3333333333333334259, 0.3333333333333334814, 0.3333333333333333148, 0.3333333333333333703, 0.3333333333333333703, 0.3333333333333334259, 0.3333333333333333148, 0.3333333333333334814, 0.3333333333333333148, 0.3333333333333334814, 0.3333333333333333703, 0.3333333333333334814, 0.3333333333333333148, 0.3333333333333334259, 0.3333333333333332593, 0.3333333333333335369, 0.3333333333333333148, 0.3333333333333334814, 0.3333333333333333148, 0.3333333333333334259, 0.3333333333333333703, 0.3333333333333333148, 0.3333333333333333703, 0.3333333333333333703, 0.3333333333333334259, 0.3333333333333333148, 0.3333333333333334259, 0.3333333333333333148, 0.3333333333333334814, 0.3333333333333333148, 0.3333333333333334259, 0.3333333333333334259, 0.3333333333333333703, 0.3333333333333334259, 0.3333333333333333703, 0.3333333333333333703, 0.3333333333333335369, 0.3333333333333332593, 0.3333333333333334259, 0.3333333333333333703, 0.3333333333333333703, 0.3333333333333333148, 0.3333333333333335369, 0.3333333333333333148, 0.3333333333333334259, 0.3333333333333333703, 0.3333333333333333703, 0.3333333333333334259, 0.3333333333333333148, 0.3333333333333333703, 0.3333333333333333148, 0.3333333333333333148, 0.3333333333333334814, 0.3333333333333332593, 0.3333333333333334259, 0.3333333333333333703, 0.3333333333333334814, 0.3333333333333334259, 0.3333333333333333148, 0.3333333333333333703, 0.3333333333333333703, 0.3333333333333335369, 0.3333333333333333148, 0.3333333333333334259, 0.3333333333333333703, 0.3333333333333333148, 0.3333333333333334259, 0.3333333333333334259, 0.3333333333333333703, 0.3333333333333333703, 0.3333333333333334259, 0.3333333333333334259, 0.3333333333333333703, 0.3333333333333333148, 0.3333333333333334259, 0.3333333333333333703, 0.3333333333333334814, 0.3333333333333333703, 0.3333333333333333703, 0.3333333333333333703, 0.3333333333333334259, 0.3333333333333333148, 0.3333333333333333703, 0.3333333333333334259, 0.3333333333333334259, 0.3333333333333333148, 0.3333333333333333703, 0.3333333333333333148, 0.3333333333333333703, 0.3333333333333335369, 0.3333333333333333148, 0.3333333333333334259, 0.3333333333333333703, 0.3333333333333334259, 0.3333333333333333148, 0.3333333333333333148, 0.3333333333333335369, 0.3333333333333333703, 0.3333333333333333148, 0.3333333333333333703, 0.3333333333333333703),
 ( 0.3333333333333333703, 0.3333333333333333703, 0.3333333333333334259, 0.3333333333333334259, 0.3333333333333333703, 0.3333333333333334259, 0.3333333333333333148, 0.3333333333333333703, 0.3333333333333333148, 0.3333333333333333703, 0.3333333333333333703, 0.3333333333333334259, 0.3333333333333333703, 0.3333333333333333703, 0.3333333333333333703, 0.3333333333333333703, 0.3333333333333333703, 0.3333333333333333148, 0.3333333333333333703, 0.3333333333333334814, 0.3333333333333333148, 0.3333333333333334259, 0.3333333333333333148, 0.3333333333333334259, 0.3333333333333332593, 0.3333333333333335369, 0.3333333333333333703, 0.3333333333333333703, 0.3333333333333333703, 0.3333333333333333703, 0.3333333333333333703, 0.3333333333333333703, 0.3333333333333334259, 0.3333333333333333703, 0.3333333333333333703, 0.3333333333333333703, 0.3333333333333334814, 0.3333333333333333703, 0.3333333333333333703, 0.3333333333333333703, 0.3333333333333334259, 0.3333333333333332593, 0.3333333333333334814, 0.3333333333333332593, 0.3333333333333334259, 0.3333333333333332038, 0.3333333333333335369, 0.3333333333333332593, 0.3333333333333334814, 0.3333333333333333703, 0.3333333333333333148, 0.3333333333333333703, 0.3333333333333333703, 0.3333333333333333148, 0.3333333333333333148, 0.3333333333333334814, 0.3333333333333332593, 0.3333333333333334259, 0.3333333333333332593, 0.3333333333333333703, 0.3333333333333333703, 0.3333333333333334259, 0.3333333333333333148, 0.3333333333333333148, 0.3333333333333334259, 0.3333333333333333703, 0.3333333333333333703, 0.3333333333333333703, 0.3333333333333334814, 0.3333333333333332038, 0.3333333333333335924, 0.3333333333333332593, 0.3333333333333335369, 0.3333333333333333148, 0.3333333333333332593, 0.3333333333333335924, 0.3333333333333332038, 0.3333333333333333703, 0.3333333333333333703, 0.3333333333333334259, 0.3333333333333333148, 0.3333333333333334259, 0.3333333333333333703, 0.3333333333333334259, 0.3333333333333332038, 0.3333333333333333703, 0.3333333333333333703, 0.3333333333333333703, 0.3333333333333332593, 0.3333333333333333703, 0.3333333333333333148, 0.3333333333333334259, 0.3333333333333333148, 0.3333333333333334259, 0.3333333333333333148, 0.3333333333333334814, 0.3333333333333333703, 0.3333333333333334259, 0.3333333333333333703, 0.3333333333333333148, 0.3333333333333333703, 0.3333333333333334259, 0.3333333333333333148, 0.3333333333333334814, 0.3333333333333334259, 0.3333333333333333703, 0.3333333333333334259, 0.3333333333333333703, 0.3333333333333334259, 0.3333333333333334814, 0.3333333333333332038, 0.3333333333333334259, 0.3333333333333334259, 0.3333333333333333703, 0.3333333333333333148, 0.3333333333333334259, 0.3333333333333334259, 0.3333333333333334259, 0.3333333333333333703, 0.3333333333333333148, 0.3333333333333334259, 0.3333333333333333703, 0.3333333333333334259, 0.3333333333333333703, 0.3333333333333333148, 0.3333333333333332593, 0.3333333333333334259, 0.3333333333333333148, 0.3333333333333335369, 0.3333333333333332593, 0.3333333333333334814, 0.3333333333333334259, 0.3333333333333334259, 0.3333333333333333148, 0.3333333333333334259, 0.3333333333333333148, 0.3333333333333333148, 0.3333333333333333703, 0.3333333333333333703, 0.3333333333333332593, 0.3333333333333334259, 0.3333333333333333148, 0.3333333333333333703, 0.3333333333333334259, 0.3333333333333333148, 0.3333333333333334814, 0.3333333333333332593, 0.3333333333333333703, 0.3333333333333334259, 0.3333333333333332038, 0.3333333333333335369, 0.3333333333333333703, 0.3333333333333333703, 0.3333333333333333148, 0.3333333333333334259, 0.3333333333333333703, 0.3333333333333332593, 0.3333333333333335369, 0.3333333333333332593, 0.3333333333333333703, 0.3333333333333334814, 0.3333333333333333703, 0.3333333333333334259, 0.3333333333333332593, 0.3333333333333334259, 0.3333333333333332593, 0.3333333333333333703, 0.3333333333333334259, 0.3333333333333333703, 0.3333333333333334814, 0.3333333333333332593, 0.3333333333333333703, 0.3333333333333333703, 0.3333333333333333703, 0.3333333333333334259, 0.3333333333333333148, 0.3333333333333334259, 0.3333333333333332593, 0.3333333333333333703, 0.3333333333333332593, 0.3333333333333334814, 0.3333333333333333703, 0.3333333333333334259, 0.3333333333333334259, 0.3333333333333332593, 0.3333333333333334814, 0.3333333333333333148, 0.3333333333333333148, 0.3333333333333333148, 0.3333333333333333703, 0.3333333333333333703, 0.3333333333333334259, 0.3333333333333332593, 0.3333333333333335369, 0.3333333333333332038, 0.3333333333333335924, 0.3333333333333332593, 0.3333333333333334814, 0.3333333333333333703, 0.3333333333333333703, 0.3333333333333333703, 0.3333333333333333148, 0.3333333333333334259, 0.3333333333333333703, 0.3333333333333333703, 0.3333333333333333148, 0.3333333333333333703, 0.3333333333333333148, 0.3333333333333333703, 0.3333333333333332593, 0.3333333333333334259, 0.3333333333333333703, 0.3333333333333334259, 0.3333333333333333148, 0.3333333333333334259, 0.3333333333333333703, 0.3333333333333334259, 0.3333333333333334259, 0.3333333333333334259, 0.3333333333333332593, 0.3333333333333334259, 0.3333333333333333703, 0.3333333333333333148, 0.3333333333333333148, 0.3333333333333335369, 0.3333333333333332593, 0.3333333333333333148, 0.3333333333333333703, 0.3333333333333333148, 0.3333333333333334814, 0.3333333333333333703, 0.3333333333333334814, 0.3333333333333333703, 0.3333333333333332593, 0.3333333333333334259, 0.3333333333333333703, 0.3333333333333335369, 0.3333333333333333148, 0.3333333333333334259, 0.3333333333333333148, 0.3333333333333335924, 0.3333333333333332593, 0.3333333333333334259, 0.3333333333333334259, 0.3333333333333333703, 0.3333333333333333703, 0.3333333333333334259, 0.3333333333333334259, 0.3333333333333334259, 0.3333333333333333703, 0.3333333333333333703, 0.3333333333333334259, 0.3333333333333333148, 0.3333333333333333703, 0.3333333333333332038, 0.3333333333333334259, 0.3333333333333334814, 0.3333333333333332593, 0.3333333333333333703, 0.3333333333333333148, 0.3333333333333334814, 0.3333333333333332593, 0.3333333333333334259, 0.3333333333333333703, 0.3333333333333333703, 0.3333333333333333703, 0.3333333333333333148, 0.3333333333333334259, 0.3333333333333333703, 0.3333333333333333148, 0.3333333333333334259, 0.3333333333333332038, 0.3333333333333334259, 0.3333333333333333703, 0.3333333333333333703, 0.3333333333333333703, 0.3333333333333334259, 0.3333333333333333148, 0.3333333333333333703, 0.3333333333333333703, 0.3333333333333333703, 0.3333333333333333703, 0.3333333333333334259, 0.3333333333333334814, 0.3333333333333332593, 0.3333333333333333703, 0.3333333333333334259, 0.3333333333333334814, 0.3333333333333333148, 0.3333333333333333703, 0.3333333333333333703, 0.3333333333333334259, 0.3333333333333333148, 0.3333333333333334814, 0.3333333333333333148, 0.3333333333333334814, 0.3333333333333333703, 0.3333333333333334814, 0.3333333333333333148, 0.3333333333333334259, 0.3333333333333332593, 0.3333333333333335369, 0.3333333333333333148, 0.3333333333333334814, 0.3333333333333333148, 0.3333333333333334259, 0.3333333333333333703, 0.3333333333333333148, 0.3333333333333333703, 0.3333333333333333703, 0.3333333333333334259, 0.3333333333333333148, 0.3333333333333334259, 0.3333333333333333148, 0.3333333333333334814, 0.3333333333333333148, 0.3333333333333334259, 0.3333333333333334259, 0.3333333333333333703, 0.3333333333333334259, 0.3333333333333333703, 0.3333333333333333703, 0.3333333333333335369, 0.3333333333333332593, 0.3333333333333334259, 0.3333333333333333703, 0.3333333333333333703, 0.3333333333333333148, 0.3333333333333335369, 0.3333333333333333148, 0.3333333333333334259, 0.3333333333333333703, 0.3333333333333333703, 0.3333333333333334259, 0.3333333333333333148, 0.3333333333333333703, 0.3333333333333333148, 0.3333333333333333148, 0.3333333333333334814, 0.3333333333333332593, 0.3333333333333334259, 0.3333333333333333703, 0.3333333333333334814, 0.3333333333333334259, 0.3333333333333333148, 0.3333333333333333703, 0.3333333333333333703, 0.3333333333333335369, 0.3333333333333333148, 0.3333333333333334259, 0.3333333333333333703, 0.3333333333333333148, 0.3333333333333334259, 0.3333333333333334259, 0.3333333333333333703, 0.3333333333333333703, 0.3333333333333334259, 0.3333333333333334259, 0.3333333333333333703, 0.3333333333333333148, 0.3333333333333334259, 0.3333333333333333703, 0.3333333333333334814, 0.3333333333333333703, 0.3333333333333333703, 0.3333333333333333703, 0.3333333333333334259, 0.3333333333333333148, 0.3333333333333333703, 0.3333333333333334259, 0.3333333333333334259, 0.3333333333333333148, 0.3333333333333333703, 0.3333333333333333148, 0.3333333333333333703, 0.3333333333333335369, 0.3333333333333333148, 0.3333333333333334259, 0.3333333333333333703, 0.3333333333333334259, 0.3333333333333333148, 0.3333333333333333148, 0.3333333333333335369, 0.3333333333333333703, 0.3333333333333333148, 0.3333333333333333703, 0.3333333333333333703),
 ( 1.000000000000000000, 1.000000000000000000, 1.000000000000000000, 1.000000000000000222, 0.9999999999999997780, 1.000000000000000444, 0.9999999999999997780, 1.000000000000000222, 0.9999999999999996669, 1.000000000000000000, 1.000000000000000000, 1.000000000000000222, 1.000000000000000000, 1.000000000000000000, 0.9999999999999997780, 1.000000000000000000, 1.000000000000000000, 1.000000000000000000, 0.9999999999999997780, 1.000000000000000444, 0.9999999999999997780, 1.000000000000000222, 1.000000000000000000, 0.9999999999999997780, 1.000000000000000000, 1.000000000000000222, 0.9999999999999997780, 1.000000000000000222, 0.9999999999999997780, 1.000000000000000222, 1.000000000000000000, 0.9999999999999997780, 1.000000000000000444, 0.9999999999999997780, 1.000000000000000222, 0.9999999999999997780, 1.000000000000000444, 1.000000000000000000, 1.000000000000000000, 1.000000000000000000, 1.000000000000000000, 1.000000000000000000, 1.000000000000000000, 0.9999999999999997780, 1.000000000000000222, 0.9999999999999996669, 1.000000000000000444, 0.9999999999999994449, 1.000000000000000222, 1.000000000000000000, 1.000000000000000000, 1.000000000000000000, 1.000000000000000000, 1.000000000000000000, 0.9999999999999996669, 1.000000000000000444, 0.9999999999999997780, 1.000000000000000222, 0.9999999999999996669, 1.000000000000000000, 1.000000000000000000, 1.000000000000000222, 0.9999999999999997780, 1.000000000000000000, 1.000000000000000222, 0.9999999999999997780, 1.000000000000000000, 0.9999999999999997780, 1.000000000000000222, 0.9999999999999997780, 1.000000000000000444, 0.9999999999999994449, 1.000000000000000444, 0.9999999999999997780, 0.9999999999999997780, 1.000000000000000444, 0.9999999999999996669, 1.000000000000000000, 1.000000000000000000, 1.000000000000000000, 1.000000000000000000, 1.000000000000000222, 1.000000000000000000, 1.000000000000000000, 0.9999999999999996669, 1.000000000000000222, 1.000000000000000000, 0.9999999999999997780, 0.9999999999999997780, 0.9999999999999997780, 1.000000000000000000, 1.000000000000000222, 0.9999999999999997780, 1.000000000000000222, 0.9999999999999996669, 1.000000000000000444, 0.9999999999999997780, 1.000000000000000222, 1.000000000000000222, 0.9999999999999997780, 1.000000000000000222, 1.000000000000000000, 0.9999999999999997780, 1.000000000000000444, 1.000000000000000000, 1.000000000000000000, 1.000000000000000222, 1.000000000000000000, 1.000000000000000000, 1.000000000000000222, 0.9999999999999993339, 1.000000000000000444, 1.000000000000000222, 0.9999999999999997780, 1.000000000000000000, 1.000000000000000222, 1.000000000000000444, 1.000000000000000000, 1.000000000000000222, 0.9999999999999997780, 1.000000000000000222, 0.9999999999999997780, 1.000000000000000222, 1.000000000000000000, 0.9999999999999997780, 0.9999999999999996669, 1.000000000000000444, 0.9999999999999997780, 1.000000000000000444, 0.9999999999999997780, 1.000000000000000222, 1.000000000000000222, 1.000000000000000000, 0.9999999999999997780, 1.000000000000000222, 0.9999999999999997780, 1.000000000000000000, 1.000000000000000000, 1.000000000000000000, 0.9999999999999997780, 1.000000000000000222, 1.000000000000000000, 1.000000000000000000, 1.000000000000000000, 1.000000000000000222, 1.000000000000000222, 0.9999999999999994449, 1.000000000000000222, 1.000000000000000000, 0.9999999999999994449, 1.000000000000000444, 0.9999999999999997780, 1.000000000000000222, 0.9999999999999996669, 1.000000000000000444, 1.000000000000000000, 0.9999999999999996669, 1.000000000000000444, 0.9999999999999997780, 1.000000000000000000, 1.000000000000000444, 1.000000000000000000, 1.000000000000000222, 0.9999999999999996669, 1.000000000000000000, 0.9999999999999997780, 0.9999999999999997780, 1.000000000000000222, 1.000000000000000000, 1.000000000000000444, 0.9999999999999996669, 1.000000000000000222, 0.9999999999999997780, 0.9999999999999997780, 1.000000000000000444, 0.9999999999999997780, 1.000000000000000444, 0.9999999999999996669, 1.000000000000000222, 0.9999999999999996669, 1.000000000000000222, 0.9999999999999997780, 1.000000000000000444, 1.000000000000000222, 0.9999999999999996669, 1.000000000000000444, 0.9999999999999996669, 1.000000000000000000, 0.9999999999999997780, 1.000000000000000000, 1.000000000000000000, 1.000000000000000222, 0.9999999999999994449, 1.000000000000000444, 0.9999999999999993339, 1.000000000000000666, 0.9999999999999994449, 1.000000000000000222, 1.000000000000000222, 1.000000000000000000, 1.000000000000000000, 0.9999999999999997780, 1.000000000000000222, 0.9999999999999996669, 1.000000000000000222, 0.9999999999999996669, 1.000000000000000222, 1.000000000000000000, 1.000000000000000222, 0.9999999999999997780, 1.000000000000000222, 1.000000000000000222, 1.000000000000000000, 0.9999999999999997780, 1.000000000000000222, 1.000000000000000222, 1.000000000000000000, 1.000000000000000000, 1.000000000000000222, 0.9999999999999997780, 1.000000000000000000, 1.000000000000000222, 0.9999999999999996669, 0.9999999999999997780, 1.000000000000000222, 0.9999999999999997780, 1.000000000000000000, 0.9999999999999997780, 0.9999999999999997780, 1.000000000000000222, 1.000000000000000000, 1.000000000000000000, 1.000000000000000222, 0.9999999999999996669, 1.000000000000000444, 1.000000000000000000, 1.000000000000000222, 0.9999999999999997780, 1.000000000000000222, 0.9999999999999997780, 1.000000000000000444, 0.9999999999999997780, 1.000000000000000222, 0.9999999999999997780, 1.000000000000000222, 0.9999999999999997780, 1.000000000000000222, 1.000000000000000000, 1.000000000000000222, 1.000000000000000000, 1.000000000000000000, 1.000000000000000222, 1.000000000000000000, 1.000000000000000000, 0.9999999999999997780, 1.000000000000000000, 1.000000000000000444, 0.9999999999999996669, 1.000000000000000222, 0.9999999999999997780, 1.000000000000000000, 0.9999999999999997780, 1.000000000000000222, 1.000000000000000222, 1.000000000000000000, 1.000000000000000000, 0.9999999999999996669, 1.000000000000000444, 0.9999999999999997780, 1.000000000000000000, 1.000000000000000222, 0.9999999999999996669, 1.000000000000000444, 1.000000000000000000, 0.9999999999999997780, 1.000000000000000222, 0.9999999999999997780, 1.000000000000000000, 1.000000000000000000, 1.000000000000000000, 1.000000000000000000, 1.000000000000000000, 1.000000000000000222, 1.000000000000000444, 0.9999999999999997780, 1.000000000000000222, 1.000000000000000000, 1.000000000000000444, 0.9999999999999997780, 1.000000000000000222, 0.9999999999999997780, 1.000000000000000222, 0.9999999999999997780, 1.000000000000000222, 1.000000000000000000, 1.000000000000000222, 1.000000000000000222, 1.000000000000000222, 0.9999999999999997780, 1.000000000000000222, 0.9999999999999997780, 1.000000000000000222, 0.9999999999999997780, 1.000000000000000444, 0.9999999999999996669, 1.000000000000000444, 1.000000000000000000, 1.000000000000000000, 0.9999999999999997780, 1.000000000000000222, 1.000000000000000000, 0.9999999999999997780, 1.000000000000000000, 0.9999999999999997780, 1.000000000000000222, 1.000000000000000000, 1.000000000000000000, 1.000000000000000222, 0.9999999999999997780, 1.000000000000000444, 0.9999999999999996669, 1.000000000000000222, 1.000000000000000222, 0.9999999999999997780, 1.000000000000000000, 0.9999999999999997780, 1.000000000000000000, 0.9999999999999996669, 1.000000000000000444, 0.9999999999999997780, 1.000000000000000222, 1.000000000000000000, 1.000000000000000000, 1.000000000000000000, 0.9999999999999997780, 0.9999999999999997780, 1.000000000000000000, 0.9999999999999997780, 1.000000000000000444, 0.9999999999999996669, 1.000000000000000222, 1.000000000000000000, 1.000000000000000444, 1.000000000000000222, 1.000000000000000000, 0.9999999999999997780, 1.000000000000000222, 1.000000000000000444, 0.9999999999999997780, 1.000000000000000222, 0.9999999999999997780, 1.000000000000000000, 1.000000000000000000, 1.000000000000000222, 0.9999999999999997780, 1.000000000000000222, 1.000000000000000000, 1.000000000000000222, 0.9999999999999997780, 1.000000000000000000, 1.000000000000000222, 1.000000000000000000, 1.000000000000000222, 1.000000000000000000, 1.000000000000000000, 0.9999999999999997780, 1.000000000000000444, 0.9999999999999997780, 1.000000000000000000, 1.000000000000000000, 1.000000000000000444, 0.9999999999999996669, 1.000000000000000222, 1.000000000000000000, 0.9999999999999996669, 1.000000000000000444, 0.9999999999999996669, 1.000000000000000444, 0.9999999999999997780, 1.000000000000000222, 0.9999999999999997780, 1.000000000000000222, 1.000000000000000222, 1.000000000000000222, 1.000000000000000000, 1.000000000000000000, 1.000000000000000000),
 ( 0.3333333333333333703, 0.3333333333333333703, 0.3333333333333334259, 0.3333333333333334259, 0.3333333333333333703, 0.3333333333333334259, 0.3333333333333333148, 0.3333333333333333703, 0.3333333333333333148, 0.3333333333333333703, 0.3333333333333333703, 0.3333333333333334259, 0.3333333333333333703, 0.3333333333333333703, 0.3333333333333333703, 0.3333333333333333703, 0.3333333333333333703, 0.3333333333333333148, 0.3333333333333333703, 0.3333333333333334814, 0.3333333333333333148, 0.3333333333333334259, 0.3333333333333333148, 0.3333333333333334259, 0.3333333333333332593, 0.3333333333333335369, 0.3333333333333333703, 0.3333333333333333703, 0.3333333333333333703, 0.3333333333333333703, 0.3333333333333333703, 0.3333333333333333703, 0.3333333333333334259, 0.3333333333333333703, 0.3333333333333333703, 0.3333333333333333703, 0.3333333333333334814, 0.3333333333333333703, 0.3333333333333333703, 0.3333333333333333703, 0.3333333333333334259, 0.3333333333333332593, 0.3333333333333334814, 0.3333333333333332593, 0.3333333333333334259, 0.3333333333333332038, 0.3333333333333335369, 0.3333333333333332593, 0.3333333333333334814, 0.3333333333333333703, 0.3333333333333333148, 0.3333333333333333703, 0.3333333333333333703, 0.3333333333333333148, 0.3333333333333333148, 0.3333333333333334814, 0.3333333333333332593, 0.3333333333333334259, 0.3333333333333332593, 0.3333333333333333703, 0.3333333333333333703, 0.3333333333333334259, 0.3333333333333333148, 0.3333333333333333148, 0.3333333333333334259, 0.3333333333333333703, 0.3333333333333333703, 0.3333333333333333703, 0.3333333333333334814, 0.3333333333333332038, 0.3333333333333335924, 0.3333333333333332593, 0.3333333333333335369, 0.3333333333333333148, 0.3333333333333332593, 0.3333333333333335924, 0.3333333333333332038, 0.3333333333333333703, 0.3333333333333333703, 0.3333333333333334259, 0.3333333333333333148, 0.3333333333333334259, 0.3333333333333333703, 0.3333333333333334259, 0.3333333333333332038, 0.3333333333333333703, 0.3333333333333333703, 0.3333333333333333703, 0.3333333333333332593, 0.3333333333333333703, 0.3333333333333333148, 0.3333333333333334259, 0.3333333333333333148, 0.3333333333333334259, 0.3333333333333333148, 0.3333333333333334814, 0.3333333333333333703, 0.3333333333333334259, 0.3333333333333333703, 0.3333333333333333148, 0.3333333333333333703, 0.3333333333333334259, 0.3333333333333333148, 0.3333333333333334814, 0.3333333333333334259, 0.3333333333333333703, 0.3333333333333334259, 0.3333333333333333703, 0.3333333333333334259, 0.3333333333333334814, 0.3333333333333332038, 0.3333333333333334259, 0.3333333333333334259, 0.3333333333333333703, 0.3333333333333333148, 0.3333333333333334259, 0.3333333333333334259, 0.3333333333333334259, 0.3333333333333333703, 0.3333333333333333148, 0.3333333333333334259, 0.3333333333333333703, 0.3333333333333334259, 0.3333333333333333703, 0.3333333333333333148, 0.3333333333333332593, 0.3333333333333334259, 0.3333333333333333148, 0.3333333333333335369, 0.3333333333333332593, 0.3333333333333334814, 0.3333333333333334259, 0.3333333333333334259, 0.3333333333333333148, 0.3333333333333334259, 0.3333333333333333148, 0.3333333333333333148, 0.3333333333333333703, 0.3333333333333333703, 0.3333333333333332593, 0.3333333333333334259, 0.3333333333333333148, 0.3333333333333333703, 0.3333333333333334259, 0.3333333333333333148, 0.3333333333333334814, 0.3333333333333332593, 0.3333333333333333703, 0.3333333333333334259, 0.3333333333333332038, 0.3333333333333335369, 0.3333333333333333703, 0.3333333333333333703, 0.3333333333333333148, 0.3333333333333334259, 0.3333333333333333703, 0.3333333333333332593, 0.3333333333333335369, 0.3333333333333332593, 0.3333333333333333703, 0.3333333333333334814, 0.3333333333333333703, 0.3333333333333334259, 0.3333333333333332593, 0.3333333333333334259, 0.3333333333333332593, 0.3333333333333333703, 0.3333333333333334259, 0.3333333333333333703, 0.3333333333333334814, 0.3333333333333332593, 0.3333333333333333703, 0.3333333333333333703, 0.3333333333333333703, 0.3333333333333334259, 0.3333333333333333148, 0.3333333333333334259, 0.3333333333333332593, 0.3333333333333333703, 0.3333333333333332593, 0.3333333333333334814, 0.3333333333333333703, 0.3333333333333334259, 0.3333333333333334259, 0.3333333333333332593, 0.3333333333333334814, 0.3333333333333333148, 0.3333333333333333148, 0.3333333333333333148, 0.3333333333333333703, 0.3333333333333333703, 0.3333333333333334259, 0.3333333333333332593, 0.3333333333333335369, 0.3333333333333332038, 0.3333333333333335924, 0.3333333333333332593, 0.3333333333333334814, 0.3333333333333333703, 0.3333333333333333703, 0.3333333333333333703, 0.3333333333333333148, 0.3333333333333334259, 0.3333333333333333703, 0.3333333333333333703, 0.3333333333333333148, 0.3333333333333333703, 0.3333333333333333148, 0.3333333333333333703, 0.3333333333333332593, 0.3333333333333334259, 0.3333333333333333703, 0.3333333333333334259, 0.3333333333333333148, 0.3333333333333334259, 0.3333333333333333703, 0.3333333333333334259, 0.3333333333333334259, 0.3333333333333334259, 0.3333333333333332593, 0.3333333333333334259, 0.3333333333333333703, 0.3333333333333333148, 0.3333333333333333148, 0.3333333333333335369, 0.3333333333333332593, 0.3333333333333333148, 0.3333333333333333703, 0.3333333333333333148, 0.3333333333333334814, 0.3333333333333333703, 0.3333333333333334814, 0.3333333333333333703, 0.3333333333333332593, 0.3333333333333334259, 0.3333333333333333703, 0.3333333333333335369, 0.3333333333333333148, 0.3333333333333334259, 0.3333333333333333148, 0.3333333333333335924, 0.3333333333333332593, 0.3333333333333334259, 0.3333333333333334259, 0.3333333333333333703, 0.3333333333333333703, 0.3333333333333334259, 0.3333333333333334259, 0.3333333333333334259, 0.3333333333333333703, 0.3333333333333333703, 0.3333333333333334259, 0.3333333333333333148, 0.3333333333333333703, 0.3333333333333332038, 0.3333333333333334259, 0.3333333333333334814, 0.3333333333333332593, 0.3333333333333333703, 0.3333333333333333148, 0.3333333333333334814, 0.3333333333333332593, 0.3333333333333334259, 0.3333333333333333703, 0.3333333333333333703, 0.3333333333333333703, 0.3333333333333333148, 0.3333333333333334259, 0.3333333333333333703, 0.3333333333333333148, 0.3333333333333334259, 0.3333333333333332038, 0.3333333333333334259, 0.3333333333333333703, 0.3333333333333333703, 0.3333333333333333703, 0.3333333333333334259, 0.3333333333333333148, 0.3333333333333333703, 0.3333333333333333703, 0.3333333333333333703, 0.3333333333333333703, 0.3333333333333334259, 0.3333333333333334814, 0.3333333333333332593, 0.3333333333333333703, 0.3333333333333334259, 0.3333333333333334814, 0.3333333333333333148, 0.3333333333333333703, 0.3333333333333333703, 0.3333333333333334259, 0.3333333333333333148, 0.3333333333333334814, 0.3333333333333333148, 0.3333333333333334814, 0.3333333333333333703, 0.3333333333333334814, 0.3333333333333333148, 0.3333333333333334259, 0.3333333333333332593, 0.3333333333333335369, 0.3333333333333333148, 0.3333333333333334814, 0.3333333333333333148, 0.3333333333333334259, 0.3333333333333333703, 0.3333333333333333148, 0.3333333333333333703, 0.3333333333333333703, 0.3333333333333334259, 0.3333333333333333148, 0.3333333333333334259, 0.3333333333333333148, 0.3333333333333334814, 0.3333333333333333148, 0.3333333333333334259, 0.3333333333333334259, 0.3333333333333333703, 0.3333333333333334259, 0.3333333333333333703, 0.3333333333333333703, 0.3333333333333335369, 0.3333333333333332593, 0.3333333333333334259, 0.3333333333333333703, 0.3333333333333333703, 0.3333333333333333148, 0.3333333333333335369, 0.3333333333333333148, 0.3333333333333334259, 0.3333333333333333703, 0.3333333333333333703, 0.3333333333333334259, 0.3333333333333333148, 0.3333333333333333703, 0.3333333333333333148, 0.3333333333333333148, 0.3333333333333334814, 0.3333333333333332593, 0.3333333333333334259, 0.3333333333333333703, 0.3333333333333334814, 0.3333333333333334259, 0.3333333333333333148, 0.3333333333333333703, 0.3333333333333333703, 0.3333333333333335369, 0.3333333333333333148, 0.3333333333333334259, 0.3333333333333333703, 0.3333333333333333148, 0.3333333333333334259, 0.3333333333333334259, 0.3333333333333333703, 0.3333333333333333703, 0.3333333333333334259, 0.3333333333333334259, 0.3333333333333333703, 0.3333333333333333148, 0.3333333333333334259, 0.3333333333333333703, 0.3333333333333334814, 0.3333333333333333703, 0.3333333333333333703, 0.3333333333333333703, 0.3333333333333334259, 0.3333333333333333148, 0.3333333333333333703, 0.3333333333333334259, 0.3333333333333334259, 0.3333333333333333148, 0.3333333333333333703, 0.3333333333333333148, 0.3333333333333333703, 0.3333333333333335369, 0.3333333333333333148, 0.3333333333333334259, 0.3333333333333333703, 0.3333333333333334259, 0.3333333333333333148, 0.3333333333333333148, 0.3333333333333335369, 0.3333333333333333703, 0.3333333333333333148, 0.3333333333333333703, 0.3333333333333333703),
 ( 0.3333333333333333703, 0.3333333333333333703, 0.3333333333333334259, 0.3333333333333334259, 0.3333333333333333703, 0.3333333333333334259, 0.3333333333333333148, 0.3333333333333333703, 0.3333333333333333148, 0.3333333333333333703, 0.3333333333333333703, 0.3333333333333334259, 0.3333333333333333703, 0.3333333333333333703, 0.3333333333333333703, 0.3333333333333333703, 0.3333333333333333703, 0.3333333333333333148, 0.3333333333333333703, 0.3333333333333334814, 0.3333333333333333148, 0.3333333333333334259, 0.3333333333333333148, 0.3333333333333334259, 0.3333333333333332593, 0.3333333333333335369, 0.3333333333333333703, 0.3333333333333333703, 0.3333333333333333703, 0.3333333333333333703, 0.3333333333333333703, 0.3333333333333333703, 0.3333333333333334259, 0.3333333333333333703, 0.3333333333333333703, 0.3333333333333333703, 0.3333333333333334814, 0.3333333333333333703, 0.3333333333333333703, 0.3333333333333333703, 0.3333333333333334259, 0.3333333333333332593, 0.3333333333333334814, 0.3333333333333332593, 0.3333333333333334259, 0.3333333333333332038, 0.3333333333333335369, 0.3333333333333332593, 0.3333333333333334814, 0.3333333333333333703, 0.3333333333333333148, 0.3333333333333333703, 0.3333333333333333703, 0.3333333333333333148, 0.3333333333333333148, 0.3333333333333334814, 0.3333333333333332593, 0.3333333333333334259, 0.3333333333333332593, 0.3333333333333333703, 0.3333333333333333703, 0.3333333333333334259, 0.3333333333333333148, 0.3333333333333333148, 0.3333333333333334259, 0.3333333333333333703, 0.3333333333333333703, 0.3333333333333333703, 0.3333333333333334814, 0.3333333333333332038, 0.3333333333333335924, 0.3333333333333332593, 0.3333333333333335369, 0.3333333333333333148, 0.3333333333333332593, 0.3333333333333335924, 0.3333333333333332038, 0.3333333333333333703, 0.3333333333333333703, 0.3333333333333334259, 0.3333333333333333148, 0.3333333333333334259, 0.3333333333333333703, 0.3333333333333334259, 0.3333333333333332038, 0.3333333333333333703, 0.3333333333333333703, 0.3333333333333333703, 0.3333333333333332593, 0.3333333333333333703, 0.3333333333333333148, 0.3333333333333334259, 0.3333333333333333148, 0.3333333333333334259, 0.3333333333333333148, 0.3333333333333334814, 0.3333333333333333703, 0.3333333333333334259, 0.3333333333333333703, 0.3333333333333333148, 0.3333333333333333703, 0.3333333333333334259, 0.3333333333333333148, 0.3333333333333334814, 0.3333333333333334259, 0.3333333333333333703, 0.3333333333333334259, 0.3333333333333333703, 0.3333333333333334259, 0.3333333333333334814, 0.3333333333333332038, 0.3333333333333334259, 0.3333333333333334259, 0.3333333333333333703, 0.3333333333333333148, 0.3333333333333334259, 0.3333333333333334259, 0.3333333333333334259, 0.3333333333333333703, 0.3333333333333333148, 0.3333333333333334259, 0.3333333333333333703, 0.3333333333333334259, 0.3333333333333333703, 0.3333333333333333148, 0.3333333333333332593, 0.3333333333333334259, 0.3333333333333333148, 0.3333333333333335369, 0.3333333333333332593, 0.3333333333333334814, 0.3333333333333334259, 0.3333333333333334259, 0.3333333333333333148, 0.3333333333333334259, 0.3333333333333333148, 0.3333333333333333148, 0.3333333333333333703, 0.3333333333333333703, 0.3333333333333332593, 0.3333333333333334259, 0.3333333333333333148, 0.3333333333333333703, 0.3333333333333334259, 0.3333333333333333148, 0.3333333333333334814, 0.3333333333333332593, 0.3333333333333333703, 0.3333333333333334259, 0.3333333333333332038, 0.3333333333333335369, 0.3333333333333333703, 0.3333333333333333703, 0.3333333333333333148, 0.3333333333333334259, 0.3333333333333333703, 0.3333333333333332593, 0.3333333333333335369, 0.3333333333333332593, 0.3333333333333333703, 0.3333333333333334814, 0.3333333333333333703, 0.3333333333333334259, 0.3333333333333332593, 0.3333333333333334259, 0.3333333333333332593, 0.3333333333333333703, 0.3333333333333334259, 0.3333333333333333703, 0.3333333333333334814, 0.3333333333333332593, 0.3333333333333333703, 0.3333333333333333703, 0.3333333333333333703, 0.3333333333333334259, 0.3333333333333333148, 0.3333333333333334259, 0.3333333333333332593, 0.3333333333333333703, 0.3333333333333332593, 0.3333333333333334814, 0.3333333333333333703, 0.3333333333333334259, 0.3333333333333334259, 0.3333333333333332593, 0.3333333333333334814, 0.3333333333333333148, 0.3333333333333333148, 0.3333333333333333148, 0.3333333333333333703, 0.3333333333333333703, 0.3333333333333334259, 0.3333333333333332593, 0.3333333333333335369, 0.3333333333333332038, 0.3333333333333335924, 0.3333333333333332593, 0.3333333333333334814, 0.3333333333333333703, 0.3333333333333333703, 0.3333333333333333703, 0.3333333333333333148, 0.3333333333333334259, 0.3333333333333333703, 0.3333333333333333703, 0.3333333333333333148, 0.3333333333333333703, 0.3333333333333333148, 0.3333333333333333703, 0.3333333333333332593, 0.3333333333333334259, 0.3333333333333333703, 0.3333333333333334259, 0.3333333333333333148, 0.3333333333333334259, 0.3333333333333333703, 0.3333333333333334259, 0.3333333333333334259, 0.3333333333333334259, 0.3333333333333332593, 0.3333333333333334259, 0.3333333333333333703, 0.3333333333333333148, 0.3333333333333333148, 0.3333333333333335369, 0.3333333333333332593, 0.3333333333333333148, 0.3333333333333333703, 0.3333333333333333148, 0.3333333333333334814, 0.3333333333333333703, 0.3333333333333334814, 0.3333333333333333703, 0.3333333333333332593, 0.3333333333333334259, 0.3333333333333333703, 0.3333333333333335369, 0.3333333333333333148, 0.3333333333333334259, 0.3333333333333333148, 0.3333333333333335924, 0.3333333333333332593, 0.3333333333333334259, 0.3333333333333334259, 0.3333333333333333703, 0.3333333333333333703, 0.3333333333333334259, 0.3333333333333334259, 0.3333333333333334259, 0.3333333333333333703, 0.3333333333333333703, 0.3333333333333334259, 0.3333333333333333148, 0.3333333333333333703, 0.3333333333333332038, 0.3333333333333334259, 0.3333333333333334814, 0.3333333333333332593, 0.3333333333333333703, 0.3333333333333333148, 0.3333333333333334814, 0.3333333333333332593, 0.3333333333333334259, 0.3333333333333333703, 0.3333333333333333703, 0.3333333333333333703, 0.3333333333333333148, 0.3333333333333334259, 0.3333333333333333703, 0.3333333333333333148, 0.3333333333333334259, 0.3333333333333332038, 0.3333333333333334259, 0.3333333333333333703, 0.3333333333333333703, 0.3333333333333333703, 0.3333333333333334259, 0.3333333333333333148, 0.3333333333333333703, 0.3333333333333333703, 0.3333333333333333703, 0.3333333333333333703, 0.3333333333333334259, 0.3333333333333334814, 0.3333333333333332593, 0.3333333333333333703, 0.3333333333333334259, 0.3333333333333334814, 0.3333333333333333148, 0.3333333333333333703, 0.3333333333333333703, 0.3333333333333334259, 0.3333333333333333148, 0.3333333333333334814, 0.3333333333333333148, 0.3333333333333334814, 0.3333333333333333703, 0.3333333333333334814, 0.3333333333333333148, 0.3333333333333334259, 0.3333333333333332593, 0.3333333333333335369, 0.3333333333333333148, 0.3333333333333334814, 0.3333333333333333148, 0.3333333333333334259, 0.3333333333333333703, 0.3333333333333333148, 0.3333333333333333703, 0.3333333333333333703, 0.3333333333333334259, 0.3333333333333333148, 0.3333333333333334259, 0.3333333333333333148, 0.3333333333333334814, 0.3333333333333333148, 0.3333333333333334259, 0.3333333333333334259, 0.3333333333333333703, 0.3333333333333334259, 0.3333333333333333703, 0.3333333333333333703, 0.3333333333333335369, 0.3333333333333332593, 0.3333333333333334259, 0.3333333333333333703, 0.3333333333333333703, 0.3333333333333333148, 0.3333333333333335369, 0.3333333333333333148, 0.3333333333333334259, 0.3333333333333333703, 0.3333333333333333703, 0.3333333333333334259, 0.3333333333333333148, 0.3333333333333333703, 0.3333333333333333148, 0.3333333333333333148, 0.3333333333333334814, 0.3333333333333332593, 0.3333333333333334259, 0.3333333333333333703, 0.3333333333333334814, 0.3333333333333334259, 0.3333333333333333148, 0.3333333333333333703, 0.3333333333333333703, 0.3333333333333335369, 0.3333333333333333148, 0.3333333333333334259, 0.3333333333333333703, 0.3333333333333333148, 0.3333333333333334259, 0.3333333333333334259, 0.3333333333333333703, 0.3333333333333333703, 0.3333333333333334259, 0.3333333333333334259, 0.3333333333333333703, 0.3333333333333333148, 0.3333333333333334259, 0.3333333333333333703, 0.3333333333333334814, 0.3333333333333333703, 0.3333333333333333703, 0.3333333333333333703, 0.3333333333333334259, 0.3333333333333333148, 0.3333333333333333703, 0.3333333333333334259, 0.3333333333333334259, 0.3333333333333333148, 0.3333333333333333703, 0.3333333333333333148, 0.3333333333333333703, 0.3333333333333335369, 0.3333333333333333148, 0.3333333333333334259, 0.3333333333333333703, 0.3333333333333334259, 0.3333333333333333148, 0.3333333333333333148, 0.3333333333333335369, 0.3333333333333333703, 0.3333333333333333148, 0.3333333333333333703, 0.3333333333333333703),
 ( 1.000000000000000000, 1.000000000000000000, 1.000000000000000000, 1.000000000000000222, 0.9999999999999997780, 1.000000000000000444, 0.9999999999999997780, 1.000000000000000222, 0.9999999999999996669, 1.000000000000000000, 1.000000000000000000, 1.000000000000000222, 1.000000000000000000, 1.000000000000000000, 0.9999999999999997780, 1.000000000000000000, 1.000000000000000000, 1.000000000000000000, 0.9999999999999997780, 1.000000000000000444, 0.9999999999999997780, 1.000000000000000222, 1.000000000000000000, 0.9999999999999997780, 1.000000000000000000, 1.000000000000000222, 0.9999999999999997780, 1.000000000000000222, 0.9999999999999997780, 1.000000000000000222, 1.000000000000000000, 0.9999999999999997780, 1.000000000000000444, 0.9999999999999997780, 1.000000000000000222, 0.9999999999999997780, 1.000000000000000444, 1.000000000000000000, 1.000000000000000000, 1.000000000000000000, 1.000000000000000000, 1.000000000000000000, 1.000000000000000000, 0.9999999999999997780, 1.000000000000000222, 0.9999999999999996669, 1.000000000000000444, 0.9999999999999994449, 1.000000000000000222, 1.000000000000000000, 1.000000000000000000, 1.000000000000000000, 1.000000000000000000, 1.000000000000000000, 0.9999999999999996669, 1.000000000000000444, 0.9999999999999997780, 1.000000000000000222, 0.9999999999999996669, 1.000000000000000000, 1.000000000000000000, 1.000000000000000222, 0.9999999999999997780, 1.000000000000000000, 1.000000000000000222, 0.9999999999999997780, 1.000000000000000000, 0.9999999999999997780, 1.000000000000000222, 0.9999999999999997780, 1.000000000000000444, 0.9999999999999994449, 1.000000000000000444, 0.9999999999999997780, 0.9999999999999997780, 1.000000000000000444, 0.9999999999999996669, 1.000000000000000000, 1.000000000000000000, 1.000000000000000000, 1.000000000000000000, 1.000000000000000222, 1.000000000000000000, 1.000000000000000000, 0.9999999999999996669, 1.000000000000000222, 1.000000000000000000, 0.9999999999999997780, 0.9999999999999997780, 0.9999999999999997780, 1.000000000000000000, 1.000000000000000222, 0.9999999999999997780, 1.000000000000000222, 0.9999999999999996669, 1.000000000000000444, 0.9999999999999997780, 1.000000000000000222, 1.000000000000000222, 0.9999999999999997780, 1.000000000000000222, 1.000000000000000000, 0.9999999999999997780, 1.000000000000000444, 1.000000000000000000, 1.000000000000000000, 1.000000000000000222, 1.000000000000000000, 1.000000000000000000, 1.000000000000000222, 0.9999999999999993339, 1.000000000000000444, 1.000000000000000222, 0.9999999999999997780, 1.000000000000000000, 1.000000000000000222, 1.000000000000000444, 1.000000000000000000, 1.000000000000000222, 0.9999999999999997780, 1.000000000000000222, 0.9999999999999997780, 1.000000000000000222, 1.000000000000000000, 0.9999999999999997780, 0.9999999999999996669, 1.000000000000000444, 0.9999999999999997780, 1.000000000000000444, 0.9999999999999997780, 1.000000000000000222, 1.000000000000000222, 1.000000000000000000, 0.9999999999999997780, 1.000000000000000222, 0.9999999999999997780, 1.000000000000000000, 1.000000000000000000, 1.000000000000000000, 0.9999999999999997780, 1.000000000000000222, 1.000000000000000000, 1.000000000000000000, 1.000000000000000000, 1.000000000000000222, 1.000000000000000222, 0.9999999999999994449, 1.000000000000000222, 1.000000000000000000, 0.9999999999999994449, 1.000000000000000444, 0.9999999999999997780, 1.000000000000000222, 0.9999999999999996669, 1.000000000000000444, 1.000000000000000000, 0.9999999999999996669, 1.000000000000000444, 0.9999999999999997780, 1.000000000000000000, 1.000000000000000444, 1.000000000000000000, 1.000000000000000222, 0.9999999999999996669, 1.000000000000000000, 0.9999999999999997780, 0.9999999999999997780, 1.000000000000000222, 1.000000000000000000, 1.000000000000000444, 0.9999999999999996669, 1.000000000000000222, 0.9999999999999997780, 0.9999999999999997780, 1.000000000000000444, 0.9999999999999997780, 1.000000000000000444, 0.9999999999999996669, 1.000000000000000222, 0.9999999999999996669, 1.000000000000000222, 0.9999999999999997780, 1.000000000000000444, 1.000000000000000222, 0.9999999999999996669, 1.000000000000000444, 0.9999999999999996669, 1.000000000000000000, 0.9999999999999997780, 1.000000000000000000, 1.000000000000000000, 1.000000000000000222, 0.9999999999999994449, 1.000000000000000444, 0.9999999999999993339, 1.000000000000000666, 0.9999999999999994449, 1.000000000000000222, 1.000000000000000222, 1.000000000000000000, 1.000000000000000000, 0.9999999999999997780, 1.000000000000000222, 0.9999999999999996669, 1.000000000000000222, 0.9999999999999996669, 1.000000000000000222, 1.000000000000000000, 1.000000000000000222, 0.9999999999999997780, 1.000000000000000222, 1.000000000000000222, 1.000000000000000000, 0.9999999999999997780, 1.000000000000000222, 1.000000000000000222, 1.000000000000000000, 1.000000000000000000, 1.000000000000000222, 0.9999999999999997780, 1.000000000000000000, 1.000000000000000222, 0.9999999999999996669, 0.9999999999999997780, 1.000000000000000222, 0.9999999999999997780, 1.000000000000000000, 0.9999999999999997780, 0.9999999999999997780, 1.000000000000000222, 1.000000000000000000, 1.000000000000000000, 1.000000000000000222, 0.9999999999999996669, 1.000000000000000444, 1.000000000000000000, 1.000000000000000222, 0.9999999999999997780, 1.000000000000000222, 0.9999999999999997780, 1.000000000000000444, 0.9999999999999997780, 1.000000000000000222, 0.9999999999999997780, 1.000000000000000222, 0.9999999999999997780, 1.000000000000000222, 1.000000000000000000, 1.000000000000000222, 1.000000000000000000, 1.000000000000000000, 1.000000000000000222, 1.000000000000000000, 1.000000000000000000, 0.9999999999999997780, 1.000000000000000000, 1.000000000000000444, 0.9999999999999996669, 1.000000000000000222, 0.9999999999999997780, 1.000000000000000000, 0.9999999999999997780, 1.000000000000000222, 1.000000000000000222, 1.000000000000000000, 1.000000000000000000, 0.9999999999999996669, 1.000000000000000444, 0.9999999999999997780, 1.000000000000000000, 1.000000000000000222, 0.9999999999999996669, 1.000000000000000444, 1.000000000000000000, 0.9999999999999997780, 1.000000000000000222, 0.9999999999999997780, 1.000000000000000000, 1.000000000000000000, 1.000000000000000000, 1.000000000000000000, 1.000000000000000000, 1.000000000000000222, 1.000000000000000444, 0.9999999999999997780, 1.000000000000000222, 1.000000000000000000, 1.000000000000000444, 0.9999999999999997780, 1.000000000000000222, 0.9999999999999997780, 1.000000000000000222, 0.9999999999999997780, 1.000000000000000222, 1.000000000000000000, 1.000000000000000222, 1.000000000000000222, 1.000000000000000222, 0.9999999999999997780, 1.000000000000000222, 0.9999999999999997780, 1.000000000000000222, 0.9999999999999997780, 1.000000000000000444, 0.9999999999999996669, 1.000000000000000444, 1.000000000000000000, 1.000000000000000000, 0.9999999999999997780, 1.000000000000000222, 1.000000000000000000, 0.9999999999999997780, 1.000000000000000000, 0.9999999999999997780, 1.000000000000000222, 1.000000000000000000, 1.000000000000000000, 1.000000000000000222, 0.9999999999999997780, 1.000000000000000444, 0.9999999999999996669, 1.000000000000000222, 1.000000000000000222, 0.9999999999999997780, 1.000000000000000000, 0.9999999999999997780, 1.000000000000000000, 0.9999999999999996669, 1.000000000000000444, 0.9999999999999997780, 1.000000000000000222, 1.000000000000000000, 1.000000000000000000, 1.000000000000000000, 0.9999999999999997780, 0.9999999999999997780, 1.000000000000000000, 0.9999999999999997780, 1.000000000000000444, 0.9999999999999996669, 1.000000000000000222, 1.000000000000000000, 1.000000000000000444, 1.000000000000000222, 1.000000000000000000, 0.9999999999999997780, 1.000000000000000222, 1.000000000000000444, 0.9999999999999997780, 1.000000000000000222, 0.9999999999999997780, 1.000000000000000000, 1.000000000000000000, 1.000000000000000222, 0.9999999999999997780, 1.000000000000000222, 1.000000000000000000, 1.000000000000000222, 0.9999999999999997780, 1.000000000000000000, 1.000000000000000222, 1.000000000000000000, 1.000000000000000222, 1.000000000000000000, 1.000000000000000000, 0.9999999999999997780, 1.000000000000000444, 0.9999999999999997780, 1.000000000000000000, 1.000000000000000000, 1.000000000000000444, 0.9999999999999996669, 1.000000000000000222, 1.000000000000000000, 0.9999999999999996669, 1.000000000000000444, 0.9999999999999996669, 1.000000000000000444, 0.9999999999999997780, 1.000000000000000222, 0.9999999999999997780, 1.000000000000000222, 1.000000000000000222, 1.000000000000000222, 1.000000000000000000, 1.000000000000000000, 1.000000000000000000) ) ) 
 REPRESENTATION_ITEM ( '' )  SURFACE ( )  );
#163055=CARTESIAN_POINT ( 'NONE',  ( 5.559502693676295237, 0.4258712887980077300, -2.119171757835013548 ) ) ;
#163058=CARTESIAN_POINT ( 'NONE',  ( 1.810938747355747447, -0.5704394276861005642, -2.042344090522000055 ) ) ;
#163061=CARTESIAN_POINT ( 'NONE',  ( 3.673081450605990117, 0.05180205286909286139, -1.970847691630872811 ) ) ;
#163063=CARTESIAN_POINT ( 'NONE',  ( 5.625241921295836889, 1.689600096388569561, 0.8957793909229803120 ) ) ;
#163065=CARTESIAN_POINT ( 'NONE',  ( 0.1509401653462701109, -0.4529219869476922011, -2.027634260368789576 ) ) ;
#163066=CARTESIAN_POINT ( 'NONE',  ( 1.675622358955121571, -1.039060084690484942, 1.640409814757173734 ) ) ;
#163071=CARTESIAN_POINT ( 'NONE',  ( 2.361375956566538648, 2.050102581710811389, -0.4087646360023765024 ) ) ;
#163074=CARTESIAN_POINT ( 'NONE',  ( 6.533860241792342372, -1.853627334332415888, 0.4695604596292660138 ) ) ;
#163076=CARTESIAN_POINT ( 'NONE',  ( 4.670673364294657404, -1.443042178620690841, 1.669811033208345341 ) ) ;
#163077=CARTESIAN_POINT ( 'NONE',  ( 3.399657359236216703, 1.738403758043248759, 1.359216269546263511 ) ) ;
#163081=CARTESIAN_POINT ( 'NONE',  ( 1.734869227892420707, 1.784761669998648381, 0.6870963898520031643 ) ) ;
#163084=CARTESIAN_POINT ( 'NONE',  ( 4.334477209444559165, -1.194628513295314720, 1.690740121169509225 ) ) ;
#163086=CARTESIAN_POINT ( 'NONE',  ( 1.323354039402934390, -0.05256100377049736927, 2.161234000603563299 ) ) ;
#163087=CARTESIAN_POINT ( 'NONE',  ( 3.808297599986898430, 1.548825491099754315, -1.550762550882843094 ) ) ;
#163088=CARTESIAN_POINT ( 'NONE',  ( -0.02968770228140016343, 0.003472272166151618711, -1.826291111852257343 ) ) ;
#163093=CARTESIAN_POINT ( 'NONE',  ( 0.1412502902482688505, 0.7743183493036235321, 1.862015731718666078 ) ) ;
#163096=CARTESIAN_POINT ( 'NONE',  ( 5.032118066406459533, 1.187563481491529460, 1.695602288408842417 ) ) ;
#163097=CARTESIAN_POINT ( 'NONE',  ( 2.859893552614915180, 1.917175687707149967, -0.1893568897016733310 ) ) ;
#163098=CARTESIAN_POINT ( 'NONE',  ( 6.239883422132978197, 2.111550094393780608, -0.1561052605421053563 ) ) ;
#163101=CARTESIAN_POINT ( 'NONE',  ( 3.959776185634265921, -0.5760637367184845425, 1.883274482577349973 ) ) ;
#163102=CARTESIAN_POINT ( 'NONE',  ( 5.507889418014947580, -1.026508118683837401, -2.049657838918368391 ) ) ;
#163103=CARTESIAN_POINT ( 'NONE',  ( 4.389149243953620605, 1.629682310347341456, -0.8231139397327084106 ) ) ;
#163110=CARTESIAN_POINT ( 'NONE',  ( 4.816656863388896426, -0.6821788116995251006, -1.894207565886153910 ) ) ;
#163111=CARTESIAN_POINT ( 'NONE',  ( 0.2108991129620274019, -1.778944881630979413, -1.454728436597878316 ) ) ;
#163112=CARTESIAN_POINT ( 'NONE',  ( 5.506681978947471912, 0.5658967987182733639, 1.878394690154854496 ) ) ;
#163117=CARTESIAN_POINT ( 'NONE',  ( 1.558266987246118562, -1.476132899515494534, 1.480894285863892934 ) ) ;
#163118=CARTESIAN_POINT ( 'NONE',  ( 0.2329894512427649333, -1.712236961970284632, 0.7538099095961707796 ) ) ;
#163120=CARTESIAN_POINT ( 'NONE',  ( 5.701106494887172360, -0.4696333794993942101, 1.884192904834626869 ) ) ;
#163122=CARTESIAN_POINT ( 'NONE',  ( 1.364397727108757730, 0.1285707514647760064, -1.735724436397204196 ) ) ;
#163124=CARTESIAN_POINT ( 'NONE',  ( 6.875078400183575411, 7.629137130509070275, 2.455651831298297338 ) ) ;
#163125=CARTESIAN_POINT ( 'NONE',  ( 1.752176261082264208, 0.5389683859425442591, 1.638572262730133566 ) ) ;
#163126=CARTESIAN_POINT ( 'NONE',  ( 2.120887600855193345, 0.003649250790785373531, 2.191739723551556551 ) ) ;
#163127=CARTESIAN_POINT ( 'NONE',  ( 3.862124860921032354, 2.190326239153097543, -0.2693113811002012525 ) ) ;
#163129=CARTESIAN_POINT ( 'NONE',  ( 1.358521007292138538, -2.171239805896512554, -0.002410242577662382712 ) ) ;
#163130=CARTESIAN_POINT ( 'NONE',  ( 0.4865809202317071813, -0.2202831055867389420, -1.812292406919484344 ) ) ;
#163131=CARTESIAN_POINT ( 'NONE',  ( 2.009133639091817525, 0.005444305534021975056, 2.117513411327852868 ) ) ;
#163132=CARTESIAN_POINT ( 'NONE',  ( 6.639320575229276322, 3.701785489019034259, 2.411212692025939131 ) ) ;
#163134=CARTESIAN_POINT ( 'NONE',  ( 2.331904285594294191, 1.077338530963572127, -2.023425408739158105 ) ) ;
#163139=CARTESIAN_POINT ( 'NONE',  ( 5.180443790456886077, 1.093758630767979412, 1.933306047416243567 ) ) ;
#163145=CARTESIAN_POINT ( 'NONE',  ( 2.443982611291168450, -1.755769474653746665, -0.9913988478210812305 ) ) ;
#163147=CARTESIAN_POINT ( 'NONE',  ( 1.868110439076278384, -2.047461887716729656, 0.2484499435305431159 ) ) ;
#163150=ORIENTED_EDGE ( 'NONE', *, *, #149244, .T. ) ;
#163153=CARTESIAN_POINT ( 'NONE',  ( 4.593798273609356997, -2.190911875110569174, -0.05534364095756416635 ) ) ;
#163154=CARTESIAN_POINT ( 'NONE',  ( 2.690077459517980163, 1.704938782060089864, 1.076316768488336351 ) ) ;
#163155=CARTESIAN_POINT ( 'NONE',  ( 0.6613494997313728030, 0.9071737413179328247, 1.602200521169500957 ) ) ;
#163157=CARTESIAN_POINT ( 'NONE',  ( 5.122008332510333162, -0.9777984688263160473, -1.541441239866998103 ) ) ;
#163158=CARTESIAN_POINT ( 'NONE',  ( 6.363907750917786821, -0.1017471579566435469, -2.013986097687201049 ) ) ;
#163160=CARTESIAN_POINT ( 'NONE',  ( 6.192268726830573833, -2.250890937568471362, -0.2291988078206678991 ) ) ;
#163162=CARTESIAN_POINT ( 'NONE',  ( 0.9265589629697315033, 1.253077620556674932, -1.692570004448453957 ) ) ;
#163164=CARTESIAN_POINT ( 'NONE',  ( 4.246580143467587831, -2.047389768388275577, -0.3068500204662719666 ) ) ;
#163174=CARTESIAN_POINT ( 'NONE',  ( 1.529697670087664108, -0.2543295609688834835, 2.105205558366497698 ) ) ;
#163175=CARTESIAN_POINT ( 'NONE',  ( 2.619623270456972630, 1.879045213996872965, 1.184562869268386054 ) ) ;
#163179=CARTESIAN_POINT ( 'NONE',  ( 3.314850587115983238, -1.487306837207631238, 1.279512770686676681 ) ) ;
#163186=CARTESIAN_POINT ( 'NONE',  ( 1.863691559860299884, -1.706161385809309650, -1.259181899442491037 ) ) ;
#163188=CARTESIAN_POINT ( 'NONE',  ( 4.944278945467968533, 2.155654431248493985, 0.1625706239713892443 ) ) ;
#163189=CARTESIAN_POINT ( 'NONE',  ( 3.245484093776138668, 1.841430844176932480, -0.003062914905635482320 ) ) ;
#163193=CARTESIAN_POINT ( 'NONE',  ( 5.490116972639333071, -0.4286210177542044697, -1.686591927243533240 ) ) ;
#163194=CARTESIAN_POINT ( 'NONE',  ( 6.727182134110196721, 2.084960209934753284, 2.120171393779949565 ) ) ;
#163197=CARTESIAN_POINT ( 'NONE',  ( 3.555696680978126079, 0.5271953485486252644, -2.096301903996622862 ) ) ;
#163198=CARTESIAN_POINT ( 'NONE',  ( 4.024767406304472495, 2.001204788683898617, -0.2439926020210633206 ) ) ;
#163200=CARTESIAN_POINT ( 'NONE',  ( 1.973706723050288936, 2.068691090354588091, -0.6273066937243013674 ) ) ;
#163202=CARTESIAN_POINT ( 'NONE',  ( 2.741432468550320412, -1.458365196291089072, -1.326584384502631719 ) ) ;
#163204=CARTESIAN_POINT ( 'NONE',  ( 4.124509801231989847, 0.09871269697571230517, 1.939684287242355420 ) ) ;
#163214=CARTESIAN_POINT ( 'NONE',  ( 1.536444635327537833, 1.086998388645914027, -1.920427013416255768 ) ) ;
#163216=CARTESIAN_POINT ( 'NONE',  ( 5.401206054008879320, -1.684469800357458302, 1.005230755432365175 ) ) ;
#163221=CARTESIAN_POINT ( 'NONE',  ( 4.611176429654996412, -1.805050139478355353, 0.3618648703537508671 ) ) ;
#163226=CARTESIAN_POINT ( 'NONE',  ( 5.344028447597857223, -1.346983732444573256, -1.637812552581649594 ) ) ;
#163229=CARTESIAN_POINT ( 'NONE',  ( 6.872340646960426902, -1.271554428311357565, 1.622191329735128029 ) ) ;
#163231=CARTESIAN_POINT ( 'NONE',  ( 0.6603357414211168397, -0.6217855776655777378, -1.754263843975149006 ) ) ;
#163232=CARTESIAN_POINT ( 'NONE',  ( 4.142028884782995135, 0.4951553702221401232, 1.773339192993342639 ) ) ;
#163237=CARTESIAN_POINT ( 'NONE',  ( 3.229339687698820072, 0.05429069646168545316, 2.206380697113208722 ) ) ;
#163238=CARTESIAN_POINT ( 'NONE',  ( 6.503223684228603751, 1.875565888388399660, 1.264963274899598256 ) ) ;
#163240=CARTESIAN_POINT ( 'NONE',  ( 6.134996530155978789, 1.693739186514784167, 0.6432786700914516764 ) ) ;
#163241=CARTESIAN_POINT ( 'NONE',  ( 5.893738820153655134, -1.900388249151972353, 0.2415585323580979049 ) ) ;
#163243=CARTESIAN_POINT ( 'NONE',  ( 5.840666405660361882, 0.3664468388623157158, 1.834233659845653897 ) ) ;
#163244=CARTESIAN_POINT ( 'NONE',  ( 6.496546432963370421, 1.840999872533972903, 0.2716635292502044829 ) ) ;
#163247=CARTESIAN_POINT ( 'NONE',  ( 0.1450994221751950586, -1.442925249786636943, -1.190247126510869613 ) ) ;
#163248=CARTESIAN_POINT ( 'NONE',  ( 1.376185782568883020, -2.007256511855738612, -0.1928315418098166534 ) ) ;
#163250=CARTESIAN_POINT ( 'NONE',  ( 2.420660912963272349, 1.375124471020009231, -1.595256772795665023 ) ) ;
#163255=CARTESIAN_POINT ( 'NONE',  ( 2.636978264590104537, 1.903244974434484371, 0.6766128908266034747 ) ) ;
#163258=CARTESIAN_POINT ( 'NONE',  ( 2.970174626046932609, 1.153603175066318931, 1.827835936144058371 ) ) ;
#163259=CARTESIAN_POINT ( 'NONE',  ( 6.890000000000047642, 2.940278081043229186, 2.731889818495436995 ) ) ;
#163266=CARTESIAN_POINT ( 'NONE',  ( 2.261505105119133052, 2.148611799745976381, -0.4309092228176118478 ) ) ;
#163268=CARTESIAN_POINT ( 'NONE',  ( 2.237552233957947667, -2.020869686619676919, 1.017492276205993695 ) ) ;
#163276=CARTESIAN_POINT ( 'NONE',  ( 2.688433849602299031, -0.2980574676569973658, -1.744271549386553932 ) ) ;
#163277=CARTESIAN_POINT ( 'NONE',  ( 6.317417574511640765, -0.2763070477263400715, 2.189352377801502936 ) ) ;
#163280=CARTESIAN_POINT ( 'NONE',  ( 4.657827466662149973, 1.163286545301238206, 1.646828140416577879 ) ) ;
#163283=CARTESIAN_POINT ( 'NONE',  ( 4.117926171558832671, -0.9613396577640184182, -1.604580606731422776 ) ) ;
#163284=CARTESIAN_POINT ( 'NONE',  ( 3.801679563076823420, -1.564429233171928058, -1.355977067927462976 ) ) ;
#163290=CARTESIAN_POINT ( 'NONE',  ( 1.599720133015330337, 1.321132142916726204, 1.382909031182079307 ) ) ;
#163292=CARTESIAN_POINT ( 'NONE',  ( 3.209375601822930690, -1.602329130913646926, -1.131729396966949963 ) ) ;
#163293=CARTESIAN_POINT ( 'NONE',  ( 0.6849224457974397717, -1.076149790962807495, -1.704679027301945649 ) ) ;
#163297=CARTESIAN_POINT ( 'NONE',  ( 6.239525796224010712, -1.426203020326064275, -1.361167568813693718 ) ) ;
#163299=CARTESIAN_POINT ( 'NONE',  ( 1.722903956744771481, 1.489010464042400450, -1.355078301658399820 ) ) ;
#163301=CARTESIAN_POINT ( 'NONE',  ( 2.179462045401040715, 1.638881033884627803, 1.340452329455198210 ) ) ;
#163303=CARTESIAN_POINT ( 'NONE',  ( 4.316890830952234914, -1.536253448065309613, 1.388129241271539138 ) ) ;
#163305=CARTESIAN_POINT ( 'NONE',  ( 5.665992906516797767, -1.327130266483244059, 1.615391119202228332 ) ) ;
#163307=CARTESIAN_POINT ( 'NONE',  ( 3.838725952263983388, 0.2674066485093031242, 1.805754746396167176 ) ) ;
#163315=CARTESIAN_POINT ( 'NONE',  ( 4.951771945676144426, -1.355037094400749487, -1.349591858340569717 ) ) ;
#163324=CARTESIAN_POINT ( 'NONE',  ( 0.5207438388301621757, -1.748553680932497745, 0.5769860859521497298 ) ) ;
#163327=CARTESIAN_POINT ( 'NONE',  ( 4.534354090784907143, 1.834037221929617711, 0.3668691113338993781 ) ) ;
#163328=CARTESIAN_POINT ( 'NONE',  ( -0.02319159430947542386, 5.725354828811364705, -2.405035539666657840 ) ) ;
#163334=CARTESIAN_POINT ( 'NONE',  ( 1.815228950277411712, -1.686530385472130744, -1.016810816036699316 ) ) ;
#163336=CARTESIAN_POINT ( 'NONE',  ( 2.812125237574263803, 1.117814398428567557, -1.678018709429726307 ) ) ;
#163340=CARTESIAN_POINT ( 'NONE',  ( 2.888834398507355239, 1.879202789969806497, -1.127179367409691935 ) ) ;
#163353=CARTESIAN_POINT ( 'NONE',  ( 4.528748383445759806, -1.681502307688139908, 0.7506017836093890061 ) ) ;
#163354=CARTESIAN_POINT ( 'NONE',  ( 1.295565486743395889, 1.859180707359459284, -0.7724582428273608636 ) ) ;
#163355=CARTESIAN_POINT ( 'NONE',  ( 3.374663776259867909, -0.4515557078652779333, 2.253457335377069271 ) ) ;
#163357=CARTESIAN_POINT ( 'NONE',  ( 2.342426049922683884, -1.823874001192757666, -0.3686824239186973218 ) ) ;
#163359=CARTESIAN_POINT ( 'NONE',  ( 6.883263157960362477, -0.004191378316371896506, 2.053658919477070910 ) ) ;
#163360=CARTESIAN_POINT ( 'NONE',  ( 5.871340715825057011, -1.643613990083541143, -0.9773822251149253404 ) ) ;
#163363=CARTESIAN_POINT ( 'NONE',  ( 5.425362623596053702, -1.327343567673059166, -1.615326566546205767 ) ) ;
#163364=CARTESIAN_POINT ( 'NONE',  ( 3.942156681999692491, 1.861596489644477437, 0.1839347620080991341 ) ) ;
#163366=CARTESIAN_POINT ( 'NONE',  ( 5.812015183962491172, 1.231757822100377320, -1.368757117762291253 ) ) ;
#163370=CARTESIAN_POINT ( 'NONE',  ( 5.479022876622000382, -0.04827441000932602283, -1.724383337574379116 ) ) ;
#163374=SURFACE_STYLE_USAGE ( .BOTH. , #31241 ) ;
#163375=CARTESIAN_POINT ( 'NONE',  ( 4.206061555090504278, 0.7368182104705008895, -2.042320221205825792 ) ) ;
#163376=CARTESIAN_POINT ( 'NONE',  ( 3.686012862905340803, -0.8985999850123352894, 1.589152278004740237 ) ) ;
#163377=CARTESIAN_POINT ( 'NONE',  ( 0.8308171121041010299, -1.845250773774274267, -0.6662997747023180484 ) ) ;
#163379=CARTESIAN_POINT ( 'NONE',  ( 5.858642105998121963, -2.011370865819528397, -0.6617598028889163375 ) ) ;
#163380=CARTESIAN_POINT ( 'NONE',  ( 6.286719507307084065, 1.996765193862446885, -1.125943789698529818 ) ) ;
#163384=CARTESIAN_POINT ( 'NONE',  ( 2.033984416766075665, -2.056095976692096094, 0.5180656111221926263 ) ) ;
#163389=CARTESIAN_POINT ( 'NONE',  ( 6.385609454247954453, -2.047150228866960298, 0.7234482234039444348 ) ) ;
#163390=CARTESIAN_POINT ( 'NONE',  ( 6.983263157960330147, 7.051826758666251749, 2.751962080009969114 ) ) ;
#163392=CARTESIAN_POINT ( 'NONE',  ( 2.807538669062619174, 1.903917518177394630, -1.144040067606937550 ) ) ;
#163394=CARTESIAN_POINT ( 'NONE',  ( 0.01878015289935238558, -2.097885004189947278, 0.9400277066241318202 ) ) ;
#163396=CARTESIAN_POINT ( 'NONE',  ( 5.313357764218651802, -1.739529159241906875, -1.108013508251452395 ) ) ;
#163401=CARTESIAN_POINT ( 'NONE',  ( 0.2333540202161610289, 4.089650199633740435, -2.600675808310505044 ) ) ;
#163402=CARTESIAN_POINT ( 'NONE',  ( 5.460457653299121361, -1.667157065227730106, -0.7818181906407914994 ) ) ;
#163405=CARTESIAN_POINT ( 'NONE',  ( 2.133451061308448526, -1.123891114067215424, -1.308414479858905022 ) ) ;
#163406=CARTESIAN_POINT ( 'NONE',  ( -0.03006412033006514162, -0.9462945741195265548, 1.780671068589256834 ) ) ;
#163407=CARTESIAN_POINT ( 'NONE',  ( 2.075183622135381434, -0.9789826713841279782, 2.079913408810558195 ) ) ;
#163409=CARTESIAN_POINT ( 'NONE',  ( 2.864839704461724867, -1.562160111903969417, 1.636705750015782224 ) ) ;
#163410=CARTESIAN_POINT ( 'NONE',  ( 4.108114811375044084, -2.100464006233178083, 0.1544923775467464122 ) ) ;
#163412=CARTESIAN_POINT ( 'NONE',  ( 2.073191327021279839, 1.695144128639828551, -0.5084401619379045334 ) ) ;
#163419=CARTESIAN_POINT ( 'NONE',  ( 5.836230100724939085, -1.233609159639902142, -1.847210489216906781 ) ) ;
#163420=CARTESIAN_POINT ( 'NONE',  ( 3.117305861062225958, -2.111875107304355570, 0.5849144002756587746 ) ) ;
#163423=CARTESIAN_POINT ( 'NONE',  ( 6.445950376775947177, -1.384621037358444662, -1.606076714075025613 ) ) ;
#163427=CARTESIAN_POINT ( 'NONE',  ( 6.082307721193076944, 1.091511717630256673, 1.817998432235830908 ) ) ;
#163432=CARTESIAN_POINT ( 'NONE',  ( 6.146043377905669125, 0.5841948715668408010, 1.746183665442810007 ) ) ;
#163436=CARTESIAN_POINT ( 'NONE',  ( 2.630072014739594177, 0.2149344560898290013, 1.727053582138169618 ) ) ;
#163444=CARTESIAN_POINT ( 'NONE',  ( 5.928642344448160628, 2.082074431819755045, 0.5810635428650026135 ) ) ;
#163448=CARTESIAN_POINT ( 'NONE',  ( 6.415303688471941435, -0.2438443212883933120, 1.956177878852760177 ) ) ;
#163449=CARTESIAN_POINT ( 'NONE',  ( 5.624279254961046526, 0.3357223255188810374, -1.700804604882939053 ) ) ;
#163451=CARTESIAN_POINT ( 'NONE',  ( 2.120887600855193345, 0.003649250790785373531, 2.191739723551556551 ) ) ;
#163452=CARTESIAN_POINT ( 'NONE',  ( 3.329449612262088021, 0.05463889213834548231, 2.307092628889866326 ) ) ;
#163453=CARTESIAN_POINT ( 'NONE',  ( 6.380161626619829107, -1.106262522808113324, 1.738493956250926287 ) ) ;
#163454=CARTESIAN_POINT ( 'NONE',  ( 0.8845914429877841378, 1.712865214261191316, -0.9150308779080836841 ) ) ;
#163459=CARTESIAN_POINT ( 'NONE',  ( 4.219064148821600746, 1.637239594409030330, -1.347683705884415106 ) ) ;
#163460=CARTESIAN_POINT ( 'NONE',  ( 1.811172873341511336, 1.158687402475454098, -1.650082692374904125 ) ) ;
#163462=CARTESIAN_POINT ( 'NONE',  ( 4.278500955059440614, -1.273273528111932063, 1.802203266693293671 ) ) ;
#163471=CARTESIAN_POINT ( 'NONE',  ( 4.909085936489448798, 1.792118714629163057, 1.017505292531006189 ) ) ;
#163474=CARTESIAN_POINT ( 'NONE',  ( 3.035811672558884400, -1.945802561663440455, 0.5409189654149139104 ) ) ;
#163478=CARTESIAN_POINT ( 'NONE',  ( 3.520434746236697610, 1.308796515248649817, -1.591936018771279659 ) ) ;
#163479=CARTESIAN_POINT ( 'NONE',  ( 6.727182134110202938, 2.016807574165893513, 2.492494991173600738 ) ) ;
#163482=CARTESIAN_POINT ( 'NONE',  ( -0.1408020194050146334, 0.2351808081714431564, -2.134421755367508666 ) ) ;
#163483=CARTESIAN_POINT ( 'NONE',  ( 1.077780131904103156, -1.795810734350095750, -0.4053039038426772267 ) ) ;
#163485=CARTESIAN_POINT ( 'NONE',  ( 0.1535068347273665368, -1.849414538273885578, 1.380102022147772667 ) ) ;
#163487=CARTESIAN_POINT ( 'NONE',  ( 2.337400524717429207, -1.931973293601353392, 0.9696072025056484689 ) ) ;
#163489=CARTESIAN_POINT ( 'NONE',  ( 1.393767942625488532, -2.000731169080074423, 0.2516357431460446992 ) ) ;
#163491=CARTESIAN_POINT ( 'NONE',  ( 2.478211020838327894, 2.052291828077044133, 1.034905392717075046 ) ) ;
#163495=CARTESIAN_POINT ( 'NONE',  ( 4.065273027966066266, 0.2426392691956253123, -1.956424757721614949 ) ) ;
#163496=CARTESIAN_POINT ( 'NONE',  ( 4.962125165302472496, -1.116212726388360998, 1.679221540125563905 ) ) ;
#163500=CARTESIAN_POINT ( 'NONE',  ( 5.953767555512091469, 0.6130212357637642162, -2.014879775860946687 ) ) ;
#163501=CARTESIAN_POINT ( 'NONE',  ( 6.672334155782003506, -0.9722939650993901450, -1.827837255792996718 ) ) ;
#163505=CARTESIAN_POINT ( 'NONE',  ( -0.1753031400193918732, -0.9122597987226389593, -1.912455998546586544 ) ) ;
#163507=CARTESIAN_POINT ( 'NONE',  ( 4.266487514486948740, 1.085833288323118095, 2.036285375418740884 ) ) ;
#163508=CARTESIAN_POINT ( 'NONE',  ( 1.586864402838471522, 1.986712475098152408, 0.5538950855334312529 ) ) ;
#163515=CARTESIAN_POINT ( 'NONE',  ( 3.684171759641508448, -1.290596846074614223, -1.745836057026050714 ) ) ;
#163518=CARTESIAN_POINT ( 'NONE',  ( 3.456447201099471123, -1.625387274077850996, -0.8650149607793489182 ) ) ;
#163520=CARTESIAN_POINT ( 'NONE',  ( 5.566036750361066154, -1.391122746885119499, 1.693456055751572986 ) ) ;
#163522=CARTESIAN_POINT ( 'NONE',  ( 6.262609139476608355, -1.605266756365858027, 1.594658822776671592 ) ) ;
#163525=AXIS2_PLACEMENT_3D ( 'NONE', #186749, #138021, #40525 ) ;
#163528=CARTESIAN_POINT ( 'NONE',  ( 6.608682216863940084, 1.309337763449496705, -1.190854552318038051 ) ) ;
#163530=CARTESIAN_POINT ( 'NONE',  ( 4.512362120423671463, -2.012691318418479813, -0.04721358428917859368 ) ) ;
#163532=CARTESIAN_POINT ( 'NONE',  ( 2.467921950875014314, 2.065534160692492627, -0.4097329821706324204 ) ) ;
#163533=CARTESIAN_POINT ( 'NONE',  ( 2.126450742919711256, 0.4219061677965991741, 1.868383228629175719 ) ) ;
#163535=CARTESIAN_POINT ( 'NONE',  ( 2.875404442980381781, -0.1956706474990059230, 1.959820717905029097 ) ) ;
#163537=CARTESIAN_POINT ( 'NONE',  ( 2.096370420935515178, -0.4963513585865795275, -1.803540123670114736 ) ) ;
#163538=CARTESIAN_POINT ( 'NONE',  ( 0.7308173252688826560, -1.846041318942293286, -0.6644482084196751126 ) ) ;
#163539=CARTESIAN_POINT ( 'NONE',  ( 3.510098308409233869, -0.7004517935718050925, -1.576443202522736842 ) ) ;
#163540=CARTESIAN_POINT ( 'NONE',  ( 6.504213119055646253, -0.7662104867102972339, 1.640237621407932167 ) ) ;
#163541=ORIENTED_EDGE ( 'NONE', *, *, #45298, .T. ) ;
#163542=CARTESIAN_POINT ( 'NONE',  ( 1.225528936851564721, -0.05108506852482053856, 2.206457870188942572 ) ) ;
#163549=CARTESIAN_POINT ( 'NONE',  ( 6.614133338355735248, 2.065126723422955557, -0.1462301744803648496 ) ) ;
#163551=CARTESIAN_POINT ( 'NONE',  ( 1.100149375694438714, 0.8407228983892693908, -1.892171374333020406 ) ) ;
#163556=CARTESIAN_POINT ( 'NONE',  ( 5.338584462458719315, 1.262900380722062454, -1.703257760751579530 ) ) ;
#163562=CARTESIAN_POINT ( 'NONE',  ( 6.549272904993657995, 1.707534169505098953, -0.9658701945045378157 ) ) ;
#163564=CARTESIAN_POINT ( 'NONE',  ( 4.270861128529729989, -2.010896307770511537, 0.1455111863851859810 ) ) ;
#163565=CARTESIAN_POINT ( 'NONE',  ( 3.555789339581526320, 1.068723753765013162, 1.589688962476828005 ) ) ;
#163568=CARTESIAN_POINT ( 'NONE',  ( 1.312353134292881141, 1.468346937154514364, -1.627112938194043235 ) ) ;
#163569=CARTESIAN_POINT ( 'NONE',  ( 0.1333692844072801587, 4.087911462428309051, -2.608372271572469092 ) ) ;
#163570=CARTESIAN_POINT ( 'NONE',  ( 3.549935554046261821, 1.870726058081632504, 0.003126486288931861444 ) ) ;
#163574=CARTESIAN_POINT ( 'NONE',  ( 5.870749427052773584, -0.3112397890362226249, -2.094129459642315005 ) ) ;
#163576=CARTESIAN_POINT ( 'NONE',  ( 2.683241491500857556, 1.480437668936212869, 1.476589516890645104 ) ) ;
#163578=CARTESIAN_POINT ( 'NONE',  ( 1.219288043345586159, -1.683946549099228029, 0.3722564037182389818 ) ) ;
#163590=CARTESIAN_POINT ( 'NONE',  ( 1.629273880293732768, -0.2214294203813528539, 1.797790724094426418 ) ) ;
#163594=CARTESIAN_POINT ( 'NONE',  ( 6.639320575229255006, 1.299223727596211519, 1.914393416674460946 ) ) ;
#163599=CARTESIAN_POINT ( 'NONE',  ( 3.086215985183130339, 1.036139677906501300, -1.545717422611452729 ) ) ;
#163600=CARTESIAN_POINT ( 'NONE',  ( 0.5971114826688945776, -0.2799204757548044986, 1.894894164429518746 ) ) ;
#163601=CARTESIAN_POINT ( 'NONE',  ( 6.756866522006341746, -1.488468187722398417, 1.222521302487014072 ) ) ;
#163608=CARTESIAN_POINT ( 'NONE',  ( 4.487129304207951641, 0.09229547738082846675, 1.967383831439367903 ) ) ;
#163610=CARTESIAN_POINT ( 'NONE',  ( 1.190261156817543631, 1.266008754425467897, 1.700926646755014593 ) ) ;
#163614=CARTESIAN_POINT ( 'NONE',  ( 5.402338782601354694, 1.661146971675907302, -1.429436781345946317 ) ) ;
#163616=CARTESIAN_POINT ( 'NONE',  ( 4.823225626762606133, -0.09501261394700975804, 1.924175346943966414 ) ) ;
#163619=CARTESIAN_POINT ( 'NONE',  ( 0.7272432748211544729, -1.735090175422876246, 0.5678700757711930835 ) ) ;
#163620=CARTESIAN_POINT ( 'NONE',  ( 0.7860941533469124609, 1.484900681275106216, 1.632775826992872492 ) ) ;
#163625=CARTESIAN_POINT ( 'NONE',  ( 5.910992199152527604, -1.554775717584104378, 1.208803697826433599 ) ) ;
#163626=CARTESIAN_POINT ( 'NONE',  ( 1.118581540066618141, -0.04615595083166770807, 1.941663063996822869 ) ) ;
#163627=CARTESIAN_POINT ( 'NONE',  ( 6.884150280000160826, -0.1566355309425542519, 2.263600626914013869 ) ) ;
#163629=CARTESIAN_POINT ( 'NONE',  ( 5.682414339916787682, 1.109973489246698808, -1.493480506080862469 ) ) ;
#163631=CARTESIAN_POINT ( 'NONE',  ( 6.509000000000010999, 0.004788705324892603143, 2.000274819378269786 ) ) ;
#163634=CARTESIAN_POINT ( 'NONE',  ( 1.470551405592795957, -2.082434148983134392, -0.6831980896230758216 ) ) ;
#163639=CARTESIAN_POINT ( 'NONE',  ( 1.980809073483770000, -0.08854697198140694392, -1.823669195971427071 ) ) ;
#163643=CARTESIAN_POINT ( 'NONE',  ( 6.509000000000045638, 3.691181720027385094, 2.614238911931165088 ) ) ;
#163646=CARTESIAN_POINT ( 'NONE',  ( 0.08247339995742437868, -1.868340020190910833, -0.4694531300831055742 ) ) ;
#163647=CARTESIAN_POINT ( 'NONE',  ( 4.346505277090593644, -1.939800950321630690, -0.2920161945778113055 ) ) ;
#163650=CARTESIAN_POINT ( 'NONE',  ( 3.773127072069931032, 2.063069237518061705, -0.7396954945804237180 ) ) ;
#163652=CARTESIAN_POINT ( 'NONE',  ( 2.606376076552410659, 2.069701014239883730, 0.05521581806712527740 ) ) ;
#163656=CARTESIAN_POINT ( 'NONE',  ( 3.604340556743702795, -0.1682163741436558391, 2.292568252494499692 ) ) ;
#163660=CARTESIAN_POINT ( 'NONE',  ( 6.720655732516701342, 6.039000170257122768, 2.421169367564251385 ) ) ;
#163662=CARTESIAN_POINT ( 'NONE',  ( 3.995986895217980894, -0.6101256969637807170, -1.843678354830182053 ) ) ;
#163665=CARTESIAN_POINT ( 'NONE',  ( 3.726736447152957599, 1.348887845406310682, -1.355897031963343213 ) ) ;
#163667=CARTESIAN_POINT ( 'NONE',  ( 5.069259022003644866, 0.1660796517843898534, -1.716765078168249969 ) ) ;
#163668=CARTESIAN_POINT ( 'NONE',  ( 4.680875185974167074, 1.673856063443099673, -1.124242729735332347 ) ) ;
#163669=CARTESIAN_POINT ( 'NONE',  ( 4.869944851454918400, -0.2802274231045227548, -2.281517807288702127 ) ) ;
#163671=CARTESIAN_POINT ( 'NONE',  ( 0.9267433102794273569, 1.311770220233858586, -1.774563083084364834 ) ) ;
#163674=CARTESIAN_POINT ( 'NONE',  ( 6.046140008783082109, 1.767849252625730783, 0.08484812824352709615 ) ) ;
#163676=CARTESIAN_POINT ( 'NONE',  ( 1.517954844142660464, -1.276539353255158105, -1.903739821206115623 ) ) ;
#163677=CARTESIAN_POINT ( 'NONE',  ( 0.8842106040080777163, 1.536738824236941747, -0.8168212061390681678 ) ) ;
#163679=CARTESIAN_POINT ( 'NONE',  ( 6.316381784907311392, 2.043361914081378128, 0.7923855730916643525 ) ) ;
#163680=CARTESIAN_POINT ( 'NONE',  ( 0.6492036743409674848, -0.2036512653956819019, -1.721755200737408842 ) ) ;
#163683=CARTESIAN_POINT ( 'NONE',  ( 0.8366658991775147713, -1.206067806592339142, 1.805196218089277549 ) ) ;
#163684=CARTESIAN_POINT ( 'NONE',  ( 2.079314900164643820, 1.561883299538204151, 1.275554356156020308 ) ) ;
#163686=CARTESIAN_POINT ( 'NONE',  ( 5.496683133134654398, -0.4700625557551000866, -1.868158488084943780 ) ) ;
#163688=CARTESIAN_POINT ( 'NONE',  ( 1.758359454726521998, 0.8447074013377148249, -2.054735579953733904 ) ) ;
#163695=CARTESIAN_POINT ( 'NONE',  ( 5.601031023413125531, -0.4148525734360584138, 1.690157204064596019 ) ) ;
#163696=CARTESIAN_POINT ( 'NONE',  ( 3.174217076811707727, -0.9646401420641316227, -1.708233030250068785 ) ) ;
#163700=CARTESIAN_POINT ( 'NONE',  ( 4.692800188189328203, -0.4894541170284586462, -2.208696565397149314 ) ) ;
#163703=CARTESIAN_POINT ( 'NONE',  ( 1.504421023514388889, 2.060217768730878696, 0.1034037034779722308 ) ) ;
#163705=CARTESIAN_POINT ( 'NONE',  ( 2.747247497433321861, -1.881545503785379436, 1.256212651835092231 ) ) ;
#163708=CARTESIAN_POINT ( 'NONE',  ( 2.741296213614560440, -1.383352855433259698, -1.259238407996167153 ) ) ;
#163709=CARTESIAN_POINT ( 'NONE',  ( 1.775574910200255818, 1.508776774498999718, -0.8547552410581791271 ) ) ;
#163710=CARTESIAN_POINT ( 'NONE',  ( 5.566036750361066154, -1.391122746885119499, 1.693456055751572986 ) ) ;
#163711=CARTESIAN_POINT ( 'NONE',  ( 0.07755575628183573877, -0.002876890934064984650, -2.188974970840869005 ) ) ;
#163712=CARTESIAN_POINT ( 'NONE',  ( 3.801785103514757846, -0.6297183656660889639, 2.067937956787009757 ) ) ;
#163713=CARTESIAN_POINT ( 'NONE',  ( 4.189351911999553479, -0.7420460110593477543, 1.794775118790333135 ) ) ;
#163715=CARTESIAN_POINT ( 'NONE',  ( 6.626239551081194001, 1.076695052409048614, -1.529385127534782951 ) ) ;
#163716=CARTESIAN_POINT ( 'NONE',  ( 2.125000000000001332, -2.052068128417950277, 1.216660472349556312E-13 ) ) ;
#163721=CARTESIAN_POINT ( 'NONE',  ( 5.977185442992979603, -2.006959616289708315, -0.1948445219252663840 ) ) ;
#163725=CARTESIAN_POINT ( 'NONE',  ( 3.141029808440584326, -1.609794727316344209, 0.8612202190056221784 ) ) ;
#163731=CARTESIAN_POINT ( 'NONE',  ( 0.07057728186875102117, 0.7769860399358395897, 1.864564603342239835 ) ) ;
#163732=CARTESIAN_POINT ( 'NONE',  ( 1.489100733002651555, -2.014586327357254181, -0.6619970261998938676 ) ) ;
#163737=CARTESIAN_POINT ( 'NONE',  ( 6.350472301779563900, 0.6441285046014081361, 1.957720813820832850 ) ) ;
#163738=CARTESIAN_POINT ( 'NONE',  ( 6.188124994278806135, 1.678003296889327034, 1.117835524071027598 ) ) ;
#163748=CARTESIAN_POINT ( 'NONE',  ( 6.714220164357198151, -1.617572894677368422, -1.203167480739217643 ) ) ;
#163749=CARTESIAN_POINT ( 'NONE',  ( 4.576008823784957436, -1.786506429242448624, -0.4446734633927542091 ) ) ;
#163751=CARTESIAN_POINT ( 'NONE',  ( 3.088805445243738568, -2.273621702497233166, -0.3942619731671925254 ) ) ;
#163753=CARTESIAN_POINT ( 'NONE',  ( 5.677088005223024147, -0.04676544374488527528, -2.161250967910962828 ) ) ;
#163755=CARTESIAN_POINT ( 'NONE',  ( 0.9603743489425471402, -1.756279846738018291, -0.8291483874790173125 ) ) ;
#163760=CARTESIAN_POINT ( 'NONE',  ( 4.358954191739877082, -0.8846011062542002978, 2.121510506163324372 ) ) ;
#163763=CARTESIAN_POINT ( 'NONE',  ( 3.467518583331068438, 1.825290416974333807, -0.4087457676540603990 ) ) ;
#163764=CARTESIAN_POINT ( 'NONE',  ( 0.9141475326900462273, -1.912571728325639153, 0.002704284578637640348 ) ) ;
#163767=CARTESIAN_POINT ( 'NONE',  ( 3.211752199052122503, -0.4303563718574507369, 2.164345902561148005 ) ) ;
#163773=CARTESIAN_POINT ( 'NONE',  ( 0.7902269029948695289, -1.955937164205447054, -0.2457751801602201802 ) ) ;
#163774=CARTESIAN_POINT ( 'NONE',  ( 1.642099192286674336, -1.672607260348612845, -1.589979871525433408 ) ) ;
#163775=CARTESIAN_POINT ( 'NONE',  ( 1.363640982571033611, -0.4799814350611387725, 1.902108589862220311 ) ) ;
#163776=CARTESIAN_POINT ( 'NONE',  ( 5.243062877513432696, -0.2472539590166565604, -2.047610945800168114 ) ) ;
#163783=CARTESIAN_POINT ( 'NONE',  ( 1.340952317110634118, -2.117647682651255803, -0.4779334406839957916 ) ) ;
#163785=CARTESIAN_POINT ( 'NONE',  ( 6.321814700078944860, 1.054209175812788502, -1.509406368332133930 ) ) ;
#163788=CARTESIAN_POINT ( 'NONE',  ( 1.176777557245082262, -0.04011917365428705612, -1.870279424122413658 ) ) ;
#163789=CARTESIAN_POINT ( 'NONE',  ( 5.677088005223024147, -0.04676544374488527528, -2.161250967910962828 ) ) ;
#163794=CARTESIAN_POINT ( 'NONE',  ( 2.754443878939544454, 1.898071056134968959, 0.2320119769325945103 ) ) ;
#163796=CARTESIAN_POINT ( 'NONE',  ( 2.588433964080754546, -0.3000524435079615637, -1.744042203426913629 ) ) ;
#163797=CARTESIAN_POINT ( 'NONE',  ( 0.5922591856823838929, -1.062013159134197693, 1.590055880637729402 ) ) ;
#163800=CARTESIAN_POINT ( 'NONE',  ( 5.958580499074456860, -1.820587016788511647, -0.5960958187592230173 ) ) ;
#163801=CARTESIAN_POINT ( 'NONE',  ( 6.355907380368630122, -0.6650989860433678125, 1.853973344504164622 ) ) ;
#163803=CARTESIAN_POINT ( 'NONE',  ( 1.353939357992512305, -1.539690173578952770, -1.458446627980537480 ) ) ;
#163805=CARTESIAN_POINT ( 'NONE',  ( 4.838664814796108438, 0.3202261158844340594, 1.842872994462002367 ) ) ;
#163806=CARTESIAN_POINT ( 'NONE',  ( 0.9788029507734037349, -0.04229004422508231970, -1.825371421953936757 ) ) ;
#163808=CARTESIAN_POINT ( 'NONE',  ( 4.073040751519330094, -2.058760688187323495, -0.7953439701907027981 ) ) ;
#163811=CARTESIAN_POINT ( 'NONE',  ( 2.119651477787509730, 0.3549358516394903740, -2.031769927719127455 ) ) ;
#163818=CARTESIAN_POINT ( 'NONE',  ( 4.070807014193541740, 1.466255041752505539, -1.461937513464212079 ) ) ;
#163820=CARTESIAN_POINT ( 'NONE',  ( 1.651884467337715989, 0.6291892518628816600, -2.067965918892029631 ) ) ;
#163823=CARTESIAN_POINT ( 'NONE',  ( 1.752609234595727816, 1.998021763388730720, 0.2939949305936078172 ) ) ;
#163830=CARTESIAN_POINT ( 'NONE',  ( 0.4972802279516430612, -0.2910764605805628014, 1.995268990643041640 ) ) ;
#163831=CARTESIAN_POINT ( 'NONE',  ( 4.528971853086540378, -2.003544689622422936, 0.8885388601788182239 ) ) ;
#163833=CARTESIAN_POINT ( 'NONE',  ( 3.498220628606643956, -0.9384276995785534314, 1.666209768436441419 ) ) ;
#163837=CARTESIAN_POINT ( 'NONE',  ( 2.073842424929934314, -0.8596134062341630466, 1.824128527830502833 ) ) ;
#163839=CARTESIAN_POINT ( 'NONE',  ( 0.7324523162463879578, 2.259705603777485639, 0.3848113418177290801 ) ) ;
#163841=CARTESIAN_POINT ( 'NONE',  ( 3.785938739704467260, -0.8500231715772713637, 1.500685565699668933 ) ) ;
#163846=CARTESIAN_POINT ( 'NONE',  ( 0.07536363704233049743, 0.2309889609098912111, -2.177957698420322163 ) ) ;
#163848=CARTESIAN_POINT ( 'NONE',  ( 0.4442981077158770775, -0.9790059121952739973, 1.824179074426744762 ) ) ;
#163850=CARTESIAN_POINT ( 'NONE',  ( 4.916585655956178691, -0.6154711373431708266, -1.703840371469134807 ) ) ;
#163854=CARTESIAN_POINT ( 'NONE',  ( 6.024035747493574178, -1.796918165027236780, 0.2286857708345239326 ) ) ;
#163857=CARTESIAN_POINT ( 'NONE',  ( 3.504031732436951874, -0.8880451304637152488, -2.003635182500095535 ) ) ;
#163858=CARTESIAN_POINT ( 'NONE',  ( 6.250447302982959030, -1.852220608400175994, -0.1812639614414724432 ) ) ;
#163861=CARTESIAN_POINT ( 'NONE',  ( 3.497576124367638872, -1.886684243562693597, 0.3306681954469546936 ) ) ;
#163870=CARTESIAN_POINT ( 'NONE',  ( 0.3038912542124502236, -0.5749842496362895794, 2.083749421223294540 ) ) ;
#163873=CARTESIAN_POINT ( 'NONE',  ( 2.326929888710258965, -0.002694909042751796133, 1.825762228105472840 ) ) ;
#163876=CARTESIAN_POINT ( 'NONE',  ( 3.838725952263983388, 0.2674066485093031242, 1.805754746396167176 ) ) ;
#163879=CARTESIAN_POINT ( 'NONE',  ( 2.461071540317420592, -1.587761714688111780, 1.065645112462119570 ) ) ;
#163881=CARTESIAN_POINT ( 'NONE',  ( 2.348051406654600104, -0.8447338538565999366, 1.779358369178071886 ) ) ;
#163883=CARTESIAN_POINT ( 'NONE',  ( 4.862805241732807815, 0.1868221656222105176, -1.933040885264789122 ) ) ;
#163887=CARTESIAN_POINT ( 'NONE',  ( 5.730757696090861941, 1.422813033107739988, -1.572628729999878905 ) ) ;
#163889=CARTESIAN_POINT ( 'NONE',  ( 2.543496672408153358, -1.783599581865771500, 0.6900697577220117340 ) ) ;
#163894=CARTESIAN_POINT ( 'NONE',  ( 4.037747573665031453, -1.925786081212683465, 0.5863696817766034242 ) ) ;
#163896=CARTESIAN_POINT ( 'NONE',  ( 5.232948167349782409, 0.1380416123818763163, 1.820529236867339584 ) ) ;
#163897=CARTESIAN_POINT ( 'NONE',  ( 0.8540665308606997241, -0.7467690478978536994, 1.931163149162813619 ) ) ;
#163901=CARTESIAN_POINT ( 'NONE',  ( 5.242975984329111050, -1.603930480038592510, 0.9624218375651683033 ) ) ;
#163910=CARTESIAN_POINT ( 'NONE',  ( 1.639598513223254006, 1.914365469054382540, -0.7886191548351070280 ) ) ;
#163911=CARTESIAN_POINT ( 'NONE',  ( 2.407945773967453462, -1.221608841751795405, -1.729074501506906225 ) ) ;
#163914=CARTESIAN_POINT ( 'NONE',  ( 6.977413707831522593, -0.1558467299303326059, 2.036386162850227333 ) ) ;
#163919=CARTESIAN_POINT ( 'NONE',  ( 2.150677785613893889, -1.770481577899532644, 1.455972101185269985 ) ) ;
#163921=CARTESIAN_POINT ( 'NONE',  ( 2.267699027020404490, 0.5063876334258295975, -1.844086191983687062 ) ) ;
#163924=( BOUNDED_CURVE ( )  B_SPLINE_CURVE ( 3, ( #18397, #84474, #2126, #30419 ),
 .UNSPECIFIED., .F., .T. ) 
 B_SPLINE_CURVE_WITH_KNOTS ( ( 4, 4 ),
 ( 0.5000000000000008882, 1.000000000000000000 ),
 .UNSPECIFIED. ) 
 CURVE ( )  GEOMETRIC_REPRESENTATION_ITEM ( )  RATIONAL_B_SPLINE_CURVE ( ( 0.9999999999999990008, 0.3333333333333334259, 0.3333333333333345916, 1.000000000000000222 ) ) 
 REPRESENTATION_ITEM ( '' )  );
#163925=CARTESIAN_POINT ( 'NONE',  ( 0.5100215303667603450, -0.7206480643048470691, 1.879988510241884292 ) ) ;
#163926=CARTESIAN_POINT ( 'NONE',  ( 0.9890223832832998330, 0.1386981244183866091, 1.956888703154149312 ) ) ;
#163930=CARTESIAN_POINT ( 'NONE',  ( 3.697287448106700403, -0.6068447087972194121, 2.000623839779874125 ) ) ;
#163931=CARTESIAN_POINT ( 'NONE',  ( 2.342341949348641261, 0.3848992280063111004, 1.727307115810622351 ) ) ;
#163934=CARTESIAN_POINT ( 'NONE',  ( 5.121132688944100231, -2.177879115872250360, 0.7152381750462534216 ) ) ;
#163935=CARTESIAN_POINT ( 'NONE',  ( 4.452888953083543377, 0.3777208849818362579, -1.698664142626307383 ) ) ;
#163936=B_SPLINE_CURVE_WITH_KNOTS ( 'NONE', 3,
 ( #193897, #192820, #96435, #211205, #128990, #14060, #80147, #76942, #146249, #60698, #196049, #48730, #209061, #44477, #113792, #179795, #97489, #114843, #176596, #94301, #180842, #49780, #82268, #132140, #70266, #33528, #184034, #85475, #998, #214361, #119109, #69199, #148362, #181892, #151562, #149416, #152611, #32467, #17254, #166737, #182972, #35649, #135319, #50849, #150499, #101728, #54052, #84411, #67062, #4196, #99599, #65991, #167799, #98537, #16185, #118048, #201333, #133199, #185091, #168860, #164599, #19395, #2060, #83330, #198147, #100661, #115906, #165665, #3129, #52972, #199202, #116975, #34588, #134266, #18328, #36716, #102802, #20462, #68132, #200272, #86546, #136381, #51924, #202399, #188301, #5257, #186165, #153688, #6339, #124472, #23666, #205614, #139588, #122345, #7407, #90835, #38867, #39941, #207752, #37799, #8486, #71334, #106050, #42089, #21508, #189377, #120189, #9560, #103874, #138511, #204536, #56185, #73488, #190430, #156898, #41020, #89776, #169923, #87617, #172074, #155822, #104950, #57252, #170990, #74571, #137449, #107128, #206686, #140672, #154755, #123413, #173151, #58316, #75636, #141744, #22589, #203465, #55119, #24733, #108203, #174226, #121266, #187239, #25802, #88697, #91911, #72411, #157969, #45277, #61510, #127675, #79881, #195778, #59379, #194702, #163283, #44215, #144936, #94041, #192560, #208807, #62566, #191494, #109275, #210941, #13810, #27945, #212003, #47416, #125535, #128730, #78812, #179537, #160080, #143878, #14866, #46343, #60438, #112459, #43162, #10612, #175284, #12738, #26870, #145991, #30080, #63642, #11682, #209871, #129799, #178470, #96172, #193635, #162223, #113531, #31156, #97229, #142803, #80955, #177402, #147047, #92973, #111398, #161150, #159018, #110336, #29017, #76688, #126597, #176339, #77756, #95102, #183781, #67863, #151301, #135062, #118850, #101468, #52717, #36463, #201075, #84149, #99347, #150234, #15929, #213069, #66794, #83071, #214107, #2871, #131881, #50584, #197890, #35391, #64699, #134011, #85214, #167538, #33264, #116707, #132933, #182707, #184832, #49519, #19137, #68941, #102538, #16994, #82013, #149148, #198940, #168601, #1805, #65734, #196837, #148104, #114594, #164341, #20203, #115640, #200018, #34326, #181636, #728, #86290, #51669, #117791, #100400, #130843, #48477, #180585, #32208, #165398, #98282, #166468, #18061, #202135, #186981, #37538, #89516, #6080, #154502, #25550, #3936, #40764, #173977, #153431, #123167, #7152, #90584, #74319, #58058, #106869, #206434, #190184, #140416, #122084, #23403, #38612, #155570, #169670, #152361, #53795, #72151, #188045, #88439, #105786, #189128, #138260, #73223, #54862, #70006, #121015, #204273, #39675, #136121, #124224, #55928, #41840, #203217, #172897, #21256, #185902, #171812, #137194, #24471, #139331, #156644, #205360, #119927, #56994, #8237, #107951, #103617, #87362, #5001, #71076, #104690, #170739, #22325, #194457, #207504, #92722, #62332, #60188, #66292, #157712, #142548, #77506, #93791, #159828, #112219, #16486, #91660, #12498, #198439, #76441, #177150, #126347, #10364, #26621, #94851, #9309, #141496, #28768, #46102, #192307, #32762, #82566, #75382, #160902, #111150, #220, #43967, #176094, #50085, #78571, #158768, #144691, #59124, #42906, #125281, #45037, #191243, #181140, #128491, #98842 ),
 .UNSPECIFIED., .F., .F.,
 ( 4, 1, 1, 1, 1, 1, 1, 1, 1, 1, 1, 1, 1, 1, 1, 1, 1, 1, 1, 1, 1, 1, 1, 1, 1, 1, 1, 1, 1, 1, 1, 1, 1, 1, 1, 1, 1, 1, 1, 1, 1, 1, 1, 1, 1, 1, 1, 1, 1, 1, 1, 1, 1, 1, 1, 1, 1, 1, 1, 1, 1, 1, 1, 1, 1, 1, 1, 1, 1, 1, 1, 1, 1, 1, 1, 1, 1, 1, 1, 1, 1, 1, 1, 1, 1, 1, 1, 1, 1, 1, 1, 1, 1, 1, 1, 1, 1, 1, 1, 1, 1, 1, 1, 1, 1, 1, 1, 1, 1, 1, 1, 1, 1, 1, 1, 1, 1, 1, 1, 1, 1, 1, 1, 1, 1, 1, 1, 1, 1, 1, 1, 1, 1, 1, 1, 1, 1, 1, 1, 1, 1, 1, 1, 1, 1, 1, 1, 1, 1, 1, 1, 1, 1, 1, 1, 1, 1, 1, 1, 1, 1, 1, 1, 1, 1, 1, 1, 1, 1, 1, 1, 1, 1, 1, 1, 1, 1, 1, 1, 1, 1, 1, 1, 1, 1, 1, 1, 1, 1, 1, 1, 1, 1, 1, 1, 1, 1, 1, 1, 1, 1, 1, 1, 1, 1, 1, 1, 1, 1, 1, 1, 1, 1, 1, 1, 1, 1, 1, 1, 1, 1, 1, 1, 1, 1, 1, 1, 1, 1, 1, 1, 1, 1, 1, 1, 1, 1, 1, 1, 1, 1, 1, 1, 1, 1, 1, 1, 1, 1, 1, 1, 1, 1, 1, 1, 1, 1, 1, 1, 1, 1, 1, 1, 1, 1, 1, 1, 1, 1, 1, 1, 1, 1, 1, 1, 1, 1, 1, 1, 1, 1, 1, 1, 1, 1, 1, 1, 1, 1, 1, 1, 1, 1, 1, 1, 1, 1, 1, 1, 1, 1, 1, 1, 1, 1, 1, 1, 1, 1, 1, 1, 1, 1, 1, 1, 1, 1, 1, 1, 1, 1, 1, 1, 1, 1, 1, 1, 1, 1, 1, 1, 1, 1, 1, 1, 1, 1, 1, 1, 1, 1, 1, 1, 1, 1, 1, 1, 1, 1, 1, 1, 1, 1, 1, 1, 1, 1, 1, 1, 1, 1, 1, 1, 1, 1, 1, 1, 1, 1, 1, 1, 1, 1, 1, 1, 1, 1, 1, 1, 1, 1, 1, 1, 1, 4 ),
 ( 0.000000000000000000, 0.002600154539856827565, 0.005208839490340733125, 0.007813275572638063438, 0.01041576435696154809, 0.01302135854728175661, 0.01562456786780599440, 0.01822932761385693060, 0.02083324874646079461, 0.02343713590986815087, 0.02604192363554110393, 0.02864519953128016536, 0.03125045858075606309, 0.03385359029894085409, 0.03645870005206112291, 0.03906221013386886737, 0.04166657361863843057, 0.04427092160485841116, 0.04687444683368256759, 0.04947954930481244379, 0.05208268618576387260, 0.05468794662449812799, 0.05729120536831356497, 0.05989601299138836571, 0.06249988999545372931, 0.06510378435733490954, 0.06770858081828938502, 0.07031184975024351580, 0.07291710771924506118, 0.07552024060328325905, 0.07812534933470290099, 0.08072885870519988516, 0.08333322157114708695, 0.08593756915452624434, 0.08854109358761537429, 0.09114619558392741960, 0.09374933183658358538, 0.09635459170495851156, 0.09895784999447977681, 0.1015626569530685003, 0.1041665336043751944, 0.1067704272253022224, 0.1093752232910748662, 0.1119784915631429623, 0.1145837490571069844, 0.1171868814509031548, 0.1197919896162490533, 0.1223954986480551566, 0.1249998608471283579, 0.1276042081199000311, 0.1302077318846941445, 0.1328128334964322199, 0.1354159692195129883, 0.1380212286176593917, 0.1406244865514671982, 0.1432292929439143159, 0.1458331693420142072, 0.1484370623210626572, 0.1510418580899855479, 0.1536451258019158050, 0.1562503829188521542, 0.1588535149221727560, 0.1614586226195926788, 0.1640621314121666618, 0.1666664930431534797, 0.1692708401040713406, 0.1718743633000545112, 0.1744794646253388370, 0.1770825999186152189, 0.1796878589445308205, 0.1822911166222762891, 0.1848959225469683498, 0.1874997987909985397, 0.1901036912273387502, 0.1927084867977703619, 0.1953117540492253223, 0.1979170108871138589, 0.2005201425997050479, 0.2031252499273119572, 0.2057287585800815777, 0.2083331197417381819, 0.2109374666895270922, 0.2135409894161511279, 0.2161460905530729892, 0.2187492255162853672, 0.2213544842679382729, 0.2239577417892439637, 0.2265625473445374016, 0.2291664235336075273, 0.2317703155263790282, 0.2343751109966507595, 0.2369783778872631419, 0.2395836345440564008, 0.2421867660656364940, 0.2447918731215153465, 0.2473953817338825356, 0.2499997425249363969, 0.2526040894582959329, 0.2552076118149841921, 0.2578127128616094499, 0.2604158475944712281, 0.2630211061698037311, 0.2656243636342671688, 0.2682291689184919115, 0.2708330451516883230, 0.2734369368000036937, 0.2760417322684234342, 0.2786449988978000336, 0.2812502554714267355, 0.2838533869016899303, 0.2864584937839013135, 0.2890620024552456591, 0.2916663629743991848, 0.2942707099920074398, 0.2968742320781582733, 0.2994793331325310004, 0.3020824677347322962, 0.3046877262316646240, 0.3072909837388622112, 0.3098957888503254821, 0.3124996652267145181, 0.3151035566296633839, 0.3177083521945192612, 0.3203116186622446127, 0.3229168752506134110, 0.3255200066892336430, 0.3281251134958176330, 0.3307286223255002655, 0.3333329826714347410, 0.3359373298719517953, 0.3385408517869427647, 0.3411459529470890484, 0.3437490875183005223, 0.3463543460347343617, 0.3489576036842249041, 0.3515624087212146920, 0.3541662853398466204, 0.3567701765964986227, 0.3593749723560626386, 0.3619782387617029862, 0.3645834954627060198, 0.3671866270093405715, 0.3697917338383204244, 0.3723952429256875973, 0.3749996031970665444, 0.3776039506791386557, 0.3802074725223298923, 0.3828125738862612759, 0.3854157085261381011, 0.3880209671599602617, 0.3906242250512887426, 0.3932290301120778819, 0.3958329070719905363, 0.3984367982813996067, 0.4010415943339316058, 0.4036448607770379837, 0.4062501176885546794, 0.4088532494428480657, 0.4114583563922335485, 0.4140618658366201910, 0.4166662261320933647, 0.4192705739943561327, 0.4218740958650940009, 0.4244791975308115917, 0.4270823323389966175, 0.4296875911880828069, 0.4322908494207843844, 0.4348956546036337745, 0.4374995320038561619, 0.4401034232650644085, 0.4427082197088152427, 0.4453114862889279713, 0.4479167435088288185, 0.4505198755704162283, 0.4531249827382076711, 0.4557284926389418844, 0.4583328530571487147, 0.4609372013982309668, 0.4635407233958523388, 0.4661458254613498609, 0.4687489605374778323, 0.4713542196996960976, 0.4739574783732994345, 0.4765622837764619812, 0.4791661617160185016, 0.4817700531280592058, 0.4843748500612748420, 0.4869781168779269698, 0.4895833745040767959, 0.4921865069725880892, 0.4947916144567798824, 0.4973951249131855490, 0.4999994855527590265, 0.5026038344712867589, 0.5052073566951218453, 0.5078124592583899144, 0.5104155947020908579, 0.5130208542753056378, 0.5156241134893367883, 0.5182289192110610676, 0.5208327977889742888, 0.5234366894508762913, 0.5260414869718011976, 0.5286447541245218318, 0.5312500122547839654, 0.5338531452298473923, 0.5364582531284315392, 0.5390617642398328746, 0.5416661251994032700, 0.5442704747940029231, 0.5468739973433798252, 0.5494791005024090014, 0.5520822364133124438, 0.5546874964953879550, 0.5572907563493740835, 0.5598955624879079496, 0.5624994418032033261, 0.5651033338139942463, 0.5677081320208752224, 0.5703113996091939697, 0.5729166583414331271, 0.5755197919226788805, 0.5781249003336490500, 0.5807284121993739889, 0.5833327735775721834, 0.5859371239468746939, 0.5885406469211225122, 0.5911457507739076300, 0.5937488872516457628, 0.5963541479404496082, 0.5989574085339228748, 0.6015622151875171797, 0.6041660953392257172, 0.6067699877979360057, 0.6093747867890261238, 0.6119780549124759217, 0.6145833143445629254, 0.6171864486316270826, 0.6197915576529816617, 0.6223950703723655220, 0.6249994322678273928, 0.6276037835104713025, 0.6302073070089242446, 0.6328124116534677990, 0.6354155487976793637, 0.6380208101910863627, 0.6406240716235875876, 0.6432288788904997334, 0.6458327599776627626, 0.6484366529833293091, 0.6510414528568908565, 0.6536447216150126360, 0.6562499818448275235, 0.6588531169373553764, 0.6614582266671018562, 0.6640617403394915019, 0.6666661028508605868, 0.6692704550654967610, 0.6718739791874978051, 0.6744790847218130603, 0.6770822226321474568, 0.6796874848280434200, 0.6822907471991253026, 0.6848955551776233497, 0.6874994372992955238, 0.6901033309509650993, 0.6927081318052739078, 0.6953114012976200353, 0.6979166624230551674, 0.7005197984207056638, 0.7031249089568636368, 0.7057284236816204759, 0.7083327869075525252, 0.7109371401928469281, 0.7135406650377511539, 0.7161457715598668061, 0.7187489103359874232, 0.7213541734322722609, 0.7239574368415039318, 0.7265622456298695964, 0.7291661288851226663, 0.7317700232818561412, 0.7343748252152053624, 0.7369780955413426371, 0.7395833576603073611, 0.7421864946627563242, 0.7447916061033615920, 0.7473951219798656842, 0.7499994860190324353, 0.7526038404736700160, 0.7552073661408488237, 0.7578124737488122209, 0.7604156134903999886, 0.7630208775849919300, 0.7656241421319622820, 0.7682289518284949326, 0.7708328363164217434, 0.7734367315572975299, 0.7760415346680002990, 0.7786448059275148381, 0.7812500691379388185, 0.7838532072448821664, 0.7864583196879902927, 0.7890618368156444573, 0.7916662017667361884, 0.7942705574894247667, 0.7968740840782696511, 0.7994791928701499018, 0.8020823336769073997, 0.8046875988677468783, 0.8072908646520678966, 0.8098956753550886623, 0.8124995611748068169, 0.8151034573589240884, 0.8177082617453185209, 0.8203115340378186460, 0.8229167984376549727, 0.8255199377488137147, 0.8281250512925039109, 0.8307285697707365024, 0.8333329357324672504, 0.8359372928219411802, 0.8385408204318668401, 0.8411459305057594760, 0.8437490724774151518, 0.8463543388624672481, 0.8489576059837783406, 0.8515624177916331083, 0.8541663050422881875, 0.8567702022687715413, 0.8593750080292236193, 0.8619782814543437421, 0.8645835471415733720, 0.8671866877566964948, 0.8697918024990743957, 0.8723953224273439666, 0.8749996894984543028, 0.8776040480534781363, 0.8802075767839265819, 0.8828126882379567775, 0.8854158314742670566, 0.8880210991515266050, 0.8906243677094983768, 0.8932291807205616774, 0.8958330695013316802, 0.8984369678693342465, 0.9010417751022415933, 0.9036450497596462128, 0.9062503168322812996, 0.9088534588511494317, 0.9114585748903522022, 0.9140620963681507227, 0.9166664646474114164, 0.9192708247667824573, 0.9218743547172278952, 0.9244794676495572405, 0.9270826122503010858, 0.9296878813177945622, 0.9322911514121841048, 0.9348959657248061550, 0.9374998561347748227, 0.9401037557438677306, 0.9427085645475906661, 0.9453118405358371668, 0.9479171090940153865, 0.9505202526155902554, 0.9531253700418979014, 0.9557288931959170286, 0.9583332627756006028, 0.9609376244112938226, 0.9635411559431285022, 0.9661462708106475228, 0.9687494151757961580, 0.9713546862302190332, 0.9739579640138142924, 0.9765627705390533819, 0.9791666547386930208, 0.9817705986233274951, 0.9843753609709087193, 0.9869785915570626900, 0.9895841932699848131, 0.9921866851465583892, 0.9947911401134668097, 0.9973998225951543617, 1.000000000000000000 ),
 .UNSPECIFIED. ) ;
#163939=CARTESIAN_POINT ( 'NONE',  ( 3.919074646851735455, 0.6231337533108800564, 1.618193163429545223 ) ) ;
#163941=CARTESIAN_POINT ( 'NONE',  ( 4.492743645254620333, 2.128474237214292852, 0.4277247895240059994 ) ) ;
#163943=CARTESIAN_POINT ( 'NONE',  ( 6.210172754313918908, 1.157103754073171675, -1.651340222398114843 ) ) ;
#163944=CARTESIAN_POINT ( 'NONE',  ( 6.750000000000005329, 3.748112931134527976E-13, 1.999999999999984901 ) ) ;
#163946=CARTESIAN_POINT ( 'NONE',  ( 3.030207491816420795, 1.071487476811390449, -1.600714694641630853 ) ) ;
#163948=CARTESIAN_POINT ( 'NONE',  ( 5.467086432746695479, -1.751203904306109838, 1.366580491753234039 ) ) ;
#163950=CARTESIAN_POINT ( 'NONE',  ( 6.983263157960366563, -0.003091553303710344557, 1.945923119799706669 ) ) ;
#163957=CARTESIAN_POINT ( 'NONE',  ( 0.01820432788856435335, -1.842448466851685840, 0.8197770699841927522 ) ) ;
#163959=CARTESIAN_POINT ( 'NONE',  ( 4.932111759923301975, 1.184877397895794493, 1.688235060362786255 ) ) ;
#163964=CARTESIAN_POINT ( 'NONE',  ( 5.430866635118035468, 0.1366067128489474591, 1.865587184704711632 ) ) ;
#163965=CARTESIAN_POINT ( 'NONE',  ( 5.098194074801078557, -0.2466363661708069477, 1.716370243172520516 ) ) ;
#163966=CARTESIAN_POINT ( 'NONE',  ( 4.317713577401066871, 1.066398661528572989, -1.375396103214795218 ) ) ;
#163968=CARTESIAN_POINT ( 'NONE',  ( 1.980407754855911140, -2.249062817636026779, -0.4427264618648701910 ) ) ;
#163970=CARTESIAN_POINT ( 'NONE',  ( 0.8844010234979463592, 1.624802019249080853, -0.8659260420235401767 ) ) ;
#163972=CARTESIAN_POINT ( 'NONE',  ( 1.940199132888191791, 1.805219978825555627, 0.2711003711317952480 ) ) ;
#163973=CARTESIAN_POINT ( 'NONE',  ( 2.690077459517980163, 1.704938782060089864, 1.076316768488336351 ) ) ;
#163974=CARTESIAN_POINT ( 'NONE',  ( 1.113517231965298837, -2.137359700923711081, 0.4831916906855234228 ) ) ;
#163976=CARTESIAN_POINT ( 'NONE',  ( 3.997179113411051254, 1.780275165862042153, -1.124711807175354350 ) ) ;
#163978=CARTESIAN_POINT ( 'NONE',  ( 1.205626512970816355, -1.630946839658468983, -1.275175305487465049 ) ) ;
#163981=CARTESIAN_POINT ( 'NONE',  ( 3.141385665567609564, 0.05408136815227351790, 2.119969838212852675 ) ) ;
#163983=CARTESIAN_POINT ( 'NONE',  ( 6.692070433991195166, -0.7751425012093198230, 1.651373049820707317 ) ) ;
#163990=CARTESIAN_POINT ( 'NONE',  ( 3.392836290029502155, -1.947660480455270404, -0.5347636834307776255 ) ) ;
#163991=CARTESIAN_POINT ( 'NONE',  ( 0.6046866811788155216, -0.7097959115549393738, -1.982883793842766362 ) ) ;
#163994=CARTESIAN_POINT ( 'NONE',  ( 5.207777014082533462, 0.5861155943000575519, -1.766266804033526094 ) ) ;
#163999=CARTESIAN_POINT ( 'NONE',  ( 6.508673417949426110, 1.528841652884159963, -1.382195874861185336 ) ) ;
#164003=CARTESIAN_POINT ( 'NONE',  ( 3.286226705615200139, -1.671546763608670272, 0.4602933761382789202 ) ) ;
#164004=CARTESIAN_POINT ( 'NONE',  ( 1.077605773158099023, -1.697095445269660496, -0.3847248992609655915 ) ) ;
#164005=CARTESIAN_POINT ( 'NONE',  ( 0.3589920806752691096, 0.8874099113769757796, 2.130322803234908857 ) ) ;
#164008=CARTESIAN_POINT ( 'NONE',  ( 2.231779466116891708, -1.343800923419868010, -1.562491722542774797 ) ) ;
#164011=CARTESIAN_POINT ( 'NONE',  ( 1.493517298738750609, 1.942243344100362590, 0.5404107738020345053 ) ) ;
#164012=CARTESIAN_POINT ( 'NONE',  ( 6.825078400183544503, 3.684911640780349718, 2.658296617506946458 ) ) ;
#164015=CARTESIAN_POINT ( 'NONE',  ( 1.709780583834107803, -1.956794704801574358, 0.2394988650771395777 ) ) ;
#164017=CARTESIAN_POINT ( 'NONE',  ( 4.640819915729988310, 1.831716588661407963, 0.5496940206762624959 ) ) ;
#164019=CARTESIAN_POINT ( 'NONE',  ( 5.742855475442601332, 0.4270144693867898300, 2.165010647329483895 ) ) ;
#164023=CARTESIAN_POINT ( 'NONE',  ( 0.3287785284849250034, 1.391158174000119097, -1.464406657780653820 ) ) ;
#164025=CARTESIAN_POINT ( 'NONE',  ( 4.120403395486138542, -1.183043222452788257, -1.981120964393435768 ) ) ;
#164026=CARTESIAN_POINT ( 'NONE',  ( 4.510177812457000002, 1.961482754637720927, -0.04604004567236585910 ) ) ;
#164028=CARTESIAN_POINT ( 'NONE',  ( 1.920681792755131845, -1.391007931628859939, 1.383589105726056756 ) ) ;
#164032=CARTESIAN_POINT ( 'NONE',  ( -0.1353153266233823870, -2.055576600424202649, -0.5074567962913156816 ) ) ;
#164035=CARTESIAN_POINT ( 'NONE',  ( 1.007454599746326895, -0.8259622865525710900, -1.645551850779983116 ) ) ;
#164037=CARTESIAN_POINT ( 'NONE',  ( 3.749033319061449543, -0.4183670367851847205, -2.130223169982926379 ) ) ;
#164039=CARTESIAN_POINT ( 'NONE',  ( 2.021885665735908333, -0.4598567139443253682, 2.069992740399699382 ) ) ;
#164044=CARTESIAN_POINT ( 'NONE',  ( 2.495449868850362574, 1.590812333473600626, 1.309970014422021212 ) ) ;
#164046=CARTESIAN_POINT ( 'NONE',  ( -0.1296875068448159751, 0.001480089298542403009, -1.826395826379861864 ) ) ;
#164051=CARTESIAN_POINT ( 'NONE',  ( 1.775094195334154135, -2.148033089049032895, -0.7103491116851842202 ) ) ;
#164053=CARTESIAN_POINT ( 'NONE',  ( 1.652323331381430283, 1.792179557038487303, 0.2633440673391762576 ) ) ;
#164054=CARTESIAN_POINT ( 'NONE',  ( 1.885809660653874120, -1.915224419731532901, 0.05109022710406836698 ) ) ;
#164055=CARTESIAN_POINT ( 'NONE',  ( 3.648938843998358106, -0.4010542052625790110, -2.030977206718207473 ) ) ;
#164057=CARTESIAN_POINT ( 'NONE',  ( 1.217580299722145210, -1.923910348332603881, 0.4297500124877791650 ) ) ;
#164058=CARTESIAN_POINT ( 'NONE',  ( 5.531840760993587125, -1.223730149660817501, -1.487915846976423984 ) ) ;
#164059=CARTESIAN_POINT ( 'NONE',  ( 1.559632053384899741, -1.981161107035840141, -1.183202272445786907 ) ) ;
#164062=CARTESIAN_POINT ( 'NONE',  ( 5.055161771162819839, 1.716784339331741682, -1.143088790766825236 ) ) ;
#164067=CARTESIAN_POINT ( 'NONE',  ( 6.686557493494803772, -2.064527365108769885, -0.4147649638114383475 ) ) ;
#164069=CARTESIAN_POINT ( 'NONE',  ( 4.991577004318280331, 1.598001195387260154, 1.455802845438579407 ) ) ;
#164070=CARTESIAN_POINT ( 'NONE',  ( 5.496742197731416368, -1.970900515782060936, -0.4404336293717215356 ) ) ;
#164078=CARTESIAN_POINT ( 'NONE',  ( 3.467982673848205355, -0.9896861206786079501, 1.756853968756578066 ) ) ;
#164082=CARTESIAN_POINT ( 'NONE',  ( 4.750933126423753095, -1.738186171353903742, 1.284983810367075208 ) ) ;
#164087=CARTESIAN_POINT ( 'NONE',  ( 4.991814629660241920, -2.006445540622634915, 0.2004526995145126111 ) ) ;
#164089=CARTESIAN_POINT ( 'NONE',  ( 0.9083514600924915694, 1.308824770132447135, -1.123559637378883203 ) ) ;
#164094=CARTESIAN_POINT ( 'NONE',  ( 6.380143124955812262, -1.000617425381218561, 1.580232162242324545 ) ) ;
#164095=CARTESIAN_POINT ( 'NONE',  ( 1.172521868268823875, 0.8179054604866965450, 1.839630344048637678 ) ) ;
#164096=CARTESIAN_POINT ( 'NONE',  ( 3.048105859194950362, 0.7956334958073747465, -2.058523145315640956 ) ) ;
#164100=CARTESIAN_POINT ( 'NONE',  ( 2.227333921462580246, 1.895369558270381338, 0.9509248740046101211 ) ) ;
#164101=CARTESIAN_POINT ( 'NONE',  ( 2.284780001213771783, 1.617805504991537635, -1.203372706716873575 ) ) ;
#164102=CARTESIAN_POINT ( 'NONE',  ( 2.830093135299842189, -0.8964878685940536052, -1.574152086365911529 ) ) ;
#164108=CARTESIAN_POINT ( 'NONE',  ( 0.02247297916271525850, 0.3300846716227764932, 1.886903735308493424 ) ) ;
#164109=CARTESIAN_POINT ( 'NONE',  ( 0.1747926744264660381, 0.006858446013176254172, -1.855468577918440776 ) ) ;
#164116=CARTESIAN_POINT ( 'NONE',  ( 4.698454014923811428, 1.387101836239763131, -1.463925544105355803 ) ) ;
#164117=CARTESIAN_POINT ( 'NONE',  ( 5.612251347527116074, -0.9680786960581323486, -1.932885698521320306 ) ) ;
#164120=CARTESIAN_POINT ( 'NONE',  ( 1.828540510153942922, -1.004066958311781832, -1.867862179375394005 ) ) ;
#164122=CARTESIAN_POINT ( 'NONE',  ( 2.952367129307902793, 0.6606739728568145065, 1.857499748845674370 ) ) ;
#164126=CARTESIAN_POINT ( 'NONE',  ( 0.5376586404672692998, 1.932363751568724641, -0.7437053376125392079 ) ) ;
#164127=CARTESIAN_POINT ( 'NONE',  ( 1.130689739129210336, -1.755767597885007136, 0.8300169520328912753 ) ) ;
#164132=CARTESIAN_POINT ( 'NONE',  ( 2.132869701138325969, -1.867042483574256728, 0.9408474824332532238 ) ) ;
#164136=CARTESIAN_POINT ( 'NONE',  ( 6.199862383955294654, 1.322219258337012704, 1.381733411008022383 ) ) ;
#164138=CARTESIAN_POINT ( 'NONE',  ( 3.985166894971280183, -0.2153072539897090687, -2.196357064762343825 ) ) ;
#164139=CARTESIAN_POINT ( 'NONE',  ( 1.852830919558448697, 0.6925466627333075609, 2.095365425716289032 ) ) ;
#164140=CARTESIAN_POINT ( 'NONE',  ( 0.08246951281144777879, -1.249137507218839094, 1.448023666807838117 ) ) ;
#164143=CARTESIAN_POINT ( 'NONE',  ( 4.650872726564402981, -0.4503784926754761386, -2.020631409805350387 ) ) ;
#164145=CARTESIAN_POINT ( 'NONE',  ( 1.200320640528436789, -2.161883444890321915, 0.0006282887012112879947 ) ) ;
#164146=CARTESIAN_POINT ( 'NONE',  ( 3.245827600587628758, 2.191739723504753101, -0.002129563554123526260 ) ) ;
#164152=CARTESIAN_POINT ( 'NONE',  ( 0.1588275700346117869, 1.163271727376416376, 1.646837250247008777 ) ) ;
#164155=CARTESIAN_POINT ( 'NONE',  ( 5.014543041041934046, 0.7873211189074662553, 1.914903133430221338 ) ) ;
#164156=CARTESIAN_POINT ( 'NONE',  ( 5.694942756591524713, 1.867452007164069672, 0.9975914146606623678 ) ) ;
#164157=AXIS2_PLACEMENT_3D ( 'NONE', #45855, #164911, #99919 ) ;
#164160=CARTESIAN_POINT ( 'NONE',  ( 4.311352223092364433, -1.634989290354519342, -1.097634987119990191 ) ) ;
#164161=CARTESIAN_POINT ( 'NONE',  ( 5.982448691606671254, -0.3306924304021444661, -2.268186543139012024 ) ) ;
#164162=CARTESIAN_POINT ( 'NONE',  ( 3.896943178251357054, 1.541351720387572843, -0.9781566455248568159 ) ) ;
#164168=CARTESIAN_POINT ( 'NONE',  ( 5.554944837187737683, 0.3969321943368699368, 1.973527061375530023 ) ) ;
#164170=CARTESIAN_POINT ( 'NONE',  ( 6.486976479784771321, -2.298278054978039275, 0.05155775693151467415 ) ) ;
#164171=CARTESIAN_POINT ( 'NONE',  ( 3.924618397835403893, -1.320764108826902428, 1.450678906977073579 ) ) ;
#164176=CARTESIAN_POINT ( 'NONE',  ( 0.8024204784428441428, 1.580594792060415088, -1.368634514759473397 ) ) ;
#164177=CARTESIAN_POINT ( 'NONE',  ( 6.157089704101026406, -1.520188931036812185, -0.9060637366671944193 ) ) ;
#164179=CARTESIAN_POINT ( 'NONE',  ( 6.456980378258257325, 0.3295113258894696862, -1.913641714292084073 ) ) ;
#164180=CARTESIAN_POINT ( 'NONE',  ( 2.115410589380119610, -2.125216164159982046, 0.5342070311455533460 ) ) ;
#164181=CARTESIAN_POINT ( 'NONE',  ( 1.100653536641453156, -0.4241352534964801801, 1.687842229193817989 ) ) ;
#164183=CARTESIAN_POINT ( 'NONE',  ( 1.593959923740532414, -1.716304196509855329, -0.1716357895808154899 ) ) ;
#164184=CARTESIAN_POINT ( 'NONE',  ( 2.156058135970494227, 0.9403143569667195001, 1.979733194660021622 ) ) ;
#164185=CARTESIAN_POINT ( 'NONE',  ( 4.354274438496381627, 2.206422198305586058, -0.05263853172451230661 ) ) ;
#164186=CARTESIAN_POINT ( 'NONE',  ( 0.9894204570943666566, 0.1578702891864954827, 2.165348367497366144 ) ) ;
#164187=CARTESIAN_POINT ( 'NONE',  ( 0.4338677482375961070, 0.9413943332680120291, -1.564114433284753636 ) ) ;
#164188=CARTESIAN_POINT ( 'NONE',  ( 2.343091305525629497, -1.844686447908544746, -1.039184121536258942 ) ) ;
#164191=CARTESIAN_POINT ( 'NONE',  ( 2.577988946098773049, -1.175687941515238588, 1.967785589457039741 ) ) ;
#164194=CARTESIAN_POINT ( 'NONE',  ( 5.022253332556455341, -2.210719170837057934, 0.2167383629448139670 ) ) ;
#164202=CARTESIAN_POINT ( 'NONE',  ( 3.287732575140737801, 1.587837554856496691, -1.242726844152845178 ) ) ;
#164204=CARTESIAN_POINT ( 'NONE',  ( 1.006769942787159033, 0.5948965838462864086, 1.974949077847313328 ) ) ;
#164209=CARTESIAN_POINT ( 'NONE',  ( 3.855584222106961612, 2.174980185927982923, -0.2676557845137442215 ) ) ;
#164210=CARTESIAN_POINT ( 'NONE',  ( 2.162732623366144136, 1.242727809108796322, 1.587836805404294171 ) ) ;
#164211=CARTESIAN_POINT ( 'NONE',  ( 1.469984750362408388, -1.748608032326857353, -0.5769476384821782267 ) ) ;
#164214=CARTESIAN_POINT ( 'NONE',  ( 4.840742024777624053, 0.3130767520662172121, 1.798364180563789327 ) ) ;
#164215=CARTESIAN_POINT ( 'NONE',  ( 5.994767569012836361, -2.000857541758268354, 0.2496038112331094849 ) ) ;
#164217=CARTESIAN_POINT ( 'NONE',  ( 4.680719170653036443, -2.193521624435289752, -0.5540208151394544478 ) ) ;
#164219=CARTESIAN_POINT ( 'NONE',  ( 0.6628876427188118425, -1.523960678047535877, 1.453889595790233802 ) ) ;
#164221=CARTESIAN_POINT ( 'NONE',  ( 4.580570967453869713, 1.276285970795057345, -1.630082184409971324 ) ) ;
#164229=CARTESIAN_POINT ( 'NONE',  ( 1.459403507577087700, -1.788631592985808538, 1.138920039206146928 ) ) ;
#164230=CARTESIAN_POINT ( 'NONE',  ( 1.477127009259255219, -1.566406750307091533, 1.575387012651897622 ) ) ;
#164234=CARTESIAN_POINT ( 'NONE',  ( 3.033595934319989418, 1.863777508880835487, -0.6128360024686765328 ) ) ;
#164240=CARTESIAN_POINT ( 'NONE',  ( 2.057031522680652369, 0.4693188842763912905, 2.067847215655476134 ) ) ;
#164242=CARTESIAN_POINT ( 'NONE',  ( 5.723093114104088386, -1.772945450647535948, -0.8403097561825512152 ) ) ;
#164243=CARTESIAN_POINT ( 'NONE',  ( 3.502937704049163159, 1.705309618848281472, -1.328393843302433153 ) ) ;
#164244=CARTESIAN_POINT ( 'NONE',  ( 2.507154105146496725, -1.820902139252629448, 0.2722148935128121394 ) ) ;
#164247=CARTESIAN_POINT ( 'NONE',  ( 4.804519235412550771, 1.516407796731779722, 0.8538163389757484900 ) ) ;
#164252=CARTESIAN_POINT ( 'NONE',  ( 1.622176833581047806, -1.201014165160016356, -1.797165035535647659 ) ) ;
#164253=CARTESIAN_POINT ( 'NONE',  ( 4.411482401463855396, 0.5350073857553553358, 1.943773423102819864 ) ) ;
#164255=CARTESIAN_POINT ( 'NONE',  ( 1.815512348505427642, -0.2646426633909418347, 2.145385951886819242 ) ) ;
#164256=CARTESIAN_POINT ( 'NONE',  ( 2.829319923597766628, -1.840754522440336327, 0.7060794426061881568 ) ) ;
#164257=CARTESIAN_POINT ( 'NONE',  ( 2.835173002801576914, -1.651343842416473917, -1.157098616274463865 ) ) ;
#164259=CARTESIAN_POINT ( 'NONE',  ( 3.474105628906531518, -1.872487600191057755, -0.5149888314514885490 ) ) ;
#164268=CARTESIAN_POINT ( 'NONE',  ( 1.184930176456780115, -2.153272645635353033, -0.4822455307981614592 ) ) ;
#164271=CARTESIAN_POINT ( 'NONE',  ( 5.664887785843471413, 1.487927489739075959, -1.278645765186999128 ) ) ;
#164272=CARTESIAN_POINT ( 'NONE',  ( 3.503210936237437068, -0.1516218309994079028, 2.111938774394610974 ) ) ;
#164274=CARTESIAN_POINT ( 'NONE',  ( 0.07479286986302942364, 7.629137130509078268, -2.455503679634089220 ) ) ;
#164275=CARTESIAN_POINT ( 'NONE',  ( 4.593604542485023146, -1.840816577468977533, -0.04244875611379012037 ) ) ;
#164279=CARTESIAN_POINT ( 'NONE',  ( 5.431924468521282634, -2.068440459917933794, 0.4666711972392265650 ) ) ;
#164284=CARTESIAN_POINT ( 'NONE',  ( 0.2157906144764632494, -2.021207876486079691, 0.4015242071495705445 ) ) ;
#164286=CARTESIAN_POINT ( 'NONE',  ( 0.5021285002191768765, 1.855665429770089636, 0.1426183976328247727 ) ) ;
#164287=CARTESIAN_POINT ( 'NONE',  ( 3.438839575862782549, -1.396446551253815782, -1.200180114512699792 ) ) ;
#164292=CARTESIAN_POINT ( 'NONE',  ( 3.826972293661185187, 2.095320012007126476, 0.6930106488920934060 ) ) ;
#164293=CARTESIAN_POINT ( 'NONE',  ( 4.569752015286022484, 2.196007708051894269, -0.5437172964835658151 ) ) ;
#164295=CARTESIAN_POINT ( 'NONE',  ( 4.588045372560112689, 1.048790434826195384, 1.476901585074356316 ) ) ;
#164296=CARTESIAN_POINT ( 'NONE',  ( 5.594928181924037069, 1.692849881775596366, 0.8967378362389683000 ) ) ;
#164298=CARTESIAN_POINT ( 'NONE',  ( 5.752782329262380756, -1.473788443143897675, 1.151991621687727507 ) ) ;
#164299=CARTESIAN_POINT ( 'NONE',  ( 6.461375281700972195, 1.547960615844719667, 1.032782510450443114 ) ) ;
#164302=CARTESIAN_POINT ( 'NONE',  ( 6.350471991779750525, 0.5597436608810264502, 1.679089333223187985 ) ) ;
#164303=CARTESIAN_POINT ( 'NONE',  ( 1.341030165941111241, -1.731997234073547220, -1.032477317303444053 ) ) ;
#164305=CARTESIAN_POINT ( 'NONE',  ( 3.176497522518567873, -1.254329069944852382, 1.691643483388256985 ) ) ;
#164310=CARTESIAN_POINT ( 'NONE',  ( 1.740496097130298958, 1.159487406938706888, -1.653631796535762755 ) ) ;
#164313=CARTESIAN_POINT ( 'NONE',  ( 3.392016793147753617, -0.8794390384766533897, 1.974801309016629869 ) ) ;
#164314=CARTESIAN_POINT ( 'NONE',  ( 6.620655732516673275, 1.290356161719278028, 1.942653802560645460 ) ) ;
#164323=CARTESIAN_POINT ( 'NONE',  ( 0.8729168595149154886, -0.05911722906676297740, -2.190938979806676734 ) ) ;
#164325=CARTESIAN_POINT ( 'NONE',  ( 1.534417833908331863, 1.113959020207640593, -1.969227013157865303 ) ) ;
#164333=CARTESIAN_POINT ( 'NONE',  ( 3.497073372749549769, 1.393195626148287403, 1.091155617269304878 ) ) ;
#164334=CARTESIAN_POINT ( 'NONE',  ( 6.458075443588827014, 2.201329523236052577, -0.1558686762383256763 ) ) ;
#164339=CARTESIAN_POINT ( 'NONE',  ( 4.798453934790239295, 1.388474963651475269, -1.462457531588717830 ) ) ;
#164341=CARTESIAN_POINT ( 'NONE',  ( 2.324885834233282988, -0.002380789299309681549, 1.870836310375329381 ) ) ;
#164342=CARTESIAN_POINT ( 'NONE',  ( 2.957943426865859760, -0.6537446763684885420, 1.964363857337739105 ) ) ;
#164344=CARTESIAN_POINT ( 'NONE',  ( 1.423922367354793606, -1.897583212610975734, 0.2371896777705190806 ) ) ;
#164352=CARTESIAN_POINT ( 'NONE',  ( 0.9492982845318719276, -1.727743609841876138, 0.8201845251225792222 ) ) ;
#164354=CARTESIAN_POINT ( 'NONE',  ( 3.016010921186715432, 1.952665002612500533, -0.1895750030070641190 ) ) ;
#164355=CARTESIAN_POINT ( 'NONE',  ( 0.2278875137335881484, -1.799627942332830965, -0.9090566646320766830 ) ) ;
#164359=CARTESIAN_POINT ( 'NONE',  ( 6.661403070661808812, 0.3393488462513394310, -1.941789718247180607 ) ) ;
#164361=CARTESIAN_POINT ( 'NONE',  ( 1.635022589147613115, 1.879998146294536543, 0.7206230416607807276 ) ) ;
#164363=CARTESIAN_POINT ( 'NONE',  ( 1.704857254432812219, 1.976886250939764889, 0.7584849220025058347 ) ) ;
#164366=CARTESIAN_POINT ( 'NONE',  ( 3.262232429473245432, -2.068111870375147987, 0.09887451149894616043 ) ) ;
#164368=CARTESIAN_POINT ( 'NONE',  ( 5.595677694052432649, -2.090823719441712747, -0.0008997866532325231618 ) ) ;
#164370=CARTESIAN_POINT ( 'NONE',  ( 4.489149150750438189, 1.630474666268775685, -0.8212668906743822994 ) ) ;
#164374=CARTESIAN_POINT ( 'NONE',  ( 5.754950181447250124, -1.742976869204535761, 1.353379275444612784 ) ) ;
#164377=CARTESIAN_POINT ( 'NONE',  ( 4.688094572372190960, 1.103980140559155831, 1.561224650464939190 ) ) ;
#164379=( BOUNDED_SURFACE ( )  B_SPLINE_SURFACE ( 3, 3, ( 
 ( #81457, #150736, #213556, #164836, #1237, #32699, #34816, #85709, #2296, #117212, #199445, #51088, #183210, #198378, #100891, #114035, #65178, #31650, #163785, #48967, #148593, #50019, #162, #116143, #166978, #84645, #68373, #134504, #33761, #52152, #66229, #19637, #118280, #15364, #17488, #115085, #131332, #101967, #184265, #168034, #165904, #99838, #132376, #181081, #147534, #151796, #98781, #64144, #47923, #97727, #149656, #154987, #24967, #6572, #203703, #41253, #119347, #189607, #53216, #185334, #54289, #56418, #137682, #91069, #204766, #136614, #3371, #40171, #107363, #123644, #120426, #173384, #21744, #22819, #187473, #36957, #186400, #73726, #69439, #135545, #170156, #87852, #4428, #205852, #106285, #90001, #201570, #39103, #103037, #70498, #122580, #55349, #169092, #188541, #202639, #20691, #38038, #121501, #172306, #156052, #23895, #86782, #152852, #7642, #104107, #139823, #71574, #153924, #5493, #57484, #105188, #171224, #88933, #72652, #138748, #94272, #157130, #108435, #10839, #193866, #192790, #174455, #190659, #160313, #44448, #159238, #110565, #76913, #111630, #77990, #141968, #177643, #176567, #28176, #210106, #12977, #26031, #42320, #207980, #92143, #158196, #60669, #194940, #59608, #161393, #27100, #191726, #144112, #9787, #8719, #140904, #143039, #46577, #209034, #125764, #30321, #11917, #126833, #61746, #127913, #75859, #93208, #74803, #45515, #29251, #43382, #124700, #95343, #109503, #79052, #145169, #175510, #211174, #62799, #128961, #112696, #206916, #58546, #178706, #2034, #64929, #163518, #147271, #131079, #213304, #80118, #48705, #47656, #83304, #32444, #214336, #118021, #100634, #17229, #115883, #184010, #96406, #65966, #196020, #132115, #68104, #97462, #148336, #50822, #182947, #149391, #14032, #212241, #116948, #63874, #34563, #164575, #15105, #98513, #166711, #114819, #31387, #973, #16159, #198125, #33504, #162456, #113767, #82245, #133176, #49756, #179770, #130029, #99576, #181868, #165641, #67039, #199176, #18301, #84387, #81194, #150474, #134240, #200247, #51898, #146223, #197067, #180817, #86520, #52948, #185066, #153666, #73464, #20437, #39919, #120163, #70241, #22567, #36691, #35624, #19370, #103848, #139565, #87594, #152585, #123389, #137422, #5234, #37774, #169896, #102777, #186139, #101702, #88672, #6315, #4171, #3103, #71309, #136356, #21485, #138488, #168833, #201308, #188279, #202376, #54025, #85450, #151535, #203441, #155800, #55095, #121244, #187214, #38843, #104926, #69174, #170967, #119086, #154732, #72389, #204510, #57229, #106028, #56159, #122322, #167772, #135293, #172050, #23643, #89751, #7384, #205592, #191473, #90811, #174205, #96954, #189354, #40994, #9537, #75611, #124450, #80679, #44192, #163002, #24709, #175262, #107105, #42065, #110312, #109254, #196558, #126578, #108179, #26847, #59354, #125510, #25778, #141722, #156875, #60418, #179252, #91890, #74549, #92951, #157945, #43141, #30875, #207731, #206661, #14583, #158997, #10591, #8462, #140648, #76667, #64424, #142781, #208787, #192538, #146770, #212787, #58294, #130568, #190409, #173128, #104537, #71996, #192971, #172741, #89361, #187895, #44623, #168455, #138107, #53639, #204118, #186830, #39524, #55770, #135966, #137036, #24317, #20053, #86142, #120856, #38460, #169522, #156492, #205202, #40610, #152213, #121927 ),
 ( #106715, #155409, #3783, #69857, #123016, #201983, #90423, #22167, #21102, #170583, #188968, #88281, #103460, #6992, #154346, #5924, #105623, #119772, #185752, #171651, #56844, #23249, #37385, #87206, #73071, #139171, #8081, #74170, #140262, #206283, #60849, #153270, #127012, #4846, #70926, #203062, #54706, #194039, #144290, #161568, #128083, #45693, #14203, #148506, #95520, #114992, #195122, #145351, #97638, #111808, #110738, #94447, #178885, #73, #162629, #13157, #198288, #212410, #80299, #163695, #113943, #196190, #177813, #197234, #29429, #211352, #47833, #79234, #81364, #132283, #48873, #15277, #179939, #31563, #147444, #30499, #213468, #160486, #62977, #12093, #210284, #129146, #46760, #96581, #112871, #146396, #65091, #131248, #180990, #32610, #64053, #98687, #130196, #66136, #164744, #61924, #16335, #82417, #176738, #28352, #78160, #102946, #151710, #85622, #68282, #50999, #67211, #86690, #100800, #21652, #37947, #136526, #133346, #201480, #71483, #53122, #35800, #87759, #165815, #153835, #99745, #17398, #166887, #169006, #184180, #137594, #36862, #183123, #49930, #152758, #5405, #170065, #18476, #116051, #150645, #182039, #117120, #202546, #3279, #19545, #83481, #34729, #84556, #69346, #186312, #119255, #199352, #33669, #2206, #134415, #185239, #200419, #149564, #1148, #118192, #20604, #135457, #4341, #52066, #70408, #104019, #54195, #120335, #101877, #167944, #67948, #201161, #39764, #203298, #135145, #188133, #2957, #53879, #170824, #88524, #54945, #134093, #117873, #22415, #183863, #154586, #70092, #69028, #152444, #6163, #20290, #169753, #37622, #121097, #72232, #85301, #35477, #52800, #19223, #151387, #120012, #105869, #118939, #138339, #86375, #36543, #187064, #184919, #1888, #200101, #136207, #171895, #185988, #102630, #89598, #103702, #21341, #4023, #202226, #168686, #87449, #51750, #38697, #104775, #153517, #101555, #5086, #71161, #137278, #204356, #56013, #167624, #122166, #23492, #108031, #139410, #205444, #190262, #61346, #124303, #8317, #206513, #41920, #58144, #57080, #174056, #106954, #142628, #91741, #59201, #177233, #159910, #76516, #175114, #28846, #155648, #125358, #40846, #191321, #25629, #26701, #42988, #123244, #157794, #11516, #7231, #73308, #9390, #75461, #156726, #143710, #192390, #27775, #189208, #109100, #208637, #141574, #172978, #140502, #193476, #60270, #74402, #127505, #207581, #92802, #110164, #93872, #126427, #24557, #90664, #176175, #158847, #77587, #10444, #44045, #209702, #45120, #111230, #29919, #147933, #30994, #146888, #32043, #94934, #46180, #163122, #131717, #130685, #112294, #128568, #98130, #196674, #97069, #48314, #14704, #49361, #15766, #79717, #115481, #81851, #164181, #180425, #178310, #181473, #96002, #195617, #213948, #63476, #65570, #116537, #33103, #197720, #99177, #165229, #16821, #80798, #82906, #144772, #162055, #210782, #194533, #145833, #179372, #212908, #47253, #64541, #148979, #553, #66618, #132765, #114425, #198768, #50418, #182527, #160983, #13645, #12574, #211838, #129630, #78646, #62405, #113367, #135935, #69827, #52540, #35210, #51487, #70895, #85040, #5892, #22135, #120822, #117610, #185722, #55740, #37355, #20023, #71964, #150057, #138074, #83968, #1629, #151128, #87173, #168427, #121895, #21073, #167368, #34156, #137006, #204087, #154318 ),
 ( #201953, #170551, #103429, #183602, #166294, #18956, #101286, #169491, #2695, #100226, #17883, #102355, #153241, #119743, #4814, #67688, #203033, #88248, #54674, #186799, #38428, #104507, #86112, #133834, #53610, #199845, #68767, #134887, #200894, #118674, #184658, #36278, #152183, #3753, #122981, #42728, #156461, #90392, #108836, #207327, #143445, #24286, #140231, #91473, #57878, #39491, #174862, #158590, #8047, #155377, #25372, #74138, #190006, #76264, #40579, #139141, #126167, #172709, #206252, #171623, #23217, #124040, #93611, #41657, #106685, #107770, #173796, #157534, #89330, #9129, #205170, #26441, #75204, #141315, #209442, #192131, #92551, #58948, #61087, #187864, #125106, #73043, #191063, #10190, #142373, #208383, #6962, #60014, #43796, #105589, #56812, #109909, #175920, #188940, #27511, #159656, #11253, #77332, #96817, #114180, #95749, #193216, #112047, #164981, #180174, #45927, #98927, #128319, #179113, #81597, #213699, #31800, #44863, #28592, #147682, #94680, #65322, #195359, #194282, #63216, #131470, #145585, #62161, #97875, #129380, #30735, #64290, #127246, #78397, #46991, #163935, #162866, #144517, #160723, #130436, #14446, #113108, #80536, #146632, #197472, #48068, #178048, #49115, #212649, #196423, #15511, #115235, #210525, #12316, #29665, #161801, #13391, #181225, #16573, #79468, #32853, #211582, #82656, #148740, #308, #110967, #176975, #134648, #104259, #118431, #183360, #154075, #168185, #184418, #68521, #200652, #133591, #34965, #132527, #51238, #170305, #53363, #199595, #38188, #67446, #36036, #20836, #153000, #119497, #198525, #182282, #86935, #33907, #4577, #52302, #117362, #2447, #70651, #84796, #1385, #185483, #102116, #19784, #3515, #66379, #17636, #85866, #103187, #151942, #83721, #99984, #69585, #135696, #201721, #37109, #169248, #136762, #202790, #101036, #54440, #120582, #186559, #21893, #88004, #149811, #166051, #167126, #18712, #150884, #50172, #116292, #204923, #9943, #90152, #40333, #207072, #6725, #5642, #203856, #73889, #43542, #57639, #122735, #93362, #107519, #123799, #7796, #139982, #72803, #156220, #71723, #58703, #190816, #188698, #187622, #189757, #106439, #206004, #108586, #138905, #171380, #158349, #56576, #172462, #55501, #121655, #24049, #125924, #41410, #173548, #25122, #91226, #157286, #39250, #8875, #22971, #124851, #74954, #141065, #27254, #76018, #42476, #174614, #137835, #105342, #26190, #89089, #92305, #142121, #208135, #59763, #155143, #191882, #109665, #175667, #10997, #111789, #177795, #160468, #147427, #196173, #31544, #143202, #129127, #146378, #162611, #30479, #130180, #126993, #80280, #213451, #212392, #47813, #96564, #64034, #79214, #77073, #112853, #113926, #195104, #194022, #15260, #114971, #209192, #46740, #45673, #29412, #94428, #14187, #128066, #61905, #179922, #178868, #180971, #210267, #95503, #62958, #97620, #163677, #81347, #176719, #65074, #12075, #161550, #131229, #13137, #197217, #32594, #48857, #159398, #60832, #192952, #44604, #145332, #110719, #28332, #78143, #144274, #211333, #83464, #183102, #84536, #50978, #150626, #69326, #101857, #135436, #119235, #18459, #36842, #34712, #54175, #185218, #49913, #52047, #149544, #165797, #136506, #201458, #151688, #200398, #134395, #117100, #99725, #116034, #53102, #1130, #70389, #86671, #102924, #182021, #35781 ),
 ( #133329, #4319, #67192, #17381, #199333, #100782, #166864, #82399, #2187, #33651, #85600, #68263, #118173, #120315, #168985, #19524, #184160, #186289, #98670, #167925, #198270, #3258, #20585, #152737, #202526, #66120, #164725, #16314, #148489, #57, #132263, #87738, #187365, #153814, #137575, #22712, #122472, #23791, #204661, #89898, #8610, #41147, #74693, #58441, #172203, #190554, #188432, #207875, #124596, #203593, #205741, #88826, #105080, #125654, #92033, #158091, #5385, #139717, #155949, #40067, #106177, #171118, #7534, #104001, #24857, #140797, #154881, #71462, #73618, #6464, #57374, #206808, #72541, #55245, #42210, #138639, #56311, #21630, #121392, #123537, #9679, #189502, #107257, #173277, #90959, #157025, #38995, #108327, #174347, #25925, #75755, #141865, #59497, #37927, #170044, #211065, #67723, #191616, #95228, #76808, #12865, #209996, #62689, #161278, #159136, #160205, #50454, #43278, #109399, #144004, #61638, #192683, #182566, #16860, #66656, #175404, #78939, #178599, #11807, #26988, #176459, #17920, #33136, #110458, #166330, #44336, #29141, #149014, #132803, #99216, #93095, #10738, #590, #142928, #198806, #45406, #28071, #127805, #116572, #193759, #126722, #165265, #111522, #145061, #128848, #208928, #60563, #177528, #82941, #194831, #94165, #77882, #46465, #112588, #34189, #100263, #84006, #150096, #1667, #105629, #201989, #137042, #4854, #104544, #101323, #54712, #187901, #186836, #170589, #70933, #120863, #53646, #199881, #87213, #38468, #169529, #168461, #204125, #89368, #51524, #21109, #20059, #3789, #68804, #203069, #102394, #36315, #22174, #153277, #155416, #184695, #86149, #37392, #88289, #154353, #5931, #151162, #72003, #134924, #152220, #138114, #69864, #55777, #6999, #121934, #39531, #171658, #23255, #133874, #119779, #117649, #183642, #200930, #35248, #18995, #118707, #135973, #185759, #103467, #167405, #85077, #2732, #52578, #93644, #207365, #11288, #157571, #28626, #159687, #24324, #26477, #124079, #140270, #44898, #208416, #205209, #107806, #108874, #91512, #74178, #90431, #109944, #190043, #111005, #61119, #77367, #156500, #10226, #94714, #76300, #58985, #177009, #188974, #160756, #123023, #40618, #41695, #126205, #125141, #73077, #60050, #206290, #139178, #175953, #56851, #193251, #173831, #106722, #25408, #172749, #57914, #143481, #92587, #42767, #8090, #9164, #75240, #174898, #209477, #142408, #141350, #191099, #158629, #192167, #43828, #27549, #127280, #16611, #96852, #47027, #213735, #13427, #12351, #210561, #80571, #100022, #66416, #132561, #62196, #114214, #64325, #14482, #146670, #79503, #162900, #78431, #65359, #197509, #129414, #194319, #130469, #195397, #212684, #115269, #145622, #178083, #165016, #211617, #179149, #128352, #45960, #113142, #198561, #30773, #63253, #196459, #48102, #180212, #112081, #31835, #29700, #131505, #97910, #163970, #33947, #82692, #147717, #15546, #144553, #95782, #81631, #161839, #49152, #181261, #32888, #98965, #148774, #343, #50209, #116327, #182318, #118469, #184455, #167162, #154110, #202825, #38223, #149852, #135734, #153039, #134687, #17674, #150923, #203893, #4613, #84834, #137873, #18749, #3554, #120618, #104296, #70687, #83760, #67484, #186596, #133629, #170344, #19821, #2484, #102155, #21929, #36073, #101075, #136800, #168221, #69624, #103226 ),
 ( #85906, #88038, #86970, #68560, #5679, #119535, #201756, #54474, #71757, #35003, #199631, #200690, #183398, #52341, #53397, #55538, #1421, #185520, #121692, #151980, #51277, #37144, #187659, #39286, #169285, #166086, #20871, #117401, #59800, #191913, #92340, #23007, #6763, #125957, #72838, #43577, #173590, #106474, #41448, #109696, #123835, #40372, #158382, #107556, #157321, #42515, #105380, #56610, #25160, #142154, #141100, #122774, #138942, #108621, #207111, #91262, #58738, #8912, #175700, #26225, #90192, #27290, #124890, #190854, #9975, #93397, #188734, #204963, #156255, #172501, #24087, #74992, #143234, #7834, #159433, #189797, #140018, #76053, #73925, #171419, #89125, #174649, #192986, #11032, #77110, #155179, #208169, #209224, #60866, #127028, #206043, #57677, #110755, #31580, #15295, #161586, #12108, #96597, #13174, #46776, #147464, #111827, #210300, #197252, #29446, #211369, #28368, #94463, #79252, #164764, #145370, #177829, #95537, #62994, #129163, #160503, #195140, #61940, #97654, #112890, #162647, #66155, #48891, #179957, #64070, #132300, #44640, #14220, #144306, #80315, #178902, #130214, #146415, #78178, #30516, #115011, #176753, #128098, #212428, #196207, #45708, #32628, #81380, #47849, #113960, #163713, #98705, #213485, #131265, #194056, #65109, #181008, #16354, #82434, #148524, #90, #185259, #117138, #170086, #199371, #35820, #152779, #70430, #36883, #116068, #99765, #4361, #165832, #136546, #52083, #51017, #134434, #202566, #2225, #133364, #102966, #200436, #101896, #135476, #198307, #149582, #118210, #20622, #19567, #1166, #17416, #201498, #85641, #184197, #151727, #167961, #54218, #119274, #183141, #120356, #3299, #69367, #169024, #186333, #67230, #83500, #34746, #100819, #166904, #53144, #21673, #18497, #37967, #68300, #84575, #86710, #150663, #49947, #182058, #104040, #71505, #87781, #153855, #33688, #5426, #189539, #139759, #205783, #204700, #7574, #203632, #124637, #108364, #40104, #105118, #41187, #106216, #57412, #25966, #56350, #88866, #75796, #122512, #89935, #121433, #187402, #172242, #43319, #23830, #188473, #155986, #73659, #123577, #39034, #107294, #154921, #190594, #173316, #24895, #159175, #141904, #58481, #157064, #10775, #137616, #91001, #22748, #8652, #74731, #140836, #206849, #171158, #42251, #207914, #55284, #6505, #9720, #174388, #72580, #138681, #92071, #158129, #59535, #125695, #191654, #109437, #175443, #27028, #93136, #129963, #12903, #128891, #13968, #76849, #28109, #145102, #113701, #112629, #94204, #110499, #80052, #178639, #78983, #30251, #211106, #31322, #212171, #61677, #97398, #96335, #162391, #195951, #147211, #160244, #176498, #127845, #11844, #77921, #194872, #114758, #193797, #81126, #161319, #111561, #63805, #144040, #142968, #60603, #62730, #164512, #131013, #197005, #126762, #146155, #46506, #47587, #179705, #210037, #163454, #208971, #15034, #213236, #45446, #44376, #64868, #177569, #48640, #180755, #29182, #95271, #32382, #98448, #192722, #214273, #65906, #50755, #136292, #199110, #83242, #66974, #116884, #133113, #132052, #182883, #181806, #3044, #166646, #134177, #37712, #20377, #151473, #35561, #103788, #16096, #200185, #115819, #51838, #34499, #101642, #117956, #198062, #100573, #86462, #82180, #148274, #18237, #84321, #17168, #4111, #52889, #102715, #49691 ),
 ( #185006, #33439, #150407, #99516, #165573, #183951, #53962, #905, #152526, #1974, #68037, #69113, #149327, #167708, #19310, #85389, #135235, #70180, #202313, #201248, #119024, #36630, #168772, #120100, #186078, #39854, #21426, #156811, #140587, #72320, #137363, #7319, #138426, #171984, #58227, #22498, #121181, #108113, #154665, #122255, #153602, #5174, #204445, #75546, #56099, #88610, #6251, #188214, #105960, #71247, #23576, #187150, #8398, #89685, #73397, #191406, #174140, #90751, #189289, #43073, #169839, #139500, #55033, #205528, #155734, #40931, #57163, #203380, #123326, #25714, #87535, #38779, #107035, #173061, #170905, #157880, #206599, #42005, #104861, #24641, #74482, #124385, #190343, #91823, #207667, #9473, #141655, #59286, #125445, #161065, #63558, #195699, #96085, #26781, #10527, #129714, #76601, #47333, #177316, #110247, #45200, #113448, #127590, #44127, #162139, #111313, #12656, #46259, #109186, #60349, #28931, #145912, #144854, #126512, #142714, #112377, #210861, #95015, #62487, #78729, #179453, #30000, #93954, #31076, #128651, #194617, #13727, #97150, #192474, #143790, #14787, #77670, #176256, #159995, #209786, #11596, #92886, #61423, #27857, #79800, #178389, #211924, #130762, #163204, #80878, #146968, #196758, #175198, #212984, #208723, #64623, #193557, #158931, #17973, #15847, #16910, #118757, #114511, #180507, #642, #66707, #49442, #36369, #85127, #134974, #32127, #84060, #35301, #82990, #98208, #33185, #86198, #101378, #181557, #20112, #115561, #100315, #2783, #200982, #167453, #164259, #81932, #68854, #148018, #52629, #116626, #99267, #198857, #184742, #132852, #197809, #19048, #50504, #166381, #199931, #48398, #214028, #182620, #151213, #150149, #65653, #131800, #51578, #1719, #34243, #67776, #133925, #102446, #183694, #165315, #168512, #117703, #152270, #3842, #69915, #149065, #136026, #38518, #4906, #137096, #105682, #28410, #186886, #209262, #72054, #22227, #191949, #203122, #202039, #185811, #55830, #78221, #44681, #110793, #37443, #92377, #39580, #204173, #121986, #54765, #138166, #53700, #43615, #175740, #104596, #169579, #171711, #170642, #187952, #93435, #120913, #153332, #143272, #88341, #154405, #103521, #21162, #10014, #119832, #87266, #23308, #70983, #158413, #5983, #76090, #142192, #208207, #59838, #60908, #125991, #109733, #27333, #159475, #11073, #193028, #77151, #127066, #176795, #94504, #160542, #12148, #210343, #129207, #182101, #131305, #63040, #116110, #145410, #196248, #98749, #16399, #197296, #61983, #45749, #164806, #111868, #82477, #212471, #211409, #80357, #148566, #162691, #79292, #48937, #146456, #47892, #81424, #144343, #95576, #64115, #181053, #179999, #161626, #177872, #147505, #31623, #130257, #97697, #114004, #133, #65149, #195184, #66201, #163755, #15335, #115056, #132346, #13219, #29484, #46817, #112931, #178944, #213526, #33732, #30558, #198351, #14265, #96637, #32669, #49991, #128137, #194101, #99809, #17460, #165874, #120397, #67271, #3340, #19610, #184236, #35860, #166948, #52126, #149626, #185302, #169064, #2268, #199414, #85682, #68344, #101939, #86753, #18540, #117183, #70470, #84617, #200480, #133409, #1208, #134478, #186372, #118255, #150706, #168004, #151770, #69410, #51059, #135517, #183184, #36925, #201539, #53187, #21713, #136587, #119315, #103008, #20661 ),
 ( #87824, #152823, #38007, #104079, #4399, #170128, #202607, #83545, #54260, #34788, #100863, #32291, #30158, #47499, #63718, #98357, #199022, #131961, #212079, #194782, #195859, #146066, #65814, #129876, #62642, #34410, #130921, #197972, #148185, #33346, #96246, #49602, #116795, #115726, #99428, #214186, #181717, #196914, #128800, #16006, #165482, #164422, #97307, #133023, #18146, #46419, #82092, #163366, #147124, #113608, #17078, #31234, #179612, #83156, #149236, #84234, #14942, #81038, #180666, #810, #66879, #50669, #79963, #182792, #213150, #64780, #100482, #48554, #166558, #150322, #112536, #178548, #162298, #13884, #114673, #56124, #188240, #208752, #89712, #42030, #124412, #141684, #158960, #172011, #122282, #139526, #105991, #23603, #206626, #126541, #73425, #92914, #173089, #123351, #75575, #155762, #88635, #72348, #156837, #176284, #142744, #60378, #138450, #190370, #140614, #90776, #8424, #7346, #24670, #154693, #207697, #59318, #205552, #39880, #57191, #189318, #58256, #40956, #74510, #191435, #107064, #108142, #26812, #174168, #25740, #204471, #91851, #157908, #192503, #9503, #125475, #43102, #109216, #175227, #10555, #76629, #44154, #110275, #6276, #145939, #49469, #32154, #163232, #47362, #115588, #27886, #211951, #127618, #63586, #46289, #113476, #129743, #209816, #210888, #98232, #93983, #160025, #194647, #112406, #28958, #15875, #64649, #114538, #11624, #195726, #14814, #62513, #77698, #12682, #65681, #80905, #161093, #214053, #95043, #79829, #196784, #180532, #146996, #143819, #61451, #48425, #193582, #164287, #96112, #78758, #178417, #81960, #30027, #177346, #213013, #162168, #179483, #31105, #45226, #111341, #13755, #130789, #97178, #144882, #128678, #148045, #131828, #197837, #68883, #183722, #149091, #66739, #87295, #182650, #135002, #2811, #20141, #37472, #50530, #673, #18003, #198884, #116653, #85159, #4935, #166408, #185840, #51609, #1748, #168544, #34272, #181582, #165342, #35331, #54797, #21192, #153364, #16937, #201013, #19078, #101410, #167483, #100344, #117733, #33211, #86228, #152299, #137124, #84093, #133954, #151242, #3872, #184774, #52660, #150180, #53730, #67805, #199961, #118788, #36400, #69945, #203153, #119862, #136057, #102478, #202070, #103550, #169610, #71011, #83018, #99295, #132882, #6016, #105713, #205292, #106800, #73155, #172829, #91593, #124157, #157645, #141430, #40697, #59056, #56930, #76373, #207437, #72085, #74255, #171741, #187984, #92659, #41773, #38548, #155500, #156578, #139262, #122016, #138197, #9242, #23338, #158701, #108949, #125213, #204207, #57994, #142480, #190119, #24400, #10300, #22261, #208488, #170673, #88370, #89448, #173913, #90513, #120946, #107885, #39610, #186918, #75314, #104626, #26551, #7083, #154436, #123103, #55860, #189060, #191175, #140349, #8171, #206368, #25487, #42842, #174969, #196534, #129490, #209552, #192241, #193324, #143558, #63330, #61196, #60124, #31910, #128425, #195472, #145696, #30849, #27623, #47104, #114289, #113219, #96927, #211694, #179224, #194392, #126283, #13504, #162978, #95858, #94786, #130542, #15621, #43903, #161914, #160835, #144624, #127355, #14556, #28701, #177084, #80654, #79577, #78506, #146744, #29774, #93723, #12426, #48176, #110017, #176030, #210638, #62265, #44972, #180287, #212763, #64398, #159762, #97987, #164046 ) ),
 .UNSPECIFIED., .T., .F., .T. ) 
 B_SPLINE_SURFACE_WITH_KNOTS ( ( 4, 3, 4 ),
 ( 4, 1, 1, 1, 1, 1, 1, 1, 1, 1, 1, 1, 1, 1, 1, 1, 1, 1, 1, 1, 1, 1, 1, 1, 1, 1, 1, 1, 1, 1, 1, 1, 1, 1, 1, 1, 1, 1, 1, 1, 1, 1, 1, 1, 1, 1, 1, 1, 1, 1, 1, 1, 1, 1, 1, 1, 1, 1, 1, 1, 1, 1, 1, 1, 1, 1, 1, 1, 1, 1, 1, 1, 1, 1, 1, 1, 1, 1, 1, 1, 1, 1, 1, 1, 1, 1, 1, 1, 1, 1, 1, 1, 1, 1, 1, 1, 1, 1, 1, 1, 1, 1, 1, 1, 1, 1, 1, 1, 1, 1, 1, 1, 1, 1, 1, 1, 1, 1, 1, 1, 1, 1, 1, 1, 1, 1, 1, 1, 1, 1, 1, 1, 1, 1, 1, 1, 1, 1, 1, 1, 1, 1, 1, 1, 1, 1, 1, 1, 1, 1, 1, 1, 1, 1, 1, 1, 1, 1, 1, 1, 1, 1, 1, 1, 1, 1, 1, 1, 1, 1, 1, 1, 1, 1, 1, 1, 1, 1, 1, 1, 1, 1, 1, 1, 1, 1, 1, 1, 1, 1, 1, 1, 1, 1, 1, 1, 1, 1, 1, 1, 1, 1, 1, 1, 1, 1, 1, 1, 1, 1, 1, 1, 1, 1, 1, 1, 1, 1, 1, 1, 1, 1, 1, 1, 1, 1, 1, 1, 1, 1, 1, 1, 1, 1, 1, 1, 1, 1, 1, 1, 1, 1, 1, 1, 1, 1, 1, 1, 1, 1, 1, 1, 1, 1, 1, 1, 1, 1, 1, 1, 1, 1, 1, 1, 1, 1, 1, 1, 1, 1, 1, 1, 1, 1, 1, 1, 1, 1, 1, 1, 1, 1, 1, 1, 1, 1, 1, 1, 1, 1, 1, 1, 1, 1, 1, 1, 1, 1, 1, 1, 1, 1, 1, 1, 1, 1, 1, 1, 1, 1, 1, 1, 1, 1, 1, 1, 1, 1, 1, 1, 1, 1, 1, 1, 1, 1, 1, 1, 1, 1, 1, 1, 1, 1, 1, 1, 1, 1, 1, 1, 1, 1, 1, 1, 1, 1, 1, 1, 1, 1, 1, 1, 1, 1, 1, 1, 1, 1, 1, 1, 1, 1, 1, 1, 1, 1, 1, 1, 1, 1, 1, 1, 1, 1, 1, 1, 1, 1, 1, 1, 1, 1, 1, 1, 4 ),
 ( 0.000000000000000000, 0.5000000000000000000, 1.000000000000000000 ),
 ( 0.000000000000000000, 0.002600209826155936224, 0.005208878553436857226, 0.007813350965615119270, 0.01041570154746907992, 0.01302155883015148306, 0.01562460066207539862, 0.01822947720112986364, 0.02083337797298438765, 0.02343721533725894035, 0.02604213897589890969, 0.02864525980212044229, 0.03125073504456635232, 0.03385369766904555017, 0.03645898980682723417, 0.03906240375024701977, 0.04166680464497042602, 0.04427120869897264999, 0.04687461886132015393, 0.04947991130494613921, 0.05208287402783655373, 0.05468834688957619622, 0.05729146186993632622, 0.05989639238693608009, 0.06250023923939096449, 0.06510408216679804128, 0.06770901469741306966, 0.07031212675311915294, 0.07291759917081726272, 0.07552056149378454097, 0.07812585104223603027, 0.08072926279340975064, 0.08333366149866272554, 0.08593806365491549193, 0.08854147146176674643, 0.09114676191340240208, 0.09374972248801059782, 0.09635519323906190092, 0.09895830628708340848, 0.1015632345865536273, 0.1041670796237980645, 0.1067709202568039306, 0.1093758509056654005, 0.1119789607794838548, 0.1145844312107493490, 0.1171873915655986947, 0.1197926790194954738, 0.1223960889855860712, 0.1250004854864837645, 0.1276048858798866925, 0.1302082914968497596, 0.1328135800830011481, 0.1354165386474412147, 0.1380220074263333041, 0.1406251186789811980, 0.1432300448973659046, 0.1458338882574615747, 0.1484377267335943440, 0.1510426556371624596, 0.1536457634674935069, 0.1562512320483212536, 0.1588541905735017246, 0.1614594760690261366, 0.1640628843880489185, 0.1666672788216651824, 0.1692716775892487424, 0.1718750811543677814, 0.1744803680111783883, 0.1770833247038955116, 0.1796887916465979840, 0.1822919012421508056, 0.1848968255159594287, 0.1875006673364670307, 0.1901045037933276616, 0.1927094310880738681, 0.1953125370132051675, 0.1979180038795354257, 0.2005209607134520455, 0.2031262443867272172, 0.2057296511966431873, 0.2083340436999963075, 0.2109384409787386505, 0.2135418426300015604, 0.2161471278935624962, 0.2187500828529475860, 0.2213555480953768861, 0.2239586561720615654, 0.2265635786377499516, 0.2291674190561798496, 0.2317712536313151217, 0.2343761794536610432, 0.2369792836118274071, 0.2395847488995502261, 0.2421877041805577391, 0.2447929861676560459, 0.2473963916063780244, 0.2500007823164346887, 0.2526051782432667259, 0.2552085781186103075, 0.2578138619249652486, 0.2604168152893601151, 0.2630222789673848927, 0.2656253856633817301, 0.2682303064573571261, 0.2708341456111751366, 0.2734379784420828963, 0.2760429029284052760, 0.2786460054577940548, 0.2812514693027542978, 0.2838544231691620401, 0.2864597036061101165, 0.2890631078115080133, 0.2916674968651886135, 0.2942718915769991783, 0.2968752898143142138, 0.2994805722994643427, 0.3020835242071668869, 0.3046889864566129091, 0.3072920919100609050, 0.3098970111686871198, 0.3125008491953192857, 0.3151046804194536644, 0.3177096037060897493, 0.3203127047448455222, 0.3229181672828482230, 0.3255211198729257016, 0.3281263988957095479, 0.3307298020056156362, 0.3333341895397992083, 0.3359385831734401084, 0.3385419799105768290, 0.3411472612104861635, 0.3437502117997557338, 0.3463556727564109927, 0.3489587771054129539, 0.3515636949650152721, 0.3541675320018531359, 0.3567713617566292128, 0.3593762839798815834, 0.3619793836661120978, 0.3645848450329270407, 0.3671877964849088460, 0.3697930742294792128, 0.3723964763816929868, 0.3750008625332226786, 0.3776052552255140804, 0.3802086506002868016, 0.3828139308508870520, 0.3854168802599494681, 0.3880223400595693151, 0.3906254434421968513, 0.3932303600390676390, 0.3958341962234732669, 0.3984380246462727593, 0.4010429459424146859, 0.4036460444141952153, 0.4062515047455624306, 0.4088544551976535102, 0.4114597317999305615, 0.4140631331322238151, 0.4166675180379114662, 0.4192719099256467796, 0.4218753040758395079, 0.4244805834130354061, 0.4270835317800880659, 0.4296889905584002634, 0.4322920931126992272, 0.4348970085831024290, 0.4375008440524135733, 0.4401046712805898320, 0.4427095917858701601, 0.4453126891812490551, 0.4479181486128839262, 0.4505210982032648026, 0.4531263737991432228, 0.4557297744492659897, 0.4583341582458977381, 0.4609385494658484461, 0.4635419425292200413, 0.4661472210888942258, 0.4687501685521111572, 0.4713556264448209299, 0.4739587283088163017, 0.4765636427889929916, 0.4791674776805284197, 0.4817713038514113699, 0.4843762237020596273, 0.4869793201590638665, 0.4895847788266616818, 0.4921877276934932821, 0.4947930024188478271, 0.4973964025245324327, 0.5000007853488734888, 0.5026051760377950872, 0.5052085681520839255, 0.5078138460701020485, 0.5104167927676396266, 0.5130222499104345468, 0.5156253512221359303, 0.5182302648483090302, 0.5208340992993732987, 0.5234379245502747136, 0.5260428438825063280, 0.5286459395391455152, 0.5312513975783873521, 0.5338543458598166147, 0.5364596198505067193, 0.5390630195494738874, 0.5416674015382738627, 0.5442717918329101900, 0.5468751831358398263, 0.5494804605480556603, 0.5520834066180569932, 0.5546888631466128095, 0.5572919640440190392, 0.5598968769523987588, 0.5625007111002878757, 0.5651045355685063720, 0.5677094545185276120, 0.5703125495128006373, 0.5729180070593572482, 0.5755209548935220631, 0.5781262282853970591, 0.5807296277153600750, 0.5833340090053582561, 0.5859383990424469335, 0.5885417896717308750, 0.5911470667139914204, 0.5937500122945923442, 0.5963554683445766447, 0.5989585689656815592, 0.6015634812924701702, 0.6041673152744758690, 0.6067711390973024033, 0.6093760578013157625, 0.6119791522712144660, 0.6145846094607528842, 0.6171875569857874222, 0.6197928299146914233, 0.6223962292133623508, 0.6250006099412922511, 0.6276049998575695676, 0.6302083899509167697, 0.6328136667590675835, 0.6354166119884008257, 0.6380220676954796444, 0.6406251681782773044, 0.6432300800596744139, 0.6458339140130902045, 0.6484377373278128465, 0.6510426559220214848, 0.6536457500055372627, 0.6562512069737248543, 0.6588541543277639523, 0.6614594269295416273, 0.6640628262346358612, 0.6666672065372305500, 0.6692715964694370134, 0.6718749861645568755, 0.6744802628744462902, 0.6770832078906477980, 0.6796886633904898334, 0.6822917638729786294, 0.6848966754451861760, 0.6875005095073121186, 0.6901043324512210475, 0.6927092510718347862, 0.6953123449069624762, 0.6979178017894718256, 0.7005207491106575368, 0.7031260215211581066, 0.7057294209703992571, 0.7083338009843969107, 0.7109381910692819107, 0.7135415805038890502, 0.7161468572513741693, 0.7187498021925872171, 0.7213552576208688283, 0.7239583582410578089, 0.7265632696402853918, 0.7291671039484327599, 0.7317709266588259265, 0.7343758454420658000, 0.7369789391668094547, 0.7395843960993241373, 0.7421873435258099505, 0.7447926158808931829, 0.7473960156120186271, 0.7500003954741673029, 0.7526047858484943287, 0.7552081751603144655, 0.7578134520812660480, 0.7604163970856469001, 0.7630218525780576577, 0.7656249534739711926, 0.7682298648364407345, 0.7708336995279378989, 0.7734375221421257995, 0.7760424412242287184, 0.7786455349766069345, 0.7812509920948264019, 0.7838539397647821261, 0.7864592122003229990, 0.7890626123510894319, 0.7916669921981516200, 0.7942713829987035901, 0.7968747723254782089, 0.7994800495557851105, 0.8020829947615083499, 0.8046884504537559213, 0.8072915517634385862, 0.8098964632253897733, 0.8125002984375870874, 0.8151041210928977598, 0.8177090406101226172, 0.8203121345281733090, 0.8229175919678175521, 0.8255205400194353116, 0.8281258126713292311, 0.8307292133795166622, 0.8333335933482756142, 0.8359379847118599827, 0.8385413741913512187, 0.8411466518669262760, 0.8437495974121898001, 0.8463550534400045011, 0.8489581553015269622, 0.8515630669992224622, 0.8541669028694969246, 0.8567707257032814994, 0.8593756457919137226, 0.8619787400136992295, 0.8645841979105142183, 0.8671871464820134490, 0.8697924194861808012, 0.8723958208895988831, 0.8750002011168627192, 0.8776045931803160283, 0.8802079829503125508, 0.8828132612070975771, 0.8854162072301272612, 0.8880216637292678294, 0.8906247662807315058, 0.8932296783504612980, 0.8958335150162225480, 0.8984373381658604663, 0.9010422589622166800, 0.9036453536258294283, 0.9062508121155921081, 0.9088537613452241093, 0.9114590348376164775, 0.9140624370741091687, 0.9166668176967164294, 0.9192712105969091940, 0.9218746007952320909, 0.9244798797692056480, 0.9270828264082496828, 0.9296882835145078294, 0.9322913868941045124, 0.9348962994721256026, 0.9375001370706889103, 0.9401039606740361210, 0.9427088823143441321, 0.9453119775565693717, 0.9479174367776000976, 0.9505203868030935865, 0.9531256609099927335, 0.9557290641454977420, 0.9583334452981105978, 0.9609378390199675435, 0.9635412300619400350, 0.9661465102466426647, 0.9687494557931184413, 0.9713549143510965544, 0.9739580252604012056, 0.9765629275426017664, 0.9791667581373608709, 0.9817706348486141543, 0.9843755007711335603, 0.9869785191422796311, 0.9895843624858681187, 0.9921867025132995455, 0.9947911529560371502, 0.9973998138561904758, 1.000000000000000000 ),
 .UNSPECIFIED. ) 
 GEOMETRIC_REPRESENTATION_ITEM ( )  RATIONAL_B_SPLINE_SURFACE ( (
 ( 1.000000000000000222, 1.000000000000000222, 0.9999999999999997780, 1.000000000000000222, 1.000000000000000000, 1.000000000000000000, 0.9999999999999997780, 1.000000000000000000, 1.000000000000000000, 1.000000000000000000, 1.000000000000000000, 1.000000000000000222, 1.000000000000000000, 1.000000000000000000, 1.000000000000000222, 0.9999999999999994449, 1.000000000000000222, 1.000000000000000000, 0.9999999999999997780, 1.000000000000000444, 1.000000000000000000, 1.000000000000000222, 1.000000000000000000, 1.000000000000000000, 0.9999999999999996669, 1.000000000000000000, 1.000000000000000222, 0.9999999999999996669, 1.000000000000000222, 1.000000000000000000, 1.000000000000000222, 1.000000000000000000, 1.000000000000000222, 0.9999999999999997780, 1.000000000000000444, 1.000000000000000000, 1.000000000000000222, 0.9999999999999997780, 1.000000000000000222, 1.000000000000000000, 1.000000000000000000, 0.9999999999999997780, 1.000000000000000000, 0.9999999999999997780, 1.000000000000000000, 0.9999999999999997780, 1.000000000000000000, 1.000000000000000000, 0.9999999999999997780, 1.000000000000000000, 1.000000000000000222, 0.9999999999999996669, 1.000000000000000000, 1.000000000000000000, 1.000000000000000222, 0.9999999999999997780, 1.000000000000000444, 1.000000000000000000, 0.9999999999999997780, 1.000000000000000000, 1.000000000000000000, 1.000000000000000000, 1.000000000000000222, 1.000000000000000000, 1.000000000000000000, 1.000000000000000222, 1.000000000000000000, 1.000000000000000000, 0.9999999999999997780, 1.000000000000000222, 1.000000000000000000, 0.9999999999999997780, 1.000000000000000000, 1.000000000000000000, 1.000000000000000000, 1.000000000000000000, 1.000000000000000222, 0.9999999999999996669, 1.000000000000000444, 0.9999999999999996669, 1.000000000000000000, 0.9999999999999996669, 1.000000000000000444, 1.000000000000000000, 1.000000000000000000, 1.000000000000000222, 1.000000000000000000, 1.000000000000000000, 1.000000000000000222, 0.9999999999999997780, 1.000000000000000000, 1.000000000000000444, 0.9999999999999997780, 1.000000000000000444, 0.9999999999999997780, 1.000000000000000000, 1.000000000000000222, 1.000000000000000000, 0.9999999999999997780, 1.000000000000000222, 1.000000000000000222, 0.9999999999999997780, 1.000000000000000000, 1.000000000000000222, 0.9999999999999997780, 1.000000000000000444, 0.9999999999999997780, 1.000000000000000444, 0.9999999999999997780, 1.000000000000000000, 1.000000000000000222, 0.9999999999999996669, 1.000000000000000000, 1.000000000000000000, 1.000000000000000444, 1.000000000000000222, 0.9999999999999997780, 1.000000000000000222, 1.000000000000000222, 1.000000000000000000, 1.000000000000000222, 0.9999999999999997780, 1.000000000000000000, 1.000000000000000222, 0.9999999999999996669, 1.000000000000000000, 1.000000000000000000, 1.000000000000000000, 1.000000000000000000, 1.000000000000000000, 1.000000000000000000, 1.000000000000000000, 0.9999999999999997780, 1.000000000000000222, 0.9999999999999997780, 1.000000000000000000, 0.9999999999999997780, 1.000000000000000222, 1.000000000000000000, 1.000000000000000000, 1.000000000000000000, 1.000000000000000222, 0.9999999999999997780, 0.9999999999999997780, 1.000000000000000222, 1.000000000000000222, 1.000000000000000000, 1.000000000000000444, 0.9999999999999996669, 1.000000000000000444, 0.9999999999999997780, 1.000000000000000222, 1.000000000000000000, 1.000000000000000000, 1.000000000000000000, 1.000000000000000222, 0.9999999999999997780, 0.9999999999999997780, 1.000000000000000444, 1.000000000000000444, 0.9999999999999997780, 1.000000000000000000, 1.000000000000000000, 1.000000000000000000, 1.000000000000000222, 1.000000000000000000, 1.000000000000000000, 1.000000000000000222, 1.000000000000000222, 1.000000000000000000, 1.000000000000000444, 1.000000000000000000, 1.000000000000000222, 1.000000000000000000, 1.000000000000000000, 1.000000000000000444, 1.000000000000000000, 1.000000000000000222, 1.000000000000000000, 1.000000000000000222, 0.9999999999999997780, 1.000000000000000222, 1.000000000000000222, 1.000000000000000000, 0.9999999999999996669, 1.000000000000000222, 1.000000000000000000, 1.000000000000000000, 1.000000000000000222, 1.000000000000000222, 1.000000000000000222, 0.9999999999999997780, 1.000000000000000000, 1.000000000000000222, 1.000000000000000000, 1.000000000000000000, 1.000000000000000000, 0.9999999999999996669, 1.000000000000000444, 1.000000000000000222, 0.9999999999999996669, 1.000000000000000444, 1.000000000000000000, 1.000000000000000000, 1.000000000000000222, 0.9999999999999997780, 1.000000000000000444, 0.9999999999999997780, 0.9999999999999997780, 1.000000000000000444, 0.9999999999999997780, 1.000000000000000222, 1.000000000000000000, 1.000000000000000000, 1.000000000000000000, 0.9999999999999997780, 1.000000000000000000, 1.000000000000000222, 0.9999999999999996669, 1.000000000000000222, 1.000000000000000000, 1.000000000000000222, 0.9999999999999996669, 0.9999999999999997780, 1.000000000000000444, 0.9999999999999997780, 0.9999999999999997780, 1.000000000000000000, 1.000000000000000222, 1.000000000000000000, 1.000000000000000000, 0.9999999999999996669, 1.000000000000000222, 1.000000000000000000, 0.9999999999999997780, 1.000000000000000000, 1.000000000000000000, 0.9999999999999997780, 1.000000000000000444, 0.9999999999999996669, 1.000000000000000444, 0.9999999999999997780, 1.000000000000000000, 1.000000000000000222, 0.9999999999999997780, 1.000000000000000222, 1.000000000000000222, 0.9999999999999997780, 1.000000000000000000, 1.000000000000000000, 1.000000000000000000, 1.000000000000000222, 1.000000000000000000, 1.000000000000000000, 1.000000000000000222, 1.000000000000000222, 1.000000000000000000, 1.000000000000000000, 1.000000000000000222, 0.9999999999999997780, 1.000000000000000000, 1.000000000000000222, 1.000000000000000000, 1.000000000000000222, 0.9999999999999997780, 1.000000000000000222, 0.9999999999999997780, 1.000000000000000222, 0.9999999999999997780, 1.000000000000000222, 1.000000000000000000, 1.000000000000000000, 1.000000000000000444, 0.9999999999999996669, 1.000000000000000222, 0.9999999999999997780, 1.000000000000000000, 1.000000000000000222, 1.000000000000000000, 1.000000000000000222, 0.9999999999999997780, 0.9999999999999997780, 1.000000000000000000, 0.9999999999999997780, 1.000000000000000000, 1.000000000000000000, 1.000000000000000222, 1.000000000000000000, 1.000000000000000000, 1.000000000000000222, 1.000000000000000000, 1.000000000000000000, 1.000000000000000000, 1.000000000000000000, 0.9999999999999997780, 1.000000000000000222, 1.000000000000000222, 0.9999999999999997780, 1.000000000000000444, 1.000000000000000444, 0.9999999999999997780, 1.000000000000000000, 0.9999999999999997780, 1.000000000000000000, 1.000000000000000000, 1.000000000000000000, 1.000000000000000000, 0.9999999999999997780, 1.000000000000000222, 1.000000000000000000, 0.9999999999999997780, 1.000000000000000222, 1.000000000000000000, 1.000000000000000000, 1.000000000000000000, 1.000000000000000444, 1.000000000000000000, 0.9999999999999997780, 0.9999999999999997780, 0.9999999999999997780, 1.000000000000000222, 1.000000000000000222, 0.9999999999999996669, 1.000000000000000222, 0.9999999999999997780, 1.000000000000000222, 1.000000000000000000, 1.000000000000000000, 0.9999999999999996669, 1.000000000000000222, 1.000000000000000222, 1.000000000000000000, 1.000000000000000000, 1.000000000000000222, 0.9999999999999997780, 1.000000000000000000, 1.000000000000000222, 0.9999999999999994449, 1.000000000000000222, 1.000000000000000000, 1.000000000000000222, 0.9999999999999997780, 1.000000000000000000, 1.000000000000000000, 0.9999999999999997780, 1.000000000000000000, 1.000000000000000222, 0.9999999999999997780, 1.000000000000000000, 1.000000000000000000, 1.000000000000000000, 1.000000000000000000, 1.000000000000000222, 1.000000000000000000, 0.9999999999999996669, 0.9999999999999996669, 1.000000000000000222, 0.9999999999999997780, 1.000000000000000222, 1.000000000000000000, 0.9999999999999997780, 1.000000000000000222, 0.9999999999999997780, 1.000000000000000444, 1.000000000000000222, 1.000000000000000000, 1.000000000000000222, 1.000000000000000222, 1.000000000000000000, 1.000000000000000000, 1.000000000000000000, 1.000000000000000000, 1.000000000000000000, 1.000000000000000000, 1.000000000000000000, 0.9999999999999997780, 1.000000000000000000, 0.9999999999999996669, 1.000000000000000444, 0.9999999999999996669, 1.000000000000000000, 1.000000000000000000, 0.9999999999999997780, 1.000000000000000444, 1.000000000000000000, 1.000000000000000000, 1.000000000000000000),
 ( 0.3333333333333334259, 0.3333333333333334259, 0.3333333333333333703, 0.3333333333333333703, 0.3333333333333334259, 0.3333333333333333703, 0.3333333333333333703, 0.3333333333333334259, 0.3333333333333333148, 0.3333333333333334814, 0.3333333333333332593, 0.3333333333333335369, 0.3333333333333333148, 0.3333333333333333703, 0.3333333333333334259, 0.3333333333333332593, 0.3333333333333333703, 0.3333333333333333703, 0.3333333333333334259, 0.3333333333333334814, 0.3333333333333333148, 0.3333333333333334259, 0.3333333333333333703, 0.3333333333333333703, 0.3333333333333333148, 0.3333333333333333703, 0.3333333333333334259, 0.3333333333333332038, 0.3333333333333334259, 0.3333333333333333703, 0.3333333333333334259, 0.3333333333333333703, 0.3333333333333333148, 0.3333333333333334259, 0.3333333333333334259, 0.3333333333333333703, 0.3333333333333334814, 0.3333333333333332593, 0.3333333333333334259, 0.3333333333333334259, 0.3333333333333333148, 0.3333333333333333703, 0.3333333333333333148, 0.3333333333333333703, 0.3333333333333333148, 0.3333333333333333703, 0.3333333333333333703, 0.3333333333333333703, 0.3333333333333333148, 0.3333333333333333148, 0.3333333333333334259, 0.3333333333333332593, 0.3333333333333333703, 0.3333333333333333703, 0.3333333333333333703, 0.3333333333333332593, 0.3333333333333334259, 0.3333333333333333148, 0.3333333333333333148, 0.3333333333333333703, 0.3333333333333333703, 0.3333333333333333703, 0.3333333333333334259, 0.3333333333333333148, 0.3333333333333334259, 0.3333333333333334259, 0.3333333333333333703, 0.3333333333333333703, 0.3333333333333333148, 0.3333333333333333703, 0.3333333333333333703, 0.3333333333333333148, 0.3333333333333333703, 0.3333333333333332593, 0.3333333333333334814, 0.3333333333333333148, 0.3333333333333333703, 0.3333333333333332593, 0.3333333333333335369, 0.3333333333333333703, 0.3333333333333333703, 0.3333333333333333703, 0.3333333333333334259, 0.3333333333333334259, 0.3333333333333333148, 0.3333333333333334259, 0.3333333333333333148, 0.3333333333333333703, 0.3333333333333335369, 0.3333333333333333148, 0.3333333333333334259, 0.3333333333333334814, 0.3333333333333333148, 0.3333333333333335369, 0.3333333333333332593, 0.3333333333333333703, 0.3333333333333333148, 0.3333333333333334259, 0.3333333333333333148, 0.3333333333333334814, 0.3333333333333333703, 0.3333333333333333148, 0.3333333333333333703, 0.3333333333333334259, 0.3333333333333333703, 0.3333333333333334259, 0.3333333333333332593, 0.3333333333333335924, 0.3333333333333333148, 0.3333333333333333148, 0.3333333333333334259, 0.3333333333333332593, 0.3333333333333333703, 0.3333333333333333148, 0.3333333333333335369, 0.3333333333333333703, 0.3333333333333333703, 0.3333333333333334259, 0.3333333333333334259, 0.3333333333333333703, 0.3333333333333333703, 0.3333333333333333703, 0.3333333333333333703, 0.3333333333333334259, 0.3333333333333333703, 0.3333333333333333703, 0.3333333333333333703, 0.3333333333333334259, 0.3333333333333333148, 0.3333333333333333703, 0.3333333333333333703, 0.3333333333333334259, 0.3333333333333333148, 0.3333333333333333703, 0.3333333333333333703, 0.3333333333333333703, 0.3333333333333333148, 0.3333333333333334259, 0.3333333333333333148, 0.3333333333333333703, 0.3333333333333334259, 0.3333333333333333703, 0.3333333333333333703, 0.3333333333333333703, 0.3333333333333333703, 0.3333333333333334259, 0.3333333333333334259, 0.3333333333333334259, 0.3333333333333333148, 0.3333333333333334259, 0.3333333333333333148, 0.3333333333333334259, 0.3333333333333334259, 0.3333333333333333703, 0.3333333333333333148, 0.3333333333333333703, 0.3333333333333333703, 0.3333333333333333148, 0.3333333333333334259, 0.3333333333333335369, 0.3333333333333333148, 0.3333333333333332593, 0.3333333333333334814, 0.3333333333333332593, 0.3333333333333333703, 0.3333333333333333703, 0.3333333333333333703, 0.3333333333333334259, 0.3333333333333334259, 0.3333333333333334259, 0.3333333333333335369, 0.3333333333333333703, 0.3333333333333333703, 0.3333333333333333703, 0.3333333333333334259, 0.3333333333333333703, 0.3333333333333333703, 0.3333333333333334259, 0.3333333333333333703, 0.3333333333333334259, 0.3333333333333332593, 0.3333333333333334259, 0.3333333333333334259, 0.3333333333333333148, 0.3333333333333333703, 0.3333333333333333703, 0.3333333333333333703, 0.3333333333333333703, 0.3333333333333334259, 0.3333333333333334259, 0.3333333333333334259, 0.3333333333333333148, 0.3333333333333333703, 0.3333333333333334259, 0.3333333333333332593, 0.3333333333333334814, 0.3333333333333333148, 0.3333333333333332593, 0.3333333333333335369, 0.3333333333333333148, 0.3333333333333333703, 0.3333333333333334259, 0.3333333333333333148, 0.3333333333333333703, 0.3333333333333334259, 0.3333333333333333148, 0.3333333333333335369, 0.3333333333333332593, 0.3333333333333333703, 0.3333333333333334259, 0.3333333333333333148, 0.3333333333333334259, 0.3333333333333333148, 0.3333333333333333703, 0.3333333333333333703, 0.3333333333333333703, 0.3333333333333333703, 0.3333333333333334259, 0.3333333333333332593, 0.3333333333333334259, 0.3333333333333334259, 0.3333333333333333703, 0.3333333333333333703, 0.3333333333333333148, 0.3333333333333334814, 0.3333333333333333703, 0.3333333333333332593, 0.3333333333333334259, 0.3333333333333334259, 0.3333333333333334259, 0.3333333333333333703, 0.3333333333333332038, 0.3333333333333335369, 0.3333333333333333148, 0.3333333333333333148, 0.3333333333333333703, 0.3333333333333333703, 0.3333333333333333703, 0.3333333333333334259, 0.3333333333333333148, 0.3333333333333334814, 0.3333333333333333148, 0.3333333333333333703, 0.3333333333333334259, 0.3333333333333333148, 0.3333333333333334259, 0.3333333333333333148, 0.3333333333333334259, 0.3333333333333333148, 0.3333333333333333703, 0.3333333333333333703, 0.3333333333333334259, 0.3333333333333333703, 0.3333333333333333148, 0.3333333333333334814, 0.3333333333333334259, 0.3333333333333333703, 0.3333333333333333148, 0.3333333333333334259, 0.3333333333333333703, 0.3333333333333333703, 0.3333333333333334259, 0.3333333333333333703, 0.3333333333333334814, 0.3333333333333333148, 0.3333333333333334259, 0.3333333333333333703, 0.3333333333333334259, 0.3333333333333333148, 0.3333333333333333703, 0.3333333333333334259, 0.3333333333333333703, 0.3333333333333334259, 0.3333333333333332593, 0.3333333333333333703, 0.3333333333333332593, 0.3333333333333334259, 0.3333333333333333703, 0.3333333333333334259, 0.3333333333333334259, 0.3333333333333333148, 0.3333333333333333148, 0.3333333333333334259, 0.3333333333333333148, 0.3333333333333333148, 0.3333333333333333703, 0.3333333333333333703, 0.3333333333333334259, 0.3333333333333333703, 0.3333333333333334814, 0.3333333333333332593, 0.3333333333333334259, 0.3333333333333333703, 0.3333333333333333703, 0.3333333333333334259, 0.3333333333333333703, 0.3333333333333333703, 0.3333333333333334259, 0.3333333333333334259, 0.3333333333333334814, 0.3333333333333333148, 0.3333333333333333148, 0.3333333333333333703, 0.3333333333333333148, 0.3333333333333334259, 0.3333333333333333703, 0.3333333333333333148, 0.3333333333333332593, 0.3333333333333334259, 0.3333333333333334259, 0.3333333333333333148, 0.3333333333333333703, 0.3333333333333334259, 0.3333333333333333148, 0.3333333333333334259, 0.3333333333333334259, 0.3333333333333334814, 0.3333333333333333148, 0.3333333333333333703, 0.3333333333333332593, 0.3333333333333334814, 0.3333333333333333703, 0.3333333333333332593, 0.3333333333333334814, 0.3333333333333332593, 0.3333333333333334259, 0.3333333333333333703, 0.3333333333333333148, 0.3333333333333333148, 0.3333333333333334259, 0.3333333333333333703, 0.3333333333333333703, 0.3333333333333333703, 0.3333333333333333703, 0.3333333333333334259, 0.3333333333333333148, 0.3333333333333334259, 0.3333333333333332038, 0.3333333333333334259, 0.3333333333333333148, 0.3333333333333334814, 0.3333333333333333703, 0.3333333333333333703, 0.3333333333333334259, 0.3333333333333333148, 0.3333333333333333703, 0.3333333333333333703, 0.3333333333333333703, 0.3333333333333333703, 0.3333333333333333703, 0.3333333333333334259, 0.3333333333333333148, 0.3333333333333334814, 0.3333333333333334259, 0.3333333333333332593, 0.3333333333333333703, 0.3333333333333333703, 0.3333333333333333703, 0.3333333333333333703, 0.3333333333333333703, 0.3333333333333334259, 0.3333333333333333148, 0.3333333333333333703, 0.3333333333333334259, 0.3333333333333335369, 0.3333333333333333148, 0.3333333333333333703, 0.3333333333333334259, 0.3333333333333333703, 0.3333333333333333703, 0.3333333333333333703, 0.3333333333333333703, 0.3333333333333333703, 0.3333333333333333703, 0.3333333333333333703, 0.3333333333333333703, 0.3333333333333334259, 0.3333333333333332593, 0.3333333333333334814, 0.3333333333333332593, 0.3333333333333334259, 0.3333333333333333703, 0.3333333333333333703, 0.3333333333333334814, 0.3333333333333333148, 0.3333333333333333703, 0.3333333333333333703),
 ( 0.3333333333333334259, 0.3333333333333334259, 0.3333333333333333703, 0.3333333333333333703, 0.3333333333333334259, 0.3333333333333333703, 0.3333333333333333703, 0.3333333333333334259, 0.3333333333333333148, 0.3333333333333334814, 0.3333333333333332593, 0.3333333333333335369, 0.3333333333333333148, 0.3333333333333333703, 0.3333333333333334259, 0.3333333333333332593, 0.3333333333333333703, 0.3333333333333333703, 0.3333333333333334259, 0.3333333333333334814, 0.3333333333333333148, 0.3333333333333334259, 0.3333333333333333703, 0.3333333333333333703, 0.3333333333333333148, 0.3333333333333333703, 0.3333333333333334259, 0.3333333333333332038, 0.3333333333333334259, 0.3333333333333333703, 0.3333333333333334259, 0.3333333333333333703, 0.3333333333333333148, 0.3333333333333334259, 0.3333333333333334259, 0.3333333333333333703, 0.3333333333333334814, 0.3333333333333332593, 0.3333333333333334259, 0.3333333333333334259, 0.3333333333333333148, 0.3333333333333333703, 0.3333333333333333148, 0.3333333333333333703, 0.3333333333333333148, 0.3333333333333333703, 0.3333333333333333703, 0.3333333333333333703, 0.3333333333333333148, 0.3333333333333333148, 0.3333333333333334259, 0.3333333333333332593, 0.3333333333333333703, 0.3333333333333333703, 0.3333333333333333703, 0.3333333333333332593, 0.3333333333333334259, 0.3333333333333333148, 0.3333333333333333148, 0.3333333333333333703, 0.3333333333333333703, 0.3333333333333333703, 0.3333333333333334259, 0.3333333333333333148, 0.3333333333333334259, 0.3333333333333334259, 0.3333333333333333703, 0.3333333333333333703, 0.3333333333333333148, 0.3333333333333333703, 0.3333333333333333703, 0.3333333333333333148, 0.3333333333333333703, 0.3333333333333332593, 0.3333333333333334814, 0.3333333333333333148, 0.3333333333333333703, 0.3333333333333332593, 0.3333333333333335369, 0.3333333333333333703, 0.3333333333333333703, 0.3333333333333333703, 0.3333333333333334259, 0.3333333333333334259, 0.3333333333333333148, 0.3333333333333334259, 0.3333333333333333148, 0.3333333333333333703, 0.3333333333333335369, 0.3333333333333333148, 0.3333333333333334259, 0.3333333333333334814, 0.3333333333333333148, 0.3333333333333335369, 0.3333333333333332593, 0.3333333333333333703, 0.3333333333333333148, 0.3333333333333334259, 0.3333333333333333148, 0.3333333333333334814, 0.3333333333333333703, 0.3333333333333333148, 0.3333333333333333703, 0.3333333333333334259, 0.3333333333333333703, 0.3333333333333334259, 0.3333333333333332593, 0.3333333333333335924, 0.3333333333333333148, 0.3333333333333333148, 0.3333333333333334259, 0.3333333333333332593, 0.3333333333333333703, 0.3333333333333333148, 0.3333333333333335369, 0.3333333333333333703, 0.3333333333333333703, 0.3333333333333334259, 0.3333333333333334259, 0.3333333333333333703, 0.3333333333333333703, 0.3333333333333333703, 0.3333333333333333703, 0.3333333333333334259, 0.3333333333333333703, 0.3333333333333333703, 0.3333333333333333703, 0.3333333333333334259, 0.3333333333333333148, 0.3333333333333333703, 0.3333333333333333703, 0.3333333333333334259, 0.3333333333333333148, 0.3333333333333333703, 0.3333333333333333703, 0.3333333333333333703, 0.3333333333333333148, 0.3333333333333334259, 0.3333333333333333148, 0.3333333333333333703, 0.3333333333333334259, 0.3333333333333333703, 0.3333333333333333703, 0.3333333333333333703, 0.3333333333333333703, 0.3333333333333334259, 0.3333333333333334259, 0.3333333333333334259, 0.3333333333333333148, 0.3333333333333334259, 0.3333333333333333148, 0.3333333333333334259, 0.3333333333333334259, 0.3333333333333333703, 0.3333333333333333148, 0.3333333333333333703, 0.3333333333333333703, 0.3333333333333333148, 0.3333333333333334259, 0.3333333333333335369, 0.3333333333333333148, 0.3333333333333332593, 0.3333333333333334814, 0.3333333333333332593, 0.3333333333333333703, 0.3333333333333333703, 0.3333333333333333703, 0.3333333333333334259, 0.3333333333333334259, 0.3333333333333334259, 0.3333333333333335369, 0.3333333333333333703, 0.3333333333333333703, 0.3333333333333333703, 0.3333333333333334259, 0.3333333333333333703, 0.3333333333333333703, 0.3333333333333334259, 0.3333333333333333703, 0.3333333333333334259, 0.3333333333333332593, 0.3333333333333334259, 0.3333333333333334259, 0.3333333333333333148, 0.3333333333333333703, 0.3333333333333333703, 0.3333333333333333703, 0.3333333333333333703, 0.3333333333333334259, 0.3333333333333334259, 0.3333333333333334259, 0.3333333333333333148, 0.3333333333333333703, 0.3333333333333334259, 0.3333333333333332593, 0.3333333333333334814, 0.3333333333333333148, 0.3333333333333332593, 0.3333333333333335369, 0.3333333333333333148, 0.3333333333333333703, 0.3333333333333334259, 0.3333333333333333148, 0.3333333333333333703, 0.3333333333333334259, 0.3333333333333333148, 0.3333333333333335369, 0.3333333333333332593, 0.3333333333333333703, 0.3333333333333334259, 0.3333333333333333148, 0.3333333333333334259, 0.3333333333333333148, 0.3333333333333333703, 0.3333333333333333703, 0.3333333333333333703, 0.3333333333333333703, 0.3333333333333334259, 0.3333333333333332593, 0.3333333333333334259, 0.3333333333333334259, 0.3333333333333333703, 0.3333333333333333703, 0.3333333333333333148, 0.3333333333333334814, 0.3333333333333333703, 0.3333333333333332593, 0.3333333333333334259, 0.3333333333333334259, 0.3333333333333334259, 0.3333333333333333703, 0.3333333333333332038, 0.3333333333333335369, 0.3333333333333333148, 0.3333333333333333148, 0.3333333333333333703, 0.3333333333333333703, 0.3333333333333333703, 0.3333333333333334259, 0.3333333333333333148, 0.3333333333333334814, 0.3333333333333333148, 0.3333333333333333703, 0.3333333333333334259, 0.3333333333333333148, 0.3333333333333334259, 0.3333333333333333148, 0.3333333333333334259, 0.3333333333333333148, 0.3333333333333333703, 0.3333333333333333703, 0.3333333333333334259, 0.3333333333333333703, 0.3333333333333333148, 0.3333333333333334814, 0.3333333333333334259, 0.3333333333333333703, 0.3333333333333333148, 0.3333333333333334259, 0.3333333333333333703, 0.3333333333333333703, 0.3333333333333334259, 0.3333333333333333703, 0.3333333333333334814, 0.3333333333333333148, 0.3333333333333334259, 0.3333333333333333703, 0.3333333333333334259, 0.3333333333333333148, 0.3333333333333333703, 0.3333333333333334259, 0.3333333333333333703, 0.3333333333333334259, 0.3333333333333332593, 0.3333333333333333703, 0.3333333333333332593, 0.3333333333333334259, 0.3333333333333333703, 0.3333333333333334259, 0.3333333333333334259, 0.3333333333333333148, 0.3333333333333333148, 0.3333333333333334259, 0.3333333333333333148, 0.3333333333333333148, 0.3333333333333333703, 0.3333333333333333703, 0.3333333333333334259, 0.3333333333333333703, 0.3333333333333334814, 0.3333333333333332593, 0.3333333333333334259, 0.3333333333333333703, 0.3333333333333333703, 0.3333333333333334259, 0.3333333333333333703, 0.3333333333333333703, 0.3333333333333334259, 0.3333333333333334259, 0.3333333333333334814, 0.3333333333333333148, 0.3333333333333333148, 0.3333333333333333703, 0.3333333333333333148, 0.3333333333333334259, 0.3333333333333333703, 0.3333333333333333148, 0.3333333333333332593, 0.3333333333333334259, 0.3333333333333334259, 0.3333333333333333148, 0.3333333333333333703, 0.3333333333333334259, 0.3333333333333333148, 0.3333333333333334259, 0.3333333333333334259, 0.3333333333333334814, 0.3333333333333333148, 0.3333333333333333703, 0.3333333333333332593, 0.3333333333333334814, 0.3333333333333333703, 0.3333333333333332593, 0.3333333333333334814, 0.3333333333333332593, 0.3333333333333334259, 0.3333333333333333703, 0.3333333333333333148, 0.3333333333333333148, 0.3333333333333334259, 0.3333333333333333703, 0.3333333333333333703, 0.3333333333333333703, 0.3333333333333333703, 0.3333333333333334259, 0.3333333333333333148, 0.3333333333333334259, 0.3333333333333332038, 0.3333333333333334259, 0.3333333333333333148, 0.3333333333333334814, 0.3333333333333333703, 0.3333333333333333703, 0.3333333333333334259, 0.3333333333333333148, 0.3333333333333333703, 0.3333333333333333703, 0.3333333333333333703, 0.3333333333333333703, 0.3333333333333333703, 0.3333333333333334259, 0.3333333333333333148, 0.3333333333333334814, 0.3333333333333334259, 0.3333333333333332593, 0.3333333333333333703, 0.3333333333333333703, 0.3333333333333333703, 0.3333333333333333703, 0.3333333333333333703, 0.3333333333333334259, 0.3333333333333333148, 0.3333333333333333703, 0.3333333333333334259, 0.3333333333333335369, 0.3333333333333333148, 0.3333333333333333703, 0.3333333333333334259, 0.3333333333333333703, 0.3333333333333333703, 0.3333333333333333703, 0.3333333333333333703, 0.3333333333333333703, 0.3333333333333333703, 0.3333333333333333703, 0.3333333333333333703, 0.3333333333333334259, 0.3333333333333332593, 0.3333333333333334814, 0.3333333333333332593, 0.3333333333333334259, 0.3333333333333333703, 0.3333333333333333703, 0.3333333333333334814, 0.3333333333333333148, 0.3333333333333333703, 0.3333333333333333703),
 ( 1.000000000000000222, 1.000000000000000222, 0.9999999999999997780, 1.000000000000000222, 1.000000000000000000, 1.000000000000000000, 0.9999999999999997780, 1.000000000000000000, 1.000000000000000000, 1.000000000000000000, 1.000000000000000000, 1.000000000000000222, 1.000000000000000000, 1.000000000000000000, 1.000000000000000222, 0.9999999999999994449, 1.000000000000000222, 1.000000000000000000, 0.9999999999999997780, 1.000000000000000444, 1.000000000000000000, 1.000000000000000222, 1.000000000000000000, 1.000000000000000000, 0.9999999999999996669, 1.000000000000000000, 1.000000000000000222, 0.9999999999999996669, 1.000000000000000222, 1.000000000000000000, 1.000000000000000222, 1.000000000000000000, 1.000000000000000222, 0.9999999999999997780, 1.000000000000000444, 1.000000000000000000, 1.000000000000000222, 0.9999999999999997780, 1.000000000000000222, 1.000000000000000000, 1.000000000000000000, 0.9999999999999997780, 1.000000000000000000, 0.9999999999999997780, 1.000000000000000000, 0.9999999999999997780, 1.000000000000000000, 1.000000000000000000, 0.9999999999999997780, 1.000000000000000000, 1.000000000000000222, 0.9999999999999996669, 1.000000000000000000, 1.000000000000000000, 1.000000000000000222, 0.9999999999999997780, 1.000000000000000444, 1.000000000000000000, 0.9999999999999997780, 1.000000000000000000, 1.000000000000000000, 1.000000000000000000, 1.000000000000000222, 1.000000000000000000, 1.000000000000000000, 1.000000000000000222, 1.000000000000000000, 1.000000000000000000, 0.9999999999999997780, 1.000000000000000222, 1.000000000000000000, 0.9999999999999997780, 1.000000000000000000, 1.000000000000000000, 1.000000000000000000, 1.000000000000000000, 1.000000000000000222, 0.9999999999999996669, 1.000000000000000444, 0.9999999999999996669, 1.000000000000000000, 0.9999999999999996669, 1.000000000000000444, 1.000000000000000000, 1.000000000000000000, 1.000000000000000222, 1.000000000000000000, 1.000000000000000000, 1.000000000000000222, 0.9999999999999997780, 1.000000000000000000, 1.000000000000000444, 0.9999999999999997780, 1.000000000000000444, 0.9999999999999997780, 1.000000000000000000, 1.000000000000000222, 1.000000000000000000, 0.9999999999999997780, 1.000000000000000222, 1.000000000000000222, 0.9999999999999997780, 1.000000000000000000, 1.000000000000000222, 0.9999999999999997780, 1.000000000000000444, 0.9999999999999997780, 1.000000000000000444, 0.9999999999999997780, 1.000000000000000000, 1.000000000000000222, 0.9999999999999996669, 1.000000000000000000, 1.000000000000000000, 1.000000000000000444, 1.000000000000000222, 0.9999999999999997780, 1.000000000000000222, 1.000000000000000222, 1.000000000000000000, 1.000000000000000222, 0.9999999999999997780, 1.000000000000000000, 1.000000000000000222, 0.9999999999999996669, 1.000000000000000000, 1.000000000000000000, 1.000000000000000000, 1.000000000000000000, 1.000000000000000000, 1.000000000000000000, 1.000000000000000000, 0.9999999999999997780, 1.000000000000000222, 0.9999999999999997780, 1.000000000000000000, 0.9999999999999997780, 1.000000000000000222, 1.000000000000000000, 1.000000000000000000, 1.000000000000000000, 1.000000000000000222, 0.9999999999999997780, 0.9999999999999997780, 1.000000000000000222, 1.000000000000000222, 1.000000000000000000, 1.000000000000000444, 0.9999999999999996669, 1.000000000000000444, 0.9999999999999997780, 1.000000000000000222, 1.000000000000000000, 1.000000000000000000, 1.000000000000000000, 1.000000000000000222, 0.9999999999999997780, 0.9999999999999997780, 1.000000000000000444, 1.000000000000000444, 0.9999999999999997780, 1.000000000000000000, 1.000000000000000000, 1.000000000000000000, 1.000000000000000222, 1.000000000000000000, 1.000000000000000000, 1.000000000000000222, 1.000000000000000222, 1.000000000000000000, 1.000000000000000444, 1.000000000000000000, 1.000000000000000222, 1.000000000000000000, 1.000000000000000000, 1.000000000000000444, 1.000000000000000000, 1.000000000000000222, 1.000000000000000000, 1.000000000000000222, 0.9999999999999997780, 1.000000000000000222, 1.000000000000000222, 1.000000000000000000, 0.9999999999999996669, 1.000000000000000222, 1.000000000000000000, 1.000000000000000000, 1.000000000000000222, 1.000000000000000222, 1.000000000000000222, 0.9999999999999997780, 1.000000000000000000, 1.000000000000000222, 1.000000000000000000, 1.000000000000000000, 1.000000000000000000, 0.9999999999999996669, 1.000000000000000444, 1.000000000000000222, 0.9999999999999996669, 1.000000000000000444, 1.000000000000000000, 1.000000000000000000, 1.000000000000000222, 0.9999999999999997780, 1.000000000000000444, 0.9999999999999997780, 0.9999999999999997780, 1.000000000000000444, 0.9999999999999997780, 1.000000000000000222, 1.000000000000000000, 1.000000000000000000, 1.000000000000000000, 0.9999999999999997780, 1.000000000000000000, 1.000000000000000222, 0.9999999999999996669, 1.000000000000000222, 1.000000000000000000, 1.000000000000000222, 0.9999999999999996669, 0.9999999999999997780, 1.000000000000000444, 0.9999999999999997780, 0.9999999999999997780, 1.000000000000000000, 1.000000000000000222, 1.000000000000000000, 1.000000000000000000, 0.9999999999999996669, 1.000000000000000222, 1.000000000000000000, 0.9999999999999997780, 1.000000000000000000, 1.000000000000000000, 0.9999999999999997780, 1.000000000000000444, 0.9999999999999996669, 1.000000000000000444, 0.9999999999999997780, 1.000000000000000000, 1.000000000000000222, 0.9999999999999997780, 1.000000000000000222, 1.000000000000000222, 0.9999999999999997780, 1.000000000000000000, 1.000000000000000000, 1.000000000000000000, 1.000000000000000222, 1.000000000000000000, 1.000000000000000000, 1.000000000000000222, 1.000000000000000222, 1.000000000000000000, 1.000000000000000000, 1.000000000000000222, 0.9999999999999997780, 1.000000000000000000, 1.000000000000000222, 1.000000000000000000, 1.000000000000000222, 0.9999999999999997780, 1.000000000000000222, 0.9999999999999997780, 1.000000000000000222, 0.9999999999999997780, 1.000000000000000222, 1.000000000000000000, 1.000000000000000000, 1.000000000000000444, 0.9999999999999996669, 1.000000000000000222, 0.9999999999999997780, 1.000000000000000000, 1.000000000000000222, 1.000000000000000000, 1.000000000000000222, 0.9999999999999997780, 0.9999999999999997780, 1.000000000000000000, 0.9999999999999997780, 1.000000000000000000, 1.000000000000000000, 1.000000000000000222, 1.000000000000000000, 1.000000000000000000, 1.000000000000000222, 1.000000000000000000, 1.000000000000000000, 1.000000000000000000, 1.000000000000000000, 0.9999999999999997780, 1.000000000000000222, 1.000000000000000222, 0.9999999999999997780, 1.000000000000000444, 1.000000000000000444, 0.9999999999999997780, 1.000000000000000000, 0.9999999999999997780, 1.000000000000000000, 1.000000000000000000, 1.000000000000000000, 1.000000000000000000, 0.9999999999999997780, 1.000000000000000222, 1.000000000000000000, 0.9999999999999997780, 1.000000000000000222, 1.000000000000000000, 1.000000000000000000, 1.000000000000000000, 1.000000000000000444, 1.000000000000000000, 0.9999999999999997780, 0.9999999999999997780, 0.9999999999999997780, 1.000000000000000222, 1.000000000000000222, 0.9999999999999996669, 1.000000000000000222, 0.9999999999999997780, 1.000000000000000222, 1.000000000000000000, 1.000000000000000000, 0.9999999999999996669, 1.000000000000000222, 1.000000000000000222, 1.000000000000000000, 1.000000000000000000, 1.000000000000000222, 0.9999999999999997780, 1.000000000000000000, 1.000000000000000222, 0.9999999999999994449, 1.000000000000000222, 1.000000000000000000, 1.000000000000000222, 0.9999999999999997780, 1.000000000000000000, 1.000000000000000000, 0.9999999999999997780, 1.000000000000000000, 1.000000000000000222, 0.9999999999999997780, 1.000000000000000000, 1.000000000000000000, 1.000000000000000000, 1.000000000000000000, 1.000000000000000222, 1.000000000000000000, 0.9999999999999996669, 0.9999999999999996669, 1.000000000000000222, 0.9999999999999997780, 1.000000000000000222, 1.000000000000000000, 0.9999999999999997780, 1.000000000000000222, 0.9999999999999997780, 1.000000000000000444, 1.000000000000000222, 1.000000000000000000, 1.000000000000000222, 1.000000000000000222, 1.000000000000000000, 1.000000000000000000, 1.000000000000000000, 1.000000000000000000, 1.000000000000000000, 1.000000000000000000, 1.000000000000000000, 0.9999999999999997780, 1.000000000000000000, 0.9999999999999996669, 1.000000000000000444, 0.9999999999999996669, 1.000000000000000000, 1.000000000000000000, 0.9999999999999997780, 1.000000000000000444, 1.000000000000000000, 1.000000000000000000, 1.000000000000000000),
 ( 0.3333333333333334259, 0.3333333333333334259, 0.3333333333333333703, 0.3333333333333333703, 0.3333333333333334259, 0.3333333333333333703, 0.3333333333333333703, 0.3333333333333334259, 0.3333333333333333148, 0.3333333333333334814, 0.3333333333333332593, 0.3333333333333335369, 0.3333333333333333148, 0.3333333333333333703, 0.3333333333333334259, 0.3333333333333332593, 0.3333333333333333703, 0.3333333333333333703, 0.3333333333333334259, 0.3333333333333334814, 0.3333333333333333148, 0.3333333333333334259, 0.3333333333333333703, 0.3333333333333333703, 0.3333333333333333148, 0.3333333333333333703, 0.3333333333333334259, 0.3333333333333332038, 0.3333333333333334259, 0.3333333333333333703, 0.3333333333333334259, 0.3333333333333333703, 0.3333333333333333148, 0.3333333333333334259, 0.3333333333333334259, 0.3333333333333333703, 0.3333333333333334814, 0.3333333333333332593, 0.3333333333333334259, 0.3333333333333334259, 0.3333333333333333148, 0.3333333333333333703, 0.3333333333333333148, 0.3333333333333333703, 0.3333333333333333148, 0.3333333333333333703, 0.3333333333333333703, 0.3333333333333333703, 0.3333333333333333148, 0.3333333333333333148, 0.3333333333333334259, 0.3333333333333332593, 0.3333333333333333703, 0.3333333333333333703, 0.3333333333333333703, 0.3333333333333332593, 0.3333333333333334259, 0.3333333333333333148, 0.3333333333333333148, 0.3333333333333333703, 0.3333333333333333703, 0.3333333333333333703, 0.3333333333333334259, 0.3333333333333333148, 0.3333333333333334259, 0.3333333333333334259, 0.3333333333333333703, 0.3333333333333333703, 0.3333333333333333148, 0.3333333333333333703, 0.3333333333333333703, 0.3333333333333333148, 0.3333333333333333703, 0.3333333333333332593, 0.3333333333333334814, 0.3333333333333333148, 0.3333333333333333703, 0.3333333333333332593, 0.3333333333333335369, 0.3333333333333333703, 0.3333333333333333703, 0.3333333333333333703, 0.3333333333333334259, 0.3333333333333334259, 0.3333333333333333148, 0.3333333333333334259, 0.3333333333333333148, 0.3333333333333333703, 0.3333333333333335369, 0.3333333333333333148, 0.3333333333333334259, 0.3333333333333334814, 0.3333333333333333148, 0.3333333333333335369, 0.3333333333333332593, 0.3333333333333333703, 0.3333333333333333148, 0.3333333333333334259, 0.3333333333333333148, 0.3333333333333334814, 0.3333333333333333703, 0.3333333333333333148, 0.3333333333333333703, 0.3333333333333334259, 0.3333333333333333703, 0.3333333333333334259, 0.3333333333333332593, 0.3333333333333335924, 0.3333333333333333148, 0.3333333333333333148, 0.3333333333333334259, 0.3333333333333332593, 0.3333333333333333703, 0.3333333333333333148, 0.3333333333333335369, 0.3333333333333333703, 0.3333333333333333703, 0.3333333333333334259, 0.3333333333333334259, 0.3333333333333333703, 0.3333333333333333703, 0.3333333333333333703, 0.3333333333333333703, 0.3333333333333334259, 0.3333333333333333703, 0.3333333333333333703, 0.3333333333333333703, 0.3333333333333334259, 0.3333333333333333148, 0.3333333333333333703, 0.3333333333333333703, 0.3333333333333334259, 0.3333333333333333148, 0.3333333333333333703, 0.3333333333333333703, 0.3333333333333333703, 0.3333333333333333148, 0.3333333333333334259, 0.3333333333333333148, 0.3333333333333333703, 0.3333333333333334259, 0.3333333333333333703, 0.3333333333333333703, 0.3333333333333333703, 0.3333333333333333703, 0.3333333333333334259, 0.3333333333333334259, 0.3333333333333334259, 0.3333333333333333148, 0.3333333333333334259, 0.3333333333333333148, 0.3333333333333334259, 0.3333333333333334259, 0.3333333333333333703, 0.3333333333333333148, 0.3333333333333333703, 0.3333333333333333703, 0.3333333333333333148, 0.3333333333333334259, 0.3333333333333335369, 0.3333333333333333148, 0.3333333333333332593, 0.3333333333333334814, 0.3333333333333332593, 0.3333333333333333703, 0.3333333333333333703, 0.3333333333333333703, 0.3333333333333334259, 0.3333333333333334259, 0.3333333333333334259, 0.3333333333333335369, 0.3333333333333333703, 0.3333333333333333703, 0.3333333333333333703, 0.3333333333333334259, 0.3333333333333333703, 0.3333333333333333703, 0.3333333333333334259, 0.3333333333333333703, 0.3333333333333334259, 0.3333333333333332593, 0.3333333333333334259, 0.3333333333333334259, 0.3333333333333333148, 0.3333333333333333703, 0.3333333333333333703, 0.3333333333333333703, 0.3333333333333333703, 0.3333333333333334259, 0.3333333333333334259, 0.3333333333333334259, 0.3333333333333333148, 0.3333333333333333703, 0.3333333333333334259, 0.3333333333333332593, 0.3333333333333334814, 0.3333333333333333148, 0.3333333333333332593, 0.3333333333333335369, 0.3333333333333333148, 0.3333333333333333703, 0.3333333333333334259, 0.3333333333333333148, 0.3333333333333333703, 0.3333333333333334259, 0.3333333333333333148, 0.3333333333333335369, 0.3333333333333332593, 0.3333333333333333703, 0.3333333333333334259, 0.3333333333333333148, 0.3333333333333334259, 0.3333333333333333148, 0.3333333333333333703, 0.3333333333333333703, 0.3333333333333333703, 0.3333333333333333703, 0.3333333333333334259, 0.3333333333333332593, 0.3333333333333334259, 0.3333333333333334259, 0.3333333333333333703, 0.3333333333333333703, 0.3333333333333333148, 0.3333333333333334814, 0.3333333333333333703, 0.3333333333333332593, 0.3333333333333334259, 0.3333333333333334259, 0.3333333333333334259, 0.3333333333333333703, 0.3333333333333332038, 0.3333333333333335369, 0.3333333333333333148, 0.3333333333333333148, 0.3333333333333333703, 0.3333333333333333703, 0.3333333333333333703, 0.3333333333333334259, 0.3333333333333333148, 0.3333333333333334814, 0.3333333333333333148, 0.3333333333333333703, 0.3333333333333334259, 0.3333333333333333148, 0.3333333333333334259, 0.3333333333333333148, 0.3333333333333334259, 0.3333333333333333148, 0.3333333333333333703, 0.3333333333333333703, 0.3333333333333334259, 0.3333333333333333703, 0.3333333333333333148, 0.3333333333333334814, 0.3333333333333334259, 0.3333333333333333703, 0.3333333333333333148, 0.3333333333333334259, 0.3333333333333333703, 0.3333333333333333703, 0.3333333333333334259, 0.3333333333333333703, 0.3333333333333334814, 0.3333333333333333148, 0.3333333333333334259, 0.3333333333333333703, 0.3333333333333334259, 0.3333333333333333148, 0.3333333333333333703, 0.3333333333333334259, 0.3333333333333333703, 0.3333333333333334259, 0.3333333333333332593, 0.3333333333333333703, 0.3333333333333332593, 0.3333333333333334259, 0.3333333333333333703, 0.3333333333333334259, 0.3333333333333334259, 0.3333333333333333148, 0.3333333333333333148, 0.3333333333333334259, 0.3333333333333333148, 0.3333333333333333148, 0.3333333333333333703, 0.3333333333333333703, 0.3333333333333334259, 0.3333333333333333703, 0.3333333333333334814, 0.3333333333333332593, 0.3333333333333334259, 0.3333333333333333703, 0.3333333333333333703, 0.3333333333333334259, 0.3333333333333333703, 0.3333333333333333703, 0.3333333333333334259, 0.3333333333333334259, 0.3333333333333334814, 0.3333333333333333148, 0.3333333333333333148, 0.3333333333333333703, 0.3333333333333333148, 0.3333333333333334259, 0.3333333333333333703, 0.3333333333333333148, 0.3333333333333332593, 0.3333333333333334259, 0.3333333333333334259, 0.3333333333333333148, 0.3333333333333333703, 0.3333333333333334259, 0.3333333333333333148, 0.3333333333333334259, 0.3333333333333334259, 0.3333333333333334814, 0.3333333333333333148, 0.3333333333333333703, 0.3333333333333332593, 0.3333333333333334814, 0.3333333333333333703, 0.3333333333333332593, 0.3333333333333334814, 0.3333333333333332593, 0.3333333333333334259, 0.3333333333333333703, 0.3333333333333333148, 0.3333333333333333148, 0.3333333333333334259, 0.3333333333333333703, 0.3333333333333333703, 0.3333333333333333703, 0.3333333333333333703, 0.3333333333333334259, 0.3333333333333333148, 0.3333333333333334259, 0.3333333333333332038, 0.3333333333333334259, 0.3333333333333333148, 0.3333333333333334814, 0.3333333333333333703, 0.3333333333333333703, 0.3333333333333334259, 0.3333333333333333148, 0.3333333333333333703, 0.3333333333333333703, 0.3333333333333333703, 0.3333333333333333703, 0.3333333333333333703, 0.3333333333333334259, 0.3333333333333333148, 0.3333333333333334814, 0.3333333333333334259, 0.3333333333333332593, 0.3333333333333333703, 0.3333333333333333703, 0.3333333333333333703, 0.3333333333333333703, 0.3333333333333333703, 0.3333333333333334259, 0.3333333333333333148, 0.3333333333333333703, 0.3333333333333334259, 0.3333333333333335369, 0.3333333333333333148, 0.3333333333333333703, 0.3333333333333334259, 0.3333333333333333703, 0.3333333333333333703, 0.3333333333333333703, 0.3333333333333333703, 0.3333333333333333703, 0.3333333333333333703, 0.3333333333333333703, 0.3333333333333333703, 0.3333333333333334259, 0.3333333333333332593, 0.3333333333333334814, 0.3333333333333332593, 0.3333333333333334259, 0.3333333333333333703, 0.3333333333333333703, 0.3333333333333334814, 0.3333333333333333148, 0.3333333333333333703, 0.3333333333333333703),
 ( 0.3333333333333334259, 0.3333333333333334259, 0.3333333333333333703, 0.3333333333333333703, 0.3333333333333334259, 0.3333333333333333703, 0.3333333333333333703, 0.3333333333333334259, 0.3333333333333333148, 0.3333333333333334814, 0.3333333333333332593, 0.3333333333333335369, 0.3333333333333333148, 0.3333333333333333703, 0.3333333333333334259, 0.3333333333333332593, 0.3333333333333333703, 0.3333333333333333703, 0.3333333333333334259, 0.3333333333333334814, 0.3333333333333333148, 0.3333333333333334259, 0.3333333333333333703, 0.3333333333333333703, 0.3333333333333333148, 0.3333333333333333703, 0.3333333333333334259, 0.3333333333333332038, 0.3333333333333334259, 0.3333333333333333703, 0.3333333333333334259, 0.3333333333333333703, 0.3333333333333333148, 0.3333333333333334259, 0.3333333333333334259, 0.3333333333333333703, 0.3333333333333334814, 0.3333333333333332593, 0.3333333333333334259, 0.3333333333333334259, 0.3333333333333333148, 0.3333333333333333703, 0.3333333333333333148, 0.3333333333333333703, 0.3333333333333333148, 0.3333333333333333703, 0.3333333333333333703, 0.3333333333333333703, 0.3333333333333333148, 0.3333333333333333148, 0.3333333333333334259, 0.3333333333333332593, 0.3333333333333333703, 0.3333333333333333703, 0.3333333333333333703, 0.3333333333333332593, 0.3333333333333334259, 0.3333333333333333148, 0.3333333333333333148, 0.3333333333333333703, 0.3333333333333333703, 0.3333333333333333703, 0.3333333333333334259, 0.3333333333333333148, 0.3333333333333334259, 0.3333333333333334259, 0.3333333333333333703, 0.3333333333333333703, 0.3333333333333333148, 0.3333333333333333703, 0.3333333333333333703, 0.3333333333333333148, 0.3333333333333333703, 0.3333333333333332593, 0.3333333333333334814, 0.3333333333333333148, 0.3333333333333333703, 0.3333333333333332593, 0.3333333333333335369, 0.3333333333333333703, 0.3333333333333333703, 0.3333333333333333703, 0.3333333333333334259, 0.3333333333333334259, 0.3333333333333333148, 0.3333333333333334259, 0.3333333333333333148, 0.3333333333333333703, 0.3333333333333335369, 0.3333333333333333148, 0.3333333333333334259, 0.3333333333333334814, 0.3333333333333333148, 0.3333333333333335369, 0.3333333333333332593, 0.3333333333333333703, 0.3333333333333333148, 0.3333333333333334259, 0.3333333333333333148, 0.3333333333333334814, 0.3333333333333333703, 0.3333333333333333148, 0.3333333333333333703, 0.3333333333333334259, 0.3333333333333333703, 0.3333333333333334259, 0.3333333333333332593, 0.3333333333333335924, 0.3333333333333333148, 0.3333333333333333148, 0.3333333333333334259, 0.3333333333333332593, 0.3333333333333333703, 0.3333333333333333148, 0.3333333333333335369, 0.3333333333333333703, 0.3333333333333333703, 0.3333333333333334259, 0.3333333333333334259, 0.3333333333333333703, 0.3333333333333333703, 0.3333333333333333703, 0.3333333333333333703, 0.3333333333333334259, 0.3333333333333333703, 0.3333333333333333703, 0.3333333333333333703, 0.3333333333333334259, 0.3333333333333333148, 0.3333333333333333703, 0.3333333333333333703, 0.3333333333333334259, 0.3333333333333333148, 0.3333333333333333703, 0.3333333333333333703, 0.3333333333333333703, 0.3333333333333333148, 0.3333333333333334259, 0.3333333333333333148, 0.3333333333333333703, 0.3333333333333334259, 0.3333333333333333703, 0.3333333333333333703, 0.3333333333333333703, 0.3333333333333333703, 0.3333333333333334259, 0.3333333333333334259, 0.3333333333333334259, 0.3333333333333333148, 0.3333333333333334259, 0.3333333333333333148, 0.3333333333333334259, 0.3333333333333334259, 0.3333333333333333703, 0.3333333333333333148, 0.3333333333333333703, 0.3333333333333333703, 0.3333333333333333148, 0.3333333333333334259, 0.3333333333333335369, 0.3333333333333333148, 0.3333333333333332593, 0.3333333333333334814, 0.3333333333333332593, 0.3333333333333333703, 0.3333333333333333703, 0.3333333333333333703, 0.3333333333333334259, 0.3333333333333334259, 0.3333333333333334259, 0.3333333333333335369, 0.3333333333333333703, 0.3333333333333333703, 0.3333333333333333703, 0.3333333333333334259, 0.3333333333333333703, 0.3333333333333333703, 0.3333333333333334259, 0.3333333333333333703, 0.3333333333333334259, 0.3333333333333332593, 0.3333333333333334259, 0.3333333333333334259, 0.3333333333333333148, 0.3333333333333333703, 0.3333333333333333703, 0.3333333333333333703, 0.3333333333333333703, 0.3333333333333334259, 0.3333333333333334259, 0.3333333333333334259, 0.3333333333333333148, 0.3333333333333333703, 0.3333333333333334259, 0.3333333333333332593, 0.3333333333333334814, 0.3333333333333333148, 0.3333333333333332593, 0.3333333333333335369, 0.3333333333333333148, 0.3333333333333333703, 0.3333333333333334259, 0.3333333333333333148, 0.3333333333333333703, 0.3333333333333334259, 0.3333333333333333148, 0.3333333333333335369, 0.3333333333333332593, 0.3333333333333333703, 0.3333333333333334259, 0.3333333333333333148, 0.3333333333333334259, 0.3333333333333333148, 0.3333333333333333703, 0.3333333333333333703, 0.3333333333333333703, 0.3333333333333333703, 0.3333333333333334259, 0.3333333333333332593, 0.3333333333333334259, 0.3333333333333334259, 0.3333333333333333703, 0.3333333333333333703, 0.3333333333333333148, 0.3333333333333334814, 0.3333333333333333703, 0.3333333333333332593, 0.3333333333333334259, 0.3333333333333334259, 0.3333333333333334259, 0.3333333333333333703, 0.3333333333333332038, 0.3333333333333335369, 0.3333333333333333148, 0.3333333333333333148, 0.3333333333333333703, 0.3333333333333333703, 0.3333333333333333703, 0.3333333333333334259, 0.3333333333333333148, 0.3333333333333334814, 0.3333333333333333148, 0.3333333333333333703, 0.3333333333333334259, 0.3333333333333333148, 0.3333333333333334259, 0.3333333333333333148, 0.3333333333333334259, 0.3333333333333333148, 0.3333333333333333703, 0.3333333333333333703, 0.3333333333333334259, 0.3333333333333333703, 0.3333333333333333148, 0.3333333333333334814, 0.3333333333333334259, 0.3333333333333333703, 0.3333333333333333148, 0.3333333333333334259, 0.3333333333333333703, 0.3333333333333333703, 0.3333333333333334259, 0.3333333333333333703, 0.3333333333333334814, 0.3333333333333333148, 0.3333333333333334259, 0.3333333333333333703, 0.3333333333333334259, 0.3333333333333333148, 0.3333333333333333703, 0.3333333333333334259, 0.3333333333333333703, 0.3333333333333334259, 0.3333333333333332593, 0.3333333333333333703, 0.3333333333333332593, 0.3333333333333334259, 0.3333333333333333703, 0.3333333333333334259, 0.3333333333333334259, 0.3333333333333333148, 0.3333333333333333148, 0.3333333333333334259, 0.3333333333333333148, 0.3333333333333333148, 0.3333333333333333703, 0.3333333333333333703, 0.3333333333333334259, 0.3333333333333333703, 0.3333333333333334814, 0.3333333333333332593, 0.3333333333333334259, 0.3333333333333333703, 0.3333333333333333703, 0.3333333333333334259, 0.3333333333333333703, 0.3333333333333333703, 0.3333333333333334259, 0.3333333333333334259, 0.3333333333333334814, 0.3333333333333333148, 0.3333333333333333148, 0.3333333333333333703, 0.3333333333333333148, 0.3333333333333334259, 0.3333333333333333703, 0.3333333333333333148, 0.3333333333333332593, 0.3333333333333334259, 0.3333333333333334259, 0.3333333333333333148, 0.3333333333333333703, 0.3333333333333334259, 0.3333333333333333148, 0.3333333333333334259, 0.3333333333333334259, 0.3333333333333334814, 0.3333333333333333148, 0.3333333333333333703, 0.3333333333333332593, 0.3333333333333334814, 0.3333333333333333703, 0.3333333333333332593, 0.3333333333333334814, 0.3333333333333332593, 0.3333333333333334259, 0.3333333333333333703, 0.3333333333333333148, 0.3333333333333333148, 0.3333333333333334259, 0.3333333333333333703, 0.3333333333333333703, 0.3333333333333333703, 0.3333333333333333703, 0.3333333333333334259, 0.3333333333333333148, 0.3333333333333334259, 0.3333333333333332038, 0.3333333333333334259, 0.3333333333333333148, 0.3333333333333334814, 0.3333333333333333703, 0.3333333333333333703, 0.3333333333333334259, 0.3333333333333333148, 0.3333333333333333703, 0.3333333333333333703, 0.3333333333333333703, 0.3333333333333333703, 0.3333333333333333703, 0.3333333333333334259, 0.3333333333333333148, 0.3333333333333334814, 0.3333333333333334259, 0.3333333333333332593, 0.3333333333333333703, 0.3333333333333333703, 0.3333333333333333703, 0.3333333333333333703, 0.3333333333333333703, 0.3333333333333334259, 0.3333333333333333148, 0.3333333333333333703, 0.3333333333333334259, 0.3333333333333335369, 0.3333333333333333148, 0.3333333333333333703, 0.3333333333333334259, 0.3333333333333333703, 0.3333333333333333703, 0.3333333333333333703, 0.3333333333333333703, 0.3333333333333333703, 0.3333333333333333703, 0.3333333333333333703, 0.3333333333333333703, 0.3333333333333334259, 0.3333333333333332593, 0.3333333333333334814, 0.3333333333333332593, 0.3333333333333334259, 0.3333333333333333703, 0.3333333333333333703, 0.3333333333333334814, 0.3333333333333333148, 0.3333333333333333703, 0.3333333333333333703),
 ( 1.000000000000000222, 1.000000000000000222, 0.9999999999999997780, 1.000000000000000222, 1.000000000000000000, 1.000000000000000000, 0.9999999999999997780, 1.000000000000000000, 1.000000000000000000, 1.000000000000000000, 1.000000000000000000, 1.000000000000000222, 1.000000000000000000, 1.000000000000000000, 1.000000000000000222, 0.9999999999999994449, 1.000000000000000222, 1.000000000000000000, 0.9999999999999997780, 1.000000000000000444, 1.000000000000000000, 1.000000000000000222, 1.000000000000000000, 1.000000000000000000, 0.9999999999999996669, 1.000000000000000000, 1.000000000000000222, 0.9999999999999996669, 1.000000000000000222, 1.000000000000000000, 1.000000000000000222, 1.000000000000000000, 1.000000000000000222, 0.9999999999999997780, 1.000000000000000444, 1.000000000000000000, 1.000000000000000222, 0.9999999999999997780, 1.000000000000000222, 1.000000000000000000, 1.000000000000000000, 0.9999999999999997780, 1.000000000000000000, 0.9999999999999997780, 1.000000000000000000, 0.9999999999999997780, 1.000000000000000000, 1.000000000000000000, 0.9999999999999997780, 1.000000000000000000, 1.000000000000000222, 0.9999999999999996669, 1.000000000000000000, 1.000000000000000000, 1.000000000000000222, 0.9999999999999997780, 1.000000000000000444, 1.000000000000000000, 0.9999999999999997780, 1.000000000000000000, 1.000000000000000000, 1.000000000000000000, 1.000000000000000222, 1.000000000000000000, 1.000000000000000000, 1.000000000000000222, 1.000000000000000000, 1.000000000000000000, 0.9999999999999997780, 1.000000000000000222, 1.000000000000000000, 0.9999999999999997780, 1.000000000000000000, 1.000000000000000000, 1.000000000000000000, 1.000000000000000000, 1.000000000000000222, 0.9999999999999996669, 1.000000000000000444, 0.9999999999999996669, 1.000000000000000000, 0.9999999999999996669, 1.000000000000000444, 1.000000000000000000, 1.000000000000000000, 1.000000000000000222, 1.000000000000000000, 1.000000000000000000, 1.000000000000000222, 0.9999999999999997780, 1.000000000000000000, 1.000000000000000444, 0.9999999999999997780, 1.000000000000000444, 0.9999999999999997780, 1.000000000000000000, 1.000000000000000222, 1.000000000000000000, 0.9999999999999997780, 1.000000000000000222, 1.000000000000000222, 0.9999999999999997780, 1.000000000000000000, 1.000000000000000222, 0.9999999999999997780, 1.000000000000000444, 0.9999999999999997780, 1.000000000000000444, 0.9999999999999997780, 1.000000000000000000, 1.000000000000000222, 0.9999999999999996669, 1.000000000000000000, 1.000000000000000000, 1.000000000000000444, 1.000000000000000222, 0.9999999999999997780, 1.000000000000000222, 1.000000000000000222, 1.000000000000000000, 1.000000000000000222, 0.9999999999999997780, 1.000000000000000000, 1.000000000000000222, 0.9999999999999996669, 1.000000000000000000, 1.000000000000000000, 1.000000000000000000, 1.000000000000000000, 1.000000000000000000, 1.000000000000000000, 1.000000000000000000, 0.9999999999999997780, 1.000000000000000222, 0.9999999999999997780, 1.000000000000000000, 0.9999999999999997780, 1.000000000000000222, 1.000000000000000000, 1.000000000000000000, 1.000000000000000000, 1.000000000000000222, 0.9999999999999997780, 0.9999999999999997780, 1.000000000000000222, 1.000000000000000222, 1.000000000000000000, 1.000000000000000444, 0.9999999999999996669, 1.000000000000000444, 0.9999999999999997780, 1.000000000000000222, 1.000000000000000000, 1.000000000000000000, 1.000000000000000000, 1.000000000000000222, 0.9999999999999997780, 0.9999999999999997780, 1.000000000000000444, 1.000000000000000444, 0.9999999999999997780, 1.000000000000000000, 1.000000000000000000, 1.000000000000000000, 1.000000000000000222, 1.000000000000000000, 1.000000000000000000, 1.000000000000000222, 1.000000000000000222, 1.000000000000000000, 1.000000000000000444, 1.000000000000000000, 1.000000000000000222, 1.000000000000000000, 1.000000000000000000, 1.000000000000000444, 1.000000000000000000, 1.000000000000000222, 1.000000000000000000, 1.000000000000000222, 0.9999999999999997780, 1.000000000000000222, 1.000000000000000222, 1.000000000000000000, 0.9999999999999996669, 1.000000000000000222, 1.000000000000000000, 1.000000000000000000, 1.000000000000000222, 1.000000000000000222, 1.000000000000000222, 0.9999999999999997780, 1.000000000000000000, 1.000000000000000222, 1.000000000000000000, 1.000000000000000000, 1.000000000000000000, 0.9999999999999996669, 1.000000000000000444, 1.000000000000000222, 0.9999999999999996669, 1.000000000000000444, 1.000000000000000000, 1.000000000000000000, 1.000000000000000222, 0.9999999999999997780, 1.000000000000000444, 0.9999999999999997780, 0.9999999999999997780, 1.000000000000000444, 0.9999999999999997780, 1.000000000000000222, 1.000000000000000000, 1.000000000000000000, 1.000000000000000000, 0.9999999999999997780, 1.000000000000000000, 1.000000000000000222, 0.9999999999999996669, 1.000000000000000222, 1.000000000000000000, 1.000000000000000222, 0.9999999999999996669, 0.9999999999999997780, 1.000000000000000444, 0.9999999999999997780, 0.9999999999999997780, 1.000000000000000000, 1.000000000000000222, 1.000000000000000000, 1.000000000000000000, 0.9999999999999996669, 1.000000000000000222, 1.000000000000000000, 0.9999999999999997780, 1.000000000000000000, 1.000000000000000000, 0.9999999999999997780, 1.000000000000000444, 0.9999999999999996669, 1.000000000000000444, 0.9999999999999997780, 1.000000000000000000, 1.000000000000000222, 0.9999999999999997780, 1.000000000000000222, 1.000000000000000222, 0.9999999999999997780, 1.000000000000000000, 1.000000000000000000, 1.000000000000000000, 1.000000000000000222, 1.000000000000000000, 1.000000000000000000, 1.000000000000000222, 1.000000000000000222, 1.000000000000000000, 1.000000000000000000, 1.000000000000000222, 0.9999999999999997780, 1.000000000000000000, 1.000000000000000222, 1.000000000000000000, 1.000000000000000222, 0.9999999999999997780, 1.000000000000000222, 0.9999999999999997780, 1.000000000000000222, 0.9999999999999997780, 1.000000000000000222, 1.000000000000000000, 1.000000000000000000, 1.000000000000000444, 0.9999999999999996669, 1.000000000000000222, 0.9999999999999997780, 1.000000000000000000, 1.000000000000000222, 1.000000000000000000, 1.000000000000000222, 0.9999999999999997780, 0.9999999999999997780, 1.000000000000000000, 0.9999999999999997780, 1.000000000000000000, 1.000000000000000000, 1.000000000000000222, 1.000000000000000000, 1.000000000000000000, 1.000000000000000222, 1.000000000000000000, 1.000000000000000000, 1.000000000000000000, 1.000000000000000000, 0.9999999999999997780, 1.000000000000000222, 1.000000000000000222, 0.9999999999999997780, 1.000000000000000444, 1.000000000000000444, 0.9999999999999997780, 1.000000000000000000, 0.9999999999999997780, 1.000000000000000000, 1.000000000000000000, 1.000000000000000000, 1.000000000000000000, 0.9999999999999997780, 1.000000000000000222, 1.000000000000000000, 0.9999999999999997780, 1.000000000000000222, 1.000000000000000000, 1.000000000000000000, 1.000000000000000000, 1.000000000000000444, 1.000000000000000000, 0.9999999999999997780, 0.9999999999999997780, 0.9999999999999997780, 1.000000000000000222, 1.000000000000000222, 0.9999999999999996669, 1.000000000000000222, 0.9999999999999997780, 1.000000000000000222, 1.000000000000000000, 1.000000000000000000, 0.9999999999999996669, 1.000000000000000222, 1.000000000000000222, 1.000000000000000000, 1.000000000000000000, 1.000000000000000222, 0.9999999999999997780, 1.000000000000000000, 1.000000000000000222, 0.9999999999999994449, 1.000000000000000222, 1.000000000000000000, 1.000000000000000222, 0.9999999999999997780, 1.000000000000000000, 1.000000000000000000, 0.9999999999999997780, 1.000000000000000000, 1.000000000000000222, 0.9999999999999997780, 1.000000000000000000, 1.000000000000000000, 1.000000000000000000, 1.000000000000000000, 1.000000000000000222, 1.000000000000000000, 0.9999999999999996669, 0.9999999999999996669, 1.000000000000000222, 0.9999999999999997780, 1.000000000000000222, 1.000000000000000000, 0.9999999999999997780, 1.000000000000000222, 0.9999999999999997780, 1.000000000000000444, 1.000000000000000222, 1.000000000000000000, 1.000000000000000222, 1.000000000000000222, 1.000000000000000000, 1.000000000000000000, 1.000000000000000000, 1.000000000000000000, 1.000000000000000000, 1.000000000000000000, 1.000000000000000000, 0.9999999999999997780, 1.000000000000000000, 0.9999999999999996669, 1.000000000000000444, 0.9999999999999996669, 1.000000000000000000, 1.000000000000000000, 0.9999999999999997780, 1.000000000000000444, 1.000000000000000000, 1.000000000000000000, 1.000000000000000000) ) ) 
 REPRESENTATION_ITEM ( '' )  SURFACE ( )  );
#164385=CARTESIAN_POINT ( 'NONE',  ( 0.2218712608162629052, 1.761692264604281633, 0.5354471447000588302 ) ) ;
#164388=CARTESIAN_POINT ( 'NONE',  ( 4.710133486059870478, -0.7981590245086762625, -1.691823354513532163 ) ) ;
#164395=CARTESIAN_POINT ( 'NONE',  ( 1.463649477047322733, -0.4837646206634453883, 1.908952741056660685 ) ) ;
#164396=CARTESIAN_POINT ( 'NONE',  ( 2.003530013310977242, -1.955168117277843898, 0.4926643476272293820 ) ) ;
#164400=CARTESIAN_POINT ( 'NONE',  ( 2.502122453320880346, -0.8398649383675671487, -2.024319193490734303 ) ) ;
#164409=CARTESIAN_POINT ( 'NONE',  ( 5.179192671508887180, 1.240781939916297372, 1.360553736468192554 ) ) ;
#164410=CARTESIAN_POINT ( 'NONE',  ( 1.770182950735105898, 2.007541250849652847, -0.1504272076729237795 ) ) ;
#164411=CARTESIAN_POINT ( 'NONE',  ( 3.409784427348498070, 0.5549599139818006677, 2.230294995599948926 ) ) ;
#164413=CARTESIAN_POINT ( 'NONE',  ( 0.9361096364171941353, -1.039984170849604039, 1.543015978488631923 ) ) ;
#164416=CARTESIAN_POINT ( 'NONE',  ( 5.326388512780113160, -0.8654452107222168067, -1.705464787417856787 ) ) ;
#164419=CARTESIAN_POINT ( 'NONE',  ( 3.474242889556743652, -2.015522812629696237, -0.5555695364270489822 ) ) ;
#164420=CARTESIAN_POINT ( 'NONE',  ( 3.625732356982212412, -1.113523340526129335, -1.502988901547596567 ) ) ;
#164422=CARTESIAN_POINT ( 'NONE',  ( 5.917501325027624048, -1.028386522942719816, -1.527094029191010893 ) ) ;
#164426=CARTESIAN_POINT ( 'NONE',  ( 4.564925566169513615, -1.542601567919573258, -0.7719000744037025630 ) ) ;
#164430=CARTESIAN_POINT ( 'NONE',  ( 4.715793416201278454, 0.4818634375548909166, -2.116767182733831021 ) ) ;
#164431=CARTESIAN_POINT ( 'NONE',  ( 3.105874302609371362, -1.823586186413633126, 0.09019715141062728536 ) ) ;
#164432=CARTESIAN_POINT ( 'NONE',  ( 0.9362904128984714802, -1.094497954693674391, 1.627855050370475620 ) ) ;
#164433=CARTESIAN_POINT ( 'NONE',  ( 5.928941916292417957, -1.787427330561262906, 1.134758347235584885 ) ) ;
#164434=CARTESIAN_POINT ( 'NONE',  ( 5.618756969397510126, -0.05950314066365805510, 2.291748599322357194 ) ) ;
#164438=CARTESIAN_POINT ( 'NONE',  ( 1.700013272279196963, 1.464590769506744161, 1.533662747278791816 ) ) ;
#164443=CARTESIAN_POINT ( 'NONE',  ( 6.508646264616319677, 0.6728166153291449403, 2.064291235436790384 ) ) ;
#164444=CARTESIAN_POINT ( 'NONE',  ( 6.983263157960365675, 7.629137130509070275, 2.653810918356712900 ) ) ;
#164447=CARTESIAN_POINT ( 'NONE',  ( 1.911064425300706526, -0.5960121562160587416, -2.139774337300159424 ) ) ;
#164449=CARTESIAN_POINT ( 'NONE',  ( 6.240861317752083970, 2.010826688392798101, -0.1511364921914087889 ) ) ;
#164451=CARTESIAN_POINT ( 'NONE',  ( 6.104357437187505120, 2.059938769829409377, 0.1070097549743902060 ) ) ;
#164456=CARTESIAN_POINT ( 'NONE',  ( 0.1329588055935578272, 2.045323036463253086, -2.262667038281248377 ) ) ;
#164457=CARTESIAN_POINT ( 'NONE',  ( 4.159580895514263688, 0.8717668643758098579, 1.621812032879976329 ) ) ;
#164461=CARTESIAN_POINT ( 'NONE',  ( 2.150978262527812213, -1.382985381756835608, -1.030390371524889659 ) ) ;
#164462=CARTESIAN_POINT ( 'NONE',  ( 0.4797043241997685503, -0.7212876333932433104, 1.883314553594167107 ) ) ;
#164463=CARTESIAN_POINT ( 'NONE',  ( 2.426789430794534130, -1.706071328008453625, -1.540741829672709118 ) ) ;
#164465=CARTESIAN_POINT ( 'NONE',  ( 0.9840795919474578657, 1.519885296779641681, 1.676025758627389450 ) ) ;
#164466=CARTESIAN_POINT ( 'NONE',  ( 4.231157339275457119, 0.1028475037690677746, 2.103686673710772670 ) ) ;
#164468=CARTESIAN_POINT ( 'NONE',  ( 2.143481220494340533, 0.6824282661134513095, -1.633078482676100007 ) ) ;
#164473=CARTESIAN_POINT ( 'NONE',  ( 5.361676289133297857, -1.751401506552331400, -1.366425036640180446 ) ) ;
#164474=CARTESIAN_POINT ( 'NONE',  ( 3.908297495596550597, 1.550167135825938569, -1.549264980215167231 ) ) ;
#164479=CARTESIAN_POINT ( 'NONE',  ( 6.889999999999973035, 7.629137130509070275, 2.319999999999996287 ) ) ;
#164480=COLOUR_RGB ( '', 0.08235294, 0.09019608, 0.10196078) ;
#164482=CARTESIAN_POINT ( 'NONE',  ( 5.801066647469003357, -0.3129311994157328303, -2.097281602037828208 ) ) ;
#164484=ORIENTED_EDGE ( 'NONE', *, *, #56424, .T. ) ;
#164488=CARTESIAN_POINT ( 'NONE',  ( 6.480030769895370746, -1.807141314969593848, -0.3518929191878711338 ) ) ;
#164492=CARTESIAN_POINT ( 'NONE',  ( 1.786251233324965826, 1.514223802825481302, -0.8579289008448316434 ) ) ;
#164498=CARTESIAN_POINT ( 'NONE',  ( 6.332923096303629151, 0.2067577541180857514, 2.151790036905242953 ) ) ;
#164502=CARTESIAN_POINT ( 'NONE',  ( 6.245025451202089073, -1.828886558906620774, 1.152162773130911644 ) ) ;
#164506=CARTESIAN_POINT ( 'NONE',  ( 5.624284779170636739, 1.176309258369928390, -1.581782371169083712 ) ) ;
#164507=CARTESIAN_POINT ( 'NONE',  ( 5.571581879130038217, 1.311117947217877555, -1.134664832369073117 ) ) ;
#164509=CARTESIAN_POINT ( 'NONE',  ( 2.472451708263478931, -2.098117355222902436, -0.6331711661175795092 ) ) ;
#164510=CARTESIAN_POINT ( 'NONE',  ( 3.891899753260852801, 1.669126095664546838, 1.593640439619238514 ) ) ;
#164511=CARTESIAN_POINT ( 'NONE',  ( 4.727839713825126466, -1.264755334911156881, -1.626962714342747196 ) ) ;
#164512=CARTESIAN_POINT ( 'NONE',  ( 1.042798325077255450, -1.530655164913260702, -1.195007349728629764 ) ) ;
#164515=CARTESIAN_POINT ( 'NONE',  ( -0.1110810684432985002, 0.002541288824218451356, -1.796853612742685069 ) ) ;
#164516=CARTESIAN_POINT ( 'NONE',  ( 3.656581996618038843, 2.110704406498860486, 0.2042969539849878724 ) ) ;
#164518=CARTESIAN_POINT ( 'NONE',  ( 0.8971115437808926396, -0.9091470795906559932, -1.799921601489597123 ) ) ;
#164520=CARTESIAN_POINT ( 'NONE',  ( 4.858537417550492954, 0.8407558337346630051, 2.040536144146696707 ) ) ;
#164525=CARTESIAN_POINT ( 'NONE',  ( 6.825078400183579141, 1.241995729952071637, 2.258014901253778461 ) ) ;
#164528=CARTESIAN_POINT ( 'NONE',  ( 4.926665654204026801, 1.971471998011574467, 0.6004258549221918040 ) ) ;
#164532=CARTESIAN_POINT ( 'NONE',  ( 3.826823269871942657, 1.426704988148481901, -1.429811943454310397 ) ) ;
#164536=CARTESIAN_POINT ( 'NONE',  ( 2.870052109166462362, 1.101224123558439905, 1.741800865840010593 ) ) ;
#164540=CARTESIAN_POINT ( 'NONE',  ( 0.7613493127172387132, 0.9053670157611827252, 1.603083849714491027 ) ) ;
#164542=CARTESIAN_POINT ( 'NONE',  ( 6.445939570963194143, 0.8488519614954292969, -2.037301952897092594 ) ) ;
#164544=CARTESIAN_POINT ( 'NONE',  ( 0.9312127099814873077, 0.1580370610147242560, 2.155845405312675211 ) ) ;
#164546=CARTESIAN_POINT ( 'NONE',  ( 1.657435761918718331, 1.928256795251210631, -0.5899901959932273288 ) ) ;
#164547=CARTESIAN_POINT ( 'NONE',  ( 1.775234297868668376, -2.280957755244545027, 0.2818987734495673192 ) ) ;
#164549=CARTESIAN_POINT ( 'NONE',  ( 0.4087956859853311142, 1.625333209436867321, 0.9259686016569528277 ) ) ;
#164550=CARTESIAN_POINT ( 'NONE',  ( 4.662937792257120684, -1.760523130880174314, -0.8874255463059472770 ) ) ;
#164551=CARTESIAN_POINT ( 'NONE',  ( 4.223842396274177347, 0.8578445224393380641, -1.825075645057252505 ) ) ;
#164556=CARTESIAN_POINT ( 'NONE',  ( 6.270163029207718175, 1.081028068854476665, 1.807315287263556280 ) ) ;
#164557=CARTESIAN_POINT ( 'NONE',  ( 5.617656447048144486, 0.4075009240860455462, -2.029694874052537568 ) ) ;
#164561=CARTESIAN_POINT ( 'NONE',  ( 5.431901110126942989, -1.969610648168946376, 0.4466083225366457854 ) ) ;
#164563=CARTESIAN_POINT ( 'NONE',  ( 3.897355454345535097, 1.950357463199345442, -1.233256315927799607 ) ) ;
#164564=CARTESIAN_POINT ( 'NONE',  ( 1.516546868092843781, 0.8322427235708649285, 1.887369835301610621 ) ) ;
#164571=CARTESIAN_POINT ( 'NONE',  ( 3.666621648402784484, -0.8769701800699877259, -1.986351817242467677 ) ) ;
#164575=CARTESIAN_POINT ( 'NONE',  ( 2.929072846782492245, -1.238530643895646488, -1.362589426554157157 ) ) ;
#164577=CARTESIAN_POINT ( 'NONE',  ( 3.843468145482428877, 0.7371271433744167600, -2.064019554291535830 ) ) ;
#164579=CARTESIAN_POINT ( 'NONE',  ( 5.436487035374818255, 2.228047177662040301, 0.3926572465528885281 ) ) ;
#164584=CARTESIAN_POINT ( 'NONE',  ( 6.344957943996793581, -1.493715166628902580, 0.9487403735100213842 ) ) ;
#164585=CARTESIAN_POINT ( 'NONE',  ( 3.598294619042395226, -0.9903900195140210583, 1.752531985089557098 ) ) ;
#164587=CARTESIAN_POINT ( 'NONE',  ( 2.872209793879555217, 1.125368584265328264, 1.779858853945482489 ) ) ;
#164588=CARTESIAN_POINT ( 'NONE',  ( 1.686979003181095615, 1.593666142434764454, 1.062572995559516009 ) ) ;
#164590=CARTESIAN_POINT ( 'NONE',  ( 3.279706249791583872, -1.898816934168370496, 0.5228806403664593150 ) ) ;
#164591=CARTESIAN_POINT ( 'NONE',  ( 4.851822172175670467, -1.431287984025449100, -1.425384875499214443 ) ) ;
#164592=CARTESIAN_POINT ( 'NONE',  ( 0.2505829665140328899, -1.505242420826727656, 1.110479572284161831 ) ) ;
#164593=CARTESIAN_POINT ( 'NONE',  ( 0.7659737006216191801, -1.952758744216346765, 0.1886366088557633325 ) ) ;
#164594=CARTESIAN_POINT ( 'NONE',  ( 0.2813230411330031044, 0.1852680230450229892, -1.903361379684164412 ) ) ;
#164599=CARTESIAN_POINT ( 'NONE',  ( 5.787941465827733722, -0.8397648285632768328, 1.671655200917811168 ) ) ;
#164605=CARTESIAN_POINT ( 'NONE',  ( 0.6255436495894195481, 0.2045281481408110225, -2.060252820462626477 ) ) ;
#164611=CARTESIAN_POINT ( 'NONE',  ( 5.479186192515411946, -1.917069751554843160, -0.9065152316691318379 ) ) ;
#164615=CARTESIAN_POINT ( 'NONE',  ( 6.004347769543215030, 1.959566550440184907, 0.09775035808561728656 ) ) ;
#164617=CARTESIAN_POINT ( 'NONE',  ( 4.077499844852236599, 1.427718728413525318, -1.423743541103118737 ) ) ;
#164618=CARTESIAN_POINT ( 'NONE',  ( 3.678834806144789749, 1.615436204272060472, -1.029439157428935658 ) ) ;
#164620=CARTESIAN_POINT ( 'NONE',  ( 1.786939262935317130, 1.904797134731281538, -1.083727916527020607 ) ) ;
#164621=CARTESIAN_POINT ( 'NONE',  ( 0.1331715793776314105, 6.947497095909970000, -2.548608419791003055 ) ) ;
#164622=CARTESIAN_POINT ( 'NONE',  ( 3.268673085221412311, -1.727008210369033847, -0.7190761260571986169 ) ) ;
#164626=CARTESIAN_POINT ( 'NONE',  ( 5.097310499321968003, -0.3096355862501755096, 2.094337834851481617 ) ) ;
#164630=CARTESIAN_POINT ( 'NONE',  ( 2.296528860280427686, 1.677371239548936854, -1.247825592998616617 ) ) ;
#164632=CARTESIAN_POINT ( 'NONE',  ( 1.043494860557155679, 0.7046062621528689229, -1.574481895975497592 ) ) ;
#164642=CARTESIAN_POINT ( 'NONE',  ( 1.928074960669722504, -0.8543848903827315766, -1.597334059258429972 ) ) ;
#164653=CARTESIAN_POINT ( 'NONE',  ( 3.420197418661593769, 0.8345380353566893561, 1.663503485505882118 ) ) ;
#164654=CARTESIAN_POINT ( 'NONE',  ( 0.8080361750046762825, 1.140156559909396128, -1.539198610912548171 ) ) ;
#164655=CARTESIAN_POINT ( 'NONE',  ( 6.616243401494351417, -0.9090183210780745648, -1.698415751782512695 ) ) ;
#164656=CARTESIAN_POINT ( 'NONE',  ( 5.898901817742317810, 0.4001337562283372451, 2.031160294743330486 ) ) ;
#164662=CARTESIAN_POINT ( 'NONE',  ( 4.170725306337518923, 1.395817779951594950, -1.389658704579323611 ) ) ;
#164663=CARTESIAN_POINT ( 'NONE',  ( 1.576976220782677185, -1.497206391897941691, 1.501870991332490357 ) ) ;
#164667=CARTESIAN_POINT ( 'NONE',  ( 5.472676780243426187, -0.05103125619924236966, -2.191024458042860168 ) ) ;
#164669=CARTESIAN_POINT ( 'NONE',  ( 3.961874236345910294, 1.911929771648058995, -0.2350156305768891229 ) ) ;
#164671=CARTESIAN_POINT ( 'NONE',  ( 0.3229203692996869823, -0.09522068211164493035, 1.823229820405058099 ) ) ;
#164672=CARTESIAN_POINT ( 'NONE',  ( 0.5400322017136415242, -1.563516176313231920, -1.557742479837947558 ) ) ;
#164676=CARTESIAN_POINT ( 'NONE',  ( 5.998876245820001785, 0.3805640578184403822, 1.932138370648580628 ) ) ;
#164677=CARTESIAN_POINT ( 'NONE',  ( 1.487729058832359952, -1.932848847819462756, -0.1887428500492206451 ) ) ;
#164678=CARTESIAN_POINT ( 'NONE',  ( 6.415373042369045820, 0.7112672321729663905, 2.185653275185605704 ) ) ;
#164680=CARTESIAN_POINT ( 'NONE',  ( 5.612096381091351560, 1.858897858770152789, -0.08933831184920922042 ) ) ;
#164687=CARTESIAN_POINT ( 'NONE',  ( 1.031118135130421498, -1.979082047791239418, 0.9416876394413642437 ) ) ;
#164690=CARTESIAN_POINT ( 'NONE',  ( 1.277666653898035021, 1.085793613588705853, 1.467558327050644484 ) ) ;
#164693=CARTESIAN_POINT ( 'NONE',  ( 6.609000000000047947, 2.032467779867861868, 2.404707446487294842 ) ) ;
#164695=CARTESIAN_POINT ( 'NONE',  ( 6.463509179248937642, 0.3066564278407272748, -1.799597105106438777 ) ) ;
#164696=CARTESIAN_POINT ( 'NONE',  ( 4.381663332995835880, -1.878531202089319896, 0.5654445158327011667 ) ) ;
#164699=CARTESIAN_POINT ( 'NONE',  ( 5.127636373287420390, -0.3106611864900839515, 2.097473367668806876 ) ) ;
#164701=CARTESIAN_POINT ( 'NONE',  ( 6.609000000000036401, 0.5823242425131782696, 2.053003180352876100 ) ) ;
#164702=CARTESIAN_POINT ( 'NONE',  ( 2.870052101067874339, -2.048368873657464118, 0.2992715783270774588 ) ) ;
#164706=CARTESIAN_POINT ( 'NONE',  ( 2.813438166105670657, 1.274540910030600216, -1.912834453734891804 ) ) ;
#164714=CARTESIAN_POINT ( 'NONE',  ( 4.447458312869024155, -1.746245811230532130, 0.7801085911468002010 ) ) ;
#164716=CARTESIAN_POINT ( 'NONE',  ( 4.963727558602625933, 1.705580761961351444, -0.2555711148431466517 ) ) ;
#164717=CARTESIAN_POINT ( 'NONE',  ( 2.993375309983861143, -0.3886322325962355273, 1.978555244300662874 ) ) ;
#164718=CARTESIAN_POINT ( 'NONE',  ( 5.309350125645185159, 1.371050412704700516, -1.844953357796705218 ) ) ;
#164720=CARTESIAN_POINT ( 'NONE',  ( 0.6278963055918493907, -2.094311335337955882, 0.6960538111202837497 ) ) ;
#164722=CARTESIAN_POINT ( 'NONE',  ( 5.624192029756354572, 1.053330351427090639, -1.421934073773284180 ) ) ;
#164724=CARTESIAN_POINT ( 'NONE',  ( 2.115536061532933942, -2.222870945405757137, 0.5592890022133433225 ) ) ;
#164725=CARTESIAN_POINT ( 'NONE',  ( 6.281194495005370193, 1.273289214079580622, 1.330099835651930684 ) ) ;
#164731=CARTESIAN_POINT ( 'NONE',  ( 0.1511277727459575393, -0.4806850054440474085, -2.125521221522770787 ) ) ;
#164732=CARTESIAN_POINT ( 'NONE',  ( 2.237517880698642880, 0.5331670712399002587, -1.944730990508992008 ) ) ;
#164734=CARTESIAN_POINT ( 'NONE',  ( 5.654890666209754002, -1.517393486936137403, 1.186882646050735346 ) ) ;
#164736=CARTESIAN_POINT ( 'NONE',  ( 2.057158355326561772, 0.4919409011131297138, 2.166103627455501890 ) ) ;
#164744=CARTESIAN_POINT ( 'NONE',  ( 4.985792865680892305, -1.728136641771714777, -0.2059490554011476626 ) ) ;
#164745=CARTESIAN_POINT ( 'NONE',  ( 3.033595934319989418, 1.863777508880835487, -0.6128360024686765328 ) ) ;
#164750=CARTESIAN_POINT ( 'NONE',  ( 5.079486683540675784, 2.113528219476542347, -0.8076395688127128158 ) ) ;
#164752=CARTESIAN_POINT ( 'NONE',  ( 1.539586554034046539, 1.906627302964102988, -0.7874849336161419133 ) ) ;
#164756=CARTESIAN_POINT ( 'NONE',  ( 1.868429791336771340, 1.163878172895687069, 1.940057763798187951 ) ) ;
#164759=CARTESIAN_POINT ( 'NONE',  ( 2.196370303256788503, -0.4943915968025693330, -1.803980227719769847 ) ) ;
#164760=CARTESIAN_POINT ( 'NONE',  ( 0.8438932004057161373, 0.3398822538093429491, -1.700291973301551129 ) ) ;
#164761=CARTESIAN_POINT ( 'NONE',  ( 5.812113132715003516, 1.472855484078567700, -1.623034594306454137 ) ) ;
#164762=CARTESIAN_POINT ( 'NONE',  ( 6.299901696735699552, -0.7855725015378700604, 2.169893659913350259 ) ) ;
#164763=CARTESIAN_POINT ( 'NONE',  ( 0.7079729303958534059, -2.051031625230379074, 0.2011725655505970656 ) ) ;
#164764=CARTESIAN_POINT ( 'NONE',  ( 4.822180446859828606, 1.858854579410177843, 0.5619951038204271665 ) ) ;
#164767=CARTESIAN_POINT ( 'NONE',  ( 6.643822754079466542, 0.7155741859487285694, -1.728458771772640512 ) ) ;
#164768=CARTESIAN_POINT ( 'NONE',  ( 1.000000000000000666, -5.752119711681284071E-14, -2.052068128417952053 ) ) ;
#164770=CARTESIAN_POINT ( 'NONE',  ( 6.872432811717262169, -0.4447407475622888740, 1.973694069355651282 ) ) ;
#164773=CARTESIAN_POINT ( 'NONE',  ( 6.065077313367789102, -1.076319894221990259, 1.704936797084610101 ) ) ;
#164777=CARTESIAN_POINT ( 'NONE',  ( 2.209345402013741300, -0.4006574107652469130, 1.781019818369505847 ) ) ;
#164784=CARTESIAN_POINT ( 'NONE',  ( 0.3869806665078223129, -1.903265420633104332, -0.6765555904410057719 ) ) ;
#164785=CARTESIAN_POINT ( 'NONE',  ( 0.2938078718510480081, 1.976988316466289142, -0.7672523047414223640 ) ) ;
#164789=CARTESIAN_POINT ( 'NONE',  ( 6.121960869219821966, -1.142753529713343763, -1.714830629803126616 ) ) ;
#164790=CARTESIAN_POINT ( 'NONE',  ( 4.729138786257041538, 2.011204126674607462, 0.1455352507326590494 ) ) ;
#164799=CARTESIAN_POINT ( 'NONE',  ( 5.009138659175729202, 2.010518709310470609, 0.1511151588593287465 ) ) ;
#164800=CARTESIAN_POINT ( 'NONE',  ( 4.505690185649424251, -0.7896136771840707169, -1.663358820747300237 ) ) ;
#164801=CARTESIAN_POINT ( 'NONE',  ( -0.02338929933909470252, 5.726375320706490690, -2.305055744220934066 ) ) ;
#164802=CARTESIAN_POINT ( 'NONE',  ( 3.563348594130168578, -2.034784092110089926, -1.088618498840478566 ) ) ;
#164804=CARTESIAN_POINT ( 'NONE',  ( 6.011032505573889573, 1.903242638633116712, 1.024824547371510075 ) ) ;
#164806=CARTESIAN_POINT ( 'NONE',  ( 1.470153547685297823, -1.844723335029124112, -0.6073778784492619431 ) ) ;
#164809=CARTESIAN_POINT ( 'NONE',  ( 4.974093195743899187, 1.996273031041963408, 1.139003188958290780 ) ) ;
#164812=CARTESIAN_POINT ( 'NONE',  ( 2.975316878787794828, 1.776827963633962559, -0.5852370025475408521 ) ) ;
#164813=CARTESIAN_POINT ( 'NONE',  ( 1.441514601552947417, -1.799640695080907182, 0.6472408003148700795 ) ) ;
#164817=CARTESIAN_POINT ( 'NONE',  ( 2.368051099418837069, 2.164043333312406503, -0.4318774905316472013 ) ) ;
#164823=CARTESIAN_POINT ( 'NONE',  ( 0.4210825541404016326, -0.1013260788591107547, 1.968891031686560211 ) ) ;
#164825=CARTESIAN_POINT ( 'NONE',  ( 0.07775346131144458828, -0.005211914751935413023, -2.288974916015192651 ) ) ;
#164826=CARTESIAN_POINT ( 'NONE',  ( 1.469116868872882620, 1.728625619535430369, 0.9278086228877155950 ) ) ;
#164827=CARTESIAN_POINT ( 'NONE',  ( 5.207907603007337016, 0.6519758639490059737, -1.956853833162349066 ) ) ;
#164834=CARTESIAN_POINT ( 'NONE',  ( 0.6554289830566867314, 1.805916262795668192, -1.204791683884984810 ) ) ;
#164836=CARTESIAN_POINT ( 'NONE',  ( 6.585540641348407220, -0.7802508550805786758, 1.666130356082275998 ) ) ;
#164839=CARTESIAN_POINT ( 'NONE',  ( 1.422894040683621242, -0.05142188859055820543, 1.870020055627517275 ) ) ;
#164840=CARTESIAN_POINT ( 'NONE',  ( 5.483715611629243369, 1.447241891022777560, 1.605803905980404123 ) ) ;
#164844=CARTESIAN_POINT ( 'NONE',  ( 1.330556988563241561, 1.283596529665396169, -1.417643162000304935 ) ) ;
#164845=CARTESIAN_POINT ( 'NONE',  ( 3.238855601640895809, -1.561498447111120402, 0.8330696194922878606 ) ) ;
#164846=CARTESIAN_POINT ( 'NONE',  ( 0.3813228709106940006, 0.1872568833237615027, -1.903067810102520241 ) ) ;
#164848=CARTESIAN_POINT ( 'NONE',  ( 5.149962951811881240, 0.9480454039230011842, 1.664493911490998679 ) ) ;
#164849=CARTESIAN_POINT ( 'NONE',  ( 6.848121164528643945, -0.8440317545377834518, 1.778091661420333702 ) ) ;
#164851=CARTESIAN_POINT ( 'NONE',  ( 1.494549364340029163, -1.129948290531690658, 1.794289463044356436 ) ) ;
#164853=CARTESIAN_POINT ( 'NONE',  ( 4.082764389539480732, -0.1829629792115642917, -1.861669828791753467 ) ) ;
#164854=CARTESIAN_POINT ( 'NONE',  ( 0.08226035653636187828, -1.769965142718381124, -0.4472663993063328847 ) ) ;
#164856=CARTESIAN_POINT ( 'NONE',  ( 5.004599478379411437, -0.7411955310945415043, -2.078817424605138964 ) ) ;
#164858=CARTESIAN_POINT ( 'NONE',  ( 1.838405449727827268, -1.105357634037696046, 1.741336484761913272 ) ) ;
#164865=CARTESIAN_POINT ( 'NONE',  ( 3.947765587739564097, 1.497496809916948779, 1.429883829622953462 ) ) ;
#164867=CARTESIAN_POINT ( 'NONE',  ( 0.9663661119345480222, 1.064502738163356721, 1.881203019380036867 ) ) ;
#164869=CARTESIAN_POINT ( 'NONE',  ( 2.490883850439883140, -1.933321517186505245, -0.5842891067564592866 ) ) ;
#164875=CARTESIAN_POINT ( 'NONE',  ( -0.1003747550864658999, -1.976661868047492998, 0.3981153667176607902 ) ) ;
#164876=CARTESIAN_POINT ( 'NONE',  ( 6.539320575229233157, 0.001224430076711413356, 2.103502572931112091 ) ) ;
#164877=CARTESIAN_POINT ( 'NONE',  ( 5.425378541715013547, -1.389685604419872655, -1.694579525865949066 ) ) ;
#164880=CARTESIAN_POINT ( 'NONE',  ( 3.410326831400651404, -1.910418641682644969, -0.08914582809275289899 ) ) ;
#164884=CARTESIAN_POINT ( 'NONE',  ( 2.653922917551009952, 1.081085551080329443, 1.701936510390424928 ) ) ;
#164886=CARTESIAN_POINT ( 'NONE',  ( -0.07607780150072247782, -1.417851297177070258, -1.802264747598992800 ) ) ;
#164888=CARTESIAN_POINT ( 'NONE',  ( 3.821100691872282518, -0.1266977344972844144, 1.720184112200423332 ) ) ;
#164889=CARTESIAN_POINT ( 'NONE',  ( -0.1399997263889611598, 6.947783040739049731, -2.595329734540325006 ) ) ;
#164894=CARTESIAN_POINT ( 'NONE',  ( 0.07516593201275456604, 0.0004601587237917924593, -2.044269526395313452 ) ) ;
#164896=CARTESIAN_POINT ( 'NONE',  ( 0.2509399751232620490, -0.4509356589572112162, -2.027996233343106081 ) ) ;
#164898=CARTESIAN_POINT ( 'NONE',  ( 5.092358660276916638, -1.001593112396873098, 1.509162939045370466 ) ) ;
#164902=CARTESIAN_POINT ( 'NONE',  ( 6.287769681992382509, 1.731225344711059266, -0.5331814487182000573 ) ) ;
#164905=CARTESIAN_POINT ( 'NONE',  ( 3.222796723461582413, 0.05406831605479084368, 2.190948157972896659 ) ) ;
#164906=CARTESIAN_POINT ( 'NONE',  ( 6.478945253086064504, 1.736940705955980269, 0.6686975948369151546 ) ) ;
#164908=CARTESIAN_POINT ( 'NONE',  ( 3.726117878570588626, 1.906711264527670258, 0.1841570787439601176 ) ) ;
#164911=DIRECTION ( 'NONE',  ( 2.949029909160572061E-17, 1.000000000000000000, -8.673600428462503284E-15 ) ) ;
#164915=CARTESIAN_POINT ( 'NONE',  ( 5.243409334377605369, 0.4101777817676309223, -2.077071965933465769 ) ) ;
#164916=CARTESIAN_POINT ( 'NONE',  ( 0.5323697292517782786, 1.110078392871534314, -1.854780036684190669 ) ) ;
#164919=CARTESIAN_POINT ( 'NONE',  ( 1.061231560844998034, 0.3605832424212577769, -1.789441408372116182 ) ) ;
#164921=CARTESIAN_POINT ( 'NONE',  ( 3.592628304870106870, -0.3553021837224104584, -1.790491875447843606 ) ) ;
#164923=CARTESIAN_POINT ( 'NONE',  ( 2.970861089138316036, -1.445268511421276214, 1.252435071843561731 ) ) ;
#164925=CARTESIAN_POINT ( 'NONE',  ( 2.488665619784910188, 1.909654154697162598, 0.4814545106021291265 ) ) ;
#164927=CARTESIAN_POINT ( 'NONE',  ( 5.355005569747676830, 0.3749256243090701712, -1.905367961469102811 ) ) ;
#164930=CARTESIAN_POINT ( 'NONE',  ( 5.080389167821143026, 1.047295930500062866, 1.843893106414703054 ) ) ;
#164931=MANIFOLD_SOLID_BREP ( 'Sweep1[4]', #36059 ) ;
#164933=CARTESIAN_POINT ( 'NONE',  ( 2.859904825981678833, 0.6862549603197342085, -1.785085608301796523 ) ) ;
#164937=CARTESIAN_POINT ( 'NONE',  ( 3.809243135778153100, 1.699416117590052622, -1.078869421455890709 ) ) ;
#164939=CARTESIAN_POINT ( 'NONE',  ( 4.670415550810885996, -1.190324863180821646, 1.384379922071424351 ) ) ;
#164940=CARTESIAN_POINT ( 'NONE',  ( 0.3970419974134198338, 0.3524218036512065111, 2.039982198586967943 ) ) ;
#164945=CARTESIAN_POINT ( 'NONE',  ( 5.647288160985431738, -1.475499438119257878, -1.149758287351684949 ) ) ;
#164955=CARTESIAN_POINT ( 'NONE',  ( 0.2685318824256071601, -0.8817220219094963340, -1.871193708407721035 ) ) ;
#164956=CARTESIAN_POINT ( 'NONE',  ( 2.706785462534053277, 1.994624666228937526, 0.7104243659002054123 ) ) ;
#164959=CARTESIAN_POINT ( 'NONE',  ( 5.946161111532238586, -0.9360204806616537754, 1.846680006623670156 ) ) ;
#164964=CARTESIAN_POINT ( 'NONE',  ( 2.748291532463055020, 0.7732563850255981253, 2.158024254592408209 ) ) ;
#164967=CARTESIAN_POINT ( 'NONE',  ( 2.250135261179100343, 0.8981609309555339538, -1.688322754368525747 ) ) ;
#164971=CARTESIAN_POINT ( 'NONE',  ( 0.5451820649361303062, 0.1524121550021810545, 2.007518037476815564 ) ) ;
#164972=CARTESIAN_POINT ( 'NONE',  ( 0.9362904128984714802, -1.094497954693674391, 1.627855050370475620 ) ) ;
#164976=CARTESIAN_POINT ( 'NONE',  ( 3.556657146437085970, -1.843967315269653628, -0.9851420625589295543 ) ) ;
#164977=CARTESIAN_POINT ( 'NONE',  ( 2.148939158097754376, -1.419410118233652485, -1.056944606630695560 ) ) ;
#164980=CARTESIAN_POINT ( 'NONE',  ( 5.718756930148481743, -0.06150597819632765140, 2.291595365457484323 ) ) ;
#164981=CARTESIAN_POINT ( 'NONE',  ( 4.927569761290923722, 0.8905454123377859466, -1.495065219958094938 ) ) ;
#164985=CARTESIAN_POINT ( 'NONE',  ( 3.057622914094188626, 1.488722154369751083, -0.8884403576015533766 ) ) ;
#164986=( BOUNDED_SURFACE ( )  B_SPLINE_SURFACE ( 3, 3, ( 
 ( #56776, #140189, #206210, #157495, #208342, #109865, #77291, #13352, #207283, #189968, #93567, #144475, #194239, #143402, #159612, #41617, #43751, #59973, #191022, #125066, #12276, #91433, #112005, #145545, #42689, #9089, #29623, #27469, #141273, #107730, #209398, #210480, #211542, #79427, #174822, #63177, #45884, #161761, #110926, #26398, #62118, #11209, #178006, #173756, #176930, #25333, #10146, #95707, #58911, #175879, #75164, #28548, #61043, #78352, #108796, #94637, #92511, #158548, #76221, #142330, #126126, #192086, #127204, #193171, #44821, #160681, #128278, #180133, #84755, #31760, #167085, #48025, #150842, #166009, #18676, #34922, #97831, #2403, #15472, #129342, #195320, #100995, #98887, #130393, #1343, #46951, #163896, #80496, #212611, #81556, #199553, #16532, #181186, #197432, #113068, #50131, #146593, #198486, #64251, #17594, #133546, #196384, #147639, #114141, #131430, #213658, #65283, #66338, #116253, #49073, #179074, #115193, #30695, #33866, #96777, #32812, #162828, #14405, #164939, #82614, #148699, #67405, #268, #132484, #182241, #99944, #83677, #51198, #149767, #117320, #183318, #52260, #203812, #85822, #137793, #19742, #171334, #72762, #69544, #37062, #135652, #70607, #152958, #151901, #5598, #55457, #202746, #134609, #20796, #200613, #187580, #40286, #156176, #24008, #90110, #201675, #122693, #22929, #136721, #89044, #4533, #188654, #39207, #118386, #68482, #119455, #86892, #186514, #35994, #54398, #120538, #170265, #106395, #3476, #184374, #38145, #155101, #138861, #21851, #104218, #102075, #87958, #154032, #53322, #185442, #105298, #168142, #204876, #103144, #169203, #71679, #172419, #121610, #6685, #56531, #27215, #176679, #177752, #111746, #207031, #45629, #12031, #193981, #143158, #58660, #28292, #43503, #78103, #29367, #209152, #139938, #42437, #144230, #173505, #75977, #57597, #60791, #191840, #44564, #25079, #126950, #124813, #190775, #91182, #108543, #205965, #74914, #141022, #157242, #142080, #8836, #174573, #26149, #95462, #92264, #7756, #158309, #73843, #110679, #123755, #128027, #9901, #189717, #208095, #41369, #59722, #107481, #125881, #109623, #175628, #93321, #94386, #159357, #10955, #77029, #192907, #160426, #210224, #61862, #213414, #15221, #145288, #82360, #178828, #16276, #112814, #49871, #165758, #162573, #130145, #14147, #163639, #31507, #30440, #98630, #148450, #81311, #13092, #113888, #79172, #66083, #133287, #34674, #117063, #183061, #80241, #1090, #115997, #147387, #181985, #97581, #67152, #132226, #211293, #161511, #212353, #179883, #65036, #129086, #131193, #197181, #48818, #199294, #96525, #62918, #114934, #33617, #17343, #180931, #32554, #195058, #164690, #19, #146339, #63993, #198235, #46697, #83425, #196135, #47774, #99687, #50939, #149506, #52008, #100744, #120274, #55203, #56271, #204619, #85558, #138596, #105035, #72497, #21591, #151648, #121348, #136467, #171073, #122429, #87695, #18420, #135397, #22669, #118134, #168945, #150585, #153770, #70350, #137532, #184120, #5338, #3218, #69285, #35740, #201420, #84495, #167883, #19483, #101815, #20547, #53058, #119193, #185179, #188386, #36803, #166826, #102886, #2147, #203548, #68224, #6423, #134355, #202486, #86631, #187324, #200360, #152698, #4279, #54138, #186248, #88781, #37883, #103960, #170003, #71421, #38953, #154838 ),
 ( #26948, #174306, #106135, #206767, #172158, #159094, #11763, #127762, #209954, #61591, #173236, #94125, #208888, #42171, #142887, #124556, #160163, #10694, #23751, #40023, #90918, #58401, #158050, #7491, #190514, #25881, #141828, #77837, #57334, #89855, #9636, #60519, #44295, #207830, #75714, #155906, #108287, #91991, #41105, #189462, #76765, #73575, #176420, #139676, #107214, #205699, #143959, #59458, #123498, #24816, #125616, #126680, #156982, #8571, #74651, #140756, #110417, #191575, #175366, #43238, #192642, #109355, #28027, #93056, #114676, #111478, #13887, #197976, #145016, #47503, #29099, #32295, #163370, #16010, #211021, #180669, #30161, #96249, #62645, #162302, #177485, #46422, #112539, #128804, #113612, #194786, #178551, #79966, #149239, #146070, #17082, #212083, #814, #82095, #83159, #99432, #63721, #66882, #129879, #193718, #45361, #148188, #49605, #147127, #97311, #95183, #179617, #195862, #31237, #14945, #214190, #161232, #115729, #12819, #81042, #78893, #33350, #213153, #64783, #130925, #196918, #65817, #48557, #98361, #164426, #131964, #181720, #165485, #53882, #117877, #87454, #168690, #137282, #104780, #120016, #50672, #167626, #203301, #84238, #201165, #182796, #185992, #102633, #169757, #150325, #37626, #183867, #35482, #1892, #101559, #116798, #200104, #51755, #67951, #52805, #134096, #19227, #85305, #88528, #151391, #170827, #2961, #154589, #21344, #22418, #38701, #69032, #6167, #135149, #133026, #199025, #34415, #20294, #118943, #5090, #100487, #184923, #36546, #86380, #152448, #54948, #4026, #70096, #136211, #166562, #103706, #202230, #153521, #71165, #121101, #187068, #18151, #40851, #139415, #74406, #156731, #89602, #9394, #59205, #206517, #138344, #24562, #204361, #191325, #44049, #159914, #27779, #93877, #205448, #126431, #26705, #140506, #175118, #8321, #192394, #42991, #56017, #72236, #123248, #90668, #190266, #39768, #58149, #124307, #174061, #110169, #155653, #122171, #41924, #108035, #176179, #189211, #109104, #60274, #91745, #188137, #157798, #25633, #75466, #105873, #141578, #171898, #23496, #7235, #73312, #57083, #106958, #172983, #207585, #125361, #92807, #10448, #158851, #76521, #208642, #142632, #211842, #180428, #128573, #78650, #177237, #48317, #193480, #127510, #77590, #131720, #146891, #79721, #99180, #194537, #144777, #62409, #46184, #112298, #209706, #178314, #28850, #179376, #197724, #63480, #11521, #29923, #160986, #45124, #163125, #195621, #96006, #212911, #12578, #162060, #210786, #94938, #143714, #164183, #13649, #61350, #145838, #64544, #114428, #33106, #129634, #47256, #65573, #113370, #130688, #196678, #30997, #111234, #97072, #14707, #32045, #80801, #98133, #15769, #81854, #181476, #147936, #213952, #49364, #115483, #7786, #188688, #168430, #40324, #82909, #101289, #106429, #183605, #100228, #133837, #68770, #167371, #189747, #132768, #205994, #102358, #20026, #198771, #36281, #86116, #557, #41399, #66621, #18959, #200897, #50420, #116540, #73879, #166296, #52544, #182530, #34159, #172452, #69830, #17887, #53613, #123789, #199848, #134890, #165232, #16825, #117613, #83971, #148982, #139972, #24039, #152186, #90142, #150060, #85043, #156210, #35214, #1632, #51491, #118677, #151131, #67691, #2698, #57630, #3755, #135938, #184661, #201956, #119746, #157276, #195092, #8865 ),
 ( #141055, #210256, #62947, #159388, #161539, #158339, #144263, #95492, #126982, #129116, #192941, #191872, #175657, #79204, #44593, #107509, #13126, #145321, #74944, #58692, #211322, #174604, #110708, #190806, #92295, #45660, #60821, #61894, #29400, #207062, #93351, #128055, #9933, #26180, #124840, #194011, #42466, #108576, #173538, #25112, #28321, #27245, #91215, #76008, #142111, #208124, #59753, #125913, #43532, #109655, #10986, #176708, #77060, #143190, #209181, #94417, #160456, #12064, #78133, #111778, #177784, #182011, #47803, #15250, #113916, #212382, #46729, #199322, #81337, #112841, #114962, #33642, #83455, #68253, #147416, #196162, #100772, #16305, #99716, #165788, #213441, #178857, #31535, #48848, #17371, #65064, #149535, #18450, #1121, #30468, #131220, #50969, #64024, #180962, #96553, #67183, #82390, #133320, #130170, #117091, #97610, #163667, #179912, #197208, #162600, #32584, #98661, #164716, #148479, #47, #66111, #132254, #2177, #198261, #84527, #49904, #134386, #183091, #150616, #166854, #116026, #14176, #34703, #80269, #146367, #172193, #170035, #201448, #72531, #23782, #36832, #151678, #69316, #102915, #56301, #87729, #37917, #54167, #184148, #121382, #3248, #55235, #135426, #88813, #204652, #53091, #168975, #119224, #202517, #70380, #185208, #137566, #187355, #120305, #52037, #152727, #118163, #105070, #89888, #73608, #155939, #7525, #20576, #40057, #154871, #186280, #6454, #136496, #106166, #171108, #35772, #200389, #86660, #4308, #103991, #167916, #21621, #153801, #5374, #101846, #71453, #19513, #203583, #138628, #122463, #38985, #22701, #85590, #188421, #9669, #140785, #74684, #176450, #41137, #61627, #95217, #206799, #107247, #193748, #191607, #90949, #139707, #159127, #94155, #161267, #29130, #124585, #177517, #143993, #111511, #60553, #190545, #160194, #175394, #209985, #126713, #108317, #109389, #12853, #205730, #92024, #173268, #57366, #45394, #11796, #142919, #77870, #123528, #75745, #127793, #158082, #58432, #174338, #43269, #141857, #189493, #24848, #157016, #76798, #208919, #8600, #10728, #192673, #42202, #25916, #207864, #59488, #26980, #125645, #93085, #44327, #110449, #28062, #30196, #112576, #165524, #198013, #178588, #181753, #34452, #130962, #133064, #129914, #115764, #66922, #98397, #100524, #164461, #163405, #147162, #50708, #16047, #166599, #199062, #116834, #128837, #96285, #182835, #146106, #82131, #162337, #63754, #17115, #32328, #33387, #856, #194819, #64816, #99465, #195900, #212116, #13920, #83193, #46454, #80000, #145051, #78928, #214225, #213189, #211053, #47535, #113649, #179653, #31273, #97348, #62677, #14980, #81076, #148223, #196954, #48592, #114710, #180705, #65853, #132003, #49641, #149275, #201201, #153554, #19261, #52840, #85343, #183904, #18188, #170861, #118976, #84273, #86414, #5125, #54985, #39804, #184955, #167660, #72271, #202265, #71200, #137316, #36581, #150360, #2997, #20328, #203332, #102669, #21380, #67990, #105911, #134132, #152481, #53916, #200140, #117912, #138380, #151424, #120053, #35514, #51793, #104815, #121138, #101592, #187100, #188170, #70132, #204398, #69066, #38734, #6202, #37664, #1930, #103740, #168726, #4063, #56051, #169791, #135186, #122207, #136245, #186027, #87488, #22452, #88564, #154622, #40886, #156767, #110200, #125393, #208675, #93910 ),
 ( #8353, #209741, #90705, #193513, #60305, #61384, #77624, #74438, #127542, #58181, #45154, #23528, #143746, #141610, #173015, #44082, #171937, #140538, #123284, #106990, #206553, #27812, #59235, #9428, #25667, #155687, #92840, #189247, #26738, #24596, #126464, #176210, #124340, #190297, #41955, #174094, #108067, #91774, #109138, #158885, #157832, #89636, #75498, #7271, #76555, #73347, #139449, #205483, #57115, #207619, #11554, #192427, #191360, #159951, #43026, #175151, #142665, #10481, #66659, #162094, #63517, #14742, #78685, #129670, #31031, #212941, #149018, #128605, #111268, #80833, #65603, #115515, #64578, #13683, #132806, #79753, #593, #29955, #198810, #147973, #177271, #16864, #145869, #28886, #211877, #94970, #161017, #82944, #146924, #112335, #197758, #12612, #195655, #62442, #194572, #47289, #181510, #130719, #163157, #179410, #144810, #32078, #46217, #180462, #178347, #213983, #33139, #96041, #113404, #97105, #196710, #48351, #114462, #98166, #164214, #15801, #210817, #81887, #131753, #49396, #99219, #165269, #5934, #72005, #183646, #104547, #4857, #52581, #153281, #134928, #170592, #21111, #34192, #138118, #101326, #2735, #168464, #17924, #68806, #184697, #152222, #88294, #67725, #50456, #20062, #70936, #54716, #3793, #86151, #116575, #118709, #200933, #51528, #199883, #87217, #166332, #186839, #182570, #117653, #84008, #22178, #102396, #1671, #100267, #69867, #137046, #150099, #154355, #35250, #133876, #120865, #167407, #185762, #18999, #203072, #135976, #38471, #85080, #37394, #151164, #36318, #201991, #53649, #119781, #103469, #169531, #173833, #26480, #7003, #191102, #40622, #106725, #73080, #172752, #187903, #56853, #123027, #139181, #124083, #205211, #188978, #204127, #24327, #90435, #105634, #141354, #25410, #156503, #125145, #8092, #74181, #140274, #155419, #55780, #142411, #206293, #121937, #57918, #42770, #92590, #11290, #190046, #41698, #43831, #91515, #108877, #174901, #107808, #39533, #157574, #9167, #158632, #75242, #10229, #207368, #58988, #159691, #171662, #76304, #23258, #89370, #109947, #208419, #60053, #126208, #192170, #175956, #27552, #93648, #77370, #128354, #145625, #95785, #147720, #44900, #15548, #113146, #30776, #111008, #47031, #179152, #127282, #213737, #193253, #161842, #63256, #177013, #28630, #97913, #160760, #129418, #94717, #12354, #130471, #14485, #78433, #146673, #143484, #211620, #163972, #62198, #212688, #31837, #96855, #209481, #162903, #13430, #79506, #81635, #80574, #61122, #144555, #210564, #178086, #195401, #194322, #64330, #45964, #196462, #48104, #112085, #29704, #114216, #180215, #172388, #108511, #76995, #25049, #189685, #73807, #159323, #90078, #23976, #188621, #28259, #43467, #190740, #210189, #91151, #41337, #173470, #157205, #8802, #106364, #74881, #139901, #75942, #94352, #174537, #206997, #123722, #57565, #10919, #156141, #44528, #78069, #107445, #7725, #176647, #26113, #205932, #122658, #142043, #143122, #144195, #11994, #140988, #160393, #126915, #40253, #109586, #58628, #209114, #158276, #192872, #124781, #175591, #42404, #92225, #110646, #9866, #208058, #59685, #27181, #125845, #60752, #191802, #93287, #112779, #178791, #79136, #30404, #45596, #129050, #195025, #145252, #196100, #62881, #46658, #96491, #17308, #162541, #99651, #14111, #83386, #98592, #165720 ),
 ( #80200, #13055, #211258, #146304, #132191, #163601, #113851, #130107, #111712, #197144, #212316, #131154, #63952, #164655, #66048, #47733, #179846, #31470, #97543, #15183, #81272, #213377, #48782, #147350, #127994, #65000, #193949, #180896, #33578, #149468, #61827, #177721, #114898, #115959, #16239, #32518, #82323, #148416, #181949, #156065, #29330, #95424, #198200, #49834, #161477, #36291, #181484, #70908, #33113, #148990, #4828, #118686, #102368, #565, #52554, #184670, #16834, #54686, #99190, #137018, #165241, #66632, #203045, #168438, #20037, #132777, #86123, #152197, #82917, #198780, #50429, #183616, #2706, #116548, #182540, #87188, #34167, #68780, #100238, #166306, #53623, #3764, #17895, #69839, #83981, #18969, #21085, #150069, #135950, #169503, #200905, #1641, #201965, #51498, #35223, #153253, #119755, #67699, #133846, #199856, #117625, #101299, #167379, #85052, #185734, #151139, #134899, #37367, #103442, #157545, #42741, #170565, #106697, #75215, #23231, #187877, #71977, #9141, #88262, #22147, #186812, #26452, #41670, #188952, #208392, #89343, #39504, #171634, #155391, #6974, #104520, #73055, #138086, #74149, #92561, #172722, #120836, #139154, #55752, #154330, #57889, #90404, #205184, #107781, #121908, #56825, #105603, #204100, #38440, #58961, #122995, #5904, #40592, #173806, #141326, #142383, #24300, #156474, #174872, #8063, #25385, #91484, #140243, #206264, #124052, #190018, #207339, #125116, #191074, #108846, #158601, #76275, #10200, #12326, #93621, #192141, #114188, #80546, #63227, #146643, #43805, #210536, #212658, #78406, #64300, #196433, #129390, #109918, #147691, #175929, #62170, #95758, #27522, #159663, #180187, #61096, #161811, #11264, #77342, #130445, #179123, #143454, #162875, #15521, #112056, #31809, #110978, #96826, #48077, #79477, #81607, #145595, #144527, #128329, #97885, #211591, #60026, #163946, #126177, #209452, #127255, #193226, #44873, #195369, #176984, #28602, #94691, #13401, #14455, #160732, #194292, #45937, #178056, #29674, #47001, #113117, #30745, #181234, #115244, #65332, #119507, #134659, #67454, #86944, #182292, #66389, #50181, #33919, #116302, #197483, #166060, #164992, #167136, #185493, #199605, #213709, #99994, #148749, #32862, #150894, #183370, #17647, #200662, #319, #83731, #132537, #16583, #131479, #151953, #149823, #49126, #133600, #52311, #36045, #20845, #1393, #198535, #53372, #34975, #118441, #184428, #51248, #98938, #117373, #101046, #102125, #18721, #168194, #84805, #2455, #169259, #82665, #68531, #19793, #85876, #37118, #3523, #69597, #135705, #201731, #103197, #6736, #74964, #54449, #7808, #153011, #42487, #4587, #120592, #190828, #90165, #73901, #186569, #24062, #139994, #189771, #174624, #187633, #88013, #207082, #122747, #206015, #57651, #121666, #70661, #137846, #155155, #123810, #39260, #41422, #105354, #188709, #108596, #136771, #171391, #38197, #202800, #58713, #173561, #156231, #25133, #104270, #170315, #72815, #141074, #21903, #107530, #154084, #26200, #5652, #71732, #203867, #91235, #157295, #55511, #8885, #124862, #22982, #89101, #138917, #204936, #40345, #56587, #106451, #172475, #93372, #194032, #43553, #125933, #178877, #211343, #191891, #195113, #47823, #144283, #146387, #143212, #129137, #80289, #111799, #113934, #177805, #176730, #160478, #64043, #29421, #179930 ),
 ( #46750, #14196, #142131, #78152, #112862, #209202, #159408, #109674, #30489, #59774, #208145, #158359, #212401, #13148, #12085, #92318, #60842, #11008, #127004, #192962, #44615, #76028, #110730, #175676, #45683, #130188, #210276, #9952, #28344, #27265, #77085, #95512, #61916, #94439, #79225, #128076, #161560, #145342, #62968, #96573, #162620, #196181, #31554, #99734, #119244, #85611, #151699, #81355, #197226, #135446, #98678, #34720, #114982, #16325, #184170, #199342, #68273, #167934, #147435, #17390, #200409, #148497, #164734, #48866, #134405, #213459, #65083, #97629, #3268, #166875, #165806, #163686, #65, #82408, #66129, #132273, #198281, #15268, #49922, #180982, #50989, #69335, #83473, #131238, #116043, #32603, #182031, #183112, #1139, #33660, #18467, #149554, #67201, #133338, #117110, #100791, #35790, #84545, #150635, #2196, #52055, #118182, #53111, #101866, #19534, #201468, #154893, #23801, #172212, #153823, #36851, #170055, #187374, #89906, #5394, #155958, #71472, #6474, #140806, #102935, #137585, #4329, #168995, #24867, #205751, #188441, #57382, #20594, #70398, #39005, #107265, #86680, #40075, #185228, #74702, #152747, #136516, #8620, #122480, #106187, #202535, #56320, #7544, #54184, #58452, #120324, #105089, #72551, #186300, #37936, #90971, #104010, #138649, #21640, #87747, #123546, #73629, #203602, #139728, #206818, #22721, #157033, #55255, #189511, #173285, #204671, #121402, #41156, #171127, #88835, #96303, #61648, #192693, #605, #93105, #191626, #175415, #159147, #26999, #108338, #76819, #75767, #77892, #162359, #110469, #124607, #10748, #59507, #25936, #127815, #94176, #142939, #45416, #125664, #208939, #43289, #141875, #190565, #62698, #60574, #42221, #44347, #111532, #161288, #146124, #126733, #109410, #178609, #160215, #177539, #29150, #176470, #174358, #28080, #11816, #95239, #144013, #12874, #210006, #193770, #80021, #92044, #78950, #158101, #9690, #30219, #145072, #211075, #128859, #207884, #194841, #46474, #112597, #13938, #135989, #66670, #170605, #132819, #34204, #104561, #3805, #202004, #100278, #152234, #69879, #116587, #154370, #182582, #68817, #102409, #166344, #17935, #186852, #67737, #168476, #84020, #150111, #153293, #185775, #1683, #169545, #22192, #118721, #120878, #117665, #103482, #54728, #86163, #88306, #53662, #151176, #134939, #38484, #119795, #198822, #50468, #133887, #199894, #51540, #183657, #35262, #37408, #101338, #167420, #4870, #20074, #21124, #203083, #19011, #52594, #87230, #85092, #2747, #200945, #70948, #184708, #36330, #137059, #126220, #141367, #91528, #90448, #74194, #192181, #157587, #93661, #60064, #43844, #55793, #171675, #109959, #73093, #9182, #89383, #205224, #158642, #173846, #42781, #142421, #121949, #206307, #174912, #123040, #139193, #23271, #108890, #187915, #39546, #72017, #175969, #207379, #140287, #5947, #188992, #56865, #40634, #106737, #172765, #204139, #24339, #155431, #25422, #27563, #57931, #138130, #156515, #7017, #105647, #75253, #190059, #8105, #59000, #124095, #41711, #107821, #125156, #191115, #10240, #26493, #92600, #76315, #208430, #196474, #181273, #194333, #94728, #213747, #129429, #212700, #146684, #128366, #11302, #144565, #161853, #64341, #45975, #130486, #112096, #195413, #115281, #77380, #178098, #193265, #143496, #65370, #180226, #162915 ),
 ( #159702, #63268, #114228, #163983, #113159, #47042, #209492, #13442, #29715, #160774, #12367, #48116, #61133, #81645, #32899, #78447, #127294, #131517, #211632, #111019, #44911, #179163, #31848, #177024, #49164, #210577, #197520, #15558, #28641, #97925, #62209, #147732, #95797, #30787, #79518, #145637, #96866, #14496, #80588, #54484, #184464, #183408, #167172, #70695, #36082, #186605, #153049, #4624, #148784, #50220, #202835, #166096, #102165, #182330, #83770, #37158, #52352, #135744, #20880, #354, #84844, #53407, #1431, #17684, #116339, #201767, #66427, #132570, #165030, #136809, #19831, #18759, #98977, #67496, #149863, #133640, #199641, #51287, #82705, #117412, #33958, #118479, #120629, #150933, #16623, #35012, #100034, #198571, #168233, #68569, #101083, #85915, #2495, #134696, #200700, #151989, #3563, #103235, #69636, #119545, #185530, #169295, #86979, #59812, #72847, #187668, #92351, #7846, #91273, #25172, #6771, #104307, #23019, #40382, #157330, #138952, #8922, #204973, #73933, #208180, #170355, #56619, #71768, #21940, #158389, #58748, #41457, #124901, #88050, #137884, #106485, #174658, #154121, #107565, #38232, #142163, #5691, #203904, #76064, #189805, #173600, #55550, #123844, #75003, #121704, #125967, #39298, #172512, #140027, #105391, #171431, #9986, #89136, #206052, #155190, #122783, #190864, #141112, #188743, #207123, #24098, #57687, #90201, #156265, #42527, #108632, #26234, #31592, #212441, #195154, #64083, #109705, #11042, #45721, #113973, #93407, #46788, #191923, #81393, #43588, #159444, #15305, #129177, #112902, #77121, #63007, #178913, #27300, #65120, #143244, #194068, #13187, #209233, #60878, #97667, #192997, #79265, #127037, #44650, #130226, #96608, #110764, #80326, #147478, #29457, #163725, #28379, #14231, #179970, #211380, #213498, #30528, #61951, #111840, #175710, #162662, #176763, #94473, #160514, #12117, #78191, #144317, #210315, #146427, #128110, #177844, #196220, #145382, #47862, #95546, #161598, #117151, #85651, #33701, #198320, #82445, #167973, #98718, #32641, #197264, #36894, #52094, #199382, #4369, #99778, #49960, #182069, #165843, #17429, #115024, #83512, #148535, #84589, #102976, #183154, #131276, #149595, #66168, #164777, #68314, #100831, #1179, #118221, #132315, #67243, #116079, #102, #48904, #69378, #133377, #181021, #51029, #184207, #19579, #152789, #34757, #166916, #185271, #18510, #35830, #101908, #150676, #16367, #2237, #134445, #200448, #151738, #3308, #135486, #201508, #53156, #119285, #169034, #20631, #86720, #189548, #42261, #158138, #25975, #92081, #203642, #124646, #24905, #72590, #173327, #154929, #190603, #41196, #54228, #70439, #71513, #107303, #139767, #8662, #206858, #108374, #91011, #174397, #87791, #136555, #188484, #157073, #74742, #23838, #40114, #202576, #138691, #6514, #137625, #5434, #140846, #186341, #58490, #120366, #55293, #37976, #104049, #122521, #21681, #170095, #89946, #153865, #121443, #187412, #39043, #105128, #171168, #22758, #205793, #88875, #204708, #106225, #56358, #172251, #57423, #155996, #7583, #73668, #123585, #77933, #59546, #62741, #193807, #46519, #27037, #211117, #60615, #126774, #93146, #192732, #207924, #76859, #142978, #159183, #144054, #10784, #208978, #44387, #179716, #110508, #47598, #176508, #31333, #112641, #113712, #129976, #28120 ) ),
 .UNSPECIFIED., .T., .F., .T. ) 
 B_SPLINE_SURFACE_WITH_KNOTS ( ( 4, 3, 4 ),
 ( 4, 1, 1, 1, 1, 1, 1, 1, 1, 1, 1, 1, 1, 1, 1, 1, 1, 1, 1, 1, 1, 1, 1, 1, 1, 1, 1, 1, 1, 1, 1, 1, 1, 1, 1, 1, 1, 1, 1, 1, 1, 1, 1, 1, 1, 1, 1, 1, 1, 1, 1, 1, 1, 1, 1, 1, 1, 1, 1, 1, 1, 1, 1, 1, 1, 1, 1, 1, 1, 1, 1, 1, 1, 1, 1, 1, 1, 1, 1, 1, 1, 1, 1, 1, 1, 1, 1, 1, 1, 1, 1, 1, 1, 1, 1, 1, 1, 1, 1, 1, 1, 1, 1, 1, 1, 1, 1, 1, 1, 1, 1, 1, 1, 1, 1, 1, 1, 1, 1, 1, 1, 1, 1, 1, 1, 1, 1, 1, 1, 1, 1, 1, 1, 1, 1, 1, 1, 1, 1, 1, 1, 1, 1, 1, 1, 1, 1, 1, 1, 1, 1, 1, 1, 1, 1, 1, 1, 1, 1, 1, 1, 1, 1, 1, 1, 1, 1, 1, 1, 1, 1, 1, 1, 1, 1, 1, 1, 1, 1, 1, 1, 1, 1, 1, 1, 1, 1, 1, 1, 1, 1, 1, 1, 1, 1, 1, 1, 1, 1, 1, 1, 1, 1, 1, 1, 1, 1, 1, 1, 1, 1, 1, 1, 1, 1, 1, 1, 1, 1, 1, 1, 1, 1, 1, 1, 1, 1, 1, 1, 1, 1, 1, 1, 1, 1, 1, 1, 1, 1, 1, 1, 1, 1, 1, 1, 1, 1, 1, 1, 1, 1, 1, 1, 1, 1, 1, 1, 1, 1, 1, 1, 1, 1, 1, 1, 1, 1, 1, 1, 1, 1, 1, 1, 1, 1, 1, 1, 1, 1, 1, 1, 1, 1, 1, 1, 1, 1, 1, 1, 1, 1, 1, 1, 1, 1, 1, 1, 1, 1, 1, 1, 1, 1, 1, 1, 1, 1, 1, 1, 1, 1, 1, 1, 1, 1, 1, 1, 1, 1, 1, 1, 1, 1, 1, 1, 1, 1, 1, 1, 1, 1, 1, 1, 1, 1, 1, 1, 1, 1, 1, 1, 1, 1, 1, 1, 1, 1, 1, 1, 1, 1, 1, 1, 1, 1, 1, 1, 1, 1, 1, 1, 1, 1, 1, 1, 1, 1, 1, 1, 1, 1, 1, 1, 1, 1, 1, 1, 1, 1, 1, 1, 1, 1, 1, 4 ),
 ( 0.000000000000000000, 0.5000000000000000000, 1.000000000000000000 ),
 ( 0.000000000000000000, 0.002600214693118923798, 0.005208871813129847643, 0.007813341859462101871, 0.01041561011214237054, 0.01302159838915000617, 0.01562452542669844589, 0.01822945805747129902, 0.02083332260852943998, 0.02343713088342555886, 0.02604210653276634729, 0.02864513693292065552, 0.03125071383394792401, 0.03385356881896259273, 0.03645895053148855841, 0.03906228851054763251, 0.04166670673482164577, 0.04427111720854654681, 0.04687446234244373178, 0.04947983976256019323, 0.05208269766733494843, 0.05468827385445936690, 0.05729129101459448647, 0.05989628262864687969, 0.06250008845252298662, 0.06510390268380349121, 0.06770888856031336001, 0.07031191025079500112, 0.07291748459129859805, 0.07552033970978830335, 0.07812571920045624507, 0.08072905536012038585, 0.08333347174482363950, 0.08593788071299547637, 0.08854122383090638759, 0.09114659965375219997, 0.09374945576594469199, 0.09635503022752239799, 0.09895804583665256116, 0.1015630356028039000, 0.1041668400134527495, 0.1067706523020897913, 0.1093756367037285043, 0.1119786565701353653, 0.1145842293264338063, 0.1171870828570002881, 0.1197924606432616973, 0.1223957954228293843, 0.1250002099740243899, 0.1276046175975352470, 0.1302079588893767237, 0.1328133332639841735, 0.1354161877457908392, 0.1380217606440506395, 0.1406247748629219918, 0.1432297629411592166, 0.1458335661004374617, 0.1484373766077259071, 0.1510423596945167368, 0.1536453778991425101, 0.1562509492307036785, 0.1588538013357113088, 0.1614591775772540871, 0.1640625111385781432, 0.1666669240170048083, 0.1692713304565471311, 0.1718746700842041231, 0.1744800431702197008, 0.1770828961840006377, 0.1796884676783837009, 0.1822914806691622869, 0.1848964672195632097, 0.1875002692887918765, 0.1901040781760970355, 0.1927090601080766463, 0.1953120768130981733, 0.1979176468793322763, 0.2005204977210985895, 0.2031258725775486607, 0.2057292050824250096, 0.2083336164487647746, 0.2109380218649763994, 0.2135413599902747928, 0.2161467319472901716, 0.2187495836553486062, 0.2213551539052408534, 0.2239581658300387468, 0.2265631510126252801, 0.2291669521530730058, 0.2317707595817034838, 0.2343757405188569010, 0.2369787558863956922, 0.2395843248466610342, 0.2421871745874512594, 0.2447925482183819501, 0.2473958798285567084, 0.2500002898434375842, 0.2526046943969075254, 0.2552080311816201097, 0.2578134021691782518, 0.2604162527337665622, 0.2630218218985046486, 0.2656248329193858781, 0.2682298168941298910, 0.2708336172670197106, 0.2734374233982336255, 0.2760424035005001331, 0.2786454176926287940, 0.2812509857062375773, 0.2838538345082703418, 0.2864592070732082663, 0.2890625379503836689, 0.2916669467743862043, 0.2942713506256608436, 0.2968746862315132518, 0.2994800564091141259, 0.3020829059924399762, 0.3046884742313171190, 0.3072914845103039694, 0.3098964674371332273, 0.3125002672036480411, 0.3151040721986592130, 0.3177090516259382103, 0.3203120648046862140, 0.3229176320309106729, 0.3255204800563645251, 0.3281258517147956355, 0.3307291820206363919, 0.3333335898142997245, 0.3359379931238887229, 0.3385413277125659537, 0.3411466972396727249, 0.3437495460039050044, 0.3463551134761772565, 0.3489581231752558743, 0.3515631052140602009, 0.3541669045353489920, 0.3567707085553323276, 0.3593756874674896018, 0.3619786997948497009, 0.3645842663929277916, 0.3671871138039469185, 0.3697924847153226668, 0.3723958146114617063, 0.3750002215352895019, 0.3776046244636719340, 0.3802079581968237365, 0.3828133272328684833, 0.3854161753401436075, 0.3880217422050354359, 0.3906247514861621029, 0.3932297327967993472, 0.3958335318339832876, 0.3984373350400814418, 0.4010423135969549691, 0.4036453252348887744, 0.4062508913640303643, 0.4088537383227308641, 0.4114591086464738368, 0.4140624382945181647, 0.4166668445089845574, 0.4192712472166146842, 0.4218745802558619973, 0.4244799489602520959, 0.4270827965726798348, 0.4296883629893904488, 0.4322913720144979099, 0.4348963527567997200, 0.4375001516709778882, 0.4401039542243071478, 0.4427089325857130886, 0.4453119436961573974, 0.4479175095155500941, 0.4505203561840259718, 0.4531257260795358843, 0.4557290556410732441, 0.4583334613066292196, 0.4609378639539425948, 0.4635411964608836533, 0.4661465649930071620, 0.4687494122726767465, 0.4713549784003855381, 0.4739579873313886638, 0.4765629676651664814, 0.4791667666174222462, 0.4817705686790782482, 0.4843755470048167200, 0.4869785577496898998, 0.4895841234185048796, 0.4921869699588339309, 0.4947923395854939010, 0.4973956692220981579, 0.5000000744991768276, 0.5026044772465965149, 0.5052078093828125116, 0.5078131779020444991, 0.5104160250110306718, 0.5130215910089035436, 0.5156246000077054914, 0.5182295800927568807, 0.5208333792441637300, 0.5234371809752277338, 0.5260421594250891397, 0.5286451699662961801, 0.5312507356436946271, 0.5338535822179446555, 0.5364589517351265879, 0.5390622816083643354, 0.5416666866573878192, 0.5442710896653298880, 0.5468744215923915242, 0.5494797902580997873, 0.5520826373584690749, 0.5546882033856646022, 0.5572912126141627009, 0.5598961926102767883, 0.5624999921219043797, 0.5651037936834493181, 0.5677087724172201755, 0.5703117829166597375, 0.5729173487617980065, 0.5755201955320329299, 0.5781255650991041772, 0.5807288953705399548, 0.5833333003519244331, 0.5859377037808047861, 0.5885410356602774895, 0.5911464046318289922, 0.5937492518856454238, 0.5963548181013198501, 0.5989578277214122615, 0.6015628077883760083, 0.6041666078212959423, 0.6067704093743923055, 0.6093753885518610192, 0.6119783991714310423, 0.6145839653434672645, 0.6171868124717531101, 0.6197921822480817466, 0.6223955130792849788, 0.6249999181534476866, 0.6276043221636865566, 0.6302076541571374202, 0.6328130235939036785, 0.6354158711632348355, 0.6380214377265494008, 0.6406244479001403924, 0.6432294281977445349, 0.6458332289130368498, 0.6484370306187589028, 0.6510420103997216490, 0.6536450213013255128, 0.6562505879594253688, 0.6588534356078361576, 0.6614588057527972520, 0.6640621373053481324, 0.6666665426327121891, 0.6692709473847417989, 0.6718742796537453543, 0.6744796497151083203, 0.6770824977620315543, 0.6796880648321572682, 0.6822910757211636534, 0.6848960564092084757, 0.6874998579679674204, 0.6901036599873985322, 0.6927086405316660311, 0.6953116518772185506, 0.6979172191805607106, 0.7005200675111846742, 0.7031254381841663958, 0.7057287706196612165, 0.7083331763606625087, 0.7109375820149322900, 0.7135409147210758363, 0.7161462855664346705, 0.7187491342530435423, 0.7213547019891674017, 0.7239577137555243125, 0.7265626949938263079, 0.7291664975571658935, 0.7317703000514055311, 0.7343752815188082650, 0.7369782934702413524, 0.7395838615780243597, 0.7421867107529701579, 0.7447920821133793279, 0.7473954155934371402, 0.7499998219085300954, 0.7526042286255122393, 0.7552075619304030596, 0.7578129337191791270, 0.7604157832075884027, 0.7630213517689198310, 0.7656243645745874904, 0.7682293465229839136, 0.7708331502520449074, 0.7734369533822141873, 0.7760419359326080624, 0.7786449486518774998, 0.7812505177233250997, 0.7838533679047272607, 0.7864587401119955690, 0.7890620747982641792, 0.7916664818479275390, 0.7942708897881238794, 0.7968742238533942368, 0.7994795967450375462, 0.8020824471973901915, 0.8046880167431663677, 0.8072910307501349747, 0.8098960135684915018, 0.8124998186244467568, 0.8151036225516941069, 0.8177086063449673370, 0.8203116199940584385, 0.8229171901884252405, 0.8255200415384508217, 0.8281254147520410447, 0.8307287508062024539, 0.8333331587509454907, 0.8359375680748931670, 0.8385409030622068549, 0.8411462772162020540, 0.8437491287946751184, 0.8463546994841673055, 0.8489577148544642515, 0.8515626987026798655, 0.8541665052467400931, 0.8567703101322480252, 0.8593752953283267937, 0.8619783100692604005, 0.8645838815458386506, 0.8671867342266933454, 0.8697921086061042306, 0.8723954461898817403, 0.8749998551902504751, 0.8776042660585271493, 0.8802076021295854868, 0.8828129777054576355, 0.8854158305722678035, 0.8880214025647872322, 0.8906244194604823194, 0.8932294044984951942, 0.8958332126919159588, 0.8984370186969063976, 0.9010420054557602976, 0.9036450214505988843, 0.9062505943687239052, 0.9088534485426573717, 0.9114588242474312985, 0.9140621635225948394, 0.9166665737391771485, 0.9192709863124074454, 0.9218743236289563825, 0.9244797007862803895, 0.9270825551036790957, 0.9296881285585824051, 0.9322911471418501295, 0.9348961335295734587, 0.9374999435335269471, 0.9401037508197458425, 0.9427087393012421046, 0.9453117567106092967, 0.9479173312323898593, 0.9505201870615167525, 0.9531255642405720430, 0.9557289053967781278, 0.9583333169903581750, 0.9609377312744702415, 0.9635410702737328137, 0.9661464495301401723, 0.9687493035862174695, 0.9713548794777306927, 0.9739579066090123804, 0.9765628826531806972, 0.9791666865793459129, 0.9817705523293528413, 0.9843754818126480011, 0.9869784094881522973, 0.9895843956701340094, 0.9921866610829068733, 0.9947911313000845634, 0.9973997837621362272, 1.000000000000000000 ),
 .UNSPECIFIED. ) 
 GEOMETRIC_REPRESENTATION_ITEM ( )  RATIONAL_B_SPLINE_SURFACE ( (
 ( 1.000000000000000222, 1.000000000000000222, 1.000000000000000000, 1.000000000000000222, 1.000000000000000000, 0.9999999999999997780, 1.000000000000000222, 1.000000000000000000, 1.000000000000000222, 1.000000000000000222, 1.000000000000000000, 0.9999999999999997780, 1.000000000000000000, 1.000000000000000222, 0.9999999999999997780, 1.000000000000000222, 0.9999999999999994449, 1.000000000000000444, 0.9999999999999996669, 1.000000000000000000, 1.000000000000000222, 1.000000000000000000, 1.000000000000000000, 0.9999999999999997780, 1.000000000000000444, 0.9999999999999996669, 1.000000000000000000, 1.000000000000000222, 0.9999999999999997780, 1.000000000000000000, 0.9999999999999997780, 0.9999999999999997780, 1.000000000000000444, 0.9999999999999994449, 1.000000000000000444, 0.9999999999999997780, 0.9999999999999997780, 0.9999999999999996669, 1.000000000000000222, 1.000000000000000000, 0.9999999999999997780, 1.000000000000000222, 0.9999999999999997780, 1.000000000000000222, 1.000000000000000000, 1.000000000000000222, 1.000000000000000000, 1.000000000000000000, 1.000000000000000444, 0.9999999999999996669, 0.9999999999999997780, 1.000000000000000000, 0.9999999999999997780, 0.9999999999999997780, 1.000000000000000000, 1.000000000000000000, 0.9999999999999997780, 1.000000000000000444, 1.000000000000000000, 0.9999999999999997780, 1.000000000000000222, 0.9999999999999996669, 1.000000000000000222, 1.000000000000000000, 0.9999999999999997780, 1.000000000000000222, 0.9999999999999997780, 1.000000000000000000, 0.9999999999999997780, 1.000000000000000222, 0.9999999999999996669, 1.000000000000000000, 1.000000000000000222, 0.9999999999999997780, 1.000000000000000222, 0.9999999999999996669, 1.000000000000000444, 1.000000000000000000, 1.000000000000000000, 1.000000000000000222, 1.000000000000000222, 1.000000000000000000, 0.9999999999999997780, 1.000000000000000222, 0.9999999999999997780, 1.000000000000000000, 1.000000000000000000, 1.000000000000000000, 0.9999999999999997780, 1.000000000000000000, 0.9999999999999997780, 1.000000000000000222, 0.9999999999999997780, 1.000000000000000000, 1.000000000000000222, 0.9999999999999997780, 1.000000000000000000, 0.9999999999999996669, 1.000000000000000444, 0.9999999999999997780, 1.000000000000000000, 1.000000000000000000, 1.000000000000000000, 0.9999999999999997780, 0.9999999999999997780, 1.000000000000000222, 1.000000000000000222, 0.9999999999999997780, 1.000000000000000000, 1.000000000000000000, 1.000000000000000222, 1.000000000000000222, 1.000000000000000000, 0.9999999999999997780, 1.000000000000000222, 1.000000000000000000, 1.000000000000000000, 0.9999999999999997780, 0.9999999999999997780, 1.000000000000000222, 1.000000000000000000, 1.000000000000000000, 1.000000000000000000, 0.9999999999999997780, 1.000000000000000222, 1.000000000000000000, 1.000000000000000000, 1.000000000000000000, 1.000000000000000444, 0.9999999999999997780, 0.9999999999999997780, 1.000000000000000000, 1.000000000000000000, 0.9999999999999997780, 1.000000000000000222, 0.9999999999999997780, 1.000000000000000222, 1.000000000000000000, 1.000000000000000222, 1.000000000000000222, 1.000000000000000000, 1.000000000000000222, 1.000000000000000000, 0.9999999999999996669, 1.000000000000000222, 0.9999999999999997780, 1.000000000000000444, 0.9999999999999997780, 1.000000000000000000, 0.9999999999999997780, 1.000000000000000222, 1.000000000000000000, 0.9999999999999997780, 1.000000000000000222, 0.9999999999999994449, 1.000000000000000000, 1.000000000000000222, 1.000000000000000222, 0.9999999999999997780, 1.000000000000000444, 0.9999999999999997780, 1.000000000000000222, 0.9999999999999997780, 1.000000000000000222, 0.9999999999999997780, 1.000000000000000000, 1.000000000000000000, 1.000000000000000222, 0.9999999999999997780, 0.9999999999999996669, 1.000000000000000444, 0.9999999999999997780, 1.000000000000000222, 1.000000000000000000, 1.000000000000000222, 0.9999999999999994449, 1.000000000000000444, 0.9999999999999997780, 1.000000000000000000, 1.000000000000000222, 1.000000000000000000, 1.000000000000000000, 0.9999999999999997780, 1.000000000000000444, 0.9999999999999997780, 1.000000000000000444, 0.9999999999999997780, 1.000000000000000000, 1.000000000000000222, 0.9999999999999996669, 1.000000000000000222, 1.000000000000000000, 1.000000000000000000, 0.9999999999999996669, 1.000000000000000222, 1.000000000000000444, 0.9999999999999997780, 1.000000000000000222, 0.9999999999999996669, 1.000000000000000444, 0.9999999999999997780, 1.000000000000000444, 0.9999999999999996669, 0.9999999999999997780, 1.000000000000000000, 0.9999999999999997780, 1.000000000000000000, 1.000000000000000000, 1.000000000000000000, 1.000000000000000000, 0.9999999999999997780, 1.000000000000000000, 0.9999999999999997780, 1.000000000000000000, 1.000000000000000000, 1.000000000000000000, 1.000000000000000000, 0.9999999999999997780, 1.000000000000000222, 0.9999999999999997780, 1.000000000000000222, 0.9999999999999997780, 1.000000000000000222, 0.9999999999999994449, 1.000000000000000444, 1.000000000000000000, 1.000000000000000222, 0.9999999999999997780, 1.000000000000000000, 0.9999999999999997780, 1.000000000000000222, 1.000000000000000000, 1.000000000000000000, 1.000000000000000222, 1.000000000000000222, 0.9999999999999996669, 1.000000000000000444, 0.9999999999999996669, 1.000000000000000444, 0.9999999999999996669, 1.000000000000000000, 1.000000000000000000, 1.000000000000000000, 0.9999999999999997780, 1.000000000000000222, 0.9999999999999997780, 1.000000000000000222, 1.000000000000000000, 0.9999999999999997780, 1.000000000000000000, 1.000000000000000222, 1.000000000000000222, 1.000000000000000000, 1.000000000000000000, 1.000000000000000000, 1.000000000000000000, 0.9999999999999997780, 1.000000000000000444, 1.000000000000000000, 0.9999999999999997780, 1.000000000000000222, 0.9999999999999996669, 1.000000000000000444, 1.000000000000000000, 1.000000000000000222, 1.000000000000000222, 0.9999999999999997780, 1.000000000000000222, 0.9999999999999997780, 1.000000000000000000, 1.000000000000000000, 0.9999999999999997780, 1.000000000000000000, 1.000000000000000000, 0.9999999999999997780, 1.000000000000000222, 1.000000000000000000, 1.000000000000000000, 1.000000000000000222, 1.000000000000000000, 1.000000000000000000, 1.000000000000000000, 1.000000000000000222, 0.9999999999999997780, 1.000000000000000222, 1.000000000000000000, 0.9999999999999997780, 1.000000000000000222, 0.9999999999999997780, 1.000000000000000222, 1.000000000000000222, 1.000000000000000000, 0.9999999999999997780, 1.000000000000000000, 1.000000000000000222, 1.000000000000000000, 1.000000000000000000, 0.9999999999999996669, 1.000000000000000444, 0.9999999999999994449, 1.000000000000000444, 0.9999999999999997780, 1.000000000000000000, 1.000000000000000000, 0.9999999999999997780, 1.000000000000000222, 0.9999999999999997780, 1.000000000000000000, 1.000000000000000444, 0.9999999999999997780, 1.000000000000000000, 0.9999999999999997780, 1.000000000000000000, 1.000000000000000000, 0.9999999999999997780, 0.9999999999999997780, 1.000000000000000000, 1.000000000000000444, 1.000000000000000000, 1.000000000000000444, 1.000000000000000000, 1.000000000000000000, 1.000000000000000000, 0.9999999999999997780, 1.000000000000000000, 1.000000000000000000, 1.000000000000000000, 1.000000000000000000, 0.9999999999999997780, 1.000000000000000222, 1.000000000000000000, 0.9999999999999997780, 1.000000000000000444, 0.9999999999999997780, 1.000000000000000222, 0.9999999999999996669, 1.000000000000000444, 1.000000000000000000, 0.9999999999999997780, 1.000000000000000000, 1.000000000000000000, 1.000000000000000000, 0.9999999999999997780, 1.000000000000000000, 1.000000000000000000, 0.9999999999999997780, 1.000000000000000444, 0.9999999999999997780, 0.9999999999999997780, 1.000000000000000000, 1.000000000000000000, 1.000000000000000222, 1.000000000000000222, 0.9999999999999997780, 1.000000000000000000, 1.000000000000000222, 1.000000000000000000, 0.9999999999999997780, 1.000000000000000222, 1.000000000000000000, 1.000000000000000000, 1.000000000000000000, 0.9999999999999997780, 1.000000000000000000, 1.000000000000000000, 1.000000000000000000, 1.000000000000000000, 0.9999999999999997780, 1.000000000000000666, 0.9999999999999996669, 0.9999999999999996669, 1.000000000000000444, 0.9999999999999996669, 1.000000000000000222, 1.000000000000000000, 1.000000000000000000, 1.000000000000000000, 1.000000000000000000, 1.000000000000000000, 0.9999999999999997780, 1.000000000000000222, 1.000000000000000222, 0.9999999999999996669, 0.9999999999999997780, 1.000000000000000000, 1.000000000000000222, 1.000000000000000222),
 ( 0.3333333333333334259, 0.3333333333333334259, 0.3333333333333333703, 0.3333333333333334259, 0.3333333333333333703, 0.3333333333333332593, 0.3333333333333334814, 0.3333333333333333703, 0.3333333333333334814, 0.3333333333333334259, 0.3333333333333333148, 0.3333333333333333148, 0.3333333333333333703, 0.3333333333333334259, 0.3333333333333332593, 0.3333333333333334814, 0.3333333333333331483, 0.3333333333333334814, 0.3333333333333333148, 0.3333333333333333148, 0.3333333333333334259, 0.3333333333333333703, 0.3333333333333333703, 0.3333333333333333148, 0.3333333333333335369, 0.3333333333333332593, 0.3333333333333333703, 0.3333333333333333703, 0.3333333333333334259, 0.3333333333333333148, 0.3333333333333333148, 0.3333333333333333148, 0.3333333333333334259, 0.3333333333333332593, 0.3333333333333334259, 0.3333333333333334259, 0.3333333333333333148, 0.3333333333333332593, 0.3333333333333333703, 0.3333333333333333703, 0.3333333333333332593, 0.3333333333333334814, 0.3333333333333333703, 0.3333333333333333703, 0.3333333333333333148, 0.3333333333333334259, 0.3333333333333333703, 0.3333333333333333703, 0.3333333333333334814, 0.3333333333333332038, 0.3333333333333334259, 0.3333333333333333703, 0.3333333333333333148, 0.3333333333333333148, 0.3333333333333333703, 0.3333333333333333703, 0.3333333333333333148, 0.3333333333333334814, 0.3333333333333333148, 0.3333333333333333703, 0.3333333333333333148, 0.3333333333333333148, 0.3333333333333334259, 0.3333333333333333703, 0.3333333333333333703, 0.3333333333333334259, 0.3333333333333333148, 0.3333333333333333148, 0.3333333333333333703, 0.3333333333333333703, 0.3333333333333332593, 0.3333333333333333703, 0.3333333333333333703, 0.3333333333333333703, 0.3333333333333333148, 0.3333333333333333148, 0.3333333333333334814, 0.3333333333333333703, 0.3333333333333334259, 0.3333333333333334259, 0.3333333333333334814, 0.3333333333333333148, 0.3333333333333333703, 0.3333333333333334259, 0.3333333333333333148, 0.3333333333333333703, 0.3333333333333333703, 0.3333333333333333703, 0.3333333333333333703, 0.3333333333333333703, 0.3333333333333333148, 0.3333333333333334814, 0.3333333333333332593, 0.3333333333333334259, 0.3333333333333333703, 0.3333333333333333703, 0.3333333333333333148, 0.3333333333333333703, 0.3333333333333334259, 0.3333333333333332593, 0.3333333333333334259, 0.3333333333333333703, 0.3333333333333333148, 0.3333333333333333148, 0.3333333333333332593, 0.3333333333333334259, 0.3333333333333333703, 0.3333333333333333703, 0.3333333333333333148, 0.3333333333333334259, 0.3333333333333333148, 0.3333333333333335369, 0.3333333333333333148, 0.3333333333333333703, 0.3333333333333333703, 0.3333333333333333703, 0.3333333333333334259, 0.3333333333333332593, 0.3333333333333333703, 0.3333333333333333703, 0.3333333333333333703, 0.3333333333333333703, 0.3333333333333333148, 0.3333333333333333703, 0.3333333333333333703, 0.3333333333333334259, 0.3333333333333333703, 0.3333333333333333703, 0.3333333333333335369, 0.3333333333333333148, 0.3333333333333333148, 0.3333333333333333703, 0.3333333333333333703, 0.3333333333333333148, 0.3333333333333334259, 0.3333333333333333148, 0.3333333333333333703, 0.3333333333333333148, 0.3333333333333334814, 0.3333333333333334259, 0.3333333333333333703, 0.3333333333333334259, 0.3333333333333334259, 0.3333333333333332593, 0.3333333333333333703, 0.3333333333333334259, 0.3333333333333334259, 0.3333333333333333148, 0.3333333333333334259, 0.3333333333333333148, 0.3333333333333334259, 0.3333333333333333703, 0.3333333333333333148, 0.3333333333333334814, 0.3333333333333332038, 0.3333333333333333703, 0.3333333333333334259, 0.3333333333333333703, 0.3333333333333333703, 0.3333333333333334814, 0.3333333333333332593, 0.3333333333333334814, 0.3333333333333332593, 0.3333333333333334259, 0.3333333333333334259, 0.3333333333333332593, 0.3333333333333334259, 0.3333333333333334259, 0.3333333333333333148, 0.3333333333333332593, 0.3333333333333334259, 0.3333333333333333148, 0.3333333333333334259, 0.3333333333333333703, 0.3333333333333334259, 0.3333333333333332038, 0.3333333333333334814, 0.3333333333333333148, 0.3333333333333333703, 0.3333333333333334259, 0.3333333333333333703, 0.3333333333333333703, 0.3333333333333334259, 0.3333333333333334259, 0.3333333333333333148, 0.3333333333333334259, 0.3333333333333333148, 0.3333333333333333703, 0.3333333333333333703, 0.3333333333333333148, 0.3333333333333335369, 0.3333333333333333148, 0.3333333333333334259, 0.3333333333333333148, 0.3333333333333334259, 0.3333333333333335369, 0.3333333333333332593, 0.3333333333333333703, 0.3333333333333333148, 0.3333333333333334259, 0.3333333333333333148, 0.3333333333333334814, 0.3333333333333332593, 0.3333333333333333703, 0.3333333333333333148, 0.3333333333333334259, 0.3333333333333333703, 0.3333333333333333148, 0.3333333333333333703, 0.3333333333333334814, 0.3333333333333333148, 0.3333333333333333703, 0.3333333333333333148, 0.3333333333333333703, 0.3333333333333333148, 0.3333333333333333703, 0.3333333333333333148, 0.3333333333333332593, 0.3333333333333334814, 0.3333333333333332593, 0.3333333333333335369, 0.3333333333333333703, 0.3333333333333333703, 0.3333333333333332038, 0.3333333333333335369, 0.3333333333333333703, 0.3333333333333334259, 0.3333333333333333148, 0.3333333333333334259, 0.3333333333333333148, 0.3333333333333334259, 0.3333333333333333703, 0.3333333333333333703, 0.3333333333333333703, 0.3333333333333334814, 0.3333333333333332038, 0.3333333333333334814, 0.3333333333333333148, 0.3333333333333334259, 0.3333333333333333148, 0.3333333333333333703, 0.3333333333333333703, 0.3333333333333333703, 0.3333333333333332593, 0.3333333333333334814, 0.3333333333333333148, 0.3333333333333333703, 0.3333333333333334259, 0.3333333333333333148, 0.3333333333333334259, 0.3333333333333333703, 0.3333333333333334814, 0.3333333333333333148, 0.3333333333333333703, 0.3333333333333334259, 0.3333333333333333703, 0.3333333333333333148, 0.3333333333333334814, 0.3333333333333333703, 0.3333333333333332593, 0.3333333333333335369, 0.3333333333333332038, 0.3333333333333335369, 0.3333333333333333148, 0.3333333333333334259, 0.3333333333333333703, 0.3333333333333333703, 0.3333333333333334259, 0.3333333333333333703, 0.3333333333333333703, 0.3333333333333333703, 0.3333333333333332593, 0.3333333333333334259, 0.3333333333333334259, 0.3333333333333333148, 0.3333333333333333703, 0.3333333333333333148, 0.3333333333333334259, 0.3333333333333334259, 0.3333333333333333148, 0.3333333333333333703, 0.3333333333333333703, 0.3333333333333333703, 0.3333333333333333703, 0.3333333333333334259, 0.3333333333333334259, 0.3333333333333333703, 0.3333333333333334259, 0.3333333333333333148, 0.3333333333333334814, 0.3333333333333334259, 0.3333333333333333148, 0.3333333333333333703, 0.3333333333333333703, 0.3333333333333334259, 0.3333333333333333703, 0.3333333333333333703, 0.3333333333333333148, 0.3333333333333335924, 0.3333333333333332038, 0.3333333333333335924, 0.3333333333333333148, 0.3333333333333333703, 0.3333333333333333148, 0.3333333333333333148, 0.3333333333333334814, 0.3333333333333332038, 0.3333333333333334814, 0.3333333333333334259, 0.3333333333333333703, 0.3333333333333334259, 0.3333333333333333148, 0.3333333333333333703, 0.3333333333333334259, 0.3333333333333333148, 0.3333333333333333148, 0.3333333333333334259, 0.3333333333333334259, 0.3333333333333333148, 0.3333333333333334814, 0.3333333333333333703, 0.3333333333333334259, 0.3333333333333333703, 0.3333333333333333148, 0.3333333333333333703, 0.3333333333333333703, 0.3333333333333333703, 0.3333333333333333703, 0.3333333333333333703, 0.3333333333333334814, 0.3333333333333333148, 0.3333333333333334259, 0.3333333333333334259, 0.3333333333333333148, 0.3333333333333334259, 0.3333333333333332038, 0.3333333333333335369, 0.3333333333333332593, 0.3333333333333333703, 0.3333333333333333703, 0.3333333333333333148, 0.3333333333333334259, 0.3333333333333333148, 0.3333333333333334259, 0.3333333333333333148, 0.3333333333333333703, 0.3333333333333334259, 0.3333333333333333703, 0.3333333333333333148, 0.3333333333333333703, 0.3333333333333333148, 0.3333333333333334259, 0.3333333333333334259, 0.3333333333333333148, 0.3333333333333333148, 0.3333333333333333703, 0.3333333333333333703, 0.3333333333333333703, 0.3333333333333333703, 0.3333333333333334259, 0.3333333333333333148, 0.3333333333333334814, 0.3333333333333332593, 0.3333333333333334259, 0.3333333333333333703, 0.3333333333333333703, 0.3333333333333333703, 0.3333333333333333148, 0.3333333333333335369, 0.3333333333333333703, 0.3333333333333332593, 0.3333333333333334814, 0.3333333333333333703, 0.3333333333333333703, 0.3333333333333333703, 0.3333333333333333703, 0.3333333333333333703, 0.3333333333333333703, 0.3333333333333333703, 0.3333333333333333703, 0.3333333333333333703, 0.3333333333333334259, 0.3333333333333332593, 0.3333333333333333148, 0.3333333333333334259, 0.3333333333333334259, 0.3333333333333334259),
 ( 0.3333333333333334259, 0.3333333333333334259, 0.3333333333333333703, 0.3333333333333334259, 0.3333333333333333703, 0.3333333333333332593, 0.3333333333333334814, 0.3333333333333333703, 0.3333333333333334814, 0.3333333333333334259, 0.3333333333333333148, 0.3333333333333333148, 0.3333333333333333703, 0.3333333333333334259, 0.3333333333333332593, 0.3333333333333334814, 0.3333333333333331483, 0.3333333333333334814, 0.3333333333333333148, 0.3333333333333333148, 0.3333333333333334259, 0.3333333333333333703, 0.3333333333333333703, 0.3333333333333333148, 0.3333333333333335369, 0.3333333333333332593, 0.3333333333333333703, 0.3333333333333333703, 0.3333333333333334259, 0.3333333333333333148, 0.3333333333333333148, 0.3333333333333333148, 0.3333333333333334259, 0.3333333333333332593, 0.3333333333333334259, 0.3333333333333334259, 0.3333333333333333148, 0.3333333333333332593, 0.3333333333333333703, 0.3333333333333333703, 0.3333333333333332593, 0.3333333333333334814, 0.3333333333333333703, 0.3333333333333333703, 0.3333333333333333148, 0.3333333333333334259, 0.3333333333333333703, 0.3333333333333333703, 0.3333333333333334814, 0.3333333333333332038, 0.3333333333333334259, 0.3333333333333333703, 0.3333333333333333148, 0.3333333333333333148, 0.3333333333333333703, 0.3333333333333333703, 0.3333333333333333148, 0.3333333333333334814, 0.3333333333333333148, 0.3333333333333333703, 0.3333333333333333148, 0.3333333333333333148, 0.3333333333333334259, 0.3333333333333333703, 0.3333333333333333703, 0.3333333333333334259, 0.3333333333333333148, 0.3333333333333333148, 0.3333333333333333703, 0.3333333333333333703, 0.3333333333333332593, 0.3333333333333333703, 0.3333333333333333703, 0.3333333333333333703, 0.3333333333333333148, 0.3333333333333333148, 0.3333333333333334814, 0.3333333333333333703, 0.3333333333333334259, 0.3333333333333334259, 0.3333333333333334814, 0.3333333333333333148, 0.3333333333333333703, 0.3333333333333334259, 0.3333333333333333148, 0.3333333333333333703, 0.3333333333333333703, 0.3333333333333333703, 0.3333333333333333703, 0.3333333333333333703, 0.3333333333333333148, 0.3333333333333334814, 0.3333333333333332593, 0.3333333333333334259, 0.3333333333333333703, 0.3333333333333333703, 0.3333333333333333148, 0.3333333333333333703, 0.3333333333333334259, 0.3333333333333332593, 0.3333333333333334259, 0.3333333333333333703, 0.3333333333333333148, 0.3333333333333333148, 0.3333333333333332593, 0.3333333333333334259, 0.3333333333333333703, 0.3333333333333333703, 0.3333333333333333148, 0.3333333333333334259, 0.3333333333333333148, 0.3333333333333335369, 0.3333333333333333148, 0.3333333333333333703, 0.3333333333333333703, 0.3333333333333333703, 0.3333333333333334259, 0.3333333333333332593, 0.3333333333333333703, 0.3333333333333333703, 0.3333333333333333703, 0.3333333333333333703, 0.3333333333333333148, 0.3333333333333333703, 0.3333333333333333703, 0.3333333333333334259, 0.3333333333333333703, 0.3333333333333333703, 0.3333333333333335369, 0.3333333333333333148, 0.3333333333333333148, 0.3333333333333333703, 0.3333333333333333703, 0.3333333333333333148, 0.3333333333333334259, 0.3333333333333333148, 0.3333333333333333703, 0.3333333333333333148, 0.3333333333333334814, 0.3333333333333334259, 0.3333333333333333703, 0.3333333333333334259, 0.3333333333333334259, 0.3333333333333332593, 0.3333333333333333703, 0.3333333333333334259, 0.3333333333333334259, 0.3333333333333333148, 0.3333333333333334259, 0.3333333333333333148, 0.3333333333333334259, 0.3333333333333333703, 0.3333333333333333148, 0.3333333333333334814, 0.3333333333333332038, 0.3333333333333333703, 0.3333333333333334259, 0.3333333333333333703, 0.3333333333333333703, 0.3333333333333334814, 0.3333333333333332593, 0.3333333333333334814, 0.3333333333333332593, 0.3333333333333334259, 0.3333333333333334259, 0.3333333333333332593, 0.3333333333333334259, 0.3333333333333334259, 0.3333333333333333148, 0.3333333333333332593, 0.3333333333333334259, 0.3333333333333333148, 0.3333333333333334259, 0.3333333333333333703, 0.3333333333333334259, 0.3333333333333332038, 0.3333333333333334814, 0.3333333333333333148, 0.3333333333333333703, 0.3333333333333334259, 0.3333333333333333703, 0.3333333333333333703, 0.3333333333333334259, 0.3333333333333334259, 0.3333333333333333148, 0.3333333333333334259, 0.3333333333333333148, 0.3333333333333333703, 0.3333333333333333703, 0.3333333333333333148, 0.3333333333333335369, 0.3333333333333333148, 0.3333333333333334259, 0.3333333333333333148, 0.3333333333333334259, 0.3333333333333335369, 0.3333333333333332593, 0.3333333333333333703, 0.3333333333333333148, 0.3333333333333334259, 0.3333333333333333148, 0.3333333333333334814, 0.3333333333333332593, 0.3333333333333333703, 0.3333333333333333148, 0.3333333333333334259, 0.3333333333333333703, 0.3333333333333333148, 0.3333333333333333703, 0.3333333333333334814, 0.3333333333333333148, 0.3333333333333333703, 0.3333333333333333148, 0.3333333333333333703, 0.3333333333333333148, 0.3333333333333333703, 0.3333333333333333148, 0.3333333333333332593, 0.3333333333333334814, 0.3333333333333332593, 0.3333333333333335369, 0.3333333333333333703, 0.3333333333333333703, 0.3333333333333332038, 0.3333333333333335369, 0.3333333333333333703, 0.3333333333333334259, 0.3333333333333333148, 0.3333333333333334259, 0.3333333333333333148, 0.3333333333333334259, 0.3333333333333333703, 0.3333333333333333703, 0.3333333333333333703, 0.3333333333333334814, 0.3333333333333332038, 0.3333333333333334814, 0.3333333333333333148, 0.3333333333333334259, 0.3333333333333333148, 0.3333333333333333703, 0.3333333333333333703, 0.3333333333333333703, 0.3333333333333332593, 0.3333333333333334814, 0.3333333333333333148, 0.3333333333333333703, 0.3333333333333334259, 0.3333333333333333148, 0.3333333333333334259, 0.3333333333333333703, 0.3333333333333334814, 0.3333333333333333148, 0.3333333333333333703, 0.3333333333333334259, 0.3333333333333333703, 0.3333333333333333148, 0.3333333333333334814, 0.3333333333333333703, 0.3333333333333332593, 0.3333333333333335369, 0.3333333333333332038, 0.3333333333333335369, 0.3333333333333333148, 0.3333333333333334259, 0.3333333333333333703, 0.3333333333333333703, 0.3333333333333334259, 0.3333333333333333703, 0.3333333333333333703, 0.3333333333333333703, 0.3333333333333332593, 0.3333333333333334259, 0.3333333333333334259, 0.3333333333333333148, 0.3333333333333333703, 0.3333333333333333148, 0.3333333333333334259, 0.3333333333333334259, 0.3333333333333333148, 0.3333333333333333703, 0.3333333333333333703, 0.3333333333333333703, 0.3333333333333333703, 0.3333333333333334259, 0.3333333333333334259, 0.3333333333333333703, 0.3333333333333334259, 0.3333333333333333148, 0.3333333333333334814, 0.3333333333333334259, 0.3333333333333333148, 0.3333333333333333703, 0.3333333333333333703, 0.3333333333333334259, 0.3333333333333333703, 0.3333333333333333703, 0.3333333333333333148, 0.3333333333333335924, 0.3333333333333332038, 0.3333333333333335924, 0.3333333333333333148, 0.3333333333333333703, 0.3333333333333333148, 0.3333333333333333148, 0.3333333333333334814, 0.3333333333333332038, 0.3333333333333334814, 0.3333333333333334259, 0.3333333333333333703, 0.3333333333333334259, 0.3333333333333333148, 0.3333333333333333703, 0.3333333333333334259, 0.3333333333333333148, 0.3333333333333333148, 0.3333333333333334259, 0.3333333333333334259, 0.3333333333333333148, 0.3333333333333334814, 0.3333333333333333703, 0.3333333333333334259, 0.3333333333333333703, 0.3333333333333333148, 0.3333333333333333703, 0.3333333333333333703, 0.3333333333333333703, 0.3333333333333333703, 0.3333333333333333703, 0.3333333333333334814, 0.3333333333333333148, 0.3333333333333334259, 0.3333333333333334259, 0.3333333333333333148, 0.3333333333333334259, 0.3333333333333332038, 0.3333333333333335369, 0.3333333333333332593, 0.3333333333333333703, 0.3333333333333333703, 0.3333333333333333148, 0.3333333333333334259, 0.3333333333333333148, 0.3333333333333334259, 0.3333333333333333148, 0.3333333333333333703, 0.3333333333333334259, 0.3333333333333333703, 0.3333333333333333148, 0.3333333333333333703, 0.3333333333333333148, 0.3333333333333334259, 0.3333333333333334259, 0.3333333333333333148, 0.3333333333333333148, 0.3333333333333333703, 0.3333333333333333703, 0.3333333333333333703, 0.3333333333333333703, 0.3333333333333334259, 0.3333333333333333148, 0.3333333333333334814, 0.3333333333333332593, 0.3333333333333334259, 0.3333333333333333703, 0.3333333333333333703, 0.3333333333333333703, 0.3333333333333333148, 0.3333333333333335369, 0.3333333333333333703, 0.3333333333333332593, 0.3333333333333334814, 0.3333333333333333703, 0.3333333333333333703, 0.3333333333333333703, 0.3333333333333333703, 0.3333333333333333703, 0.3333333333333333703, 0.3333333333333333703, 0.3333333333333333703, 0.3333333333333333703, 0.3333333333333334259, 0.3333333333333332593, 0.3333333333333333148, 0.3333333333333334259, 0.3333333333333334259, 0.3333333333333334259),
 ( 1.000000000000000222, 1.000000000000000222, 1.000000000000000000, 1.000000000000000222, 1.000000000000000000, 0.9999999999999997780, 1.000000000000000222, 1.000000000000000000, 1.000000000000000222, 1.000000000000000222, 1.000000000000000000, 0.9999999999999997780, 1.000000000000000000, 1.000000000000000222, 0.9999999999999997780, 1.000000000000000222, 0.9999999999999994449, 1.000000000000000444, 0.9999999999999996669, 1.000000000000000000, 1.000000000000000222, 1.000000000000000000, 1.000000000000000000, 0.9999999999999997780, 1.000000000000000444, 0.9999999999999996669, 1.000000000000000000, 1.000000000000000222, 0.9999999999999997780, 1.000000000000000000, 0.9999999999999997780, 0.9999999999999997780, 1.000000000000000444, 0.9999999999999994449, 1.000000000000000444, 0.9999999999999997780, 0.9999999999999997780, 0.9999999999999996669, 1.000000000000000222, 1.000000000000000000, 0.9999999999999997780, 1.000000000000000222, 0.9999999999999997780, 1.000000000000000222, 1.000000000000000000, 1.000000000000000222, 1.000000000000000000, 1.000000000000000000, 1.000000000000000444, 0.9999999999999996669, 0.9999999999999997780, 1.000000000000000000, 0.9999999999999997780, 0.9999999999999997780, 1.000000000000000000, 1.000000000000000000, 0.9999999999999997780, 1.000000000000000444, 1.000000000000000000, 0.9999999999999997780, 1.000000000000000222, 0.9999999999999996669, 1.000000000000000222, 1.000000000000000000, 0.9999999999999997780, 1.000000000000000222, 0.9999999999999997780, 1.000000000000000000, 0.9999999999999997780, 1.000000000000000222, 0.9999999999999996669, 1.000000000000000000, 1.000000000000000222, 0.9999999999999997780, 1.000000000000000222, 0.9999999999999996669, 1.000000000000000444, 1.000000000000000000, 1.000000000000000000, 1.000000000000000222, 1.000000000000000222, 1.000000000000000000, 0.9999999999999997780, 1.000000000000000222, 0.9999999999999997780, 1.000000000000000000, 1.000000000000000000, 1.000000000000000000, 0.9999999999999997780, 1.000000000000000000, 0.9999999999999997780, 1.000000000000000222, 0.9999999999999997780, 1.000000000000000000, 1.000000000000000222, 0.9999999999999997780, 1.000000000000000000, 0.9999999999999996669, 1.000000000000000444, 0.9999999999999997780, 1.000000000000000000, 1.000000000000000000, 1.000000000000000000, 0.9999999999999997780, 0.9999999999999997780, 1.000000000000000222, 1.000000000000000222, 0.9999999999999997780, 1.000000000000000000, 1.000000000000000000, 1.000000000000000222, 1.000000000000000222, 1.000000000000000000, 0.9999999999999997780, 1.000000000000000222, 1.000000000000000000, 1.000000000000000000, 0.9999999999999997780, 0.9999999999999997780, 1.000000000000000222, 1.000000000000000000, 1.000000000000000000, 1.000000000000000000, 0.9999999999999997780, 1.000000000000000222, 1.000000000000000000, 1.000000000000000000, 1.000000000000000000, 1.000000000000000444, 0.9999999999999997780, 0.9999999999999997780, 1.000000000000000000, 1.000000000000000000, 0.9999999999999997780, 1.000000000000000222, 0.9999999999999997780, 1.000000000000000222, 1.000000000000000000, 1.000000000000000222, 1.000000000000000222, 1.000000000000000000, 1.000000000000000222, 1.000000000000000000, 0.9999999999999996669, 1.000000000000000222, 0.9999999999999997780, 1.000000000000000444, 0.9999999999999997780, 1.000000000000000000, 0.9999999999999997780, 1.000000000000000222, 1.000000000000000000, 0.9999999999999997780, 1.000000000000000222, 0.9999999999999994449, 1.000000000000000000, 1.000000000000000222, 1.000000000000000222, 0.9999999999999997780, 1.000000000000000444, 0.9999999999999997780, 1.000000000000000222, 0.9999999999999997780, 1.000000000000000222, 0.9999999999999997780, 1.000000000000000000, 1.000000000000000000, 1.000000000000000222, 0.9999999999999997780, 0.9999999999999996669, 1.000000000000000444, 0.9999999999999997780, 1.000000000000000222, 1.000000000000000000, 1.000000000000000222, 0.9999999999999994449, 1.000000000000000444, 0.9999999999999997780, 1.000000000000000000, 1.000000000000000222, 1.000000000000000000, 1.000000000000000000, 0.9999999999999997780, 1.000000000000000444, 0.9999999999999997780, 1.000000000000000444, 0.9999999999999997780, 1.000000000000000000, 1.000000000000000222, 0.9999999999999996669, 1.000000000000000222, 1.000000000000000000, 1.000000000000000000, 0.9999999999999996669, 1.000000000000000222, 1.000000000000000444, 0.9999999999999997780, 1.000000000000000222, 0.9999999999999996669, 1.000000000000000444, 0.9999999999999997780, 1.000000000000000444, 0.9999999999999996669, 0.9999999999999997780, 1.000000000000000000, 0.9999999999999997780, 1.000000000000000000, 1.000000000000000000, 1.000000000000000000, 1.000000000000000000, 0.9999999999999997780, 1.000000000000000000, 0.9999999999999997780, 1.000000000000000000, 1.000000000000000000, 1.000000000000000000, 1.000000000000000000, 0.9999999999999997780, 1.000000000000000222, 0.9999999999999997780, 1.000000000000000222, 0.9999999999999997780, 1.000000000000000222, 0.9999999999999994449, 1.000000000000000444, 1.000000000000000000, 1.000000000000000222, 0.9999999999999997780, 1.000000000000000000, 0.9999999999999997780, 1.000000000000000222, 1.000000000000000000, 1.000000000000000000, 1.000000000000000222, 1.000000000000000222, 0.9999999999999996669, 1.000000000000000444, 0.9999999999999996669, 1.000000000000000444, 0.9999999999999996669, 1.000000000000000000, 1.000000000000000000, 1.000000000000000000, 0.9999999999999997780, 1.000000000000000222, 0.9999999999999997780, 1.000000000000000222, 1.000000000000000000, 0.9999999999999997780, 1.000000000000000000, 1.000000000000000222, 1.000000000000000222, 1.000000000000000000, 1.000000000000000000, 1.000000000000000000, 1.000000000000000000, 0.9999999999999997780, 1.000000000000000444, 1.000000000000000000, 0.9999999999999997780, 1.000000000000000222, 0.9999999999999996669, 1.000000000000000444, 1.000000000000000000, 1.000000000000000222, 1.000000000000000222, 0.9999999999999997780, 1.000000000000000222, 0.9999999999999997780, 1.000000000000000000, 1.000000000000000000, 0.9999999999999997780, 1.000000000000000000, 1.000000000000000000, 0.9999999999999997780, 1.000000000000000222, 1.000000000000000000, 1.000000000000000000, 1.000000000000000222, 1.000000000000000000, 1.000000000000000000, 1.000000000000000000, 1.000000000000000222, 0.9999999999999997780, 1.000000000000000222, 1.000000000000000000, 0.9999999999999997780, 1.000000000000000222, 0.9999999999999997780, 1.000000000000000222, 1.000000000000000222, 1.000000000000000000, 0.9999999999999997780, 1.000000000000000000, 1.000000000000000222, 1.000000000000000000, 1.000000000000000000, 0.9999999999999996669, 1.000000000000000444, 0.9999999999999994449, 1.000000000000000444, 0.9999999999999997780, 1.000000000000000000, 1.000000000000000000, 0.9999999999999997780, 1.000000000000000222, 0.9999999999999997780, 1.000000000000000000, 1.000000000000000444, 0.9999999999999997780, 1.000000000000000000, 0.9999999999999997780, 1.000000000000000000, 1.000000000000000000, 0.9999999999999997780, 0.9999999999999997780, 1.000000000000000000, 1.000000000000000444, 1.000000000000000000, 1.000000000000000444, 1.000000000000000000, 1.000000000000000000, 1.000000000000000000, 0.9999999999999997780, 1.000000000000000000, 1.000000000000000000, 1.000000000000000000, 1.000000000000000000, 0.9999999999999997780, 1.000000000000000222, 1.000000000000000000, 0.9999999999999997780, 1.000000000000000444, 0.9999999999999997780, 1.000000000000000222, 0.9999999999999996669, 1.000000000000000444, 1.000000000000000000, 0.9999999999999997780, 1.000000000000000000, 1.000000000000000000, 1.000000000000000000, 0.9999999999999997780, 1.000000000000000000, 1.000000000000000000, 0.9999999999999997780, 1.000000000000000444, 0.9999999999999997780, 0.9999999999999997780, 1.000000000000000000, 1.000000000000000000, 1.000000000000000222, 1.000000000000000222, 0.9999999999999997780, 1.000000000000000000, 1.000000000000000222, 1.000000000000000000, 0.9999999999999997780, 1.000000000000000222, 1.000000000000000000, 1.000000000000000000, 1.000000000000000000, 0.9999999999999997780, 1.000000000000000000, 1.000000000000000000, 1.000000000000000000, 1.000000000000000000, 0.9999999999999997780, 1.000000000000000666, 0.9999999999999996669, 0.9999999999999996669, 1.000000000000000444, 0.9999999999999996669, 1.000000000000000222, 1.000000000000000000, 1.000000000000000000, 1.000000000000000000, 1.000000000000000000, 1.000000000000000000, 0.9999999999999997780, 1.000000000000000222, 1.000000000000000222, 0.9999999999999996669, 0.9999999999999997780, 1.000000000000000000, 1.000000000000000222, 1.000000000000000222),
 ( 0.3333333333333334259, 0.3333333333333334259, 0.3333333333333333703, 0.3333333333333334259, 0.3333333333333333703, 0.3333333333333332593, 0.3333333333333334814, 0.3333333333333333703, 0.3333333333333334814, 0.3333333333333334259, 0.3333333333333333148, 0.3333333333333333148, 0.3333333333333333703, 0.3333333333333334259, 0.3333333333333332593, 0.3333333333333334814, 0.3333333333333331483, 0.3333333333333334814, 0.3333333333333333148, 0.3333333333333333148, 0.3333333333333334259, 0.3333333333333333703, 0.3333333333333333703, 0.3333333333333333148, 0.3333333333333335369, 0.3333333333333332593, 0.3333333333333333703, 0.3333333333333333703, 0.3333333333333334259, 0.3333333333333333148, 0.3333333333333333148, 0.3333333333333333148, 0.3333333333333334259, 0.3333333333333332593, 0.3333333333333334259, 0.3333333333333334259, 0.3333333333333333148, 0.3333333333333332593, 0.3333333333333333703, 0.3333333333333333703, 0.3333333333333332593, 0.3333333333333334814, 0.3333333333333333703, 0.3333333333333333703, 0.3333333333333333148, 0.3333333333333334259, 0.3333333333333333703, 0.3333333333333333703, 0.3333333333333334814, 0.3333333333333332038, 0.3333333333333334259, 0.3333333333333333703, 0.3333333333333333148, 0.3333333333333333148, 0.3333333333333333703, 0.3333333333333333703, 0.3333333333333333148, 0.3333333333333334814, 0.3333333333333333148, 0.3333333333333333703, 0.3333333333333333148, 0.3333333333333333148, 0.3333333333333334259, 0.3333333333333333703, 0.3333333333333333703, 0.3333333333333334259, 0.3333333333333333148, 0.3333333333333333148, 0.3333333333333333703, 0.3333333333333333703, 0.3333333333333332593, 0.3333333333333333703, 0.3333333333333333703, 0.3333333333333333703, 0.3333333333333333148, 0.3333333333333333148, 0.3333333333333334814, 0.3333333333333333703, 0.3333333333333334259, 0.3333333333333334259, 0.3333333333333334814, 0.3333333333333333148, 0.3333333333333333703, 0.3333333333333334259, 0.3333333333333333148, 0.3333333333333333703, 0.3333333333333333703, 0.3333333333333333703, 0.3333333333333333703, 0.3333333333333333703, 0.3333333333333333148, 0.3333333333333334814, 0.3333333333333332593, 0.3333333333333334259, 0.3333333333333333703, 0.3333333333333333703, 0.3333333333333333148, 0.3333333333333333703, 0.3333333333333334259, 0.3333333333333332593, 0.3333333333333334259, 0.3333333333333333703, 0.3333333333333333148, 0.3333333333333333148, 0.3333333333333332593, 0.3333333333333334259, 0.3333333333333333703, 0.3333333333333333703, 0.3333333333333333148, 0.3333333333333334259, 0.3333333333333333148, 0.3333333333333335369, 0.3333333333333333148, 0.3333333333333333703, 0.3333333333333333703, 0.3333333333333333703, 0.3333333333333334259, 0.3333333333333332593, 0.3333333333333333703, 0.3333333333333333703, 0.3333333333333333703, 0.3333333333333333703, 0.3333333333333333148, 0.3333333333333333703, 0.3333333333333333703, 0.3333333333333334259, 0.3333333333333333703, 0.3333333333333333703, 0.3333333333333335369, 0.3333333333333333148, 0.3333333333333333148, 0.3333333333333333703, 0.3333333333333333703, 0.3333333333333333148, 0.3333333333333334259, 0.3333333333333333148, 0.3333333333333333703, 0.3333333333333333148, 0.3333333333333334814, 0.3333333333333334259, 0.3333333333333333703, 0.3333333333333334259, 0.3333333333333334259, 0.3333333333333332593, 0.3333333333333333703, 0.3333333333333334259, 0.3333333333333334259, 0.3333333333333333148, 0.3333333333333334259, 0.3333333333333333148, 0.3333333333333334259, 0.3333333333333333703, 0.3333333333333333148, 0.3333333333333334814, 0.3333333333333332038, 0.3333333333333333703, 0.3333333333333334259, 0.3333333333333333703, 0.3333333333333333703, 0.3333333333333334814, 0.3333333333333332593, 0.3333333333333334814, 0.3333333333333332593, 0.3333333333333334259, 0.3333333333333334259, 0.3333333333333332593, 0.3333333333333334259, 0.3333333333333334259, 0.3333333333333333148, 0.3333333333333332593, 0.3333333333333334259, 0.3333333333333333148, 0.3333333333333334259, 0.3333333333333333703, 0.3333333333333334259, 0.3333333333333332038, 0.3333333333333334814, 0.3333333333333333148, 0.3333333333333333703, 0.3333333333333334259, 0.3333333333333333703, 0.3333333333333333703, 0.3333333333333334259, 0.3333333333333334259, 0.3333333333333333148, 0.3333333333333334259, 0.3333333333333333148, 0.3333333333333333703, 0.3333333333333333703, 0.3333333333333333148, 0.3333333333333335369, 0.3333333333333333148, 0.3333333333333334259, 0.3333333333333333148, 0.3333333333333334259, 0.3333333333333335369, 0.3333333333333332593, 0.3333333333333333703, 0.3333333333333333148, 0.3333333333333334259, 0.3333333333333333148, 0.3333333333333334814, 0.3333333333333332593, 0.3333333333333333703, 0.3333333333333333148, 0.3333333333333334259, 0.3333333333333333703, 0.3333333333333333148, 0.3333333333333333703, 0.3333333333333334814, 0.3333333333333333148, 0.3333333333333333703, 0.3333333333333333148, 0.3333333333333333703, 0.3333333333333333148, 0.3333333333333333703, 0.3333333333333333148, 0.3333333333333332593, 0.3333333333333334814, 0.3333333333333332593, 0.3333333333333335369, 0.3333333333333333703, 0.3333333333333333703, 0.3333333333333332038, 0.3333333333333335369, 0.3333333333333333703, 0.3333333333333334259, 0.3333333333333333148, 0.3333333333333334259, 0.3333333333333333148, 0.3333333333333334259, 0.3333333333333333703, 0.3333333333333333703, 0.3333333333333333703, 0.3333333333333334814, 0.3333333333333332038, 0.3333333333333334814, 0.3333333333333333148, 0.3333333333333334259, 0.3333333333333333148, 0.3333333333333333703, 0.3333333333333333703, 0.3333333333333333703, 0.3333333333333332593, 0.3333333333333334814, 0.3333333333333333148, 0.3333333333333333703, 0.3333333333333334259, 0.3333333333333333148, 0.3333333333333334259, 0.3333333333333333703, 0.3333333333333334814, 0.3333333333333333148, 0.3333333333333333703, 0.3333333333333334259, 0.3333333333333333703, 0.3333333333333333148, 0.3333333333333334814, 0.3333333333333333703, 0.3333333333333332593, 0.3333333333333335369, 0.3333333333333332038, 0.3333333333333335369, 0.3333333333333333148, 0.3333333333333334259, 0.3333333333333333703, 0.3333333333333333703, 0.3333333333333334259, 0.3333333333333333703, 0.3333333333333333703, 0.3333333333333333703, 0.3333333333333332593, 0.3333333333333334259, 0.3333333333333334259, 0.3333333333333333148, 0.3333333333333333703, 0.3333333333333333148, 0.3333333333333334259, 0.3333333333333334259, 0.3333333333333333148, 0.3333333333333333703, 0.3333333333333333703, 0.3333333333333333703, 0.3333333333333333703, 0.3333333333333334259, 0.3333333333333334259, 0.3333333333333333703, 0.3333333333333334259, 0.3333333333333333148, 0.3333333333333334814, 0.3333333333333334259, 0.3333333333333333148, 0.3333333333333333703, 0.3333333333333333703, 0.3333333333333334259, 0.3333333333333333703, 0.3333333333333333703, 0.3333333333333333148, 0.3333333333333335924, 0.3333333333333332038, 0.3333333333333335924, 0.3333333333333333148, 0.3333333333333333703, 0.3333333333333333148, 0.3333333333333333148, 0.3333333333333334814, 0.3333333333333332038, 0.3333333333333334814, 0.3333333333333334259, 0.3333333333333333703, 0.3333333333333334259, 0.3333333333333333148, 0.3333333333333333703, 0.3333333333333334259, 0.3333333333333333148, 0.3333333333333333148, 0.3333333333333334259, 0.3333333333333334259, 0.3333333333333333148, 0.3333333333333334814, 0.3333333333333333703, 0.3333333333333334259, 0.3333333333333333703, 0.3333333333333333148, 0.3333333333333333703, 0.3333333333333333703, 0.3333333333333333703, 0.3333333333333333703, 0.3333333333333333703, 0.3333333333333334814, 0.3333333333333333148, 0.3333333333333334259, 0.3333333333333334259, 0.3333333333333333148, 0.3333333333333334259, 0.3333333333333332038, 0.3333333333333335369, 0.3333333333333332593, 0.3333333333333333703, 0.3333333333333333703, 0.3333333333333333148, 0.3333333333333334259, 0.3333333333333333148, 0.3333333333333334259, 0.3333333333333333148, 0.3333333333333333703, 0.3333333333333334259, 0.3333333333333333703, 0.3333333333333333148, 0.3333333333333333703, 0.3333333333333333148, 0.3333333333333334259, 0.3333333333333334259, 0.3333333333333333148, 0.3333333333333333148, 0.3333333333333333703, 0.3333333333333333703, 0.3333333333333333703, 0.3333333333333333703, 0.3333333333333334259, 0.3333333333333333148, 0.3333333333333334814, 0.3333333333333332593, 0.3333333333333334259, 0.3333333333333333703, 0.3333333333333333703, 0.3333333333333333703, 0.3333333333333333148, 0.3333333333333335369, 0.3333333333333333703, 0.3333333333333332593, 0.3333333333333334814, 0.3333333333333333703, 0.3333333333333333703, 0.3333333333333333703, 0.3333333333333333703, 0.3333333333333333703, 0.3333333333333333703, 0.3333333333333333703, 0.3333333333333333703, 0.3333333333333333703, 0.3333333333333334259, 0.3333333333333332593, 0.3333333333333333148, 0.3333333333333334259, 0.3333333333333334259, 0.3333333333333334259),
 ( 0.3333333333333334259, 0.3333333333333334259, 0.3333333333333333703, 0.3333333333333334259, 0.3333333333333333703, 0.3333333333333332593, 0.3333333333333334814, 0.3333333333333333703, 0.3333333333333334814, 0.3333333333333334259, 0.3333333333333333148, 0.3333333333333333148, 0.3333333333333333703, 0.3333333333333334259, 0.3333333333333332593, 0.3333333333333334814, 0.3333333333333331483, 0.3333333333333334814, 0.3333333333333333148, 0.3333333333333333148, 0.3333333333333334259, 0.3333333333333333703, 0.3333333333333333703, 0.3333333333333333148, 0.3333333333333335369, 0.3333333333333332593, 0.3333333333333333703, 0.3333333333333333703, 0.3333333333333334259, 0.3333333333333333148, 0.3333333333333333148, 0.3333333333333333148, 0.3333333333333334259, 0.3333333333333332593, 0.3333333333333334259, 0.3333333333333334259, 0.3333333333333333148, 0.3333333333333332593, 0.3333333333333333703, 0.3333333333333333703, 0.3333333333333332593, 0.3333333333333334814, 0.3333333333333333703, 0.3333333333333333703, 0.3333333333333333148, 0.3333333333333334259, 0.3333333333333333703, 0.3333333333333333703, 0.3333333333333334814, 0.3333333333333332038, 0.3333333333333334259, 0.3333333333333333703, 0.3333333333333333148, 0.3333333333333333148, 0.3333333333333333703, 0.3333333333333333703, 0.3333333333333333148, 0.3333333333333334814, 0.3333333333333333148, 0.3333333333333333703, 0.3333333333333333148, 0.3333333333333333148, 0.3333333333333334259, 0.3333333333333333703, 0.3333333333333333703, 0.3333333333333334259, 0.3333333333333333148, 0.3333333333333333148, 0.3333333333333333703, 0.3333333333333333703, 0.3333333333333332593, 0.3333333333333333703, 0.3333333333333333703, 0.3333333333333333703, 0.3333333333333333148, 0.3333333333333333148, 0.3333333333333334814, 0.3333333333333333703, 0.3333333333333334259, 0.3333333333333334259, 0.3333333333333334814, 0.3333333333333333148, 0.3333333333333333703, 0.3333333333333334259, 0.3333333333333333148, 0.3333333333333333703, 0.3333333333333333703, 0.3333333333333333703, 0.3333333333333333703, 0.3333333333333333703, 0.3333333333333333148, 0.3333333333333334814, 0.3333333333333332593, 0.3333333333333334259, 0.3333333333333333703, 0.3333333333333333703, 0.3333333333333333148, 0.3333333333333333703, 0.3333333333333334259, 0.3333333333333332593, 0.3333333333333334259, 0.3333333333333333703, 0.3333333333333333148, 0.3333333333333333148, 0.3333333333333332593, 0.3333333333333334259, 0.3333333333333333703, 0.3333333333333333703, 0.3333333333333333148, 0.3333333333333334259, 0.3333333333333333148, 0.3333333333333335369, 0.3333333333333333148, 0.3333333333333333703, 0.3333333333333333703, 0.3333333333333333703, 0.3333333333333334259, 0.3333333333333332593, 0.3333333333333333703, 0.3333333333333333703, 0.3333333333333333703, 0.3333333333333333703, 0.3333333333333333148, 0.3333333333333333703, 0.3333333333333333703, 0.3333333333333334259, 0.3333333333333333703, 0.3333333333333333703, 0.3333333333333335369, 0.3333333333333333148, 0.3333333333333333148, 0.3333333333333333703, 0.3333333333333333703, 0.3333333333333333148, 0.3333333333333334259, 0.3333333333333333148, 0.3333333333333333703, 0.3333333333333333148, 0.3333333333333334814, 0.3333333333333334259, 0.3333333333333333703, 0.3333333333333334259, 0.3333333333333334259, 0.3333333333333332593, 0.3333333333333333703, 0.3333333333333334259, 0.3333333333333334259, 0.3333333333333333148, 0.3333333333333334259, 0.3333333333333333148, 0.3333333333333334259, 0.3333333333333333703, 0.3333333333333333148, 0.3333333333333334814, 0.3333333333333332038, 0.3333333333333333703, 0.3333333333333334259, 0.3333333333333333703, 0.3333333333333333703, 0.3333333333333334814, 0.3333333333333332593, 0.3333333333333334814, 0.3333333333333332593, 0.3333333333333334259, 0.3333333333333334259, 0.3333333333333332593, 0.3333333333333334259, 0.3333333333333334259, 0.3333333333333333148, 0.3333333333333332593, 0.3333333333333334259, 0.3333333333333333148, 0.3333333333333334259, 0.3333333333333333703, 0.3333333333333334259, 0.3333333333333332038, 0.3333333333333334814, 0.3333333333333333148, 0.3333333333333333703, 0.3333333333333334259, 0.3333333333333333703, 0.3333333333333333703, 0.3333333333333334259, 0.3333333333333334259, 0.3333333333333333148, 0.3333333333333334259, 0.3333333333333333148, 0.3333333333333333703, 0.3333333333333333703, 0.3333333333333333148, 0.3333333333333335369, 0.3333333333333333148, 0.3333333333333334259, 0.3333333333333333148, 0.3333333333333334259, 0.3333333333333335369, 0.3333333333333332593, 0.3333333333333333703, 0.3333333333333333148, 0.3333333333333334259, 0.3333333333333333148, 0.3333333333333334814, 0.3333333333333332593, 0.3333333333333333703, 0.3333333333333333148, 0.3333333333333334259, 0.3333333333333333703, 0.3333333333333333148, 0.3333333333333333703, 0.3333333333333334814, 0.3333333333333333148, 0.3333333333333333703, 0.3333333333333333148, 0.3333333333333333703, 0.3333333333333333148, 0.3333333333333333703, 0.3333333333333333148, 0.3333333333333332593, 0.3333333333333334814, 0.3333333333333332593, 0.3333333333333335369, 0.3333333333333333703, 0.3333333333333333703, 0.3333333333333332038, 0.3333333333333335369, 0.3333333333333333703, 0.3333333333333334259, 0.3333333333333333148, 0.3333333333333334259, 0.3333333333333333148, 0.3333333333333334259, 0.3333333333333333703, 0.3333333333333333703, 0.3333333333333333703, 0.3333333333333334814, 0.3333333333333332038, 0.3333333333333334814, 0.3333333333333333148, 0.3333333333333334259, 0.3333333333333333148, 0.3333333333333333703, 0.3333333333333333703, 0.3333333333333333703, 0.3333333333333332593, 0.3333333333333334814, 0.3333333333333333148, 0.3333333333333333703, 0.3333333333333334259, 0.3333333333333333148, 0.3333333333333334259, 0.3333333333333333703, 0.3333333333333334814, 0.3333333333333333148, 0.3333333333333333703, 0.3333333333333334259, 0.3333333333333333703, 0.3333333333333333148, 0.3333333333333334814, 0.3333333333333333703, 0.3333333333333332593, 0.3333333333333335369, 0.3333333333333332038, 0.3333333333333335369, 0.3333333333333333148, 0.3333333333333334259, 0.3333333333333333703, 0.3333333333333333703, 0.3333333333333334259, 0.3333333333333333703, 0.3333333333333333703, 0.3333333333333333703, 0.3333333333333332593, 0.3333333333333334259, 0.3333333333333334259, 0.3333333333333333148, 0.3333333333333333703, 0.3333333333333333148, 0.3333333333333334259, 0.3333333333333334259, 0.3333333333333333148, 0.3333333333333333703, 0.3333333333333333703, 0.3333333333333333703, 0.3333333333333333703, 0.3333333333333334259, 0.3333333333333334259, 0.3333333333333333703, 0.3333333333333334259, 0.3333333333333333148, 0.3333333333333334814, 0.3333333333333334259, 0.3333333333333333148, 0.3333333333333333703, 0.3333333333333333703, 0.3333333333333334259, 0.3333333333333333703, 0.3333333333333333703, 0.3333333333333333148, 0.3333333333333335924, 0.3333333333333332038, 0.3333333333333335924, 0.3333333333333333148, 0.3333333333333333703, 0.3333333333333333148, 0.3333333333333333148, 0.3333333333333334814, 0.3333333333333332038, 0.3333333333333334814, 0.3333333333333334259, 0.3333333333333333703, 0.3333333333333334259, 0.3333333333333333148, 0.3333333333333333703, 0.3333333333333334259, 0.3333333333333333148, 0.3333333333333333148, 0.3333333333333334259, 0.3333333333333334259, 0.3333333333333333148, 0.3333333333333334814, 0.3333333333333333703, 0.3333333333333334259, 0.3333333333333333703, 0.3333333333333333148, 0.3333333333333333703, 0.3333333333333333703, 0.3333333333333333703, 0.3333333333333333703, 0.3333333333333333703, 0.3333333333333334814, 0.3333333333333333148, 0.3333333333333334259, 0.3333333333333334259, 0.3333333333333333148, 0.3333333333333334259, 0.3333333333333332038, 0.3333333333333335369, 0.3333333333333332593, 0.3333333333333333703, 0.3333333333333333703, 0.3333333333333333148, 0.3333333333333334259, 0.3333333333333333148, 0.3333333333333334259, 0.3333333333333333148, 0.3333333333333333703, 0.3333333333333334259, 0.3333333333333333703, 0.3333333333333333148, 0.3333333333333333703, 0.3333333333333333148, 0.3333333333333334259, 0.3333333333333334259, 0.3333333333333333148, 0.3333333333333333148, 0.3333333333333333703, 0.3333333333333333703, 0.3333333333333333703, 0.3333333333333333703, 0.3333333333333334259, 0.3333333333333333148, 0.3333333333333334814, 0.3333333333333332593, 0.3333333333333334259, 0.3333333333333333703, 0.3333333333333333703, 0.3333333333333333703, 0.3333333333333333148, 0.3333333333333335369, 0.3333333333333333703, 0.3333333333333332593, 0.3333333333333334814, 0.3333333333333333703, 0.3333333333333333703, 0.3333333333333333703, 0.3333333333333333703, 0.3333333333333333703, 0.3333333333333333703, 0.3333333333333333703, 0.3333333333333333703, 0.3333333333333333703, 0.3333333333333334259, 0.3333333333333332593, 0.3333333333333333148, 0.3333333333333334259, 0.3333333333333334259, 0.3333333333333334259),
 ( 1.000000000000000222, 1.000000000000000222, 1.000000000000000000, 1.000000000000000222, 1.000000000000000000, 0.9999999999999997780, 1.000000000000000222, 1.000000000000000000, 1.000000000000000222, 1.000000000000000222, 1.000000000000000000, 0.9999999999999997780, 1.000000000000000000, 1.000000000000000222, 0.9999999999999997780, 1.000000000000000222, 0.9999999999999994449, 1.000000000000000444, 0.9999999999999996669, 1.000000000000000000, 1.000000000000000222, 1.000000000000000000, 1.000000000000000000, 0.9999999999999997780, 1.000000000000000444, 0.9999999999999996669, 1.000000000000000000, 1.000000000000000222, 0.9999999999999997780, 1.000000000000000000, 0.9999999999999997780, 0.9999999999999997780, 1.000000000000000444, 0.9999999999999994449, 1.000000000000000444, 0.9999999999999997780, 0.9999999999999997780, 0.9999999999999996669, 1.000000000000000222, 1.000000000000000000, 0.9999999999999997780, 1.000000000000000222, 0.9999999999999997780, 1.000000000000000222, 1.000000000000000000, 1.000000000000000222, 1.000000000000000000, 1.000000000000000000, 1.000000000000000444, 0.9999999999999996669, 0.9999999999999997780, 1.000000000000000000, 0.9999999999999997780, 0.9999999999999997780, 1.000000000000000000, 1.000000000000000000, 0.9999999999999997780, 1.000000000000000444, 1.000000000000000000, 0.9999999999999997780, 1.000000000000000222, 0.9999999999999996669, 1.000000000000000222, 1.000000000000000000, 0.9999999999999997780, 1.000000000000000222, 0.9999999999999997780, 1.000000000000000000, 0.9999999999999997780, 1.000000000000000222, 0.9999999999999996669, 1.000000000000000000, 1.000000000000000222, 0.9999999999999997780, 1.000000000000000222, 0.9999999999999996669, 1.000000000000000444, 1.000000000000000000, 1.000000000000000000, 1.000000000000000222, 1.000000000000000222, 1.000000000000000000, 0.9999999999999997780, 1.000000000000000222, 0.9999999999999997780, 1.000000000000000000, 1.000000000000000000, 1.000000000000000000, 0.9999999999999997780, 1.000000000000000000, 0.9999999999999997780, 1.000000000000000222, 0.9999999999999997780, 1.000000000000000000, 1.000000000000000222, 0.9999999999999997780, 1.000000000000000000, 0.9999999999999996669, 1.000000000000000444, 0.9999999999999997780, 1.000000000000000000, 1.000000000000000000, 1.000000000000000000, 0.9999999999999997780, 0.9999999999999997780, 1.000000000000000222, 1.000000000000000222, 0.9999999999999997780, 1.000000000000000000, 1.000000000000000000, 1.000000000000000222, 1.000000000000000222, 1.000000000000000000, 0.9999999999999997780, 1.000000000000000222, 1.000000000000000000, 1.000000000000000000, 0.9999999999999997780, 0.9999999999999997780, 1.000000000000000222, 1.000000000000000000, 1.000000000000000000, 1.000000000000000000, 0.9999999999999997780, 1.000000000000000222, 1.000000000000000000, 1.000000000000000000, 1.000000000000000000, 1.000000000000000444, 0.9999999999999997780, 0.9999999999999997780, 1.000000000000000000, 1.000000000000000000, 0.9999999999999997780, 1.000000000000000222, 0.9999999999999997780, 1.000000000000000222, 1.000000000000000000, 1.000000000000000222, 1.000000000000000222, 1.000000000000000000, 1.000000000000000222, 1.000000000000000000, 0.9999999999999996669, 1.000000000000000222, 0.9999999999999997780, 1.000000000000000444, 0.9999999999999997780, 1.000000000000000000, 0.9999999999999997780, 1.000000000000000222, 1.000000000000000000, 0.9999999999999997780, 1.000000000000000222, 0.9999999999999994449, 1.000000000000000000, 1.000000000000000222, 1.000000000000000222, 0.9999999999999997780, 1.000000000000000444, 0.9999999999999997780, 1.000000000000000222, 0.9999999999999997780, 1.000000000000000222, 0.9999999999999997780, 1.000000000000000000, 1.000000000000000000, 1.000000000000000222, 0.9999999999999997780, 0.9999999999999996669, 1.000000000000000444, 0.9999999999999997780, 1.000000000000000222, 1.000000000000000000, 1.000000000000000222, 0.9999999999999994449, 1.000000000000000444, 0.9999999999999997780, 1.000000000000000000, 1.000000000000000222, 1.000000000000000000, 1.000000000000000000, 0.9999999999999997780, 1.000000000000000444, 0.9999999999999997780, 1.000000000000000444, 0.9999999999999997780, 1.000000000000000000, 1.000000000000000222, 0.9999999999999996669, 1.000000000000000222, 1.000000000000000000, 1.000000000000000000, 0.9999999999999996669, 1.000000000000000222, 1.000000000000000444, 0.9999999999999997780, 1.000000000000000222, 0.9999999999999996669, 1.000000000000000444, 0.9999999999999997780, 1.000000000000000444, 0.9999999999999996669, 0.9999999999999997780, 1.000000000000000000, 0.9999999999999997780, 1.000000000000000000, 1.000000000000000000, 1.000000000000000000, 1.000000000000000000, 0.9999999999999997780, 1.000000000000000000, 0.9999999999999997780, 1.000000000000000000, 1.000000000000000000, 1.000000000000000000, 1.000000000000000000, 0.9999999999999997780, 1.000000000000000222, 0.9999999999999997780, 1.000000000000000222, 0.9999999999999997780, 1.000000000000000222, 0.9999999999999994449, 1.000000000000000444, 1.000000000000000000, 1.000000000000000222, 0.9999999999999997780, 1.000000000000000000, 0.9999999999999997780, 1.000000000000000222, 1.000000000000000000, 1.000000000000000000, 1.000000000000000222, 1.000000000000000222, 0.9999999999999996669, 1.000000000000000444, 0.9999999999999996669, 1.000000000000000444, 0.9999999999999996669, 1.000000000000000000, 1.000000000000000000, 1.000000000000000000, 0.9999999999999997780, 1.000000000000000222, 0.9999999999999997780, 1.000000000000000222, 1.000000000000000000, 0.9999999999999997780, 1.000000000000000000, 1.000000000000000222, 1.000000000000000222, 1.000000000000000000, 1.000000000000000000, 1.000000000000000000, 1.000000000000000000, 0.9999999999999997780, 1.000000000000000444, 1.000000000000000000, 0.9999999999999997780, 1.000000000000000222, 0.9999999999999996669, 1.000000000000000444, 1.000000000000000000, 1.000000000000000222, 1.000000000000000222, 0.9999999999999997780, 1.000000000000000222, 0.9999999999999997780, 1.000000000000000000, 1.000000000000000000, 0.9999999999999997780, 1.000000000000000000, 1.000000000000000000, 0.9999999999999997780, 1.000000000000000222, 1.000000000000000000, 1.000000000000000000, 1.000000000000000222, 1.000000000000000000, 1.000000000000000000, 1.000000000000000000, 1.000000000000000222, 0.9999999999999997780, 1.000000000000000222, 1.000000000000000000, 0.9999999999999997780, 1.000000000000000222, 0.9999999999999997780, 1.000000000000000222, 1.000000000000000222, 1.000000000000000000, 0.9999999999999997780, 1.000000000000000000, 1.000000000000000222, 1.000000000000000000, 1.000000000000000000, 0.9999999999999996669, 1.000000000000000444, 0.9999999999999994449, 1.000000000000000444, 0.9999999999999997780, 1.000000000000000000, 1.000000000000000000, 0.9999999999999997780, 1.000000000000000222, 0.9999999999999997780, 1.000000000000000000, 1.000000000000000444, 0.9999999999999997780, 1.000000000000000000, 0.9999999999999997780, 1.000000000000000000, 1.000000000000000000, 0.9999999999999997780, 0.9999999999999997780, 1.000000000000000000, 1.000000000000000444, 1.000000000000000000, 1.000000000000000444, 1.000000000000000000, 1.000000000000000000, 1.000000000000000000, 0.9999999999999997780, 1.000000000000000000, 1.000000000000000000, 1.000000000000000000, 1.000000000000000000, 0.9999999999999997780, 1.000000000000000222, 1.000000000000000000, 0.9999999999999997780, 1.000000000000000444, 0.9999999999999997780, 1.000000000000000222, 0.9999999999999996669, 1.000000000000000444, 1.000000000000000000, 0.9999999999999997780, 1.000000000000000000, 1.000000000000000000, 1.000000000000000000, 0.9999999999999997780, 1.000000000000000000, 1.000000000000000000, 0.9999999999999997780, 1.000000000000000444, 0.9999999999999997780, 0.9999999999999997780, 1.000000000000000000, 1.000000000000000000, 1.000000000000000222, 1.000000000000000222, 0.9999999999999997780, 1.000000000000000000, 1.000000000000000222, 1.000000000000000000, 0.9999999999999997780, 1.000000000000000222, 1.000000000000000000, 1.000000000000000000, 1.000000000000000000, 0.9999999999999997780, 1.000000000000000000, 1.000000000000000000, 1.000000000000000000, 1.000000000000000000, 0.9999999999999997780, 1.000000000000000666, 0.9999999999999996669, 0.9999999999999996669, 1.000000000000000444, 0.9999999999999996669, 1.000000000000000222, 1.000000000000000000, 1.000000000000000000, 1.000000000000000000, 1.000000000000000000, 1.000000000000000000, 0.9999999999999997780, 1.000000000000000222, 1.000000000000000222, 0.9999999999999996669, 0.9999999999999997780, 1.000000000000000000, 1.000000000000000222, 1.000000000000000222) ) ) 
 REPRESENTATION_ITEM ( '' )  SURFACE ( )  );
#164987=CARTESIAN_POINT ( 'NONE',  ( 4.984931625306495029, 2.076298541577546342, 0.6347802954964998357 ) ) ;
#164989=CARTESIAN_POINT ( 'NONE',  ( 5.805875103277515770, -1.124240986939632592, -1.673857227857282082 ) ) ;
#164990=CARTESIAN_POINT ( 'NONE',  ( 0.7500000000000005551, 4.270513119278528127E-14, 2.052068128417952497 ) ) ;
#164992=CARTESIAN_POINT ( 'NONE',  ( 2.432535651424679646, 1.868085840533942221, 0.4698736581597633966 ) ) ;
#164994=CARTESIAN_POINT ( 'NONE',  ( 6.082328216444968128, 1.141246503175277205, 1.905736721132505140 ) ) ;
#164996=CARTESIAN_POINT ( 'NONE',  ( 6.983263157960368339, 4.695310640067480001, 2.508805386165738227 ) ) ;
#164999=CARTESIAN_POINT ( 'NONE',  ( 1.647463811467297701, 0.2220449547728920447, 2.210189655316461277 ) ) ;
#165000=CARTESIAN_POINT ( 'NONE',  ( 6.461383593301071926, 1.630371061775518271, 1.090930979547571456 ) ) ;
#165004=DIRECTION ( 'NONE',  ( 2.949029909160572061E-17, 1.000000000000000000, -8.673600428462579015E-15 ) ) ;
#165005=CARTESIAN_POINT ( 'NONE',  ( 4.299324853187779460, -1.796095115987613955, 1.014086197209535634 ) ) ;
#165009=CARTESIAN_POINT ( 'NONE',  ( 6.116445839754358182, 1.256427234498383561, -1.385894902050835542 ) ) ;
#165010=CARTESIAN_POINT ( 'NONE',  ( 4.711369565069784215, 1.661324788532690500, 0.4972849887868810437 ) ) ;
#165011=CARTESIAN_POINT ( 'NONE',  ( 4.950617407298735451, -1.474004690277466834, -0.9251219707713809193 ) ) ;
#165013=CARTESIAN_POINT ( 'NONE',  ( 1.593750267980385882, -0.7671775610453807070, 2.160330554385545110 ) ) ;
#165015=CARTESIAN_POINT ( 'NONE',  ( 6.023005994326640078, -1.968326514718239828, 0.7052485104920204195 ) ) ;
#165016=CARTESIAN_POINT ( 'NONE',  ( 1.183273638618479673, -0.8294958387620559037, 1.643756842616146630 ) ) ;
#165020=CARTESIAN_POINT ( 'NONE',  ( 3.182267690267494231, 1.591318367894577701, 1.238320962759748234 ) ) ;
#165021=CARTESIAN_POINT ( 'NONE',  ( -0.01142137120296871262, -0.4863542539808898280, -2.144715426241408984 ) ) ;
#165024=CARTESIAN_POINT ( 'NONE',  ( 1.293514844328220281, -1.872496763586928514, 0.8835221827151735763 ) ) ;
#165027=CARTESIAN_POINT ( 'NONE',  ( 3.580828998445852562, -1.422877522674294903, 1.572404880189558485 ) ) ;
#165030=CARTESIAN_POINT ( 'NONE',  ( 5.549374350267230582, -1.441814640532925074, -1.119852386600270533 ) ) ;
#165037=CARTESIAN_POINT ( 'NONE',  ( 3.603775140268844712, 1.465814181579458753, 1.389848736882649094 ) ) ;
#165038=CARTESIAN_POINT ( 'NONE',  ( 6.493228066955544442, 1.923254169853494178, -1.081975473724585690 ) ) ;
#165041=CARTESIAN_POINT ( 'NONE',  ( 5.682414339916787682, 1.109973489246698808, -1.493480506080862469 ) ) ;
#165048=CARTESIAN_POINT ( 'NONE',  ( 6.420785563114608685, 1.921975812937461781, 0.7442927364858693551 ) ) ;
#165052=CARTESIAN_POINT ( 'NONE',  ( 2.090756734626127766, 1.002568922338117563, -1.414341044747928766 ) ) ;
#165053=CARTESIAN_POINT ( 'NONE',  ( 1.429236002152774576, 0.8600564655791165247, -1.512861638240108997 ) ) ;
#165054=CARTESIAN_POINT ( 'NONE',  ( 6.551428954101934821, -1.849038126066489207, -1.380618780084260644 ) ) ;
#165057=CARTESIAN_POINT ( 'NONE',  ( 2.179047869568909945, -0.09785464545388269930, -2.058565441667548068 ) ) ;
#165059=CARTESIAN_POINT ( 'NONE',  ( 0.9134352171796227271, 0.5825640498151598567, 1.930122961472901855 ) ) ;
#165062=CARTESIAN_POINT ( 'NONE',  ( 6.543822781336226413, 0.7137633992815132222, -1.729328153040734506 ) ) ;
#165064=CARTESIAN_POINT ( 'NONE',  ( 4.974826827724895928, -1.381046924789817831, 1.323090558688621909 ) ) ;
#165067=CARTESIAN_POINT ( 'NONE',  ( 6.410767893487317792, 1.638320036227768783, -1.478771730184471389 ) ) ;
#165071=CARTESIAN_POINT ( 'NONE',  ( 0.2760433103432077262, 1.997375541027920587, -0.2984889601853820129 ) ) ;
#165075=CARTESIAN_POINT ( 'NONE',  ( 5.016800025512162975, 1.595470874386342608, -1.667385368739245255 ) ) ;
#165076=CARTESIAN_POINT ( 'NONE',  ( 4.879329150013382410, -0.09822140645733207220, 1.959542894978071992 ) ) ;
#165077=CARTESIAN_POINT ( 'NONE',  ( 2.395295693335119935, -1.754585731169123752, 0.8775363634117984146 ) ) ;
#165080=CARTESIAN_POINT ( 'NONE',  ( 0.5150563930837145366, 0.1624822992478615336, 2.111197286521369065 ) ) ;
#165083=CARTESIAN_POINT ( 'NONE',  ( 0.6207436649305307919, -1.749090901066195691, 0.5750481222980761142 ) ) ;
#165085=CARTESIAN_POINT ( 'NONE',  ( 4.364261492936694076, -2.165649721281979190, 0.1538544128360258556 ) ) ;
#165087=CARTESIAN_POINT ( 'NONE',  ( 1.547299434221154124, 0.2130619955753136618, 2.109896976817266179 ) ) ;
#165092=CARTESIAN_POINT ( 'NONE',  ( 2.003267984693514858, 1.711604303819891593, 1.147383568780909302 ) ) ;
#165095=CARTESIAN_POINT ( 'NONE',  ( 0.07735805125220260314, 1.351236195817316466, -2.344668200922094492 ) ) ;
#165097=CARTESIAN_POINT ( 'NONE',  ( 6.006500814222540008, -1.903516144586704151, -0.1827706444143817055 ) ) ;
#165100=CARTESIAN_POINT ( 'NONE',  ( 1.985968398796404299, 1.559226912063184534, 1.639530705753606821 ) ) ;
#165102=CARTESIAN_POINT ( 'NONE',  ( 1.564434226245875026, 0.5705330181091838870, 1.719429346978663897 ) ) ;
#165103=CARTESIAN_POINT ( 'NONE',  ( 1.710024596074321002, 1.099767263899156244, -1.568400350156524459 ) ) ;
#165104=CARTESIAN_POINT ( 'NONE',  ( 3.525891238081061640, 2.020528833579691597, -0.4508363271973143682 ) ) ;
#165106=CARTESIAN_POINT ( 'NONE',  ( 1.991034414115494089, 1.716142376821601534, -0.9701854037313780710 ) ) ;
#165107=CARTESIAN_POINT ( 'NONE',  ( 5.145112535762402572, -1.651256390841379762, 0.9921342509419928124 ) ) ;
#165108=CARTESIAN_POINT ( 'NONE',  ( 1.331197006551400497, 2.225188506942116895, 0.6113326355875832174 ) ) ;
#165111=CARTESIAN_POINT ( 'NONE',  ( 5.652800580869365099, -0.4976084531597444460, -2.001653870753268283 ) ) ;
#165115=CARTESIAN_POINT ( 'NONE',  ( 6.668975466350578252, -1.923848446808050783, -0.8571054451525415008 ) ) ;
#165118=CARTESIAN_POINT ( 'NONE',  ( 5.307972821619873827, -2.151738229465068653, 0.2060058040841972193 ) ) ;
#165119=CARTESIAN_POINT ( 'NONE',  ( 5.356120063770971385, 0.8164924478912498618, -1.847455861782754782 ) ) ;
#165127=CARTESIAN_POINT ( 'NONE',  ( 3.432827581131673522, -1.645759781613131967, 1.164986487700324425 ) ) ;
#165132=CARTESIAN_POINT ( 'NONE',  ( 4.557600102482579629, 0.4766696971462945909, -2.108333899287537339 ) ) ;
#165137=CARTESIAN_POINT ( 'NONE',  ( 5.396111305808362957, -0.9091601233324579923, -1.799916296964368279 ) ) ;
#165139=CARTESIAN_POINT ( 'NONE',  ( 1.154464490038846547, -1.361941861570209467, 1.058318063114448648 ) ) ;
#165144=CARTESIAN_POINT ( 'NONE',  ( 0.3503969169679886919, -1.426633182142377443, 1.047046497418676392 ) ) ;
#165145=CARTESIAN_POINT ( 'NONE',  ( 0.7154901591317133214, 1.647040347281914396, 1.157252022262734714 ) ) ;
#165146=CARTESIAN_POINT ( 'NONE',  ( 6.539320575229245591, 2.459069921018588900, 2.280790101157427419 ) ) ;
#165151=CARTESIAN_POINT ( 'NONE',  ( 2.297662419472700002, 1.937625723843895864, -0.8618613456389671024 ) ) ;
#165152=CARTESIAN_POINT ( 'NONE',  ( 2.302361438560030393, 1.314982760645909465, -1.528754769246756240 ) ) ;
#165153=CARTESIAN_POINT ( 'NONE',  ( 2.197251250676080847, 1.655042475022786785, -0.7371099161151051238 ) ) ;
#165155=CARTESIAN_POINT ( 'NONE',  ( 6.227428301493934448, -2.037140905555033576, 0.7235935974677574212 ) ) ;
#165158=CARTESIAN_POINT ( 'NONE',  ( 0.5322733027907312620, 0.5591794568308214863, 1.832249074504808783 ) ) ;
#165164=CARTESIAN_POINT ( 'NONE',  ( 4.153314892778156242, -1.795761387672462961, -1.203114871582221079 ) ) ;
#165167=CARTESIAN_POINT ( 'NONE',  ( 2.021885665735908333, -0.4598567139443253682, 2.069992740399699382 ) ) ;
#165168=CARTESIAN_POINT ( 'NONE',  ( 6.440460073785046369, 1.806197173870389694, 0.2645596887278709453 ) ) ;
#165169=( BOUNDED_SURFACE ( )  B_SPLINE_SURFACE ( 3, 3, ( 
 ( #185156, #56247, #139654, #3193, #69264, #85537, #37860, #201399, #153748, #71398 ),
 ( #73550, #184099, #54117, #151628, #135380, #40003, #55180, #203526, #53036, #19462 ),
 ( #120251, #121325, #202462, #169982, #152676, #86609, #187301, #168922, #172133, #38927 ),
 ( #20527, #119171, #36780, #171050, #21569, #102865, #138572, #51989, #4259, #7471 ),
 ( #70329, #105010, #101795, #6400, #103940, #22648, #118114, #136446, #88758, #106112 ),
 ( #87676, #5316, #154815, #23728, #204594, #122405, #188363, #89834, #155882, #35719 ),
 ( #8548, #95159, #94100, #193693, #160139, #45337, #208864, #127736, #174283, #190489 ) ),
 .UNSPECIFIED., .T., .F., .T. ) 
 B_SPLINE_SURFACE_WITH_KNOTS ( ( 4, 3, 4 ),
 ( 4, 1, 1, 1, 1, 1, 1, 4 ),
 ( 0.000000000000000000, 0.5000000000000000000, 1.000000000000000000 ),
 ( 0.000000000000000000, 0.09853459476447307130, 0.1926867929487333375, 0.2613852218134048999, 0.3629775382994345767, 0.5216635214973427415, 0.7338723600040717443, 1.000000000000000000 ),
 .UNSPECIFIED. ) 
 GEOMETRIC_REPRESENTATION_ITEM ( )  RATIONAL_B_SPLINE_SURFACE ( (
 ( 1.000000000000000000, 1.000000000000000000, 1.000000000000000222, 1.000000000000000000, 0.9999999999999997780, 1.000000000000000000, 0.9999999999999997780, 0.9999999999999997780, 1.000000000000000000, 1.000000000000000000),
 ( 0.3333333333333333703, 0.3333333333333333703, 0.3333333333333334259, 0.3333333333333333703, 0.3333333333333332593, 0.3333333333333334259, 0.3333333333333333148, 0.3333333333333333148, 0.3333333333333333703, 0.3333333333333333703),
 ( 0.3333333333333333703, 0.3333333333333333703, 0.3333333333333334259, 0.3333333333333333703, 0.3333333333333332593, 0.3333333333333334259, 0.3333333333333333148, 0.3333333333333333148, 0.3333333333333333703, 0.3333333333333333703),
 ( 1.000000000000000000, 1.000000000000000000, 1.000000000000000222, 1.000000000000000000, 0.9999999999999997780, 1.000000000000000000, 0.9999999999999997780, 0.9999999999999997780, 1.000000000000000000, 1.000000000000000000),
 ( 0.3333333333333333703, 0.3333333333333333703, 0.3333333333333334259, 0.3333333333333333703, 0.3333333333333332593, 0.3333333333333334259, 0.3333333333333333148, 0.3333333333333333148, 0.3333333333333333703, 0.3333333333333333703),
 ( 0.3333333333333333703, 0.3333333333333333703, 0.3333333333333334259, 0.3333333333333333703, 0.3333333333333332593, 0.3333333333333334259, 0.3333333333333333148, 0.3333333333333333148, 0.3333333333333333703, 0.3333333333333333703),
 ( 1.000000000000000000, 1.000000000000000000, 1.000000000000000222, 1.000000000000000000, 0.9999999999999997780, 1.000000000000000000, 0.9999999999999997780, 0.9999999999999997780, 1.000000000000000000, 1.000000000000000000) ) ) 
 REPRESENTATION_ITEM ( '' )  SURFACE ( )  );
#165170=CARTESIAN_POINT ( 'NONE',  ( 3.848864690211077466, -1.613568265775822130, 1.132301161112803545 ) ) ;
#165171=CARTESIAN_POINT ( 'NONE',  ( 5.748291730981218706, 0.9368611416523886515, -1.667099895225135686 ) ) ;
#165174=CARTESIAN_POINT ( 'NONE',  ( 6.566861343609567747, 1.460344857008318398, -1.321773145083295464 ) ) ;
#165175=CARTESIAN_POINT ( 'NONE',  ( 1.939301023820143577, 0.7432367423349227620, -1.794281902191755540 ) ) ;
#165180=CARTESIAN_POINT ( 'NONE',  ( 2.080132315211229876, -2.050506710900898977, -0.4067329413659624970 ) ) ;
#165184=CARTESIAN_POINT ( 'NONE',  ( 5.777967262743825216, 1.883199444611630691, -0.3313529498064629597 ) ) ;
#165186=CARTESIAN_POINT ( 'NONE',  ( 4.793709216081707858, 1.633822259641436903, 1.483752339651790653 ) ) ;
#165188=CARTESIAN_POINT ( 'NONE',  ( 1.483733071427257411, 2.038639745401783721, -0.8453341458589253010 ) ) ;
#165189=CARTESIAN_POINT ( 'NONE',  ( 0.8031952904608251620, 1.686239601473665140, -0.9019194118903075541 ) ) ;
#165192=CARTESIAN_POINT ( 'NONE',  ( 3.754400092289136293, -2.067862582909282487, -0.1045053291982081939 ) ) ;
#165196=CARTESIAN_POINT ( 'NONE',  ( 1.850665834824256173, 0.6780317805383448970, 2.052694239800388676 ) ) ;
#165197=CARTESIAN_POINT ( 'NONE',  ( 4.019203527901527018, -2.096847714747759106, 0.6372333828079318474 ) ) ;
#165206=CARTESIAN_POINT ( 'NONE',  ( 6.223290642006293893, 1.716731611696775683, 0.2442158411369663995 ) ) ;
#165208=CARTESIAN_POINT ( 'NONE',  ( 4.399325512199628641, -1.803763729973751451, 1.015883459259236954 ) ) ;
#165209=CARTESIAN_POINT ( 'NONE',  ( 5.782842150838196638, 1.730585719646136056, -1.219460781990765463 ) ) ;
#165212=CARTESIAN_POINT ( 'NONE',  ( 3.080859285270169057, 1.852775266960526412, 0.6680929264101590492 ) ) ;
#165213=CARTESIAN_POINT ( 'NONE',  ( 6.087847202767847854, -2.280615992951875448, -0.2307264670357595804 ) ) ;
#165214=CARTESIAN_POINT ( 'NONE',  ( 2.596107596775329540, -1.820790993511243849, -0.1344670722737417168 ) ) ;
#165220=CARTESIAN_POINT ( 'NONE',  ( 4.131111929362305091, 1.842322257054655354, 0.8120569753113301426 ) ) ;
#165221=CARTESIAN_POINT ( 'NONE',  ( 4.926587646396720643, -1.284401507782207963, 1.482881906352449874 ) ) ;
#165225=CARTESIAN_POINT ( 'NONE',  ( 0.02900754732045561154, -1.909850462538491778, 0.8511534736125156986 ) ) ;
#165226=CARTESIAN_POINT ( 'NONE',  ( 5.418734442855144273, 1.636401904928608042, 0.6746929113052438920 ) ) ;
#165228=CARTESIAN_POINT ( 'NONE',  ( 1.359612608069911133, 2.158557413232742750, -0.3773744582575569995 ) ) ;
#165229=CARTESIAN_POINT ( 'NONE',  ( 0.8721245864499425071, -0.04093463707061052725, -1.740139661330299514 ) ) ;
#165231=CARTESIAN_POINT ( 'NONE',  ( 0.1333692844072316419, 7.629137130509075604, -2.653547345224521514 ) ) ;
#165232=CARTESIAN_POINT ( 'NONE',  ( 0.4336905314940731060, 0.8911838752851186651, -1.476660275499335873 ) ) ;
#165233=CARTESIAN_POINT ( 'NONE',  ( 0.5272844384777974902, 2.272924705895418285, -0.3403917945235325204 ) ) ;
#165234=CARTESIAN_POINT ( 'NONE',  ( 0.6443834720083198020, 0.6415979653194536780, 2.095529601600601755 ) ) ;
#165235=CARTESIAN_POINT ( 'NONE',  ( 2.807470779205251343, 1.864772411128329477, 1.179945617918669143 ) ) ;
#165237=CARTESIAN_POINT ( 'NONE',  ( 1.446384731406271218, -0.9785283779201507937, 1.938150590114567473 ) ) ;
#165239=CARTESIAN_POINT ( 'NONE',  ( 1.868513053102664356, -2.077584836267523105, -0.4075993926472165074 ) ) ;
#165240=CARTESIAN_POINT ( 'NONE',  ( 6.827182134110238110, -0.009824402486291110986, 2.288967694407703313 ) ) ;
#165241=CARTESIAN_POINT ( 'NONE',  ( 5.790048612033079856, -0.8660258810785811390, 1.720834695440204509 ) ) ;
#165243=CARTESIAN_POINT ( 'NONE',  ( 2.454944477651953783, -1.996203790030710801, -1.126857184891062236 ) ) ;
#165248=CARTESIAN_POINT ( 'NONE',  ( 5.074942145771424329, -1.609735135204511280, 1.530878986171863687 ) ) ;
#165255=CARTESIAN_POINT ( 'NONE',  ( 2.690077459517980163, 1.704938782060089864, 1.076316768488336351 ) ) ;
#165257=CARTESIAN_POINT ( 'NONE',  ( 1.411062195701995980, -1.628543573593312921, 1.265665014175233916 ) ) ;
#165262=CARTESIAN_POINT ( 'NONE',  ( 3.697391623616069101, -0.6365095100077067247, 2.096977347260075231 ) ) ;
#165263=CARTESIAN_POINT ( 'NONE',  ( 1.512342498431101134, -1.897697209584522815, 0.6819976561535444626 ) ) ;
#165264=CARTESIAN_POINT ( 'NONE',  ( 1.223879446662301307, 1.774596971308094018, 0.4907264878865265634 ) ) ;
#165265=CARTESIAN_POINT ( 'NONE',  ( 4.259580805731934205, 0.8699401392010926992, 1.622648742527862620 ) ) ;
#165269=CARTESIAN_POINT ( 'NONE',  ( 4.717693524642503355, -1.790169364231732674, 0.3569235582787863570 ) ) ;
#165270=CARTESIAN_POINT ( 'NONE',  ( 5.783827325522512552, 1.646840809264274119, -1.163266671679111353 ) ) ;
#165272=CARTESIAN_POINT ( 'NONE',  ( 4.258826902089789535, -1.679047235397194804, 1.516690725115140692 ) ) ;
#165274=CARTESIAN_POINT ( 'NONE',  ( 0.4519647057620000408, 0.6586765168765180700, -2.000488393216502292 ) ) ;
#165276=CARTESIAN_POINT ( 'NONE',  ( 4.193848433072798088, -1.425472641756184489, -1.501718461524886195 ) ) ;
#165285=CARTESIAN_POINT ( 'NONE',  ( 0.2113915902133572944, 1.759560880827226947, -1.183302968686468226 ) ) ;
#165286=CARTESIAN_POINT ( 'NONE',  ( 1.564984312397620814, 0.7026195195478746047, 2.107413697313319290 ) ) ;
#165290=CARTESIAN_POINT ( 'NONE',  ( 2.857805160684105950, -0.6180756922911297968, 1.862011555624979886 ) ) ;
#165296=CARTESIAN_POINT ( 'NONE',  ( 2.619513681940002670, 1.793805257907291395, 1.130712135851599465 ) ) ;
#165298=CARTESIAN_POINT ( 'NONE',  ( 4.369553226407375313, -0.3375162941181614751, 1.932460123137308861 ) ) ;
#165299=CARTESIAN_POINT ( 'NONE',  ( 2.764712544972968811, -1.491509591961351910, 1.564943835847030229 ) ) ;
#165300=CARTESIAN_POINT ( 'NONE',  ( 2.595044651933966495, -0.5755060336137384214, 1.749081985381637061 ) ) ;
#165303=CARTESIAN_POINT ( 'NONE',  ( 4.540767487494163035, -1.347652659646558115, -1.101159657664248170 ) ) ;
#165308=CARTESIAN_POINT ( 'NONE',  ( 2.167066695894452888, -1.976221826324360498, -0.8764929760368763700 ) ) ;
#165309=CARTESIAN_POINT ( 'NONE',  ( 4.938827285099913311, 1.158512636183751665, 1.649828125244500843 ) ) ;
#165311=CARTESIAN_POINT ( 'NONE',  ( 1.340939272977889951, 0.4221563536682856332, 2.119910705745978508 ) ) ;
#165312=CARTESIAN_POINT ( 'NONE',  ( 2.975414797803474176, 1.872564425654202225, -0.6168198417838985925 ) ) ;
#165313=CARTESIAN_POINT ( 'NONE',  ( 3.163306973099208275, 0.2928498925126362673, -1.949387327701812334 ) ) ;
#165314=CARTESIAN_POINT ( 'NONE',  ( 6.509000000000034980, 7.629137130509102249, 2.699999999999993516 ) ) ;
#165315=CARTESIAN_POINT ( 'NONE',  ( 2.964326597902953608, -1.795398894311397209, -0.7408281928331180710 ) ) ;
#165325=CARTESIAN_POINT ( 'NONE',  ( 1.079469989902905214, -0.05558308599296066244, -2.206230565744627281 ) ) ;
#165327=CARTESIAN_POINT ( 'NONE',  ( 5.260583753728677259, -0.6573284944802314511, -1.848511375219172415 ) ) ;
#165329=CARTESIAN_POINT ( 'NONE',  ( 3.450509668567053545, -1.418736885945747428, 1.571922360790501738 ) ) ;
#165331=CARTESIAN_POINT ( 'NONE',  ( 0.07479286986305544449, 2.888457405263197941, -2.344396930208477947 ) ) ;
#165332=CARTESIAN_POINT ( 'NONE',  ( 3.995923475689294513, -0.5793754966058572986, -1.747668199984537152 ) ) ;
#165337=CARTESIAN_POINT ( 'NONE',  ( 5.045234882716379765, 0.1584239314957915090, 2.114765283346302205 ) ) ;
#165339=CARTESIAN_POINT ( 'NONE',  ( 5.782513925583750769, -2.009559558911724775, -0.4558285042701361589 ) ) ;
#165341=CARTESIAN_POINT ( 'NONE',  ( 0.5724163261710726314, 1.287614217418028506, -1.343956351914729952 ) ) ;
#165342=CARTESIAN_POINT ( 'NONE',  ( 2.647807870277216757, 0.6224553824519338807, 1.732961026760751366 ) ) ;
#165348=CARTESIAN_POINT ( 'NONE',  ( 2.772332522587173997, 1.181257105606844160, 1.863944272329665086 ) ) ;
#165349=CARTESIAN_POINT ( 'NONE',  ( 4.376441990627045087, -1.307286168679543614, 1.846302370218126265 ) ) ;
#165350=CARTESIAN_POINT ( 'NONE',  ( 3.643767777461913493, 2.000731686840724333, -0.2516315899964287617 ) ) ;
#165352=CARTESIAN_POINT ( 'NONE',  ( 4.939644399817936460, -1.717766137778716118, 0.5755910463909068575 ) ) ;
#165353=CARTESIAN_POINT ( 'NONE',  ( 5.208173988833650903, 1.135812200204017630, -1.542565181195413526 ) ) ;
#165354=CARTESIAN_POINT ( 'NONE',  ( 4.979306205331720747, 1.745251617482036943, -0.6738592683939447214 ) ) ;
#165355=CARTESIAN_POINT ( 'NONE',  ( 5.265987090187672415, -1.852092866064008803, 0.1821183643400964280 ) ) ;
#165358=CARTESIAN_POINT ( 'NONE',  ( 5.981276632755388789, 1.633781900041403334, -0.6810181619275444964 ) ) ;
#165361=CARTESIAN_POINT ( 'NONE',  ( 0.09298292169932984019, 1.756857073293972116, 0.9896806593640145033 ) ) ;
#165363=CARTESIAN_POINT ( 'NONE',  ( 3.264387862500417903, 0.9470664325190655264, 1.881190857022313478 ) ) ;
#165368=CARTESIAN_POINT ( 'NONE',  ( 1.898700399197379651, -1.981625571768164340, -0.3898374508689693152 ) ) ;
#165372=CARTESIAN_POINT ( 'NONE',  ( 2.214359598146302677, -1.016813397907929239, -1.907474440234189217 ) ) ;
#165373=CARTESIAN_POINT ( 'NONE',  ( 6.609999999999968345, 7.051749200714771959, 2.878153929105996323 ) ) ;
#165380=CARTESIAN_POINT ( 'NONE',  ( 0.7147126110796617748, 2.027027023440019171, 0.8336157706642086662 ) ) ;
#165382=CARTESIAN_POINT ( 'NONE',  ( 1.991474686832030994, 1.968180706754483644, -1.115757519136374221 ) ) ;
#165389=CARTESIAN_POINT ( 'NONE',  ( 3.549836697621409964, 1.769921775324476698, 0.002857994197370468913 ) ) ;
#165390=CARTESIAN_POINT ( 'NONE',  ( 6.616270032800761314, -1.034323699838369359, -1.949367651511712207 ) ) ;
#165394=CARTESIAN_POINT ( 'NONE',  ( 5.044546077387519922, -1.458546410489666600, 1.392558106302365095 ) ) ;
#165395=CARTESIAN_POINT ( 'NONE',  ( 4.834136970758627250, -0.9753174380719393799, -1.526440946957215994 ) ) ;
#165398=CARTESIAN_POINT ( 'NONE',  ( 2.061206331123175861, 0.3224310286589862629, -1.842498087946140561 ) ) ;
#165400=CARTESIAN_POINT ( 'NONE',  ( 3.766520095694513515, -0.8345382577515869649, -1.894767260282135490 ) ) ;
#165402=CARTESIAN_POINT ( 'NONE',  ( 1.757924209179074770, 0.7287868685415777037, -1.768279316124596878 ) ) ;
#165407=CARTESIAN_POINT ( 'NONE',  ( 0.7910927259777954523, -0.04954035392716604758, -1.911929172785244102 ) ) ;
#165408=B_SPLINE_CURVE_WITH_KNOTS ( 'NONE', 3,
 ( #179070, #97826, #95702, #79422, #30690, #211537, #162823, #93561, #142325, #63172, #59967 ),
 .UNSPECIFIED., .F., .F.,
 ( 4, 1, 1, 1, 1, 1, 1, 1, 4 ),
 ( 0.000000000000000000, 0.2254704865597413344, 0.3973194950497592193, 0.5246576192285303808, 0.6166070239209043846, 0.6823180413592140336, 0.7309932997181896042, 0.7717238569598857678, 1.000000000000000000 ),
 .UNSPECIFIED. ) ;
#165410=CARTESIAN_POINT ( 'NONE',  ( 2.734756269166933151, -1.876540383875524576, -0.5722209215143353456 ) ) ;
#165411=CARTESIAN_POINT ( 'NONE',  ( 0.2806244687772480040, -1.977743564115455932, 0.3905345501400147024 ) ) ;
#165413=CARTESIAN_POINT ( 'NONE',  ( 5.678019686890188211, 2.088907387943875982, -0.3644037002746222664 ) ) ;
#165416=CARTESIAN_POINT ( 'NONE',  ( 6.432890565879505473, 0.1910017811236862373, 1.962057160394870881 ) ) ;
#165418=CARTESIAN_POINT ( 'NONE',  ( 1.986589674187682064, -1.235133946311824049, 1.589746892572386994 ) ) ;
#165420=CARTESIAN_POINT ( 'NONE',  ( 1.476322311366547124, -2.107388574805735271, -0.2037450385454323831 ) ) ;
#165422=CARTESIAN_POINT ( 'NONE',  ( 2.770052221688572125, -2.048192801557855436, 0.3012726569043902569 ) ) ;
#165424=CARTESIAN_POINT ( 'NONE',  ( 6.158164957586691912, -1.479299979846586455, 1.477571280793017694 ) ) ;
#165426=CARTESIAN_POINT ( 'NONE',  ( 4.295794115256676982, -0.6985059363485807138, 1.686860163339451990 ) ) ;
#165430=CARTESIAN_POINT ( 'NONE',  ( 6.890000000000005898, 2.048573291599069091, 2.305811639209849773 ) ) ;
#165432=CARTESIAN_POINT ( 'NONE',  ( 5.016741729952475914, 1.524926965779101140, -1.595359541877178877 ) ) ;
#165435=CARTESIAN_POINT ( 'NONE',  ( 4.248624793116656306, 1.876006594227698221, 0.3698101955103145211 ) ) ;
#165442=CARTESIAN_POINT ( 'NONE',  ( 0.01093749962182561340, -1.805946196879630872, 0.3578947576599255109 ) ) ;
#165446=CARTESIAN_POINT ( 'NONE',  ( 4.833189656263336964, -1.710893631887340005, 0.7565425265826586365 ) ) ;
#165451=CARTESIAN_POINT ( 'NONE',  ( 1.516386633922983895, 0.7932475597272764523, 1.802804710252394527 ) ) ;
#165452=CARTESIAN_POINT ( 'NONE',  ( 1.933220473845993492, -1.621196910160098925, -1.198842755339262212 ) ) ;
#165456=CARTESIAN_POINT ( 'NONE',  ( 3.011879173929287834, -1.080601074572758558, -1.906429682232862799 ) ) ;
#165457=CARTESIAN_POINT ( 'NONE',  ( 6.568987803155795113, -1.671525225137669102, -0.7347104647430282576 ) ) ;
#165459=CARTESIAN_POINT ( 'NONE',  ( 6.825078400183548055, 2.461594334264828987, 2.239602747093616841 ) ) ;
#165467=CARTESIAN_POINT ( 'NONE',  ( 4.810013364240863787, 1.265987717737980134, -1.337210144835267345 ) ) ;
#165468=CARTESIAN_POINT ( 'NONE',  ( 1.084635982312625924, -1.275300252541565538, 1.557628696486039077 ) ) ;
#165469=CARTESIAN_POINT ( 'NONE',  ( 2.970384050378202634, 1.940355284992447027, 1.231690374697077095 ) ) ;
#165471=CARTESIAN_POINT ( 'NONE',  ( 1.234942694251008000, -0.03850059531256519452, -1.860717468297488297 ) ) ;
#165475=CARTESIAN_POINT ( 'NONE',  ( 4.148624843374196125, 1.876505540506741010, 0.3678670841067502861 ) ) ;
#165478=CARTESIAN_POINT ( 'NONE',  ( 4.054300615058183510, -1.547851416709244310, 1.405648825684354897 ) ) ;
#165479=CARTESIAN_POINT ( 'NONE',  ( 2.817106861211693847, -0.1851908181382568019, 1.861470920997858380 ) ) ;
#165482=CARTESIAN_POINT ( 'NONE',  ( 5.935073298327618652, -1.338256116417003927, -1.264887592264056559 ) ) ;
#165485=CARTESIAN_POINT ( 'NONE',  ( 4.512129967005336084, -0.7409026826630369378, -1.557792038885176700 ) ) ;
#165487=CARTESIAN_POINT ( 'NONE',  ( 0.2989044949552251418, 1.198067244415670141, -1.254020425504979164 ) ) ;
#165492=CARTESIAN_POINT ( 'NONE',  ( 4.592743594998466072, 2.127975290613278503, 0.4296678846467619772 ) ) ;
#165493=CARTESIAN_POINT ( 'NONE',  ( 2.965264444195826243, 0.2674972279559268973, -1.805858685475017378 ) ) ;
#165494=CARTESIAN_POINT ( 'NONE',  ( 0.5671465430379521999, 1.703994235754960451, 0.9719838849941149217 ) ) ;
#165495=CARTESIAN_POINT ( 'NONE',  ( 5.981681833671104620, -0.7110503908294771858, 1.994531755910114112 ) ) ;
#165498=CARTESIAN_POINT ( 'NONE',  ( 5.583585467610721054, -1.033564708330332316, 2.046191781174087509 ) ) ;
#165501=CARTESIAN_POINT ( 'NONE',  ( 1.752743329737327826, 2.097873456429504735, 0.3079802404963859486 ) ) ;
#165506=CARTESIAN_POINT ( 'NONE',  ( 6.772352023501587936, -1.015705593385501482, -1.918810339808636023 ) ) ;
#165507=CARTESIAN_POINT ( 'NONE',  ( 6.883263157960330503, 7.629137130509037412, 2.753810918356710769 ) ) ;
#165509=CARTESIAN_POINT ( 'NONE',  ( 1.805654246593148660, 1.930672025830199479, -1.098395813934008425 ) ) ;
#165511=CARTESIAN_POINT ( 'NONE',  ( 6.451795992440088057, -1.844709169062180409, -0.8146298745319994206 ) ) ;
#165513=CARTESIAN_POINT ( 'NONE',  ( 4.487212223095434105, 0.09620561770018636050, 2.060423205476647812 ) ) ;
#165519=CARTESIAN_POINT ( 'NONE',  ( 0.2520486530714799445, 0.8021226228236020273, 1.930841216200715360 ) ) ;
#165520=CARTESIAN_POINT ( 'NONE',  ( 4.089279031174639201, -0.7008038172400687937, 1.702867937621636463 ) ) ;
#165524=CARTESIAN_POINT ( 'NONE',  ( 2.361930338997704659, 0.7344707938763440636, 1.560707491107244715 ) ) ;
#165525=CARTESIAN_POINT ( 'NONE',  ( 0.5675926644314840397, 1.357872185771633156, 1.490966652548594285 ) ) ;
#165526=CARTESIAN_POINT ( 'NONE',  ( 1.565480925793379274, -1.225038264044479686, 1.944918359529357543 ) ) ;
#165528=CARTESIAN_POINT ( 'NONE',  ( 1.810245590833154283, -2.245401999695510575, 0.2761584955175334644 ) ) ;
#165529=CARTESIAN_POINT ( 'NONE',  ( 4.424511703531566198, 1.296206220603330461, -1.659847191385990239 ) ) ;
#165531=CARTESIAN_POINT ( 'NONE',  ( 2.565387841970759197, 1.736461783412158955, -0.3405875811831828859 ) ) ;
#165534=CARTESIAN_POINT ( 'NONE',  ( 6.031250000000003553, -0.7852924748303007352, -1.895863743163946680 ) ) ;
#165538=CARTESIAN_POINT ( 'NONE',  ( 5.045291550738682851, 0.1642389012704112972, 2.215424048113129540 ) ) ;
#165539=CARTESIAN_POINT ( 'NONE',  ( 3.064592470464472029, -2.024993410009158890, -0.8382372354380845936 ) ) ;
#165542=CARTESIAN_POINT ( 'NONE',  ( 5.813165546740090228, 1.733599321496303691, -1.220823391460408303 ) ) ;
#165544=CARTESIAN_POINT ( 'NONE',  ( 6.610000000000011866, 2.967812824040619191, 2.453181572820534395 ) ) ;
#165546=CARTESIAN_POINT ( 'NONE',  ( 5.291314375706784645, -0.05428322906628547939, -2.120082430678168706 ) ) ;
#165550=CARTESIAN_POINT ( 'NONE',  ( 6.631704542599726082, -1.407888343591977121, -1.640466528430361670 ) ) ;
#165552=CARTESIAN_POINT ( 'NONE',  ( 5.741722636381444644, 1.839460222191912742, 0.08393339073512616488 ) ) ;
#165555=CARTESIAN_POINT ( 'NONE',  ( 0.9951963871240524506, -1.740626720728695620, -0.001451476259923395245 ) ) ;
#165560=CARTESIAN_POINT ( 'NONE',  ( 5.067319851952804655, 0.2155487944876262052, -2.150937003660175595 ) ) ;
#165563=CARTESIAN_POINT ( 'NONE',  ( 4.961884481312108797, 2.138711985806662330, -0.3135959325617638238 ) ) ;
#165567=CARTESIAN_POINT ( 'NONE',  ( 5.466080325957246799, 0.9693943247218398396, 1.716448534147915650 ) ) ;
#165568=CARTESIAN_POINT ( 'NONE',  ( 5.184772435558752335, -0.9287019638352255191, -1.463892056132688024 ) ) ;
#165570=CARTESIAN_POINT ( 'NONE',  ( 1.611130907606239004, -0.2639259086049255965, 2.175532687872412829 ) ) ;
#165571=CARTESIAN_POINT ( 'NONE',  ( 1.677271382912606246, -2.191714306423699021, -0.7221938283701042627 ) ) ;
#165572=CARTESIAN_POINT ( 'NONE',  ( 4.886040457987857799, -0.9749269275126177803, 1.815604017143893634 ) ) ;
#165573=CARTESIAN_POINT ( 'NONE',  ( 6.567919353034534780, -1.191429365117269157, 1.534444726360333799 ) ) ;
#165577=CARTESIAN_POINT ( 'NONE',  ( -0.2108831679770960255, -0.001785917861228669690, -1.896958272444612792 ) ) ;
#165578=CARTESIAN_POINT ( 'NONE',  ( 4.131183091185314460, 1.940096312829143299, 0.8565103500411813675 ) ) ;
#165580=CARTESIAN_POINT ( 'NONE',  ( 1.266250242576156815, 1.862016182229693673, -0.7743172429433076154 ) ) ;
#165582=CARTESIAN_POINT ( 'NONE',  ( 4.594872931952145301, -0.4798491958124780910, -2.153818993410236970 ) ) ;
#165589=CARTESIAN_POINT ( 'NONE',  ( -0.1290005225502675879, -0.006633637972621592160, -2.173875058097324064 ) ) ;
#165592=CARTESIAN_POINT ( 'NONE',  ( 3.221608841920938993, -1.986550002599724252, 0.5482939856576442006 ) ) ;
#165596=CARTESIAN_POINT ( 'NONE',  ( 3.000653711923051414, -1.990157830909113024, -0.3430147326864175783 ) ) ;
#165600=CARTESIAN_POINT ( 'NONE',  ( 1.780222679459046997, -1.103320402871512673, 1.740482491890801287 ) ) ;
#165604=CARTESIAN_POINT ( 'NONE',  ( -0.2411972340276360705, 6.947779742164541972, -2.495493578726155182 ) ) ;
#165605=CARTESIAN_POINT ( 'NONE',  ( 1.499689682683522207, -0.6613356838569836027, -1.718437284301529422 ) ) ;
#165606=CARTESIAN_POINT ( 'NONE',  ( 6.604147088760183415, -2.206502607372296421, 0.04933187264975073122 ) ) ;
#165608=CARTESIAN_POINT ( 'NONE',  ( 1.651884467337715989, 0.6291892518628816600, -2.067965918892029631 ) ) ;
#165611=CARTESIAN_POINT ( 'NONE',  ( 1.885954221117658092, -2.015980662343511032, 0.05432778586660082232 ) ) ;
#165612=CARTESIAN_POINT ( 'NONE',  ( 2.126706441246130286, 0.3935840842550219487, -2.264316624754546314 ) ) ;
#165614=CARTESIAN_POINT ( 'NONE',  ( 0.09234973940512071489, -0.4041859633337717694, -1.833079292876439670 ) ) ;
#165617=CARTESIAN_POINT ( 'NONE',  ( 4.733256667524862848, -1.802829663221987788, 0.7981805449851049339 ) ) ;
#165618=CARTESIAN_POINT ( 'NONE',  ( 3.081267818761534549, 1.592661989535900657, 1.236799713577160231 ) ) ;
#165622=CARTESIAN_POINT ( 'NONE',  ( 5.707678396406405064, -0.5131847548165735518, 2.042461488563215966 ) ) ;
#165623=CARTESIAN_POINT ( 'NONE',  ( 4.861816338261779613, -0.5554421346023461492, 1.994381909410049669 ) ) ;
#165626=CARTESIAN_POINT ( 'NONE',  ( 6.639320575229291421, 2.053731943030055795, 2.310327526069462234 ) ) ;
#165627=CARTESIAN_POINT ( 'NONE',  ( 5.467059065379825888, -1.589572006150547168, 1.245957840514285042 ) ) ;
#165629=CARTESIAN_POINT ( 'NONE',  ( 3.457953323470845941, 0.5611853863643158080, -2.238310864172543546 ) ) ;
#165630=CARTESIAN_POINT ( 'NONE',  ( 0.6728087625662204641, 1.424998530877854552, -1.491364779339200641 ) ) ;
#165637=CARTESIAN_POINT ( 'NONE',  ( 3.209609721163650509, -1.773450621654437009, -1.252290679139915319 ) ) ;
#165641=CARTESIAN_POINT ( 'NONE',  ( 2.595044651933966495, -0.5755060336137384214, 1.749081985381637061 ) ) ;
#165643=CARTESIAN_POINT ( 'NONE',  ( 4.107102485094754840, -0.3736803571842538529, 2.159302612355806339 ) ) ;
#165645=CARTESIAN_POINT ( 'NONE',  ( 4.803764043965432329, -0.6079002506334645339, 2.179255796609281148 ) ) ;
#165650=CARTESIAN_POINT ( 'NONE',  ( 6.309784262603465699, -1.756040378898944043, 0.2188775834443684731 ) ) ;
#165653=CARTESIAN_POINT ( 'NONE',  ( 4.371743676962040581, 0.4387793907001916738, -1.964547544987900851 ) ) ;
#165655=CARTESIAN_POINT ( 'NONE',  ( 2.801903084826493640, -0.6620233120280398786, 1.999254901717039790 ) ) ;
#165656=CARTESIAN_POINT ( 'NONE',  ( 0.4916157762205043413, -1.906313760269543911, 0.1885876022650559980 ) ) ;
#165658=CARTESIAN_POINT ( 'NONE',  ( 1.873436276770530595, -0.2440693053713405281, 1.954313301998261920 ) ) ;
#165659=CARTESIAN_POINT ( 'NONE',  ( 0.9361565222895779081, 1.842281575443193375, 0.3236747858033904302 ) ) ;
#165660=CARTESIAN_POINT ( 'NONE',  ( 1.486689167417578394, 1.889818972856545987, 0.5264814339432166701 ) ) ;
#165661=CARTESIAN_POINT ( 'NONE',  ( 6.411931881972196610E-05, -0.8997486769052507327, 1.687471195204979457 ) ) ;
#165662=VERTEX_POINT ( 'NONE', #83380 ) ;
#165665=CARTESIAN_POINT ( 'NONE',  ( 5.664887262500884368, -1.691755685069219695, -0.7986314380193232365 ) ) ;
#165670=CARTESIAN_POINT ( 'NONE',  ( 1.346235217667652417, -0.9325981557438846048, 1.848514419461377845 ) ) ;
#165675=CARTESIAN_POINT ( 'NONE',  ( 5.004590575528129470, -2.104527602236761386, -0.2589986953433416894 ) ) ;
#165680=CARTESIAN_POINT ( 'NONE',  ( 5.934033239752055877, 1.167398200610193282, 1.576599764842034457 ) ) ;
#165682=CARTESIAN_POINT ( 'NONE',  ( 2.759138561942891421, -2.010518527590241966, -0.1511176148010634768 ) ) ;
#165683=CARTESIAN_POINT ( 'NONE',  ( 3.415159944131008096, -1.768026670962073110, 0.7381028802780668086 ) ) ;
#165685=CARTESIAN_POINT ( 'NONE',  ( 1.048660896456204528, -1.724490848714568259, 1.352309724062021878 ) ) ;
#165686=CARTESIAN_POINT ( 'NONE',  ( 0.2335667940002320309, 1.326312899344052276, -2.404742575607053734 ) ) ;
#165687=CARTESIAN_POINT ( 'NONE',  ( 3.444469828353763141, 0.4513171681363346566, 1.815172769691273835 ) ) ;
#165691=CARTESIAN_POINT ( 'NONE',  ( 5.923477664823041167, -1.533883339688602465, -1.459648931523350068 ) ) ;
#165694=CARTESIAN_POINT ( 'NONE',  ( 2.859016124132291115, 0.3040538821531354463, -2.068378887337805949 ) ) ;
#165696=CARTESIAN_POINT ( 'NONE',  ( 0.7094338256347174632, -1.717145877019264022, 0.1620263704987124354 ) ) ;
#165706=CARTESIAN_POINT ( 'NONE',  ( 0.2404698186789978875, 1.732857435387507250, 0.5278947837941138088 ) ) ;
#165711=CARTESIAN_POINT ( 'NONE',  ( 6.539320575229250920, 2.072231551265828475, 2.205269387046896679 ) ) ;
#165717=CARTESIAN_POINT ( 'NONE',  ( 2.611566863951066519, 0.4996721132001956112, -1.792629727676842144 ) ) ;
#165719=CARTESIAN_POINT ( 'NONE',  ( 0.4213150654816185114, -1.355317750890722595, -1.354022888547769421 ) ) ;
#165720=CARTESIAN_POINT ( 'NONE',  ( 0.07680821025393690105, 0.005952109439256307241, -1.810863387344714193 ) ) ;
#165726=CARTESIAN_POINT ( 'NONE',  ( 4.961744348476156752, -0.5292939252423340957, 1.896881419486784681 ) ) ;
#165727=CARTESIAN_POINT ( 'NONE',  ( 1.243013918421622233, 2.044566944090483229, 0.5621290157047582614 ) ) ;
#165731=CARTESIAN_POINT ( 'NONE',  ( 5.841772037242090931, 2.188765561305112683, 0.1107676204459909497 ) ) ;
#165733=CARTESIAN_POINT ( 'NONE',  ( 4.348602224742101008, 0.5129591300635885087, 1.856786894687269207 ) ) ;
#165736=CARTESIAN_POINT ( 'NONE',  ( 1.313402753022639091, 1.947697196196996217, 1.037691534346518729 ) ) ;
#165741=CARTESIAN_POINT ( 'NONE',  ( 5.805506361076694155, -1.550124894993635261, -1.214668715896784379 ) ) ;
#165742=CARTESIAN_POINT ( 'NONE',  ( 1.997508135846944421, -1.941589802808607157, 0.04981292379131925518 ) ) ;
#165744=CARTESIAN_POINT ( 'NONE',  ( 6.098996632684510644, 1.141130774408656068, -1.995064312872560697 ) ) ;
#165746=CARTESIAN_POINT ( 'NONE',  ( 4.557361202124784683, 1.492679318236398878, 1.111055945242465093 ) ) ;
#165752=CARTESIAN_POINT ( 'NONE',  ( -0.05867695357848409787, -1.698172713885632401, -1.384993232510664640 ) ) ;
#165758=CARTESIAN_POINT ( 'NONE',  ( 2.051128252772801641, -1.465761996925791122, -1.088229512710245261 ) ) ;
#165760=CARTESIAN_POINT ( 'NONE',  ( 4.166485388134741008, 1.137239580169274067, 1.309253364134143505 ) ) ;
#165763=CARTESIAN_POINT ( 'NONE',  ( 0.1331565106231571705, 4.092041177288479048, -2.500854978060399691 ) ) ;
#165764=CARTESIAN_POINT ( 'NONE',  ( 6.252569598636129378, 0.5776572744066664766, 1.731972519516040032 ) ) ;
#165765=CARTESIAN_POINT ( 'NONE',  ( 4.188298518248590341, 1.053080760608171129, -1.654974388233184657 ) ) ;
#165770=CARTESIAN_POINT ( 'NONE',  ( 5.356147330077114077, 0.8591290142025626020, -1.938821108677920346 ) ) ;
#165774=CARTESIAN_POINT ( 'NONE',  ( 3.028250241984064228, 1.103615759228196325, 1.751372171329562688 ) ) ;
#165778=CARTESIAN_POINT ( 'NONE',  ( 2.883697495508124042, -0.6696099726914479522, -2.198986239785024388 ) ) ;
#165786=CARTESIAN_POINT ( 'NONE',  ( 4.043146078444789460, 0.09904687726844901841, 1.909973672635330910 ) ) ;
#165788=CARTESIAN_POINT ( 'NONE',  ( 5.455954713372185516, 1.722626330383254745, -0.08824682005538657392 ) ) ;
#165789=CARTESIAN_POINT ( 'NONE',  ( 3.942592416894859841, -1.490970858180176162, 1.357867534901323614 ) ) ;
#165790=CARTESIAN_POINT ( 'NONE',  ( 5.590575961319281362, -0.5612465257360791382, 2.229044676911738687 ) ) ;
#165792=CARTESIAN_POINT ( 'NONE',  ( 0.6103625832605160673, -2.195865045534075133, 0.2202409711149767024 ) ) ;
#165794=CARTESIAN_POINT ( 'NONE',  ( 5.606658687911298955, 1.339352548545174937, -1.156898068784556255 ) ) ;
#165796=CARTESIAN_POINT ( 'NONE',  ( 1.781587602986109742, 1.582980622272272653, 1.658122128702421261 ) ) ;
#165797=CARTESIAN_POINT ( 'NONE',  ( 0.2162406733101406298, -0.09061050886127393345, 1.738091409524551878 ) ) ;
#165802=CARTESIAN_POINT ( 'NONE',  ( 0.1687529456618936941, -0.9278834597439933329, -1.960587321289827267 ) ) ;
#165803=CARTESIAN_POINT ( 'NONE',  ( 2.589077643123653072, 1.706113014995232380, 1.074661422923957055 ) ) ;
#165806=CARTESIAN_POINT ( 'NONE',  ( 5.514262516685338511, -0.8683059565382322820, -1.719797162412556535 ) ) ;
#165808=CARTESIAN_POINT ( 'NONE',  ( 2.443850186789862100, -2.070980460497043651, 0.8039724962528942420 ) ) ;
#165815=CARTESIAN_POINT ( 'NONE',  ( 4.563825558218141509, -1.132311722701891510, 1.321849635945840706 ) ) ;
#165816=CARTESIAN_POINT ( 'NONE',  ( 3.930091730393743710, 1.087902980620155891, 1.632394305395828304 ) ) ;
#165821=CARTESIAN_POINT ( 'NONE',  ( 0.5903720789649337108, 1.061967407477812264, -1.768178413720230990 ) ) ;
#165824=CARTESIAN_POINT ( 'NONE',  ( 1.762946358529001056, -1.599227303849257043, 1.600698272852623338 ) ) ;
#165827=CARTESIAN_POINT ( 'NONE',  ( 3.004993591039197831, 1.578202713744047303, 1.003818400984110681 ) ) ;
#165828=CARTESIAN_POINT ( 'NONE',  ( 1.898628203569406203, -0.8177110325628260679, -1.529257715385720307 ) ) ;
#165829=CARTESIAN_POINT ( 'NONE',  ( 5.460537066722415567, -1.980877156148381335, -0.9378266216248376530 ) ) ;
#165830=CARTESIAN_POINT ( 'NONE',  ( 0.1478802723770406002, -1.707511933842900564, -1.397569297917726550 ) ) ;
#165831=CARTESIAN_POINT ( 'NONE',  ( 1.024374290915401442, 1.228313541842564138, -1.654675390109799693 ) ) ;
#165832=CARTESIAN_POINT ( 'NONE',  ( 3.802622829840444751, 1.666041102563616816, 0.9975114776080131751 ) ) ;
#165834=CARTESIAN_POINT ( 'NONE',  ( 5.378141472655761923, -1.040010688794581029, 1.554561134376866383 ) ) ;
#165835=CARTESIAN_POINT ( 'NONE',  ( 0.5937500000000017764, -1.895863743164141191, -0.7852924748299565660 ) ) ;
#165837=CARTESIAN_POINT ( 'NONE',  ( 6.802112138117927920, -1.802125342305498146, 0.9040232568291312054 ) ) ;
#165839=CARTESIAN_POINT ( 'NONE',  ( 4.817029820108094995, 1.034167108704350024, -1.730865207599366240 ) ) ;
#165843=CARTESIAN_POINT ( 'NONE',  ( 2.402731849113007190, 1.466575434288765800, -1.087121784572639527 ) ) ;
#165852=CARTESIAN_POINT ( 'NONE',  ( 6.633471379370169174, -0.1512203817595116073, 1.986116118494333227 ) ) ;
#165853=CARTESIAN_POINT ( 'NONE',  ( 0.5223349339509277822, -2.109880975928311031, 0.2119513895993754005 ) ) ;
#165858=CARTESIAN_POINT ( 'NONE',  ( 6.543830163797104582, 0.7912256320986108538, -1.903158165889913045 ) ) ;
#165859=CARTESIAN_POINT ( 'NONE',  ( 5.098279808040273586, -0.2930726886911337870, 1.994869512123042199 ) ) ;
#165862=CARTESIAN_POINT ( 'NONE',  ( -0.2108831679770959699, 2.036692374882024037, -2.313561348563981657 ) ) ;
#165867=CARTESIAN_POINT ( 'NONE',  ( 5.026720154644213068, 1.994564127574052215, -0.2930270067487000252 ) ) ;
#165868=CARTESIAN_POINT ( 'NONE',  ( 4.769393013670423009, 1.062472638025207416, 1.503447196605799174 ) ) ;
#165869=CARTESIAN_POINT ( 'NONE',  ( -0.02338929933904005179, 0.7691289590099622542, -1.796825425911799723 ) ) ;
#165870=CARTESIAN_POINT ( 'NONE',  ( 3.457953323470845941, 0.5611853863643158080, -2.238310864172543546 ) ) ;
#165872=CARTESIAN_POINT ( 'NONE',  ( 4.991577004318280331, 1.598001195387260154, 1.455802845438579407 ) ) ;
#165874=CARTESIAN_POINT ( 'NONE',  ( 0.5912263705248020917, -0.6977439394254668636, 1.812568619595144925 ) ) ;
#165879=CARTESIAN_POINT ( 'NONE',  ( 3.889402362484274622, 1.354500474538382626, 1.290456140434749654 ) ) ;
#165881=CARTESIAN_POINT ( 'NONE',  ( 1.617294888471169312, 1.591762500684265946, 1.059657513450793953 ) ) ;
#165884=CARTESIAN_POINT ( 'NONE',  ( 2.438337523484556790, 1.039148161723329578, -1.946916322307743474 ) ) ;
#165891=CARTESIAN_POINT ( 'NONE',  ( 0.4386656386161046917, 0.3326637607320662160, 1.942932543480476726 ) ) ;
#165892=CARTESIAN_POINT ( 'NONE',  ( 0.3238087740765641653, -0.1086241252120211664, 2.305164108462977701 ) ) ;
#165893=CARTESIAN_POINT ( 'NONE',  ( 1.398799877119625501, 0.3793605821263335565, 1.924665094374561791 ) ) ;
#165894=CARTESIAN_POINT ( 'NONE',  ( 4.575086232891404592, 1.883663672660494504, 0.8406736911329756312 ) ) ;
#165902=CARTESIAN_POINT ( 'NONE',  ( 0.9015274132509668581, -1.862984440646279438, 1.114554472006025865 ) ) ;
#165904=CARTESIAN_POINT ( 'NONE',  ( 5.935073298327618652, -1.338256116417003927, -1.264887592264056559 ) ) ;
#165907=CARTESIAN_POINT ( 'NONE',  ( 1.721729502718066795, -1.034818790731323990, -1.558030248997283040 ) ) ;
#165908=CARTESIAN_POINT ( 'NONE',  ( 5.184929619776310616, -0.2588774643964042999, -2.145956309214678726 ) ) ;
#165912=CARTESIAN_POINT ( 'NONE',  ( 0.7856316122640573107, 1.842795011522216697, -0.5104879603500325214 ) ) ;
#165913=CARTESIAN_POINT ( 'NONE',  ( 2.992752380588555638, 1.518849080061919654, -0.9082622674112093009 ) ) ;
#165914=CARTESIAN_POINT ( 'NONE',  ( 0.7856316122640573107, 1.842795011522216697, -0.5104879603500325214 ) ) ;
#165916=CARTESIAN_POINT ( 'NONE',  ( 3.972214814312221343, -1.895280843596976350, -0.2773303961090283765 ) ) ;
#165917=CARTESIAN_POINT ( 'NONE',  ( 5.160591359625510854, -0.6618325696593707619, -1.855173450206740071 ) ) ;
#165918=CARTESIAN_POINT ( 'NONE',  ( 1.371502371489873751, -1.821557607348308405, -1.085495857948336251 ) ) ;
#165920=CARTESIAN_POINT ( 'NONE',  ( 3.766346201128992988, -1.256895078192099335, 1.385637336983977397 ) ) ;
#165921=CARTESIAN_POINT ( 'NONE',  ( 0.3459771380207553593, 1.820543102168985961, 0.1377627428671979182 ) ) ;
#165923=CARTESIAN_POINT ( 'NONE',  ( 2.930518499080053907, 1.225513248159842083, -1.835134156090315605 ) ) ;
#165927=CARTESIAN_POINT ( 'NONE',  ( 1.416547059616825699, 0.8341270235591256021, 1.886661834507087798 ) ) ;
#165932=CARTESIAN_POINT ( 'NONE',  ( 6.416268857797894576, -1.911816439625917852, 0.05404522429636184067 ) ) ;
#165934=CARTESIAN_POINT ( 'NONE',  ( 4.527825515032589898, 2.008996319933327612, -0.4998958796476050681 ) ) ;
#165936=CARTESIAN_POINT ( 'NONE',  ( 1.880366631079612771, -1.158069840294423392, 1.825029014904603342 ) ) ;
#165938=CARTESIAN_POINT ( 'NONE',  ( 2.350265711909118593, 0.9499565981557709371, -1.782299418695271198 ) ) ;
#165944=CARTESIAN_POINT ( 'NONE',  ( 0.3566581422463632189, -1.900417414521380133, -0.6748426577906708745 ) ) ;
#165945=CARTESIAN_POINT ( 'NONE',  ( 6.639320575229255894, 7.629137130509070275, 2.703262396134015866 ) ) ;
#165946=CARTESIAN_POINT ( 'NONE',  ( 5.249643141573060667, 2.189086832579402842, -0.1069518675670885766 ) ) ;
#165948=CARTESIAN_POINT ( 'NONE',  ( 3.744317949583543470, 1.018843395500759197, -1.618198357137661469 ) ) ;
#165952=CARTESIAN_POINT ( 'NONE',  ( 2.618767733003044551, 0.2496279305150179983, 2.000855661889962445 ) ) ;
#165954=CARTESIAN_POINT ( 'NONE',  ( 0.4336627441306003528, -1.626622142924066594, -1.615526755278140492 ) ) ;
#165956=CARTESIAN_POINT ( 'NONE',  ( 4.190264469598516506, -1.706116514292443931, -0.2520994348873573654 ) ) ;
#165960=CARTESIAN_POINT ( 'NONE',  ( 0.9593383959572501229, 1.601786533887459507, 1.132500672181527168 ) ) ;
#165963=CARTESIAN_POINT ( 'NONE',  ( 0.1753634416057497925, 7.629137130509101361, -2.744001747789548418 ) ) ;
#165966=CARTESIAN_POINT ( 'NONE',  ( 5.408800935855493819, -0.4461688933581753336, -1.755527745762341718 ) ) ;
#165969=CARTESIAN_POINT ( 'NONE',  ( 6.890000000000050306, -0.002781820520068867264, 1.999840353888074240 ) ) ;
#165970=CARTESIAN_POINT ( 'NONE',  ( 4.793523346383269157, 1.688353701584244915, -0.6568948891843768845 ) ) ;
#165976=CARTESIAN_POINT ( 'NONE',  ( 6.338329682780378782, -0.9945775373912761896, 1.572806762946916903 ) ) ;
#165978=CARTESIAN_POINT ( 'NONE',  ( 3.567908551050925858, -0.9411222629213971125, 1.668380548182837542 ) ) ;
#165984=CARTESIAN_POINT ( 'NONE',  ( 5.401600794869550803, -2.065136407520694828, 0.4665587172485561318 ) ) ;
#165985=CARTESIAN_POINT ( 'NONE',  ( 0.6730137850648570952, -2.035850703004048246, -0.7271551459356735414 ) ) ;
#165989=CARTESIAN_POINT ( 'NONE',  ( 0.8502975112493587062, 0.5252643332615304361, 1.748389446526978031 ) ) ;
#165991=CARTESIAN_POINT ( 'NONE',  ( 4.049673113991675955, 0.6152068410551281286, -1.718917501701062056 ) ) ;
#165993=CARTESIAN_POINT ( 'NONE',  ( 2.425908952446104827, -1.891012092455180760, 0.2844710172774585488 ) ) ;
#165995=CARTESIAN_POINT ( 'NONE',  ( 2.857809274136946520, -0.6206004443085939570, 1.869272957157315007 ) ) ;
#165996=CARTESIAN_POINT ( 'NONE',  ( 5.337426827915986216, 0.7834791095375337466, -1.777179163755914448 ) ) ;
#165999=CARTESIAN_POINT ( 'NONE',  ( 5.642871316567687145, 2.044259226470702462, 0.5637153772257290640 ) ) ;
#166001=CARTESIAN_POINT ( 'NONE',  ( 3.088426618631805454, -1.137173348016347063, 1.537276688398482083 ) ) ;
#166009=CARTESIAN_POINT ( 'NONE',  ( 5.461492464141177727, 0.3521552718798379722, -1.791230276788812414 ) ) ;
#166014=CARTESIAN_POINT ( 'NONE',  ( 5.946149726614579301, 1.868617323842229894, 0.09011704611043556967 ) ) ;
#166024=CARTESIAN_POINT ( 'NONE',  ( 0.6024989291013755910, 2.064475859885641640, 0.1558578049991043990 ) ) ;
#166025=CARTESIAN_POINT ( 'NONE',  ( 1.406030203601447592, -1.179493747730875342, -1.758069577626440116 ) ) ;
#166028=CARTESIAN_POINT ( 'NONE',  ( 6.649288540346695697, 1.804226486660088558, -1.015068834323729297 ) ) ;
#166029=CARTESIAN_POINT ( 'NONE',  ( 2.067674361007607597, -1.131582805410412673, 1.452419944642673100 ) ) ;
#166034=CARTESIAN_POINT ( 'NONE',  ( 1.869451396563295065, 2.192715141705191773, -0.6681815460085840375 ) ) ;
#166036=CARTESIAN_POINT ( 'NONE',  ( 0.2333690889706959148, 4.088440985731725874, -2.608190362703251441 ) ) ;
#166037=CARTESIAN_POINT ( 'NONE',  ( 2.742330423940505302, 1.058908597569432120, -1.592262909973440888 ) ) ;
#166041=CARTESIAN_POINT ( 'NONE',  ( 1.142838885277572825, 1.941394601512283602, 0.5327644489504842484 ) ) ;
#166042=CARTESIAN_POINT ( 'NONE',  ( 1.217545072937670225, 0.3881152535412414339, -1.922811240370206232 ) ) ;
#166046=CARTESIAN_POINT ( 'NONE',  ( 3.468770583794348550, 0.05092928562340763576, -2.090184462658881248 ) ) ;
#166047=CARTESIAN_POINT ( 'NONE',  ( 1.955557038561178240, 1.765385265556310701, -0.1263916157485909797 ) ) ;
#166050=CARTESIAN_POINT ( 'NONE',  ( 4.980587577705724911, -0.2770739538935252932, -2.275404589957805701 ) ) ;
#166051=CARTESIAN_POINT ( 'NONE',  ( 2.870765623479579531, 1.652405209062355773, -0.5463526510798635272 ) ) ;
#166054=CARTESIAN_POINT ( 'NONE',  ( 3.637800481086241433, 0.04416708034036923719, -1.733463101117929339 ) ) ;
#166055=CARTESIAN_POINT ( 'NONE',  ( 3.227178390111482553, -2.005013095889785824, -0.8334813368568798619 ) ) ;
#166057=CARTESIAN_POINT ( 'NONE',  ( 5.911342272548038679, -1.897112096406332382, 0.6839327336411115121 ) ) ;
#166058=CARTESIAN_POINT ( 'NONE',  ( 0.9687500000000008882, 0.7852924748299362490, -1.895863743164110327 ) ) ;
#166060=CARTESIAN_POINT ( 'NONE',  ( 2.450113916266524416, 1.925923877722035105, 0.04935297016485720029 ) ) ;
#166062=B_SPLINE_CURVE_WITH_KNOTS ( 'NONE', 3,
 ( #4146, #89726, #70217, #155774, #104901, #153636, #102752, #57204, #107081, #173102, #88647, #6288, #72362, #55070, #138463, #24683, #37748, #121219, #8435, #168808, #90788, #20413, #56135, #136328, #202347, #169869, #71284, #181340, #74524, #92929, #209829, #190386, #206638, #147796, #111354, #143833, #192516, #165097, #42043, #76643, #110289, #207711, #126555, #59333, #157922, #25754, #32967, #141699, #77712, #193597, #109230, #108156, #15626, #177359, #174182, #75589, #45238, #28973, #191450, #125488, #91866, #158974, #61465, #127631, #95058, #10569, #44169, #161107, #43115, #99043, #81715, #115349, #197586, #175240, #140626, #26825, #176298, #213814, #9516, #142759, #58271, #65433, #208765, #131584, #60391, #27901, #93996, #160037, #11641, #49229, #124428, #69703, #117478, #16689, #148847, #184525, #3625, #53474, #38295, #51355, #166158, #101147, #34024, #135805, #182394, #201829, #134758, #183470, #82773, #119611, #202901, #20946, #200766, #102228, #36146, #18822, #118542, #185596, #149925, #84907, #104373, #66491, #1494, #50286, #150995, #153114, #132632, #85979, #420, #120692, #198638, #35077, #152054, #116405, #100097, #87043, #37225, #103299, #52416, #17745, #83833, #67559, #4687, #133703, #68634, #199708, #167235, #70762, #169360, #2560, #136875, #168298, #19894, #54545, #186668, #126027, #59876, #155253, #190928, #140092, #205040, #139018, #40447, #24157, #142232, #107630, #76128, #42592, #123907, #206118, #8991, #55611, #208244, #10052, #56685, #172576, #75066, #122851, #157398, #73999, #108698, #188813, #121766, #173663, #90260, #57749, #189876, #6834, #5755, #72913, #203964, #156328, #92413, #71833, #25236, #170418, #191989, #22006, #106548, #91339, #137943, #41518, #7910, #141178, #187733, #88117, #207188, #58813, #171494, #174726, #89200, #124967, #26299, #39363, #43655, #158452, #23085, #154187, #105459, #161663, #29521, #13258, #163794, #160578, #146493, #93473, #80398, #27373, #78257, #194139, #177908, #81466, #46855, #15372, #130295, #63079, #193068, #60947, #213564, #176834, #112969, #79330, #111906, #95614, #212512, #145447, #147543, #96682, #12185, #159512, #28448, #94538, #30595, #45788, #178981, #162731, #64153, #211445, #129246, #14303, #144381, #210380, #62022, #128177, #195219, #11111, #196284, #127104, #47931, #114044, #180037, #31659, #97737, #65186, #131340, #197334, #109772, #175779, #77185, #143308, #44720, #110827, #209299, #48976, #171, #148602, #53224, #151806, #119355, #50029, #17497, #116153, #51095, #133447, #19645, #182140, #117221, #136621, #115093, #3379, #70505, #183218, #185342, #164844, #118288, #181090, #152858, #32708, #67306, #184274, #16436, #98789, #36965, #85718, #35898, #166987, #82515, #66238, #34823, #84655, #199453, #100898, #33770, #132387, #103046, #201578, #99849, #69446, #83584, #18577, #150744, #135554, #4436, #198387, #165912, #169101, #2306, #149666, #68382, #1245, #20698, #86789, #200516, #134512, #52161, #101975, #168043, #153932, #92154, #55357, #205862, #107373, #22827, #21752, #140914, #91080, #104115, #203710, #173394, #157140, #105195, #121509, #123655, #72660, #57495, #189617, #8732, #138756, #172315, #41264, #187482, #9796, #24977, #26041, #108445, #39111, #158207, #88942, #40181, #74813, #137689, #154995, #204775, #206927, #171232, #58557, #6581 ),
 .UNSPECIFIED., .F., .F.,
 ( 4, 1, 1, 1, 1, 1, 1, 1, 1, 1, 1, 1, 1, 1, 1, 1, 1, 1, 1, 1, 1, 1, 1, 1, 1, 1, 1, 1, 1, 1, 1, 1, 1, 1, 1, 1, 1, 1, 1, 1, 1, 1, 1, 1, 1, 1, 1, 1, 1, 1, 1, 1, 1, 1, 1, 1, 1, 1, 1, 1, 1, 1, 1, 1, 1, 1, 1, 1, 1, 1, 1, 1, 1, 1, 1, 1, 1, 1, 1, 1, 1, 1, 1, 1, 1, 1, 1, 1, 1, 1, 1, 1, 1, 1, 1, 1, 1, 1, 1, 1, 1, 1, 1, 1, 1, 1, 1, 1, 1, 1, 1, 1, 1, 1, 1, 1, 1, 1, 1, 1, 1, 1, 1, 1, 1, 1, 1, 1, 1, 1, 1, 1, 1, 1, 1, 1, 1, 1, 1, 1, 1, 1, 1, 1, 1, 1, 1, 1, 1, 1, 1, 1, 1, 1, 1, 1, 1, 1, 1, 1, 1, 1, 1, 1, 1, 1, 1, 1, 1, 1, 1, 1, 1, 1, 1, 1, 1, 1, 1, 1, 1, 1, 1, 1, 1, 1, 1, 1, 1, 1, 1, 1, 1, 1, 1, 1, 1, 1, 1, 1, 1, 1, 1, 1, 1, 1, 1, 1, 1, 1, 1, 1, 1, 1, 1, 1, 1, 1, 1, 1, 1, 1, 1, 1, 1, 1, 1, 1, 1, 1, 1, 1, 1, 1, 1, 1, 1, 1, 1, 1, 1, 1, 1, 1, 1, 1, 1, 1, 1, 1, 1, 1, 1, 1, 1, 1, 1, 1, 1, 1, 1, 1, 1, 1, 1, 1, 1, 1, 1, 1, 1, 1, 1, 1, 1, 1, 1, 1, 1, 1, 1, 1, 1, 1, 1, 1, 1, 1, 1, 1, 1, 1, 1, 1, 1, 1, 1, 1, 1, 1, 1, 1, 1, 1, 1, 1, 1, 1, 1, 1, 1, 1, 1, 1, 1, 1, 1, 1, 1, 1, 1, 1, 1, 1, 1, 1, 1, 1, 1, 1, 1, 1, 1, 1, 1, 1, 1, 1, 1, 1, 1, 1, 1, 1, 1, 1, 1, 1, 1, 1, 1, 1, 1, 1, 1, 1, 1, 1, 1, 1, 1, 1, 1, 1, 1, 1, 1, 1, 1, 1, 1, 1, 1, 1, 1, 1, 1, 1, 1, 1, 1, 1, 1, 1, 4 ),
 ( 0.000000000000000000, 0.002600137934918278840, 0.005208846947063642402, 0.007813284371963545236, 0.01041597565644012714, 0.01302123463190214131, 0.01562472912267370319, 0.01822934229245065652, 0.02083335053635077330, 0.02343730581734793095, 0.02604195799539401474, 0.02864545692284610826, 0.03125045498156164142, 0.03385385361191795006, 0.03645873261014952182, 0.03906243010681619693, 0.04166674480109257978, 0.04427107247243720900, 0.04687475664952634596, 0.04947964045798968619, 0.05208303702386667122, 0.05468803228817373241, 0.05729153353077973132, 0.05989618223844375006, 0.06250015876865079589, 0.06510412050499821135, 0.06770877833268285073, 0.07031227041168378045, 0.07291726700687002627, 0.07552066596874357218, 0.07812554330212571896, 0.08072923942118487295, 0.08333355289058355653, 0.08593787945419822938, 0.08854156225015286097, 0.09114644488045960113, 0.09374984019314609729, 0.09635483420994474246, 0.09895833431534489799, 0.1015629817166532611, 0.1041669571688737805, 0.1067709175595765864, 0.1093755742645453749, 0.1119790650618166516, 0.1145840604711090005, 0.1171874582687142119, 0.1197923343547293018, 0.1223960294069747767, 0.1250003415701952669, 0.1276046670722256471, 0.1302083485727723866, 0.1328132300777099817, 0.1354166241949035232, 0.1380216170238739992, 0.1406251160503516617, 0.1432297622036773077, 0.1458337366370238142, 0.1484376957407889386, 0.1510423513813509144, 0.1536458409560605698, 0.1562508352375901466, 0.1588542319300798034, 0.1614591068269417562, 0.1640628008713490293, 0.1666671117869774343, 0.1692714362859856492, 0.1718751165501164191, 0.1744799969878772505, 0.1770833899687347668, 0.1796883816679979429, 0.1822918796746371972, 0.1848965246383280081, 0.1875004981115827030, 0.1901044559872153150, 0.1927091106216977379, 0.1953125990329364348, 0.1979175922448092595, 0.2005209878913200294, 0.2031258616572126918, 0.2057295547527302204, 0.2083338644793258920, 0.2109381880338489224, 0.2135418671205281671, 0.2161467465492790951, 0.2187501384529311477, 0.2213551290805818306, 0.2239586261264417955, 0.2265632699588193688, 0.2291672425307399730, 0.2317711992370185270, 0.2343758529237242316, 0.2369793402305566954, 0.2395843324308542799, 0.2421877270904984059, 0.2447925997835804779, 0.2473962919891333490, 0.2500006005852301039, 0.2526049232537817546, 0.2552086012219486610, 0.2578134796998332035, 0.2604168705853860954, 0.2630218601994954719, 0.2656253563436123954, 0.2682299991029740149, 0.2708339708322964334, 0.2734379264279751531, 0.2760425792251849364, 0.2786460654866522724, 0.2812510567334335909, 0.2838544504653006673, 0.2864593221437078951, 0.2890630135181997962, 0.2916673210423081364, 0.2942716428833813125, 0.2968753197919519748, 0.2994801973770923054, 0.3020835873036303854, 0.3046885759622478540, 0.3072920712636373342, 0.3098967130082584398, 0.3125006839536987324, 0.3151046384975096371, 0.3177092904634842285, 0.3203127757386058927, 0.3229177660899096303, 0.3255211589530693228, 0.3281260296749167193, 0.3307297202772326306, 0.3333340267878420748, 0.3359383478599109463, 0.3385420237677806976, 0.3411469005182800607, 0.3437502895448679152, 0.3463552773060237788, 0.3489587718236830116, 0.3515634126118191150, 0.3541673828320756612, 0.3567713363827305639, 0.3593759875757128741, 0.3619794719234893932, 0.3645844614373360826, 0.3671878534908398217, 0.3697927233142242476, 0.3723964132032320795, 0.3750007187588132451, 0.3776050391203355505, 0.3802087140863810166, 0.3828135900603256703, 0.3854169782460106219, 0.3880219651677176973, 0.3906254589606275029, 0.3932300988505167960, 0.3958340684042725433, 0.3984380210204655492, 0.4010426714986830565, 0.4036461549780977487, 0.4062511437124918245, 0.4088545350153757196, 0.4114594039983773821, 0.4140630932329303349, 0.4166673978919369636, 0.4192717176013560643, 0.4218753916844373286, 0.4244802669398990425, 0.4270836543437129262, 0.4296886404839689866, 0.4322921336110964741, 0.4348967726609613837, 0.4375007416068860122, 0.4401046933472957945, 0.4427093431689624881, 0.4453128258389836835, 0.4479178138519160357, 0.4505212044632024293, 0.4531260726638874359, 0.4557297613028266636, 0.4583340651236982866, 0.4609383842394453867, 0.4635420574984087105, 0.4661469320934465421, 0.4687503187744080368, 0.4713553041911981989, 0.4739587967114984313, 0.4765634349795482838, 0.4791674033763006491, 0.4817713542995921694, 0.4843760035229108252, 0.4869794854424946973, 0.4895844727919445583, 0.4921878627706443576, 0.4947927302470669919, 0.4973964183492232127, 0.5000007213903868708, 0.5026050399708832384, 0.5052087124645624483, 0.5078135864572254077, 0.5104169724743423675, 0.5130219572256408123, 0.5156254491980594157, 0.5182300867424926016, 0.5208340546487225664, 0.5234380048135498509, 0.5260426534967141965, 0.5286461347248060383, 0.5312511214687432037, 0.5338545108738584899, 0.5364593776840630435, 0.5390630653082590928, 0.5416673676281316130, 0.5442716857317909662, 0.5468753575190105076, 0.5494802309673390006, 0.5520836163796108975, 0.5546886005233833128, 0.5572920920068584749, 0.5598967288858642810, 0.5625006963602153798, 0.5651046458252231286, 0.5677092940264200083, 0.5703127746219572858, 0.5729177608183441128, 0.5755211497088699169, 0.5781260159108934094, 0.5807297031159460721, 0.5833340047729366207, 0.5859383224581667937, 0.5885419935977430628, 0.5911468665597719996, 0.5937502514261915332, 0.5963552350203973340, 0.5989587260738620245, 0.6015633623456233536, 0.6041673294467342359, 0.6067712782705607655, 0.6093759260479724160, 0.6119794060698863225, 0.6145843917766802278, 0.6171877802116071399, 0.6197926458634805957, 0.6223963327082033814, 0.6250006337607152407, 0.6276049510859208480, 0.6302086216366651339, 0.6328134941704254279, 0.6354168785499811900, 0.6380218616525755726, 0.6406253523349600965, 0.6432299880576550777, 0.6458339548441623945, 0.6484379030854412473, 0.6510425504972472410, 0.6536460300044655281, 0.6562510152796211527, 0.6588544033179367654, 0.6614592684776883225, 0.6640629550208935195, 0.6666672555273263079, 0.6692715725509107427, 0.6718752425716313370, 0.6744801147351520143, 0.6770834986868305982, 0.6796884813557668714, 0.6822919717260003125, 0.6848966069578048543, 0.6875005734883452568, 0.6901045212057073108, 0.6927091683100871089, 0.6953126473615357517, 0.6979176322630067375, 0.7005210199636988655, 0.7031258846893556624, 0.7057295709898557812, 0.7083338710086078960, 0.7109381877889758838, 0.7135418573384794128, 0.7161467291897904985, 0.7187501127725786088, 0.7213550950658099703, 0.7239585851828231888, 0.7265632199819130888, 0.7291671863151253374, 0.7317711335672014705, 0.7343757804223364216, 0.7369792590769420615, 0.7395842436626837157, 0.7421876310847422831, 0.7447924954343322357, 0.7473961815509432283, 0.7500004811404139549, 0.7526047977359727748, 0.7552084668730677519, 0.7578133384702019359, 0.7604167217430886083, 0.7630217037185706985, 0.7656251936412983294, 0.7682298280658512724, 0.7708337942603785686, 0.7734377411058018792, 0.7760423877698768846, 0.7786458660865690495, 0.7812508504145402322, 0.7838542376169586046, 0.7864591016485131814, 0.7890627876400562180, 0.7916670868586475063, 0.7942714033278103214, 0.7968750721113085911, 0.7994799435123028930, 0.8020833265342820484, 0.8046883082499752815, 0.8072917980373575109, 0.8098964321455554005, 0.8125003982600473851, 0.8151043447574546352, 0.8177089912886614798, 0.8203124693263749156, 0.8229174534545398156, 0.8255208404963184643, 0.8281257042678743518, 0.8307293901931780411, 0.8333336890992975032, 0.8359380055004849153, 0.8385416739892034288, 0.8411465452521027508, 0.8437499280821748604, 0.8463549095960458679, 0.8489583993070312085, 0.8515630331570626099, 0.8541669992501779163, 0.8567709454582125295, 0.8593755919147509914, 0.8619790697324273276, 0.8645840537187589048, 0.8671874406589066275, 0.8697923042285079509, 0.8723959901464106714, 0.8750002887984731359, 0.8776046051901155165, 0.8802082734428797739, 0.8828131446257380111, 0.8854165273229123168, 0.8880215086929368340, 0.8906249983864840125, 0.8932296320365455955, 0.8958335981669537373, 0.8984375441442679078, 0.9010421905843485346, 0.9036456682409392815, 0.9062506521434200435, 0.9088540390409564074, 0.9114589024666573946, 0.9140625884360091824, 0.9166668868924389146, 0.9192712033329777377, 0.9218748714086243412, 0.9244797425695093773, 0.9270831251927963423, 0.9296881064769593195, 0.9322915962120889022, 0.9348962297203436966, 0.9375001959466012780, 0.9401041417521586174, 0.9427087882339971747, 0.9453122657876905643, 0.9479172496658602176, 0.9505206365780075606, 0.9531254999124115779, 0.9557291860198475764, 0.9583334843266348990, 0.9609378007344983041, 0.9635414689593263526, 0.9661463405142474148, 0.9687497214891268582, 0.9713547029754164841, 0.9739581985331400293, 0.9765628250748574768, 0.9791667834374845336, 0.9817707607320566021, 0.9843753697534296521, 0.9869788348889786400, 0.9895840831931937975, 0.9921867700316038263, 0.9947911815772807476, 0.9973998924267860611, 1.000000000000000000 ),
 .UNSPECIFIED. ) ;
#166063=CARTESIAN_POINT ( 'NONE',  ( 5.431947826915617838, -2.167270271666811077, 0.4867340719418070671 ) ) ;
#166064=ORIENTED_EDGE ( 'NONE', *, *, #207763, .F. ) ;
#166065=CARTESIAN_POINT ( 'NONE',  ( -0.2108831679771167866, 1.375689764684871808, -2.152500126786048185 ) ) ;
#166075=CARTESIAN_POINT ( 'NONE',  ( 4.879373355499653897, -0.1046096447297485965, 2.060157192773376611 ) ) ;
#166079=CARTESIAN_POINT ( 'NONE',  ( 5.747288119592351308, -1.474170506619469023, -1.151262835514428540 ) ) ;
#166080=CARTESIAN_POINT ( 'NONE',  ( 4.887242738553729815, -0.5912784195612891258, -1.630374673469140223 ) ) ;
#166081=CARTESIAN_POINT ( 'NONE',  ( 4.405614404729386813, -0.7493292006620960732, -1.571029527175720863 ) ) ;
#166083=CARTESIAN_POINT ( 'NONE',  ( 1.734309787148346382, 2.268178062924830041, 0.3313793973579847729 ) ) ;
#166085=CARTESIAN_POINT ( 'NONE',  ( 5.179275120254928311, 1.405169897584326089, 1.548284651509527210 ) ) ;
#166086=CARTESIAN_POINT ( 'NONE',  ( 6.298774621056003831, 1.615917059943820622, 1.076740554856120413 ) ) ;
#166088=CARTESIAN_POINT ( 'NONE',  ( 1.108046318188542489, -0.04667474159409169127, 2.016033875899234662 ) ) ;
#166089=CARTESIAN_POINT ( 'NONE',  ( 0.2522424171345696298, 0.8426718423822797677, 2.023156535103701970 ) ) ;
#166094=CARTESIAN_POINT ( 'NONE',  ( 3.615986862044855421, -0.6139777315949942471, 2.029667854546577388 ) ) ;
#166096=CARTESIAN_POINT ( 'NONE',  ( 5.848246728868278232, 1.823843535133644389, 0.08496628090458313576 ) ) ;
#166104=CARTESIAN_POINT ( 'NONE',  ( 3.094014924146833323, 1.284692261361711774, 1.558518293110554565 ) ) ;
#166105=CARTESIAN_POINT ( 'NONE',  ( 6.739307351729481255, -1.974284904759715298, 0.9861035376414882814 ) ) ;
#166107=CARTESIAN_POINT ( 'NONE',  ( 3.678407310798579299, 1.183884816018574426, -1.435758196845798418 ) ) ;
#166113=CARTESIAN_POINT ( 'NONE',  ( 0.07536363704235826688, -0.001874865094115066300, -2.144269471569634877 ) ) ;
#166117=CARTESIAN_POINT ( 'NONE',  ( 1.229404279783296694, -1.564619330878062931, -0.7474530596254543857 ) ) ;
#166118=CARTESIAN_POINT ( 'NONE',  ( 0.8315134001313486678, 1.713846476070936653, 0.3014184826048373900 ) ) ;
#166119=CARTESIAN_POINT ( 'NONE',  ( 6.322925365441865786, 2.150718969097795696, 0.8370602354567517889 ) ) ;
#166122=CARTESIAN_POINT ( 'NONE',  ( 1.897801681018367548, -0.6972820500400818133, 1.939346266731331259 ) ) ;
#166124=CARTESIAN_POINT ( 'NONE',  ( 6.380222486609858912, -0.2913964880489598452, 2.279815279960105467 ) ) ;
#166126=CARTESIAN_POINT ( 'NONE',  ( 6.332864056472936376, 0.1854757364097951722, 1.861418627818342664 ) ) ;
#166127=CARTESIAN_POINT ( 'NONE',  ( 5.185773951807310489, 1.841398108398510480, -0.5159224025059682139 ) ) ;
#166129=CARTESIAN_POINT ( 'NONE',  ( 6.358075476802443227, 2.201304964888863402, -0.1578768562689457922 ) ) ;
#166132=CARTESIAN_POINT ( 'NONE',  ( 6.633471380297788045, -0.1541069161683609745, 2.086224335282916620 ) ) ;
#166134=CARTESIAN_POINT ( 'NONE',  ( 2.960362034815271048, 2.296572897674476810, -0.2250602657276803420 ) ) ;
#166135=CARTESIAN_POINT ( 'NONE',  ( 4.633228507203630997, 0.002057781214020309134, -1.962046631861932067 ) ) ;
#166136=CARTESIAN_POINT ( 'NONE',  ( 2.237090426018002454, -0.09115598566783281176, -1.959741687340323946 ) ) ;
#166140=CARTESIAN_POINT ( 'NONE',  ( -0.1880716927101276914, -1.308626981353334662, -1.665352682907685233 ) ) ;
#166143=CARTESIAN_POINT ( 'NONE',  ( 0.04061758243546764735, -1.421021341975825969, -1.170429047309962112 ) ) ;
#166144=CARTESIAN_POINT ( 'NONE',  ( 3.995131740874768411, 0.3131294011963717816, 2.148239739743092347 ) ) ;
#166146=CARTESIAN_POINT ( 'NONE',  ( 2.267978396857213585, 0.5610993688725562922, -2.044979925899123252 ) ) ;
#166151=CARTESIAN_POINT ( 'NONE',  ( 2.038423305949757847, 2.037923218716758633, 0.3053300769366319445 ) ) ;
#166155=CARTESIAN_POINT ( 'NONE',  ( 0.07775346131141079586, 1.298946786380944074, -2.537735853881052162 ) ) ;
#166158=CARTESIAN_POINT ( 'NONE',  ( 4.899028947338643469, -0.2378672112019978024, -1.897373119303269018 ) ) ;
#166160=CARTESIAN_POINT ( 'NONE',  ( 1.159873712335700802, 0.4409813497070895760, -2.218855480106549649 ) ) ;
#166162=CARTESIAN_POINT ( 'NONE',  ( 0.8085208021518180965, -0.4412475195509023562, -1.756857618417038358 ) ) ;
#166163=CARTESIAN_POINT ( 'NONE',  ( 1.833070758936614864, -1.541008679516321589, -1.137915016233618015 ) ) ;
#166164=CARTESIAN_POINT ( 'NONE',  ( 2.822784111170244525, -1.429543836668966561, 1.497820115680066344 ) ) ;
#166166=CARTESIAN_POINT ( 'NONE',  ( 0.5671783758751040017, 0.1957704533250003986, -1.961731083161978306 ) ) ;
#166167=CARTESIAN_POINT ( 'NONE',  ( 5.004483369110711344, -0.6506757832731756563, -1.813419023564779353 ) ) ;
#166169=CARTESIAN_POINT ( 'NONE',  ( 6.516270054225981490, -1.036149114087565382, -1.948532232987249424 ) ) ;
#166172=CARTESIAN_POINT ( 'NONE',  ( 5.160619382589332282, -0.6916465251813638249, -1.943403241031741002 ) ) ;
#166176=( BOUNDED_SURFACE ( )  B_SPLINE_SURFACE ( 3, 3, ( 
 ( #62607, #127718, #129840, #96212, #162263, #29060, #112501, #163328, #63684, #95143 ),
 ( #11723, #47461, #146033, #81002, #44256, #93015, #147090, #110377, #60479, #64745 ),
 ( #192603, #191537, #194745, #79926, #12781, #178511, #94084, #159058, #10654, #78854 ),
 ( #27988, #143918, #144975, #134849, #5854, #104467, #103390, #187826, #22096, #169451 ),
 ( #71926, #86070, #39452, #151090, #204049, #89291, #105547, #2654, #180632, #38385 ),
 ( #152146, #88209, #171582, #53570, #32254, #170514, #154280, #3713, #69790, #68728 ),
 ( #138036, #6924, #52502, #55699, #121855, #135898, #185686, #36237, #201916, #37315 ) ),
 .UNSPECIFIED., .T., .F., .T. ) 
 B_SPLINE_SURFACE_WITH_KNOTS ( ( 4, 3, 4 ),
 ( 4, 1, 1, 1, 1, 1, 1, 4 ),
 ( 0.000000000000000000, 0.5000000000000000000, 1.000000000000000000 ),
 ( 0.000000000000000000, 0.09884949474608377418, 0.1930937302289311708, 0.2616037862002966730, 0.3630310524065313849, 0.5216543902990324888, 0.7338513509102306820, 0.9999999999999998890 ),
 .UNSPECIFIED. ) 
 GEOMETRIC_REPRESENTATION_ITEM ( )  RATIONAL_B_SPLINE_SURFACE ( (
 ( 1.000000000000000222, 1.000000000000000222, 1.000000000000000000, 1.000000000000000222, 1.000000000000000444, 1.000000000000000222, 1.000000000000000222, 1.000000000000000222, 1.000000000000000222, 1.000000000000000222),
 ( 0.3333333333333334259, 0.3333333333333334259, 0.3333333333333334814, 0.3333333333333333703, 0.3333333333333334814, 0.3333333333333333703, 0.3333333333333334814, 0.3333333333333333703, 0.3333333333333334259, 0.3333333333333334259),
 ( 0.3333333333333334259, 0.3333333333333334259, 0.3333333333333334814, 0.3333333333333333703, 0.3333333333333334814, 0.3333333333333333703, 0.3333333333333334814, 0.3333333333333333703, 0.3333333333333334259, 0.3333333333333334259),
 ( 1.000000000000000222, 1.000000000000000222, 1.000000000000000000, 1.000000000000000222, 1.000000000000000444, 1.000000000000000222, 1.000000000000000222, 1.000000000000000222, 1.000000000000000222, 1.000000000000000222),
 ( 0.3333333333333334259, 0.3333333333333334259, 0.3333333333333334814, 0.3333333333333333703, 0.3333333333333334814, 0.3333333333333333703, 0.3333333333333334814, 0.3333333333333333703, 0.3333333333333334259, 0.3333333333333334259),
 ( 0.3333333333333334259, 0.3333333333333334259, 0.3333333333333334814, 0.3333333333333333703, 0.3333333333333334814, 0.3333333333333333703, 0.3333333333333334814, 0.3333333333333333703, 0.3333333333333334259, 0.3333333333333334259),
 ( 1.000000000000000222, 1.000000000000000222, 1.000000000000000000, 1.000000000000000222, 1.000000000000000444, 1.000000000000000222, 1.000000000000000222, 1.000000000000000222, 1.000000000000000222, 1.000000000000000222) ) ) 
 REPRESENTATION_ITEM ( '' )  SURFACE ( )  );
#166177=CARTESIAN_POINT ( 'NONE',  ( 4.823321527849568469, -0.1059641466341002675, 2.103426968240690087 ) ) ;
#166179=CARTESIAN_POINT ( 'NONE',  ( 1.328853926488116510, -1.377647258212051362, 1.678094904287985800 ) ) ;
#166181=CARTESIAN_POINT ( 'NONE',  ( 5.184929619776310616, -0.2588774643964043554, -2.145956309214678726 ) ) ;
#166182=CARTESIAN_POINT ( 'NONE',  ( 5.338538087541965460, 1.201400599988803108, -1.623342581396812090 ) ) ;
#166183=CARTESIAN_POINT ( 'NONE',  ( -0.1399997263889820043, 5.722209607272843002, -2.594334538518060729 ) ) ;
#166188=CARTESIAN_POINT ( 'NONE',  ( 3.678922940808615483, 1.700962499606586853, -1.082838980105811366 ) ) ;
#166192=CARTESIAN_POINT ( 'NONE',  ( 4.803692121107413726, -0.5798474923815257753, 2.082409481564663434 ) ) ;
#166196=CARTESIAN_POINT ( 'NONE',  ( 5.905875104417894761, -1.122515283938491537, -1.674877678029200068 ) ) ;
#166199=CARTESIAN_POINT ( 'NONE',  ( 0.8028309281867166414, 1.407482529003287075, 0.9968052580264019635 ) ) ;
#166205=CARTESIAN_POINT ( 'NONE',  ( 6.151601556293980977, 0.5431611868166182910, -1.789914130245950696 ) ) ;
#166206=CARTESIAN_POINT ( 'NONE',  ( 5.888937080504050847, -1.913070152547487579, -0.6273127349021755395 ) ) ;
#166211=CARTESIAN_POINT ( 'NONE',  ( 1.893382502257603850, -0.1070854039621378373, -2.117916637519041689 ) ) ;
#166212=CARTESIAN_POINT ( 'NONE',  ( 1.669546221992053603, 1.392560760841387246, 1.458543886677300394 ) ) ;
#166213=CARTESIAN_POINT ( 'NONE',  ( 2.619172825086816037, 1.532478635541080214, 0.9657477217557136617 ) ) ;
#166216=CARTESIAN_POINT ( 'NONE',  ( 6.069229152942409833, 0.1638285306290177823, -2.155560115052157055 ) ) ;
#166221=CARTESIAN_POINT ( 'NONE',  ( 0.1103573706816539240, 1.834011727325855379, 0.5536052920952787559 ) ) ;
#166229=CARTESIAN_POINT ( 'NONE',  ( 4.170900312159072421, -2.016029151617684256, -0.7805680927704603533 ) ) ;
#166233=CARTESIAN_POINT ( 'NONE',  ( 1.969135536805465492, -1.636093909763213228, 1.349083368969570262 ) ) ;
#166235=CARTESIAN_POINT ( 'NONE',  ( 3.708241208800214572, -0.7959428688352770953, -1.803694655455597262 ) ) ;
#166236=CARTESIAN_POINT ( 'NONE',  ( 5.449440537890920311, -1.726199344983204265, 0.8234401749890255529 ) ) ;
#166239=CARTESIAN_POINT ( 'NONE',  ( 6.004353349036935406, 1.967244357045078607, 0.09818725807526038074 ) ) ;
#166240=CARTESIAN_POINT ( 'NONE',  ( 1.042798325077255450, -1.530655164913260702, -1.195007349728629764 ) ) ;
#166248=CARTESIAN_POINT ( 'NONE',  ( 5.971340724440283410, -1.642497693792897451, -0.9790476769208908969 ) ) ;
#166250=CARTESIAN_POINT ( 'NONE',  ( 2.772332522587173997, 1.181257105606844160, 1.863944272329665086 ) ) ;
#166251=CARTESIAN_POINT ( 'NONE',  ( 2.169229845753062325, -2.017539712319418310, -0.8944986170207609444 ) ) ;
#166253=CARTESIAN_POINT ( 'NONE',  ( 0.6625817696367036769, 0.5554855734208345996, 1.829800363923417716 ) ) ;
#166257=CARTESIAN_POINT ( 'NONE',  ( 2.787621587699981696, -1.932700977737045633, 0.7428295258242523236 ) ) ;
#166260=CARTESIAN_POINT ( 'NONE',  ( 2.184651956524386041, -2.119909832212972578, -0.4221607449544013679 ) ) ;
#166261=CARTESIAN_POINT ( 'NONE',  ( 3.667680160636753506, 1.218766932906123479, 1.821211977396507198 ) ) ;
#166267=CARTESIAN_POINT ( 'NONE',  ( 6.170542255345159433, 1.203217383492904746, 1.249094692781686611 ) ) ;
#166269=CARTESIAN_POINT ( 'NONE',  ( 3.010663864534826928, 0.6931938328994196041, 1.950912564768356727 ) ) ;
#166270=CARTESIAN_POINT ( 'NONE',  ( 5.150072296613558365, 1.044590698784592542, 1.841551053096659230 ) ) ;
#166274=CARTESIAN_POINT ( 'NONE',  ( 2.905082208348725548, -1.640047651136176565, 1.090064613274278837 ) ) ;
#166275=CARTESIAN_POINT ( 'NONE',  ( 1.388764059443419407, -1.816923020173771830, -0.5969786173363604842 ) ) ;
#166276=CARTESIAN_POINT ( 'NONE',  ( 5.402359069383361856, 1.738778441700383315, -1.493778605308769603 ) ) ;
#166277=CARTESIAN_POINT ( 'NONE',  ( 2.877373901574116211, 1.733520850877915187, -0.5729475677913041798 ) ) ;
#166285=CARTESIAN_POINT ( 'NONE',  ( 3.586193004068451540, 1.121915001286919233, 1.671427700405977212 ) ) ;
#166286=CARTESIAN_POINT ( 'NONE',  ( 3.854310441289869882, -1.959320932037407426, -0.1006921081871253454 ) ) ;
#166289=CARTESIAN_POINT ( 'NONE',  ( 0.1755611466353291517, 7.629137130509040077, -2.844001552353003781 ) ) ;
#166290=CARTESIAN_POINT ( 'NONE',  ( -0.09403702165171158589, -0.8981432076055823055, -1.886421477387869361 ) ) ;
#166291=CARTESIAN_POINT ( 'NONE',  ( 5.278098682986631651, -0.9809853834585824384, 1.472868624863521880 ) ) ;
#166293=CARTESIAN_POINT ( 'NONE',  ( 1.728746526384251858, 0.2170652002222578369, 2.180672313318913869 ) ) ;
#166294=CARTESIAN_POINT ( 'NONE',  ( 6.667905886031927132, -1.063982290101581185, 1.377602455597818132 ) ) ;
#166296=CARTESIAN_POINT ( 'NONE',  ( 0.6270765232691848379, -1.639361371195736439, 0.5365680580288884061 ) ) ;
#166297=CARTESIAN_POINT ( 'NONE',  ( 1.036931080102401426, 2.214701571188535834, -0.6144361423649072895 ) ) ;
#166298=CARTESIAN_POINT ( 'NONE',  ( 1.048660896456204528, -1.724490848714568259, 1.352309724062021878 ) ) ;
#166299=CARTESIAN_POINT ( 'NONE',  ( 6.643864291637132879, -0.08952462543848457854, -1.731637005886511593 ) ) ;
#166300=CARTESIAN_POINT ( 'NONE',  ( 3.088704478669739295, -2.174299887604825177, -0.3769171259565203269 ) ) ;
#166302=CARTESIAN_POINT ( 'NONE',  ( 6.830535128024421532, -1.341686296255087063, 1.707861204732928018 ) ) ;
#166304=CARTESIAN_POINT ( 'NONE',  ( 1.763061546204633290, -0.1096309319212440264, -2.114649557665876145 ) ) ;
#166306=CARTESIAN_POINT ( 'NONE',  ( 5.456054696845579421, 1.924170334762603574, -0.09472988109167354565 ) ) ;
#166308=CARTESIAN_POINT ( 'NONE',  ( 2.525266882823226311, -2.137704731703232053, 0.8281840208047249741 ) ) ;
#166312=CARTESIAN_POINT ( 'NONE',  ( 4.899211331842913353, -0.2710981195956448375, -2.204650271698949116 ) ) ;
#166320=CARTESIAN_POINT ( 'NONE',  ( 2.531875153343257523, -1.674887184936912909, 1.122499117612890673 ) ) ;
#166322=CARTESIAN_POINT ( 'NONE',  ( 1.305618366820593179, -1.623578218988607658, -1.271935013979957452 ) ) ;
#166326=CARTESIAN_POINT ( 'NONE',  ( 3.609492757825348175, -2.159078094573213757, 0.3743817768235499499 ) ) ;
#166327=CARTESIAN_POINT ( 'NONE',  ( 1.529922885524274134, -1.701946718671920600, 1.081067414773040802 ) ) ;
#166328=CARTESIAN_POINT ( 'NONE',  ( 0.9602180038516641147, -1.664555262390180257, -0.7873027242753791732 ) ) ;
#166329=CARTESIAN_POINT ( 'NONE',  ( 5.073898020828643496, -1.275178753180395530, 1.904781575909524349 ) ) ;
#166330=CARTESIAN_POINT ( 'NONE',  ( 4.558453444723221892, -1.645810703501834560, -0.8254300276653583346 ) ) ;
#166332=CARTESIAN_POINT ( 'NONE',  ( 4.119992258926360229, -0.9384382104282267267, -1.565754920925747973 ) ) ;
#166333=CARTESIAN_POINT ( 'NONE',  ( 4.430314669760617718, -1.560499787156752971, -1.277043788614096176 ) ) ;
#166335=CARTESIAN_POINT ( 'NONE',  ( 4.575235619729528302, 0.004297453766812646056, -2.262689076577176106 ) ) ;
#166337=CARTESIAN_POINT ( 'NONE',  ( 6.545935606868724221, 0.8096169477174266493, -1.944322875993751421 ) ) ;
#166339=CARTESIAN_POINT ( 'NONE',  ( 4.756339170418532269, -2.069830778647030023, -0.05414847147890837487 ) ) ;
#166344=CARTESIAN_POINT ( 'NONE',  ( 2.350114058346234547, 1.926077408352431464, 0.04734757869597795016 ) ) ;
#166346=CARTESIAN_POINT ( 'NONE',  ( 0.2034765232073352526, -1.520001300341488948, -1.252246736068510335 ) ) ;
#166350=CARTESIAN_POINT ( 'NONE',  ( 1.178162429063234207, 2.088287186665960693, -0.3679680078583212333 ) ) ;
#166351=CARTESIAN_POINT ( 'NONE',  ( 1.160717840558170622, 2.219164385786871030, 0.1022553982447590853 ) ) ;
#166352=CARTESIAN_POINT ( 'NONE',  ( 3.417109911095609132, 1.903178947333901583, 0.9019662245143298396 ) ) ;
#166356=CARTESIAN_POINT ( 'NONE',  ( 3.437899435096212208, 1.242623406730450908, 1.518177208742684803 ) ) ;
#166362=CARTESIAN_POINT ( 'NONE',  ( 1.371502371489873751, -1.821557607348308405, -1.085495857948336251 ) ) ;
#166365=CARTESIAN_POINT ( 'NONE',  ( 4.967221142815226642, 1.706001049663580460, 0.9686458024478412643 ) ) ;
#166366=CARTESIAN_POINT ( 'NONE',  ( 3.678741886385179072, -2.082744454470350615, -0.5786317199799119182 ) ) ;
#166367=CARTESIAN_POINT ( 'NONE',  ( 2.067674361007607597, -1.131582805410412673, 1.452419944642673100 ) ) ;
#166369=FACE_OUTER_BOUND ( 'NONE', #208395, .T. ) ;
#166370=CARTESIAN_POINT ( 'NONE',  ( 4.874825007975835511, 1.622202256106145102, -0.6307315249329782381 ) ) ;
#166375=CARTESIAN_POINT ( 'NONE',  ( 1.674925575805393585, -2.052671086741376882, -0.6780288057936025847 ) ) ;
#166376=CARTESIAN_POINT ( 'NONE',  ( 4.745470142856022200, -1.954873481938533608, -0.4925652823710227612 ) ) ;
#166378=CARTESIAN_POINT ( 'NONE',  ( 1.446389902895691693, 2.159248346720197276, 0.1057134262518744372 ) ) ;
#166379=CARTESIAN_POINT ( 'NONE',  ( 3.924654207020538355, 1.871676352785199393, 0.6194476946735865130 ) ) ;
#166381=CARTESIAN_POINT ( 'NONE',  ( 3.245582950214185303, 1.942234966672530261, -0.002794291004394599230 ) ) ;
#166391=CARTESIAN_POINT ( 'NONE',  ( 6.335062919620514599, 0.2175189359726207861, 2.297324976709664845 ) ) ;
#166393=CARTESIAN_POINT ( 'NONE',  ( 5.752778578519474273, -0.4731148833870613690, -1.903749215227706015 ) ) ;
#166394=CARTESIAN_POINT ( 'NONE',  ( 1.406875202279284753, -1.122500148236497575, -1.674886495921081853 ) ) ;
#166396=CARTESIAN_POINT ( 'NONE',  ( 3.995394017595743641, -0.3581701549109669869, 2.086669383214428297 ) ) ;
#166400=CARTESIAN_POINT ( 'NONE',  ( 4.031074566243696644, -1.271087849624694233, -1.332192834049110486 ) ) ;
#166403=CARTESIAN_POINT ( 'NONE',  ( 4.711248855110969913, 1.761570823303935551, -1.180294879073326308 ) ) ;
#166406=CARTESIAN_POINT ( 'NONE',  ( 5.659468487958158711, 0.4062720387869744876, -2.020156115232510707 ) ) ;
#166407=CARTESIAN_POINT ( 'NONE',  ( 1.152544200391303786, -0.4473333697519957242, -1.806370492606963474 ) ) ;
#166408=CARTESIAN_POINT ( 'NONE',  ( 2.770863647982471534, 1.747605724785822767, -0.5798694457997202178 ) ) ;
#166411=CARTESIAN_POINT ( 'NONE',  ( 3.015880874418576330, 1.852360388558017545, -0.1794404841957262797 ) ) ;
#166415=CARTESIAN_POINT ( 'NONE',  ( 1.998912159191484905, -0.5904864226158462737, -2.126349760018491963 ) ) ;
#166416=CARTESIAN_POINT ( 'NONE',  ( 4.956464464747484477, 0.8595337117903809609, 2.092967149517725112 ) ) ;
#166417=CARTESIAN_POINT ( 'NONE',  ( 3.591030000661588062, 1.731995077137841843, 1.032480907900306111 ) ) ;
#166420=CARTESIAN_POINT ( 'NONE',  ( 4.341949102618557710, -1.119799544600053265, -1.423922225892548354 ) ) ;
#166421=CARTESIAN_POINT ( 'NONE',  ( 5.665228803577522676, 1.767359255132592066, -0.7397141715129780248 ) ) ;
#166424=CARTESIAN_POINT ( 'NONE',  ( 3.766447953776773883, -1.324889289065459774, 1.460063511008972137 ) ) ;
#166425=CARTESIAN_POINT ( 'NONE',  ( 4.504681594071535677, 1.446009304718363087, -1.186774495104812699 ) ) ;
#166427=CARTESIAN_POINT ( 'NONE',  ( 5.090230039108806892, 0.9569469540476289726, -1.596034515973473455 ) ) ;
#166429=CARTESIAN_POINT ( 'NONE',  ( 4.768267862989370443, -1.154894395163852616, 1.341171105668465646 ) ) ;
#166430=CARTESIAN_POINT ( 'NONE',  ( 0.5148617154710420918, 0.1531739628206352510, 2.010800830040265996 ) ) ;
#166432=CARTESIAN_POINT ( 'NONE',  ( 1.910898437428062646, 1.559696066972179107, -1.415416642437119954 ) ) ;
#166436=CARTESIAN_POINT ( 'NONE',  ( 3.287459871768631636, 0.04819156399121089784, -2.120204644799832394 ) ) ;
#166438=CARTESIAN_POINT ( 'NONE',  ( 2.390883991616198578, -1.934022345091526818, -0.5824046739145176677 ) ) ;
#166440=CARTESIAN_POINT ( 'NONE',  ( 6.933263157960367629, 7.629137130509066722, 2.653810918356712900 ) ) ;
#166443=CARTESIAN_POINT ( 'NONE',  ( 2.249508738127777630, -1.734628566516350778, -1.289557925820798090 ) ) ;
#166444=CARTESIAN_POINT ( 'NONE',  ( 6.890000000000009450, 0.5473178204696281801, 2.329866691457019190 ) ) ;
#166453=CARTESIAN_POINT ( 'NONE',  ( 0.4686481397476391364, -2.065551408369214137, -0.7328327568804984260 ) ) ;
#166455=CARTESIAN_POINT ( 'NONE',  ( 1.429016818436980474, 2.180957219565873295, 0.6017249355739097139 ) ) ;
#166462=CARTESIAN_POINT ( 'NONE',  ( 3.602599932655100812, 1.396742099285839256, -1.086680525292152977 ) ) ;
#166463=CARTESIAN_POINT ( 'NONE',  ( 6.668967514498191029, -2.014860697535350020, -0.9005387006749266954 ) ) ;
#166466=CARTESIAN_POINT ( 'NONE',  ( 4.886342304379578394, -0.6820123065829877262, -1.897693145932321634 ) ) ;
#166468=CARTESIAN_POINT ( 'NONE',  ( 2.026040307571222332, 1.079255042350239391, -1.527726335390042545 ) ) ;
#166469=CARTESIAN_POINT ( 'NONE',  ( 2.500909639826456754, 0.4493149015136475022, 2.020762751476639529 ) ) ;
#166472=CARTESIAN_POINT ( 'NONE',  ( 2.091926199050548441, 1.179367891222588005, 1.505316542580182659 ) ) ;
#166476=B_SPLINE_CURVE_WITH_KNOTS ( 'NONE', 3,
 ( #137255, #53856, #203274, #85277, #52776, #184895, #69005, #182768, #132997, #198998, #165457, #84210, #151363, #149211, #87425, #34385, #201138, #134070, #50644, #86350, #100457, #168661, #119989, #115701, #183841, #71137, #135122, #167600, #118914, #2933, #117849, #166532, #181693, #18122, #150298, #66853, #19199, #1864, #21318, #200079, #116771, #786, #36520, #185966, #37598, #67925, #33323, #102607, #20266, #17052, #152421, #4000, #136182, #202200, #169729, #153492, #5062, #121072, #90643, #188108, #175093, #140480, #73283, #72208, #25608, #39738, #206492, #174036, #24535, #91720, #88499, #6138, #41898, #204330, #138315, #55989, #122140, #189186, #157771, #191301, #74378, #172956, #155625, #26681, #139387, #105843, #9370, #142607, #171870, #59181, #23466, #92783, #89576, #123222, #40823, #7210, #156703, #58122, #205420, #76496, #57057, #10424, #42969, #125338, #106932, #8294, #124281, #75441, #158828, #54921, #190240, #109077, #108009, #187040, #141553, #38672, #104751, #207560, #170800, #22389, #154561, #14683, #78628, #12553, #112275, #176156, #80780, #15747, #94914, #144752, #180406, #28826, #128548, #44025, #163103, #194514, #79700, #60249, #210764, #113348, #196655, #62384, #47231, #178290, #97050, #110143, #208616, #160963, #32025, #179353, #30975, #46162, #63457, #130666, #146868, #29898, #212889, #95984, #64520, #48295, #114407, #27756, #164162, #61326, #126406, #127486, #98110, #192366, #93851, #159889, #81832, #162036, #13627, #193457, #11496, #45101, #111210, #77568, #145813, #211820, #143690, #209682, #177213, #129611, #195596, #152170, #3739, #116520, #147915, #86094, #83951, #135920, #150042, #1613, #181456, #134874, #65553, #37342, #103416, #69814, #201939, #131698, #53595, #52526, #151114, #49346, #67672, #167353, #133816, #51471, #99161, #18940, #119729, #2680, #148965, #213931, #185708, #199830, #168413, #17868, #166277, #200881, #35194, #102341, #117595, #183586, #197704, #169476, #82889, #36263, #115465, #101269, #21061, #33086, #182511, #184644, #165214, #85025, #68752, #118660, #20010, #16804, #537, #66604, #132750, #198753, #50400, #34141, #100210, #56798, #38412, #9114, #186786, #153229, #54661, #40564, #41643, #39477, #5877, #70879, #57864, #87158, #154303, #191050, #136992, #4799, #120809, #108823, #25358, #174848, #122967, #24273, #156448, #106671, #71951, #104494, #170537, #203019, #55726, #188926, #22122, #207311, #88234, #91458, #75190, #125092, #157519, #204074, #140218, #141302, #138061, #155364, #42715, #172695, #6949, #90379, #8032, #189992, #205155, #58934, #121880, #187851, #74122, #206237, #124026, #107757, #105576, #171608, #173783, #23202, #89317, #73029, #139128, #160707, #129366, #162852, #45912, #110953, #62144, #192116, #12301, #109893, #195344, #114166, #159641, #30720, #11238, #146618, #27497, #94664, #78381, #175906, #128304, #112030, #176960, #48053, #28576, #113092, #194266, #43780, #96803, #144502, #178032, #46976, #64276, #130421, #44847, #14430, #79453, #80520, #13378, #212635, #26425, #210509, #29650, #10176, #196408, #92537, #95735, #161787, #158577, #208369, #179098, #76250, #127230, #145569, #142359, #61071, #211568, #60000, #126153, #63202, #93597, #77317, #143430, #209426, #193199, #101020, #116277, #82640, #102099, #81584, #180159, #132511, #3500, #84781, #18699 ),
 .UNSPECIFIED., .F., .F.,
 ( 4, 1, 1, 1, 1, 1, 1, 1, 1, 1, 1, 1, 1, 1, 1, 1, 1, 1, 1, 1, 1, 1, 1, 1, 1, 1, 1, 1, 1, 1, 1, 1, 1, 1, 1, 1, 1, 1, 1, 1, 1, 1, 1, 1, 1, 1, 1, 1, 1, 1, 1, 1, 1, 1, 1, 1, 1, 1, 1, 1, 1, 1, 1, 1, 1, 1, 1, 1, 1, 1, 1, 1, 1, 1, 1, 1, 1, 1, 1, 1, 1, 1, 1, 1, 1, 1, 1, 1, 1, 1, 1, 1, 1, 1, 1, 1, 1, 1, 1, 1, 1, 1, 1, 1, 1, 1, 1, 1, 1, 1, 1, 1, 1, 1, 1, 1, 1, 1, 1, 1, 1, 1, 1, 1, 1, 1, 1, 1, 1, 1, 1, 1, 1, 1, 1, 1, 1, 1, 1, 1, 1, 1, 1, 1, 1, 1, 1, 1, 1, 1, 1, 1, 1, 1, 1, 1, 1, 1, 1, 1, 1, 1, 1, 1, 1, 1, 1, 1, 1, 1, 1, 1, 1, 1, 1, 1, 1, 1, 1, 1, 1, 1, 1, 1, 1, 1, 1, 1, 1, 1, 1, 1, 1, 1, 1, 1, 1, 1, 1, 1, 1, 1, 1, 1, 1, 1, 1, 1, 1, 1, 1, 1, 1, 1, 1, 1, 1, 1, 1, 1, 1, 1, 1, 1, 1, 1, 1, 1, 1, 1, 1, 1, 1, 1, 1, 1, 1, 1, 1, 1, 1, 1, 1, 1, 1, 1, 1, 1, 1, 1, 1, 1, 1, 1, 1, 1, 1, 1, 1, 1, 1, 1, 1, 1, 1, 1, 1, 1, 1, 1, 1, 1, 1, 1, 1, 1, 1, 1, 1, 1, 1, 1, 1, 1, 1, 1, 1, 1, 1, 1, 1, 1, 1, 1, 1, 1, 1, 1, 1, 1, 1, 1, 1, 1, 1, 1, 1, 1, 1, 1, 1, 1, 1, 1, 1, 1, 1, 1, 1, 1, 1, 1, 1, 1, 1, 1, 1, 1, 1, 1, 1, 1, 1, 1, 1, 1, 1, 1, 1, 1, 1, 1, 1, 1, 1, 1, 1, 1, 1, 1, 1, 1, 1, 1, 1, 1, 1, 1, 1, 1, 1, 1, 1, 1, 1, 1, 1, 1, 1, 1, 1, 1, 1, 1, 1, 1, 1, 1, 1, 1, 1, 1, 1, 1, 4 ),
 ( 0.000000000000000000, 0.002600214693118923798, 0.005208871813129847643, 0.007813341859462101871, 0.01041561011214237054, 0.01302159838915000617, 0.01562452542669844589, 0.01822945805747129902, 0.02083332260852943998, 0.02343713088342555886, 0.02604210653276634729, 0.02864513693292065552, 0.03125071383394792401, 0.03385356881896259273, 0.03645895053148855841, 0.03906228851054763251, 0.04166670673482164577, 0.04427111720854654681, 0.04687446234244373178, 0.04947983976256019323, 0.05208269766733494843, 0.05468827385445936690, 0.05729129101459448647, 0.05989628262864687969, 0.06250008845252298662, 0.06510390268380349121, 0.06770888856031336001, 0.07031191025079500112, 0.07291748459129859805, 0.07552033970978830335, 0.07812571920045624507, 0.08072905536012038585, 0.08333347174482363950, 0.08593788071299547637, 0.08854122383090638759, 0.09114659965375219997, 0.09374945576594469199, 0.09635503022752239799, 0.09895804583665256116, 0.1015630356028039000, 0.1041668400134527495, 0.1067706523020897913, 0.1093756367037285043, 0.1119786565701353653, 0.1145842293264338063, 0.1171870828570002881, 0.1197924606432616973, 0.1223957954228293843, 0.1250002099740243899, 0.1276046175975352470, 0.1302079588893767237, 0.1328133332639841735, 0.1354161877457908392, 0.1380217606440506395, 0.1406247748629219918, 0.1432297629411592166, 0.1458335661004374617, 0.1484373766077259071, 0.1510423596945167368, 0.1536453778991425101, 0.1562509492307036785, 0.1588538013357113088, 0.1614591775772540871, 0.1640625111385781432, 0.1666669240170048083, 0.1692713304565471311, 0.1718746700842041231, 0.1744800431702197008, 0.1770828961840006377, 0.1796884676783837009, 0.1822914806691622869, 0.1848964672195632097, 0.1875002692887918765, 0.1901040781760970355, 0.1927090601080766463, 0.1953120768130981733, 0.1979176468793322763, 0.2005204977210985895, 0.2031258725775486607, 0.2057292050824250096, 0.2083336164487647746, 0.2109380218649763994, 0.2135413599902747928, 0.2161467319472901716, 0.2187495836553486062, 0.2213551539052408534, 0.2239581658300387468, 0.2265631510126252801, 0.2291669521530730058, 0.2317707595817034838, 0.2343757405188569010, 0.2369787558863956922, 0.2395843248466610342, 0.2421871745874512594, 0.2447925482183819501, 0.2473958798285567084, 0.2500002898434375842, 0.2526046943969075254, 0.2552080311816201097, 0.2578134021691782518, 0.2604162527337665622, 0.2630218218985046486, 0.2656248329193858781, 0.2682298168941298910, 0.2708336172670197106, 0.2734374233982336255, 0.2760424035005001331, 0.2786454176926287940, 0.2812509857062375773, 0.2838538345082703418, 0.2864592070732082663, 0.2890625379503836689, 0.2916669467743862043, 0.2942713506256608436, 0.2968746862315132518, 0.2994800564091141259, 0.3020829059924399762, 0.3046884742313171190, 0.3072914845103039694, 0.3098964674371332273, 0.3125002672036480411, 0.3151040721986592130, 0.3177090516259382103, 0.3203120648046862140, 0.3229176320309106729, 0.3255204800563645251, 0.3281258517147956355, 0.3307291820206363919, 0.3333335898142997245, 0.3359379931238887229, 0.3385413277125659537, 0.3411466972396727249, 0.3437495460039050044, 0.3463551134761772565, 0.3489581231752558743, 0.3515631052140602009, 0.3541669045353489920, 0.3567707085553323276, 0.3593756874674896018, 0.3619786997948497009, 0.3645842663929277916, 0.3671871138039469185, 0.3697924847153226668, 0.3723958146114617063, 0.3750002215352895019, 0.3776046244636719340, 0.3802079581968237365, 0.3828133272328684833, 0.3854161753401436075, 0.3880217422050354359, 0.3906247514861621029, 0.3932297327967993472, 0.3958335318339832876, 0.3984373350400814418, 0.4010423135969549691, 0.4036453252348887744, 0.4062508913640303643, 0.4088537383227308641, 0.4114591086464738368, 0.4140624382945181647, 0.4166668445089845574, 0.4192712472166146842, 0.4218745802558619973, 0.4244799489602520959, 0.4270827965726798348, 0.4296883629893904488, 0.4322913720144979099, 0.4348963527567997200, 0.4375001516709778882, 0.4401039542243071478, 0.4427089325857130886, 0.4453119436961573974, 0.4479175095155500941, 0.4505203561840259718, 0.4531257260795358843, 0.4557290556410732441, 0.4583334613066292196, 0.4609378639539425948, 0.4635411964608836533, 0.4661465649930071620, 0.4687494122726767465, 0.4713549784003855381, 0.4739579873313886638, 0.4765629676651664814, 0.4791667666174222462, 0.4817705686790782482, 0.4843755470048167200, 0.4869785577496898998, 0.4895841234185048796, 0.4921869699588339309, 0.4947923395854939010, 0.4973956692220981579, 0.5000000744991768276, 0.5026044772465965149, 0.5052078093828125116, 0.5078131779020444991, 0.5104160250110306718, 0.5130215910089035436, 0.5156246000077054914, 0.5182295800927568807, 0.5208333792441637300, 0.5234371809752277338, 0.5260421594250891397, 0.5286451699662961801, 0.5312507356436946271, 0.5338535822179446555, 0.5364589517351265879, 0.5390622816083643354, 0.5416666866573878192, 0.5442710896653298880, 0.5468744215923915242, 0.5494797902580997873, 0.5520826373584690749, 0.5546882033856646022, 0.5572912126141627009, 0.5598961926102767883, 0.5624999921219043797, 0.5651037936834493181, 0.5677087724172201755, 0.5703117829166597375, 0.5729173487617980065, 0.5755201955320329299, 0.5781255650991041772, 0.5807288953705399548, 0.5833333003519244331, 0.5859377037808047861, 0.5885410356602774895, 0.5911464046318289922, 0.5937492518856454238, 0.5963548181013198501, 0.5989578277214122615, 0.6015628077883760083, 0.6041666078212959423, 0.6067704093743923055, 0.6093753885518610192, 0.6119783991714310423, 0.6145839653434672645, 0.6171868124717531101, 0.6197921822480817466, 0.6223955130792849788, 0.6249999181534476866, 0.6276043221636865566, 0.6302076541571374202, 0.6328130235939036785, 0.6354158711632348355, 0.6380214377265494008, 0.6406244479001403924, 0.6432294281977445349, 0.6458332289130368498, 0.6484370306187589028, 0.6510420103997216490, 0.6536450213013255128, 0.6562505879594253688, 0.6588534356078361576, 0.6614588057527972520, 0.6640621373053481324, 0.6666665426327121891, 0.6692709473847417989, 0.6718742796537453543, 0.6744796497151083203, 0.6770824977620315543, 0.6796880648321572682, 0.6822910757211636534, 0.6848960564092084757, 0.6874998579679674204, 0.6901036599873985322, 0.6927086405316660311, 0.6953116518772185506, 0.6979172191805607106, 0.7005200675111846742, 0.7031254381841663958, 0.7057287706196612165, 0.7083331763606625087, 0.7109375820149322900, 0.7135409147210758363, 0.7161462855664346705, 0.7187491342530435423, 0.7213547019891674017, 0.7239577137555243125, 0.7265626949938263079, 0.7291664975571658935, 0.7317703000514055311, 0.7343752815188082650, 0.7369782934702413524, 0.7395838615780243597, 0.7421867107529701579, 0.7447920821133793279, 0.7473954155934371402, 0.7499998219085300954, 0.7526042286255122393, 0.7552075619304030596, 0.7578129337191791270, 0.7604157832075884027, 0.7630213517689198310, 0.7656243645745874904, 0.7682293465229839136, 0.7708331502520449074, 0.7734369533822141873, 0.7760419359326080624, 0.7786449486518774998, 0.7812505177233250997, 0.7838533679047272607, 0.7864587401119955690, 0.7890620747982641792, 0.7916664818479275390, 0.7942708897881238794, 0.7968742238533942368, 0.7994795967450375462, 0.8020824471973901915, 0.8046880167431663677, 0.8072910307501349747, 0.8098960135684915018, 0.8124998186244467568, 0.8151036225516941069, 0.8177086063449673370, 0.8203116199940584385, 0.8229171901884252405, 0.8255200415384508217, 0.8281254147520410447, 0.8307287508062024539, 0.8333331587509454907, 0.8359375680748931670, 0.8385409030622068549, 0.8411462772162020540, 0.8437491287946751184, 0.8463546994841673055, 0.8489577148544642515, 0.8515626987026798655, 0.8541665052467400931, 0.8567703101322480252, 0.8593752953283267937, 0.8619783100692604005, 0.8645838815458386506, 0.8671867342266933454, 0.8697921086061042306, 0.8723954461898817403, 0.8749998551902504751, 0.8776042660585271493, 0.8802076021295854868, 0.8828129777054576355, 0.8854158305722678035, 0.8880214025647872322, 0.8906244194604823194, 0.8932294044984951942, 0.8958332126919159588, 0.8984370186969063976, 0.9010420054557602976, 0.9036450214505988843, 0.9062505943687239052, 0.9088534485426573717, 0.9114588242474312985, 0.9140621635225948394, 0.9166665737391771485, 0.9192709863124074454, 0.9218743236289563825, 0.9244797007862803895, 0.9270825551036790957, 0.9296881285585824051, 0.9322911471418501295, 0.9348961335295734587, 0.9374999435335269471, 0.9401037508197458425, 0.9427087393012421046, 0.9453117567106092967, 0.9479173312323898593, 0.9505201870615167525, 0.9531255642405720430, 0.9557289053967781278, 0.9583333169903581750, 0.9609377312744702415, 0.9635410702737328137, 0.9661464495301401723, 0.9687493035862174695, 0.9713548794777306927, 0.9739579066090123804, 0.9765628826531806972, 0.9791666865793459129, 0.9817705523293528413, 0.9843754818126480011, 0.9869784094881522973, 0.9895843956701340094, 0.9921866610829068733, 0.9947911313000845634, 0.9973997837621362272, 1.000000000000000000 ),
 .UNSPECIFIED. ) ;
#166478=CARTESIAN_POINT ( 'NONE',  ( 0.4746845637013074604, -1.383529810647101455, 1.320479256824915071 ) ) ;
#166480=CARTESIAN_POINT ( 'NONE',  ( 1.363640982571033611, -0.4799814350611387725, 1.902108589862220311 ) ) ;
#166481=FACE_OUTER_BOUND ( 'NONE', #208545, .T. ) ;
#166484=CARTESIAN_POINT ( 'NONE',  ( 5.133110336712339183, 1.960249873928998410, 0.8093987030339530042 ) ) ;
#166487=CARTESIAN_POINT ( 'NONE',  ( 6.626250064558294461, 1.136881752820615432, -1.610320780329032253 ) ) ;
#166489=CARTESIAN_POINT ( 'NONE',  ( 2.285404485177256362, 0.09469097253389560653, -2.011075120970148511 ) ) ;
#166491=CARTESIAN_POINT ( 'NONE',  ( 1.159931391799984279, 1.264437666799199889, 1.698043086552150749 ) ) ;
#166493=CARTESIAN_POINT ( 'NONE',  ( 2.154816067267216084, -0.5500195584662926906, -1.995915215819036748 ) ) ;
#166497=CARTESIAN_POINT ( 'NONE',  ( 5.437476023981094642, 0.8479630442611612029, -1.911130889300112878 ) ) ;
#166499=CARTESIAN_POINT ( 'NONE',  ( 3.996943106591983597, 1.542326501817241180, -0.9764022233923685956 ) ) ;
#166500=CARTESIAN_POINT ( 'NONE',  ( 2.877393275988342047, 0.2635569349610377143, -1.792047384982973890 ) ) ;
#166505=CARTESIAN_POINT ( 'NONE',  ( 5.526482418920476647, 1.318621124876094397, -1.769340128416618363 ) ) ;
#166509=CARTESIAN_POINT ( 'NONE',  ( 4.406835678522929456, -0.4222698756407486931, -1.864907683101609370 ) ) ;
#166516=CARTESIAN_POINT ( 'NONE',  ( 0.02850758872123548837, -1.683968158181762043, 0.7450552726024004535 ) ) ;
#166520=CARTESIAN_POINT ( 'NONE',  ( 3.620239363633662055, 1.188986022374241225, -1.444006105232334969 ) ) ;
#166525=CARTESIAN_POINT ( 'NONE',  ( 0.6726246190636753219, 1.362232206854155914, -1.422558973980556418 ) ) ;
#166526=CARTESIAN_POINT ( 'NONE',  ( 1.757435634535610136, 1.928746520693159550, -0.5880414618760835266 ) ) ;
#166531=CARTESIAN_POINT ( 'NONE',  ( 2.906388222866810978, 1.586772471669075424, -1.511725739355776366 ) ) ;
#166532=CARTESIAN_POINT ( 'NONE',  ( 6.199803715563785289, -0.6102442156579388488, 1.720816905678754560 ) ) ;
#166541=CARTESIAN_POINT ( 'NONE',  ( 4.177188522404684079, 1.205947341878073287, 1.391433828303423326 ) ) ;
#166542=CARTESIAN_POINT ( 'NONE',  ( 0.4869769290230832048, -1.896302947978160791, -0.6760925243112311245 ) ) ;
#166543=CARTESIAN_POINT ( 'NONE',  ( 3.515276618313140311, 2.298542322452525877, 0.003563541299675049897 ) ) ;
#166545=CARTESIAN_POINT ( 'NONE',  ( 0.7251815698985024650, 0.1899481183357653036, -1.851258252060000498 ) ) ;
#166549=CARTESIAN_POINT ( 'NONE',  ( 4.816621285000030284, -0.6497861859515661198, -1.798733151862880186 ) ) ;
#166554=CARTESIAN_POINT ( 'NONE',  ( 3.509396081178951743, -2.059435208860632915, 0.3595599189689518416 ) ) ;
#166555=CARTESIAN_POINT ( 'NONE',  ( 2.008475284031425723, 1.387998011844304491, -1.254312187223500796 ) ) ;
#166558=CARTESIAN_POINT ( 'NONE',  ( 5.442854017605395889, -1.455216020186438364, -1.127989967910733915 ) ) ;
#166562=CARTESIAN_POINT ( 'NONE',  ( 3.510098308409233869, -0.7004517935718050925, -1.576443202522736842 ) ) ;
#166564=CARTESIAN_POINT ( 'NONE',  ( 6.270183524512255246, 1.130759168108757873, 1.895055401287759178 ) ) ;
#166565=CARTESIAN_POINT ( 'NONE',  ( 6.983263157960366563, 7.629137130509066722, 2.653810918356712900 ) ) ;
#166568=CARTESIAN_POINT ( 'NONE',  ( 5.295835511405859286, -1.530271966869084954, -1.540324818649402072 ) ) ;
#166569=CARTESIAN_POINT ( 'NONE',  ( 2.859763506297557711, 1.816872213737670938, -0.1792109616642542924 ) ) ;
#166570=CARTESIAN_POINT ( 'NONE',  ( 0.5319879461419263489, 1.124744735265088780, 1.607134405190835391 ) ) ;
#166571=CARTESIAN_POINT ( 'NONE',  ( 5.190659055775300956, 1.601436234092843414, -1.385157061098884146 ) ) ;
#166574=CARTESIAN_POINT ( 'NONE',  ( 6.321853416579415352, 1.323700039822506280, -1.871417125626378075 ) ) ;
#166577=CARTESIAN_POINT ( 'NONE',  ( 1.629697543846151619, -0.2563088357964183883, 2.104862515383609800 ) ) ;
#166581=CARTESIAN_POINT ( 'NONE',  ( 6.666846200133992539, 1.614693783697606522, -1.451540455714307010 ) ) ;
#166584=CARTESIAN_POINT ( 'NONE',  ( 1.700152687198818402, 1.534743396142525640, 1.606060300191413548 ) ) ;
#166586=CARTESIAN_POINT ( 'NONE',  ( 0.05395445667428447334, -1.494411465983748855, 1.746745294031383455 ) ) ;
#166588=CARTESIAN_POINT ( 'NONE',  ( 4.680570805348211572, 1.272886101012826288, -1.622837931747274975 ) ) ;
#166594=CARTESIAN_POINT ( 'NONE',  ( 0.9727375897880451427, -0.05299885879509737968, -2.090136731789421276 ) ) ;
#166595=CARTESIAN_POINT ( 'NONE',  ( 4.149064681782777875, 0.9530105817698063531, 1.777011888912001014 ) ) ;
#166596=CARTESIAN_POINT ( 'NONE',  ( 4.616662711240536510, -0.08544939198026380023, 1.839383977539174264 ) ) ;
#166599=CARTESIAN_POINT ( 'NONE',  ( 2.063112832053456636, 0.2986308487272717471, -1.698545238003341673 ) ) ;
#166601=CARTESIAN_POINT ( 'NONE',  ( 0.7920821852162404086, 1.736045259359697335, -1.506783991232300446 ) ) ;
#166603=CARTESIAN_POINT ( 'NONE',  ( 1.001694622806301060, 1.849986872810194694, 1.302049432249830607 ) ) ;
#166604=CARTESIAN_POINT ( 'NONE',  ( 2.508543264270487683, -0.8067718606631252287, -1.945620686511064790 ) ) ;
#166608=EDGE_CURVE ( 'NONE', #55444, #77820, #121775, .T. ) ;
#166609=CARTESIAN_POINT ( 'NONE',  ( 6.343749999995762501, 1.895863743059895246, 0.7852924748296488122 ) ) ;
#166613=CARTESIAN_POINT ( 'NONE',  ( 4.799211390369230834, -0.2731021391014861188, -2.204526388291703221 ) ) ;
#166614=CARTESIAN_POINT ( 'NONE',  ( 3.961010909407123304, 0.2689195440248594027, -2.174814543647784593 ) ) ;
#166619=CARTESIAN_POINT ( 'NONE',  ( 6.152600690169603759, 2.097733681304454034, 0.3095894981632040244 ) ) ;
#166623=CARTESIAN_POINT ( 'NONE',  ( 6.455963997168007396, 2.156291961557708525, -0.1537611777119098910 ) ) ;
#166625=CARTESIAN_POINT ( 'NONE',  ( 6.269096963164666469, 1.759884223096353173, -0.5412972069449849544 ) ) ;
#166627=CARTESIAN_POINT ( 'NONE',  ( 1.364397727108757730, 0.1285707514647760064, -1.735724436397204196 ) ) ;
#166632=CARTESIAN_POINT ( 'NONE',  ( 5.682550338946039226, -2.108058120380253087, -0.4779004524640489970 ) ) ;
#166637=CARTESIAN_POINT ( 'NONE',  ( 4.997027575558514734, 1.799266821141291661, -1.197868618907194316 ) ) ;
#166640=CARTESIAN_POINT ( 'NONE',  ( 6.169206948603202179, 0.1476589778573663692, -1.965905794126821426 ) ) ;
#166641=CARTESIAN_POINT ( 'NONE',  ( 4.815645707022956579, -1.391897370064384631, 1.033600972745553070 ) ) ;
#166643=CARTESIAN_POINT ( 'NONE',  ( 1.962683346935737205, -2.005255389829229351, -0.8846387633431598285 ) ) ;
#166644=CARTESIAN_POINT ( 'NONE',  ( 1.765117381242779615, -1.630797578202509701, 1.632866094832433834 ) ) ;
#166645=CARTESIAN_POINT ( 'NONE',  ( 4.710263567924342532, -0.8773996900517248010, -1.864791387430650094 ) ) ;
#166646=CARTESIAN_POINT ( 'NONE',  ( 0.3923911919363164413, 1.615042221312415371, -1.078049841609552306 ) ) ;
#166650=CARTESIAN_POINT ( 'NONE',  ( 3.340189922722580196, -1.266226476691566738, -1.700888996046201029 ) ) ;
#166652=CARTESIAN_POINT ( 'NONE',  ( 1.318982659667154334, 0.9913977828604101372, -1.755770081111128977 ) ) ;
#166655=CARTESIAN_POINT ( 'NONE',  ( 4.190592561755676293, -2.182319254149690302, -0.3268587364041104504 ) ) ;
#166657=CARTESIAN_POINT ( 'NONE',  ( 1.428301029171385794, -1.185968821734217027, 1.434052760600286858 ) ) ;
#166658=CARTESIAN_POINT ( 'NONE',  ( -0.1288028175206907822, 7.629137130509059617, -2.873994896247424435 ) ) ;
#166665=CARTESIAN_POINT ( 'NONE',  ( 3.784101207196560068, -1.017168810052709205, 1.792309825713923166 ) ) ;
#166668=CARTESIAN_POINT ( 'NONE',  ( 1.840495965525708932, 1.161060486998789942, -1.652382956570614736 ) ) ;
#166672=CARTESIAN_POINT ( 'NONE',  ( 1.551711473626409266, 0.5993144932881481202, -1.971807626030545268 ) ) ;
#166676=CARTESIAN_POINT ( 'NONE',  ( -0.2408018239684278916, 6.947782644136219155, -2.695524888730389090 ) ) ;
#166677=CARTESIAN_POINT ( 'NONE',  ( 1.042614295247261680, -1.450156864641814369, -1.134287774663629733 ) ) ;
#166678=CARTESIAN_POINT ( 'NONE',  ( 5.707716145626243964, -0.5396369327701348029, 2.139774205771049154 ) ) ;
#166680=CARTESIAN_POINT ( 'NONE',  ( 1.300320450452172594, -2.161773191439372965, -0.001381507821696103871 ) ) ;
#166682=CARTESIAN_POINT ( 'NONE',  ( 2.026577684455236561, 0.4465047249504557891, 1.966304233017155845 ) ) ;
#166684=CARTESIAN_POINT ( 'NONE',  ( 0.6373110600932235803, -1.319858442276698129, -1.325903642019378381 ) ) ;
#166686=CARTESIAN_POINT ( 'NONE',  ( 4.223478185285460818, -1.886956702611849002, 0.5710618836329334203 ) ) ;
#166687=CARTESIAN_POINT ( 'NONE',  ( 3.327361509216096191, -1.530157842762596143, -1.313544516083162028 ) ) ;
#166691=CARTESIAN_POINT ( 'NONE',  ( 6.322895070704796616, 1.964426112044151518, 0.7597984924697271936 ) ) ;
#166692=CARTESIAN_POINT ( 'NONE',  ( 5.600075274486990828, 0.8424382930321882013, -1.891409743246947217 ) ) ;
#166696=CARTESIAN_POINT ( 'NONE',  ( 4.693620712453854260, 1.883065523094022753, -0.7309246526977104530 ) ) ;
#166698=CARTESIAN_POINT ( 'NONE',  ( 1.358340336993546726, -2.062741126468564890, -0.004002619933256982773 ) ) ;
#166705=( NAMED_UNIT ( * ) PLANE_ANGLE_UNIT ( ) SI_UNIT ( $, .RADIAN. ) );
#166707=CARTESIAN_POINT ( 'NONE',  ( 2.647136220323087485, -0.3691774202370365354, -2.139407045683580755 ) ) ;
#166709=CARTESIAN_POINT ( 'NONE',  ( 6.608665842073913055, 1.606649649811153768, -1.446306907624186344 ) ) ;
#166711=CARTESIAN_POINT ( 'NONE',  ( 2.876309626556411203, -0.1380247437976732383, -1.836149222064882514 ) ) ;
#166713=CARTESIAN_POINT ( 'NONE',  ( 4.476244563333130699, -2.125884358948509689, -0.5320566845071761364 ) ) ;
#166715=CARTESIAN_POINT ( 'NONE',  ( 4.733442339874294191, -2.070396585149585356, 0.9127746130930917134 ) ) ;
#166721=CARTESIAN_POINT ( 'NONE',  ( 0.1625042017948316320, -1.577765994087614310, -0.8020051908347087810 ) ) ;
#166723=CARTESIAN_POINT ( 'NONE',  ( 4.582685675920167512, -1.313125608480088635, 1.525959163679012187 ) ) ;
#166725=CARTESIAN_POINT ( 'NONE',  ( 2.837057662192625340, 0.2562861413469962879, 2.090225181913709207 ) ) ;
#166726=CARTESIAN_POINT ( 'NONE',  ( 1.493601000189462624, -1.900943851588072997, 0.2360903481228252554 ) ) ;
#166730=CARTESIAN_POINT ( 'NONE',  ( 2.154690271565715687, -0.5224902820043091367, -1.898924457017936662 ) ) ;
#166731=CARTESIAN_POINT ( 'NONE',  ( 0.1275333129481092398, -1.147091320445620566, -1.478225367208672703 ) ) ;
#166732=CARTESIAN_POINT ( 'NONE',  ( 0.8714495147512549833, -0.2914478312704605889, 1.939986204769503786 ) ) ;
#166733=CARTESIAN_POINT ( 'NONE',  ( -0.03509584499547176162, -1.534781374734139670, 1.140672443274578729 ) ) ;
#166737=CARTESIAN_POINT ( 'NONE',  ( 6.157094445334826638, -1.605393284960114242, -0.9600186418455139981 ) ) ;
#166739=CARTESIAN_POINT ( 'NONE',  ( 5.875854205266582753, -2.021069926245163906, 0.4479438709683660202 ) ) ;
#166742=CARTESIAN_POINT ( 'NONE',  ( -0.02319159430949970652, 0.003959926571647092407, -1.810968101872318714 ) ) ;
#166749=CARTESIAN_POINT ( 'NONE',  ( 5.687936657224680559, -1.243353266631580523, -1.517579924814119074 ) ) ;
#166751=CARTESIAN_POINT ( 'NONE',  ( 3.286482353612128371, -1.943773746517188039, 0.5350062169211176055 ) ) ;
#166753=CARTESIAN_POINT ( 'NONE',  ( 3.045994482203842502, 0.8657459236516149570, 1.709044100283881429 ) ) ;
#166755=CARTESIAN_POINT ( 'NONE',  ( 2.050558489324630251, -1.691691439650149897, 1.393213601605561180 ) ) ;
#166756=CARTESIAN_POINT ( 'NONE',  ( 0.1331715793776913348, 0.7364730991098663582, -2.038600455735229300 ) ) ;
#166757=CARTESIAN_POINT ( 'NONE',  ( 2.899504437521780442, -0.5904213222340527478, 1.774967144274109287 ) ) ;
#166762=CARTESIAN_POINT ( 'NONE',  ( 3.954788147838703249, -1.976257328041197470, -0.7601183944087180899 ) ) ;
#166764=CARTESIAN_POINT ( 'NONE',  ( 5.775854211382815073, -2.020734006234246927, 0.4499205674863211990 ) ) ;
#166765=CARTESIAN_POINT ( 'NONE',  ( 2.718400508848108466, 1.969533948853121386, 0.7019594197221010745 ) ) ;
#166766=CARTESIAN_POINT ( 'NONE',  ( 6.620655732516649294, 0.5674144795907026806, 2.226195167976598110 ) ) ;
#166767=CARTESIAN_POINT ( 'NONE',  ( 1.254464346661397833, -1.363098773983735024, 1.056675342818178542 ) ) ;
#166776=CARTESIAN_POINT ( 'NONE',  ( 0.1350377444619410283, -0.09094779274463302143, 1.809295058508665566 ) ) ;
#166785=ORIENTED_EDGE ( 'NONE', *, *, #124624, .T. ) ;
#166786=CARTESIAN_POINT ( 'NONE',  ( 0.8256309606260933132, 0.7751641160983432366, -1.751937020314651150 ) ) ;
#166787=CARTESIAN_POINT ( 'NONE',  ( 0.2762449081346768920, 2.096790360132039233, -0.3154013857558089495 ) ) ;
#166790=CARTESIAN_POINT ( 'NONE',  ( -0.1399997263889611598, 6.947783040739049731, -2.595329734540325006 ) ) ;
#166794=CARTESIAN_POINT ( 'NONE',  ( 4.610180678033913182, 1.969109005737102347, -0.04407691609572064739 ) ) ;
#166795=CARTESIAN_POINT ( 'NONE',  ( 1.875790325896836919, 0.3594715711359475208, -2.089634487563592824 ) ) ;
#166800=CARTESIAN_POINT ( 'NONE',  ( 2.483611571103708116, -0.6279893487078171965, 1.916353726171161620 ) ) ;
#166801=CARTESIAN_POINT ( 'NONE',  ( 5.753911783233988331, 0.8852683131516884130, 2.004867968450708915 ) ) ;
#166803=CARTESIAN_POINT ( 'NONE',  ( 3.786086853528514151, -0.9505683805260138897, 1.675471031514904396 ) ) ;
#166805=CARTESIAN_POINT ( 'NONE',  ( 0.1119280604304096899, -0.7754228321929098611, -1.651232954423286436 ) ) ;
#166806=CARTESIAN_POINT ( 'NONE',  ( 1.190363680384380229, -0.9894552095768920363, 1.972713631218452557 ) ) ;
#166810=CARTESIAN_POINT ( 'NONE',  ( 6.315293006042116630, -1.687366247620238457, -1.015419155273014740 ) ) ;
#166811=CARTESIAN_POINT ( 'NONE',  ( 0.6966983018150345597, 1.588492033560371830, 1.117026046969020303 ) ) ;
#166812=CARTESIAN_POINT ( 'NONE',  ( 6.433027599926354867, 1.173280253959343211, 1.976260322036479167 ) ) ;
#166814=CARTESIAN_POINT ( 'NONE',  ( 4.522197165953073750, 0.8743044213657903407, 1.642730557785059053 ) ) ;
#166819=B_SPLINE_CURVE_WITH_KNOTS ( 'NONE', 3,
 ( #90118, #170274, #4541, #22938, #102083, #54407, #187590, #136730, #85831, #69551, #21859, #203820, #19751, #105306, #204888, #186525, #87966, #104227, #151910, #70616, #56539, #122701, #154041, #171343, #3484, #120546, #155110, #156184, #188664, #5606, #20804, #89053, #7762, #6695, #71688, #72770, #138869, #40293, #106404, #73851, #53330, #139946, #201685, #205972, #123763, #37071, #36002, #103152, #189725, #158317, #12039, #79180, #208102, #9908, #74920, #62925, #145296, #91188, #41378, #142088, #13100, #160433, #27222, #26157, #207038, #211301, #78110, #177759, #144237, #29375, #192916, #111754, #59731, #108549, #173513, #210231, #125889, #107488, #95470, #60798, #174581, #8842, #25087, #128034, #157249, #159364, #126957, #44572, #141031, #58669, #61869, #124818, #190782, #75984, #10963, #42446, #93328, #92271, #191847, #161518, #109631, #143165, #43510, #175636, #77038, #209160, #193988, #110688, #176686, #28298, #94395, #45636, #117070, #64000, #80248, #181991, #114940, #32560, #178833, #15227, #34682, #149514, #199301, #14154, #148457, #133295, #50946, #83432, #116005, #98637, #16282, #183068, #131199, #65043, #162580, #132233, #130151, #100751, #196141, #198242, #146347, #49880, #27, #47781, #96531, #150592, #197187, #66091, #48824, #164696, #81317, #163647, #33624, #31513, #166833, #99695, #212359, #97588, #30447, #113895, #165765, #195065, #82368, #1099, #180940, #17350, #67159, #18429, #84502, #179889, #147393, #2154, #213420, #129094, #46705, #112820, #171082, #134362, #101823, #89865, #6432, #70359, #155915, #119200, #136473, #21600, #202494, #54146, #154848, #56279, #200366, #103970, #105046, #167890, #3225, #69293, #137542, #72506, #87706, #68230, #120282, #36809, #102892, #55212, #52015, #184126, #186257, #170012, #38962, #71430, #151655, #135404, #204628, #106144, #153778, #201427, #19491, #37892, #88790, #138605, #85566, #122438, #188396, #22678, #121358, #5348, #203559, #40032, #187333, #4287, #53067, #172168, #185186, #23760, #168951, #118141, #20553, #35749, #86638, #152705, #60527, #29107, #9645, #26956, #158059, #125625, #108294, #42179, #142896, #124563, #127770, #93063, #189471, #190522, #123506, #90926, #126688, #191583, #41113, #94132, #95190, #59466, #75721, #73584, #174315, #28037, #107222, #25889, #177494, #7500, #91999, #44303, #111486, #141835, #207840, #173246, #139687, #205708, #24824, #57343, #43245, #110425, #192650, #109364, #58409, #156992, #8579, #176428, #209961, #160171, #61600, #10704, #11771, #76773, #77844, #193726, #74659, #175373, #143967, #45370, #140763, #159102, #208896, #206775, #66892, #180677, #128812, #63727, #62653, #30168, #65826, #130934, #194793, #33358, #182805, #47509, #116805, #181727, #212091, #148197, #211028, #179624, #34422, #161241, #129886, #197984, #50680, #31244, #195870, #46430, #12827, #78902, #112548, #145024, #113621, #199032, #64790, #178558, #96256, #162309, #13894, #49612, #149249, #115737, #822, #164432, #83166, #97321, #79975, #146079, #131974, #163377, #14952, #133032, #32302, #81049, #147134, #213160, #196927, #48564, #114684, #98369, #16018, #82104, #214197, #99439, #165494, #17088, #166570, #136216, #137289, #200112, #35488, #101566, #169763, #104787, #53888, #188143, #168696, #20301, #184929, #87459, #100495, #1899, #102640, #202236, #71171 ),
 .UNSPECIFIED., .F., .F.,
 ( 4, 1, 1, 1, 1, 1, 1, 1, 1, 1, 1, 1, 1, 1, 1, 1, 1, 1, 1, 1, 1, 1, 1, 1, 1, 1, 1, 1, 1, 1, 1, 1, 1, 1, 1, 1, 1, 1, 1, 1, 1, 1, 1, 1, 1, 1, 1, 1, 1, 1, 1, 1, 1, 1, 1, 1, 1, 1, 1, 1, 1, 1, 1, 1, 1, 1, 1, 1, 1, 1, 1, 1, 1, 1, 1, 1, 1, 1, 1, 1, 1, 1, 1, 1, 1, 1, 1, 1, 1, 1, 1, 1, 1, 1, 1, 1, 1, 1, 1, 1, 1, 1, 1, 1, 1, 1, 1, 1, 1, 1, 1, 1, 1, 1, 1, 1, 1, 1, 1, 1, 1, 1, 1, 1, 1, 1, 1, 1, 1, 1, 1, 1, 1, 1, 1, 1, 1, 1, 1, 1, 1, 1, 1, 1, 1, 1, 1, 1, 1, 1, 1, 1, 1, 1, 1, 1, 1, 1, 1, 1, 1, 1, 1, 1, 1, 1, 1, 1, 1, 1, 1, 1, 1, 1, 1, 1, 1, 1, 1, 1, 1, 1, 1, 1, 1, 1, 1, 1, 1, 1, 1, 1, 1, 1, 1, 1, 1, 1, 1, 1, 1, 1, 1, 1, 1, 1, 1, 1, 1, 1, 1, 1, 1, 1, 1, 1, 1, 1, 1, 1, 1, 1, 1, 1, 1, 1, 1, 1, 1, 1, 1, 1, 1, 1, 1, 1, 1, 1, 1, 1, 1, 1, 1, 1, 1, 1, 1, 1, 1, 1, 1, 1, 1, 1, 1, 1, 1, 1, 1, 1, 1, 1, 1, 1, 1, 1, 1, 1, 1, 1, 1, 1, 1, 1, 1, 1, 1, 1, 1, 1, 1, 1, 1, 1, 1, 1, 1, 1, 1, 1, 1, 1, 1, 1, 1, 1, 1, 1, 1, 1, 1, 1, 1, 1, 1, 1, 1, 1, 1, 1, 1, 1, 1, 1, 1, 1, 1, 1, 1, 1, 1, 1, 1, 1, 1, 1, 1, 1, 1, 1, 1, 1, 1, 1, 1, 1, 1, 1, 1, 1, 1, 1, 1, 1, 1, 1, 1, 1, 1, 1, 1, 1, 1, 1, 1, 1, 1, 1, 1, 1, 1, 1, 1, 1, 1, 1, 1, 1, 1, 1, 1, 1, 1, 1, 1, 1, 1, 1, 1, 1, 1, 1, 1, 1, 4 ),
 ( 0.000000000000000000, 0.002600063085273907840, 0.005208809393482579861, 0.007813201938950280895, 0.01041611862257568050, 0.01302098276518856741, 0.01562474632808895890, 0.01822919105953027183, 0.02083324087635668453, 0.02343728507989274734, 0.02604173773626635227, 0.02864548761524753420, 0.03125016255115702773, 0.03385383280295282959, 0.03645844125268089125, 0.03906229690237970897, 0.04166656525949016115, 0.04427081591349327910, 0.04687468903198145631, 0.04947928942627017462, 0.05208296534865054783, 0.05468764290212216328, 0.05729137561078536528, 0.05989584521530456201, 0.06249987723257615507, 0.06510392926424246607, 0.06770838613806146045, 0.07031213076997053224, 0.07291680575263978503, 0.07552047744215656389, 0.07812508546332513903, 0.08072894086165181837, 0.08333320924388483431, 0.08593745993457323207, 0.08854133291633270453, 0.09114593330519306369, 0.09374960916840779923, 0.09635428668231969807, 0.09895801939011879267, 0.1015624889210437753, 0.1041665209728785957, 0.1067705729027476208, 0.1093750297965602747, 0.1119787743537518920, 0.1145834493281674554, 0.1171871210017138010, 0.1197917289818775377, 0.1223955844170728779, 0.1249998527215379351, 0.1276041034591044177, 0.1302079763611066199, 0.1328125767709825433, 0.1354162526020633861, 0.1380209301064295735, 0.1406246628425296130, 0.1432291323291436380, 0.1458331644451768827, 0.1484372163025670099, 0.1510416732455448496, 0.1536454177576472568, 0.1562500927529001105, 0.1588537644400710158, 0.1614583724083656635, 0.1640622279099430147, 0.1666664961659596600, 0.1692707469797122277, 0.1718746198314790308, 0.1744792202914958457, 0.1770828961200470730, 0.1796875736439581817, 0.1822913064379278192, 0.1848957759094348730, 0.1874998081190861754, 0.1901038599334289314, 0.1927083169547665342, 0.1953120614513534081, 0.1979167364965291054, 0.2005204082269216870, 0.2031250162124720871, 0.2057288718099357372, 0.2083331400468157457, 0.2109373909660553770, 0.2135412637971000893, 0.2161458643363758370, 0.2187495401919937743, 0.2213542177645327069, 0.2239579506459335456, 0.2265624201315297737, 0.2291664524642116896, 0.2317705042649303715, 0.2343749613938155840, 0.2369787059044528299, 0.2395833810286300269, 0.2421870528318344207, 0.2447916608637582536, 0.2473955165866061623, 0.2499997848336539263, 0.2526040358876752157, 0.2552079087275039293, 0.2578125093751503782, 0.2604161852874245509, 0.2630208629376679097, 0.2656245959360551967, 0.2682290654649299166, 0.2708330979500496172, 0.2734371497665608608, 0.2760416070321756732, 0.2786453515864226738, 0.2812500268186742258, 0.2838536987242743503, 0.2864583068316831627, 0.2890621627094078216, 0.2916664309959213219, 0.2942706822140139789, 0.2968745550921262355, 0.2994791558772498252, 0.3020828318757637354, 0.3046875096327826826, 0.3072912427777066413, 0.3098957123790437307, 0.3124997450460035853, 0.3151037969077182255, 0.3177082543392401592, 0.3203119989666507461, 0.3229166743360447622, 0.3255203463736199843, 0.3281249545856204097, 0.3307288106477103140, 0.3333330790029824242, 0.3359373304144318562, 0.3385412033603223403, 0.3411458043120255135, 0.3437494804263583337, 0.3463541583192197293, 0.3489578916402267250, 0.3515623613432052874, 0.3541663942214042238, 0.3567704461577280162, 0.3593749037843310123, 0.3619786485144548260, 0.3645833240500557237, 0.3671869962491814965, 0.3697916045948764219, 0.3723954608708167080, 0.3749997293241361662, 0.3776039809582251716, 0.3802078540013843488, 0.3828124551487663840, 0.3854161314084936785, 0.3880208094662612184, 0.3906245429928945634, 0.3932290128266905938, 0.3958330459455252637, 0.3984370979858605777, 0.4010415558367163569, 0.4036453006990994852, 0.4062499764299690730, 0.4088536488202184072, 0.4114582573287078326, 0.4140621138479816388, 0.4166663824286341855, 0.4192706343146435644, 0.4218745074845589027, 0.4244791088567174686, 0.4270827852914125256, 0.4296874635431477407, 0.4322911973049493040, 0.4348956672987361882, 0.4374997006876018557, 0.4401037528613486738, 0.4427082109656274023, 0.4453119559898139901, 0.4479166319450127998, 0.4505203045559570407, 0.4531249132563394122, 0.4557287700484292658, 0.4583330387856985322, 0.4609372909529084184, 0.4635411642790657205, 0.4661457659050973201, 0.4687494425443319290, 0.4713541210190953512, 0.4739578550456061690, 0.4765623252285562383, 0.4791663589168480009, 0.4817704112534048067, 0.4843748696402766507, 0.4869786148558097882, 0.4895832910643978519, 0.4921869639256079565, 0.4947915728469811647, 0.4973954299413693159, 0.4999996988645384333, 0.5026039513422294602, 0.5052078248541136407, 0.5078124267631153321, 0.5104161036364611714, 0.5130207823633133879, 0.5156245166840751626, 0.5182289870853604707, 0.5208330211024742029, 0.5234370736312391470, 0.5260415323298749390, 0.5286452777662975500, 0.5312499542573357880, 0.5338536273983837122, 0.5364582365698458144, 0.5390620939960163449, 0.5416663631343685559, 0.5442706159518226894, 0.5468744896789192733, 0.5494790918999890028, 0.5520827690370186946, 0.5546874480450217915, 0.5572911826895774468, 0.5598956533383712131, 0.5624996877137050655, 0.5651037404640770756, 0.5677081995036498130, 0.5703119451905063197, 0.5729166219930570403, 0.5755202954435161278, 0.5781249048941674573, 0.5807287626816063364, 0.5833330320644263267, 0.5859372852509285856, 0.5885411592227242084, 0.5911457617849628088, 0.5937494392152512512, 0.5963541185334689798, 0.5989578535313645480, 0.6015623244568418793, 0.6041663592197970001, 0.6067704122211770024, 0.6093748716308627911, 0.6119786175976995590, 0.6145832947408284008, 0.6171869685302752151, 0.6197915782892181591, 0.6223954364674153528, 0.6249997061239902507, 0.6276039597088286515, 0.6302078339548128350, 0.6328124368873246919, 0.6354161146404495586, 0.6380207942979494451, 0.6406245296787346222, 0.6432290009100736228, 0.6458330360900554901, 0.6484370893718474083, 0.6510415491808263511, 0.6536452954571934093, 0.6562499729699700080, 0.6588536471279848872, 0.6614582572243260516, 0.6640621158227759668, 0.6666663857823964534, 0.6692706397948642305, 0.6718745143445301604, 0.6744791176764239893, 0.6770827957819672838, 0.6796874758078212952, 0.6822912116010506622, 0.6848956831674339885, 0.6874997187938534093, 0.6901037723854651640, 0.6927082326229228038, 0.6953119792383747333, 0.6979166571498732763, 0.7005203317060422208, 0.7031249421688929857, 0.7057288012170955804, 0.7083330715090569996, 0.7109373259784533827, 0.7135412008612989077, 0.7161458046216893081, 0.7187494831092385850, 0.7213541635325240176, 0.7239578997677582617, 0.7265623716983737879, 0.7291664078006476757, 0.7317704617314926274, 0.7343749224266207243, 0.7369786694107173242, 0.7395833477500189934, 0.7421870227339337767, 0.7447916335924112952, 0.7473954931198736329, 0.7499997637734774347, 0.7526040187291080930, 0.7552078939746372788, 0.7578124981926457338, 0.7604161770917949870, 0.7630208579415957981, 0.7656245946484027121, 0.7682290669724446408, 0.7708331035799980135, 0.7734371578794957403, 0.7760416190614934928, 0.7786453664438016675, 0.7812500452399944173, 0.7838537206812543623, 0.7864583319644831150, 0.7890621920007202528, 0.7916664630452742157, 0.7942707185164536998, 0.7968745941541772737, 0.7994791988589329268, 0.8020828781992835887, 0.8046875595046918406, 0.8072912967126475436, 0.8098957694593176271, 0.8124998066015838294, 0.8151038612991610144, 0.8177083229972362810, 0.8203120708073305956, 0.8229167500895105958, 0.8255204260177235742, 0.8281250377548363684, 0.8307288983293719120, 0.8333331697941922522, 0.8359374258102438837, 0.8385413018696807885, 0.8411459070903221091, 0.8437495869014844940, 0.8463542686916004643, 0.8489580064302900686, 0.8515624796287988296, 0.8541665173352209761, 0.8567705724603134065, 0.8593750347036837045, 0.8619787829711476057, 0.8645834627684209073, 0.8671871392132045608, 0.8697917514333429745, 0.8723956125757112989, 0.8749998844901232253, 0.8776041410803804288, 0.8802080175910590443, 0.8828126233567346048, 0.8854163036683286858, 0.8880209859722626442, 0.8906247242712825862, 0.8932291979508502067, 0.8958332362508822921, 0.8984372918329353030, 0.9010417546508288078, 0.9036455034052560675, 0.9062501837467389354, 0.9088538607377212308, 0.9114584734700372781, 0.9140623352097841936, 0.9166666076031229071, 0.9192708647969299873, 0.9218747417883903505, 0.9244793481282622682, 0.9270830289699085736, 0.9296877118167798937, 0.9322914507057830091, 0.9348959248956096868, 0.9374999638185942397, 0.9401040198872741005, 0.9427084833090058069, 0.9453122325795346725, 0.9479169134952544207, 0.9505205910598265584, 0.9531252043308329203, 0.9557290667238423909, 0.9583333396063040688, 0.9609375973010293448, 0.9635414750455153499, 0.9661460823481272664, 0.9687497623469286667, 0.9713544456720903941, 0.9739581901020435417, 0.9765626606554614897, 0.9791666924408860551, 0.9817707657828746992, 0.9843752055175947202, 0.9869789906880002128, 0.9895838567146432174, 0.9921867690109741345, 0.9947911791560083428, 0.9973999138825643263, 0.9999999999999998890 ),
 .UNSPECIFIED. ) ;
#166821=CARTESIAN_POINT ( 'NONE',  ( -0.1114211809780316365, -0.4883405756051837354, -2.144353428667714390 ) ) ;
#166826=CARTESIAN_POINT ( 'NONE',  ( 0.3283667639546791195, 1.746078182827022429, 0.5332771064449209897 ) ) ;
#166828=CARTESIAN_POINT ( 'NONE',  ( 3.832397100292153524, 0.5799717274662331556, -1.634443932507266384 ) ) ;
#166832=CARTESIAN_POINT ( 'NONE',  ( 0.3461526914491962481, 1.921225470409862357, 0.1432632881103387268 ) ) ;
#166833=CARTESIAN_POINT ( 'NONE',  ( 4.293769791895286403, -1.349757117914761384, -1.423854091114319598 ) ) ;
#166836=CARTESIAN_POINT ( 'NONE',  ( 5.145234815219777325, 0.1564148900096741512, 2.114790009947895122 ) ) ;
#166840=CARTESIAN_POINT ( 'NONE',  ( 2.676698048161993082, 1.355622082481915847, -1.564734663558226879 ) ) ;
#166844=CARTESIAN_POINT ( 'NONE',  ( 3.358291665479910648, 0.05479990919179249936, -2.298175070600398939 ) ) ;
#166850=EDGE_LOOP ( 'NONE', ( #23173, #4386, #25388, #118226 ) ) ;
#166852=CARTESIAN_POINT ( 'NONE',  ( 4.060738401289211374, 0.5150538496448524572, 1.841637258418599155 ) ) ;
#166854=CARTESIAN_POINT ( 'NONE',  ( 4.752814332062330394, -1.383916046847250669, 1.029161146002472549 ) ) ;
#166855=CARTESIAN_POINT ( 'NONE',  ( 3.714077560468319827, 1.074663192196689376, -1.706111893292367343 ) ) ;
#166856=CARTESIAN_POINT ( 'NONE',  ( 5.010469735608720221, -2.183386834666663390, 0.7190086036765501731 ) ) ;
#166858=CARTESIAN_POINT ( 'NONE',  ( 0.7685542157043163680, 1.090964843879228097, 1.918292034055509632 ) ) ;
#166860=EDGE_LOOP ( 'NONE', ( #31155, #87389, #133472, #1575 ) ) ;
#166861=CARTESIAN_POINT ( 'NONE',  ( 5.325387591137793919, -1.680293062798293713, 0.5557786991975487423 ) ) ;
#166863=CARTESIAN_POINT ( 'NONE',  ( 2.045279198001882737, -1.842668879747776156, -1.363283251902024817 ) ) ;
#166864=CARTESIAN_POINT ( 'NONE',  ( 6.632757984263843554, -1.642112545546599023, 0.8327811610863435909 ) ) ;
#166871=CARTESIAN_POINT ( 'NONE',  ( 0.1335669894368500255, -0.0009366757763962055587, -2.153671288142432250 ) ) ;
#166872=CARTESIAN_POINT ( 'NONE',  ( 0.7257964430846426396, 0.8128130212789463904, -1.845628942776005088 ) ) ;
#166875=CARTESIAN_POINT ( 'NONE',  ( 5.531840760993587125, -1.223730149660817501, -1.487915846976423984 ) ) ;
#166878=CARTESIAN_POINT ( 'NONE',  ( 2.725082634249659463, 1.605975871135911559, -1.534981474645187971 ) ) ;
#166887=CARTESIAN_POINT ( 'NONE',  ( 4.493551464656197147, -1.740228352261258049, -0.03666429755099299970 ) ) ;
#166888=CARTESIAN_POINT ( 'NONE',  ( 2.682025323810240280, -1.127217178123595565, -1.605522638798158264 ) ) ;
#166893=CARTESIAN_POINT ( 'NONE',  ( 0.4849267205471480269, 1.973383872003172224, 0.6002626889692606049 ) ) ;
#166896=CARTESIAN_POINT ( 'NONE',  ( 1.341102801589135529, 0.4431706325995210527, 2.218532444564396577 ) ) ;
#166899=CARTESIAN_POINT ( 'NONE',  ( 3.040157689216971715, 1.855973101128991054, 0.2326549598439253685 ) ) ;
#166900=CARTESIAN_POINT ( 'NONE',  ( 1.881130407182354469, -0.4634198587198985475, -1.670964061236743348 ) ) ;
#166901=CARTESIAN_POINT ( 'NONE',  ( 5.091441847573507928, -0.7891374179831472935, 2.044738775321436997 ) ) ;
#166902=CARTESIAN_POINT ( 'NONE',  ( 5.421043267468262705, 2.129509263528307716, 0.8893739899358196199 ) ) ;
#166903=CARTESIAN_POINT ( 'NONE',  ( 1.446242185974885963, 2.058501543756698915, 0.1019544441857832273 ) ) ;
#166904=CARTESIAN_POINT ( 'NONE',  ( 3.169799299931614911, -1.156099248863748485, 1.560184043245048890 ) ) ;
#166906=CARTESIAN_POINT ( 'NONE',  ( 5.606678975738343951, 1.416997745663551633, -1.221222563005261552 ) ) ;
#166907=CARTESIAN_POINT ( 'NONE',  ( 1.156250000000000888, -1.895863743164063031, 0.7852924748300492697 ) ) ;
#166909=CARTESIAN_POINT ( 'NONE',  ( 0.3152591496230552348, -1.397726865852641387, 1.025726801146044531 ) ) ;
#166912=CARTESIAN_POINT ( 'NONE',  ( 5.027970288326706338, -1.728003250605243180, 1.038991650911202713 ) ) ;
#166916=CARTESIAN_POINT ( 'NONE',  ( 1.892912435568369744, 1.589020553905008626, -0.8988452475950716725 ) ) ;
#166921=EDGE_LOOP ( 'NONE', ( #83045, #184866, #59898, #26816 ) ) ;
#166925=CARTESIAN_POINT ( 'NONE',  ( 0.2990895800742687793, -0.2513629124439535345, -2.004038569727568664 ) ) ;
#166926=CARTESIAN_POINT ( 'NONE',  ( -0.05774110376318035420, -1.308430771297010908, -1.669371405835825550 ) ) ;
#166931=CARTESIAN_POINT ( 'NONE',  ( 4.961820856888925491, 2.038780864349061250, -0.3001439806698430468 ) ) ;
#166932=CARTESIAN_POINT ( 'NONE',  ( 5.221327349844218091, 1.987046161919112430, 0.3419379449052239450 ) ) ;
#166940=CARTESIAN_POINT ( 'NONE',  ( 4.763045971468515383, -2.015604388477490350, -0.05228862439247972116 ) ) ;
#166941=CARTESIAN_POINT ( 'NONE',  ( 4.593604542485023146, -1.840816577468977533, -0.04244875611379012037 ) ) ;
#166942=CARTESIAN_POINT ( 'NONE',  ( 0.07661050522435490506, 0.2583762315121455599, -1.746200777818290195 ) ) ;
#166943=CARTESIAN_POINT ( 'NONE',  ( 2.508792734928457335, -0.8846401781386037388, -2.131589412884911106 ) ) ;
#166945=CARTESIAN_POINT ( 'NONE',  ( 5.149776166300943814, 0.6834882490109328579, -2.050742609271530181 ) ) ;
#166946=CARTESIAN_POINT ( 'NONE',  ( 3.415250174187448362, -1.861344788686780438, 0.7762291900053899241 ) ) ;
#166948=CARTESIAN_POINT ( 'NONE',  ( 0.4681772292557941917, -1.829107974901639899, -0.6530565061142034056 ) ) ;
#166954=CARTESIAN_POINT ( 'NONE',  ( 3.660894226558962128, -1.649352935060313552, -0.8826137995501317501 ) ) ;
#166956=CARTESIAN_POINT ( 'NONE',  ( 1.107505169401588274, 1.450017293480215352, 1.247013401884336403 ) ) ;
#166959=CARTESIAN_POINT ( 'NONE',  ( 2.754729969050898841, 0.7443088323898851000, 2.077706851784946185 ) ) ;
#166965=CARTESIAN_POINT ( 'NONE',  ( 0.1749903794560749015, 0.004523422195312763391, -1.955468523092759536 ) ) ;
#166966=CARTESIAN_POINT ( 'NONE',  ( 6.410760325301650298, 1.714854236211732941, -1.544436965994408828 ) ) ;
#166967=CARTESIAN_POINT ( 'NONE',  ( 1.117545225965112188, 0.3861695934333775337, -1.923310697798483293 ) ) ;
#166968=CARTESIAN_POINT ( 'NONE',  ( 4.047761193102417110, 1.490534549623608873, 1.425871689066391168 ) ) ;
#166976=CARTESIAN_POINT ( 'NONE',  ( 6.320782530974223157, -1.539933897815339403, 1.530818809132200142 ) ) ;
#166978=CARTESIAN_POINT ( 'NONE',  ( 6.216338285296751920, 1.720575329815833943, 0.6561210673821931127 ) ) ;
#166981=CARTESIAN_POINT ( 'NONE',  ( 1.862360739135361376, -1.326353699019737098, 1.319252464149045734 ) ) ;
#166987=CARTESIAN_POINT ( 'NONE',  ( 1.119614361207950548, -0.4638517909370845071, 1.855054000551699778 ) ) ;
#166988=CARTESIAN_POINT ( 'NONE',  ( 3.115802406598367824, -0.8709184464271730874, -1.540630773470308190 ) ) ;
#166989=CARTESIAN_POINT ( 'NONE',  ( 0.3110002902955294468, 1.589785527739733695, -1.062417771062994287 ) ) ;
#166991=CARTESIAN_POINT ( 'NONE',  ( 4.569893716599374933, -0.8992288252529623271, 1.691407037985042772 ) ) ;
#166993=CARTESIAN_POINT ( 'NONE',  ( 5.758249387092365446, -1.969739562807392819, -0.001740234774137705337 ) ) ;
#166994=CARTESIAN_POINT ( 'NONE',  ( 0.7211286721200690364, 1.601891702520108485, -1.389630591760198541 ) ) ;
#166996=CARTESIAN_POINT ( 'NONE',  ( 4.276139911362797363, -1.077190196239918851, 1.529178877381555335 ) ) ;
#166997=CARTESIAN_POINT ( 'NONE',  ( 0.5217476098421744979, -0.9739702522407606144, -1.544006022310390192 ) ) ;
#166999=CARTESIAN_POINT ( 'NONE',  ( 3.264504910713565078, 0.9923201075644829672, 1.971275125648555449 ) ) ;
#167002=CARTESIAN_POINT ( 'NONE',  ( 0.6606829430093235089, -0.6931630328321845003, -1.942862509804524906 ) ) ;
#167009=CARTESIAN_POINT ( 'NONE',  ( 3.314952806421948672, -1.569539724514938950, 1.350292352848787569 ) ) ;
#167011=CARTESIAN_POINT ( 'NONE',  ( 1.317891493549529391, -2.109231647155560108, 0.4722262556789079135 ) ) ;
#167013=CARTESIAN_POINT ( 'NONE',  ( 2.438154291397228501, -1.164718066671111885, -1.649793688766809430 ) ) ;
#167018=CARTESIAN_POINT ( 'NONE',  ( 0.6379081216283178923, 2.014007883293071899, -0.1037844182863178755 ) ) ;
#167019=CARTESIAN_POINT ( 'NONE',  ( 5.284801750429747536, 1.933107837519608685, -1.032524723389722787 ) ) ;
#167021=CARTESIAN_POINT ( 'NONE',  ( 3.234525475359388391, 1.209690070866603406, -1.481213593849866728 ) ) ;
#167025=CARTESIAN_POINT ( 'NONE',  ( 0.8257962581623284892, 0.8146080751335778025, -1.844719337431327544 ) ) ;
#167027=CARTESIAN_POINT ( 'NONE',  ( 0.6621918981609349331, 1.136352663792916662, 1.990853321008963395 ) ) ;
#167029=CARTESIAN_POINT ( 'NONE',  ( 4.471539400256457242, 1.672567520934200136, -0.4206060815013599741 ) ) ;
#167033=CARTESIAN_POINT ( 'NONE',  ( 1.627322669196319849, 0.1476378700930695564, -1.956383933670035713 ) ) ;
#167036=CARTESIAN_POINT ( 'NONE',  ( 0.1755611466353629579, -0.002217706044341584935, -2.244164702216360219 ) ) ;
#167038=CARTESIAN_POINT ( 'NONE',  ( 0.4091448426733998445, -1.664836780672280803, 1.230395522420649979 ) ) ;
#167041=CARTESIAN_POINT ( 'NONE',  ( 4.072783076529101542, -1.339505953097392066, 1.219664821550008549 ) ) ;
#167042=ORIENTED_EDGE ( 'NONE', *, *, #109079, .T. ) ;
#167046=CARTESIAN_POINT ( 'NONE',  ( 5.127533414443554705, -0.2600442617171055404, 1.792572003776324197 ) ) ;
#167048=SURFACE_SIDE_STYLE ('',( #34885 ) ) ;
#167050=CARTESIAN_POINT ( 'NONE',  ( 5.898848723475273559, 0.3636257040535681995, 1.824992291636283293 ) ) ;
#167052=CARTESIAN_POINT ( 'NONE',  ( 3.831564657165886789, 0.6421465917123435618, -1.804920456748728474 ) ) ;
#167060=CARTESIAN_POINT ( 'NONE',  ( 1.253037233087474611, -1.703760181015579134, 1.330383891403746688 ) ) ;
#167063=CARTESIAN_POINT ( 'NONE',  ( 0.3932109892899987580, 1.349039491128176449, 1.230163767592551638 ) ) ;
#167065=CARTESIAN_POINT ( 'NONE',  ( 3.856323340278215550, 0.6566615474184741563, 1.703573633380930374 ) ) ;
#167067=CARTESIAN_POINT ( 'NONE',  ( 1.582132296805271787, 0.9858968508435607125, 1.638552900098678045 ) ) ;
#167069=CARTESIAN_POINT ( 'NONE',  ( 2.207411625193840266, -1.579985490969371575, -1.175680343436244391 ) ) ;
#167070=CARTESIAN_POINT ( 'NONE',  ( 5.038593826026604994, -1.663644762202406646, 1.001748047271956876 ) ) ;
#167073=CARTESIAN_POINT ( 'NONE',  ( 4.271814301144261528, 0.4616217191124799002, -2.069597271375968273 ) ) ;
#167085=CARTESIAN_POINT ( 'NONE',  ( 5.514214477338500231, -0.8245889995748825196, -1.628937154514856545 ) ) ;
#167089=CARTESIAN_POINT ( 'NONE',  ( 6.925078400183577010, 7.053014648177382995, 2.453806744102948745 ) ) ;
#167090=CARTESIAN_POINT ( 'NONE',  ( 6.139502064137229986, -1.356240498024411600, -1.288626068300227523 ) ) ;
#167092=CARTESIAN_POINT ( 'NONE',  ( 2.719263968888342653, -0.1887435353777958125, 1.917229668948018162 ) ) ;
#167102=CARTESIAN_POINT ( 'NONE',  ( 1.529080078018136390, -1.786526079506415288, 1.135962973836294854 ) ) ;
#167105=CARTESIAN_POINT ( 'NONE',  ( 5.998901810315326877, 0.3981486965325408134, 2.031442706791640074 ) ) ;
#167106=CARTESIAN_POINT ( 'NONE',  ( 1.768857366986800184, 1.761637791510446860, -0.5354853023365884201 ) ) ;
#167111=CARTESIAN_POINT ( 'NONE',  ( 1.693750089093534861, -0.7690282282955845927, 2.159540072747981654 ) ) ;
#167115=CARTESIAN_POINT ( 'NONE',  ( 0.5275904727545431827, -0.2913634075805496271, 1.991877199276798516 ) ) ;
#167116=CARTESIAN_POINT ( 'NONE',  ( 0.8132426064601482318, -1.654215606812576400, -1.054277637385622857 ) ) ;
#167119=CARTESIAN_POINT ( 'NONE',  ( 6.639320575229252341, 0.005161017367553630275, 1.896863882003448021 ) ) ;
#167121=CARTESIAN_POINT ( 'NONE',  ( 3.714856679239968873, -0.1534820204720024339, 2.085054752100850894 ) ) ;
#167122=CARTESIAN_POINT ( 'NONE',  ( 1.885279724593362793, 1.217781634009064806, 1.284517237999055039 ) ) ;
#167125=CARTESIAN_POINT ( 'NONE',  ( 4.910265066218413743, 1.583196867009181608, -1.657922308084827545 ) ) ;
#167126=CARTESIAN_POINT ( 'NONE',  ( 2.853125853291237579, 1.731928873650347311, -0.1707260732264591074 ) ) ;
#167130=CARTESIAN_POINT ( 'NONE',  ( 3.215853349543820183, -1.415750056632815168, -1.000566135699741066 ) ) ;
#167131=CARTESIAN_POINT ( 'NONE',  ( 3.174467775116470936, -1.067885509202262773, -1.890316989176257234 ) ) ;
#167133=CARTESIAN_POINT ( 'NONE',  ( 4.698454014923811428, 1.387101836239763131, -1.463925544105355803 ) ) ;
#167134=CARTESIAN_POINT ( 'NONE',  ( 6.531249988543854634, -0.7852927567036558365, -1.895863743163934245 ) ) ;
#167136=CARTESIAN_POINT ( 'NONE',  ( 2.414956338186133422, 1.719780681555121982, 0.8681123839546500687 ) ) ;
#167138=CARTESIAN_POINT ( 'NONE',  ( 5.344044365905453731, -1.409322151232726750, -1.717068368634220299 ) ) ;
#167140=CARTESIAN_POINT ( 'NONE',  ( -0.1108833634137010304, 0.2458664895051872190, -1.931623620491630611 ) ) ;
#167145=CARTESIAN_POINT ( 'NONE',  ( 6.004347769543215030, 1.959566550440184907, 0.09775035808561728656 ) ) ;
#167148=CARTESIAN_POINT ( 'NONE',  ( 6.889870058830950938, -0.9756824853745720283, 2.038933460117636542 ) ) ;
#167151=CARTESIAN_POINT ( 'NONE',  ( 3.930177659428602865, 1.143423634368987196, 1.716560605327678513 ) ) ;
#167155=CARTESIAN_POINT ( 'NONE',  ( 6.309813054293936574, -1.856383540575656799, 0.2289572138471432372 ) ) ;
#167156=CARTESIAN_POINT ( 'NONE',  ( 4.342224273253515676, 0.3742292800460333413, -1.693095411864028677 ) ) ;
#167157=CARTESIAN_POINT ( 'NONE',  ( 4.704519267438088015, 1.517481324781422503, 0.8521212890505409643 ) ) ;
#167159=CARTESIAN_POINT ( 'NONE',  ( 2.244040508683461166, 2.291928982054102004, 0.05232369179298743123 ) ) ;
#167161=CARTESIAN_POINT ( 'NONE',  ( 5.706606250695148042, 1.844387978369428582, 0.9845570724962575682 ) ) ;
#167162=CARTESIAN_POINT ( 'NONE',  ( 0.5328340850149284602, -1.300071877079148841, -1.303948673260245439 ) ) ;
#167165=CARTESIAN_POINT ( 'NONE',  ( 1.459611520199757706, -1.915600648959712382, -0.6298732728240025169 ) ) ;
#167166=CARTESIAN_POINT ( 'NONE',  ( 0.3401085955914602277, 2.185883683461706362, 0.1570275565265024931 ) ) ;
#167170=CARTESIAN_POINT ( 'NONE',  ( 4.090573159264241809, -1.219870178150096462, 1.734285844867427651 ) ) ;
#167172=CARTESIAN_POINT ( 'NONE',  ( 6.006453938882227561, -0.6616566355047011072, -1.701761020394356283 ) ) ;
#167177=CARTESIAN_POINT ( 'NONE',  ( 3.586198609924298175, 1.125526462575956010, 1.676902781687271915 ) ) ;
#167178=CARTESIAN_POINT ( 'NONE',  ( 6.405322867445039314, 1.831175526881479776, 1.231239259074583092 ) ) ;
#167180=CARTESIAN_POINT ( 'NONE',  ( 3.520197291191272448, 0.8326901208413343136, 1.664296038758736440 ) ) ;
#167190=CARTESIAN_POINT ( 'NONE',  ( 1.774300323613137165, -1.721452415463576635, 0.2060816229845687519 ) ) ;
#167191=CARTESIAN_POINT ( 'NONE',  ( 1.323703871734905890, 1.676395044522845712, 0.4671252976603932350 ) ) ;
#167192=CARTESIAN_POINT ( 'NONE',  ( 6.639320299308884010, -2.064767919570985821, 1.030881497364994681 ) ) ;
#167195=CARTESIAN_POINT ( 'NONE',  ( 1.598976361298432014, 1.686402000465867301, -1.184152512226148923 ) ) ;
#167197=CARTESIAN_POINT ( 'NONE',  ( 0.1575669172422279607, -0.4392406603518673736, -1.974865693180789750 ) ) ;
#167200=CARTESIAN_POINT ( 'NONE',  ( 6.702024585102262400, -1.870183347854617040, 0.04844413084104796929 ) ) ;
#167201=CARTESIAN_POINT ( 'NONE',  ( 5.097880177178074845, 1.288836597028759634, 1.412999258680311510 ) ) ;
#167203=CARTESIAN_POINT ( 'NONE',  ( 6.533804136697315634, -1.437950210024591780, -1.674183229976949905 ) ) ;
#167209=CARTESIAN_POINT ( 'NONE',  ( 6.428397668822618094, -0.9990526908794925554, -1.870407359624715937 ) ) ;
#167211=CARTESIAN_POINT ( 'NONE',  ( 3.505163243484223479, 1.820685690116738531, -1.417681053453226703 ) ) ;
#167212=CARTESIAN_POINT ( 'NONE',  ( 4.861744986159981075, -0.5251177144562025889, 1.890194517805739771 ) ) ;
#167213=CARTESIAN_POINT ( 'NONE',  ( 0.7605091544688712402, -0.6555486260201286441, -1.849146037077718852 ) ) ;
#167217=CARTESIAN_POINT ( 'NONE',  ( 0.1986506717676014555, 1.455101728037408337, -1.538369530143603559 ) ) ;
#167221=CARTESIAN_POINT ( 'NONE',  ( 3.028372864778381413, 1.157752252206078358, 1.836431199091348665 ) ) ;
#167223=CARTESIAN_POINT ( 'NONE',  ( 2.373420902723611725, -1.847293605357634982, -1.041186957106011723 ) ) ;
#167228=CARTESIAN_POINT ( 'NONE',  ( 1.809912028077927282, -2.045576594096469414, 0.2490995888081939946 ) ) ;
#167232=CARTESIAN_POINT ( 'NONE',  ( 0.07735805125224680390, 0.7159309182679198802, -2.172969595131315934 ) ) ;
#167235=CARTESIAN_POINT ( 'NONE',  ( 4.090413894173472009, -1.098427525215146749, 1.565146720495188104 ) ) ;
#167236=CARTESIAN_POINT ( 'NONE',  ( 1.335668079023267119, -2.045225487398461883, 0.9674528744543411385 ) ) ;
#167238=CARTESIAN_POINT ( 'NONE',  ( 1.230386416485089729, 1.215489027575139769, -1.343484786563201805 ) ) ;
#167240=CARTESIAN_POINT ( 'NONE',  ( 1.270553553854154361, -0.2845990055821822629, -1.894349495789057647 ) ) ;
#167241=CARTESIAN_POINT ( 'NONE',  ( 1.680221237283368696, -1.148429780529091948, -1.722445320287042447 ) ) ;
#167243=CARTESIAN_POINT ( 'NONE',  ( 0.3035114269093022732, -0.5280327476409033549, 1.899365994968700955 ) ) ;
#167244=CARTESIAN_POINT ( 'NONE',  ( 5.865835041973252117, 1.897565194821029033, -0.3318024074076031948 ) ) ;
#167245=CARTESIAN_POINT ( 'NONE',  ( 0.2238089703245670359, -0.1066217210726662923, 2.305362286893299917 ) ) ;
#167248=CARTESIAN_POINT ( 'NONE',  ( 4.299324853187779460, -1.796095115987613955, 1.014086197209535634 ) ) ;
#167255=CARTESIAN_POINT ( 'NONE',  ( 5.086996280900090817, -0.2547426189827053378, -2.090417274992136587 ) ) ;
#167258=CARTESIAN_POINT ( 'NONE',  ( 0.9069515603133030401, 0.6301693757862131262, 2.077734764916533639 ) ) ;
#167261=CARTESIAN_POINT ( 'NONE',  ( 4.886082254767631916, -1.023713625618065004, 1.903838226609423590 ) ) ;
#167262=CARTESIAN_POINT ( 'NONE',  ( 5.813150814160550794, 1.649844410012293539, -1.164645984317608463 ) ) ;
#167269=CARTESIAN_POINT ( 'NONE',  ( 3.977750132953357998, -0.7672935630990398437, 1.865046046545227654 ) ) ;
#167273=CARTESIAN_POINT ( 'NONE',  ( 4.873979933848565871, 1.241796773192262116, 1.769252301715443565 ) ) ;
#167278=CARTESIAN_POINT ( 'NONE',  ( 5.782827418265350516, 1.646828846085298448, -1.163285542026312847 ) ) ;
#167280=CARTESIAN_POINT ( 'NONE',  ( 0.8555558213108410692, 1.723155885897029282, -0.08016331026279581440 ) ) ;
#167285=CARTESIAN_POINT ( 'NONE',  ( 5.184763189090160651, -0.2277032997176874074, -1.856539885857370953 ) ) ;
#167286=CARTESIAN_POINT ( 'NONE',  ( 0.1705643940957324023, 0.7724326726834315204, 1.859191304955130297 ) ) ;
#167287=CARTESIAN_POINT ( 'NONE',  ( 6.539320575229274901, 7.053161517996441532, 2.494893549996656912 ) ) ;
#167290=CARTESIAN_POINT ( 'NONE',  ( 1.998837940877351116, -2.080155006269391205, -0.4107514010402503746 ) ) ;
#167291=CARTESIAN_POINT ( 'NONE',  ( 0.5972800738224989248, -0.2930464221381039458, 1.994874516246990748 ) ) ;
#167292=CARTESIAN_POINT ( 'NONE',  ( 1.107327745774109529, 1.372724574380719043, 1.182278994020573792 ) ) ;
#167294=CARTESIAN_POINT ( 'NONE',  ( 6.104392421991035711, -0.7735064434604683736, -2.018760209060527444 ) ) ;
#167298=CARTESIAN_POINT ( 'NONE',  ( -0.04785004733596533166, -1.249461711056678803, 1.452303129844798590 ) ) ;
#167305=CARTESIAN_POINT ( 'NONE',  ( 4.575171270262055501, 0.003154952768896768234, -2.161883445794945846 ) ) ;
#167308=CARTESIAN_POINT ( 'NONE',  ( 2.162495577681341707, 2.120227376586072854, 0.04728746717985036346 ) ) ;
#167309=CARTESIAN_POINT ( 'NONE',  ( 6.563509198815888901, 0.3086105522638155629, -1.799150958419073909 ) ) ;
#167310=CARTESIAN_POINT ( 'NONE',  ( 2.337131052746133975, -1.762546391092616238, 0.8830908230641126844 ) ) ;
#167311=CARTESIAN_POINT ( 'NONE',  ( 4.289254230599209627, -0.005406649120142519548, -1.912571728590661380 ) ) ;
#167314=CARTESIAN_POINT ( 'NONE',  ( 5.705506402468259353, -1.551454039220935055, -1.213164361648248368 ) ) ;
#167315=CARTESIAN_POINT ( 'NONE',  ( 1.851409727902778357, 1.936748846533197677, -0.1429498737708263245 ) ) ;
#167323=CARTESIAN_POINT ( 'NONE',  ( 4.934190575774549892, -1.026228162776990027, -1.613408319405706504 ) ) ;
#167325=CARTESIAN_POINT ( 'NONE',  ( 3.809358915828209735, 1.892446193107431451, 1.135094405146239049 ) ) ;
#167326=CARTESIAN_POINT ( 'NONE',  ( 2.116530880626496192, -1.040147864624408003, -1.946245422063937802 ) ) ;
#167328=CARTESIAN_POINT ( 'NONE',  ( 0.1879522776407696050, 1.101030317643518330, 1.563299796079109072 ) ) ;
#167332=CARTESIAN_POINT ( 'NONE',  ( 3.350112325975619587, -0.8415805752714689003, 1.891790567983504312 ) ) ;
#167336=CARTESIAN_POINT ( 'NONE',  ( 1.481558191429487970, 1.997200094811113491, -0.8276061316847342919 ) ) ;
#167337=CARTESIAN_POINT ( 'NONE',  ( 4.124703146219878214, 0.1084699374758208573, 2.189010777610411740 ) ) ;
#167344=CARTESIAN_POINT ( 'NONE',  ( 5.748594953515238082, 1.706903099953221759, -0.3051902176867369865 ) ) ;
#167346=CARTESIAN_POINT ( 'NONE',  ( 3.801679563076823420, -1.564429233171928058, -1.355977067927462754 ) ) ;
#167347=CARTESIAN_POINT ( 'NONE',  ( 5.132460035084068117, 0.6155034331737432307, 2.025765117643091529 ) ) ;
#167350=CARTESIAN_POINT ( 'NONE',  ( 2.957809129533952142, -0.6224678976109696560, 1.868526426519439898 ) ) ;
#167351=CARTESIAN_POINT ( 'NONE',  ( 1.054777118923880597, 0.3758132965740559883, 1.874924941132802836 ) ) ;
#167352=CARTESIAN_POINT ( 'NONE',  ( 5.050848094970262991, -1.934468200101526758, -1.229489151810001735 ) ) ;
#167353=CARTESIAN_POINT ( 'NONE',  ( 3.105874302609371362, -1.823586186413633126, 0.09019715141062728536 ) ) ;
#167359=CARTESIAN_POINT ( 'NONE',  ( 3.445567785929729343, -1.858493022056451949, 0.7744065704922193927 ) ) ;
#167360=CARTESIAN_POINT ( 'NONE',  ( 4.698074428120575519, 0.8425069249109422564, -1.771795133841248981 ) ) ;
#167363=CARTESIAN_POINT ( 'NONE',  ( 0.1755611466353811378, 5.720003923744535257, -2.838048273117784959 ) ) ;
#167364=CARTESIAN_POINT ( 'NONE',  ( 0.2750908068406934803, 1.949304727321942599, -0.7563943737528535660 ) ) ;
#167365=CARTESIAN_POINT ( 'NONE',  ( 5.770295338139614927, -1.120113875738535825, 1.370259874377998788 ) ) ;
#167367=CARTESIAN_POINT ( 'NONE',  ( 1.570551226722196381, -2.081687204081467346, -0.6850663153453034893 ) ) ;
#167368=CARTESIAN_POINT ( 'NONE',  ( -0.07713737713477014646, -1.067615817814296042, -1.374817276609247907 ) ) ;
#167370=CARTESIAN_POINT ( 'NONE',  ( 0.1335669894368317900, 1.324834237272943360, -2.404533294357531048 ) ) ;
#167371=CARTESIAN_POINT ( 'NONE',  ( 0.9258787065367773961, 1.030881334376580805, -1.382772916119678897 ) ) ;
#167372=CARTESIAN_POINT ( 'NONE',  ( 1.247910673863032116, -2.242740372501272006, -0.5020730165456227523 ) ) ;
#167373=CARTESIAN_POINT ( 'NONE',  ( 0.2752733618501881363, 2.042644424557562122, -0.7945232813236638991 ) ) ;
#167374=CARTESIAN_POINT ( 'NONE',  ( 2.508667999599442755, -0.8457060194008919618, -2.038605049697986615 ) ) ;
#167375=CARTESIAN_POINT ( 'NONE',  ( 6.654729725391004713, -0.5723678854598751586, -2.094333189781839355 ) ) ;
#167377=CARTESIAN_POINT ( 'NONE',  ( 1.323616076398025587, -1.537765720040217055, -1.455736727087880489 ) ) ;
#167379=CARTESIAN_POINT ( 'NONE',  ( 5.051747076446268636, 0.6043308924107357871, -1.829198057362067198 ) ) ;
#167381=CARTESIAN_POINT ( 'NONE',  ( 1.945279335750784711, -1.843959696387540204, -1.361743503316152681 ) ) ;
#167385=CARTESIAN_POINT ( 'NONE',  ( 4.846434531455360073, 1.142681229152305633, -1.904705486840562179 ) ) ;
#167392=VERTEX_POINT ( 'NONE', #157980 ) ;
#167393=CARTESIAN_POINT ( 'NONE',  ( 3.076796235938107138, -0.8146265060355701859, 1.844709937164576097 ) ) ;
#167395=CARTESIAN_POINT ( 'NONE',  ( 0.7431262955939599291, -0.2488486719821168813, -2.047412193126110225 ) ) ;
#167401=CARTESIAN_POINT ( 'NONE',  ( 4.084055714405177895, -2.167483682527316713, -0.3223708474724209516 ) ) ;
#167402=CARTESIAN_POINT ( 'NONE',  ( 1.846327496167538884, 0.3419342931599393398, -1.987046799686801757 ) ) ;
#167403=CARTESIAN_POINT ( 'NONE',  ( 1.346931166825489967, 0.5339940059071214273, -1.762130705996706181 ) ) ;
#167404=CARTESIAN_POINT ( 'NONE',  ( 5.829661053323575537, 1.133102282163217955, -1.992656795126966252 ) ) ;
#167405=CARTESIAN_POINT ( 'NONE',  ( 2.888418961059231904, 1.578855305991919478, -0.9468669452540460219 ) ) ;
#167407=CARTESIAN_POINT ( 'NONE',  ( 3.838725952263983388, 0.2674066485093031242, 1.805754746396167176 ) ) ;
#167408=CARTESIAN_POINT ( 'NONE',  ( 4.940077362011475515, -1.704937458037486531, -1.076318853994034930 ) ) ;
#167410=CARTESIAN_POINT ( 'NONE',  ( 4.926805006903203221, 2.163674774341369123, 0.6614253976126910350 ) ) ;
#167412=CARTESIAN_POINT ( 'NONE',  ( 6.510775453876758156, 1.563058401041140133, -1.411553977168745977 ) ) ;
#167415=CARTESIAN_POINT ( 'NONE',  ( 3.561042923925850978, 1.633862107263984065, -1.271492733312264090 ) ) ;
#167420=CARTESIAN_POINT ( 'NONE',  ( 1.770020429662170658, 0.9901332625182661662, 1.652458556229096320 ) ) ;
#167422=CARTESIAN_POINT ( 'NONE',  ( 6.948121156015312216, -0.8458062566301125518, 1.777170381402736865 ) ) ;
#167426=CARTESIAN_POINT ( 'NONE',  ( 1.318920400837508167, -0.8056321388932115024, -2.070341401348996691 ) ) ;
#167427=CARTESIAN_POINT ( 'NONE',  ( 2.801903084826493640, -0.6620233120280398786, 1.999254901717039790 ) ) ;
#167430=CARTESIAN_POINT ( 'NONE',  ( 0.8536796107712171233, -0.6749765833247187707, 1.734523287792593571 ) ) ;
#167435=CARTESIAN_POINT ( 'NONE',  ( 1.055114822555893728, 0.4192091730233596381, 2.078585086915801128 ) ) ;
#167438=CARTESIAN_POINT ( 'NONE',  ( 4.211346380768822506, -1.629847038978438079, -1.091715234301626314 ) ) ;
#167439=CARTESIAN_POINT ( 'NONE',  ( 2.905317003618158367, 1.825515667692039878, 1.157497049167732550 ) ) ;
#167440=CARTESIAN_POINT ( 'NONE',  ( 2.243484787601189634, 1.840893492186860492, 0.04347913094143729396 ) ) ;
#167444=CARTESIAN_POINT ( 'NONE',  ( 4.909954989264024405, 1.196826376938535219, -1.263709391550037031 ) ) ;
#167447=CARTESIAN_POINT ( 'NONE',  ( 2.149508875876861236, -1.735919364271593768, -1.288018159417112729 ) ) ;
#167448=CARTESIAN_POINT ( 'NONE',  ( 3.163435312993330140, -0.5825663732807913053, -1.930122257003751063 ) ) ;
#167449=CARTESIAN_POINT ( 'NONE',  ( 0.8312129145573650124, 0.1600495679085281175, 2.155820468135719814 ) ) ;
#167450=CARTESIAN_POINT ( 'NONE',  ( 3.186357099593698283, -1.942036093696447363, -0.3385421596419062595 ) ) ;
#167452=CARTESIAN_POINT ( 'NONE',  ( 6.509000000000010999, 0.007656933339201045172, 1.900274884395843245 ) ) ;
#167453=CARTESIAN_POINT ( 'NONE',  ( 3.491681510897004959, -1.939965067831977530, -0.09248793024771610749 ) ) ;
#167463=CARTESIAN_POINT ( 'NONE',  ( 6.633790087849154027, -1.500048720590658302, -1.753619728580549708 ) ) ;
#167465=CARTESIAN_POINT ( 'NONE',  ( 4.451973756923766068, -0.7546651901383871763, 1.810992078419524365 ) ) ;
#167466=CARTESIAN_POINT ( 'NONE',  ( 1.705704151892040832, 1.882474636155605507, 0.7231385473688843879 ) ) ;
#167468=CARTESIAN_POINT ( 'NONE',  ( 3.714152660773429648, 1.129254856714853261, -1.790882643308453703 ) ) ;
#167470=CARTESIAN_POINT ( 'NONE',  ( 0.07459516483344308391, 2.893589955008399883, -2.244599473808198020 ) ) ;
#167472=CARTESIAN_POINT ( 'NONE',  ( 3.363068133243895197, 1.796009578954290253, -0.4044003374430102382 ) ) ;
#167477=CARTESIAN_POINT ( 'NONE',  ( 4.851869265964163347, -1.501451181749386743, -1.497782127133556518 ) ) ;
#167478=CARTESIAN_POINT ( 'NONE',  ( 6.825078400183573812, 0.002648415797040087893, 1.855566311045192540 ) ) ;
#167480=CARTESIAN_POINT ( 'NONE',  ( 5.430957059787441032, 0.1471976826952873518, 2.055563341089384988 ) ) ;
#167482=CARTESIAN_POINT ( 'NONE',  ( 0.3966288646398182238, 0.3121968076400126746, 1.834509442227350462 ) ) ;
#167483=CARTESIAN_POINT ( 'NONE',  ( 2.489598673502769977, -1.836455140896048999, -0.1334285330320400531 ) ) ;
#167488=CARTESIAN_POINT ( 'NONE',  ( 2.473496279428960776, 0.1070396533628548558, -2.204406164007084445 ) ) ;
#167489=CARTESIAN_POINT ( 'NONE',  ( 5.220128827380259295, -1.204132088723122385, -1.915181361845545105 ) ) ;
#167491=CARTESIAN_POINT ( 'NONE',  ( 4.851724922005476337, -1.286371495869711667, -1.275854292049487304 ) ) ;
#167492=CARTESIAN_POINT ( 'NONE',  ( 3.661272352971048694, 1.801931492627879106, -0.6507149165355142761 ) ) ;
#167494=CARTESIAN_POINT ( 'NONE',  ( 4.381683959536594841, 1.286834623079432083, 1.493660651562748853 ) ) ;
#167495=CARTESIAN_POINT ( 'NONE',  ( 5.119927267529915227, -1.001353885182048931, -1.579878405157906673 ) ) ;
#167496=CARTESIAN_POINT ( 'NONE',  ( 5.160548226176637776, -0.6268552802725676498, -1.752456121274186263 ) ) ;
#167497=CARTESIAN_POINT ( 'NONE',  ( -0.04763828917917976857, -1.313539345393003321, 1.530161206715647149 ) ) ;
#167499=CARTESIAN_POINT ( 'NONE',  ( 2.104260374134783174, -2.105582044810641484, 0.05271062337313356383 ) ) ;
#167504=CARTESIAN_POINT ( 'NONE',  ( 2.953504815971871977, -1.868289524550557523, 1.003269902519101864 ) ) ;
#167506=CARTESIAN_POINT ( 'NONE',  ( 2.039325177177089721, 0.004250232316239943575, 2.019972748817438823 ) ) ;
#167512=CARTESIAN_POINT ( 'NONE',  ( 2.126461914815626297, 1.246462439515462650, -1.765816729463750123 ) ) ;
#167513=CARTESIAN_POINT ( 'NONE',  ( 6.609999999999973674, -0.005249217919313375023, 2.280159464062641916 ) ) ;
#167519=CARTESIAN_POINT ( 'NONE',  ( 1.435386855117400717, -1.590506285900999295, -1.507976327226906443 ) ) ;
#167521=CARTESIAN_POINT ( 'NONE',  ( 1.200488511320395579, -2.262689073810118412, 0.002107776778791786276 ) ) ;
#167528=CARTESIAN_POINT ( 'NONE',  ( 3.949580097687496405, 0.5788178622721011912, -1.624998464860913705 ) ) ;
#167530=CARTESIAN_POINT ( 'NONE',  ( 1.616075582413665002, 1.193477697079999178, -1.306907023524202183 ) ) ;
#167532=CARTESIAN_POINT ( 'NONE',  ( 5.157340341976529352, -1.861842412690998039, -1.184373046124863160 ) ) ;
#167534=CARTESIAN_POINT ( 'NONE',  ( 4.517835093568582927, -0.5347929126107499043, 1.947652422195633504 ) ) ;
#167536=CARTESIAN_POINT ( 'NONE',  ( 4.780875152847498200, 1.674876996157638187, -1.122516304564516565 ) ) ;
#167538=CARTESIAN_POINT ( 'NONE',  ( 2.676452114398766291, -1.789519730395791486, -0.5449050523786898026 ) ) ;
#167541=CARTESIAN_POINT ( 'NONE',  ( 1.617294888471169312, 1.591762500684265946, 1.059657513450793953 ) ) ;
#167547=CARTESIAN_POINT ( 'NONE',  ( 0.2988868148526523383, -0.2362956723594503705, -1.897694653714178781 ) ) ;
#167549=CARTESIAN_POINT ( 'NONE',  ( 2.172246964874047670, -0.9220853831424129510, -1.731647142839589648 ) ) ;
#167552=CARTESIAN_POINT ( 'NONE',  ( 5.519825572852568030, -0.5132647233585425628, 2.057443900658859182 ) ) ;
#167555=CARTESIAN_POINT ( 'NONE',  ( 0.3329892237508432773, -1.712944741146247063, 0.7519245212838022718 ) ) ;
#167558=CARTESIAN_POINT ( 'NONE',  ( 0.7912717950901988484, -0.05365516122857225123, -2.012662812414119706 ) ) ;
#167560=CARTESIAN_POINT ( 'NONE',  ( 0.6502104730865595483, 1.047635159188778031, 1.839821444870335165 ) ) ;
#167562=CARTESIAN_POINT ( 'NONE',  ( 2.805202726412972858, -1.722705984639979704, 1.148039668612794051 ) ) ;
#167566=CARTESIAN_POINT ( 'NONE',  ( 4.558587588987070838, -1.867386427489168055, -0.9401465391167336261 ) ) ;
#167568=CARTESIAN_POINT ( 'NONE',  ( 2.555444900642935391, 0.4891320457309326075, -1.758753460580727790 ) ) ;
#167569=CARTESIAN_POINT ( 'NONE',  ( 3.035611470257699285, -1.745090209790541191, 0.4855505718092138490 ) ) ;
#167571=CARTESIAN_POINT ( 'NONE',  ( 6.182275136424624229, -1.184133725572718676, 1.862117674348878760 ) ) ;
#167574=CARTESIAN_POINT ( 'NONE',  ( 5.825267882404531861, -0.05969703229705652925, 2.206138628428089277 ) ) ;
#167577=CARTESIAN_POINT ( 'NONE',  ( 3.510326737904199135, -1.910220267131033323, -0.09114558060911714943 ) ) ;
#167587=CARTESIAN_POINT ( 'NONE',  ( 3.426877311086639288, 0.04264493303338459662, 1.870215716092846314 ) ) ;
#167589=CARTESIAN_POINT ( 'NONE',  ( -0.2409995289980224054, 7.629137130509101361, -2.600476469121244527 ) ) ;
#167594=CARTESIAN_POINT ( 'NONE',  ( 0.5847281401991512029, 1.882922653073782815, 0.5772291209212175866 ) ) ;
#167595=CARTESIAN_POINT ( 'NONE',  ( 0.9840001696646907270, -2.016598147255070472, 0.002831364411433334727 ) ) ;
#167599=CARTESIAN_POINT ( 'NONE',  ( 0.9904705247469265394, -0.5356807779838267392, -2.124848333686576662 ) ) ;
#167600=CARTESIAN_POINT ( 'NONE',  ( 6.270122753791413928, 0.9430518052575274091, 1.563124558401955300 ) ) ;
#167608=CARTESIAN_POINT ( 'NONE',  ( 3.614658571667620279, -0.1319153736358945894, 1.836568937333193485 ) ) ;
#167609=CARTESIAN_POINT ( 'NONE',  ( 0.5748582965167781111, -1.456639466575420538, 1.389732462146851200 ) ) ;
#167610=CARTESIAN_POINT ( 'NONE',  ( 2.917634960997887994, 0.7719352619847442698, 2.165007881682521784 ) ) ;
#167612=CARTESIAN_POINT ( 'NONE',  ( 0.9185399124422718442, -1.353032588479759157, 1.277947871810279246 ) ) ;
#167616=CARTESIAN_POINT ( 'NONE',  ( 4.763870730211980487, 0.5944114921396548290, -1.817767169311027997 ) ) ;
#167620=CARTESIAN_POINT ( 'NONE',  ( 3.579701903670178709, -1.028438467219190411, 1.820211688285853446 ) ) ;
#167621=CARTESIAN_POINT ( 'NONE',  ( 1.902992089709685031, 1.553661375375714471, 1.041555772207984676 ) ) ;
#167624=CARTESIAN_POINT ( 'NONE',  ( 2.665247472508886606, 0.9327722559238416089, 1.469172323213832065 ) ) ;
#167626=CARTESIAN_POINT ( 'NONE',  ( 4.353923116202039978, 1.724447095217627401, -0.04574849716902986557 ) ) ;
#167628=CARTESIAN_POINT ( 'NONE',  ( 4.159861740090546434, 1.033864333764370702, 1.932389678422803181 ) ) ;
#167629=CARTESIAN_POINT ( 'NONE',  ( 6.041676539500916654, -1.595688354349385607, -1.524751901930617715 ) ) ;
#167631=CARTESIAN_POINT ( 'NONE',  ( 3.995131740874768411, 0.3131294011963717816, 2.148239739743092347 ) ) ;
#167632=CARTESIAN_POINT ( 'NONE',  ( 2.139018802738294589, -1.631172329757241801, 0.8201644002571031322 ) ) ;
#167634=CARTESIAN_POINT ( 'NONE',  ( 5.155504860159462410, 2.039786097693491396, -0.5674642188294597434 ) ) ;
#167636=CARTESIAN_POINT ( 'NONE',  ( 5.970342212645192603, -2.175549559325986149, -0.7227481681704952532 ) ) ;
#167639=CARTESIAN_POINT ( 'NONE',  ( 1.049659257133638945, -1.915429643647760249, 0.9100379840868355608 ) ) ;
#167646=CARTESIAN_POINT ( 'NONE',  ( 1.735333443468607184, 2.074102030253548445, 0.7956244722606919950 ) ) ;
#167648=CARTESIAN_POINT ( 'NONE',  ( 6.100232455412330168, -0.2440331339308223768, 2.001510902166554473 ) ) ;
#167650=CARTESIAN_POINT ( 'NONE',  ( 4.469619655223175947, -0.3576850913847802182, 2.031185480813563426 ) ) ;
#167652=CARTESIAN_POINT ( 'NONE',  ( -0.2409995289980246258, 1.355929887833319469, -2.254219809973062816 ) ) ;
#167656=CARTESIAN_POINT ( 'NONE',  ( 0.5684512833941969268, -1.969177116664261762, -0.7025944222667882544 ) ) ;
#167657=CARTESIAN_POINT ( 'NONE',  ( 4.729138786257041538, 2.011204126674607462, 0.1455352507326590494 ) ) ;
#167658=CARTESIAN_POINT ( 'NONE',  ( 4.071694929070113211, -1.056692140236010102, 1.507659738195665788 ) ) ;
#167660=CARTESIAN_POINT ( 'NONE',  ( 1.008351294761783423, 1.310062561100222123, -1.121974927168223335 ) ) ;
#167661=CARTESIAN_POINT ( 'NONE',  ( -0.2351498743046881446, -0.1506043639611966134, -1.983733596389973597 ) ) ;
#167662=CARTESIAN_POINT ( 'NONE',  ( 1.266696122786495904, 2.121433860451333420, -0.8855928530677835697 ) ) ;
#167664=CARTESIAN_POINT ( 'NONE',  ( 1.142281600899584193, 0.9165754381605104584, -2.068608644781688710 ) ) ;
#167665=CARTESIAN_POINT ( 'NONE',  ( 3.123755640277770418, -2.029568314945415786, 0.5621985482912382759 ) ) ;
#167669=CARTESIAN_POINT ( 'NONE',  ( 6.593749840436431420, -1.895867669153237456, -0.7852924748296338242 ) ) ;
#167674=CARTESIAN_POINT ( 'NONE',  ( 5.449557989901563815, -2.008192194917140849, 0.9499826718327757380 ) ) ;
#167675=CARTESIAN_POINT ( 'NONE',  ( 3.873126987144244193, 2.063651454400210028, -0.7377723227853100196 ) ) ;
#167677=EDGE_CURVE ( 'NONE', #15524, #65102, #147984, .T. ) ;
#167679=CARTESIAN_POINT ( 'NONE',  ( 5.635196431686764207, -0.04651148872366302894, -1.961470878453225763 ) ) ;
#167681=CARTESIAN_POINT ( 'NONE',  ( 6.890000000000005898, 2.048573291599069091, 2.305811639209849773 ) ) ;
#167683=CARTESIAN_POINT ( 'NONE',  ( 4.746395313581045272, 1.087821826000658909, -1.820160695957805608 ) ) ;
#167688=CARTESIAN_POINT ( 'NONE',  ( 4.827609030688454261, 0.9420861819694618111, -1.581835861328761528 ) ) ;
#167692=CARTESIAN_POINT ( 'NONE',  ( 1.223704041615133464, 1.677047869609141983, 0.4652235607782040372 ) ) ;
#167696=CARTESIAN_POINT ( 'NONE',  ( 5.770447993230207295, -1.374857387916775364, 1.668144713590607120 ) ) ;
#167700=CARTESIAN_POINT ( 'NONE',  ( 4.926735330553584369, 2.067573386176469796, 0.6309256262674377558 ) ) ;
#167702=CARTESIAN_POINT ( 'NONE',  ( 5.184826486558015368, -0.2386506126292788632, -1.956774853079599197 ) ) ;
#167703=CARTESIAN_POINT ( 'NONE',  ( 4.112396791320716005, 0.5851491843551993588, -1.632232688200731197 ) ) ;
#167705=CARTESIAN_POINT ( 'NONE',  ( 1.259612756803454525, 2.158328104161820526, -0.3793702838810895095 ) ) ;
#167706=CARTESIAN_POINT ( 'NONE',  ( 2.274872074667996458, -1.419342104801555982, 1.819364073307845997 ) ) ;
#167707=CARTESIAN_POINT ( 'NONE',  ( 4.639950097937448170, 0.8846809987467202374, -1.861387103252240660 ) ) ;
#167708=CARTESIAN_POINT ( 'NONE',  ( 6.409718653046240000, -0.9196952807892575521, -1.710506293091022201 ) ) ;
#167714=CARTESIAN_POINT ( 'NONE',  ( 1.213517774399593740, 1.944071949784083264, 0.5350861613380719639 ) ) ;
#167716=CARTESIAN_POINT ( 'NONE',  ( 3.434799832723956836, 2.152550277175222515, 0.4854691814954179563 ) ) ;
#167718=CARTESIAN_POINT ( 'NONE',  ( 1.305250306655120207, -1.462593314309963866, -1.150481100809984891 ) ) ;
#167719=( BOUNDED_CURVE ( )  B_SPLINE_CURVE ( 3, ( #114762, #164515, #35564, #165577 ),
 .UNSPECIFIED., .F., .T. ) 
 B_SPLINE_CURVE_WITH_KNOTS ( ( 4, 4 ),
 ( 0.4999999999999995004, 1.000000000000000000 ),
 .UNSPECIFIED. ) 
 CURVE ( )  GEOMETRIC_REPRESENTATION_ITEM ( )  RATIONAL_B_SPLINE_CURVE ( ( 1.000000000000000444, 0.3333333333333333148, 0.3333333333333326487, 1.000000000000000000 ) ) 
 REPRESENTATION_ITEM ( '' )  );
#167724=CARTESIAN_POINT ( 'NONE',  ( 6.925078400183537042, 4.686282476709005884, 2.806848198465234479 ) ) ;
#167725=CARTESIAN_POINT ( 'NONE',  ( 6.597600327481837112, -1.840612352326329804, 0.05063316525460298534 ) ) ;
#167727=CARTESIAN_POINT ( 'NONE',  ( 3.256764320543267921, -1.561506546599530143, 1.345091337369247242 ) ) ;
#167730=CARTESIAN_POINT ( 'NONE',  ( 1.893228994919902153, -0.1012422250811425839, -2.017274448259358977 ) ) ;
#167733=CARTESIAN_POINT ( 'NONE',  ( 2.465760480296646850, 2.021364445465044124, -0.4007626210408669620 ) ) ;
#167738=CARTESIAN_POINT ( 'NONE',  ( -0.2409995289980003397, 0.7158067089181943121, -2.082568332340509087 ) ) ;
#167740=CARTESIAN_POINT ( 'NONE',  ( 5.514374426699260923, -0.9893691592960799364, -1.972764877262770833 ) ) ;
#167742=CARTESIAN_POINT ( 'NONE',  ( 1.317891493549529391, -2.109231647155560108, 0.4722262556789079135 ) ) ;
#167744=CARTESIAN_POINT ( 'NONE',  ( 2.061732777098632230, 1.244387006429502396, 1.586668050434843158 ) ) ;
#167745=CARTESIAN_POINT ( 'NONE',  ( 2.267358445155386981, -2.297842707097216053, 0.05573287391750710029 ) ) ;
#167748=CARTESIAN_POINT ( 'NONE',  ( 2.377632874612686020, 1.149002834218125102, 1.476114537088555112 ) ) ;
#167750=CARTESIAN_POINT ( 'NONE',  ( 3.151577601795185757, 1.966304690962265234, -0.4465026806126579095 ) ) ;
#167753=CARTESIAN_POINT ( 'NONE',  ( 5.637368906844186789, -1.904612104999114708, 0.8991850809280316215 ) ) ;
#167757=CARTESIAN_POINT ( 'NONE',  ( 6.539320575229280230, 7.629137130509070275, 2.703262396134015866 ) ) ;
#167758=CARTESIAN_POINT ( 'NONE',  ( 5.010023637874760460, -0.7231455074051349463, 1.886094130455595375 ) ) ;
#167762=CARTESIAN_POINT ( 'NONE',  ( 1.164971494057164492, 1.564520514315300481, -1.344193796132137964 ) ) ;
#167770=CARTESIAN_POINT ( 'NONE',  ( 3.315042099977282497, -1.646035655820307309, 1.415953490726479469 ) ) ;
#167772=CARTESIAN_POINT ( 'NONE',  ( 1.364538772237647413, 0.1349417713633893900, -1.836341338755695940 ) ) ;
#167775=B_SPLINE_CURVE_WITH_KNOTS ( 'NONE', 3,
 ( #152088, #3658, #125003, #141212, #159548, #92450, #62060, #143341, #111943, #209335, #107668, #109807, #175816, #177945, #58847, #27409, #157434, #145485, #77222, #93507, #11145, #210418, #9027, #108735, #78289, #76162, #79367, #173696, #158489, #60983, #127137, #193109, #128215, #29559, #25272, #28483, #211481, #10088, #44758, #142267, #26336, #75102, #110865, #91374, #176871, #94574, #42625, #174763, #45822, #95650, #207223, #160617, #12218, #161701, #208278, #59910, #63117, #144416, #126064, #194177, #190960, #192027, #43690, #13294, #129282, #195256, #68419, #81500, #32745, #164877, #16472, #15409, #146534, #18613, #100932, #147578, #34857, #167019, #130333, #165946, #82552, #132423, #47966, #30632, #196322, #162767, #212551, #150780, #114082, #50068, #17530, #213597, #80434, #199487, #149701, #14345, #180073, #83619, #65221, #84692, #113006, #182176, #131373, #116191, #33805, #1282, #197369, #148639, #99884, #134546, #205, #49011, #2342, #31696, #64192, #67340, #179016, #98828, #133485, #97771, #163831, #46892, #96718, #198424, #51133, #115130, #181125, #66275, #117254, #183254, #201610, #203747, #200550, #151839, #85759, #204812, #88977, #56463, #53260, #169137, #22864, #104154, #170202, #20732, #3416, #172351, #40219, #86827, #188586, #106328, #69482, #105230, #21786, #72697, #35933, #152891, #135590, #137728, #54334, #87895, #5535, #52197, #155032, #7689, #119390, #171270, #55392, #138792, #122625, #23941, #6617, #118323, #73772, #184309, #90045, #71615, #4469, #121547, #185378, #102011, #120473, #202685, #153968, #136660, #187518, #156103, #186445, #168081, #19679, #39149, #36998, #38082, #103081, #70541, #193915, #191774, #45562, #190708, #176614, #94319, #61794, #43430, #124748, #160360, #175558, #144160, #27149, #13022, #41303, #142012, #93253, #75909, #159287, #110614, #208027, #107411, #189652, #10886, #76961, #59655, #143087, #125812, #11963, #95390, #29296, #42369, #173434, #157175, #25014, #109554, #108480, #78036, #209080, #210152, #60717, #139868, #126880, #192838, #127962, #91116, #44497, #28226, #111678, #174504, #8769, #177685, #161441, #74852, #140951, #205899, #26080, #57533, #123690, #92195, #206964, #58593, #158243, #9833, #1017, #79099, #214382, #166755, #197111, #113814, #50869, #80167, #194988, #82287, #211223, #131123, #66012, #14077, #146273, #17274, #67081, #145217, #164620, #132161, #133216, #130074, #63918, #162507, #112744, #49800, #198167, #179814, #62849, #129011, #32485, #115926, #181914, #100677, #31433, #64969, #48750, #114863, #47700, #178757, #116991, #199222, #97510, #46623, #30369, #163568, #83350, #180864, #16205, #98559, #81237, #148381, #33546, #212284, #147319, #96456, #196069, #99619, #15151, #213346, #165685, #149435, #182991, #34608, #122363, #18351, #39960, #6356, #202416, #103891, #119128, #169939, #35671, #3148, #21523, #52992, #151581, #167816, #136400, #38883, #118066, #102820, #104968, #19416, #171009, #72426, #84429, #87635, #5275, #138528, #69218, #135337, #188319, #153706, #85494, #71352, #150518, #184052, #101749, #22606, #121280, #88714, #201351, #185108, #4215, #54071, #120206, #36733, #168875, #204551, #56200, #20479, #106067, #2079, #86566, #137468, #186181, #154773, #68152, #152628, #70284, #203482, #37815, #55135, #134286, #200291, #187256, #51942, #173171 ),
 .UNSPECIFIED., .F., .F.,
 ( 4, 1, 1, 1, 1, 1, 1, 1, 1, 1, 1, 1, 1, 1, 1, 1, 1, 1, 1, 1, 1, 1, 1, 1, 1, 1, 1, 1, 1, 1, 1, 1, 1, 1, 1, 1, 1, 1, 1, 1, 1, 1, 1, 1, 1, 1, 1, 1, 1, 1, 1, 1, 1, 1, 1, 1, 1, 1, 1, 1, 1, 1, 1, 1, 1, 1, 1, 1, 1, 1, 1, 1, 1, 1, 1, 1, 1, 1, 1, 1, 1, 1, 1, 1, 1, 1, 1, 1, 1, 1, 1, 1, 1, 1, 1, 1, 1, 1, 1, 1, 1, 1, 1, 1, 1, 1, 1, 1, 1, 1, 1, 1, 1, 1, 1, 1, 1, 1, 1, 1, 1, 1, 1, 1, 1, 1, 1, 1, 1, 1, 1, 1, 1, 1, 1, 1, 1, 1, 1, 1, 1, 1, 1, 1, 1, 1, 1, 1, 1, 1, 1, 1, 1, 1, 1, 1, 1, 1, 1, 1, 1, 1, 1, 1, 1, 1, 1, 1, 1, 1, 1, 1, 1, 1, 1, 1, 1, 1, 1, 1, 1, 1, 1, 1, 1, 1, 1, 1, 1, 1, 1, 1, 1, 1, 1, 1, 1, 1, 1, 1, 1, 1, 1, 1, 1, 1, 1, 1, 1, 1, 1, 1, 1, 1, 1, 1, 1, 1, 1, 1, 1, 1, 1, 1, 1, 1, 1, 1, 1, 1, 1, 1, 1, 1, 1, 1, 1, 1, 1, 1, 1, 1, 1, 1, 1, 1, 1, 1, 1, 1, 1, 1, 1, 1, 1, 1, 1, 1, 1, 1, 1, 1, 1, 1, 1, 1, 1, 1, 1, 1, 1, 1, 1, 1, 1, 1, 1, 1, 1, 1, 1, 1, 1, 1, 1, 1, 1, 1, 1, 1, 1, 1, 1, 1, 1, 1, 1, 1, 1, 1, 1, 1, 1, 1, 1, 1, 1, 1, 1, 1, 1, 1, 1, 1, 1, 1, 1, 1, 1, 1, 1, 1, 1, 1, 1, 1, 1, 1, 1, 1, 1, 1, 1, 1, 1, 1, 1, 1, 1, 1, 1, 1, 1, 1, 1, 1, 1, 1, 1, 1, 1, 1, 1, 1, 1, 1, 1, 1, 1, 1, 1, 1, 1, 1, 1, 1, 1, 1, 1, 1, 1, 1, 1, 1, 1, 1, 1, 1, 1, 1, 1, 1, 1, 1, 4 ),
 ( 0.000000000000000000, 0.002599888508634240914, 0.005208754120092145765, 0.007813069968323356138, 0.01041690100177071650, 0.01302019566086259385, 0.01562517182793091500, 0.01822893254318404960, 0.02083328139698771564, 0.02343764900838959594, 0.02604139750447371365, 0.02864615928571910553, 0.03124958462592061434, 0.03385442086835698666, 0.03645794792899405279, 0.03906256697173399878, 0.04166661757251870907, 0.04427067912273281725, 0.04687528696281444140, 0.04947881815967773017, 0.05208365228821221909, 0.05468707701066444909, 0.05729184299815447134, 0.05989557646906591704, 0.06249996333325048142, 0.06510433798480201595, 0.06770807906337909798, 0.07031283757201339801, 0.07291626355048291819, 0.07552109983967189577, 0.07812462590386089201, 0.08072924387304455940, 0.08333329402460390445, 0.08593735478041557296, 0.08854196204427712547, 0.09114549249794960672, 0.09375032597506528786, 0.09635375006294695510, 0.09895851527076646170, 0.1015622481948881828, 0.1041666342325376776, 0.1067710083972730206, 0.1093747487337090180, 0.1119795066911244419, 0.1145829320296284648, 0.1171877676425944481, 0.1197912931610935483, 0.1223959103579086161, 0.1249999600491941698, 0.1276040200539713398, 0.1302086268569593308, 0.1328121566649932417, 0.1354169895755736042, 0.1380204131161003600, 0.1406251776355303407, 0.1432289101024236955, 0.1458332954032181272, 0.1484376691708411133, 0.1510414088543486633, 0.1536461663508109643, 0.1562495911381983071, 0.1588544261652600487, 0.1614579512270202244, 0.1640625677415503691, 0.1666666170620310916, 0.1692706764052687440, 0.1718752828374313091, 0.1744788120887783289, 0.1770836445231302458, 0.1796870676051354199, 0.1822918315264069888, 0.1848955636252137269, 0.1874999482789682093, 0.1901043217392619777, 0.1927080608589964439, 0.1953128179847096746, 0.1979162423098047296, 0.2005210768412587219, 0.2031246015352002054, 0.2057292174574958665, 0.2083332664966131842, 0.2109373252677763377, 0.2135419314191336626, 0.2161454602027163274, 0.2187502922511180836, 0.2213537149634070833, 0.2239584783767220588, 0.2265622101965570623, 0.2291665942930569411, 0.2317709675357785548, 0.2343747061808670040, 0.2369794630260087243, 0.2395828869776091552, 0.2421877211037245237, 0.2447912455187418734, 0.2473958609388257068, 0.2499999097859964270, 0.2526039680745227334, 0.2552085740350705789, 0.2578121024397855843, 0.2604169341924902348, 0.2630203566238439872, 0.2656251196193780695, 0.2682288512493328225, 0.2708332348783377697, 0.2734376079932215875, 0.2760413462527663842, 0.2786461029074911444, 0.2812495265743710227, 0.2838543603853929120, 0.2864578846103582599, 0.2890624996182282747, 0.2916665483628478883, 0.2942706062581511572, 0.2968752121178640513, 0.2994787402325856385, 0.3020835717798243114, 0.3046869940190023440, 0.3072917566869088346, 0.3098954882160545599, 0.3124998714673014044, 0.3151042445440625506, 0.3177079825071445485, 0.3203127390615869707, 0.3229161625325003282, 0.3255209961186533163, 0.3281245202424198926, 0.3307291349280532256, 0.3333331836594992104, 0.3359372412509727956, 0.3385418470998076690, 0.3411453750133909280, 0.3437502064453764050, 0.3463536285811206206, 0.3489583910115333087, 0.3515621225289245477, 0.3541665054921307454, 0.3567708786204680238, 0.3593746163761498691, 0.3619793729204284771, 0.3645827962841124981, 0.3671876297356038710, 0.3697911538470093351, 0.3723957683003653041, 0.3749998171080005105, 0.3776038744850206963, 0.3802084804129200468, 0.3828120082142042468, 0.3854168396211344327, 0.3880202617421720235, 0.3906250240252089334, 0.3932287556198868494, 0.3958331383847540352, 0.3984375116543538153, 0.4010412492916836102, 0.4036460059159037717, 0.4062494292610819846, 0.4088542626681055392, 0.4114577868559751161, 0.4140624011669984950, 0.4166664501401745602, 0.4192705073921035863, 0.4218751134889988097, 0.4244786412668108966, 0.4270834727388717056, 0.4296868949339185950, 0.4322916571596854274, 0.4348953889206810253, 0.4374997715768980666, 0.4401041450774376140, 0.4427078826854516369, 0.4453126394797092824, 0.4479160628950952239, 0.4505208963478340434, 0.4531244207009840763, 0.4557290349596088697, 0.4583330841876695483, 0.4609371414038593850, 0.4635417477596745495, 0.4661452756028321986, 0.4687501072302013849, 0.4713535295879656695, 0.4739582918465587991, 0.4765620238628961447, 0.4791664065001429718, 0.4817707803212932793, 0.4843745179890200370, 0.4869792750434049911, 0.4895826986177053142, 0.4921875322063354874, 0.4947910568135764908, 0.4973956711097291539, 0.4999997206820134821, 0.5026037779518089943, 0.5052083846564635605, 0.5078119126537786743, 0.5104167445266291070, 0.5130201671358142201, 0.5156249295173244152, 0.5182286618780244103, 0.5208330445859747915, 0.5234374188174044651, 0.5260411566338674128, 0.5286459140384663913, 0.5312493378603841965, 0.5338541716750782040, 0.5364576966252184720, 0.5390623110488209635, 0.5416663610546670338, 0.5442704184674093115, 0.5468750256108222407, 0.5494785538511040013, 0.5520833860596070508, 0.5546868090089153158, 0.5572915716034309019, 0.5598953043975141153, 0.5624996872658396541, 0.5651040619972180767, 0.5677078000514395040, 0.5703125578963399445, 0.5729159820545779436, 0.5755208161855079885, 0.5781243415673570363, 0.5807289562083304268, 0.5833330067370782190, 0.5859370643821081304, 0.5885416720542003821, 0.5911452006262593040, 0.5937500332605881725, 0.5963534566387238556, 0.5989582195363342132, 0.6015619528528246551, 0.6041663359711972880, 0.6067707112921981727, 0.6093744496732020899, 0.6119792080484952601, 0.6145826326317597177, 0.6171874671691013337, 0.6197909930714722293, 0.6223956080197403651, 0.6249996591607356322, 0.6276037171273963766, 0.6302083254180952387, 0.6328118544107458332, 0.6354166875610788301, 0.6380201114567515264, 0.6406248747475506988, 0.6432286086754787080, 0.6458329921335752566, 0.6484373681338796436, 0.6510411069306952792, 0.6536458659264798854, 0.6562492910234830612, 0.6588541260574176661, 0.6614576525691320263, 0.6640622679146246377, 0.6666663197572214594, 0.6692703781348633418, 0.6718749871341050950, 0.6744785166361690898, 0.6770833503926931840, 0.6796867748946214816, 0.6822915386687108397, 0.6848952732971168578, 0.6874996571846213600, 0.6901040339539210589, 0.6927077732555863010, 0.6953125329619718187, 0.6979159586614360755, 0.7005207942821553013, 0.7031243214920454010, 0.7057289373247008779, 0.7083329899582661016, 0.7109370488362486418, 0.7135416586339821121, 0.7161451887342924483, 0.7187500231872065992, 0.7213534483841206324, 0.7239582127316128712, 0.7265619481495508847, 0.7291663325561579256, 0.7317707101841592898, 0.7343744500797240171, 0.7369792105868335774, 0.7395826369774940456, 0.7421874732752028470, 0.7447910012721150608, 0.7473956176818850050, 0.7499996711958007989, 0.7526037306634962842, 0.7552083413496862851, 0.7578118721370898925, 0.7604167073766084917, 0.7630201333572542710, 0.7656248983682768516, 0.7682286346648167230, 0.7708330196802359868, 0.7734373982566630223, 0.7760411388351919904, 0.7786459002331664880, 0.7812493274037752844, 0.7838541644686951582, 0.7864576933414935134, 0.7890623104183455139, 0.7916663649020125870, 0.7942704250488100692, 0.7968750367134410650, 0.7994785682768023038, 0.8020834043931583945, 0.8046868312463003603, 0.8072915970109983963, 0.8098953342752303053, 0.8124997199891885735, 0.8151040996037859365, 0.8177078409543626636, 0.8203126033333638656, 0.8229160313726919806, 0.8255208692950642968, 0.8281243991326340259, 0.8307290169665545454, 0.8333330725093962554, 0.8359371334247044372, 0.8385417461577832077, 0.8411452785859873105, 0.8437501156694361404, 0.8463535434838604932, 0.8489583100924004144, 0.8515620484134380774, 0.8541664349156833369, 0.8567708156582201084, 0.8593745578699503174, 0.8619793213201638604, 0.8645827503170061545, 0.8671875891870957087, 0.8697911200783463581, 0.8723957387593448409, 0.8749997954508100806, 0.8776038572240605351, 0.8802084711156200614, 0.8828120044975765746, 0.8854168426383988155, 0.8880202715029178462, 0.8906250390454908406, 0.8932287785124739532, 0.8958331658927787267, 0.8984375478530519654, 0.9010412910150662480, 0.9036460556267057465, 0.9062494856698833923, 0.9088543255779816255, 0.9114578576118502751, 0.9140624772299625889, 0.9166665351595286726, 0.9192705978801787303, 0.9218752130202838568, 0.9244787474449313036, 0.9270835867334279445, 0.9296870167368762594, 0.9322917853037333558, 0.9348955260058576799, 0.9374999143539141100, 0.9401042976215825409, 0.9427080418234272674, 0.9453128076877782560, 0.9479162388645026027, 0.9505210798953250828, 0.9531246131693177359, 0.9557292338404025367, 0.9583332930514818493, 0.9609373567081632705, 0.9635419734050364449, 0.9661455093234165847, 0.9687503490003109841, 0.9713537788664922124, 0.9739585512809396661, 0.9765622998769101226, 0.9791666815729623830, 0.9817710277688282972, 0.9843747994658795797, 0.9869797739623470401, 0.9895830763955310028, 0.9921869177308453303, 0.9947912343601759133, 0.9974001139318913189, 1.000000000000000000 ),
 .UNSPECIFIED. ) ;
#167776=CARTESIAN_POINT ( 'NONE',  ( 4.669572502782517454, 1.262004115398765780, 1.791526714441132873 ) ) ;
#167777=CARTESIAN_POINT ( 'NONE',  ( 6.983263157960333700, 2.949816178198962024, 2.606004571833001382 ) ) ;
#167778=CARTESIAN_POINT ( 'NONE',  ( 5.155258101147136784, -1.908469616433384086, -1.214953784003909520 ) ) ;
#167785=CARTESIAN_POINT ( 'NONE',  ( 4.973781575966475188, 1.018845774273930749, 1.446830399915491006 ) ) ;
#167786=CARTESIAN_POINT ( 'NONE',  ( 3.264317399697822530, 2.013265973121576291, -0.002229150246490021157 ) ) ;
#167788=CARTESIAN_POINT ( 'NONE',  ( 1.659346488253128804, -1.806016679666972546, -1.082987972701171309 ) ) ;
#167789=CARTESIAN_POINT ( 'NONE',  ( 0.9310837752575386039, -1.510843254991366402, -1.177573636344444896 ) ) ;
#167792=CARTESIAN_POINT ( 'NONE',  ( 2.541402807867772840, 1.801932494976875576, -0.7955018757880153446 ) ) ;
#167793=CARTESIAN_POINT ( 'NONE',  ( 0.5142528298564854605, 1.293200884458247657, -1.351890787750304135 ) ) ;
#167794=CARTESIAN_POINT ( 'NONE',  ( 0.6077679335219284829, 0.6189715888181289705, -1.861716921216026055 ) ) ;
#167795=CARTESIAN_POINT ( 'NONE',  ( -0.1933232215488022709, -0.4202133615931051835, -1.872389726556406897 ) ) ;
#167799=CARTESIAN_POINT ( 'NONE',  ( 5.928550619183989845, 1.803260976426118489, 0.4972845834502263584 ) ) ;
#167801=CARTESIAN_POINT ( 'NONE',  ( 4.996967907133109676, 0.3485794866864948549, 2.040532872733556768 ) ) ;
#167811=CARTESIAN_POINT ( 'NONE',  ( 5.019951445752288244, 1.940773837913706057, -0.2859759768028962146 ) ) ;
#167813=CARTESIAN_POINT ( 'NONE',  ( 3.708361104356564297, -1.524809962200252444, -1.319026932540816599 ) ) ;
#167814=CARTESIAN_POINT ( 'NONE',  ( 2.993272137104509678, -0.3688056758139393043, 1.879696595719517083 ) ) ;
#167816=CARTESIAN_POINT ( 'NONE',  ( 0.7498831369015903636, 2.188782640433343474, -0.1130235578899463078 ) ) ;
#167817=CARTESIAN_POINT ( 'NONE',  ( 0.1331715793776782342, 4.090830978607494117, -2.508370148267160538 ) ) ;
#167818=CARTESIAN_POINT ( 'NONE',  ( 3.040157689216971715, 1.855973101128991054, 0.2326549598439253685 ) ) ;
#167822=CARTESIAN_POINT ( 'NONE',  ( 4.693022120063472080, 1.842747525957793009, 1.042402977009656340 ) ) ;
#167824=CARTESIAN_POINT ( 'NONE',  ( 5.477033855465498924, 1.911541192706748715, 0.7957256658025002594 ) ) ;
#167825=CARTESIAN_POINT ( 'NONE',  ( 1.136401537022444508, 0.4113854086121961351, 2.049693714879106121 ) ) ;
#167826=CARTESIAN_POINT ( 'NONE',  ( 6.720655732516663150, 7.051555433583626353, 2.871889998671435240 ) ) ;
#167827=CARTESIAN_POINT ( 'NONE',  ( 0.1645217639845691082, -1.537023147574669402, -0.7826882907640534404 ) ) ;
#167836=CARTESIAN_POINT ( 'NONE',  ( 0.7151241933986829391, 1.480140477221444373, 1.044027612606616140 ) ) ;
#167845=CARTESIAN_POINT ( 'NONE',  ( 5.765249964824501028, 1.862012222821707308, -0.7743297468396084238 ) ) ;
#167846=CARTESIAN_POINT ( 'NONE',  ( 0.7684181764250409552, 2.117871390293009526, -0.1079879263860619443 ) ) ;
#167849=CARTESIAN_POINT ( 'NONE',  ( -0.1394461523060987751, 0.6550469493228279205, -2.357635998629922902 ) ) ;
#167854=CARTESIAN_POINT ( 'NONE',  ( 3.186336211243359084, 1.097972430180796266, -1.634763817068272784 ) ) ;
#167856=CARTESIAN_POINT ( 'NONE',  ( 0.9617728337494994006, -1.673954878106189925, -1.301583125534570673 ) ) ;
#167859=CARTESIAN_POINT ( 'NONE',  ( 6.727182134110201162, 1.237345558575110083, 2.302850971298702198 ) ) ;
#167860=CARTESIAN_POINT ( 'NONE',  ( 6.281208295753298643, 1.508423295503196648, 1.589913042345507455 ) ) ;
#167862=CARTESIAN_POINT ( 'NONE',  ( 4.559546607354286074, 0.4225000031176616710, -1.879333123156016860 ) ) ;
#167864=FACE_OUTER_BOUND ( 'NONE', #43107, .T. ) ;
#167865=CARTESIAN_POINT ( 'NONE',  ( 1.418904949497600487, 1.480075412272121360, -1.637148382315711359 ) ) ;
#167869=CARTESIAN_POINT ( 'NONE',  ( 6.438338856661699694, -1.056498591242978957, 1.661895973567611540 ) ) ;
#167870=CARTESIAN_POINT ( 'NONE',  ( 0.5209107642259405146, -1.843744896352221829, 0.6102272969235060796 ) ) ;
#167871=CARTESIAN_POINT ( 'NONE',  ( 6.063868583556772052, 1.884346855680006261, -1.315804018288849964 ) ) ;
#167873=CARTESIAN_POINT ( 'NONE',  ( 4.100341000477321529, 1.851659804611929472, 0.1859286059659806256 ) ) ;
#167878=CARTESIAN_POINT ( 'NONE',  ( 0.7498831369015904746, 2.188782640433343474, -0.1130235578899463078 ) ) ;
#167880=ORIENTED_EDGE ( 'NONE', *, *, #83840, .F. ) ;
#167883=CARTESIAN_POINT ( 'NONE',  ( 0.4865809202317071813, -0.2202831055867389420, -1.812292406919484344 ) ) ;
#167885=CARTESIAN_POINT ( 'NONE',  ( 2.848001011750156408, 0.2514756280368075081, -1.715647774213580501 ) ) ;
#167889=CARTESIAN_POINT ( 'NONE',  ( 6.094357461763901362, -1.817385979143220309, -0.1739998769475574192 ) ) ;
#167890=CARTESIAN_POINT ( 'NONE',  ( 3.608209768781400761, 1.961936380018937331, 0.004537341891153179319 ) ) ;
#167895=CARTESIAN_POINT ( 'NONE',  ( 4.477262591527907176, -1.894555094343739476, -0.9525379817736513433 ) ) ;
#167900=CARTESIAN_POINT ( 'NONE',  ( 3.098552089154332556, 2.054082100768514607, 0.2579794602402472603 ) ) ;
#167901=CARTESIAN_POINT ( 'NONE',  ( 6.827182134110205247, 0.5943742033862747798, 1.864010940340610212 ) ) ;
#167903=CARTESIAN_POINT ( 'NONE',  ( 4.741020875331694029, 2.125508857184394973, 0.6453399526389347329 ) ) ;
#167905=CARTESIAN_POINT ( 'NONE',  ( 2.426789430794534130, -1.706071328008453625, -1.540741829672709118 ) ) ;
#167914=CARTESIAN_POINT ( 'NONE',  ( 4.482611839828003930, -1.244964735940889522, 1.451779576051547282 ) ) ;
#167916=CARTESIAN_POINT ( 'NONE',  ( 3.768305045387724928, -1.158492864085089114, 1.277938026295278418 ) ) ;
#167917=CARTESIAN_POINT ( 'NONE',  ( 3.555875268649951959, 1.124244472066991518, 1.673854899288424347 ) ) ;
#167918=CARTESIAN_POINT ( 'NONE',  ( 4.448018067569548428, -2.052855444095956550, -1.034378808386252624 ) ) ;
#167920=CARTESIAN_POINT ( 'NONE',  ( 0.1181803206181560040, -2.163391993613572151, 0.4351206515559591370 ) ) ;
#167922=CARTESIAN_POINT ( 'NONE',  ( 4.622157715239192832, 1.089468934077148399, -1.394508319181851697 ) ) ;
#167924=CARTESIAN_POINT ( 'NONE',  ( 1.324644486801781040, 2.210297274253099520, 0.6072788910070088253 ) ) ;
#167925=CARTESIAN_POINT ( 'NONE',  ( 6.404252597826388893, 1.360807738692754176, -1.240355271200761278 ) ) ;
#167927=CARTESIAN_POINT ( 'NONE',  ( 6.580031370938625557, -2.148343778048496411, -0.4316624935760752790 ) ) ;
#167931=CARTESIAN_POINT ( 'NONE',  ( 6.877413708759195998, -0.1538780216673047430, 2.036608477593480959 ) ) ;
#167932=CARTESIAN_POINT ( 'NONE',  ( 1.200408080392855181, 1.350732740426639822, -1.497504596960941958 ) ) ;
#167934=CARTESIAN_POINT ( 'NONE',  ( 5.742784330379758551, 0.3781152824756833231, 1.888869927322960329 ) ) ;
#167936=CARTESIAN_POINT ( 'NONE',  ( 0.9849990780092006126, -1.403669121040777457, 1.721781922543249799 ) ) ;
#167944=CARTESIAN_POINT ( 'NONE',  ( 3.755166387800693339, 1.726757624646685807, -0.2173075579294906912 ) ) ;
#167945=CARTESIAN_POINT ( 'NONE',  ( 2.752341281506097470, -1.956419249932477955, -0.1471676765215298721 ) ) ;
#167949=CARTESIAN_POINT ( 'NONE',  ( 6.426224708462171087, 1.007414738832881351, 1.683299376423300853 ) ) ;
#167952=CARTESIAN_POINT ( 'NONE',  ( 5.225796113160614986, 0.8128206588041908542, -1.845625551132886288 ) ) ;
#167953=CARTESIAN_POINT ( 'NONE',  ( 1.464152659907109966, 2.228779883755461100, -0.3883945716754066968 ) ) ;
#167956=CARTESIAN_POINT ( 'NONE',  ( 2.671000074538076863, 0.09590037325727870932, -1.868228684465601752 ) ) ;
#167957=CARTESIAN_POINT ( 'NONE',  ( 1.494300775288709415, -1.721104260995092838, 0.2117000974225565491 ) ) ;
#167958=CARTESIAN_POINT ( 'NONE',  ( 4.862908538974716421, 0.2148362657848035262, -2.180980218048253150 ) ) ;
#167959=CARTESIAN_POINT ( 'NONE',  ( 5.122255714018879580, -1.229368216938999003, -1.952684467508845056 ) ) ;
#167960=CARTESIAN_POINT ( 'NONE',  ( 1.551711473626409266, 0.5993144932881481202, -1.971807626030545268 ) ) ;
#167961=CARTESIAN_POINT ( 'NONE',  ( 3.398316578678576949, 1.530473418458015100, -1.195227296853792920 ) ) ;
#167963=CARTESIAN_POINT ( 'NONE',  ( 6.204356031920277736, -0.6731288877953770511, -1.745422550748019219 ) ) ;
#167965=CARTESIAN_POINT ( 'NONE',  ( 6.784528966312857179, -1.956291195211720346, 0.4871289682274528299 ) ) ;
#167969=CARTESIAN_POINT ( 'NONE',  ( 4.518204034511161815, -1.842447959940773705, 0.8197716922626956393 ) ) ;
#167973=CARTESIAN_POINT ( 'NONE',  ( 2.596107596775329540, -1.820790993511243849, -0.1344670722737417168 ) ) ;
#167983=CARTESIAN_POINT ( 'NONE',  ( 5.988927272769587695, -1.918439801222410201, -0.6316595152702029203 ) ) ;
#167984=CARTESIAN_POINT ( 'NONE',  ( 6.516288422252827672, -2.220882151245454850, 0.05110445944340144542 ) ) ;
#167988=CARTESIAN_POINT ( 'NONE',  ( 4.856353099686935515, 0.7867916563346208925, 1.904994776275979129 ) ) ;
#167989=CARTESIAN_POINT ( 'NONE',  ( 4.711564657724523819, 1.930417226389494090, 0.5826574956761670920 ) ) ;
#167997=CARTESIAN_POINT ( 'NONE',  ( 5.097029748277864591, 1.038832625704217527, -1.727738606215820205 ) ) ;
#167998=CARTESIAN_POINT ( 'NONE',  ( 4.066218318298571610, -1.718653781379267276, -0.6607852518168353395 ) ) ;
#168000=CARTESIAN_POINT ( 'NONE',  ( 2.157223245065964967, -1.782429894076944521, 1.465742965790328700 ) ) ;
#168002=CARTESIAN_POINT ( 'NONE',  ( 4.604844690042746436, 1.674155836469687575, -1.367402732809947397 ) ) ;
#168004=CARTESIAN_POINT ( 'NONE',  ( 0.08144728253534591622, -0.9147537949990096617, 1.713110483266879980 ) ) ;
#168006=CARTESIAN_POINT ( 'NONE',  ( 3.866856096493505923, -0.6709599815711597692, 2.198256080205548635 ) ) ;
#168009=CARTESIAN_POINT ( 'NONE',  ( 3.994877460428855276, 1.580554378303768992, -1.000287695324620252 ) ) ;
#168010=CARTESIAN_POINT ( 'NONE',  ( 0.4562421353364953802, 0.7503462943320489131, 1.823165437449389081 ) ) ;
#168014=CARTESIAN_POINT ( 'NONE',  ( 1.278255639411193245, 1.316999024263129092, 1.770685722221450709 ) ) ;
#168020=CARTESIAN_POINT ( 'NONE',  ( 6.772342980177176841, -1.213407086615119423, 1.554582774731553707 ) ) ;
#168021=CARTESIAN_POINT ( 'NONE',  ( 6.674459784896970227, -1.426286490538879903, 1.815071943837057500 ) ) ;
#168022=CARTESIAN_POINT ( 'NONE',  ( 0.9241798626423223251, 0.9638202082158978667, 1.708698881219716137 ) ) ;
#168023=CARTESIAN_POINT ( 'NONE',  ( 4.469619655223175947, -0.3576850913847802182, 2.031185480813563426 ) ) ;
#168031=CARTESIAN_POINT ( 'NONE',  ( 6.057114314241694331, 1.778561107892376647, -1.245054071093915304 ) ) ;
#168034=CARTESIAN_POINT ( 'NONE',  ( 5.952668924537682038, -1.582617586749142102, -0.9407850039931386910 ) ) ;
#168038=CARTESIAN_POINT ( 'NONE',  ( 1.159204581426832803, 0.3705859133612995349, -1.833297903905316772 ) ) ;
#168043=CARTESIAN_POINT ( 'NONE',  ( 0.5746843702075511429, -1.384840223850939855, 1.318951758179337741 ) ) ;
#168044=CARTESIAN_POINT ( 'NONE',  ( 3.027930095613054817, 0.9845384034416431174, -1.470494568931050905 ) ) ;
#168046=CARTESIAN_POINT ( 'NONE',  ( 1.225099565173026761, 1.686864977381890451, 0.9006792851762451813 ) ) ;
#168048=CARTESIAN_POINT ( 'NONE',  ( 4.112823271221511590, 0.09766498815510017695, 1.913256991299339793 ) ) ;
#168050=CARTESIAN_POINT ( 'NONE',  ( 5.529738209476210642, 1.898601866877418942, -0.5236614360015124925 ) ) ;
#168051=CARTESIAN_POINT ( 'NONE',  ( 1.125412309253082332, 1.872817075645373697, 0.9946839901537674056 ) ) ;
#168053=CARTESIAN_POINT ( 'NONE',  ( 3.379631771358857950, 1.185797501207178861, 1.446808710765794315 ) ) ;
#168054=CARTESIAN_POINT ( 'NONE',  ( 6.410786927598755902, 1.272630858062718584, -1.164536656126140324 ) ) ;
#168056=CARTESIAN_POINT ( 'NONE',  ( 3.299657469156279888, 1.739734091921738557, 1.357710657151039779 ) ) ;
#168059=CARTESIAN_POINT ( 'NONE',  ( 1.047418773927465629, 1.819938098697634343, -0.9707658663142370026 ) ) ;
#168068=CARTESIAN_POINT ( 'NONE',  ( 3.525891238081061640, 2.020528833579691597, -0.4508363271973143682 ) ) ;
#168072=CARTESIAN_POINT ( 'NONE',  ( 0.9615888033541221125, -1.593469042607889463, -1.240847856016368489 ) ) ;
#168076=CARTESIAN_POINT ( 'NONE',  ( 0.07479286986303290696, 5.725009232006174287, -2.449550298930736059 ) ) ;
#168078=CARTESIAN_POINT ( 'NONE',  ( 6.345077344222471716, -1.080897578067066878, 1.701688803805063266 ) ) ;
#168079=CARTESIAN_POINT ( 'NONE',  ( 6.192599819808762618, 1.414433556397393543, -1.292206900294754490 ) ) ;
#168080=CARTESIAN_POINT ( 'NONE',  ( 6.639320575229256782, 4.691717626494606996, 2.665852771288126366 ) ) ;
#168081=CARTESIAN_POINT ( 'NONE',  ( 3.351304529449970371, 0.5305821810032870234, -2.126252377916526992 ) ) ;
#168083=CARTESIAN_POINT ( 'NONE',  ( 3.849791259674230748, -1.322437695595569673, -1.381667681676468140 ) ) ;
#168087=CARTESIAN_POINT ( 'NONE',  ( 0.7379079170338509464, 2.013986002441462198, -0.1017714793793283723 ) ) ;
#168090=CARTESIAN_POINT ( 'NONE',  ( 0.3633196395196974793, 0.2168307188613327052, -2.282096724506751162 ) ) ;
#168092=CARTESIAN_POINT ( 'NONE',  ( 4.664925512212582781, -1.541612441252750543, -0.7736475682248912245 ) ) ;
#168098=CARTESIAN_POINT ( 'NONE',  ( 0.9417639971489067952, 1.314929008279978495, 1.456166070238865018 ) ) ;
#168101=CARTESIAN_POINT ( 'NONE',  ( 0.1751657365761521701, 0.7240325161481726557, -2.128694924679303213 ) ) ;
#168104=VERTEX_POINT ( 'NONE', #129060 ) ;
#168105=CARTESIAN_POINT ( 'NONE',  ( 3.844242791777858770, 0.9658850817777319131, -1.532267982868290579 ) ) ;
#168109=CARTESIAN_POINT ( 'NONE',  ( 5.338451399618321602, 1.074232541698511900, -1.458426962581545361 ) ) ;
#168113=CARTESIAN_POINT ( 'NONE',  ( 6.707467475981614413, -1.495571456699902546, -1.107353707014941069 ) ) ;
#168115=CARTESIAN_POINT ( 'NONE',  ( 3.972214814312221343, -1.895280843596976350, -0.2773303961090283765 ) ) ;
#168121=CARTESIAN_POINT ( 'NONE',  ( 0.9717996764858798375, 2.083101276202529384, -0.5774176476955604764 ) ) ;
#168124=CARTESIAN_POINT ( 'NONE',  ( 0.8326870614539466642, 0.1294382003846420159, 1.821050407652326619 ) ) ;
#168126=CARTESIAN_POINT ( 'NONE',  ( 4.084828617465196210, -0.1788469021064206521, -1.816781805555576668 ) ) ;
#168128=CARTESIAN_POINT ( 'NONE',  ( 1.529408426332915960, -0.2309274165002393187, 1.898302859121250297 ) ) ;
#168129=CARTESIAN_POINT ( 'NONE',  ( 2.840245056987787287, -1.014795158497614036, 1.687856822838776916 ) ) ;
#168130=CARTESIAN_POINT ( 'NONE',  ( 3.948723843360758323, -1.616405859212793894, -1.076207510925797139 ) ) ;
#168133=CARTESIAN_POINT ( 'NONE',  ( 4.570628194609677841, 0.8141925398062774821, 1.958264201954627026 ) ) ;
#168142=CARTESIAN_POINT ( 'NONE',  ( 3.475057130574196407, 0.04366187338752242769, -1.825333387291371512 ) ) ;
#168143=CARTESIAN_POINT ( 'NONE',  ( 6.051970301643104122, 1.040788372175960541, 1.727066800951609249 ) ) ;
#168144=CARTESIAN_POINT ( 'NONE',  ( 0.2388460773940295212, -2.007853281042128568, -0.5044432775610437902 ) ) ;
#168148=CARTESIAN_POINT ( 'NONE',  ( 4.645289301550183936, -1.446173438076237217, -1.186536486241091204 ) ) ;
#168150=CARTESIAN_POINT ( 'NONE',  ( 3.176308805823165660, -1.146983237646619580, 1.547710939905672989 ) ) ;
#168159=CARTESIAN_POINT ( 'NONE',  ( 1.704857254432812219, 1.976886250939764889, 0.7584849220025058347 ) ) ;
#168162=CARTESIAN_POINT ( 'NONE',  ( 6.526242037438201749, 1.059062773735760521, 1.778703558766213000 ) ) ;
#168163=CARTESIAN_POINT ( 'NONE',  ( 0.7140992756325339474, 1.701125707204936166, 0.7050099338341904165 ) ) ;
#168165=CARTESIAN_POINT ( 'NONE',  ( 6.029976284357474903, -1.944044770632427976, 1.226447132130564999 ) ) ;
#168168=CARTESIAN_POINT ( 'NONE',  ( 1.974976472051133136, -0.1153332747052069479, -2.289479170392795915 ) ) ;
#168171=CARTESIAN_POINT ( 'NONE',  ( 6.158146451363091245, -1.371594178524730534, 1.374984930127883143 ) ) ;
#168175=CARTESIAN_POINT ( 'NONE',  ( 1.125244999914726263, 1.777361856972861531, 0.9454465733411165917 ) ) ;
#168180=CARTESIAN_POINT ( 'NONE',  ( 3.187526948619547884, -0.8467841439671991433, 1.911654264539459191 ) ) ;
#168181=CARTESIAN_POINT ( 'NONE',  ( 2.166550811918485753, -1.616863761265506794, -0.7202261968358366628 ) ) ;
#168184=CARTESIAN_POINT ( 'NONE',  ( 4.857543142518937707, 2.267833309424868826, -0.3330599157496324514 ) ) ;
#168185=CARTESIAN_POINT ( 'NONE',  ( 3.802475355173411842, 1.493833042257145305, 0.8925963562203437229 ) ) ;
#168188=CARTESIAN_POINT ( 'NONE',  ( 3.672919734203412112, -0.7009596788165352033, -1.586013134846143480 ) ) ;
#168189=CARTESIAN_POINT ( 'NONE',  ( 3.877515590359277287, -0.1633623659567252084, 2.165103034678467431 ) ) ;
#168191=CARTESIAN_POINT ( 'NONE',  ( 4.979703994296570180, -0.7212954316567052881, 1.883311551353183511 ) ) ;
#168192=CARTESIAN_POINT ( 'NONE',  ( 6.750000000000005329, 7.629137130509070275, 2.600000000000000533 ) ) ;
#168194=CARTESIAN_POINT ( 'NONE',  ( 1.799704718893188282, -0.6512145186477935610, 1.813102765825167273 ) ) ;
#168196=CARTESIAN_POINT ( 'NONE',  ( 6.099871961099720963, 1.531114646448136218, 1.609653004599376658 ) ) ;
#168198=CARTESIAN_POINT ( 'NONE',  ( -0.2108831679771168421, 6.948330828014878335, -2.492181822431015270 ) ) ;
#168203=CARTESIAN_POINT ( 'NONE',  ( 0.8740457437188209333, 0.4279768726487084285, -2.179530559632827824 ) ) ;
#168204=CARTESIAN_POINT ( 'NONE',  ( 5.564887814092526419, 1.486691789297952093, -1.280227714881218670 ) ) ;
#168207=CARTESIAN_POINT ( 'NONE',  ( 0.4038910500440278106, -0.5768866637368921246, 2.083095904058133385 ) ) ;
#168210=CARTESIAN_POINT ( 'NONE',  ( 4.141125080024585792, -0.1993089607698217136, -2.053009638179447371 ) ) ;
#168214=CARTESIAN_POINT ( 'NONE',  ( 5.571519856497625156, 1.802974293077023393, -0.4980454429602265698 ) ) ;
#168215=CARTESIAN_POINT ( 'NONE',  ( 4.992643705478089444, -1.725105917503889641, 0.1769386724924902066 ) ) ;
#168216=CARTESIAN_POINT ( 'NONE',  ( 2.823474877308090214, 0.9648067800103199421, -1.448311861076934104 ) ) ;
#168218=CARTESIAN_POINT ( 'NONE',  ( 1.382826565882399272, -0.3421621995536459626, -2.266597836251768250 ) ) ;
#168220=CARTESIAN_POINT ( 'NONE',  ( 5.952696063536119908, -1.793662432779649540, -1.073965677532197072 ) ) ;
#168221=CARTESIAN_POINT ( 'NONE',  ( -0.01213283819992416745, -0.3988646234997471618, -1.803908381610368261 ) ) ;
#168222=AXIS2_PLACEMENT_3D ( 'NONE', #143738, #180452, #209732 ) ;
#168225=CARTESIAN_POINT ( 'NONE',  ( 1.811172873341511336, 1.158687402475454098, -1.650082692374904125 ) ) ;
#168231=CARTESIAN_POINT ( 'NONE',  ( 2.965608807194367369, -1.734805745614193873, -1.219131234129526398 ) ) ;
#168233=CARTESIAN_POINT ( 'NONE',  ( 5.197797600609998625, -0.6536857159176562293, 1.704833070275885598 ) ) ;
#168238=CARTESIAN_POINT ( 'NONE',  ( 2.636978264590104537, 1.903244974434484371, 0.6766128908266034747 ) ) ;
#168239=CARTESIAN_POINT ( 'NONE',  ( 6.247136877606230598, -1.867572634706683443, 1.175315980461520304 ) ) ;
#168241=CARTESIAN_POINT ( 'NONE',  ( 3.906960136656021376, -1.523566986099005316, 1.068299854780943692 ) ) ;
#168247=CARTESIAN_POINT ( 'NONE',  ( 4.863791234866603475, 1.805334366393744450, -0.2710410529033688842 ) ) ;
#168251=CARTESIAN_POINT ( 'NONE',  ( 1.756802591741468245, -1.724947740463366852, -0.1754148046573481556 ) ) ;
#168252=CARTESIAN_POINT ( 'NONE',  ( 1.271012957286155709, 1.034212954684173180, 1.399518829098946204 ) ) ;
#168253=CARTESIAN_POINT ( 'NONE',  ( 5.426528828858072195, 1.378586375901286187, -1.850541897242431677 ) ) ;
#168256=CARTESIAN_POINT ( 'NONE',  ( 1.370465108300226609, -1.309671233245520483, 1.591056919209728138 ) ) ;
#168258=CARTESIAN_POINT ( 'NONE',  ( 0.4212496859960760953, 0.7689994822442263178, 1.863884711849304487 ) ) ;
#168261=CARTESIAN_POINT ( 'NONE',  ( 0.1804621682222322943, -1.911711055282316662, -0.4813082943134691094 ) ) ;
#168262=CARTESIAN_POINT ( 'NONE',  ( 3.129067941553372645, 1.730785544086024696, 0.8136490247460312908 ) ) ;
#168264=CARTESIAN_POINT ( 'NONE',  ( 5.760442859251142522, 0.8911043219209063837, 2.019162844794204048 ) ) ;
#168270=CARTESIAN_POINT ( 'NONE',  ( 6.322909428431959356, 1.571596504679906303, -1.423730336690950393 ) ) ;
#168271=CARTESIAN_POINT ( 'NONE',  ( 3.962222562901392742, 2.290579029535879219, -0.2790985642298955405 ) ) ;
#168272=CARTESIAN_POINT ( 'NONE',  ( 5.336364984333265227, -1.091323163865608459, 1.630109012322231266 ) ) ;
#168273=CARTESIAN_POINT ( 'NONE',  ( 0.8835585337332927391, -1.864609544942645414, 0.6100022000963196689 ) ) ;
#168277=CARTESIAN_POINT ( 'NONE',  ( 6.385953923436008317, -2.015982004707029596, 0.05432014494890363698 ) ) ;
#168280=CARTESIAN_POINT ( 'NONE',  ( 0.005434845660363255178, -0.7843016415976924449, -1.664241202765592176 ) ) ;
#168281=CARTESIAN_POINT ( 'NONE',  ( 3.573241956510754491, 1.960547127731948613, 0.9329660139856699175 ) ) ;
#168285=CARTESIAN_POINT ( 'NONE',  ( 0.6332531790259123827, 1.961634380476449335, 0.8060562103610890983 ) ) ;
#168292=CARTESIAN_POINT ( 'NONE',  ( 1.739600335799436737, -1.490509515545968666, -1.423327880080206720 ) ) ;
#168298=CARTESIAN_POINT ( 'NONE',  ( 4.002528454542265024, -1.891902218777557598, -0.2775262981309714605 ) ) ;
#168300=CARTESIAN_POINT ( 'NONE',  ( 6.561402770032070286, 0.3947617697056918784, -2.227681008968500631 ) ) ;
#168302=CARTESIAN_POINT ( 'NONE',  ( 1.757782220650351723, 0.6909716962627761028, -1.674832866754811578 ) ) ;
#168303=CARTESIAN_POINT ( 'NONE',  ( 0.9365811914238668656, -1.507994439141499221, 1.181323522483549437 ) ) ;
#168304=CARTESIAN_POINT ( 'NONE',  ( 1.856005582152659317, -0.6995316168164237292, 1.948720873434762080 ) ) ;
#168306=CARTESIAN_POINT ( 'NONE',  ( 0.8132764231247009423, -0.2916495841569742842, 1.949667021961091429 ) ) ;
#168307=CARTESIAN_POINT ( 'NONE',  ( 5.795520199677122619, 1.460474902364042649, 1.256451531516086684 ) ) ;
#168308=CARTESIAN_POINT ( 'NONE',  ( 0.5577797733781300060, -1.952719008213155139, -1.229525757098411942 ) ) ;
#168312=CARTESIAN_POINT ( 'NONE',  ( 4.246570442813556667, -2.039787899008322469, -0.3057716575347816934 ) ) ;
#168318=CARTESIAN_POINT ( 'NONE',  ( 5.526436043951506782, 1.257118228488460110, -1.689427636868174210 ) ) ;
#168321=CARTESIAN_POINT ( 'NONE',  ( 6.848098043024292814, -0.8888149443028300345, 1.868052569137634400 ) ) ;
#168323=CARTESIAN_POINT ( 'NONE',  ( 4.868538603872567982, -1.416007186031362330, 1.633285015310452115 ) ) ;
#168324=CARTESIAN_POINT ( 'NONE',  ( 4.319013676512412303, 1.559734590277090716, -1.283057401373039141 ) ) ;
#168325=CARTESIAN_POINT ( 'NONE',  ( 6.720655732516676473, 3.678797444539682271, 2.787578482799071278 ) ) ;
#168330=CARTESIAN_POINT ( 'NONE',  ( 2.676970549635893537, 1.727063564601112100, -1.040793759654296213 ) ) ;
#168336=CARTESIAN_POINT ( 'NONE',  ( 6.589320575229281829, 7.629137130509070275, 2.703262396134015866 ) ) ;
#168338=CARTESIAN_POINT ( 'NONE',  ( 4.745720352911135365, 1.994069623535676961, -0.2986464557954356946 ) ) ;
#168340=CARTESIAN_POINT ( 'NONE',  ( 0.4688601960516668443, 0.1741500657085493509, -1.716052735907805937 ) ) ;
#168345=CARTESIAN_POINT ( 'NONE',  ( 5.782452155351484713, -1.824793809246130438, -0.4103911052399379367 ) ) ;
#168346=CARTESIAN_POINT ( 'NONE',  ( 6.293232695293600187, -0.1032093112793490142, -2.010699630015537309 ) ) ;
#168353=CARTESIAN_POINT ( 'NONE',  ( 0.8433753223025289847, 0.3905737783656983431, -1.978056610397058490 ) ) ;
#168355=CARTESIAN_POINT ( 'NONE',  ( 6.262596564776618635, -1.532251275270900326, 1.525113613579494709 ) ) ;
#168359=CARTESIAN_POINT ( 'NONE',  ( 0.1982580178685423022, 1.319089833320963079, -1.389493073782912091 ) ) ;
#168367=CARTESIAN_POINT ( 'NONE',  ( 3.661132068870280420, -1.905464569931826446, -1.020879743040298271 ) ) ;
#168370=CARTESIAN_POINT ( 'NONE',  ( 0.8090202166558431163, -0.5209130535433897924, -2.055487714681260236 ) ) ;
#168372=CARTESIAN_POINT ( 'NONE',  ( 2.055877211876644406, 1.966332055899377762, -0.1412752051469425008 ) ) ;
#168375=CARTESIAN_POINT ( 'NONE',  ( 6.109808257530946918, 0.5734047718448382902, -1.884209069281018500 ) ) ;
#168376=CARTESIAN_POINT ( 'NONE',  ( 0.5681770160902823719, -1.828317568802136250, -0.6549081214334094847 ) ) ;
#168383=CARTESIAN_POINT ( 'NONE',  ( 4.565046243057500952, -1.533749416048999947, 1.141898535029245432 ) ) ;
#168385=CARTESIAN_POINT ( 'NONE',  ( 3.211752199052122503, -0.4303563718574506813, 2.164345902561148005 ) ) ;
#168386=CARTESIAN_POINT ( 'NONE',  ( 2.345003271878861373, 0.4830727525354863716, 2.153096645625157457 ) ) ;
#168388=CARTESIAN_POINT ( 'NONE',  ( 0.1352199593073095951, -0.09384731153385186819, 1.910084486482076294 ) ) ;
#168392=CARTESIAN_POINT ( 'NONE',  ( 2.998552181135269556, 2.054425100943928051, 0.2560010573490826835 ) ) ;
#168396=CARTESIAN_POINT ( 'NONE',  ( 0.3741789627117291239, 1.245922373857488274, 1.766349570875298758 ) ) ;
#168397=CARTESIAN_POINT ( 'NONE',  ( 2.489988787850425656, -2.185901284972164405, -0.1580625509675498419 ) ) ;
#168404=CARTESIAN_POINT ( 'NONE',  ( 6.434187037261335007, -1.398866626055271123, -1.024706079042293938 ) ) ;
#168406=CARTESIAN_POINT ( 'NONE',  ( 3.432542862244458703, -1.236986750340131946, 1.659893174209552624 ) ) ;
#168407=CARTESIAN_POINT ( 'NONE',  ( 4.200857891667449273, 1.936436120981197773, 0.8564517604346032487 ) ) ;
#168410=CARTESIAN_POINT ( 'NONE',  ( 3.186336211243359084, 1.097972430180796266, -1.634763817068272784 ) ) ;
#168411=CARTESIAN_POINT ( 'NONE',  ( 0.5801457039020865292, 0.9447208859736742070, 1.662703529197881558 ) ) ;
#168412=CARTESIAN_POINT ( 'NONE',  ( 4.857543142518937707, 2.267833309424868826, -0.3330599157496324514 ) ) ;
#168413=CARTESIAN_POINT ( 'NONE',  ( 2.912524513316586461, 1.322148455168963510, -1.259233298254287536 ) ) ;
#168417=CARTESIAN_POINT ( 'NONE',  ( 4.008068315354725186, -0.7665524943986418149, 1.861746286504823988 ) ) ;
#168418=CARTESIAN_POINT ( 'NONE',  ( 4.838696733575553743, -1.901848327180942766, -0.4805237247276354928 ) ) ;
#168422=CARTESIAN_POINT ( 'NONE',  ( 0.07556134207195497332, 5.719716873484223640, -2.838244455430352087 ) ) ;
#168423=CARTESIAN_POINT ( 'NONE',  ( 6.720655732516684466, -0.001531948155393536137, 2.073773125298985054 ) ) ;
#168424=CARTESIAN_POINT ( 'NONE',  ( 5.576936095668227900, -0.04655786065462656775, -1.769397458738901197 ) ) ;
#168425=CARTESIAN_POINT ( 'NONE',  ( 6.589320575229280053, 7.629137130509070275, 2.496737603865983868 ) ) ;
#168426=CARTESIAN_POINT ( 'NONE',  ( 1.974822964535282610, -0.1094934731284517848, -2.188836591978132518 ) ) ;
#168427=CARTESIAN_POINT ( 'NONE',  ( -0.02444708455723310775, -1.687298116421297456, -0.4264520246781302593 ) ) ;
#168429=CARTESIAN_POINT ( 'NONE',  ( 0.1335669894368890498, 2.867242032283002562, -2.641834823421157719 ) ) ;
#168430=CARTESIAN_POINT ( 'NONE',  ( 1.084105852307458040, -1.681943224540465964, -0.3816912691657590728 ) ) ;
#168431=CARTESIAN_POINT ( 'NONE',  ( 0.4744793627779358980, 2.001106834215804042, 1.130494720166761891 ) ) ;
#168432=CARTESIAN_POINT ( 'NONE',  ( 0.1346727191937693857, 0.3808678606769915209, 2.158067550307264604 ) ) ;
#168433=CARTESIAN_POINT ( 'NONE',  ( 3.422699507934781060, 1.400174360247144589, -1.705827624971032686 ) ) ;
#168434=CARTESIAN_POINT ( 'NONE',  ( 0.5323791783840629011, 1.248846938226945369, 1.775765033185220387 ) ) ;
#168436=CARTESIAN_POINT ( 'NONE',  ( 0.9896463964080002285, -0.5083134511523321741, 2.055333615346987663 ) ) ;
#168438=CARTESIAN_POINT ( 'NONE',  ( 5.737312389570451643, -1.741366515823379757, 0.8240431586447917178 ) ) ;
#168440=CARTESIAN_POINT ( 'NONE',  ( 1.154322298621703435, 0.9348496236407450866, 2.093279060508267175 ) ) ;
#168444=CARTESIAN_POINT ( 'NONE',  ( 3.668779877082572138, 0.8004024921177651519, 2.072244876181651652 ) ) ;
#168450=CARTESIAN_POINT ( 'NONE',  ( 1.652970434142877920, 1.038994816082598804, 1.728001345923817267 ) ) ;
#168452=CARTESIAN_POINT ( 'NONE',  ( 0.9188877648007650611, -1.496628706349166338, 1.419512306474308261 ) ) ;
#168455=CARTESIAN_POINT ( 'NONE',  ( 0.1867156058280826092, 1.363667594142993877, 1.237386390646778578 ) ) ;
#168458=CARTESIAN_POINT ( 'NONE',  ( 1.776017750421728270, 1.753029812786778940, -0.9963028777105964462 ) ) ;
#168459=CARTESIAN_POINT ( 'NONE',  ( -0.09456490281532430042, -0.7861721075429689565, -1.663503389917226460 ) ) ;
#168460=CARTESIAN_POINT ( 'NONE',  ( 5.495737418514557326, -2.292545469083116849, -0.002927036808696506075 ) ) ;
#168461=CARTESIAN_POINT ( 'NONE',  ( 3.644333108393753573, -1.504320797718930791, 1.061230752167609204 ) ) ;
#168464=CARTESIAN_POINT ( 'NONE',  ( 4.453998568579462969, 1.825179399820752169, -0.04523609120457571658 ) ) ;
#168465=CARTESIAN_POINT ( 'NONE',  ( 4.887342357109405455, -0.6819942819097268849, -1.897698409216505233 ) ) ;
#168467=CARTESIAN_POINT ( 'NONE',  ( 3.872163259867720253, 1.254437384476282835, 1.882731698358128369 ) ) ;
#168469=CARTESIAN_POINT ( 'NONE',  ( 6.088920695360399371, -0.3053041885118645271, -2.083579958893892137 ) ) ;
#168471=CARTESIAN_POINT ( 'NONE',  ( 3.789561645344252661, -1.914057400617325433, 0.7896510022299551013 ) ) ;
#168476=CARTESIAN_POINT ( 'NONE',  ( 2.279798536657418495, 1.185040197188882871, 1.518827336823719953 ) ) ;
#168479=CARTESIAN_POINT ( 'NONE',  ( 0.5023235590321275534, 1.964037083787707028, 0.1483792944171925254 ) ) ;
#168484=CARTESIAN_POINT ( 'NONE',  ( 1.600152846412273844, 1.536270192620782238, 1.604750372702767214 ) ) ;
#168485=CARTESIAN_POINT ( 'NONE',  ( 3.821394775679032740, -0.1568257194812898159, 2.100186923160925812 ) ) ;
#168488=CARTESIAN_POINT ( 'NONE',  ( 0.5724163261710726314, 1.287614217418028506, -1.343956351914729952 ) ) ;
#168494=CARTESIAN_POINT ( 'NONE',  ( 1.687894460584405731, 2.027760172737497424, -0.6205009303206151516 ) ) ;
#168497=CARTESIAN_POINT ( 'NONE',  ( 4.457442142980160504, 1.574409630067734156, 1.170308293268598421 ) ) ;
#168498=CARTESIAN_POINT ( 'NONE',  ( 2.940462584922590938, 2.145230175562794717, 0.2658940370997217584 ) ) ;
#168499=CARTESIAN_POINT ( 'NONE',  ( 2.014959344526063845, -1.785600367564584179, 0.4486904387498573676 ) ) ;
#168501=CARTESIAN_POINT ( 'NONE',  ( 4.241972025877470465, 0.4673694910880517583, 1.676319072879989047 ) ) ;
#168506=CARTESIAN_POINT ( 'NONE',  ( 1.411231610350563992, 1.906656261001705488, 1.018656936289302539 ) ) ;
#168507=CARTESIAN_POINT ( 'NONE',  ( 3.585314394424500062, 1.281165535658060017, -1.556669873624405120 ) ) ;
#168509=CARTESIAN_POINT ( 'NONE',  ( 0.7433210806352362754, -1.853469564684958382, 1.112228649290482263 ) ) ;
#168510=CARTESIAN_POINT ( 'NONE',  ( 3.854335392261270421, 0.7083531993744094368, 1.839989435513892380 ) ) ;
#168511=CARTESIAN_POINT ( 'NONE',  ( 6.609000000000053276, 0.5717736360873815205, 2.152148306911850995 ) ) ;
#168512=CARTESIAN_POINT ( 'NONE',  ( 2.946749062660087848, -1.589232290113586910, -1.115973732403415131 ) ) ;
#168518=CARTESIAN_POINT ( 'NONE',  ( -0.1110810684433141682, 4.095429159110416606, -2.351882046268341409 ) ) ;
#168524=CARTESIAN_POINT ( 'NONE',  ( 0.4115098346569624477, 1.921242953230850148, 1.085561749797583797 ) ) ;
#168526=CARTESIAN_POINT ( 'NONE',  ( 3.783995958019512607, -1.164969938643352299, -1.578273546942794647 ) ) ;
#168528=CARTESIAN_POINT ( 'NONE',  ( 1.231092510272915552, 2.014232830173094513, 0.09613330637052441840 ) ) ;
#168530=CARTESIAN_POINT ( 'NONE',  ( 3.081382859721363499, 1.672078201027054734, 1.298909159995583318 ) ) ;
#168534=CARTESIAN_POINT ( 'NONE',  ( 2.695044507329581673, -0.5773736025265225891, 1.748335772842606106 ) ) ;
#168538=CARTESIAN_POINT ( 'NONE',  ( 4.430007776716601953, -2.079114408633813582, 0.4165480963118637914 ) ) ;
#168542=CARTESIAN_POINT ( 'NONE',  ( 5.975869988448771153, 1.224042345451004765, 1.657734310933855815 ) ) ;
#168544=CARTESIAN_POINT ( 'NONE',  ( 2.700538275128167687, 1.556679782967337999, 0.9830204120172959525 ) ) ;
#168549=CARTESIAN_POINT ( 'NONE',  ( 2.702037527177497012, -0.6914408288211832954, 2.095836555436859872 ) ) ;
#168550=CARTESIAN_POINT ( 'NONE',  ( 4.974029133664690683, 1.296991790296280422, 1.853570637303619817 ) ) ;
#168552=CARTESIAN_POINT ( 'NONE',  ( 4.675916410682629198, 1.790815896176844335, -0.2727875059450618478 ) ) ;
#168553=CARTESIAN_POINT ( 'NONE',  ( 4.575340585108073732, 1.423666108326137048, 1.282088096497513652 ) ) ;
#168555=CARTESIAN_POINT ( 'NONE',  ( 4.135589226209329006, -1.358636868218986216, -1.428786634662780219 ) ) ;
#168556=CARTESIAN_POINT ( 'NONE',  ( 5.401189721097995111, 1.529905263132097071, 1.076157610686766075 ) ) ;
#168557=CARTESIAN_POINT ( 'NONE',  ( 5.178104514100493994, -0.9952990805809349695, -1.572330789729664779 ) ) ;
#168559=CARTESIAN_POINT ( 'NONE',  ( -0.1179535434602772825, -2.016182236903838465, -0.04464881524945257807 ) ) ;
#168561=CARTESIAN_POINT ( 'NONE',  ( 2.280028682641733973, 1.296546612978483504, 1.659573824544317455 ) ) ;
#168564=CARTESIAN_POINT ( 'NONE',  ( 0.07479286986305544449, 6.948552162806721277, -2.450557996216149892 ) ) ;
#168566=CARTESIAN_POINT ( 'NONE',  ( 2.426041109754235592, -1.997208190617974166, 0.3004318525065238776 ) ) ;
#168571=CARTESIAN_POINT ( 'NONE',  ( 2.267066545249882381, -1.975312647937790711, -0.8782872871702240847 ) ) ;
#168579=CARTESIAN_POINT ( 'NONE',  ( 0.2401087780563165297, 2.186128513634697512, 0.1550312349237955856 ) ) ;
#168581=CARTESIAN_POINT ( 'NONE',  ( 1.077466299836680630, -0.05792418700063763082, -2.261926406141855583 ) ) ;
#168588=CARTESIAN_POINT ( 'NONE',  ( 3.492533829797561218, -0.3379890457658150105, -1.691244694301207829 ) ) ;
#168590=CARTESIAN_POINT ( 'NONE',  ( 2.600565598370237819, 1.424089007750706237, -1.050482986540713926 ) ) ;
#168591=CARTESIAN_POINT ( 'NONE',  ( 2.754543805099545217, 1.998131736582898332, 0.2443565819899694291 ) ) ;
#168593=CARTESIAN_POINT ( 'NONE',  ( 5.104599427727727345, -0.7392731805347593221, -2.079399364341961487 ) ) ;
#168595=CARTESIAN_POINT ( 'NONE',  ( 4.377216478116826792, -1.806098078589046807, -0.9042721688041258643 ) ) ;
#168597=CARTESIAN_POINT ( 'NONE',  ( 4.552361342037492875, -1.314984614574012944, 1.528753174698034067 ) ) ;
#168598=CARTESIAN_POINT ( 'NONE',  ( 4.746265919983247983, 0.9249516081627707775, -1.557494045171695651 ) ) ;
#168601=CARTESIAN_POINT ( 'NONE',  ( 2.430351462470367707, 1.813921419787648315, 0.4566771774890953095 ) ) ;
#168603=CARTESIAN_POINT ( 'NONE',  ( 1.845825534506392085, -1.251752223804462272, -1.445855903880132631 ) ) ;
#168608=CARTESIAN_POINT ( 'NONE',  ( 0.3516297456669579269, -1.353986107606550249, -1.350798769753497552 ) ) ;
#168610=CARTESIAN_POINT ( 'NONE',  ( 2.066782613880484565, 1.455849762852476248, -1.315278764014264912 ) ) ;
#168613=CARTESIAN_POINT ( 'NONE',  ( 3.744478000529618100, 1.131475959888720295, -1.793321066073015224 ) ) ;
#168616=CARTESIAN_POINT ( 'NONE',  ( 5.536387714897482049, 1.941722972556509053, 0.3397322875919612795 ) ) ;
#168618=CARTESIAN_POINT ( 'NONE',  ( 1.125244999914726263, 1.777361856972861531, 0.9454465733411165917 ) ) ;
#168620=CARTESIAN_POINT ( 'NONE',  ( 1.564221677423253798, -1.129412574612179920, 1.790659096458546706 ) ) ;
#168622=CARTESIAN_POINT ( 'NONE',  ( 2.400909748719297188, 0.4512941399696759337, 2.020426262116347349 ) ) ;
#168626=CARTESIAN_POINT ( 'NONE',  ( 4.839831225001551829, 2.085006553764104265, 0.1541250707555453237 ) ) ;
#168628=CARTESIAN_POINT ( 'NONE',  ( 2.731258071184277103, -1.704167518380688140, 0.6551187846031493178 ) ) ;
#168629=CARTESIAN_POINT ( 'NONE',  ( 1.084272394670304118, -1.149816064065724230, 1.399778539804387822 ) ) ;
#168631=CARTESIAN_POINT ( 'NONE',  ( 6.533804136697315634, -1.437950210024591780, -1.674183229976949905 ) ) ;
#168634=CARTESIAN_POINT ( 'NONE',  ( 5.667066814448853407, -1.992748536412903615, -0.9483587796220711574 ) ) ;
#168637=CARTESIAN_POINT ( 'NONE',  ( 3.897043152223302886, -0.1904361752127527174, -1.902785305300330743 ) ) ;
#168641=CARTESIAN_POINT ( 'NONE',  ( 6.777786256569462431, -2.009253640576996514, 0.4989836931604470505 ) ) ;
#168644=CARTESIAN_POINT ( 'NONE',  ( 6.550331612656306035, -1.695486744446069727, 1.388264742925699569 ) ) ;
#168649=CARTESIAN_POINT ( 'NONE',  ( 3.180766902908559235, -0.1340872481324743570, -1.865776598943262199 ) ) ;
#168655=CARTESIAN_POINT ( 'NONE',  ( 6.508651864089095795, 0.6437109847576475419, 1.967739590238902991 ) ) ;
#168656=CARTESIAN_POINT ( 'NONE',  ( 0.8961114988408731552, -0.9091644883451601711, -1.799914091915676639 ) ) ;
#168660=CARTESIAN_POINT ( 'NONE',  ( 1.201424296212102893, -0.5295503721958020327, 2.126384922054704862 ) ) ;
#168661=CARTESIAN_POINT ( 'NONE',  ( 6.375623774462673587, 1.745513195383348926, -0.5351242734627087438 ) ) ;
#168663=EDGE_CURVE ( 'NONE', #157709, #90486, #200809, .T. ) ;
#168669=CARTESIAN_POINT ( 'NONE',  ( 3.333393596924072444, 0.8250370302015205271, -1.646115572170883112 ) ) ;
#168670=CARTESIAN_POINT ( 'NONE',  ( 0.4693897461072121802, -1.701762708260607715, -1.075143862628368474 ) ) ;
#168671=CARTESIAN_POINT ( 'NONE',  ( 1.810362406828632365, -1.941531176516932522, 1.229804462443480295 ) ) ;
#168673=CARTESIAN_POINT ( 'NONE',  ( 0.9712807694385624524, -0.2802886605943204490, 1.839611564956656453 ) ) ;
#168677=CARTESIAN_POINT ( 'NONE',  ( 4.113462262696740979, 1.539102623358613586, 1.134910093507961237 ) ) ;
#168682=CARTESIAN_POINT ( 'NONE',  ( 4.282818888323718376, 1.866831796845986435, -0.9415434926851961039 ) ) ;
#168683=CARTESIAN_POINT ( 'NONE',  ( 2.711613914024712191, -1.850561042518297672, 0.2725550856255419818 ) ) ;
#168686=CARTESIAN_POINT ( 'NONE',  ( 2.876183954794831354, -0.1304463317927692101, -1.735623171917876073 ) ) ;
#168690=CARTESIAN_POINT ( 'NONE',  ( 4.441862337843591746, 0.7341043403586414717, -1.561010781705338912 ) ) ;
#168691=CARTESIAN_POINT ( 'NONE',  ( 4.001666433686186686, -2.185622478633037602, 0.1623105178310546570 ) ) ;
#168692=CARTESIAN_POINT ( 'NONE',  ( 6.551417122825020201, -1.769646310455678995, -1.318412661681533260 ) ) ;
#168694=CARTESIAN_POINT ( 'NONE',  ( 3.397511025282150321, -1.916906860828609727, 1.019255427985159779 ) ) ;
#168695=CARTESIAN_POINT ( 'NONE',  ( 2.631258204695927194, -1.703542010001803275, 0.6570300758180421807 ) ) ;
#168696=CARTESIAN_POINT ( 'NONE',  ( 0.3562053913853078790, -1.961198556353323186, -0.05404869553313899899 ) ) ;
#168697=CARTESIAN_POINT ( 'NONE',  ( 4.856716432673345629, -1.994826133969303195, -0.7102248925668596113 ) ) ;
#168700=CARTESIAN_POINT ( 'NONE',  ( 5.073898020828643496, -1.275178753180395530, 1.904781575909524349 ) ) ;
#168702=CARTESIAN_POINT ( 'NONE',  ( 6.720655732516650716, 2.975630972093906923, 2.379814465338329743 ) ) ;
#168704=CARTESIAN_POINT ( 'NONE',  ( 0.4695848928168535608, -1.793611485386744420, -1.130822890709509254 ) ) ;
#168709=CARTESIAN_POINT ( 'NONE',  ( 6.883263157960362477, -0.004191378316371896506, 2.053658919477070910 ) ) ;
#168712=CARTESIAN_POINT ( 'NONE',  ( 5.115861365725078436, 0.1511377038382749338, 2.010826595755777824 ) ) ;
#168714=CARTESIAN_POINT ( 'NONE',  ( 4.399324768961708543, -1.796976987717312291, 1.012281656189101264 ) ) ;
#168721=CARTESIAN_POINT ( 'NONE',  ( 0.5860218096905758234, -2.075098906900944673, -0.2538066186672620628 ) ) ;
#168722=CARTESIAN_POINT ( 'NONE',  ( 5.080704010962952211, -0.7231418808758652839, 1.882473355234378865 ) ) ;
#168723=CARTESIAN_POINT ( 'NONE',  ( 4.739718475747470627, 1.836682745182907972, 0.1304020654292817605 ) ) ;
#168726=CARTESIAN_POINT ( 'NONE',  ( 0.3578718668165404293, 0.6529773653428347924, 1.596609206317510132 ) ) ;
#168728=CARTESIAN_POINT ( 'NONE',  ( 0.9327830709247152408, -1.816692068203207056, -1.408362870467388950 ) ) ;
#168730=CARTESIAN_POINT ( 'NONE',  ( 1.036823874139713997, 2.229064601995099260, 0.3862009557947677640 ) ) ;
#168731=CARTESIAN_POINT ( 'NONE',  ( 2.912826151168836031, 1.525034000978764626, -1.452760968584436707 ) ) ;
#168733=B_SPLINE_CURVE_WITH_KNOTS ( 'NONE', 3,
 ( #208171, #110757, #159436, #44642, #11034, #146419, #77112, #59803, #143236, #58741, #124893, #209225, #42517, #108623, #174651, #192989, #213490, #130217, #131268, #81385, #165835, #15298, #117142, #147468, #98709, #17420, #197255, #198310, #67234, #100822, #66158, #34749, #65112, #164768, #64074, #48894, #182061, #196211, #166907, #115014, #33693, #16359, #51020, #83503, #149585, #183145, #181011, #82437, #1169, #32632, #49951, #133368, #18500, #132303, #84579, #148527, #93, #47852, #116071, #99769, #113963, #199374, #150666, #2228, #68304, #212432, #179960, #31583, #97658, #163716, #11795, #4061, #170860, #188169, #94969, #211876, #33138, #51526, #210563, #180214, #204965, #91265, #74147, #88259, #122992, #124050, #56823, #172720, #23229, #205181, #170562, #8060, #140240, #55750, #4826, #171632, #91482, #206262, #188950, #57887, #173804, #21083, #107779, #38438, #138084, #169501, #141324, #24298, #70905, #203043, #87186, #187875, #71975, #90402, #121906, #153251, #75213, #53620, #119753, #137016, #25382, #156472, #190016, #204098, #39502, #54684, #41668, #157542, #185732, #186810, #9139, #37365, #105600, #89341, #22145, #155389, #6972, #120834, #40590, #154328, #103440, #104518, #73053, #5902, #139152, #106695, #93619, #142381, #44871, #60023, #193224, #192138, #211589, #43803, #10198, #76273, #128327, #58959, #208390, #45935, #14453, #113115, #13399, #178054, #63225, #110976, #27520, #126175, #109916, #62168, #125114, #11262, #29672, #112054, #175927, #179120, #159661, #77339, #79475, #95756, #176982, #46998, #143452, #209449, #108844, #80544, #161808, #158599, #61094, #174870, #127253, #28600, #145593, #94688, #26450, #207337, #191072, #42738, #160730, #30743, #12323, #129388, #78404, #144524, #210534, #195367, #96824, #92559, #194290, #162873, #167134, #148747, #198532, #49124, #82663, #50179, #31807, #83729, #115242 ),
 .UNSPECIFIED., .F., .F.,
 ( 4, 1, 1, 1, 1, 1, 1, 1, 1, 1, 1, 1, 1, 1, 1, 1, 1, 1, 1, 1, 1, 1, 1, 1, 1, 1, 1, 1, 1, 1, 1, 1, 1, 1, 1, 1, 1, 1, 1, 1, 1, 1, 1, 1, 1, 1, 1, 1, 1, 1, 1, 1, 1, 1, 1, 1, 1, 1, 1, 1, 1, 1, 1, 1, 1, 1, 1, 1, 1, 1, 1, 1, 1, 1, 1, 1, 1, 1, 1, 1, 1, 1, 1, 1, 1, 1, 1, 1, 1, 1, 1, 1, 1, 1, 1, 1, 1, 1, 1, 1, 1, 1, 1, 1, 1, 1, 1, 1, 1, 1, 1, 1, 1, 1, 1, 1, 1, 1, 1, 1, 1, 1, 1, 1, 1, 1, 1, 1, 1, 1, 1, 1, 1, 1, 1, 1, 1, 1, 1, 1, 1, 1, 1, 1, 1, 1, 1, 1, 1, 1, 1, 1, 1, 1, 1, 1, 1, 1, 1, 1, 1, 1, 1, 1, 1, 1, 1, 1, 1, 1, 1, 1, 1, 1, 1, 1, 1, 1, 1, 1, 1, 1, 1, 1, 1, 1, 1, 1, 1, 1, 1, 1, 1, 1, 1, 1, 1, 1, 1, 1, 1, 1, 1, 1, 1, 1, 1, 1, 1, 1, 1, 1, 1, 1, 1, 1, 4 ),
 ( 0.000000000000000000, 0.004629629629629626771, 0.009259259259259253541, 0.01388888888888887771, 0.01851851851851850361, 0.02314814814814812952, 0.02777777777777775542, 0.03240740740740737785, 0.03703703703703700723, 0.04166666666666662966, 0.04629629629629625903, 0.05092592592592588147, 0.05555555555555549696, 0.06018518518518511939, 0.06481481481481474183, 0.06944444444444436426, 0.07407407407407398670, 0.07870370370370359525, 0.08333333333333321769, 0.08796296296296284012, 0.09259259259259246255, 0.09722222222222209886, 0.1018518518518517213, 0.1064814814814813299, 0.1111111111111109523, 0.1157407407407405747, 0.1203703703703701972, 0.1249999999999998196, 0.1296296296296294281, 0.1342592592592590506, 0.1388888888888886730, 0.1435185185185182954, 0.1481481481481479179, 0.1527777777777775403, 0.1574074074074071627, 0.1620370370370367852, 0.1666666666666664076, 0.1712962962962960300, 0.1759259259259256525, 0.1805555555555552749, 0.1851851851851848973, 0.1898148148148145198, 0.1944444444444441145, 0.1990740740740737091, 0.2037037037037033038, 0.2083333333333328985, 0.2129629629629625209, 0.2175925925925921156, 0.2222222222222217103, 0.2268518518518513050, 0.2314814814814808996, 0.2361111111111104943, 0.2407407407407401168, 0.2453703703703697114, 0.2499999999999993061, 0.2546296296296289285, 0.2592592592592585232, 0.2638888888888881179, 0.2685185185185177126, 0.2731481481481473073, 0.2777777777777769019, 0.2824074074074064966, 0.2870370370370360913, 0.2916666666666656860, 0.2962962962962952806, 0.3009259259259249308, 0.3055555555555545255, 0.3101851851851841202, 0.3148148148148137149, 0.3194444444444433095, 0.3240740740740729042, 0.3287037037037024989, 0.3333333333333320936, 0.3379629629629616883, 0.3425925925925912829, 0.3472222222222209331, 0.3518518518518505278, 0.3564814814814801225, 0.3611111111111097172, 0.3657407407407393118, 0.3703703703703689065, 0.3749999999999985567, 0.3796296296296282069, 0.3842592592592578571, 0.3888888888888874518, 0.3935185185185171020, 0.3981481481481467521, 0.4027777777777764023, 0.4074074074074060525, 0.4120370370370357027, 0.4166666666666652974, 0.4212962962962949476, 0.4259259259259245978, 0.4305555555555542480, 0.4351851851851838981, 0.4398148148148135483, 0.4444444444444431430, 0.4490740740740727932, 0.4537037037037024434, 0.4583333333333320936, 0.4629629629629617438, 0.4675925925925913940, 0.4722222222222209886, 0.4768518518518506388, 0.4814814814814802890, 0.4861111111111099392, 0.4907407407407395894, 0.4953703703703692396, 0.4999999999999988898, 0.5046296296296285400, 0.5092592592592581902, 0.5138888888888878403, 0.5185185185185173795, 0.5231481481481470297, 0.5277777777777766799, 0.5324074074074063301, 0.5370370370370359803, 0.5416666666666656305, 0.5462962962962952806, 0.5509259259259249308, 0.5555555555555545810, 0.5601851851851842312, 0.5648148148148138814, 0.5694444444444435316, 0.5740740740740730708, 0.5787037037037027210, 0.5833333333333323711, 0.5879629629629620213, 0.5925925925925916715, 0.5972222222222213217, 0.6018518518518509719, 0.6064814814814806221, 0.6111111111111102723, 0.6157407407407399225, 0.6203703703703695727, 0.6249999999999992228, 0.6296296296296287620, 0.6342592592592584122, 0.6388888888888880624, 0.6435185185185177126, 0.6481481481481473628, 0.6527777777777770130, 0.6574074074074066631, 0.6620370370370363133, 0.6666666666666659635, 0.6712962962962956137, 0.6759259259259252639, 0.6805555555555549141, 0.6851851851851845643, 0.6898148148148141034, 0.6944444444444437536, 0.6990740740740734038, 0.7037037037037030540, 0.7083333333333327042, 0.7129629629629623544, 0.7175925925925920046, 0.7222222222222216548, 0.7268518518518513050, 0.7314814814814809552, 0.7361111111111106053, 0.7407407407407402555, 0.7453703703703697947, 0.7499999999999994449, 0.7546296296296290951, 0.7592592592592586342, 0.7638888888888882844, 0.7685185185185179346, 0.7731481481481475848, 0.7777777777777772350, 0.7824074074074068852, 0.7870370370370365354, 0.7916666666666661856, 0.7962962962962958358, 0.8009259259259254859, 0.8055555555555551361, 0.8101851851851847863, 0.8148148148148143255, 0.8194444444444439757, 0.8240740740740736259, 0.8287037037037032761, 0.8333333333333329263, 0.8379629629629625764, 0.8425925925925922266, 0.8472222222222218768, 0.8518518518518515270, 0.8564814814814811772, 0.8611111111111108274, 0.8657407407407404776, 0.8703703703703701278, 0.8749999999999996669, 0.8796296296296293171, 0.8842592592592589673, 0.8888888888888886175, 0.8935185185185182677, 0.8981481481481479179, 0.9027777777777775681, 0.9074074074074072183, 0.9120370370370368684, 0.9166666666666665186, 0.9212962962962961688, 0.9259259259259258190, 0.9305555555555553582, 0.9351851851851850084, 0.9398148148148146586, 0.9444444444444443088, 0.9490740740740739589, 0.9537037037037036091, 0.9583333333333332593, 0.9629629629629629095, 0.9675925925925925597, 0.9722222222222222099, 0.9768518518518518601, 0.9814814814814815103, 0.9861111111111110494, 0.9907407407407406996, 0.9953703703703703498, 1.000000000000000000 ),
 .UNSPECIFIED. ) ;
#168740=CARTESIAN_POINT ( 'NONE',  ( 5.554997651100567424, 0.4332456915393156915, 2.178594967391647597 ) ) ;
#168741=CARTESIAN_POINT ( 'NONE',  ( 1.922082643403967506, 1.260107670313360240, -1.792737600334909365 ) ) ;
#168744=CARTESIAN_POINT ( 'NONE',  ( 5.283633159863808437, -1.863482887291990409, 0.6137318589548645953 ) ) ;
#168746=CARTESIAN_POINT ( 'NONE',  ( 6.890000000000006786, 1.992106636881568305, 2.580154195607385237 ) ) ;
#168749=CARTESIAN_POINT ( 'NONE',  ( 4.078469121099765005, 1.002472831208834680, 1.868716877859360137 ) ) ;
#168751=ORIENTED_EDGE ( 'NONE', *, *, #161480, .F. ) ;
#168753=CARTESIAN_POINT ( 'NONE',  ( 6.737200384369169903, -1.933438233944267060, 0.9670071574134844195 ) ) ;
#168755=CARTESIAN_POINT ( 'NONE',  ( 4.722110844128335039, 1.763445737372179689, 0.5296355584529164329 ) ) ;
#168758=CARTESIAN_POINT ( 'NONE',  ( 0.5557209801456406417, -1.262220463910254331, 1.198535436172887714 ) ) ;
#168761=CARTESIAN_POINT ( 'NONE',  ( 5.155217493315787713, -1.824165352752779246, -1.159627250419709155 ) ) ;
#168765=CARTESIAN_POINT ( 'NONE',  ( 4.276362541559985075, -1.246951984143488623, 1.765614359104182629 ) ) ;
#168767=CARTESIAN_POINT ( 'NONE',  ( 5.079350664050449105, 1.840474797211266944, -0.7068060451330003824 ) ) ;
#168768=CARTESIAN_POINT ( 'NONE',  ( 4.077271355118361029, 1.226738060269889408, -1.225556752838660168 ) ) ;
#168769=CARTESIAN_POINT ( 'NONE',  ( 0.5389544483674936215, -1.876709678404146153, 1.131566444868239874 ) ) ;
#168770=CARTESIAN_POINT ( 'NONE',  ( 1.958496456072187142, 2.301298802517747877, -0.1708829291464097622 ) ) ;
#168771=CARTESIAN_POINT ( 'NONE',  ( 4.481748981177747559, 1.343215529357727478, 1.562995469165892493 ) ) ;
#168772=CARTESIAN_POINT ( 'NONE',  ( 6.251511512115349056, 1.936530502255621622, -0.1475284815631947022 ) ) ;
#168779=CARTESIAN_POINT ( 'NONE',  ( 2.995379075007987613, 1.893430763284314811, -1.133229021217339483 ) ) ;
#168781=CARTESIAN_POINT ( 'NONE',  ( 0.5845111633032008536, 1.778450750175617712, 0.5478710867917855332 ) ) ;
#168786=CARTESIAN_POINT ( 'NONE',  ( 6.825078400183550720, 0.5766433668599518780, 2.097246334241170906 ) ) ;
#168787=CARTESIAN_POINT ( 'NONE',  ( 5.982333729491329244, -0.2747192703472668418, -1.820405398140816589 ) ) ;
#168789=CARTESIAN_POINT ( 'NONE',  ( 3.274343757225039120, -1.228935477529419451, 1.654214949985348904 ) ) ;
#168792=CARTESIAN_POINT ( 'NONE',  ( 2.736978119973699108, 1.902454848370996210, 0.6784627630139413723 ) ) ;
#168795=CARTESIAN_POINT ( 'NONE',  ( 1.622021928100621624, -1.144040325636319189, -1.713970819250490552 ) ) ;
#168799=( BOUNDED_CURVE ( )  B_SPLINE_CURVE ( 3, ( #154817, #57313, #123477, #41082 ),
 .UNSPECIFIED., .F., .T. ) 
 B_SPLINE_CURVE_WITH_KNOTS ( ( 4, 4 ),
 ( 0.000000000000000000, 0.4999999999999986677 ),
 .UNSPECIFIED. ) 
 CURVE ( )  GEOMETRIC_REPRESENTATION_ITEM ( )  RATIONAL_B_SPLINE_CURVE ( ( 1.000000000000000222, 0.3333333333333352022, 0.3333333333333334259, 0.9999999999999984457 ) ) 
 REPRESENTATION_ITEM ( '' )  );
#168801=CARTESIAN_POINT ( 'NONE',  ( 5.180388087185870738, -1.228261608319089149, 1.833297759731546073 ) ) ;
#168802=CARTESIAN_POINT ( 'NONE',  ( 1.229993901927586286, -1.370328181169593096, -1.671761099108048265 ) ) ;
#168804=CARTESIAN_POINT ( 'NONE',  ( 0.9718890779336667451, -0.9023411006064323558, 1.803417998987096427 ) ) ;
#168806=CARTESIAN_POINT ( 'NONE',  ( 1.968534425330380921, 1.910819170882430695, 1.277001204893423170 ) ) ;
#168808=CARTESIAN_POINT ( 'NONE',  ( 6.322915745023367506, 1.413667134151237459, -1.287952294376143447 ) ) ;
#168811=CARTESIAN_POINT ( 'NONE',  ( 1.639302681421180852, -1.352760811461351187, -1.292285834730775074 ) ) ;
#168812=CARTESIAN_POINT ( 'NONE',  ( 3.801970467005914678, -1.040791964576088358, -1.727064642965264740 ) ) ;
#168816=CARTESIAN_POINT ( 'NONE',  ( 5.619784395276031574, -2.055015178219528948, 0.4601488667864346849 ) ) ;
#168821=CARTESIAN_POINT ( 'NONE',  ( 4.781513128076603003, 0.1936695275622651868, -2.010448953515688419 ) ) ;
#168823=CARTESIAN_POINT ( 'NONE',  ( 0.7255239074139888666, 0.2060675592777498066, -2.052282084198739920 ) ) ;
#168830=CARTESIAN_POINT ( 'NONE',  ( 3.420551359632235222, 0.9736478647841840806, 1.940675715818460878 ) ) ;
#168833=CARTESIAN_POINT ( 'NONE',  ( 1.786409390178132162, 1.601450680722369846, -0.9084932335857234253 ) ) ;
#168834=MANIFOLD_SOLID_BREP ( 'Sweep1[1]', #174487 ) ;
#168836=CARTESIAN_POINT ( 'NONE',  ( 3.825867475279482566, 1.171244075711602051, -1.852137614134836907 ) ) ;
#168838=CARTESIAN_POINT ( 'NONE',  ( 5.102513680054168610, -0.7571875712604788644, -2.132187818420825831 ) ) ;
#168846=CARTESIAN_POINT ( 'NONE',  ( 5.079261616685217362, 1.651278277306899911, -0.6370931631965012221 ) ) ;
#168848=CARTESIAN_POINT ( 'NONE',  ( 1.712088352014268899, -2.090129137712465557, 0.2570578816783394283 ) ) ;
#168851=CARTESIAN_POINT ( 'NONE',  ( 2.418351439525995961, 0.8393807748916733980, 1.781860320225916228 ) ) ;
#168853=CARTESIAN_POINT ( 'NONE',  ( 0.3911966820569385828, 1.383097094795827209, 1.259704262696823118 ) ) ;
#168855=CARTESIAN_POINT ( 'NONE',  ( 5.308800944376626418, -0.4481363076810992996, -1.755139329022289196 ) ) ;
#168860=CARTESIAN_POINT ( 'NONE',  ( 5.805500895539822181, -0.4530025297027095443, 1.814837910242727226 ) ) ;
#168861=CARTESIAN_POINT ( 'NONE',  ( 5.401260523219934662, -1.778462342247935979, 1.059464396209061521 ) ) ;
#168870=CARTESIAN_POINT ( 'NONE',  ( 4.809014631063706524, -1.576880339463518022, 1.167019128429528374 ) ) ;
#168872=CARTESIAN_POINT ( 'NONE',  ( 3.743517394402117837, -1.942243990624907823, -0.5404084370827857420 ) ) ;
#168873=CARTESIAN_POINT ( 'NONE',  ( 2.219824929201766217, 0.8990433841352833966, -1.691613514901336490 ) ) ;
#168875=CARTESIAN_POINT ( 'NONE',  ( 0.2049558871960316941, 1.909868400323280424, 1.074723926240577221 ) ) ;
#168876=CARTESIAN_POINT ( 'NONE',  ( 0.1333692844072802142, 2.017199222642913625, -2.468757726274827036 ) ) ;
#168877=CARTESIAN_POINT ( 'NONE',  ( 1.721729502718066795, -1.034818790731323990, -1.558030248997283040 ) ) ;
#168879=CARTESIAN_POINT ( 'NONE',  ( 4.113543134289789016, 1.619545278408863975, 1.195698625712667384 ) ) ;
#168882=CARTESIAN_POINT ( 'NONE',  ( 4.833676624637527119, 0.6627930923091308602, -2.010898772050497829 ) ) ;
#168884=CARTESIAN_POINT ( 'NONE',  ( 6.584440175795505112, 1.195396180001909059, -1.690200020538407566 ) ) ;
#168885=CARTESIAN_POINT ( 'NONE',  ( 1.417645169044414288, -1.164320182712182294, -1.736329362061867387 ) ) ;
#168886=CARTESIAN_POINT ( 'NONE',  ( 6.620655732516628866, 4.686767102414819419, 2.836268676114994669 ) ) ;
#168887=CARTESIAN_POINT ( 'NONE',  ( 6.756878055424797580, -1.408711550780303634, 1.160885376127060775 ) ) ;
#168897=CARTESIAN_POINT ( 'NONE',  ( 0.8206315121990900296, 1.372318096965993384, -1.182507040619881877 ) ) ;
#168905=CARTESIAN_POINT ( 'NONE',  ( 6.187125092307005580, 1.678016663812756937, 1.117817459622950649 ) ) ;
#168906=CARTESIAN_POINT ( 'NONE',  ( 0.3992906662320141464, -0.2637550127744873185, -2.103967267096308991 ) ) ;
#168909=CARTESIAN_POINT ( 'NONE',  ( 0.1405533004714383249, 7.629137130509051623, -2.879722665736083709 ) ) ;
#168913=CARTESIAN_POINT ( 'NONE',  ( 3.977371423044063103, -0.1491618029233315879, 1.963883198941584585 ) ) ;
#168914=CARTESIAN_POINT ( 'NONE',  ( 4.130482583401101415, 0.5405105419177670401, 1.942537254285629400 ) ) ;
#168918=CARTESIAN_POINT ( 'NONE',  ( 4.787173061057010237, 1.622617466453496471, 1.473133629693436975 ) ) ;
#168920=CARTESIAN_POINT ( 'NONE',  ( 2.608320942171663326, -0.7355144804263250569, -1.780640224430999563 ) ) ;
#168922=CARTESIAN_POINT ( 'NONE',  ( -0.02948999725180430354, 5.724051133006486936, -2.520349822069901879 ) ) ;
#168929=CARTESIAN_POINT ( 'NONE',  ( 5.401205523299864808, -1.691175329543142647, 1.008977833701154125 ) ) ;
#168930=CARTESIAN_POINT ( 'NONE',  ( 0.5384922876028491734, -1.664970009179422616, 0.9995421319052009146 ) ) ;
#168931=CARTESIAN_POINT ( 'NONE',  ( 4.512362120423671463, -2.012691318418479813, -0.04721358428917859368 ) ) ;
#168932=CARTESIAN_POINT ( 'NONE',  ( 5.940817214068299990, 1.361788364613376601, 1.851425077211141801 ) ) ;
#168934=CARTESIAN_POINT ( 'NONE',  ( 4.205779932802704124, 0.6304169756579135475, -1.751020666094662337 ) ) ;
#168940=CARTESIAN_POINT ( 'NONE',  ( 0.2225716830646235489, 2.098996182288978218, 0.6302611576235671587 ) ) ;
#168945=CARTESIAN_POINT ( 'NONE',  ( 0.6975366375942676500, -0.6598540886826111951, 1.702458561391326342 ) ) ;
#168947=CARTESIAN_POINT ( 'NONE',  ( 2.566726881135486416, -0.8894074178381355944, 1.488501414198806883 ) ) ;
#168948=CARTESIAN_POINT ( 'NONE',  ( 6.609000000000009756, 0.005669918681722520802, 1.900160851458796873 ) ) ;
#168950=CARTESIAN_POINT ( 'NONE',  ( 5.813091150998386247, 1.612263477354998864, 0.8566026058636074803 ) ) ;
#168951=CARTESIAN_POINT ( 'NONE',  ( 2.887496479553632422, -1.832211488775811414, 0.7015765724691160887 ) ) ;
#168955=CARTESIAN_POINT ( 'NONE',  ( 5.004590575528129470, -2.104527602236761386, -0.2589986953433416894 ) ) ;
#168958=CARTESIAN_POINT ( 'NONE',  ( 1.411079811451225074, -1.634442866182721277, 1.270590680402396311 ) ) ;
#168961=CARTESIAN_POINT ( 'NONE',  ( 4.196076301648347773, 1.450992468586336459, 1.681961854464069983 ) ) ;
#168962=EDGE_LOOP ( 'NONE', ( #855, #22619, #2707, #8315 ) ) ;
#168963=CARTESIAN_POINT ( 'NONE',  ( 3.305630555216050759, 1.456526447221625276, -1.778376517212407748 ) ) ;
#168969=CARTESIAN_POINT ( 'NONE',  ( 6.609000000000038177, 0.002801690667396730672, 2.000160786441218530 ) ) ;
#168973=CARTESIAN_POINT ( 'NONE',  ( 3.340010735810138520, -1.142844047782382466, -1.533173144288489276 ) ) ;
#168975=CARTESIAN_POINT ( 'NONE',  ( 4.278129899785966472, -0.9921777787025712891, 1.410595609005516504 ) ) ;
#168976=CARTESIAN_POINT ( 'NONE',  ( 3.960172920142067898, -1.157100329752266621, 1.651342637023434090 ) ) ;
#168978=CARTESIAN_POINT ( 'NONE',  ( 4.114144448104863017, 0.1132377192244668207, 2.296027709189680799 ) ) ;
#168980=CARTESIAN_POINT ( 'NONE',  ( 6.639294477394681593, -1.882217795646949687, 0.9450163710809048601 ) ) ;
#168982=CARTESIAN_POINT ( 'NONE',  ( 4.376060336092471026, -1.020005645217741064, 1.445989269263460386 ) ) ;
#168984=CARTESIAN_POINT ( 'NONE',  ( 0.3930492761001015967, 1.902410075555853064, -1.278529456123769892 ) ) ;
#168985=CARTESIAN_POINT ( 'NONE',  ( 6.492148756324659153, -0.4961259030743305209, -1.772972609911625419 ) ) ;
#168988=CARTESIAN_POINT ( 'NONE',  ( 6.052700813158568671, -1.877759139263988075, -1.129571069393126459 ) ) ;
#168992=CARTESIAN_POINT ( 'NONE',  ( 0.4148109920584437948, 0.8315006815404235585, 2.005833495578440928 ) ) ;
#168993=CARTESIAN_POINT ( 'NONE',  ( 0.7785302072789467287, -0.4946362931835950327, -1.954778448132548752 ) ) ;
#168995=CARTESIAN_POINT ( 'NONE',  ( 4.600175520841607302, -1.926116679539988885, -0.04579137001822254638 ) ) ;
#168997=CARTESIAN_POINT ( 'NONE',  ( 0.6509960782678033686, 2.189857587618043055, 0.3722473809256007793 ) ) ;
#168998=DIRECTION ( 'NONE',  ( -0.9999980456341537316, 0.000000000000000000, -0.001977050295958626257 ) ) ;
#169006=CARTESIAN_POINT ( 'NONE',  ( 4.475936636375839051, -1.689578365139619009, -0.4171736215478424881 ) ) ;
#169007=CARTESIAN_POINT ( 'NONE',  ( 1.926150285298435572, 1.005797860886543660, 1.684270608208485065 ) ) ;
#169011=CARTESIAN_POINT ( 'NONE',  ( 0.3970293196923400658, 0.3510089794473401081, 2.032437512258952417 ) ) ;
#169014=CARTESIAN_POINT ( 'NONE',  ( 5.331267653506235327, -1.592659417495114083, -1.236803018183525449 ) ) ;
#169015=CARTESIAN_POINT ( 'NONE',  ( 1.165308694782108301, -2.046298710749935079, -0.9655196508330918803 ) ) ;
#169019=CARTESIAN_POINT ( 'NONE',  ( 1.317418832401914930, -1.826178791559311509, 0.4043020138455517554 ) ) ;
#169020=CARTESIAN_POINT ( 'NONE',  ( 0.4571073982213811893, -1.631979074848688205, -0.5868837268243607408 ) ) ;
#169021=CARTESIAN_POINT ( 'NONE',  ( 3.773127072069931032, 2.063069237518061705, -0.7396954945804237180 ) ) ;
#169022=CARTESIAN_POINT ( 'NONE',  ( 6.053837855137599533, 0.6775820993057954933, -2.205875079116952797 ) ) ;
#169023=CARTESIAN_POINT ( 'NONE',  ( 1.657177242756900926, -1.767118338917167852, -1.060216354352721435 ) ) ;
#169024=CARTESIAN_POINT ( 'NONE',  ( 3.275267064432846098, 1.232403799581788251, 1.500778006584954749 ) ) ;
#169026=CARTESIAN_POINT ( 'NONE',  ( 5.518772846390051612, 1.727975122137341613, 0.7167417953098526029 ) ) ;
#169030=CARTESIAN_POINT ( 'NONE',  ( 4.184220324914634581, 1.621181886760931778, 1.198861198883696799 ) ) ;
#169034=CARTESIAN_POINT ( 'NONE',  ( 1.611646134362737959, -1.812087876328593916, 0.2219229778191167957 ) ) ;
#169043=CARTESIAN_POINT ( 'NONE',  ( 5.531901104011129000, -1.969946598288346618, 0.4446316349850876759 ) ) ;
#169044=CARTESIAN_POINT ( 'NONE',  ( -0.1046615654881309365, -0.1561857951268459388, -2.086345279447648249 ) ) ;
#169048=CARTESIAN_POINT ( 'NONE',  ( 5.313377624208335703, -0.3045090135303843981, 2.038146128872863283 ) ) ;
#169049=CARTESIAN_POINT ( 'NONE',  ( 4.817029820108094995, 1.034167108704350024, -1.730865207599366240 ) ) ;
#169057=CARTESIAN_POINT ( 'NONE',  ( 3.884138610457484653, -0.1511163893381066714, 2.010518618204664154 ) ) ;
#169058=CARTESIAN_POINT ( 'NONE',  ( 3.310337721246572773, 1.664907390794263531, 0.7863323413084821745 ) ) ;
#169060=CARTESIAN_POINT ( 'NONE',  ( 2.649405215588944262, -1.917952202864357414, 1.283049733485057908 ) ) ;
#169062=CARTESIAN_POINT ( 'NONE',  ( 4.850933092205481856, -1.739298515662604405, 1.283314429840809234 ) ) ;
#169064=CARTESIAN_POINT ( 'NONE',  ( 0.3978616433950994957, -0.6552777965449173569, -1.828281909955962181 ) ) ;
#169066=CARTESIAN_POINT ( 'NONE',  ( 6.890000000000007674, 7.629137130509070275, 2.600000000000001421 ) ) ;
#169068=CARTESIAN_POINT ( 'NONE',  ( 1.938157646728836614, 1.849873822469105145, 0.2772664081076986475 ) ) ;
#169070=CARTESIAN_POINT ( 'NONE',  ( 6.737195113697223903, -1.761045485681483669, 0.8863934713586976155 ) ) ;
#169073=CARTESIAN_POINT ( 'NONE',  ( 1.207977004800918852, -0.5332226995428279714, 2.141375170867452660 ) ) ;
#169079=CARTESIAN_POINT ( 'NONE',  ( 5.752796013432011080, -1.554615333184097059, 1.212288997074702834 ) ) ;
#169080=CARTESIAN_POINT ( 'NONE',  ( 0.6050338814152752542, -0.7811975584859867094, -2.171474816401474328 ) ) ;
#169081=CARTESIAN_POINT ( 'NONE',  ( 0.5901948623465642640, 1.011764341257429978, -1.680720577067334354 ) ) ;
#169082=CARTESIAN_POINT ( 'NONE',  ( 4.065324354713106381, 1.766439233411433163, 1.064669890786486661 ) ) ;
#169090=CARTESIAN_POINT ( 'NONE',  ( 6.795391773274086944, -1.942485666075419060, 0.9701230550103381312 ) ) ;
#169092=CARTESIAN_POINT ( 'NONE',  ( 5.020983453748395497, -1.746657797055195305, 0.5827527221545365510 ) ) ;
#169095=CARTESIAN_POINT ( 'NONE',  ( 0.7900579835180140398, -1.855660487967484951, -0.2351621623290362506 ) ) ;
#169101=CARTESIAN_POINT ( 'NONE',  ( 0.7680391878876170475, 1.910087531778673187, -0.09433495293535018589 ) ) ;
#169102=CARTESIAN_POINT ( 'NONE',  ( 1.498528727375374459, 1.449451107477307987, -1.015301706168385998 ) ) ;
#169103=CARTESIAN_POINT ( 'NONE',  ( 6.059245300855401695, -1.699386736952392285, 1.078915776541150340 ) ) ;
#169105=CARTESIAN_POINT ( 'NONE',  ( 3.989770193594462722, -1.910233455636681787, 0.1444642847954723808 ) ) ;
#169106=CARTESIAN_POINT ( 'NONE',  ( -0.1409997244345879697, 0.2375178066936211585, -2.034344168881811132 ) ) ;
#169107=CARTESIAN_POINT ( 'NONE',  ( 4.984792273111487759, 1.884092017856910273, 0.5737924883163454393 ) ) ;
#169108=CARTESIAN_POINT ( 'NONE',  ( 6.135022435551370279, 1.886083186425246971, 0.7231739236989165320 ) ) ;
#169111=CARTESIAN_POINT ( 'NONE',  ( 4.364026845288040413, 0.8817440624687390427, 1.649792572839225091 ) ) ;
#169112=CARTESIAN_POINT ( 'NONE',  ( 5.813083859329478464, 1.524454967706680319, 0.8070229810451818864 ) ) ;
#169114=CARTESIAN_POINT ( 'NONE',  ( 3.703933201646680828, -0.6411959742554216302, 2.111683309420588905 ) ) ;
#169117=CARTESIAN_POINT ( 'NONE',  ( 0.3091261446717024630, -1.657722840873154135, 1.227268292441574538 ) ) ;
#169126=CARTESIAN_POINT ( 'NONE',  ( 3.684089399883890614, -1.230936008959164996, -1.664559344884769088 ) ) ;
#169130=CARTESIAN_POINT ( 'NONE',  ( 0.5924517288934522119, -1.120073279264972799, 1.680413856445305498 ) ) ;
#169132=CARTESIAN_POINT ( 'NONE',  ( 0.1747926744264677035, 1.388892567315727744, -2.112808070315982167 ) ) ;
#169134=CARTESIAN_POINT ( 'NONE',  ( 6.239611212763971793, -1.913511330438378177, -0.6350998681113121380 ) ) ;
#169135=CARTESIAN_POINT ( 'NONE',  ( 5.454270856000166923, -1.210104932453776039, 1.485173795633880633 ) ) ;
#169136=CARTESIAN_POINT ( 'NONE',  ( 6.539320575229292665, 2.014857154840712372, 2.506613887083661840 ) ) ;
#169137=CARTESIAN_POINT ( 'NONE',  ( 4.195009555701286530, 1.760677850468267414, 1.304791629949946019 ) ) ;
#169139=CARTESIAN_POINT ( 'NONE',  ( 2.109489925670060551, 1.480643174185194200, 1.210387159491378650 ) ) ;
#169144=CARTESIAN_POINT ( 'NONE',  ( 1.405875298092047698, -1.122519365368032984, -1.674874950958963549 ) ) ;
#169147=CARTESIAN_POINT ( 'NONE',  ( 6.427279137517246888, -1.429865906218323435, -1.660902671979214595 ) ) ;
#169149=CARTESIAN_POINT ( 'NONE',  ( 2.854212618329458717, 0.5792176767629078071, 1.624745991979989812 ) ) ;
#169151=CARTESIAN_POINT ( 'NONE',  ( -0.1399997263889594112, -0.002789056014654289761, -2.000146600338557956 ) ) ;
#169154=CARTESIAN_POINT ( 'NONE',  ( 0.07735805125222164347, -0.0005418671161615787497, -2.088975025666544916 ) ) ;
#169155=CARTESIAN_POINT ( 'NONE',  ( 1.785527960060459440, -1.848404783191982315, 0.6579185095809261252 ) ) ;
#169162=CARTESIAN_POINT ( 'NONE',  ( 4.230988290566616072, 1.657980831523006460, 0.7301630082575115699 ) ) ;
#169166=CARTESIAN_POINT ( 'NONE',  ( 4.881432045509231266, 0.1721252788823707247, -1.803262557370821417 ) ) ;
#169171=CARTESIAN_POINT ( 'NONE',  ( 4.650750022344506185, -0.4068995778509130190, -1.815856201304208550 ) ) ;
#169173=CARTESIAN_POINT ( 'NONE',  ( 2.302218516519896507, 1.249579790052034456, -1.452036884154449314 ) ) ;
#169180=CARTESIAN_POINT ( 'NONE',  ( 0.09294085500742563233, -0.4768749645070144982, -2.116232079886640971 ) ) ;
#169182=CARTESIAN_POINT ( 'NONE',  ( 1.587951679898065294, -2.080713178594826296, -0.2033740637906420179 ) ) ;
#169184=CARTESIAN_POINT ( 'NONE',  ( 5.965835030274156736, 1.897794126051439045, -0.3298099971670089281 ) ) ;
#169186=CARTESIAN_POINT ( 'NONE',  ( 2.608196206841297826, -0.6965810133783244540, -1.687657492251873226 ) ) ;
#169189=CARTESIAN_POINT ( 'NONE',  ( 2.355592738034977263, -1.419685808644566949, -1.281520755053264571 ) ) ;
#169190=CARTESIAN_POINT ( 'NONE',  ( 1.644903635585378554, -0.2856866470503526823, -1.948579891484893079 ) ) ;
#169191=CARTESIAN_POINT ( 'NONE',  ( 4.071774441262452804, -1.115447612638842401, 1.589602391900000411 ) ) ;
#169192=ORIENTED_EDGE ( 'NONE', *, *, #168663, .T. ) ;
#169195=CARTESIAN_POINT ( 'NONE',  ( 4.025719079702368752, -0.3592959752154977204, 2.089770972018199835 ) ) ;
#169203=CARTESIAN_POINT ( 'NONE',  ( 3.422296110638740174, 1.157362003623555236, -1.411967061744797691 ) ) ;
#169210=CARTESIAN_POINT ( 'NONE',  ( 4.838664814796108438, 0.3202261158844340594, 1.842872994462002367 ) ) ;
#169212=CARTESIAN_POINT ( 'NONE',  ( 2.174328269389655066, -1.185172859381509625, 1.518732482018339436 ) ) ;
#169219=CARTESIAN_POINT ( 'NONE',  ( 0.9138395863287234189, -1.346417975848941406, -1.633941036375158973 ) ) ;
#169222=CARTESIAN_POINT ( 'NONE',  ( 6.016483110937820733, 0.8336820848486149460, 1.895147399281302825 ) ) ;
#169223=CARTESIAN_POINT ( 'NONE',  ( 0.5031362391596030381, -1.832460416942282011, 0.1798594046882526221 ) ) ;
#169225=CARTESIAN_POINT ( 'NONE',  ( 0.2460673368967214447, -2.230335335914147343, -0.5547215216719133535 ) ) ;
#169229=CARTESIAN_POINT ( 'NONE',  ( 1.922231132759700589, 1.317440867170904362, -1.875679006090027690 ) ) ;
#169233=CARTESIAN_POINT ( 'NONE',  ( 6.404245030721173570, 1.437354257190478490, -1.306004427266238777 ) ) ;
#169238=CARTESIAN_POINT ( 'NONE',  ( 6.345967646908174054, -1.254484226688237447, -1.443505786478386899 ) ) ;
#169239=CARTESIAN_POINT ( 'NONE',  ( 6.262907710099242742, -0.1037740067610822270, -2.014008436551452785 ) ) ;
#169243=CARTESIAN_POINT ( 'NONE',  ( 2.554727279587006183, -1.819456544085126026, -1.029573916123826427 ) ) ;
#169244=CARTESIAN_POINT ( 'NONE',  ( 1.217257651388839346, -1.727774110360464244, 0.3828142623626716867 ) ) ;
#169247=CARTESIAN_POINT ( 'NONE',  ( 4.224787546089771695, 0.1105535957067731723, 2.289718640476182898 ) ) ;
#169248=CARTESIAN_POINT ( 'NONE',  ( 3.046520963529773862, -1.423092868940859956, -1.001465238821471315 ) ) ;
#169253=CARTESIAN_POINT ( 'NONE',  ( 3.163173391212137808, -0.5009769021222918450, -1.659887746298273514 ) ) ;
#169254=CARTESIAN_POINT ( 'NONE',  ( 3.754478802441584495, -2.168521383071635000, -0.1100146688530565936 ) ) ;
#169256=CARTESIAN_POINT ( 'NONE',  ( 4.171111447311355747, 1.799123655847803205, -0.9110083886025857058 ) ) ;
#169257=CARTESIAN_POINT ( 'NONE',  ( 1.656250000000001554, -1.895863743164051485, 0.7852924748300756930 ) ) ;
#169259=CARTESIAN_POINT ( 'NONE',  ( 1.746969779936607292, -1.628684531152933657, 1.028491977540356705 ) ) ;
#169261=CARTESIAN_POINT ( 'NONE',  ( 4.148835382215973588, 2.178989060337086503, 0.4312644480095380040 ) ) ;
#169263=CARTESIAN_POINT ( 'NONE',  ( -0.1106856583840877956, 1.350702755748961481, -2.249207804202685956 ) ) ;
#169268=CARTESIAN_POINT ( 'NONE',  ( 1.102519259163890153, -0.9942956747860592914, 1.986404433118430291 ) ) ;
#169269=CARTESIAN_POINT ( 'NONE',  ( 5.494571831323358246, 1.932540981948445147, 0.3370517209014682325 ) ) ;
#169272=CARTESIAN_POINT ( 'NONE',  ( 6.608658273995139609, 1.683185115790312603, -1.511970481837302760 ) ) ;
#169275=CARTESIAN_POINT ( 'NONE',  ( 3.648931631147700472, -0.3995851234466942792, -2.023444851274053491 ) ) ;
#169279=CARTESIAN_POINT ( 'NONE',  ( 4.850782132498069998, -1.503350029756752804, 1.112868480285071460 ) ) ;
#169280=CARTESIAN_POINT ( 'NONE',  ( 4.096141260758720648, -0.2909454306243773325, 1.709365352543093186 ) ) ;
#169281=CARTESIAN_POINT ( 'NONE',  ( 3.544249451937312667, -1.420498570261208959, 1.005328601869423633 ) ) ;
#169282=CARTESIAN_POINT ( 'NONE',  ( 0.8379086502938500880, 0.9226890658239239595, -2.098657079483890353 ) ) ;
#169284=CARTESIAN_POINT ( 'NONE',  ( 5.653879428721274358, 0.8482012749469816093, 1.911158475179574046 ) ) ;
#169285=CARTESIAN_POINT ( 'NONE',  ( 6.316353394666050391, 1.812894500769960837, 0.6965700268309078513 ) ) ;
#169288=CARTESIAN_POINT ( 'NONE',  ( 2.022111496571117772, -1.799922141918413487, 0.9091460122201827643 ) ) ;
#169289=CARTESIAN_POINT ( 'NONE',  ( 0.1292129718690297469, -2.001788180159810970, 0.8922102942980970619 ) ) ;
#169293=CARTESIAN_POINT ( 'NONE',  ( 2.807414684038778141, 1.817529592918063708, -1.092056846721880969 ) ) ;
#169295=CARTESIAN_POINT ( 'NONE',  ( 4.969292227364340953, 0.1756445257206709631, -1.817221496977147854 ) ) ;
#169303=CARTESIAN_POINT ( 'NONE',  ( 2.215108757275308982, 1.619595947845490436, -1.206587912388109141 ) ) ;
#169304=CARTESIAN_POINT ( 'NONE',  ( 0.1476710321905516377, -1.628112296142746995, -1.335496995165935674 ) ) ;
#169306=CARTESIAN_POINT ( 'NONE',  ( 3.766312297878508630, -0.7504043340197141809, -1.703115836376113634 ) ) ;
#169312=CARTESIAN_POINT ( 'NONE',  ( 4.881388680972560401, 1.702354803207173584, -0.6601141376258444771 ) ) ;
#169316=CARTESIAN_POINT ( 'NONE',  ( 1.282125424323858898, -1.693001012030776353, 0.3732380902255887367 ) ) ;
#169317=CARTESIAN_POINT ( 'NONE',  ( 0.6908507670086707630, -0.6304954947415147837, 1.622297741125192427 ) ) ;
#169318=CARTESIAN_POINT ( 'NONE',  ( 5.039818274408326637, -1.629004898613298558, -1.634814698366208185 ) ) ;
#169321=CARTESIAN_POINT ( 'NONE',  ( 1.054063116485728813, 2.058546115662110765, -0.09824037785954514712 ) ) ;
#169324=CARTESIAN_POINT ( 'NONE',  ( 0.2630457479233569984, -2.015603748724136945, -0.05229424383911692592 ) ) ;
#169327=CARTESIAN_POINT ( 'NONE',  ( 6.631728656526095556, -1.223761959379562114, -1.414937998750566361 ) ) ;
#169329=CARTESIAN_POINT ( 'NONE',  ( 3.586107075002854305, 1.066394011600999780, 1.587261316105821551 ) ) ;
#169331=CARTESIAN_POINT ( 'NONE',  ( 4.617920694193921705, -2.164688156338661962, 0.4286357439418769788 ) ) ;
#169336=CARTESIAN_POINT ( 'NONE',  ( 5.936213163351176547, -1.177816969253571155, -1.763093882214488817 ) ) ;
#169337=CARTESIAN_POINT ( 'NONE',  ( 3.698509654486553000, -2.304784958540738060, -0.1161927354758583580 ) ) ;
#169338=CARTESIAN_POINT ( 'NONE',  ( 3.543363863352413823, 1.774678991803163575, -0.8365776047038612218 ) ) ;
#169340=CARTESIAN_POINT ( 'NONE',  ( 0.5495624486224826022, 1.449728300881658383, 1.321815246172884040 ) ) ;
#169344=CARTESIAN_POINT ( 'NONE',  ( 6.157435431667657610, 1.928259211291092123, -0.5899821858514133766 ) ) ;
#169347=CARTESIAN_POINT ( 'NONE',  ( 2.922911270491454161, -1.500192211782652718, 1.569583652781519012 ) ) ;
#169349=CARTESIAN_POINT ( 'NONE',  ( 1.248456593208754795, 1.040400552670465162, -1.847740296886036582 ) ) ;
#169354=CARTESIAN_POINT ( 'NONE',  ( 0.7903930413690943846, -2.044920356511644499, -0.2547782948326294816 ) ) ;
#169360=CARTESIAN_POINT ( 'NONE',  ( 4.055252259792781366, -1.662250449027093735, 0.9452659147194606426 ) ) ;
#169364=CARTESIAN_POINT ( 'NONE',  ( -0.07045567476893913050, -1.776642250867260575, 0.3530574836328649324 ) ) ;
#169366=CARTESIAN_POINT ( 'NONE',  ( 0.9541331885446997507, -1.212804274533643145, 1.482964625430952976 ) ) ;
#169367=CARTESIAN_POINT ( 'NONE',  ( 1.627480586986803868, 0.1543294891723171747, -2.064685722993148342 ) ) ;
#169370=CARTESIAN_POINT ( 'NONE',  ( 0.2156151883831447236, -1.933912933822299784, 0.3821239771369787097 ) ) ;
#169371=CARTESIAN_POINT ( 'NONE',  ( 3.123480263227970344, -1.759325740769552393, 0.4874977319994436287 ) ) ;
#169372=CARTESIAN_POINT ( 'NONE',  ( 6.445939570963194143, 0.8488519614954292969, -2.037301952897092594 ) ) ;
#169375=CARTESIAN_POINT ( 'NONE',  ( 4.316881300680885047, -1.530586319191833633, 1.382930202259499364 ) ) ;
#169380=CARTESIAN_POINT ( 'NONE',  ( 4.858481695672255185, 0.8034365979220282616, 1.946882858121199211 ) ) ;
#169382=CARTESIAN_POINT ( 'NONE',  ( 6.795378861676105053, -1.851214886592133846, 0.9271815693319698237 ) ) ;
#169384=CARTESIAN_POINT ( 'NONE',  ( 3.268983376858981327, -1.995845357749256976, -0.8305886511386084692 ) ) ;
#169385=CARTESIAN_POINT ( 'NONE',  ( 4.125652552961744490, -0.3430436748357457710, 1.990152796604119034 ) ) ;
#169392=CARTESIAN_POINT ( 'NONE',  ( 2.800017839408690090, -0.9981255096969069429, -1.752139039461996006 ) ) ;
#169397=CARTESIAN_POINT ( 'NONE',  ( 6.720655732516654268, 4.688933928088002467, 2.736284108207136079 ) ) ;
#169399=CARTESIAN_POINT ( 'NONE',  ( 4.306267660493944049, 1.238306454277863677, -1.591331080693689781 ) ) ;
#169402=CARTESIAN_POINT ( 'NONE',  ( 6.405283072077849305, 1.437190941405818156, 0.9532465752533066938 ) ) ;
#169408=CARTESIAN_POINT ( 'NONE',  ( 5.659403934932580427, 0.3656299861228041181, -1.834283699791404043 ) ) ;
#169410=CARTESIAN_POINT ( 'NONE',  ( 6.381113974719265336, -1.842344568942927419, -0.8120077521172417434 ) ) ;
#169415=CARTESIAN_POINT ( 'NONE',  ( 1.089470510105726708, -0.4871801946146369633, 1.956568126268923846 ) ) ;
#169416=CARTESIAN_POINT ( 'NONE',  ( 0.9315677820061087910, -1.767094751418090803, 0.3981412331970111684 ) ) ;
#169423=CARTESIAN_POINT ( 'NONE',  ( 5.853135685669797361, 0.1356727809044282473, -1.910850313501164743 ) ) ;
#169429=CARTESIAN_POINT ( 'NONE',  ( 4.399409362686744096, 1.734418756986338295, 1.290045131933370781 ) ) ;
#169432=CARTESIAN_POINT ( 'NONE',  ( 0.2465380642357860586, 1.084720387836759947, -1.822023332652397354 ) ) ;
#169433=CARTESIAN_POINT ( 'NONE',  ( 6.053692819838605743, 0.5272490726609193601, -1.747765065496959869 ) ) ;
#169435=CARTESIAN_POINT ( 'NONE',  ( 2.231653169902757750, -1.284661796483690832, -1.495404430405805174 ) ) ;
#169436=CARTESIAN_POINT ( 'NONE',  ( 4.711142613322857109, 1.586760866459841379, -1.067142987418716604 ) ) ;
#169439=CARTESIAN_POINT ( 'NONE',  ( 5.670349227943210835, -0.8838483254627060859, -1.760150121488897490 ) ) ;
#169440=CARTESIAN_POINT ( 'NONE',  ( 0.1814471035007196309, -0.9164790359779145801, 1.712077929913154328 ) ) ;
#169446=CARTESIAN_POINT ( 'NONE',  ( 4.512308969215598431, -1.911949174345693336, -0.04343532550177275214 ) ) ;
#169448=CARTESIAN_POINT ( 'NONE',  ( 0.3763673390903346516, 1.272619870141003418, 1.802674353332263335 ) ) ;
#169450=CARTESIAN_POINT ( 'NONE',  ( 5.901044691261273734, -0.2977458250903759485, -1.990848032377992016 ) ) ;
#169451=CARTESIAN_POINT ( 'NONE',  ( 0.07680821025391955381, 7.629137130509078268, -2.410791881123967251 ) ) ;
#169454=CARTESIAN_POINT ( 'NONE',  ( 2.857943571468853250, -0.6518772230660694333, 1.965110387975615991 ) ) ;
#169458=CARTESIAN_POINT ( 'NONE',  ( 0.9717996764858798375, 2.083101276202529384, -0.5774176476955604764 ) ) ;
#169466=CARTESIAN_POINT ( 'NONE',  ( 2.606657977298726614, 1.900416011228076130, 0.6748465934659984011 ) ) ;
#169467=CARTESIAN_POINT ( 'NONE',  ( 5.396976841598324803, -0.7867719702298915374, -1.545497150229415251 ) ) ;
#169469=CARTESIAN_POINT ( 'NONE',  ( 3.116144222688784549, 2.060704436481402890, -0.1983081510379124945 ) ) ;
#169470=CARTESIAN_POINT ( 'NONE',  ( 5.079753589751704546, -0.7609352437839884686, 1.975942822842210234 ) ) ;
#169473=CARTESIAN_POINT ( 'NONE',  ( 3.028127619189690201, 1.049479266250245901, 1.666313143567710542 ) ) ;
#169474=CARTESIAN_POINT ( 'NONE',  ( 0.7559434568639655794, 0.7726834774516875282, -1.749509110286852742 ) ) ;
#169475=CARTESIAN_POINT ( 'NONE',  ( 4.488395308864603805, -0.4996631572763092222, -2.236994043316854697 ) ) ;
#169476=CARTESIAN_POINT ( 'NONE',  ( 2.754317325142870754, 0.6151756178996542479, 1.719052816137212503 ) ) ;
#169481=CARTESIAN_POINT ( 'NONE',  ( 4.025643311844375738, -0.3400233446379635760, 1.984125136466656558 ) ) ;
#169482=CARTESIAN_POINT ( 'NONE',  ( 2.711707638535421960, 0.5279276851305572116, -1.889291386287835550 ) ) ;
#169487=CARTESIAN_POINT ( 'NONE',  ( 6.316366637557600860, 1.950215401406007354, 0.7537550503652605816 ) ) ;
#169488=CARTESIAN_POINT ( 'NONE',  ( 4.153014383403249354, -1.471681513620528348, -0.9827620175600642050 ) ) ;
#169490=CARTESIAN_POINT ( 'NONE',  ( 0.3577192552456122665, 2.167005522336755696, -0.3256184645209562190 ) ) ;
#169491=CARTESIAN_POINT ( 'NONE',  ( 6.615217694991038400, -1.686041314625020160, 0.4309386324203681728 ) ) ;
#169494=CARTESIAN_POINT ( 'NONE',  ( 0.5448069426677571991, 2.143542105210020754, -0.8297726512136813781 ) ) ;
#169495=CARTESIAN_POINT ( 'NONE',  ( 0.09952931447375359952, -0.5783855404800625211, 2.113812074898171023 ) ) ;
#169496=CARTESIAN_POINT ( 'NONE',  ( 6.679014442879065427, -0.8212242018711314318, -1.526972759001248514 ) ) ;
#169497=CARTESIAN_POINT ( 'NONE',  ( 3.158999515626020216, -1.670948785577108797, 1.441709373268922123 ) ) ;
#169498=CARTESIAN_POINT ( 'NONE',  ( 6.426262541905297887, 1.110578645885337501, 1.865513821534901417 ) ) ;
#169500=CARTESIAN_POINT ( 'NONE',  ( 1.429080218188124585, -1.785550482114751203, 1.137718905448012352 ) ) ;
#169501=CARTESIAN_POINT ( 'NONE',  ( 3.250000000000002665, 1.855058607017213327E-13, 2.052068128417948056 ) ) ;
#169502=CARTESIAN_POINT ( 'NONE',  ( 6.727182134110196721, 7.629137130509074716, 2.889055895399252005 ) ) ;
#169503=CARTESIAN_POINT ( 'NONE',  ( 5.280268953417031952, -1.070192140894361099, 1.601580209743416860 ) ) ;
#169505=CARTESIAN_POINT ( 'NONE',  ( 1.031297522511119613, -2.069548003639944511, 0.9861895074133855132 ) ) ;
#169509=CARTESIAN_POINT ( 'NONE',  ( 3.774281487401151214, 2.204430612424528757, -0.2728622730414613784 ) ) ;
#169517=CARTESIAN_POINT ( 'NONE',  ( 1.951796282902381163, -1.844710420878793444, -0.8146254186931353169 ) ) ;
#169519=CARTESIAN_POINT ( 'NONE',  ( 6.443808500197930833, 1.419581301535753015, 1.496705048937081006 ) ) ;
#169522=CARTESIAN_POINT ( 'NONE',  ( -0.05938221139379848412, -1.422385081007140117, -1.168950373246782526 ) ) ;
#169525=CARTESIAN_POINT ( 'NONE',  ( 2.864225066854100277, -1.223476834174407779, 1.278924851658661099 ) ) ;
#169526=CARTESIAN_POINT ( 'NONE',  ( 1.565077508395201988, -1.076315722900993643, 1.704939445326451475 ) ) ;
#169527=CARTESIAN_POINT ( 'NONE',  ( 0.4855842612344652975, -1.827229208960782447, -0.2260576252584786672 ) ) ;
#169528=CARTESIAN_POINT ( 'NONE',  ( 5.302359097629713247, 1.737542498810572322, -1.495360377712177113 ) ) ;
#169529=CARTESIAN_POINT ( 'NONE',  ( 3.661895226921571656, -1.235415792305821325, 1.365283978338522441 ) ) ;
#169531=CARTESIAN_POINT ( 'NONE',  ( 3.592628304870106870, -0.3553021837224104584, -1.790491875447843384 ) ) ;
#169532=CARTESIAN_POINT ( 'NONE',  ( 5.045546153961558922, -1.458558117013383892, 1.392544180963309230 ) ) ;
#169534=CARTESIAN_POINT ( 'NONE',  ( 2.975713975707586556, 2.148818855599075928, -0.7084362298409478953 ) ) ;
#169536=CARTESIAN_POINT ( 'NONE',  ( 6.809622064836790223, -0.4623527835773094119, 2.061910140347056331 ) ) ;
#169538=CARTESIAN_POINT ( 'NONE',  ( 3.490741092712910998, 2.019281663078629219, 0.4563312328872348722 ) ) ;
#169541=CARTESIAN_POINT ( 'NONE',  ( 5.971359625099014856, -1.818578809777360972, -1.090262957368436147 ) ) ;
#169543=MANIFOLD_SOLID_BREP ( 'Sweep1[11]', #153736 ) ;
#169545=CARTESIAN_POINT ( 'NONE',  ( 2.174328269389655066, -1.185172859381509625, 1.518732482018339436 ) ) ;
#169547=CARTESIAN_POINT ( 'NONE',  ( 0.2913706227113096459, -1.802261421121041707, 0.7947621968238273160 ) ) ;
#169552=CARTESIAN_POINT ( 'NONE',  ( 0.6158632564332514603, 1.820540700843051418, 1.272696253368794439 ) ) ;
#169553=CARTESIAN_POINT ( 'NONE',  ( 3.241344266390119078, -1.858123463236575290, 0.9911517508872002002 ) ) ;
#169556=CARTESIAN_POINT ( 'NONE',  ( 1.064655064206044166, 1.412561167129450457, -1.211817338188374782 ) ) ;
#169561=CARTESIAN_POINT ( 'NONE',  ( 0.8266187642571948269, -0.9586779626098644869, -1.891633453305548773 ) ) ;
#169564=CARTESIAN_POINT ( 'NONE',  ( 4.193769882565239193, -1.351282707657221582, -1.422545440481419510 ) ) ;
#169565=CARTESIAN_POINT ( 'NONE',  ( 2.131903390035182255, -1.411712784473453830, -1.637176306262012826 ) ) ;
#169566=CARTESIAN_POINT ( 'NONE',  ( 1.962219809069129184, -1.683971100191889336, -0.7449956418128443891 ) ) ;
#169569=CARTESIAN_POINT ( 'NONE',  ( 3.521201755802486844, -1.038059167858174092, -1.396672450663126508 ) ) ;
#169573=CARTESIAN_POINT ( 'NONE',  ( 0.3566080023540801336, 0.8287714912002723811, 1.996717379258300840 ) ) ;
#169574=CARTESIAN_POINT ( 'NONE',  ( 3.356795910091507906, -0.8196482158769199389, 1.842165019812888271 ) ) ;
#169576=CARTESIAN_POINT ( 'NONE',  ( 0.5499753625364013354, 0.6768306982547143136, -2.053065283773393368 ) ) ;
#169577=CARTESIAN_POINT ( 'NONE',  ( 3.239098446765543482, -1.739280071990648935, 0.9281937050133574063 ) ) ;
#169578=CARTESIAN_POINT ( 'NONE',  ( 6.509000000000011887, 3.696273625755361447, 2.514342382328867753 ) ) ;
#169579=CARTESIAN_POINT ( 'NONE',  ( 2.331498104393217474, 0.9136196428927362279, -1.713718834741830177 ) ) ;
#169580=CARTESIAN_POINT ( 'NONE',  ( 6.433860211133586304, -1.853236450885078712, 0.4715264990977630077 ) ) ;
#169584=CARTESIAN_POINT ( 'NONE',  ( -0.1110810684432960160, 0.2482034880273851774, -1.831546034005934853 ) ) ;
#169590=CARTESIAN_POINT ( 'NONE',  ( 0.1830476545506658226, -2.141193618969746471, -0.5335393285625378290 ) ) ;
#169592=CARTESIAN_POINT ( 'NONE',  ( 3.994932754639446859, 0.2835094185691371393, 1.941019531709553103 ) ) ;
#169595=CARTESIAN_POINT ( 'NONE',  ( 2.057267738415057057, -1.238319999287675666, 1.591319116112683396 ) ) ;
#169597=CARTESIAN_POINT ( 'NONE',  ( 2.800141503465008341, -1.047918259751862147, -1.839804015593812458 ) ) ;
#169600=CARTESIAN_POINT ( 'NONE',  ( 3.433393508698717511, 0.8267853122289525736, -1.645126075773599039 ) ) ;
#169605=CARTESIAN_POINT ( 'NONE',  ( 3.920270587443940080, -2.114697630030224929, 0.1593259359235904837 ) ) ;
#169608=CARTESIAN_POINT ( 'NONE',  ( 5.747358702077526971, -1.621750911093680081, -1.271367298817957181 ) ) ;
#169610=CARTESIAN_POINT ( 'NONE',  ( 2.032514702046281485, -1.644074058028240692, 0.8291662819630771786 ) ) ;
#169615=CARTESIAN_POINT ( 'NONE',  ( 2.543839704335303153, -1.636039663378138886, -1.481301067789652537 ) ) ;
#169616=CARTESIAN_POINT ( 'NONE',  ( 3.550319795034285519, 2.262578822424826441, 0.004170446471787879993 ) ) ;
#169618=CARTESIAN_POINT ( 'NONE',  ( 3.093827002871222920, 1.152939038403834493, 1.397299590375496336 ) ) ;
#169619=CARTESIAN_POINT ( 'NONE',  ( 4.083139574666094340, 1.542046283821847830, 1.136513224425585555 ) ) ;
#169621=ADVANCED_FACE ( 'NONE', ( #197896 ), #161156, .T. ) ;
#169622=CARTESIAN_POINT ( 'NONE',  ( 4.012542200100970291, 1.395003824703803685, -1.393317042198267020 ) ) ;
#169623=CARTESIAN_POINT ( 'NONE',  ( 1.166875649673270399, -1.740261045891202230, -0.8264182621567657261 ) ) ;
#169624=CARTESIAN_POINT ( 'NONE',  ( 5.348468966913380029, 0.5439794105128460400, 1.789823788735760646 ) ) ;
#169625=CARTESIAN_POINT ( 'NONE',  ( 3.211855371912860413, -0.4501829054360923510, 2.263203710529379187 ) ) ;
#169626=CARTESIAN_POINT ( 'NONE',  ( 4.439814405351947713, 1.214877501302736862, 1.409928613244580742 ) ) ;
#169630=CARTESIAN_POINT ( 'NONE',  ( 1.576933964714849701, -2.000244969732989819, -0.6594162861879059312 ) ) ;
#169634=CARTESIAN_POINT ( 'NONE',  ( 2.935903058640790597, -2.042584291827519660, 0.5695675404085094318 ) ) ;
#169636=CARTESIAN_POINT ( 'NONE',  ( 0.6330766797960291070, 1.867852534778514428, 0.7690482435470397116 ) ) ;
#169641=CARTESIAN_POINT ( 'NONE',  ( 2.161604200734370096, 0.3718190433680613749, -2.129227089361292791 ) ) ;
#169646=CARTESIAN_POINT ( 'NONE',  ( 6.385953923436008317, -2.015982004707029596, 0.05432014494890363698 ) ) ;
#169648=CARTESIAN_POINT ( 'NONE',  ( -0.07626876867936756288, -1.353788312843669406, -1.724171373301164767 ) ) ;
#169650=CARTESIAN_POINT ( 'NONE',  ( 0.2513181340676704512, -1.814898432050582766, 1.350810986113021750 ) ) ;
#169657=CARTESIAN_POINT ( 'NONE',  ( 3.914446297384760243, 1.218041307117226690, -1.221573883832317575 ) ) ;
#169659=CARTESIAN_POINT ( 'NONE',  ( 1.967667936517076166, 0.9046490693802499150, 1.520878277628298303 ) ) ;
#169660=CARTESIAN_POINT ( 'NONE',  ( 2.596342214666306880, -1.033070880159161264, 1.727660946855133606 ) ) ;
#169662=CARTESIAN_POINT ( 'NONE',  ( 5.385833121705805304, 1.478444731487274399, 1.638484004604986000 ) ) ;
#169665=CARTESIAN_POINT ( 'NONE',  ( 4.301511568767760529, 1.893648340000140040, -0.9544086401246790752 ) ) ;
#169666=CARTESIAN_POINT ( 'NONE',  ( 3.550407796516129366, -1.352142120786763213, 1.496064415113136592 ) ) ;
#169670=CARTESIAN_POINT ( 'NONE',  ( 1.569004590881703853, 0.1408476687595125731, -1.865417194689425795 ) ) ;
#169672=CARTESIAN_POINT ( 'NONE',  ( 5.725234622465176670, 1.600757532941178063, 0.8479277756611166561 ) ) ;
#169679=CARTESIAN_POINT ( 'NONE',  ( 1.838261372102001800, -1.052240823716396267, 1.655630454418555830 ) ) ;
#169682=CARTESIAN_POINT ( 'NONE',  ( 4.693665235656380830, 1.977662049654808740, -0.7657889336421249693 ) ) ;
#169685=CARTESIAN_POINT ( 'NONE',  ( 5.659438124648599633, 0.3871718161991606344, -1.932801920045317257 ) ) ;
#169687=CARTESIAN_POINT ( 'NONE',  ( 1.336190909427417139, -1.121870850062630653, -1.671457199112064806 ) ) ;
#169689=CARTESIAN_POINT ( 'NONE',  ( 1.581820014152079956, -0.7095999980938502150, 1.994918640774499430 ) ) ;
#169691=CARTESIAN_POINT ( 'NONE',  ( 2.260293373024503616, -2.069953001785612479, 0.04851313490940312168 ) ) ;
#169696=CARTESIAN_POINT ( 'NONE',  ( 4.365234240191905535, 2.027873629061471838, -0.5078740465511691893 ) ) ;
#169698=CARTESIAN_POINT ( 'NONE',  ( 3.100428009929767637, -0.5284298666012043899, -1.747434388548900541 ) ) ;
#169699=CARTESIAN_POINT ( 'NONE',  ( 1.629273880293732768, -0.2214294203813528539, 1.797790724094426418 ) ) ;
#169701=CARTESIAN_POINT ( 'NONE',  ( 6.235036409211808461, 0.2120174297785166195, 2.196685143856290878 ) ) ;
#169702=CARTESIAN_POINT ( 'NONE',  ( 4.524592175135637717, 1.360519573838222085, -1.737388959189073878 ) ) ;
#169706=CARTESIAN_POINT ( 'NONE',  ( 4.002528454542265024, -1.891902218777557598, -0.2775262981309714605 ) ) ;
#169709=CARTESIAN_POINT ( 'NONE',  ( 6.092251258522619395, 1.023830597077223903, -1.799436568697235783 ) ) ;
#169711=CARTESIAN_POINT ( 'NONE',  ( 6.233935805145816467, 2.167428969419796125, 0.3234103439683775894 ) ) ;
#169717=CARTESIAN_POINT ( 'NONE',  ( 3.163207368312019430, 0.2779861718534247794, -1.849665920529340646 ) ) ;
#169722=CARTESIAN_POINT ( 'NONE',  ( 0.6902129346560643697, 1.017158767820530940, -1.686321398027894825 ) ) ;
#169724=CARTESIAN_POINT ( 'NONE',  ( 0.9488424731869498086, -1.824129051820524205, -0.8596123018156722750 ) ) ;
#169728=CARTESIAN_POINT ( 'NONE',  ( 1.886939110189549185, 1.905679594745551819, -1.081921739459410059 ) ) ;
#169729=CARTESIAN_POINT ( 'NONE',  ( 5.795480788678070816, 1.385457615097264394, 1.189071861804301466 ) ) ;
#169736=CARTESIAN_POINT ( 'NONE',  ( 4.106863108761789505, -0.3106082297497716471, 1.814695527881895476 ) ) ;
#169737=CARTESIAN_POINT ( 'NONE',  ( 0.4342398884448725460, -1.078799894535716231, -1.699460183843485073 ) ) ;
#169738=CARTESIAN_POINT ( 'NONE',  ( 2.003655084434956102, 2.273349380270474729, 0.3377564834418695927 ) ) ;
#169740=CARTESIAN_POINT ( 'NONE',  ( 0.2505320230819003680, -0.3960800208489853036, -1.824604621477694311 ) ) ;
#169744=CARTESIAN_POINT ( 'NONE',  ( 4.429883728109570207, -1.874397765517330061, 0.3784635845696313061 ) ) ;
#169749=CARTESIAN_POINT ( 'NONE',  ( 3.052369502041663019, -1.581437162565798804, 1.367655637459828544 ) ) ;
#169750=CARTESIAN_POINT ( 'NONE',  ( 0.9009904985227291663, 1.526999960511504772, 1.080287613699250304 ) ) ;
#169753=CARTESIAN_POINT ( 'NONE',  ( 3.368457041919175055, 0.03905506635776007096, -1.740168019110074793 ) ) ;
#169757=CARTESIAN_POINT ( 'NONE',  ( 4.230855031843249847, 0.08773280417345018234, 1.722775095924995004 ) ) ;
#169758=CARTESIAN_POINT ( 'NONE',  ( 3.755584314896889264, 2.174856280799509545, -0.2696606696684644700 ) ) ;
#169759=CARTESIAN_POINT ( 'NONE',  ( 5.883472226557855400, 2.040502603023553796, -0.8411249186189362348 ) ) ;
#169761=CARTESIAN_POINT ( 'NONE',  ( 3.292005203939939229, -1.454527599200394539, -1.611992012647659900 ) ) ;
#169762=CARTESIAN_POINT ( 'NONE',  ( 1.664397423953474009, -1.292156093668932693, 1.290017532847971271 ) ) ;
#169763=CARTESIAN_POINT ( 'NONE',  ( 0.4265131056294459433, -1.285834093136655643, 1.481649512794058321 ) ) ;
#169764=CARTESIAN_POINT ( 'NONE',  ( 4.118443911689470660, 2.077242944681048975, 0.4093182092978660536 ) ) ;
#169766=CARTESIAN_POINT ( 'NONE',  ( 4.898102649693969468, -0.7706710736265044437, -2.159050251936722731 ) ) ;
#169768=CARTESIAN_POINT ( 'NONE',  ( 6.620655732516643965, 2.083750514537034970, 2.135603474206409835 ) ) ;
#169770=CARTESIAN_POINT ( 'NONE',  ( 0.8562900302464396818, 0.8558255631127342777, -1.940287777186230578 ) ) ;
#169778=CARTESIAN_POINT ( 'NONE',  ( 4.992814645674492624, -2.006446365708704160, 0.2004330516618065550 ) ) ;
#169780=CARTESIAN_POINT ( 'NONE',  ( 4.768458259026512103, -0.8772815012083650110, -1.866809563962401164 ) ) ;
#169782=CARTESIAN_POINT ( 'NONE',  ( 6.883263157960393563, 4.695771316066229772, 2.508818740863460572 ) ) ;
#169786=CARTESIAN_POINT ( 'NONE',  ( 0.6211766780156646739, -1.984520161701831986, 0.6578015034230285663 ) ) ;
#169787=CARTESIAN_POINT ( 'NONE',  ( 4.940077362011475515, -1.704937458037486531, -1.076318853994034930 ) ) ;
#169788=CARTESIAN_POINT ( 'NONE',  ( 2.858754248528099229, 0.2676582106064147593, -1.821554178878769470 ) ) ;
#169791=CARTESIAN_POINT ( 'NONE',  ( 0.3051044079889728144, -0.4676614632079054701, 1.660094367756638434 ) ) ;
#169793=CARTESIAN_POINT ( 'NONE',  ( 0.6164066528375180543, 0.1772060041554945342, 2.291936309153388862 ) ) ;
#169795=CARTESIAN_POINT ( 'NONE',  ( 0.5974158272751062260, 1.880195615759198136, -1.258034406164424635 ) ) ;
#169796=CARTESIAN_POINT ( 'NONE',  ( 2.666745002694201450, -1.451881433263510601, 1.525875076051644408 ) ) ;
#169800=CARTESIAN_POINT ( 'NONE',  ( 5.656250000000004441, -1.895863743163955339, 0.7852924748302813063 ) ) ;
#169805=CARTESIAN_POINT ( 'NONE',  ( 3.498459270752065198, -1.092227124545399164, 1.934249878339290740 ) ) ;
#169806=CARTESIAN_POINT ( 'NONE',  ( 1.816621679704206516, 2.045545470589833492, 0.7867152234099920038 ) ) ;
#169809=CARTESIAN_POINT ( 'NONE',  ( 5.705508943770692731, -1.545575431542939970, -1.208212526538715137 ) ) ;
#169816=CARTESIAN_POINT ( 'NONE',  ( 4.570628194609677841, 0.8141925398062774821, 1.958264201954627026 ) ) ;
#169820=CARTESIAN_POINT ( 'NONE',  ( 6.069229152942410721, 0.1638285306290178100, -2.155560115052157055 ) ) ;
#169822=CARTESIAN_POINT ( 'NONE',  ( 5.354971380013192395, 0.3533838956982695567, -1.806849549699687696 ) ) ;
#169826=CARTESIAN_POINT ( 'NONE',  ( 6.474529609311859168, -0.09325562727019585940, -1.737965710822095389 ) ) ;
#169830=CARTESIAN_POINT ( 'NONE',  ( 4.768538688506021472, -1.414568798902924307, 1.634688457493836289 ) ) ;
#169833=CARTESIAN_POINT ( 'NONE',  ( 4.803692121107413726, -0.5798474923815257753, 2.082409481564663434 ) ) ;
#169834=CARTESIAN_POINT ( 'NONE',  ( 5.114510421747438862, 1.361449769532377729, -1.425934698893965402 ) ) ;
#169835=CARTESIAN_POINT ( 'NONE',  ( 3.883936887208380373, -0.1284340723075507729, 1.729154583330833272 ) ) ;
#169836=CARTESIAN_POINT ( 'NONE',  ( 0.9256184737543894370, -1.394389637717853514, -1.690728713229103342 ) ) ;
#169837=CARTESIAN_POINT ( 'NONE',  ( 2.749405113950495583, -1.918974089273906003, 1.281321877411125909 ) ) ;
#169838=CARTESIAN_POINT ( 'NONE',  ( 3.673166697908346379, 0.05419028943656278852, -2.060251915681856616 ) ) ;
#169839=CARTESIAN_POINT ( 'NONE',  ( 5.583525073002030048, -0.8696438758921558598, 1.736526053206193243 ) ) ;
#169845=CARTESIAN_POINT ( 'NONE',  ( 2.854729849855553780, 0.7423848465729752100, 2.078289375090878632 ) ) ;
#169848=CARTESIAN_POINT ( 'NONE',  ( 1.147037741594110427, 1.644639672688326559, -0.8707446802224245719 ) ) ;
#169849=CARTESIAN_POINT ( 'NONE',  ( -0.1288028175206725467, 0.2223783146117243037, -2.307352578052775272 ) ) ;
#169852=CARTESIAN_POINT ( 'NONE',  ( 6.825078400183572036, 7.051914997414900022, 2.742498282622223726 ) ) ;
#169855=CARTESIAN_POINT ( 'NONE',  ( 3.819256682291353400, -0.1532216265913727837, 2.055260608361098473 ) ) ;
#169860=CARTESIAN_POINT ( 'NONE',  ( 2.360294219997323140, 0.8799647281299802781, 1.863710983410723943 ) ) ;
#169864=CARTESIAN_POINT ( 'NONE',  ( 5.690102719724574598, -0.9953569382129350274, 1.969734210959340093 ) ) ;
#169865=CARTESIAN_POINT ( 'NONE',  ( 6.643838010208884981, 0.8751278368869718216, -2.086507859592637626 ) ) ;
#169867=CARTESIAN_POINT ( 'NONE',  ( 1.253139057289072822, 0.1435168058863903473, -2.011451928166609893 ) ) ;
#169869=CARTESIAN_POINT ( 'NONE',  ( 6.217437059193512638, 1.592560689453832001, 1.058264445519964125 ) ) ;
#169872=CARTESIAN_POINT ( 'NONE',  ( 2.008475284031425723, 1.387998011844304491, -1.254312187223500796 ) ) ;
#169873=CARTESIAN_POINT ( 'NONE',  ( 3.344935638061694139, -1.780668040901035143, -0.9463001528628791625 ) ) ;
#169875=CARTESIAN_POINT ( 'NONE',  ( 6.639320575229257670, 0.5729255850590134758, 2.155858052613166986 ) ) ;
#169877=CARTESIAN_POINT ( 'NONE',  ( 4.986996339425863844, -0.2567466434181593371, -2.090293495131962942 ) ) ;
#169882=CARTESIAN_POINT ( 'NONE',  ( 3.955335691828856692, -1.755346444749112722, 0.9990557238469994772 ) ) ;
#169885=CARTESIAN_POINT ( 'NONE',  ( 0.2509072133702301421, -0.4515964501156078392, -2.020277220192217449 ) ) ;
#169887=CARTESIAN_POINT ( 'NONE',  ( 5.782550318682353918, -2.107506929020441788, -0.4798289361013233223 ) ) ;
#169893=CARTESIAN_POINT ( 'NONE',  ( 3.631445352573436480, 0.05657863903951602241, -2.170607583040237820 ) ) ;
#169896=CARTESIAN_POINT ( 'NONE',  ( 1.997363575765517485, -1.840834563946552649, 0.04656924640939614363 ) ) ;
#169898=CARTESIAN_POINT ( 'NONE',  ( 2.823975127348025804, 1.215230906543849354, -1.823574674616668556 ) ) ;
#169899=CARTESIAN_POINT ( 'NONE',  ( 6.983263157960387879, 4.689051080487334211, 2.716346346018564617 ) ) ;
#169900=CARTESIAN_POINT ( 'NONE',  ( 4.610415411315283762, -0.9635332438130711497, -2.047219928730920291 ) ) ;
#169905=COLOUR_RGB ( '', 0.72549020, 0.75294118, 0.79215686) ;
#169909=CARTESIAN_POINT ( 'NONE',  ( 5.870295291196549137, -1.121585077578592049, 1.368893044642209178 ) ) ;
#169911=CARTESIAN_POINT ( 'NONE',  ( 1.923017885777689839, 1.964713842245609410, 0.7587240108328905386 ) ) ;
#169915=CARTESIAN_POINT ( 'NONE',  ( 1.926157630473192217, 1.009716079121532495, 1.690873403599216562 ) ) ;
#169917=CARTESIAN_POINT ( 'NONE',  ( 0.3089402658475807195, -1.578002999302514642, 1.165503548361209063 ) ) ;
#169918=CARTESIAN_POINT ( 'NONE',  ( 5.818593503215891971, -0.6604613111419742610, -1.687090931240011527 ) ) ;
#169923=CARTESIAN_POINT ( 'NONE',  ( 4.785944050937030347, -0.8815013282119156246, 1.649949660215948688 ) ) ;
#169924=CARTESIAN_POINT ( 'NONE',  ( 6.016483110937820733, 0.8336820848486149460, 1.895147399281302603 ) ) ;
#169934=CARTESIAN_POINT ( 'NONE',  ( 4.879329150013382410, -0.09822140645733207220, 1.959542894978071992 ) ) ;
#169936=CARTESIAN_POINT ( 'NONE',  ( 2.952499795743710020, 1.423742661936340470, 1.427719607385954381 ) ) ;
#169937=CARTESIAN_POINT ( 'NONE',  ( 2.378032431427847371, -1.910899176573145342, -0.1362895805000780836 ) ) ;
#169939=CARTESIAN_POINT ( 'NONE',  ( 0.8553300576445364012, 0.4222666777726029608, -2.150330908352434012 ) ) ;
#169941=CARTESIAN_POINT ( 'NONE',  ( 2.600682448077856090, 1.504852936121018558, -1.110837741034584436 ) ) ;
#169943=CARTESIAN_POINT ( 'NONE',  ( 4.078389064453043389, 0.9529185939490876223, 1.773430079992607045 ) ) ;
#169946=CARTESIAN_POINT ( 'NONE',  ( 4.622735098982394319, 0.3634473554468270473, 2.085661844363582595 ) ) ;
#169947=CARTESIAN_POINT ( 'NONE',  ( 5.934052368846653991, 1.230181698326970885, 1.665117723180092213 ) ) ;
#169948=CARTESIAN_POINT ( 'NONE',  ( 1.646151360528936625, 0.6591259108063004524, 1.984184313626126350 ) ) ;
#169949=CARTESIAN_POINT ( 'NONE',  ( 6.720655732516647163, 2.019696082639847567, 2.477441386028636394 ) ) ;
#169950=CARTESIAN_POINT ( 'NONE',  ( 5.965807262869926575, 1.798080572464531679, -0.3147057940002598864 ) ) ;
#169958=CARTESIAN_POINT ( 'NONE',  ( 0.1525891599635448848, 0.3075033511844190159, 1.785008687375288172 ) ) ;
#169967=CARTESIAN_POINT ( 'NONE',  ( 5.730092268227672037, 2.014234620932173758, 0.09611943034040781875 ) ) ;
#169968=CARTESIAN_POINT ( 'NONE',  ( 0.4344390223590781641, -1.137927343861804053, -1.789123301873453364 ) ) ;
#169974=CARTESIAN_POINT ( 'NONE',  ( 3.678522182247864869, 1.252989934047860965, -1.519404455180313640 ) ) ;
#169975=CARTESIAN_POINT ( 'NONE',  ( 4.569935513796226978, -0.9480243344661150040, 1.779636403143824985 ) ) ;
#169978=CARTESIAN_POINT ( 'NONE',  ( 4.541096662771787251, -1.693051203114638525, -1.391418086139440957 ) ) ;
#169980=CARTESIAN_POINT ( 'NONE',  ( 2.766527970621732724, -1.329674337952547303, 1.394112488825666851 ) ) ;
#169982=CARTESIAN_POINT ( 'NONE',  ( -0.02948999725182251466, 1.364966664109868555, -2.179895196203474050 ) ) ;
#169983=CARTESIAN_POINT ( 'NONE',  ( 0.1331565106231363538, 7.629137130509071163, -2.545925718843544239 ) ) ;
#169988=CARTESIAN_POINT ( 'NONE',  ( 5.295741323871941297, -1.389945570378407380, -1.395530913269894091 ) ) ;
#169989=CARTESIAN_POINT ( 'NONE',  ( 0.08144728253534591622, -0.9147537949990096617, 1.713110483266879980 ) ) ;
#169990=CARTESIAN_POINT ( 'NONE',  ( 3.738934858379244552, 1.912307379442554689, 0.6292302551485791096 ) ) ;
#169991=CARTESIAN_POINT ( 'NONE',  ( 5.835437120055854798, -1.464435618476932488, 1.771446943145409847 ) ) ;
#169992=CARTESIAN_POINT ( 'NONE',  ( 4.030005733973434978, 1.030655172484344684, 1.549249419044882226 ) ) ;
#169998=CARTESIAN_POINT ( 'NONE',  ( 0.2049558871960316941, 1.909868400323280424, 1.074723926240577221 ) ) ;
#170003=CARTESIAN_POINT ( 'NONE',  ( 0.01192831195480706721, -0.7772932952810689411, -1.650495136788888040 ) ) ;
#170005=CARTESIAN_POINT ( 'NONE',  ( 2.689770611714628945, 1.466270380367465043, 0.9255270069659697896 ) ) ;
#170007=CARTESIAN_POINT ( 'NONE',  ( 6.508999999999981689, 4.698440520552249922, 2.462686878797680556 ) ) ;
#170010=CARTESIAN_POINT ( 'NONE',  ( 0.5673436759025469733, 1.799520464221905369, 1.023488823764052480 ) ) ;
#170011=CARTESIAN_POINT ( 'NONE',  ( 5.443921307256319508, 0.7362202147598860824, -1.670853202368662860 ) ) ;
#170012=CARTESIAN_POINT ( 'NONE',  ( 3.362109073961421224, -1.959717995770013932, 0.09162775335717905645 ) ) ;
#170016=CARTESIAN_POINT ( 'NONE',  ( 3.317144061745095129, 1.670432841370917298, -1.306055464808851818 ) ) ;
#170017=CARTESIAN_POINT ( 'NONE',  ( 6.827182134110192813, 7.051736335826703339, 2.787205296604370108 ) ) ;
#170020=CARTESIAN_POINT ( 'NONE',  ( 1.340777958403309267, -2.018934908790828597, -0.4573474576154838989 ) ) ;
#170023=CARTESIAN_POINT ( 'NONE',  ( 5.039773670486915158, -2.109617592216144644, 0.6956167390435584741 ) ) ;
#170025=CARTESIAN_POINT ( 'NONE',  ( 2.110373620506571957, 0.004507209458638748376, 2.298851035670963050 ) ) ;
#170033=CARTESIAN_POINT ( 'NONE',  ( 2.672007700615218528, 1.902801012812182169, -0.1915479950082218386 ) ) ;
#170035=CARTESIAN_POINT ( 'NONE',  ( 4.629763539376270387, -1.062658783613348534, -1.358442396976522248 ) ) ;
#170036=CARTESIAN_POINT ( 'NONE',  ( 2.641814858895009444, 2.006371511526034546, -0.2024640970367599380 ) ) ;
#170037=CARTESIAN_POINT ( 'NONE',  ( 4.131641605347593504, 0.6128431504758731219, 2.215418681923121191 ) ) ;
#170038=CARTESIAN_POINT ( 'NONE',  ( 3.497619258099498030, 1.781045823846095111, 1.394991416339389501 ) ) ;
#170039=CARTESIAN_POINT ( 'NONE',  ( 6.147117739887063337, -1.780134362386740721, 1.125150951816885403 ) ) ;
#170041=CARTESIAN_POINT ( 'NONE',  ( 4.710057611840397840, -0.7560107150014344635, -1.600242281814190148 ) ) ;
#170043=CARTESIAN_POINT ( 'NONE',  ( 0.2699993869635419208, 1.325028633338236839, 1.870336120953507875 ) ) ;
#170044=CARTESIAN_POINT ( 'NONE',  ( 5.085823778388903982, -1.827637283562512538, -0.2220107604927607503 ) ) ;
#170047=CARTESIAN_POINT ( 'NONE',  ( 5.894512528888635750, 1.793468170635740710, -1.259063434910556500 ) ) ;
#170051=CARTESIAN_POINT ( 'NONE',  ( 5.635237798060349412, -0.04710594754482424346, -2.069988403558701062 ) ) ;
#170052=CARTESIAN_POINT ( 'NONE',  ( 0.9718890779336667451, -0.9023411006064323558, 1.803417998987096427 ) ) ;
#170055=CARTESIAN_POINT ( 'NONE',  ( 4.793539397740587127, 1.428753304119126266, 1.292492988728560999 ) ) ;
#170057=CARTESIAN_POINT ( 'NONE',  ( 1.670502159040608170, 2.215024970770036017, -0.1695594764349258321 ) ) ;
#170065=CARTESIAN_POINT ( 'NONE',  ( 4.335344899790516848, 0.7389749068974335033, -1.575905762629246309 ) ) ;
#170067=CARTESIAN_POINT ( 'NONE',  ( 2.435929278166943490, 1.204617592564939166, 1.548422000036096202 ) ) ;
#170073=CARTESIAN_POINT ( 'NONE',  ( 0.1392228125525768467, -0.1412503886474673342, -2.030206775815279308 ) ) ;
#170076=CARTESIAN_POINT ( 'NONE',  ( 1.569569324160888124, 0.1651462269399027738, -2.256556122256009100 ) ) ;
#170080=CARTESIAN_POINT ( 'NONE',  ( 1.598681293450100904, 1.532267803987485077, -1.072633048482305229 ) ) ;
#170081=CARTESIAN_POINT ( 'NONE',  ( 0.4747597223977735315, -1.720734514737034093, -0.2143409017008046646 ) ) ;
#170083=CARTESIAN_POINT ( 'NONE',  ( 3.966501855323391723, -2.045284974426237579, -0.7877190255709336508 ) ) ;
#170084=CARTESIAN_POINT ( 'NONE',  ( 5.930798096255836427, 2.221851032742766741, 0.6229754028606748761 ) ) ;
#170085=CARTESIAN_POINT ( 'NONE',  ( 0.3739917644934092067, 1.186169308094830344, 1.685110605438163045 ) ) ;
#170086=CARTESIAN_POINT ( 'NONE',  ( 3.960829289611409898, 0.2367351755836170912, -1.927401316828970979 ) ) ;
#170091=CARTESIAN_POINT ( 'NONE',  ( 3.076796235938107138, -0.8146265060355701859, 1.844709937164576097 ) ) ;
#170095=CARTESIAN_POINT ( 'NONE',  ( 0.7854531640391904102, 1.224056292049885419, 1.354719642434290439 ) ) ;
#170101=CARTESIAN_POINT ( 'NONE',  ( 0.4444780689869810564, 2.156031605563761833, 0.1575401717312311101 ) ) ;
#170105=CARTESIAN_POINT ( 'NONE',  ( 6.199869188016119637, 1.394352454258035001, 1.461346697781773507 ) ) ;
#170106=CARTESIAN_POINT ( 'NONE',  ( 6.006509256357773552, -2.210310773855695743, -0.2204792344780072411 ) ) ;
#170110=CARTESIAN_POINT ( 'NONE',  ( 5.577047029790810129, -0.04816181868504652158, -2.060495320025256483 ) ) ;
#170111=CARTESIAN_POINT ( 'NONE',  ( 3.797500137148449362, 1.423962148579031917, -1.427936706820939872 ) ) ;
#170115=CIRCLE ( 'NONE', #97627, 0.04999999999999934358 ) ;
#170119=CARTESIAN_POINT ( 'NONE',  ( 4.200545946899570282, -1.388273439763810790, -1.462221600879671790 ) ) ;
#170120=CARTESIAN_POINT ( 'NONE',  ( 3.240019139272034110, 0.4481936114588759845, 1.785621944311803100 ) ) ;
#170123=CARTESIAN_POINT ( 'NONE',  ( 2.491230068042503465, -0.3961224009183231809, -2.273300736686647117 ) ) ;
#170126=CARTESIAN_POINT ( 'NONE',  ( 4.745497693432328745, -1.667575968047749546, -1.375352955852253922 ) ) ;
#170128=CARTESIAN_POINT ( 'NONE',  ( 6.550350952284553330, -1.418464805562440922, 1.173678288350611609 ) ) ;
#170129=CARTESIAN_POINT ( 'NONE',  ( 2.800017839408690090, -0.9981255096969069429, -1.752139039461996006 ) ) ;
#170131=CARTESIAN_POINT ( 'NONE',  ( 4.077728334586081083, 1.628699396557086398, -1.621930329367648138 ) ) ;
#170134=CARTESIAN_POINT ( 'NONE',  ( 2.764352523130030548, -1.291370965961564421, 1.353630663414123969 ) ) ;
#170135=CARTESIAN_POINT ( 'NONE',  ( 0.6320224300673723539, 1.017306711037075262, -1.688479424803266404 ) ) ;
#170138=CARTESIAN_POINT ( 'NONE',  ( 1.735297346119796691, 0.2185962045802778420, 2.196029071591873993 ) ) ;
#170144=CARTESIAN_POINT ( 'NONE',  ( 6.561403051094389483, 0.3373947195176879021, -1.942235834477159084 ) ) ;
#170145=CARTESIAN_POINT ( 'NONE',  ( 6.217413992247779575, -0.2892589651934658890, 2.289433544902704565 ) ) ;
#170146=CARTESIAN_POINT ( 'NONE',  ( 0.2562055958934654210, -1.961350414083770977, -0.05204156388862594962 ) ) ;
#170148=CARTESIAN_POINT ( 'NONE',  ( 3.678632908625163012, 1.312080992568062321, -1.591389186695492342 ) ) ;
#170155=CARTESIAN_POINT ( 'NONE',  ( 6.549308719555964053, 1.892307808498715049, -1.064380946037797093 ) ) ;
#170156=CARTESIAN_POINT ( 'NONE',  ( 5.231922985772964552, 1.814955821992572993, 0.3091130605668013231 ) ) ;
#170158=CARTESIAN_POINT ( 'NONE',  ( 6.058177568126345669, -1.550975213528119623, 1.548612826651605712 ) ) ;
#170159=CARTESIAN_POINT ( 'NONE',  ( 0.2275331484566482099, -1.145445245298154946, -1.479381579510357758 ) ) ;
#170165=CARTESIAN_POINT ( 'NONE',  ( 2.289615904538056412, -0.7594197407109636311, 1.598781567136787318 ) ) ;
#170166=CARTESIAN_POINT ( 'NONE',  ( 6.569000952640477564, -1.554625895936670554, 1.278542242695315689 ) ) ;
#170168=CARTESIAN_POINT ( 'NONE',  ( 4.165583994951371771, 1.254247372560507223, 1.447964403467276506 ) ) ;
#170170=CARTESIAN_POINT ( 'NONE',  ( 5.652785005015395825, -0.4769087673412530370, -1.910818445241519559 ) ) ;
#170171=CARTESIAN_POINT ( 'NONE',  ( 0.2816890862925770511, 0.2015970107726860194, -2.110973810222869229 ) ) ;
#170173=CARTESIAN_POINT ( 'NONE',  ( 2.430351462470367707, 1.813921419787648315, 0.4566771774890953095 ) ) ;
#170174=CARTESIAN_POINT ( 'NONE',  ( 6.182236774357948050, -0.9162642880373177423, 1.461205601097197659 ) ) ;
#170176=CARTESIAN_POINT ( 'NONE',  ( 3.246891520140795517, 0.5363302883765566076, 2.140594385818309409 ) ) ;
#170179=CARTESIAN_POINT ( 'NONE',  ( 0.3970293196923400658, 0.3510089794473401081, 2.032437512258952417 ) ) ;
#170187=CARTESIAN_POINT ( 'NONE',  ( 2.664580169416390643, -0.7900844611210651180, -1.913877855911281234 ) ) ;
#170191=CARTESIAN_POINT ( 'NONE',  ( 0.6100282365348074221, -0.7248652973187595938, 1.885305865817282323 ) ) ;
#170197=CARTESIAN_POINT ( 'NONE',  ( 0.07479286986305369589, 1.387406912293275729, -2.112587013352088317 ) ) ;
#170199=CARTESIAN_POINT ( 'NONE',  ( 6.362657644764970755, -0.6818896071447738683, 1.897407954007489073 ) ) ;
#170200=CARTESIAN_POINT ( 'NONE',  ( 6.069544675611900253, 1.326465198304109583, 1.382431045765440514 ) ) ;
#170201=CARTESIAN_POINT ( 'NONE',  ( 6.639320575229286092, 2.965970653406803770, 2.456291990408800086 ) ) ;
#170202=CARTESIAN_POINT ( 'NONE',  ( 4.142245973918059043, 0.5854081421233224836, 2.111838497463234710 ) ) ;
#170204=CARTESIAN_POINT ( 'NONE',  ( 2.091926199050548441, 1.179367891222588005, 1.505316542580182437 ) ) ;
#170208=CARTESIAN_POINT ( 'NONE',  ( 1.036732716359071604, -1.587823911754655315, 1.242746109592095527 ) ) ;
#170210=CARTESIAN_POINT ( 'NONE',  ( 6.532779862045914321, -1.958661757936002612, 0.9833580883553474372 ) ) ;
#170212=CARTESIAN_POINT ( 'NONE',  ( 2.555303990735880770, 0.4627875540959677236, -1.661435987504814360 ) ) ;
#170219=CARTESIAN_POINT ( 'NONE',  ( 1.662477996687723669, -0.7030478115006146833, -1.831755296705489977 ) ) ;
#170227=CARTESIAN_POINT ( 'NONE',  ( 4.494648839764849413, -1.758179434694202570, -0.4356380854809716041 ) ) ;
#170231=CARTESIAN_POINT ( 'NONE',  ( 5.057183878474817540, -1.550805960166462105, 0.9359391756664036111 ) ) ;
#170235=CARTESIAN_POINT ( 'NONE',  ( 5.459367789976862895, 1.521435002614815790, 1.071484558867175529 ) ) ;
#170237=CARTESIAN_POINT ( 'NONE',  ( 2.319824818950954270, 0.9007672528749611773, -1.690582045118453225 ) ) ;
#170244=CARTESIAN_POINT ( 'NONE',  ( 1.095779546523030668, -2.090823718873015657, 0.001679924440483454573 ) ) ;
#170246=CARTESIAN_POINT ( 'NONE',  ( 6.581085459773934332, -0.09550846514571986745, -1.924131155975503216 ) ) ;
#170248=CARTESIAN_POINT ( 'NONE',  ( 2.256629077056008015, -1.412982602626071449, 1.155960151518524937 ) ) ;
#170251=CARTESIAN_POINT ( 'NONE',  ( 1.890998328602263800, 0.1897877418215961898, 1.960365536012158127 ) ) ;
#170252=CARTESIAN_POINT ( 'NONE',  ( 3.280740747204694774, 1.754465757641409995, -0.8330476171748876224 ) ) ;
#170257=CARTESIAN_POINT ( 'NONE',  ( 3.762070191281779774, 0.7111978290502696254, -1.997938288694045550 ) ) ;
#170265=CARTESIAN_POINT ( 'NONE',  ( 3.738726038629454074, 0.2694068579384528150, 1.805578518607708016 ) ) ;
#170270=CARTESIAN_POINT ( 'NONE',  ( 6.925078400183550364, 4.698656493127392864, 2.418320467900983761 ) ) ;
#170271=CARTESIAN_POINT ( 'NONE',  ( 4.240975883383619305, -1.627667033997456381, 0.9218181776217827528 ) ) ;
#170273=CARTESIAN_POINT ( 'NONE',  ( 1.717283182695702015, -0.2364092415704423800, 1.911874917900743931 ) ) ;
#170274=CARTESIAN_POINT ( 'NONE',  ( 6.977413161700751765, -0.1449424838519241254, 1.929857014940839832 ) ) ;
#170279=CARTESIAN_POINT ( 'NONE',  ( 1.757563674541680721, 2.025006261547353414, -0.6180173261674735130 ) ) ;
#170282=CARTESIAN_POINT ( 'NONE',  ( 5.383670357325340383, -1.967593191946028996, 0.6441560278484458335 ) ) ;
#170283=CARTESIAN_POINT ( 'NONE',  ( 0.9250624443557056154, -1.167992581197497604, -1.423340509374780405 ) ) ;
#170285=CARTESIAN_POINT ( 'NONE',  ( 4.905072937705025282, -1.228516145343660826, -1.942733121961652376 ) ) ;
#170289=CARTESIAN_POINT ( 'NONE',  ( 1.412523707164672127, 1.536465969362065476, -1.701261851757162269 ) ) ;
#170292=CARTESIAN_POINT ( 'NONE',  ( 6.035097030359367842, -1.408219244926838476, -1.337428300092268652 ) ) ;
#170296=CARTESIAN_POINT ( 'NONE',  ( 5.976807594091997800, -1.347613670528555740, 1.357171208065083512 ) ) ;
#170297=CARTESIAN_POINT ( 'NONE',  ( 6.122279814772175754, 1.995267444086584518, 0.2910868170948808786 ) ) ;
#170301=CARTESIAN_POINT ( 'NONE',  ( 2.589882131170073709, -2.085102945988726031, -0.1528390284690275547 ) ) ;
#170302=CARTESIAN_POINT ( 'NONE',  ( 0.9535335928906017999, 1.768114364327963539, -0.08115213312524624523 ) ) ;
#170304=CARTESIAN_POINT ( 'NONE',  ( 3.732637569912560682, 0.3354268113090127512, 2.267480163388153169 ) ) ;
#170305=CARTESIAN_POINT ( 'NONE',  ( 3.661793474361102252, -1.167423004587186952, 1.290856655984705670 ) ) ;
#170309=CARTESIAN_POINT ( 'NONE',  ( 2.108352191060134828, 0.6683163022180199642, -1.600079515618204606 ) ) ;
#170310=CARTESIAN_POINT ( 'NONE',  ( 3.983024850003999973, 2.060528110339276520, 0.6844299113566986170 ) ) ;
#170312=CARTESIAN_POINT ( 'NONE',  ( 4.083220446344194343, 1.622485107653489633, 1.197306254465977826 ) ) ;
#170313=CARTESIAN_POINT ( 'NONE',  ( 2.812500000000002665, 1.451031289061236684, 1.451031289061000873 ) ) ;
#170315=CARTESIAN_POINT ( 'NONE',  ( 0.8328817383555222609, 0.1387611642639074438, 1.921445197033289976 ) ) ;
#170317=CARTESIAN_POINT ( 'NONE',  ( 4.781579470667713494, 0.2167243770262658464, -2.210780252931910717 ) ) ;
#170319=CARTESIAN_POINT ( 'NONE',  ( -0.2108831679770926115, 5.723481173670196043, -2.491210874135452613 ) ) ;
#170325=CARTESIAN_POINT ( 'NONE',  ( 0.5049021242206577220, -2.205252279087748235, -0.2660074523756980058 ) ) ;
#170326=CARTESIAN_POINT ( 'NONE',  ( 5.969191311310417802, 1.729517061547349632, 0.9261464158661563140 ) ) ;
#170330=CARTESIAN_POINT ( 'NONE',  ( 6.591137597455673180, 1.973280021476801149, -1.106527213950120547 ) ) ;
#170334=CARTESIAN_POINT ( 'NONE',  ( 3.561030563730323006, 1.627881067681248073, -1.266672197246907494 ) ) ;
#170338=CARTESIAN_POINT ( 'NONE',  ( 5.237510374101456812, -1.321932271818569093, -1.323673891312632245 ) ) ;
#170339=CARTESIAN_POINT ( 'NONE',  ( 3.445721922217106936, -1.531427584095602867, -0.8135701209448819027 ) ) ;
#170340=CARTESIAN_POINT ( 'NONE',  ( 2.981702274927648944, -1.715113757222336721, -0.2947475401101228853 ) ) ;
#170341=CARTESIAN_POINT ( 'NONE',  ( 1.154322298621703435, 0.9348496236407450866, 2.093279060508267175 ) ) ;
#170343=CARTESIAN_POINT ( 'NONE',  ( 4.880461040030859010, -0.2572269614671355842, -2.074807210009928848 ) ) ;
#170344=CARTESIAN_POINT ( 'NONE',  ( 0.1285073612291263989, -1.684675954457705682, 0.7431698939026829542 ) ) ;
#170347=CARTESIAN_POINT ( 'NONE',  ( 0.8795299900376440938, -0.4926441280813895762, -1.955172062459666904 ) ) ;
#170348=CARTESIAN_POINT ( 'NONE',  ( 0.9496594531581278309, -1.914679731917130479, 0.9119059213342151082 ) ) ;
#170353=CARTESIAN_POINT ( 'NONE',  ( 2.385534290476189145, 0.1013982516714604792, -2.118174289320504666 ) ) ;
#170355=CARTESIAN_POINT ( 'NONE',  ( 4.635264976507449397, -1.668059998867366778, 0.7425182445051290436 ) ) ;
#170361=CARTESIAN_POINT ( 'NONE',  ( 2.443623115440888061, -1.883043647339300186, 0.7309814453849405869 ) ) ;
#170362=CARTESIAN_POINT ( 'NONE',  ( 5.596761079150560647, -0.5311557606857522096, -2.141783596114990917 ) ) ;
#170366=CARTESIAN_POINT ( 'NONE',  ( 3.977287768980780402, -0.1405865315737795385, 1.855722876009910038 ) ) ;
#170371=CARTESIAN_POINT ( 'NONE',  ( 4.705575438601840688, -0.4840451379145363497, 1.760283039881085809 ) ) ;
#170375=CARTESIAN_POINT ( 'NONE',  ( 0.5965333524920403141, 0.8982759108043871787, -1.482850294500896560 ) ) ;
#170376=CARTESIAN_POINT ( 'NONE',  ( 6.714805130922314014, -0.1276373473727103192, 1.811824464382847832 ) ) ;
#170377=CARTESIAN_POINT ( 'NONE',  ( 5.742881039954627731, 0.4445991233769739925, 2.264314392639497520 ) ) ;
#170379=CARTESIAN_POINT ( 'NONE',  ( 1.317730169365991522, -2.011166735366700209, 0.4487503453191737934 ) ) ;
#170380=CARTESIAN_POINT ( 'NONE',  ( 6.468148293998644327, 1.905381763673856810, 1.285138856061205148 ) ) ;
#170383=CARTESIAN_POINT ( 'NONE',  ( 5.366025703835962446, 0.9229158262306772498, 1.627043297953718382 ) ) ;
#170384=CARTESIAN_POINT ( 'NONE',  ( 3.445477555875466891, -1.765175379189663607, 0.7362804355328657069 ) ) ;
#170386=CARTESIAN_POINT ( 'NONE',  ( 4.987059637548557411, -0.2676712469649074055, -2.190530366034774801 ) ) ;
#170391=CARTESIAN_POINT ( 'NONE',  ( 5.742871283745087041, 2.043606947765171267, 0.5656136300068030920 ) ) ;
#170393=CARTESIAN_POINT ( 'NONE',  ( 3.188805362043587888, -2.273175341261697291, -0.3962186847288259317 ) ) ;
#170394=CARTESIAN_POINT ( 'NONE',  ( 4.176187491914356897, -1.006606191838583131, -1.683785057063936552 ) ) ;
#170397=CARTESIAN_POINT ( 'NONE',  ( 0.9538670997781794059, -0.7113550649951918547, 1.828410001767373450 ) ) ;
#170401=CARTESIAN_POINT ( 'NONE',  ( 6.333220217719927270, -1.622483202430196725, -1.197309987464048486 ) ) ;
#170404=CARTESIAN_POINT ( 'NONE',  ( 3.010768451359053355, 0.7272417100659108735, 2.045797318486474836 ) ) ;
#170406=CARTESIAN_POINT ( 'NONE',  ( 0.8090202166558431163, -0.5209130535433897924, -2.055487714681260236 ) ) ;
#170411=CARTESIAN_POINT ( 'NONE',  ( 0.4564140224992017658, 0.7863226074062683590, 1.905069713448727775 ) ) ;
#170418=CARTESIAN_POINT ( 'NONE',  ( 3.229067839489424330, 1.729836904712976686, 0.8154208365811002057 ) ) ;
#170420=CARTESIAN_POINT ( 'NONE',  ( 5.823074959372767090, -0.03971387110058427483, 1.769581062106811986 ) ) ;
#170424=CARTESIAN_POINT ( 'NONE',  ( 0.7030050633033817498, 1.597335618216610964, -0.8546489784103310505 ) ) ;
#170426=CARTESIAN_POINT ( 'NONE',  ( 1.077184250232362306, 1.452872634298128629, 1.248800971253192005 ) ) ;
#170427=CARTESIAN_POINT ( 'NONE',  ( 2.189971326302230903, -1.350648006375281929, -1.569233719104834890 ) ) ;
#170429=CARTESIAN_POINT ( 'NONE',  ( 6.596569749568344854, -0.5012203084251048990, -1.802199723311518786 ) ) ;
#170430=CARTESIAN_POINT ( 'NONE',  ( 2.402731849113007190, 1.466575434288765800, -1.087121784572639527 ) ) ;
#170431=CARTESIAN_POINT ( 'NONE',  ( 0.2765547061623524483, 1.334074794448695034, 1.882843260577294009 ) ) ;
#170434=CARTESIAN_POINT ( 'NONE',  ( 4.439923992641017669, 1.344862922493793578, 1.564070066283109295 ) ) ;
#170440=CARTESIAN_POINT ( 'NONE',  ( 6.689897370947560873, -1.349224794794257720, -1.570457413003906177 ) ) ;
#170442=CARTESIAN_POINT ( 'NONE',  ( 3.392016793147753617, -0.8794390384766533897, 1.974801309016629869 ) ) ;
#170443=CARTESIAN_POINT ( 'NONE',  ( 4.248697963213067474, 1.981114831247460017, 0.3918398546494082368 ) ) ;
#170446=CARTESIAN_POINT ( 'NONE',  ( 6.720655732516641834, 2.402268298795938950, 2.653651172607660591 ) ) ;
#170452=CARTESIAN_POINT ( 'NONE',  ( 2.975796278104340331, -0.8128168404246680634, 1.845627246706407210 ) ) ;
#170457=CARTESIAN_POINT ( 'NONE',  ( 6.293217207623316156, -0.1008467329366956045, -1.909883259500498198 ) ) ;
#170458=CARTESIAN_POINT ( 'NONE',  ( 6.720655732516667591, 2.416141799769660370, 2.554522868665403568 ) ) ;
#170460=CARTESIAN_POINT ( 'NONE',  ( 4.025017672583341977, -1.753021876717888006, 0.9963191169995513352 ) ) ;
#170463=CARTESIAN_POINT ( 'NONE',  ( 6.299779570463345912, -0.5759050694413189175, 1.625906498142214884 ) ) ;
#170467=CARTESIAN_POINT ( 'NONE',  ( 5.167206475355686557, 0.1846639555213614448, -1.861428779493356167 ) ) ;
#170468=CARTESIAN_POINT ( 'NONE',  ( 6.082294971626270197, 1.038730605371197324, 1.724430661308763213 ) ) ;
#170470=CARTESIAN_POINT ( 'NONE',  ( 2.448173108494243078, -0.8891298726186761536, 1.869765896676472083 ) ) ;
#170473=CARTESIAN_POINT ( 'NONE',  ( 1.177361486786612899, 1.528755565978222819, 1.314981834344926437 ) ) ;
#170474=CARTESIAN_POINT ( 'NONE',  ( 1.406221933027915982, -1.803026290124358555, -0.1754379831288860880 ) ) ;
#170481=CARTESIAN_POINT ( 'NONE',  ( 6.468375100207775397, -1.879703733780390795, -0.3681822884963186215 ) ) ;
#170490=CARTESIAN_POINT ( 'NONE',  ( 3.292016909520224743, -0.8776455207864016783, 1.975710135277891633 ) ) ;
#170493=CARTESIAN_POINT ( 'NONE',  ( 1.055114822555893950, 0.4192091730233596381, 2.078585086915801128 ) ) ;
#170494=CARTESIAN_POINT ( 'NONE',  ( 5.825187583072056974, -0.04236064406601056098, 1.825263316621673848 ) ) ;
#170496=CARTESIAN_POINT ( 'NONE',  ( 1.757037784194936725, -1.688679813833958709, -1.016973138862599102 ) ) ;
#170497=CARTESIAN_POINT ( 'NONE',  ( 4.482611839828003930, -1.244964735940889522, 1.451779576051547282 ) ) ;
#170500=CARTESIAN_POINT ( 'NONE',  ( 4.562928411757408043, 1.523777916087779571, -1.247912438812292413 ) ) ;
#170501=CARTESIAN_POINT ( 'NONE',  ( 6.620655732516682157, 0.004685112605702904456, 1.926407831898164114 ) ) ;
#170508=CARTESIAN_POINT ( 'NONE',  ( 5.320932177894995618, 1.445329238430465013, -1.252218921613167169 ) ) ;
#170511=CARTESIAN_POINT ( 'NONE',  ( 0.4642757356001780966, 2.182421439735841684, -0.3260586787675948117 ) ) ;
#170513=CARTESIAN_POINT ( 'NONE',  ( 5.865890606937535168, 0.5820329372835297832, -1.927131433562751406 ) ) ;
#170514=CARTESIAN_POINT ( 'NONE',  ( -0.02338929933909470252, 2.896474228846234844, -2.200133910884606081 ) ) ;
#170517=CARTESIAN_POINT ( 'NONE',  ( 3.051297593704501043, 1.777051743073382761, -1.062048545217339601 ) ) ;
#170521=CARTESIAN_POINT ( 'NONE',  ( 0.6202742476981680797, -1.157488721396517040, -1.825510493854154426 ) ) ;
#170526=CARTESIAN_POINT ( 'NONE',  ( 6.925078400183550364, 2.460400685555228950, 2.239421262742965268 ) ) ;
#170528=CARTESIAN_POINT ( 'NONE',  ( 4.447759528527571504, -1.551977624003277212, -0.7738437340010505539 ) ) ;
#170530=CARTESIAN_POINT ( 'NONE',  ( 3.485274717979901293, 0.04603381543630095940, 2.069897711131869933 ) ) ;
#170531=CARTESIAN_POINT ( 'NONE',  ( 4.974263482967073990, -2.101360013415910721, -0.2580830166784564006 ) ) ;
#170534=CARTESIAN_POINT ( 'NONE',  ( 1.955843269872016066, -0.6684750375501640196, 1.852638994923772930 ) ) ;
#170535=CARTESIAN_POINT ( 'NONE',  ( 1.283307755816986528, 0.1377011610334301639, -1.907463248872851569 ) ) ;
#170536=CARTESIAN_POINT ( 'NONE',  ( 5.332074485713341971, 2.257618135992002895, 0.3962004586785839444 ) ) ;
#170537=CARTESIAN_POINT ( 'NONE',  ( 1.892912435568369744, 1.589020553905008626, -0.8988452475950716725 ) ) ;
#170542=CARTESIAN_POINT ( 'NONE',  ( 3.322524176979495980, -0.8198387518110359373, -1.838900561053190774 ) ) ;
#170543=CARTESIAN_POINT ( 'NONE',  ( 3.748837004188230182, -0.3782986639458625899, -1.924763881548184230 ) ) ;
#170546=CARTESIAN_POINT ( 'NONE',  ( 0.1753634416057497647, 0.0001173177735149660568, -2.144164757042036573 ) ) ;
#170547=CARTESIAN_POINT ( 'NONE',  ( 5.824191892830967276, 2.014527380540787505, 0.5587128073646082660 ) ) ;
#170548=CARTESIAN_POINT ( 'NONE',  ( 4.416719503454580753, 1.618597840523916753, 0.7163212975811702465 ) ) ;
#170550=CARTESIAN_POINT ( 'NONE',  ( 0.4104466507391414387, 1.508250410577081979, -1.590083307377434974 ) ) ;
#170551=CARTESIAN_POINT ( 'NONE',  ( 6.714805129994689814, -0.1247508129638870145, 1.711716247594262441 ) ) ;
#170554=CARTESIAN_POINT ( 'NONE',  ( 0.1331715793776600265, 2.877549198462618474, -2.442236402435117526 ) ) ;
#170555=CARTESIAN_POINT ( 'NONE',  ( 6.609999999999973674, -0.005249217919313375023, 2.280159464062641916 ) ) ;
#170557=CARTESIAN_POINT ( 'NONE',  ( 1.981372325807278623, -0.1102420082176903682, -2.204251428397439483 ) ) ;
#170559=CARTESIAN_POINT ( 'NONE',  ( 6.777770921962916972, -2.107754466287181661, 0.5206637005944132479 ) ) ;
#170561=CARTESIAN_POINT ( 'NONE',  ( 1.552129107922173068, 1.093532845977844170, 1.812997832068358850 ) ) ;
#170562=CARTESIAN_POINT ( 'NONE',  ( 2.781250000000002665, 0.7852924748301273183, 1.895863743164028170 ) ) ;
#170564=CARTESIAN_POINT ( 'NONE',  ( 6.727182134110194056, 3.682851444631680682, 2.702965647100654234 ) ) ;
#170565=CARTESIAN_POINT ( 'NONE',  ( 4.893539313097565291, 1.427316681580325763, 1.293898783310668987 ) ) ;
#170567=CARTESIAN_POINT ( 'NONE',  ( 1.804612524702827514, 1.695363242818634930, -1.543121881923440020 ) ) ;
#170572=CARTESIAN_POINT ( 'NONE',  ( 3.932468528151237042, -1.142516171320803853, -1.904832733444387971 ) ) ;
#170578=CARTESIAN_POINT ( 'NONE',  ( 1.899064777474347654, -0.9530127170578571727, -1.777010740487514173 ) ) ;
#170580=CARTESIAN_POINT ( 'NONE',  ( 6.426245203579573406, 1.057156898221789598, 1.771034054399809987 ) ) ;
#170583=CARTESIAN_POINT ( 'NONE',  ( 6.480030497237043718, -1.708793550445006248, -0.3294957622956768972 ) ) ;
#170585=CARTESIAN_POINT ( 'NONE',  ( 1.422737370818322633, -0.05026339470881428795, 1.769212045163440106 ) ) ;
#170586=CARTESIAN_POINT ( 'NONE',  ( -0.1399997263889594112, -0.002789056014654289761, -2.000146600338557956 ) ) ;
#170587=CARTESIAN_POINT ( 'NONE',  ( 6.356985390939413172, 0.2876776518413763917, -1.716344579348449084 ) ) ;
#170588=CARTESIAN_POINT ( 'NONE',  ( 3.808379203468327034, 1.620604861375672945, -1.621544036339316985 ) ) ;
#170589=CARTESIAN_POINT ( 'NONE',  ( 3.784953330938052751, 1.334695924059103644, 1.268461399425282687 ) ) ;
#170592=CARTESIAN_POINT ( 'NONE',  ( 4.559475717982610199, 0.3993622990657343941, -1.781190812766835441 ) ) ;
#170593=CARTESIAN_POINT ( 'NONE',  ( 4.535779832184696936, -1.617819081767550182, 1.203352566194588746 ) ) ;
#170595=CARTESIAN_POINT ( 'NONE',  ( 3.907294183660753539, 1.938944517003845736, 1.165763813888931688 ) ) ;
#170597=CARTESIAN_POINT ( 'NONE',  ( 0.01252217983070766719, -0.9030397145437498718, -1.901010321977952389 ) ) ;
#170599=CARTESIAN_POINT ( 'NONE',  ( 4.123533666479628046, 0.2564666318346648377, -2.054367117340555549 ) ) ;
#170602=CARTESIAN_POINT ( 'NONE',  ( 5.461630201184114242, -1.671734486004393450, -1.304435072541964447 ) ) ;
#170605=CARTESIAN_POINT ( 'NONE',  ( 2.596214140771450296, -1.921342217666447860, -0.1417109463846803752 ) ) ;
#170608=CARTESIAN_POINT ( 'NONE',  ( 0.1390025477998011738, -0.1451226239368992033, -1.937570863154890688 ) ) ;
#170613=CARTESIAN_POINT ( 'NONE',  ( 0.05339833992625257070, 0.3882609103176749010, 2.187096328411592516 ) ) ;
#170614=CARTESIAN_POINT ( 'NONE',  ( 2.889785439676189505, 1.488280975668257344, 1.490260817651526182 ) ) ;
#170617=CARTESIAN_POINT ( 'NONE',  ( 0.5196754285911856508, 1.841638447829671899, -0.2671899778997516850 ) ) ;
#170623=CARTESIAN_POINT ( 'NONE',  ( 0.8969213510382867405, -2.070190491330957006, -0.4589741369691033857 ) ) ;
#170626=CARTESIAN_POINT ( 'NONE',  ( 2.945700582358207864, 1.385421296276163838, 1.389331660621349274 ) ) ;
#170627=CARTESIAN_POINT ( 'NONE',  ( 2.377987466095924152, 1.329388817951412394, 1.704534938537699995 ) ) ;
#170628=CARTESIAN_POINT ( 'NONE',  ( 2.120424178990498731, 0.001545453418709194504, 1.841430844159386293 ) ) ;
#170631=CARTESIAN_POINT ( 'NONE',  ( 3.890341755399207013, 1.468866505370895137, -0.9330376088199500151 ) ) ;
#170634=CARTESIAN_POINT ( 'NONE',  ( 1.182749364907993206, -2.109161078630458430, -0.4729781282231394490 ) ) ;
#170636=CARTESIAN_POINT ( 'NONE',  ( 3.321638586175166719, -1.528507173905558014, 1.314795459203411676 ) ) ;
#170638=CARTESIAN_POINT ( 'NONE',  ( 0.4269344243218140544, 2.069031678568326704, 0.6260965431626740463 ) ) ;
#170640=CARTESIAN_POINT ( 'NONE',  ( 1.903138372489954655, 1.638015138609005383, 1.096796735940619660 ) ) ;
#170641=CARTESIAN_POINT ( 'NONE',  ( 6.609000000000047947, 0.5928748489389294996, 1.953858053793898542 ) ) ;
#170642=CARTESIAN_POINT ( 'NONE',  ( 2.296341162515431744, 1.558512652156778699, -1.158513924970270059 ) ) ;
#170647=CARTESIAN_POINT ( 'NONE',  ( -0.2108831679771168421, 7.629137130509075604, -2.497154329497493386 ) ) ;
#170652=CARTESIAN_POINT ( 'NONE',  ( 0.1654306582001447423, -1.972458130798220077, -0.9897840116655574061 ) ) ;
#170655=CARTESIAN_POINT ( 'NONE',  ( 3.959774770350584561, -0.5736532364168048792, 1.875976257969473648 ) ) ;
#170657=CARTESIAN_POINT ( 'NONE',  ( 2.039685609654022347, -1.556907966322677472, 1.281362143053674130 ) ) ;
#170659=CARTESIAN_POINT ( 'NONE',  ( 2.764987222883477980, -0.1607348756041589999, -2.111328481229361564 ) ) ;
#170663=CARTESIAN_POINT ( 'NONE',  ( 2.853255899669316697, 1.832232481769331844, -0.1808706098178694266 ) ) ;
#170667=CARTESIAN_POINT ( 'NONE',  ( 4.588201236890728119, 1.223260742344203900, 1.732012071221388450 ) ) ;
#170668=CARTESIAN_POINT ( 'NONE',  ( 0.1812672858593766811, -0.8707521589867758260, 1.622202602641155345 ) ) ;
#170671=CARTESIAN_POINT ( 'NONE',  ( 4.305972304023081954, -2.055534471369814487, 0.1475827967423407050 ) ) ;
#170673=CARTESIAN_POINT ( 'NONE',  ( 1.241482983173985533, 1.839155304979672501, 0.08999620058360720265 ) ) ;
#170678=CARTESIAN_POINT ( 'NONE',  ( 0.9442952520863318044, 0.8911936224933308948, -2.019119535841918278 ) ) ;
#170679=CARTESIAN_POINT ( 'NONE',  ( 3.585499571845919942, 2.047054288528706412, -0.9635960562263863327 ) ) ;
#170681=CARTESIAN_POINT ( 'NONE',  ( 3.761794061002172729, 0.6050747832711267371, -1.707706662339498749 ) ) ;
#170682=CARTESIAN_POINT ( 'NONE',  ( 3.854619899909034419, -1.789536248510626315, -0.6842995647342240417 ) ) ;
#170683=CARTESIAN_POINT ( 'NONE',  ( 5.090316257491098284, 1.067296284200716983, -1.773933887923849984 ) ) ;
#170685=CARTESIAN_POINT ( 'NONE',  ( 3.326987498081665162, 0.04702425985559504501, 1.971060134238045602 ) ) ;
#170686=CARTESIAN_POINT ( 'NONE',  ( 1.518447027862340093, 1.295632655171574665, -1.425748867336932513 ) ) ;
#170687=CARTESIAN_POINT ( 'NONE',  ( 3.590566789841375339, -0.3639703897368729568, -1.834726254853453087 ) ) ;
#170688=CARTESIAN_POINT ( 'NONE',  ( 3.018547437338540806, -1.137872740210974287, -2.007595131770247843 ) ) ;
#170689=CARTESIAN_POINT ( 'NONE',  ( 3.596024570820981037, 0.8385914878215626755, -1.661501840750801540 ) ) ;
#170692=CARTESIAN_POINT ( 'NONE',  ( 1.453890484719716492, 0.6100395758942640523, -2.015780296659912985 ) ) ;
#170697=CARTESIAN_POINT ( 'NONE',  ( 3.551138032611600437, 0.3147205237276836653, 2.097014573754731881 ) ) ;
#170699=CARTESIAN_POINT ( 'NONE',  ( 0.8967469923133252196, -1.971478154887895684, -0.4383870506769834141 ) ) ;
#170705=CARTESIAN_POINT ( 'NONE',  ( 1.142116303652768172, 0.8771353898661786719, -1.975824051420910221 ) ) ;
#170706=CARTESIAN_POINT ( 'NONE',  ( 6.890000000000025437, 2.478461836817289043, 2.104748632312344103 ) ) ;
#170711=CARTESIAN_POINT ( 'NONE',  ( 6.087125082597877324, 1.679220375458953862, 1.116214469231976869 ) ) ;
#170714=CARTESIAN_POINT ( 'NONE',  ( 6.321832389622432657, 1.203313566387714584, -1.709558936785739780 ) ) ;
#170716=CARTESIAN_POINT ( 'NONE',  ( 6.631704542599726082, -1.407888343591977121, -1.640466528430361670 ) ) ;
#170724=CARTESIAN_POINT ( 'NONE',  ( 2.894803161253765467, 1.479297447286776590, -0.8868043451095276586 ) ) ;
#170726=CARTESIAN_POINT ( 'NONE',  ( 2.090717947541526289, 1.542569122296926221, -0.8672550169683733712 ) ) ;
#170728=CARTESIAN_POINT ( 'NONE',  ( 5.491335294905154818, 1.948586811899848614, -1.035780281143129811 ) ) ;
#170731=CARTESIAN_POINT ( 'NONE',  ( 4.201429114599513959, 1.802380596022877368, -0.9117778440167979559 ) ) ;
#170733=CARTESIAN_POINT ( 'NONE',  ( 4.213620120093874988, 1.703795446819071691, 1.262174061880352083 ) ) ;
#170734=CARTESIAN_POINT ( 'NONE',  ( 3.638296137631126914, 0.7283958097016438593, 1.880429543521966007 ) ) ;
#170735=CARTESIAN_POINT ( 'NONE',  ( 4.025510356283497515, -0.3035946714039591265, 1.785781755087331391 ) ) ;
#170738=ORIENTED_EDGE ( 'NONE', *, *, #100013, .F. ) ;
#170739=CARTESIAN_POINT ( 'NONE',  ( 0.9009904985227291663, 1.526999960511504772, 1.080287613699250304 ) ) ;
#170743=CARTESIAN_POINT ( 'NONE',  ( 6.639320575229251453, 0.008029245381881154262, 1.796863947021019481 ) ) ;
#170748=CARTESIAN_POINT ( 'NONE',  ( 0.03522015555855115276, -0.09184495783944729430, 1.910282976853895587 ) ) ;
#170753=CARTESIAN_POINT ( 'NONE',  ( 3.814780496183818315, -0.6684712460508880350, -2.012520831323429515 ) ) ;
#170755=CARTESIAN_POINT ( 'NONE',  ( 5.905538618093676639, -0.4813517389176332206, 1.911553968036589390 ) ) ;
#170757=CARTESIAN_POINT ( 'NONE',  ( 0.8791531640492165067, -1.821740142837099174, -0.8571184184497283587 ) ) ;
#170759=CARTESIAN_POINT ( 'NONE',  ( -0.1408020194050146334, -0.005144001661238749128, -2.100147592658160089 ) ) ;
#170761=CARTESIAN_POINT ( 'NONE',  ( 1.539598694730393680, 1.913698299121506352, -0.7905179490511196061 ) ) ;
#170766=CARTESIAN_POINT ( 'NONE',  ( 4.523432754507224374, -1.286067535266706807, -1.648171318802932106 ) ) ;
#170768=CARTESIAN_POINT ( 'NONE',  ( 3.065264358586119009, 0.2694654384877669395, -1.805464241506696155 ) ) ;
#170769=CARTESIAN_POINT ( 'NONE',  ( 1.805022944457121081, 1.575911691392884117, -0.8931387472532796856 ) ) ;
#170772=CARTESIAN_POINT ( 'NONE',  ( 6.604147088760183415, -2.206502607372296421, 0.04933187264975073122 ) ) ;
#170773=CARTESIAN_POINT ( 'NONE',  ( 3.768774344222697970, -1.483932802477351487, 1.633493490917396151 ) ) ;
#170776=CARTESIAN_POINT ( 'NONE',  ( 3.246637215680724164, 1.866209232881730573, 0.4165188312477489663 ) ) ;
#170778=CARTESIAN_POINT ( 'NONE',  ( 6.689897370947560873, -1.349224794794257720, -1.570457413003906177 ) ) ;
#170780=CARTESIAN_POINT ( 'NONE',  ( 5.741772062182810998, 2.188963553168365994, 0.1087695542012837302 ) ) ;
#170786=CARTESIAN_POINT ( 'NONE',  ( 3.409304255485625657, -0.3681080166235695117, 1.833790788056933962 ) ) ;
#170792=CARTESIAN_POINT ( 'NONE',  ( 6.438344962566215024, -1.112565956905732456, 1.745730973219234539 ) ) ;
#170793=CARTESIAN_POINT ( 'NONE',  ( 0.9664229901367871189, -1.967894173845800898, -0.4390061282484733485 ) ) ;
#170798=B_SPLINE_CURVE_WITH_KNOTS ( 'NONE', 3,
 ( #196980, #214252, #130990, #98423, #146133, #65883, #50735, #198041, #47565, #164488, #31300, #82158, #115794, #178618, #213215, #195928, #162367, #66952, #1957, #81101, #48620, #166625, #129940, #149304, #96312, #114735, #150386, #194851, #163432, #17145, #84302, #180733, #32359, #33416, #148249, #133091, #13947, #112606, #147190, #18217, #132031, #49671, #97375, #199089, #15012, #179679, #181783, #116861, #34480, #99495, #68018, #165552, #30228, #80030, #212146, #63782, #117939, #151454, #186059, #119007, #20358, #155716, #72302, #7299, #103771, #71230, #203363, #87519, #201231, #3026, #69094, #183933, #102697, #169822, #101623, #105942, #52872, #5153, #152508, #187133, #188198, #202294, #53946, #120083, #4092, #138408, #89664, #153584, #37694, #137345, #21409, #122239, #135216, #85372, #38762, #55015, #121164, #35545, #86443, #104843, #170888, #70163, #184985, #167688, #22481, #134159, #19290, #36611, #88592, #168755, #136274, #154649, #6231, #204427, #56082, #200167, #39834, #51821, #171966, #23557, #175182, #123309, #41986, #43056, #40912, #45185, #140569, #158916, #91805, #126495, #127575, #206581, #109169, #143777, #108095, #174124, #60334, #24625, #192458, #8381, #90732, #61412, #74464, #156795, #44112, #59268, #191390, #189273, #25697, #193543, #157863, #58210, #176241, #161048, #124369, #77655, #9456, #73377, #11583, #75528, #111299, #26768, #92870, #190327, #95002, #205511, #141639, #10512, #207648, #209772, #57142, #177303, #110233, #76586, #107018, #125424, #142697, #208707, #27843, #93940, #159981, #139482, #28917, #173042, #195683, #31060, #63545, #196743, #128636, #132839, #214016, #114496, #181543, #163189, #64609, #62474, #198843, #162123, #115547, #194602, #97136, #98196, #78714, #14773, #131786, #625, #148005, #80864, #129701, #149049, #50490, #180493, #130749, #211908, #49427, #197790, #48383, #47320, #33170, #113433, #13712, #146954, #144842, #99252, #66692, #210848, #32111, #145898, #116611, #46246, #165300, #82976, #179440, #182604, #212969, #164244, #15832, #81918, #16895, #34228, #65638, #79785, #178376, #100301, #12644, #96070, #112363, #29985, #204161, #37429, #167440, #117689, #86186, #186873, #22214, #51564, #185796, #170628, #88327, #134960, #166367, #102430, #154391, #168499, #20098, #199917, #169566, #19032, #5969, #85112, #72039, #138152, #151198, #69901, #103506, #120900, #55816, #121972, #184728, #187937, #4892, #183681, #21148, #39567, #87252, #2769, #136012, #68840, #202025, #153317, #150133, #36352, #200968, #133911, #38505, #17958, #52615, #152255, #84045, #118744, #3828, #67760, #53685, #1706, #35286, #119816, #203105, #101362, #70970, #137080, #54750, #104583, #205245, #171696, #105669, #73114, #23295, #56886, #155454, #7037, #139214, #123061, #189015, #89405, #179575, #96207, #66838, #147086, #113571, #162258, #1850, #31194, #33305, #213108, #178507, #30118, #112497, #79921, #67911, #198984, #134056, #46378, #97269, #13845, #65774, #64740, #148146, #196877, #163324, #146029, #132982, #130883, #14904, #212038, #63681, #80998, #99390, #48514, #129835, #195817, #47456, #114634, #180627, #32250, #98320, #164385, #15969, #82053, #131922, #214148, #197932, #50628, #34371, #49559, #115685, #181678, #166516, #165442, #116754, #182753, #17039, #83116, #149197, #100445, #772, #18107, #84194 ),
 .UNSPECIFIED., .F., .F.,
 ( 4, 1, 1, 1, 1, 1, 1, 1, 1, 1, 1, 1, 1, 1, 1, 1, 1, 1, 1, 1, 1, 1, 1, 1, 1, 1, 1, 1, 1, 1, 1, 1, 1, 1, 1, 1, 1, 1, 1, 1, 1, 1, 1, 1, 1, 1, 1, 1, 1, 1, 1, 1, 1, 1, 1, 1, 1, 1, 1, 1, 1, 1, 1, 1, 1, 1, 1, 1, 1, 1, 1, 1, 1, 1, 1, 1, 1, 1, 1, 1, 1, 1, 1, 1, 1, 1, 1, 1, 1, 1, 1, 1, 1, 1, 1, 1, 1, 1, 1, 1, 1, 1, 1, 1, 1, 1, 1, 1, 1, 1, 1, 1, 1, 1, 1, 1, 1, 1, 1, 1, 1, 1, 1, 1, 1, 1, 1, 1, 1, 1, 1, 1, 1, 1, 1, 1, 1, 1, 1, 1, 1, 1, 1, 1, 1, 1, 1, 1, 1, 1, 1, 1, 1, 1, 1, 1, 1, 1, 1, 1, 1, 1, 1, 1, 1, 1, 1, 1, 1, 1, 1, 1, 1, 1, 1, 1, 1, 1, 1, 1, 1, 1, 1, 1, 1, 1, 1, 1, 1, 1, 1, 1, 1, 1, 1, 1, 1, 1, 1, 1, 1, 1, 1, 1, 1, 1, 1, 1, 1, 1, 1, 1, 1, 1, 1, 1, 1, 1, 1, 1, 1, 1, 1, 1, 1, 1, 1, 1, 1, 1, 1, 1, 1, 1, 1, 1, 1, 1, 1, 1, 1, 1, 1, 1, 1, 1, 1, 1, 1, 1, 1, 1, 1, 1, 1, 1, 1, 1, 1, 1, 1, 1, 1, 1, 1, 1, 1, 1, 1, 1, 1, 1, 1, 1, 1, 1, 1, 1, 1, 1, 1, 1, 1, 1, 1, 1, 1, 1, 1, 1, 1, 1, 1, 1, 1, 1, 1, 1, 1, 1, 1, 1, 1, 1, 1, 1, 1, 1, 1, 1, 1, 1, 1, 1, 1, 1, 1, 1, 1, 1, 1, 1, 1, 1, 1, 1, 1, 1, 1, 1, 1, 1, 1, 1, 1, 1, 1, 1, 1, 1, 1, 1, 1, 1, 1, 1, 1, 1, 1, 1, 1, 1, 1, 1, 1, 1, 1, 1, 1, 1, 1, 1, 1, 1, 1, 1, 1, 1, 1, 1, 1, 1, 1, 1, 1, 1, 1, 1, 1, 1, 1, 1, 1, 1, 4 ),
 ( 0.000000000000000000, 0.002600209826155936224, 0.005208878553436857226, 0.007813350965615119270, 0.01041570154746907992, 0.01302155883015148306, 0.01562460066207539862, 0.01822947720112986364, 0.02083337797298438765, 0.02343721533725894035, 0.02604213897589890969, 0.02864525980212044229, 0.03125073504456635232, 0.03385369766904555017, 0.03645898980682723417, 0.03906240375024701977, 0.04166680464497042602, 0.04427120869897264999, 0.04687461886132015393, 0.04947991130494613921, 0.05208287402783655373, 0.05468834688957619622, 0.05729146186993632622, 0.05989639238693608009, 0.06250023923939096449, 0.06510408216679804128, 0.06770901469741306966, 0.07031212675311915294, 0.07291759917081726272, 0.07552056149378454097, 0.07812585104223603027, 0.08072926279340975064, 0.08333366149866272554, 0.08593806365491549193, 0.08854147146176674643, 0.09114676191340240208, 0.09374972248801059782, 0.09635519323906190092, 0.09895830628708340848, 0.1015632345865536273, 0.1041670796237980645, 0.1067709202568039306, 0.1093758509056654005, 0.1119789607794838548, 0.1145844312107493490, 0.1171873915655986947, 0.1197926790194954738, 0.1223960889855860712, 0.1250004854864837645, 0.1276048858798866925, 0.1302082914968497596, 0.1328135800830011481, 0.1354165386474412147, 0.1380220074263333041, 0.1406251186789811980, 0.1432300448973659046, 0.1458338882574615747, 0.1484377267335943440, 0.1510426556371624596, 0.1536457634674935069, 0.1562512320483212536, 0.1588541905735017246, 0.1614594760690261366, 0.1640628843880489185, 0.1666672788216651824, 0.1692716775892487424, 0.1718750811543677814, 0.1744803680111783883, 0.1770833247038955116, 0.1796887916465979840, 0.1822919012421508056, 0.1848968255159594287, 0.1875006673364670307, 0.1901045037933276616, 0.1927094310880738681, 0.1953125370132051675, 0.1979180038795354257, 0.2005209607134520455, 0.2031262443867272172, 0.2057296511966431873, 0.2083340436999963075, 0.2109384409787386505, 0.2135418426300015604, 0.2161471278935624962, 0.2187500828529475860, 0.2213555480953768861, 0.2239586561720615654, 0.2265635786377499516, 0.2291674190561798496, 0.2317712536313151217, 0.2343761794536610432, 0.2369792836118274071, 0.2395847488995502261, 0.2421877041805577391, 0.2447929861676560459, 0.2473963916063780244, 0.2500007823164346887, 0.2526051782432667259, 0.2552085781186103075, 0.2578138619249652486, 0.2604168152893601151, 0.2630222789673848927, 0.2656253856633817301, 0.2682303064573571261, 0.2708341456111751366, 0.2734379784420828963, 0.2760429029284052760, 0.2786460054577940548, 0.2812514693027542978, 0.2838544231691620401, 0.2864597036061101165, 0.2890631078115080133, 0.2916674968651886135, 0.2942718915769991783, 0.2968752898143142138, 0.2994805722994643427, 0.3020835242071668869, 0.3046889864566129091, 0.3072920919100609050, 0.3098970111686871198, 0.3125008491953192857, 0.3151046804194536644, 0.3177096037060897493, 0.3203127047448455222, 0.3229181672828482230, 0.3255211198729257016, 0.3281263988957095479, 0.3307298020056156362, 0.3333341895397992083, 0.3359385831734401084, 0.3385419799105768290, 0.3411472612104861635, 0.3437502117997557338, 0.3463556727564109927, 0.3489587771054129539, 0.3515636949650152721, 0.3541675320018531359, 0.3567713617566292128, 0.3593762839798815834, 0.3619793836661120978, 0.3645848450329270407, 0.3671877964849088460, 0.3697930742294792128, 0.3723964763816929868, 0.3750008625332226786, 0.3776052552255140804, 0.3802086506002868016, 0.3828139308508870520, 0.3854168802599494681, 0.3880223400595693151, 0.3906254434421968513, 0.3932303600390676390, 0.3958341962234732669, 0.3984380246462727593, 0.4010429459424146859, 0.4036460444141952153, 0.4062515047455624306, 0.4088544551976535102, 0.4114597317999305615, 0.4140631331322238151, 0.4166675180379114662, 0.4192719099256467796, 0.4218753040758395079, 0.4244805834130354061, 0.4270835317800880659, 0.4296889905584002634, 0.4322920931126992272, 0.4348970085831024290, 0.4375008440524135733, 0.4401046712805898320, 0.4427095917858701601, 0.4453126891812490551, 0.4479181486128839262, 0.4505210982032648026, 0.4531263737991432228, 0.4557297744492659897, 0.4583341582458977381, 0.4609385494658484461, 0.4635419425292200413, 0.4661472210888942258, 0.4687501685521111572, 0.4713556264448209299, 0.4739587283088163017, 0.4765636427889929916, 0.4791674776805284197, 0.4817713038514113699, 0.4843762237020596273, 0.4869793201590638665, 0.4895847788266616818, 0.4921877276934932821, 0.4947930024188478271, 0.4973964025245324327, 0.5000007853488734888, 0.5026051760377950872, 0.5052085681520839255, 0.5078138460701020485, 0.5104167927676396266, 0.5130222499104345468, 0.5156253512221359303, 0.5182302648483090302, 0.5208340992993732987, 0.5234379245502747136, 0.5260428438825063280, 0.5286459395391455152, 0.5312513975783873521, 0.5338543458598166147, 0.5364596198505067193, 0.5390630195494738874, 0.5416674015382738627, 0.5442717918329101900, 0.5468751831358398263, 0.5494804605480556603, 0.5520834066180569932, 0.5546888631466128095, 0.5572919640440190392, 0.5598968769523987588, 0.5625007111002878757, 0.5651045355685063720, 0.5677094545185276120, 0.5703125495128006373, 0.5729180070593572482, 0.5755209548935220631, 0.5781262282853970591, 0.5807296277153600750, 0.5833340090053582561, 0.5859383990424469335, 0.5885417896717308750, 0.5911470667139914204, 0.5937500122945923442, 0.5963554683445766447, 0.5989585689656815592, 0.6015634812924701702, 0.6041673152744758690, 0.6067711390973024033, 0.6093760578013157625, 0.6119791522712144660, 0.6145846094607528842, 0.6171875569857874222, 0.6197928299146914233, 0.6223962292133623508, 0.6250006099412922511, 0.6276049998575695676, 0.6302083899509167697, 0.6328136667590675835, 0.6354166119884008257, 0.6380220676954796444, 0.6406251681782773044, 0.6432300800596744139, 0.6458339140130902045, 0.6484377373278128465, 0.6510426559220214848, 0.6536457500055372627, 0.6562512069737248543, 0.6588541543277639523, 0.6614594269295416273, 0.6640628262346358612, 0.6666672065372305500, 0.6692715964694370134, 0.6718749861645568755, 0.6744802628744462902, 0.6770832078906477980, 0.6796886633904898334, 0.6822917638729786294, 0.6848966754451861760, 0.6875005095073121186, 0.6901043324512210475, 0.6927092510718347862, 0.6953123449069624762, 0.6979178017894718256, 0.7005207491106575368, 0.7031260215211581066, 0.7057294209703992571, 0.7083338009843969107, 0.7109381910692819107, 0.7135415805038890502, 0.7161468572513741693, 0.7187498021925872171, 0.7213552576208688283, 0.7239583582410578089, 0.7265632696402853918, 0.7291671039484327599, 0.7317709266588259265, 0.7343758454420658000, 0.7369789391668094547, 0.7395843960993241373, 0.7421873435258099505, 0.7447926158808931829, 0.7473960156120186271, 0.7500003954741673029, 0.7526047858484943287, 0.7552081751603144655, 0.7578134520812660480, 0.7604163970856469001, 0.7630218525780576577, 0.7656249534739711926, 0.7682298648364407345, 0.7708336995279378989, 0.7734375221421257995, 0.7760424412242287184, 0.7786455349766069345, 0.7812509920948264019, 0.7838539397647821261, 0.7864592122003229990, 0.7890626123510894319, 0.7916669921981516200, 0.7942713829987035901, 0.7968747723254782089, 0.7994800495557851105, 0.8020829947615083499, 0.8046884504537559213, 0.8072915517634385862, 0.8098964632253897733, 0.8125002984375870874, 0.8151041210928977598, 0.8177090406101226172, 0.8203121345281733090, 0.8229175919678175521, 0.8255205400194353116, 0.8281258126713292311, 0.8307292133795166622, 0.8333335933482756142, 0.8359379847118599827, 0.8385413741913512187, 0.8411466518669262760, 0.8437495974121898001, 0.8463550534400045011, 0.8489581553015269622, 0.8515630669992224622, 0.8541669028694969246, 0.8567707257032814994, 0.8593756457919137226, 0.8619787400136992295, 0.8645841979105142183, 0.8671871464820134490, 0.8697924194861808012, 0.8723958208895988831, 0.8750002011168627192, 0.8776045931803160283, 0.8802079829503125508, 0.8828132612070975771, 0.8854162072301272612, 0.8880216637292678294, 0.8906247662807315058, 0.8932296783504612980, 0.8958335150162225480, 0.8984373381658604663, 0.9010422589622166800, 0.9036453536258294283, 0.9062508121155921081, 0.9088537613452241093, 0.9114590348376164775, 0.9140624370741091687, 0.9166668176967164294, 0.9192712105969091940, 0.9218746007952320909, 0.9244798797692056480, 0.9270828264082496828, 0.9296882835145078294, 0.9322913868941045124, 0.9348962994721256026, 0.9375001370706889103, 0.9401039606740361210, 0.9427088823143441321, 0.9453119775565693717, 0.9479174367776000976, 0.9505203868030935865, 0.9531256609099927335, 0.9557290641454977420, 0.9583334452981105978, 0.9609378390199675435, 0.9635412300619400350, 0.9661465102466426647, 0.9687494557931184413, 0.9713549143510965544, 0.9739580252604012056, 0.9765629275426017664, 0.9791667581373608709, 0.9817706348486141543, 0.9843755007711335603, 0.9869785191422796311, 0.9895843624858681187, 0.9921867025132995455, 0.9947911529560371502, 0.9973998138561904758, 1.000000000000000000 ),
 .UNSPECIFIED. ) ;
#170799=CARTESIAN_POINT ( 'NONE',  ( 1.289316216709124996, 1.661312375189183399, 1.429258102917586815 ) ) ;
#170800=CARTESIAN_POINT ( 'NONE',  ( 4.670415550810885996, -1.190324863180821646, 1.384379922071424351 ) ) ;
#170808=CARTESIAN_POINT ( 'NONE',  ( 3.878315922200573862, -0.1843894689829879696, -1.832007427040844183 ) ) ;
#170809=CARTESIAN_POINT ( 'NONE',  ( 5.924093355334532518, -1.997480882691978987, 0.2508417921044738819 ) ) ;
#170810=CARTESIAN_POINT ( 'NONE',  ( 1.617049182541079544, 0.6662764605713987764, -2.199669867806148371 ) ) ;
#170812=CARTESIAN_POINT ( 'NONE',  ( 6.965691013979927959, -0.4331334938386353084, 1.920344510276907890 ) ) ;
#170815=CARTESIAN_POINT ( 'NONE',  ( 3.673993457511487204, 1.897360377298975553, -0.2389773157873422427 ) ) ;
#170819=CARTESIAN_POINT ( 'NONE',  ( 2.894169963053084160, -0.6095376172369629808, -1.999899515593931199 ) ) ;
#170820=CARTESIAN_POINT ( 'NONE',  ( 1.692057038649401601, -1.861345348035767344, -0.1864469194169729449 ) ) ;
#170821=CARTESIAN_POINT ( 'NONE',  ( 2.249374845261054467, -1.976652949091894707, -0.3960421909960794018 ) ) ;
#170824=CARTESIAN_POINT ( 'NONE',  ( 3.596946774904510757, -0.5014486528964605672, 1.666646126512297821 ) ) ;
#170827=CARTESIAN_POINT ( 'NONE',  ( 3.932037377198682737, 0.9205326289291086983, -1.458499330894097668 ) ) ;
#170828=CARTESIAN_POINT ( 'NONE',  ( 3.333693798916517625, 0.9835563995168915552, -1.958507884819527867 ) ) ;
#170829=CARTESIAN_POINT ( 'NONE',  ( 6.691986956589398794, -0.9478133180038283978, 1.990996264204819122 ) ) ;
#170831=CARTESIAN_POINT ( 'NONE',  ( 4.118177926953592305, 2.155335829443456142, -0.2601999948229383741 ) ) ;
#170832=CARTESIAN_POINT ( 'NONE',  ( 1.699542765152612711, -0.6164703606487754728, 1.718597393154073671 ) ) ;
#170834=CARTESIAN_POINT ( 'NONE',  ( 4.733676700703519202, 0.6609272643324247687, -2.011644693266708916 ) ) ;
#170835=CARTESIAN_POINT ( 'NONE',  ( 6.539320575229251808, 0.004279804010676873348, 1.996977849922920267 ) ) ;
#170837=CARTESIAN_POINT ( 'NONE',  ( 4.845436733290686249, 0.7204735554154987343, -2.176297985750157427 ) ) ;
#170839=CARTESIAN_POINT ( 'NONE',  ( 6.720655732516610747, 3.700489942686377098, 2.440724243369211788 ) ) ;
#170842=CARTESIAN_POINT ( 'NONE',  ( 0.6805317496583452863, 1.048634805427307359, 1.842989218901350812 ) ) ;
#170848=CARTESIAN_POINT ( 'NONE',  ( 4.852185490356213826, 0.1948433276699329531, -2.006959737079899497 ) ) ;
#170850=CARTESIAN_POINT ( 'NONE',  ( 2.764570516439817549, -0.7852151221510113022, -1.907448154738192514 ) ) ;
#170852=CARTESIAN_POINT ( 'NONE',  ( -0.2411972340276230808, 7.629137130509075604, -2.500476664557866435 ) ) ;
#170856=CARTESIAN_POINT ( 'NONE',  ( 5.771465802492605768, 1.302860414194568550, 1.761948869136241047 ) ) ;
#170857=CARTESIAN_POINT ( 'NONE',  ( 3.920546200773936896, -1.392545040883992336, -1.458557299768625581 ) ) ;
#170858=CARTESIAN_POINT ( 'NONE',  ( 3.614658571667620279, -0.1319153736358945894, 1.836568937333193485 ) ) ;
#170860=CARTESIAN_POINT ( 'NONE',  ( 2.218750000000001332, -0.7852924748298697466, 1.895863743164134974 ) ) ;
#170861=CARTESIAN_POINT ( 'NONE',  ( 1.148929321228649991, -1.355925326379325391, -1.065857193176344309 ) ) ;
#170863=( BOUNDED_SURFACE ( )  B_SPLINE_SURFACE ( 3, 3, ( 
 ( #127605, #111329, #179468, #177332, #28946, #191422, #13742, #95030, #161080, #141671 ),
 ( #194634, #31093, #79815, #12670, #126528, #62501, #97165, #144869, #210876, #128666 ),
 ( #46276, #112392, #207682, #59302, #43088, #10542, #109201, #26796, #92901, #158947 ),
 ( #142729, #148032, #213000, #199949, #36388, #102466, #67792, #115575, #214042, #181571 ),
 ( #130776, #15864, #16924, #14802, #65668, #48414, #196771, #81949, #183710, #101396 ),
 ( #80893, #50519, #131816, #134992, #146983, #167470, #85144, #197825, #201002, #83004 ),
 ( #149080, #99283, #19066, #64637, #658, #165331, #49457, #66725, #2800, #164274 ) ),
 .UNSPECIFIED., .T., .F., .T. ) 
 B_SPLINE_SURFACE_WITH_KNOTS ( ( 4, 3, 4 ),
 ( 4, 1, 1, 1, 1, 1, 1, 4 ),
 ( 0.000000000000000000, 0.5000000000000000000, 1.000000000000000000 ),
 ( 0.000000000000000000, 0.09790276019723312406, 0.1918320694002237370, 0.2608036337010187777, 0.3626611837559554630, 0.5214803378330250538, 0.7337833476510040587, 1.000000000000000000 ),
 .UNSPECIFIED. ) 
 GEOMETRIC_REPRESENTATION_ITEM ( )  RATIONAL_B_SPLINE_SURFACE ( (
 ( 1.000000000000000444, 1.000000000000000444, 1.000000000000000000, 1.000000000000000444, 1.000000000000000222, 1.000000000000000222, 1.000000000000000444, 1.000000000000000000, 1.000000000000000222, 1.000000000000000222),
 ( 0.3333333333333334814, 0.3333333333333334814, 0.3333333333333334814, 0.3333333333333334259, 0.3333333333333333703, 0.3333333333333334259, 0.3333333333333335369, 0.3333333333333333703, 0.3333333333333334259, 0.3333333333333334259),
 ( 0.3333333333333334814, 0.3333333333333334814, 0.3333333333333334814, 0.3333333333333334259, 0.3333333333333333703, 0.3333333333333334259, 0.3333333333333335369, 0.3333333333333333703, 0.3333333333333334259, 0.3333333333333334259),
 ( 1.000000000000000444, 1.000000000000000444, 1.000000000000000000, 1.000000000000000444, 1.000000000000000222, 1.000000000000000222, 1.000000000000000444, 1.000000000000000000, 1.000000000000000222, 1.000000000000000222),
 ( 0.3333333333333334814, 0.3333333333333334814, 0.3333333333333334814, 0.3333333333333334259, 0.3333333333333333703, 0.3333333333333334259, 0.3333333333333335369, 0.3333333333333333703, 0.3333333333333334259, 0.3333333333333334259),
 ( 0.3333333333333334814, 0.3333333333333334814, 0.3333333333333334814, 0.3333333333333334259, 0.3333333333333333703, 0.3333333333333334259, 0.3333333333333335369, 0.3333333333333333703, 0.3333333333333334259, 0.3333333333333334259),
 ( 1.000000000000000444, 1.000000000000000444, 1.000000000000000000, 1.000000000000000444, 1.000000000000000222, 1.000000000000000222, 1.000000000000000444, 1.000000000000000000, 1.000000000000000222, 1.000000000000000222) ) ) 
 REPRESENTATION_ITEM ( '' )  SURFACE ( )  );
#170864=CARTESIAN_POINT ( 'NONE',  ( 0.9151166212276349299, -1.463470719828030120, -1.772635753884302057 ) ) ;
#170866=CARTESIAN_POINT ( 'NONE',  ( 0.4568015506021270156, 0.8674211623492070755, 2.089700042804636837 ) ) ;
#170867=CARTESIAN_POINT ( 'NONE',  ( 2.737057789242686390, 0.2582918889518608374, 2.090101187703028884 ) ) ;
#170875=CARTESIAN_POINT ( 'NONE',  ( 4.043395766388809598, 0.1113883285390921962, 2.218758960698932192 ) ) ;
#170876=CARTESIAN_POINT ( 'NONE',  ( 2.800927341068761844, 1.851789894747071008, 1.171597702228709181 ) ) ;
#170879=CARTESIAN_POINT ( 'NONE',  ( 5.160583804383015227, -0.6592509027269661814, -1.847929681152965520 ) ) ;
#170883=CARTESIAN_POINT ( 'NONE',  ( 4.430007776716601953, -2.079114408633813582, 0.4165480963118637914 ) ) ;
#170886=CARTESIAN_POINT ( 'NONE',  ( 6.016527291255574283, 1.455332790597754000, -1.598591904487467463 ) ) ;
#170888=CARTESIAN_POINT ( 'NONE',  ( 4.880324068823122197, -0.2306306682541107433, -1.826696389425507938 ) ) ;
#170892=CARTESIAN_POINT ( 'NONE',  ( 0.4150587399484934603, -0.9287321991380654840, -1.471733822881353015 ) ) ;
#170893=CARTESIAN_POINT ( 'NONE',  ( 6.827182134110246103, 6.039869998172250121, 2.305852349323509021 ) ) ;
#170896=CARTESIAN_POINT ( 'NONE',  ( 3.924826023212550030, 2.051882857192890430, 0.6804245187241527715 ) ) ;
#170899=CARTESIAN_POINT ( 'NONE',  ( 3.133815226704575796, -1.450665623810345473, -1.602838778681405785 ) ) ;
#170900=CARTESIAN_POINT ( 'NONE',  ( 5.272717044759430927, -1.855309747074182836, -0.6666870051924634888 ) ) ;
#170901=CARTESIAN_POINT ( 'NONE',  ( 4.165211049733441584, -0.5436426828948260903, -1.646488866570811060 ) ) ;
#170902=CARTESIAN_POINT ( 'NONE',  ( 0.6092356648998223934, -0.3158941238240610128, 2.168550393043596536 ) ) ;
#170903=CARTESIAN_POINT ( 'NONE',  ( 0.7280630558558630616, -2.190032360377992315, 0.7273814547973026512 ) ) ;
#170904=CARTESIAN_POINT ( 'NONE',  ( 3.339188440279222458, -1.819168825518402199, 0.9681599264559497264 ) ) ;
#170905=CARTESIAN_POINT ( 'NONE',  ( 5.337426827915986216, 0.7834791095375337466, -1.777179163755914448 ) ) ;
#170912=CARTESIAN_POINT ( 'NONE',  ( 3.645738483435243982, -1.669485028154977790, -1.443228448415982079 ) ) ;
#170915=CARTESIAN_POINT ( 'NONE',  ( 0.6724161089360582988, 1.288989887148813018, -1.342485977130857711 ) ) ;
#170918=CARTESIAN_POINT ( 'NONE',  ( 6.925078400183548588, 2.417948008941684268, 2.525058136801380027 ) ) ;
#170919=CARTESIAN_POINT ( 'NONE',  ( 6.351489326974223637, 1.835832825663574752, -0.1405570519043483624 ) ) ;
#170921=CARTESIAN_POINT ( 'NONE',  ( 2.518495319897054330, 1.347246837915631490, -1.559621528479130825 ) ) ;
#170927=CARTESIAN_POINT ( 'NONE',  ( 0.9013288230189763217, 1.684346374898238352, 1.187240197102001904 ) ) ;
#170932=CARTESIAN_POINT ( 'NONE',  ( 5.356176587289051660, 2.204499490778097481, -0.1052899746726426722 ) ) ;
#170933=CARTESIAN_POINT ( 'NONE',  ( 0.5093243970649004027, 1.880507610096779025, 1.065828983023514809 ) ) ;
#170935=CARTESIAN_POINT ( 'NONE',  ( 0.6680393924826667496, 1.910109291395128972, -0.09634788558426229943 ) ) ;
#170936=CARTESIAN_POINT ( 'NONE',  ( 0.7433754753295095385, 0.3886281223182270761, -1.978556061772406505 ) ) ;
#170943=CARTESIAN_POINT ( 'NONE',  ( 1.586564105604048480, -0.2713065988851799393, -1.850747533123621391 ) ) ;
#170944=CARTESIAN_POINT ( 'NONE',  ( 2.483611571103708116, -0.6279893487078171965, 1.916353726171161620 ) ) ;
#170948=CARTESIAN_POINT ( 'NONE',  ( 4.863951442137788739, 2.083289488599335826, -0.3080729427491457062 ) ) ;
#170954=CARTESIAN_POINT ( 'NONE',  ( 4.429947715222688487, -1.979980911821906497, 0.3981057063161990706 ) ) ;
#170956=CARTESIAN_POINT ( 'NONE',  ( 5.969198602517502117, 1.817331191306554850, 0.9757160385870704555 ) ) ;
#170958=CARTESIAN_POINT ( 'NONE',  ( 5.026735257907362531, 2.066873009482797841, 0.6328083787210944111 ) ) ;
#170962=CARTESIAN_POINT ( 'NONE',  ( -0.2108831679770960255, -0.001785917861228669690, -1.896958272444612792 ) ) ;
#170964=CARTESIAN_POINT ( 'NONE',  ( 1.416727708472965253, 0.8794254021464522619, 1.985261695379604507 ) ) ;
#170967=CARTESIAN_POINT ( 'NONE',  ( 1.522747961674526085, -1.733470594775164075, 0.6210259959333885860 ) ) ;
#170970=CARTESIAN_POINT ( 'NONE',  ( 2.876726420669137863, -0.1638259704515396820, -2.185508879517850112 ) ) ;
#170971=CARTESIAN_POINT ( 'NONE',  ( 6.983263157960363898, 2.958708369276577432, 2.506372104999963657 ) ) ;
#170972=CARTESIAN_POINT ( 'NONE',  ( 3.977597974223236132, 2.131470459685447238, -0.7591987100158004154 ) ) ;
#170978=CARTESIAN_POINT ( 'NONE',  ( 5.430809967973590169, 0.1307738731834498513, 1.764929826691101100 ) ) ;
#170980=CARTESIAN_POINT ( 'NONE',  ( 1.571456177274520805, 0.1552745290232947217, -2.100303177343607608 ) ) ;
#170983=CARTESIAN_POINT ( 'NONE',  ( 1.205442482676940541, -1.550459043822360661, -1.214442484561629509 ) ) ;
#170985=CARTESIAN_POINT ( 'NONE',  ( 0.3792546940144908563, -0.1001052471676349837, 1.959448305358338693 ) ) ;
#170986=CARTESIAN_POINT ( 'NONE',  ( 5.484552789610383172, -1.142847587564936207, 1.405643779654427661 ) ) ;
#170990=CARTESIAN_POINT ( 'NONE',  ( 4.680451076648031616, -1.814532364864028136, -0.4542276060127621862 ) ) ;
#170993=CARTESIAN_POINT ( 'NONE',  ( 5.418829850390409320, -1.503349927839289002, 1.423607673449282851 ) ) ;
#171005=CARTESIAN_POINT ( 'NONE',  ( 5.564887814092526419, 1.486691789297951871, -1.280227714881218892 ) ) ;
#171007=CARTESIAN_POINT ( 'NONE',  ( 2.284529629648517801, -1.956262009633228605, 0.4871271731112236658 ) ) ;
#171009=CARTESIAN_POINT ( 'NONE',  ( 0.6268464039562298140, 0.1668571106153530770, 2.185281662807083691 ) ) ;
#171011=CARTESIAN_POINT ( 'NONE',  ( 2.495189509527053762, 1.443206194050347557, 1.189963633554675937 ) ) ;
#171013=CARTESIAN_POINT ( 'NONE',  ( 3.814701174604028466, -0.6354162253871125099, -1.910337659313849024 ) ) ;
#171016=CARTESIAN_POINT ( 'NONE',  ( 4.939118062403117904, -1.789252976562827779, -1.131630611658622332 ) ) ;
#171018=CARTESIAN_POINT ( 'NONE',  ( 5.652806998763869828, -0.4994405740583847675, -2.009109930559597856 ) ) ;
#171019=CARTESIAN_POINT ( 'NONE',  ( 0.7496951219271037470, 2.088183804393455301, -0.1063107438588738879 ) ) ;
#171020=CARTESIAN_POINT ( 'NONE',  ( 6.720655732516679137, 7.052218778754904882, 2.671889809988809983 ) ) ;
#171021=CARTESIAN_POINT ( 'NONE',  ( 0.1469036390603413456, -1.327996847208750442, -1.100432056080926202 ) ) ;
#171022=ORIENTED_EDGE ( 'NONE', *, *, #68712, .T. ) ;
#171029=CARTESIAN_POINT ( 'NONE',  ( 6.516268831907007453, -1.911747763583053317, 0.05203757306279645223 ) ) ;
#171036=CARTESIAN_POINT ( 'NONE',  ( 6.099232498865051255, -0.2440123228986730841, 2.001514574626765075 ) ) ;
#171037=CARTESIAN_POINT ( 'NONE',  ( 0.8035760164417544704, 1.868272328500224289, -1.003034915376184388 ) ) ;
#171039=CARTESIAN_POINT ( 'NONE',  ( -0.1399997263889612154, 1.357298622859518078, -2.254419820505838334 ) ) ;
#171042=CARTESIAN_POINT ( 'NONE',  ( 3.854321288642187149, -1.967005588004781202, -0.1009957709416451771 ) ) ;
#171043=CARTESIAN_POINT ( 'NONE',  ( 4.112907772398490813, 0.1017678201147946826, 2.013986186455194449 ) ) ;
#171045=CARTESIAN_POINT ( 'NONE',  ( 6.727182134110222478, 4.688348259194305534, 2.751590707055273199 ) ) ;
#171046=CARTESIAN_POINT ( 'NONE',  ( 4.716832014018703667, -0.1092502567305031480, 2.188841582221649595 ) ) ;
#171048=CARTESIAN_POINT ( 'NONE',  ( 2.977471715415116460, 1.829795069231574534, -0.6025905002205227401 ) ) ;
#171050=CARTESIAN_POINT ( 'NONE',  ( -0.02968770228140016343, 1.391517546076680434, -2.083419219542380407 ) ) ;
#171058=CARTESIAN_POINT ( 'NONE',  ( 5.559413648769178096, 1.607788300429791262, 1.137107417019854072 ) ) ;
#171059=CARTESIAN_POINT ( 'NONE',  ( 0.4330194205178988232, -1.374205638499223614, -1.372529395279479703 ) ) ;
#171060=CARTESIAN_POINT ( 'NONE',  ( 3.897138702661524956, -0.1997049427340416294, -2.003176435020975088 ) ) ;
#171061=CARTESIAN_POINT ( 'NONE',  ( 5.536544918007444416, 2.217299919257350371, -0.6050018498083614693 ) ) ;
#171062=CARTESIAN_POINT ( 'NONE',  ( 3.590524784426767813, 1.814595775041549564, 0.4119230038364861679 ) ) ;
#171068=CARTESIAN_POINT ( 'NONE',  ( 5.935123052105460317, -1.514893180500265002, -1.441204661170019108 ) ) ;
#171073=CARTESIAN_POINT ( 'NONE',  ( 0.8205984872286451459, 1.685833220154912881, 0.7012733028506010768 ) ) ;
#171075=CARTESIAN_POINT ( 'NONE',  ( 3.094086244858067047, -0.3350832708051197373, 1.701246549458427015 ) ) ;
#171077=CARTESIAN_POINT ( 'NONE',  ( 6.609000000000047947, 0.5928748489389294996, 1.953858053793898542 ) ) ;
#171080=CARTESIAN_POINT ( 'NONE',  ( 0.2509399751232620490, -0.4509356589572112162, -2.027996233343106081 ) ) ;
#171081=CARTESIAN_POINT ( 'NONE',  ( 6.041596546049881944, -1.325759876995153075, -1.255439798616593716 ) ) ;
#171082=CARTESIAN_POINT ( 'NONE',  ( 3.907043859180459933, -1.606318986283064021, 1.125903821926607318 ) ) ;
#171087=CARTESIAN_POINT ( 'NONE',  ( 4.178469031319306914, 1.000645923475869559, 1.869553197578948334 ) ) ;
#171091=CARTESIAN_POINT ( 'NONE',  ( 2.061466481998303735, 1.718891244229248105, 1.153550331455879707 ) ) ;
#171096=CARTESIAN_POINT ( 'NONE',  ( 4.407017973072342443, -0.4864924038828158381, -2.167217472756521879 ) ) ;
#171098=CARTESIAN_POINT ( 'NONE',  ( 2.145563594533715257, 0.9871410470321148045, 2.076082784368099787 ) ) ;
#171100=CARTESIAN_POINT ( 'NONE',  ( 6.631690664033638605, 1.975529463507015526, -0.5929735606366983713 ) ) ;
#171106=CARTESIAN_POINT ( 'NONE',  ( 3.445477555875466891, -1.765175379189663607, 0.7362804355328657069 ) ) ;
#171108=CARTESIAN_POINT ( 'NONE',  ( 3.873808679987042147, 0.9582704680195216485, 1.433834079761304281 ) ) ;
#171109=CARTESIAN_POINT ( 'NONE',  ( 2.764861550476094276, -0.1531697945360478708, -2.010801143277194392 ) ) ;
#171110=CARTESIAN_POINT ( 'NONE',  ( 3.815287691547566418, 1.229174737571071541, -1.942296044024049761 ) ) ;
#171112=CARTESIAN_POINT ( 'NONE',  ( 3.550319795034285519, 2.262578822424826441, 0.004170446471787879993 ) ) ;
#171113=CARTESIAN_POINT ( 'NONE',  ( 0.01274299142895937362, -0.9473294304004549193, -1.991142614049784099 ) ) ;
#171115=CARTESIAN_POINT ( 'NONE',  ( 5.149538872483485186, 0.5550977867328189541, -1.680460614999980340 ) ) ;
#171117=CARTESIAN_POINT ( 'NONE',  ( 1.183963288966838334, -1.026766722195756376, 2.049517438521175183 ) ) ;
#171118=CARTESIAN_POINT ( 'NONE',  ( 5.665905727187005247, -1.164751086281138770, 1.425882759469448979 ) ) ;
#171120=CARTESIAN_POINT ( 'NONE',  ( 5.226606370275341362, 0.1587857941063846590, 2.185760735149797185 ) ) ;
#171124=CARTESIAN_POINT ( 'NONE',  ( 6.373496627357888578, -0.2573980274669443458, 2.054251119134167691 ) ) ;
#171125=CARTESIAN_POINT ( 'NONE',  ( 0.6027503803631119039, 1.865048444749048739, 0.7672877736318934883 ) ) ;
#171127=CARTESIAN_POINT ( 'NONE',  ( 3.791558849520747287, 1.396117892292214613, 1.327735796816224223 ) ) ;
#171130=CARTESIAN_POINT ( 'NONE',  ( 1.564984312397620814, 0.7026195195478746047, 2.107413697313319290 ) ) ;
#171139=CARTESIAN_POINT ( 'NONE',  ( 2.717183929654675811, -1.705535211757349456, -0.9694657131227711888 ) ) ;
#171143=CARTESIAN_POINT ( 'NONE',  ( 0.2739786698724961944, -2.023204396000506833, 0.4007670430965051822 ) ) ;
#171147=CARTESIAN_POINT ( 'NONE',  ( 6.702040708066513197, -2.161345696851162845, 0.04751196314212167288 ) ) ;
#171152=CARTESIAN_POINT ( 'NONE',  ( 1.053721402318724021, 1.868689351376726204, -0.08586956420430363890 ) ) ;
#171153=CARTESIAN_POINT ( 'NONE',  ( 0.7911957196942709380, 1.314039333434241508, -1.131676627359794240 ) ) ;
#171155=CARTESIAN_POINT ( 'NONE',  ( 4.687173145698103838, 1.624054394666199830, 1.471728111018810070 ) ) ;
#171156=CARTESIAN_POINT ( 'NONE',  ( 5.298025090176222029, -0.8365315220497183679, 2.150796518170698057 ) ) ;
#171157=CARTESIAN_POINT ( 'NONE',  ( 6.802032647988246694, -2.060431444914239130, 0.04577141437269586360 ) ) ;
#171158=CARTESIAN_POINT ( 'NONE',  ( 2.062350447250702157, -1.775486198902403778, -0.7870378659600388849 ) ) ;
#171164=CARTESIAN_POINT ( 'NONE',  ( 3.779922787921150995, 1.701948043757589124, -1.081065327119046016 ) ) ;
#171168=CARTESIAN_POINT ( 'NONE',  ( 0.6623940301842005107, -1.324425631624454036, 1.256838194884236204 ) ) ;
#171174=CARTESIAN_POINT ( 'NONE',  ( 5.190332118341006051, -2.045072267241864861, -0.2543341860123843334 ) ) ;
#171179=CARTESIAN_POINT ( 'NONE',  ( 5.215492487644303843, 1.652332223238074604, 1.161132580238199541 ) ) ;
#171180=CARTESIAN_POINT ( 'NONE',  ( 6.199871938995108245, 1.529590366309235172, 1.610960538716522006 ) ) ;
#171184=CARTESIAN_POINT ( 'NONE',  ( 5.330957127283824981, 0.1492067265368417217, 2.055538663769764796 ) ) ;
#171185=CARTESIAN_POINT ( 'NONE',  ( 3.727185537919291747, 2.006959858346604619, 0.1948421285040344286 ) ) ;
#171192=CARTESIAN_POINT ( 'NONE',  ( 4.288435361214689046, -1.930121902525683053, 0.5825675424541224556 ) ) ;
#171193=CARTESIAN_POINT ( 'NONE',  ( 3.679498877186979211, -0.9061679144062879665, 1.602619060095414216 ) ) ;
#171195=CARTESIAN_POINT ( 'NONE',  ( 1.963905137100800724, 0.3917726540721230832, -2.274054798471192296 ) ) ;
#171197=CARTESIAN_POINT ( 'NONE',  ( 4.112696061561730509, 1.531809107248631507, -1.525399859652858847 ) ) ;
#171200=CARTESIAN_POINT ( 'NONE',  ( 3.163697234774452305, -0.6641558444393131921, -2.200356767709225725 ) ) ;
#171202=CARTESIAN_POINT ( 'NONE',  ( 2.483090063216564669, 1.711211315118581711, -0.7561169667836544761 ) ) ;
#171203=CARTESIAN_POINT ( 'NONE',  ( 6.789933821422706295, -0.8420773930338676383, 1.780570074765168043 ) ) ;
#171207=CARTESIAN_POINT ( 'NONE',  ( 1.612255294781844706, -2.189918024983358080, 0.2725913246661854084 ) ) ;
#171212=CARTESIAN_POINT ( 'NONE',  ( 6.244996228834688523, -1.665663155820007013, 1.054347381401467887 ) ) ;
#171213=CARTESIAN_POINT ( 'NONE',  ( 5.883493432195608719, 2.134490442297873880, -0.8776364701479767438 ) ) ;
#171214=CARTESIAN_POINT ( 'NONE',  ( 0.1390251588108057101, -0.1389306544097475005, -1.930426113910483688 ) ) ;
#171215=CARTESIAN_POINT ( 'NONE',  ( 2.553648762129530958, 1.591643574212991297, 1.311770128662164137 ) ) ;
#171222=CARTESIAN_POINT ( 'NONE',  ( 5.916515574059204141, 0.8745146271147998807, 1.987442084954823773 ) ) ;
#171224=CARTESIAN_POINT ( 'NONE',  ( 4.686955257832659427, 1.367739038236553517, 1.232883728221023212 ) ) ;
#171232=CARTESIAN_POINT ( 'NONE',  ( -0.09332341176954483952, -0.4182270256129701491, -1.872751671355552983 ) ) ;
#171233=CARTESIAN_POINT ( 'NONE',  ( 1.604008636410862554, -0.6330215999658711512, -1.652955932040809595 ) ) ;
#171234=CARTESIAN_POINT ( 'NONE',  ( 6.340495571224031401, 1.157139813629002756, -1.647119299906736556 ) ) ;
#171236=CARTESIAN_POINT ( 'NONE',  ( 2.829585337313187399, 0.6869450147981278620, -1.788391637942953860 ) ) ;
#171238=CARTESIAN_POINT ( 'NONE',  ( 4.334397697284593676, -1.135867708366841367, 1.608802569665278348 ) ) ;
#171239=CARTESIAN_POINT ( 'NONE',  ( 0.2992908618118708675, -0.2657624787030036240, -2.103842954668332599 ) ) ;
#171241=CARTESIAN_POINT ( 'NONE',  ( 3.203821283898714345, -1.868584281295191607, 0.09040415888627445495 ) ) ;
#171242=CARTESIAN_POINT ( 'NONE',  ( 5.971300253285758863, 0.1196647562241616447, -1.720808320142935610 ) ) ;
#171244=CARTESIAN_POINT ( 'NONE',  ( 2.895379187063460424, 1.892502543702856865, -1.135010264495312837 ) ) ;
#171247=CARTESIAN_POINT ( 'NONE',  ( 1.293506021254931193, -1.865543137965872678, 0.8802379953135958113 ) ) ;
#171256=CARTESIAN_POINT ( 'NONE',  ( 2.647004975520852454, -0.3514972095969396970, -2.040143077068845123 ) ) ;
#171261=CARTESIAN_POINT ( 'NONE',  ( 0.8737014391667098367, 0.3917534382160395290, -1.981132022265948756 ) ) ;
#171262=B_SPLINE_CURVE_WITH_KNOTS ( 'NONE', 3,
 ( #110304, #143850, #45252, #98257, #81987, #49495, #181611, #64674, #164314, #1781, #65708 ),
 .UNSPECIFIED., .F., .F.,
 ( 4, 1, 1, 1, 1, 1, 1, 1, 4 ),
 ( 0.000000000000000000, 0.2254494161556361009, 0.3971188491599597081, 0.5240836380151728813, 0.6154273167216615104, 0.6803253696226415626, 0.7282602231486813293, 0.7688932809586735972, 1.000000000000000000 ),
 .UNSPECIFIED. ) ;
#171265=CARTESIAN_POINT ( 'NONE',  ( 0.07459516483343267557, 2.058153987855536382, -2.173125978204577535 ) ) ;
#171267=CARTESIAN_POINT ( 'NONE',  ( 5.255232437486731634, -2.000551055875991580, -0.2495666058281582056 ) ) ;
#171268=CARTESIAN_POINT ( 'NONE',  ( 6.210162240821837543, 1.096913934394160517, -1.570407731631766390 ) ) ;
#171270=CARTESIAN_POINT ( 'NONE',  ( 3.737968522918270864, 2.181131050170285857, 0.2133239450496857148 ) ) ;
#171273=CARTESIAN_POINT ( 'NONE',  ( 2.162237915172473546, 1.912057200688283665, 0.04323261116381121871 ) ) ;
#171277=CARTESIAN_POINT ( 'NONE',  ( 0.5269705342763851830, -1.727990693721896287, 1.039014695730144933 ) ) ;
#171279=CARTESIAN_POINT ( 'NONE',  ( 6.620655732516649294, -0.002413161512292843602, 2.173887093218459743 ) ) ;
#171281=CARTESIAN_POINT ( 'NONE',  ( 2.696000938853719830, -1.719994558248700844, -0.1292177092697097962 ) ) ;
#171294=CARTESIAN_POINT ( 'NONE',  ( 2.877393275988342047, 0.2635569349610377143, -1.792047384982973890 ) ) ;
#171299=CARTESIAN_POINT ( 'NONE',  ( 3.668453237830204827, 0.6552377326864079476, 1.688991677562341920 ) ) ;
#171303=CARTESIAN_POINT ( 'NONE',  ( 5.564867526603252124, 1.409050971242819417, -1.215897700512589052 ) ) ;
#171305=CARTESIAN_POINT ( 'NONE',  ( 3.040549542926245241, -1.448533627684518654, 1.253585735969472648 ) ) ;
#171308=CARTESIAN_POINT ( 'NONE',  ( 6.925078400183548588, 2.417948008941684268, 2.525058136801380027 ) ) ;
#171312=CARTESIAN_POINT ( 'NONE',  ( 1.394599547902091174, 1.708230453586807585, -1.204993862942314031 ) ) ;
#171314=CARTESIAN_POINT ( 'NONE',  ( 6.352563997503644977, 0.6048113787208497794, 1.829064924511276002 ) ) ;
#171316=CARTESIAN_POINT ( 'NONE',  ( 1.940199132888191791, 1.805219978825555627, 0.2711003711317952480 ) ) ;
#171318=CARTESIAN_POINT ( 'NONE',  ( 0.9141475326900462273, -1.912571728325639153, 0.002704284578637640348 ) ) ;
#171319=CARTESIAN_POINT ( 'NONE',  ( 1.293335457286367784, -1.782033794834203766, 0.8390149815750718165 ) ) ;
#171320=CARTESIAN_POINT ( 'NONE',  ( 4.159667821157567502, 0.9185609468507827113, 1.711114809252372915 ) ) ;
#171324=CARTESIAN_POINT ( 'NONE',  ( 6.737149535461696814, -0.09068363363158969681, -1.858830251952103385 ) ) ;
#171326=CARTESIAN_POINT ( 'NONE',  ( 3.990573222356631256, -1.218298518170106925, 1.735533685479621502 ) ) ;
#171334=CARTESIAN_POINT ( 'NONE',  ( 4.353998665852670591, 1.825246345946249571, -0.04724550102237072557 ) ) ;
#171340=CARTESIAN_POINT ( 'NONE',  ( 5.032044620589739559, 0.9611010790777809731, -1.604743002217932313 ) ) ;
#171342=CARTESIAN_POINT ( 'NONE',  ( 1.629391185616009707, -1.814203104720218951, 0.6484763462606003559 ) ) ;
#171343=CARTESIAN_POINT ( 'NONE',  ( 6.596542563702321615, 1.939940506139478327, 0.2910815776849539627 ) ) ;
#171351=CARTESIAN_POINT ( 'NONE',  ( 6.421125127611838401, -1.890376142121247494, 0.9539971363903186896 ) ) ;
#171354=CARTESIAN_POINT ( 'NONE',  ( 5.084861876562203342, 1.979495018489594305, 0.6061691862097525751 ) ) ;
#171355=CARTESIAN_POINT ( 'NONE',  ( 0.2922019606856861018, 1.531309713818730822, -1.022077305420886040 ) ) ;
#171357=CARTESIAN_POINT ( 'NONE',  ( 4.975319123388493914, -2.281077821084981583, -0.2834334243917625562 ) ) ;
#171361=CARTESIAN_POINT ( 'NONE',  ( 0.8500709472824579116, 2.289359419033740295, -0.1177234237379476411 ) ) ;
#171364=CARTESIAN_POINT ( 'NONE',  ( 5.331954954513311584, 1.913531179151845674, 0.3301462080481341599 ) ) ;
#171369=CARTESIAN_POINT ( 'NONE',  ( 5.836178160628028522, -1.067892152678026951, -1.586260290404594597 ) ) ;
#171370=CARTESIAN_POINT ( 'NONE',  ( 5.823453932400854960, -1.463924103857511039, -1.387103351090559933 ) ) ;
#171374=CARTESIAN_POINT ( 'NONE',  ( 2.449268230884271702, 0.5568478702235891697, -2.015041263885499756 ) ) ;
#171375=CARTESIAN_POINT ( 'NONE',  ( 1.480939207288126669, 1.637052324538622816, -0.6731226676765161843 ) ) ;
#171379=CARTESIAN_POINT ( 'NONE',  ( 4.453268702153020620, 0.5046191974597475927, -2.235886964606835559 ) ) ;
#171380=CARTESIAN_POINT ( 'NONE',  ( 2.255425419672125287, 0.7431408456733903378, 1.573829366573131328 ) ) ;
#171383=CARTESIAN_POINT ( 'NONE',  ( 2.090756734626127766, 1.002568922338117563, -1.414341044747928766 ) ) ;
#171385=CARTESIAN_POINT ( 'NONE',  ( 1.697469458906812667, -1.344883679737416404, -1.286638954052413908 ) ) ;
#171386=CARTESIAN_POINT ( 'NONE',  ( 2.119799831544411095, 0.3726140298815834861, -2.138824928699584405 ) ) ;
#171388=CARTESIAN_POINT ( 'NONE',  ( 4.469935555517978720, -0.9463019959239076240, 1.780667052345537238 ) ) ;
#171389=CARTESIAN_POINT ( 'NONE',  ( 2.656250000000001332, -1.895863743164027504, 0.7852924748301256530 ) ) ;
#171391=CARTESIAN_POINT ( 'NONE',  ( 0.9735099972556484627, 1.857407184102148001, -0.5107058244425541904 ) ) ;
#171393=CARTESIAN_POINT ( 'NONE',  ( 4.922253396635227318, -2.210645704158546554, 0.2187456033138199529 ) ) ;
#171395=CARTESIAN_POINT ( 'NONE',  ( -0.2110808730066960626, 4.094899759311981136, -2.352064028521171135 ) ) ;
#171398=ADVANCED_FACE ( 'NONE', ( #134820 ), #118603, .T. ) ;
#171400=CARTESIAN_POINT ( 'NONE',  ( 0.1357878378635381522, -0.1024811726445598314, 2.219055157331132566 ) ) ;
#171401=CARTESIAN_POINT ( 'NONE',  ( 5.266048140081638351, -1.952571265509401854, 0.1905133553196102503 ) ) ;
#171404=CARTESIAN_POINT ( 'NONE',  ( 6.919229411136463170, -0.1667645622517479609, 2.226262756130835463 ) ) ;
#171407=CARTESIAN_POINT ( 'NONE',  ( 3.051292873657907023, 1.770411945740796966, -1.058192539780268282 ) ) ;
#171413=CARTESIAN_POINT ( 'NONE',  ( 4.516781199771729760, 1.709404882366181377, 0.7599583452636837766 ) ) ;
#171414=CARTESIAN_POINT ( 'NONE',  ( 3.515997504735939305, -1.600726479906929844, 0.6675610986628178756 ) ) ;
#171415=CARTESIAN_POINT ( 'NONE',  ( 3.878220372009810291, -0.1751146298830832670, -1.731616844506628006 ) ) ;
#171416=CARTESIAN_POINT ( 'NONE',  ( 0.4336627441306003528, -1.626622142924066594, -1.615526755278140492 ) ) ;
#171418=CARTESIAN_POINT ( 'NONE',  ( 4.985920054561153059, -2.075123007882358817, -0.2543892858761549469 ) ) ;
#171419=CARTESIAN_POINT ( 'NONE',  ( 5.349535142863500070, 1.939630122921351729, -0.09734604192479337503 ) ) ;
#171424=CARTESIAN_POINT ( 'NONE',  ( 0.8971115437808926396, -0.9091470795906559932, -1.799921601489597123 ) ) ;
#171425=CARTESIAN_POINT ( 'NONE',  ( 0.9144942500491148873, -2.120778211678171488, 0.005759991200282587286 ) ) ;
#171426=CARTESIAN_POINT ( 'NONE',  ( 6.293592298849589817, 1.492257802130890765, -1.356297202127904944 ) ) ;
#171429=CARTESIAN_POINT ( 'NONE',  ( 2.754661888675050019, 2.104750880745378083, 0.2572054321872129790 ) ) ;
#171431=CARTESIAN_POINT ( 'NONE',  ( 4.107882937833263526, -1.820653182827164596, 0.1363937739093170898 ) ) ;
#171437=CARTESIAN_POINT ( 'NONE',  ( 2.285421205933793942, 0.09476354472776055138, -2.017669629103500117 ) ) ;
#171438=CARTESIAN_POINT ( 'NONE',  ( 5.421004802376033993, 2.037064969303593820, 0.8491359902737596332 ) ) ;
#171440=CARTESIAN_POINT ( 'NONE',  ( 3.186215892106421421, 1.037744835847534741, -1.544512256342661427 ) ) ;
#171446=CARTESIAN_POINT ( 'NONE',  ( 4.564971734551386717, -1.632036996880025903, -0.8184370388232551363 ) ) ;
#171451=CARTESIAN_POINT ( 'NONE',  ( 1.000851265249177890, 1.706856028473648257, 0.3036596661522768525 ) ) ;
#171452=CARTESIAN_POINT ( 'NONE',  ( 0.3393031230796061948, 1.735299727462248587, 0.1329522994921657764 ) ) ;
#171453=CARTESIAN_POINT ( 'NONE',  ( 5.760475268203285815, 0.9300522481428794563, 2.112166060234192511 ) ) ;
#171455=CARTESIAN_POINT ( 'NONE',  ( 0.7552377862659557239, -1.739527406477459515, -1.104632168941059867 ) ) ;
#171457=CARTESIAN_POINT ( 'NONE',  ( 5.185072832991014735, -1.223605693886620438, -1.945460884747321151 ) ) ;
#171460=CARTESIAN_POINT ( 'NONE',  ( 5.893391625361731556, 1.417579469995243091, 1.220656814419220249 ) ) ;
#171462=CARTESIAN_POINT ( 'NONE',  ( 2.988426722125224977, -1.135634098421594240, 1.538566774472991616 ) ) ;
#171464=CARTESIAN_POINT ( 'NONE',  ( 5.215527394842717435, -0.3265260713646127022, 2.182469266582609091 ) ) ;
#171465=CARTESIAN_POINT ( 'NONE',  ( 4.206348283080693307, 1.299600563804912623, -1.671539989125019332 ) ) ;
#171467=CARTESIAN_POINT ( 'NONE',  ( 6.883263157960399781, 2.970623603138924818, 2.399364662246627589 ) ) ;
#171470=CARTESIAN_POINT ( 'NONE',  ( 5.567072742743464531, -1.671543079161823542, 1.304629437388994395 ) ) ;
#171471=CARTESIAN_POINT ( 'NONE',  ( 2.731810774274369802, -2.153386645068070759, 0.8298372035008163561 ) ) ;
#171472=CARTESIAN_POINT ( 'NONE',  ( 3.473055881322492322, 1.772541284497713976, 0.8411618914155660764 ) ) ;
#171474=CARTESIAN_POINT ( 'NONE',  ( 1.006607400890747295, 0.5640878064397096825, 1.878940696355746454 ) ) ;
#171478=CARTESIAN_POINT ( 'NONE',  ( 6.139861302770143858, 2.010801613648224961, -0.1531635369260639090 ) ) ;
#171481=CARTESIAN_POINT ( 'NONE',  ( 3.292005203939939229, -1.454527599200394539, -1.611992012647659900 ) ) ;
#171482=DIRECTION ( 'NONE',  ( -1.000000000000000000, 1.014813233446432150E-15, 1.972152263052529514E-31 ) ) ;
#171483=CARTESIAN_POINT ( 'NONE',  ( 0.2992908618118708675, -0.2657624787030036240, -2.103842954668332599 ) ) ;
#171488=CARTESIAN_POINT ( 'NONE',  ( 1.001328657153805146, 1.683097017759589420, 1.188813969666648873 ) ) ;
#171494=CARTESIAN_POINT ( 'NONE',  ( 3.000541214264150547, -1.884352459892328024, -0.3246530749497905655 ) ) ;
#171495=CARTESIAN_POINT ( 'NONE',  ( 5.524192064727496465, 1.051792464684684347, -1.423223091708211818 ) ) ;
#171498=CARTESIAN_POINT ( 'NONE',  ( 0.6151243592659773052, 1.481389731780102137, 1.042453732408530342 ) ) ;
#171499=CARTESIAN_POINT ( 'NONE',  ( 0.4092221944725178417, -1.818073194988058194, 0.6039046695034550050 ) ) ;
#171500=CARTESIAN_POINT ( 'NONE',  ( 2.014207461368537455, 2.064961549741591185, -0.1501100615294431728 ) ) ;
#171502=CARTESIAN_POINT ( 'NONE',  ( 6.280143113937574739, -0.9989825818290422044, 1.581392243879369053 ) ) ;
#171503=CARTESIAN_POINT ( 'NONE',  ( 2.332394550857110893, 1.770734860448031300, 0.4440693575865002907 ) ) ;
#171504=CARTESIAN_POINT ( 'NONE',  ( 5.215527394842717435, -0.3265260713646127022, 2.182469266582609091 ) ) ;
#171507=CARTESIAN_POINT ( 'NONE',  ( 3.982923569253065121, 1.957725435881779941, 0.6497275974019289801 ) ) ;
#171511=CARTESIAN_POINT ( 'NONE',  ( 0.6851285477917113953, -0.2638797801631336259, -2.145333599305146333 ) ) ;
#171512=CARTESIAN_POINT ( 'NONE',  ( 6.584440175795505112, 1.195396180001909059, -1.690200020538407566 ) ) ;
#171514=CARTESIAN_POINT ( 'NONE',  ( 4.165412764819938829, 0.2691229397190370576, -2.144731622849817221 ) ) ;
#171515=CARTESIAN_POINT ( 'NONE',  ( 4.055335607603890224, -1.756228124781366917, 0.9972510931155349478 ) ) ;
#171522=CARTESIAN_POINT ( 'NONE',  ( 2.184780103950241248, 1.616692242240840960, -1.205043568535242304 ) ) ;
#171526=CARTESIAN_POINT ( 'NONE',  ( 5.554919272666569263, 0.3793472168572444292, 1.874222000232607765 ) ) ;
#171530=CARTESIAN_POINT ( 'NONE',  ( 4.376577478760902196, -0.4445230835841383898, -1.966641233467445016 ) ) ;
#171533=CARTESIAN_POINT ( 'NONE',  ( 6.018504615762162224, 1.154743246034171555, -1.281328459571188239 ) ) ;
#171537=CARTESIAN_POINT ( 'NONE',  ( 4.481629103029507455, 1.220264704679861811, 1.417821649906551906 ) ) ;
#171539=CARTESIAN_POINT ( 'NONE',  ( 2.184514099445804547, 1.195434181571125132, -1.690031224328606196 ) ) ;
#171543=CARTESIAN_POINT ( 'NONE',  ( 0.3687678296072604556, -0.2496303596870551866, -2.000855358883571800 ) ) ;
#171551=CARTESIAN_POINT ( 'NONE',  ( 6.521099267210373363, -1.708630446951715731, 0.8662611975780337703 ) ) ;
#171558=CARTESIAN_POINT ( 'NONE',  ( 3.502937704049162715, 1.705309618848281250, -1.328393843302432931 ) ) ;
#171561=CARTESIAN_POINT ( 'NONE',  ( 0.5805319366703353134, 1.050441701016216145, 1.842106252469346339 ) ) ;
#171562=CARTESIAN_POINT ( 'NONE',  ( 5.684540951402929920, -1.781552174421060064, -0.3977488440568625605 ) ) ;
#171563=CARTESIAN_POINT ( 'NONE',  ( 1.827351761895773530, -1.857630472158870116, 0.6603073207397982536 ) ) ;
#171564=CARTESIAN_POINT ( 'NONE',  ( 5.097880177178074845, 1.288836597028759634, 1.412999258680311510 ) ) ;
#171567=CARTESIAN_POINT ( 'NONE',  ( 4.457443581450992731, 1.580467340599530424, 1.175029403372893855 ) ) ;
#171568=CARTESIAN_POINT ( 'NONE',  ( 0.5857530202744161141, -1.927162159831939503, -0.2386530530817491391 ) ) ;
#171575=CARTESIAN_POINT ( 'NONE',  ( 5.074826771331380826, -1.382354945563003312, 1.321565576914075502 ) ) ;
#171578=CARTESIAN_POINT ( 'NONE',  ( 0.7630613749609324037, -1.597064910551798667, 1.523150255686569476 ) ) ;
#171581=CARTESIAN_POINT ( 'NONE',  ( 0.02974158317493520720, -1.875378228685410376, 0.3729384364157954379 ) ) ;
#171582=CARTESIAN_POINT ( 'NONE',  ( -0.02338929933904005179, 0.7691289590099622542, -1.796825425911799723 ) ) ;
#171585=CARTESIAN_POINT ( 'NONE',  ( 2.084514231050747401, 1.193861083872927109, -1.691280048542340486 ) ) ;
#171590=CARTESIAN_POINT ( 'NONE',  ( 0.4796413896344040029, 2.016494124141111399, -0.7793912508547717888 ) ) ;
#171596=CARTESIAN_POINT ( 'NONE',  ( 4.693871744853702843, 1.512258256419211078, 0.8485452647231973566 ) ) ;
#171598=B_SPLINE_CURVE_WITH_KNOTS ( 'NONE', 3,
 ( #172090, #152627, #4214, #123429, #153705, #189391, #55134, #89793, #187255, #41034 ),
 .UNSPECIFIED., .F., .F.,
 ( 4, 1, 1, 1, 1, 1, 1, 4 ),
 ( 0.000000000000000000, 0.09705918685507786137, 0.1907419858981972138, 0.2602182418918835838, 0.3625179829595637226, 0.5215049497019805802, 0.7338397267804015467, 1.000000000000000000 ),
 .UNSPECIFIED. ) ;
#171600=CARTESIAN_POINT ( 'NONE',  ( 2.711853232431875593, 0.5564382603544039130, -1.993978196652478996 ) ) ;
#171601=CARTESIAN_POINT ( 'NONE',  ( 4.693022120063472080, 1.842747525957793009, 1.042402977009656340 ) ) ;
#171604=CARTESIAN_POINT ( 'NONE',  ( 2.131642331222316500, 1.886095724437972798, -0.5669754052412961931 ) ) ;
#171607=CARTESIAN_POINT ( 'NONE',  ( 5.068466688948791266, -2.157128183272677191, -0.7757897288535390290 ) ) ;
#171608=CARTESIAN_POINT ( 'NONE',  ( 1.347985785199314668, 1.823511463271022093, 0.09156768404049858701 ) ) ;
#171614=CARTESIAN_POINT ( 'NONE',  ( 2.988542084594744797, -1.195720007494217585, 1.619529446093708636 ) ) ;
#171615=CARTESIAN_POINT ( 'NONE',  ( 2.869914117416060062, -1.941089286637355693, 0.2830422620509198128 ) ) ;
#171619=CARTESIAN_POINT ( 'NONE',  ( 5.947236541613409422, 0.6080794538029854479, -2.000250932508009782 ) ) ;
#171620=CARTESIAN_POINT ( 'NONE',  ( 4.504631171302628800, 1.367295333670435653, -1.123774403194759408 ) ) ;
#171622=CARTESIAN_POINT ( 'NONE',  ( 0.9553299046189435151, 0.4242123182428610972, -2.149831459026855907 ) ) ;
#171623=CARTESIAN_POINT ( 'NONE',  ( 5.701030997009290502, -0.4167664840721523878, 1.689554919747728423 ) ) ;
#171626=CARTESIAN_POINT ( 'NONE',  ( 0.1405533004714097089, -0.003749010675423158478, -2.279853246149381452 ) ) ;
#171628=CARTESIAN_POINT ( 'NONE',  ( 5.413366682498521598, 0.5056653987138818307, 1.658472451074376242 ) ) ;
#171629=CARTESIAN_POINT ( 'NONE',  ( 1.893488989520499377, 1.919108310403025985, -1.089527612406354873 ) ) ;
#171630=CARTESIAN_POINT ( 'NONE',  ( 5.529782829607038153, 2.093976201882574273, -0.5736635526294631138 ) ) ;
#171631=CARTESIAN_POINT ( 'NONE',  ( 1.095081093118466908, 1.870138624552514006, 0.9927810678921239473 ) ) ;
#171632=CARTESIAN_POINT ( 'NONE',  ( 2.937500000000001776, 1.451031289060998430, -1.451031289061236018 ) ) ;
#171633=CARTESIAN_POINT ( 'NONE',  ( 6.727182134110201162, 1.237345558575110083, 2.302850971298702198 ) ) ;
#171634=CARTESIAN_POINT ( 'NONE',  ( 4.612281621929555264, -0.8233390244782293754, -1.741700550419862825 ) ) ;
#171635=CARTESIAN_POINT ( 'NONE',  ( 0.7686061912218185022, 2.218469807834182017, -0.1147041126551024554 ) ) ;
#171637=CARTESIAN_POINT ( 'NONE',  ( 1.294905083876269236, 1.870644729521577565, -1.324771388537665961 ) ) ;
#171641=CARTESIAN_POINT ( 'NONE',  ( 4.266425542637849233, 2.220793247050854902, -0.05466516159106404871 ) ) ;
#171647=CARTESIAN_POINT ( 'NONE',  ( 2.285779929129946098, 1.617817622347239803, -1.203354541732377658 ) ) ;
#171649=CARTESIAN_POINT ( 'NONE',  ( 6.303195905902406970, -1.744534168554587872, 1.100284471152054300 ) ) ;
#171651=CARTESIAN_POINT ( 'NONE',  ( 6.304260172732157663, 1.282988983046409848, -1.176258868317042294 ) ) ;
#171654=CARTESIAN_POINT ( 'NONE',  ( 1.141466271755723794, 0.7239738643088615699, -1.615086939138086652 ) ) ;
#171655=CARTESIAN_POINT ( 'NONE',  ( 0.1588275700346117869, 1.163271727376416376, 1.646837250247008777 ) ) ;
#171656=CARTESIAN_POINT ( 'NONE',  ( 0.1691535571452691677, 1.059206136818511501, 1.505872603892892458 ) ) ;
#171657=CARTESIAN_POINT ( 'NONE',  ( 4.511445251964079084, -2.248337965441957742, 0.4463705457610280258 ) ) ;
#171658=CARTESIAN_POINT ( 'NONE',  ( 3.116968920156853340, -1.774181764490849522, 0.4917334186493869108 ) ) ;
#171662=CARTESIAN_POINT ( 'NONE',  ( 2.678497062878131718, -1.746332412481563567, -0.5319975912557314279 ) ) ;
#171663=CARTESIAN_POINT ( 'NONE',  ( 3.885388821667290493, -0.6351983117205138862, -1.913803978180687482 ) ) ;
#171665=CARTESIAN_POINT ( 'NONE',  ( 3.837032359523879332, 0.3291597691741187104, 2.238327980419333674 ) ) ;
#171667=CARTESIAN_POINT ( 'NONE',  ( 5.350649881110917327, 0.6085095821539068250, 2.016136239840255140 ) ) ;
#171668=CARTESIAN_POINT ( 'NONE',  ( 3.947765587739564097, 1.497496809916948779, 1.429883829622953462 ) ) ;
#171671=CARTESIAN_POINT ( 'NONE',  ( 5.760427271636393343, 2.118038551301495875, 0.1041057254967461404 ) ) ;
#171675=CARTESIAN_POINT ( 'NONE',  ( 1.312975575179779586, 1.698600376263710743, 0.9089255565387382996 ) ) ;
#171682=CARTESIAN_POINT ( 'NONE',  ( 0.5807245924134795123, 1.101748585799481095, 1.928910967146231004 ) ) ;
#171683=CARTESIAN_POINT ( 'NONE',  ( 2.151528103076968179, -1.690815887601760270, -1.255243123012689921 ) ) ;
#171686=CARTESIAN_POINT ( 'NONE',  ( 6.930517489306616596, -1.145039166549733922, 1.467359839328785664 ) ) ;
#171694=CARTESIAN_POINT ( 'NONE',  ( 3.437899435096212208, 1.242623406730450908, 1.518177208742684803 ) ) ;
#171695=CARTESIAN_POINT ( 'NONE',  ( 2.694378501574711926, -2.155843008138720762, -0.1600555415394027403 ) ) ;
#171696=CARTESIAN_POINT ( 'NONE',  ( 1.135996871135702024, 0.3593859243370273182, 1.805655672011026391 ) ) ;
#171699=CARTESIAN_POINT ( 'NONE',  ( 3.609068157710407565, -1.714216318138677808, 0.2993142247325294991 ) ) ;
#171703=CARTESIAN_POINT ( 'NONE',  ( 1.094844843509492183, -0.5259716649698794599, -2.096624219460433647 ) ) ;
#171705=CARTESIAN_POINT ( 'NONE',  ( 3.901720107437017582, 0.2930258228103881923, 1.994564303527603499 ) ) ;
#171707=CARTESIAN_POINT ( 'NONE',  ( 0.5851287433712646369, -0.2658872486876809327, -2.145209338178376335 ) ) ;
#171708=CARTESIAN_POINT ( 'NONE',  ( 2.535955197907293179, 0.9309914139831111379, -1.737806310995954728 ) ) ;
#171710=CARTESIAN_POINT ( 'NONE',  ( 6.509000000000048303, 2.074227158855263209, 2.209070705210983032 ) ) ;
#171711=CARTESIAN_POINT ( 'NONE',  ( 2.313922598539425390, 1.266723153581908567, -1.472183398282415956 ) ) ;
#171712=CARTESIAN_POINT ( 'NONE',  ( 0.2331563151865486683, 0.005903526429595904942, -1.945944850731482934 ) ) ;
#171715=CARTESIAN_POINT ( 'NONE',  ( -0.1108833634137010304, 6.948331553507800962, -2.491992042620773340 ) ) ;
#171720=CARTESIAN_POINT ( 'NONE',  ( 5.333197341169245043, 0.1633263742753125747, 2.301865194068336784 ) ) ;
#171722=CARTESIAN_POINT ( 'NONE',  ( 4.346505277090593644, -1.939800950321630690, -0.2920161945778113055 ) ) ;
#171724=CARTESIAN_POINT ( 'NONE',  ( 0.7037502660087076034, 1.864169469917423161, 0.7691187473759173443 ) ) ;
#171726=CARTESIAN_POINT ( 'NONE',  ( 2.009133639091817525, 0.005444305534021975056, 2.117513411327852868 ) ) ;
#171730=CARTESIAN_POINT ( 'NONE',  ( 3.081803158279991628, -1.813988701161291628, -0.3140598505507880556 ) ) ;
#171734=CARTESIAN_POINT ( 'NONE',  ( 3.656581996618038843, 2.110704406498860486, 0.2042969539849878724 ) ) ;
#171735=CARTESIAN_POINT ( 'NONE',  ( 0.1285073612291263989, -1.684675954457705682, 0.7431698939026829542 ) ) ;
#171739=CARTESIAN_POINT ( 'NONE',  ( 3.971991334398959239, 1.141669855754149365, 1.715422085859653833 ) ) ;
#171741=CARTESIAN_POINT ( 'NONE',  ( 1.645803748337611783, 0.5784278848013635344, 1.748079663633335334 ) ) ;
#171747=CARTESIAN_POINT ( 'NONE',  ( 1.418904949497600487, 1.480075412272121582, -1.637148382315711359 ) ) ;
#171748=CARTESIAN_POINT ( 'NONE',  ( 3.655803326253406649, 0.5538646471104657909, -2.193435612772106413 ) ) ;
#171750=CARTESIAN_POINT ( 'NONE',  ( 3.410248120744460376, -1.809760825414870267, -0.08362741940017533182 ) ) ;
#171752=CARTESIAN_POINT ( 'NONE',  ( 4.417137112658839015, -1.749089155124187389, 0.7819188135024003339 ) ) ;
#171753=CARTESIAN_POINT ( 'NONE',  ( 4.914543119725925280, 0.7892175071393169317, 1.914236960262293508 ) ) ;
#171756=CARTESIAN_POINT ( 'NONE',  ( 3.239098446765543482, -1.739280071990648935, 0.9281937050133574063 ) ) ;
#171757=CARTESIAN_POINT ( 'NONE',  ( 1.606340841434449329, -0.6908775452558654218, -1.798418176235560662 ) ) ;
#171758=CARTESIAN_POINT ( 'NONE',  ( 4.346470048663173102, 0.4987854378066917116, 1.802870001028591407 ) ) ;
#171759=CARTESIAN_POINT ( 'NONE',  ( 2.965757426574578304, 0.3381026970978153745, -2.282680038778000853 ) ) ;
#171760=CARTESIAN_POINT ( 'NONE',  ( 3.191705266286504639, -1.248028223939607884, -1.380750640708436006 ) ) ;
#171765=CARTESIAN_POINT ( 'NONE',  ( 0.5574226275508349371, -1.780365264567655759, -1.124781644112993417 ) ) ;
#171769=CARTESIAN_POINT ( 'NONE',  ( 1.881254504445781794, -1.940830296247602949, -0.8548571619346673200 ) ) ;
#171771=CARTESIAN_POINT ( 'NONE',  ( 0.6858141477139628739, 1.945346236745447488, -0.5429362378739016615 ) ) ;
#171777=CARTESIAN_POINT ( 'NONE',  ( 1.247603677004164746, -1.703183937513498281, -1.330886036463780009 ) ) ;
#171780=CARTESIAN_POINT ( 'NONE',  ( 6.925078400183553917, 6.038071034253152725, 2.450556290382682523 ) ) ;
#171783=CARTESIAN_POINT ( 'NONE',  ( 5.911342272548038679, -1.897112096406332382, 0.6839327336411115121 ) ) ;
#171785=CARTESIAN_POINT ( 'NONE',  ( 0.09952931447375359952, -0.5783855404800625211, 2.113812074898171023 ) ) ;
#171787=CARTESIAN_POINT ( 'NONE',  ( 6.789893189004300389, -0.9291300992274166282, 1.949920244826188309 ) ) ;
#171791=CARTESIAN_POINT ( 'NONE',  ( 1.106889576528688801, -0.04550283046177550778, 1.915226712711289636 ) ) ;
#171796=CARTESIAN_POINT ( 'NONE',  ( 3.193694537771115449, -0.6981934656059236577, 1.577442374586303320 ) ) ;
#171798=CARTESIAN_POINT ( 'NONE',  ( 2.547821756505376012, 1.769265940657601011, 0.04812675368598590825 ) ) ;
#171801=CARTESIAN_POINT ( 'NONE',  ( 5.192482782645277517, -2.189556457885518892, -0.2746672974567528347 ) ) ;
#171803=CARTESIAN_POINT ( 'NONE',  ( 4.394789018838915595, -1.960137222954833502, -0.4867870608649630393 ) ) ;
#171805=CARTESIAN_POINT ( 'NONE',  ( 4.125719030757846184, -0.3612518283466863434, 2.089324717668067599 ) ) ;
#171806=CARTESIAN_POINT ( 'NONE',  ( 3.884388800492278193, -0.6352171928143932611, -1.913798906059568594 ) ) ;
#171807=CARTESIAN_POINT ( 'NONE',  ( 4.166123871162411341, 1.811061351045451850, -0.05074819156030555695 ) ) ;
#171812=CARTESIAN_POINT ( 'NONE',  ( 1.164687902950040321, -1.689591380799923215, -0.8031939614948148121 ) ) ;
#171814=CARTESIAN_POINT ( 'NONE',  ( 6.164714480961021259, 0.5753438643430182076, 1.717747506070513852 ) ) ;
#171823=CARTESIAN_POINT ( 'NONE',  ( 4.377262645480927361, -1.895543854172193399, -0.9507902649282941043 ) ) ;
#171824=CARTESIAN_POINT ( 'NONE',  ( -0.1296875068448125057, 2.889142263448498227, -2.315371602238533555 ) ) ;
#171826=CARTESIAN_POINT ( 'NONE',  ( 5.378184286887115029, -1.097432272127541131, 1.637457850930480241 ) ) ;
#171828=CARTESIAN_POINT ( 'NONE',  ( 1.054940647564650336, 0.3968280277809080880, 1.973547778087578308 ) ) ;
#171831=CARTESIAN_POINT ( 'NONE',  ( 6.438674896094000566, -1.635394517905249145, 1.344423162301669361 ) ) ;
#171833=CARTESIAN_POINT ( 'NONE',  ( 1.803268859043684058, -1.750145871244257467, 1.105767233283899920 ) ) ;
#171837=CARTESIAN_POINT ( 'NONE',  ( 4.207035958355084482, -0.3574298538902004885, 2.059684413417623094 ) ) ;
#171840=CARTESIAN_POINT ( 'NONE',  ( 2.766400663125650361, -1.260407102598060103, 1.320874842943790872 ) ) ;
#171841=CARTESIAN_POINT ( 'NONE',  ( 2.103910407274149907, -0.7736040573625382333, 1.638098421638082947 ) ) ;
#171843=CARTESIAN_POINT ( 'NONE',  ( 6.721333373144884327, -0.1645177889858795151, 2.170883633896856679 ) ) ;
#171845=CARTESIAN_POINT ( 'NONE',  ( 4.313639225654395837, -0.3805011380913872476, 2.173570407251995018 ) ) ;
#171848=CARTESIAN_POINT ( 'NONE',  ( 2.525908831824146716, -1.891188341833284881, 0.2824699455093656053 ) ) ;
#171850=CARTESIAN_POINT ( 'NONE',  ( 6.654741963219191980, -0.5482099483974657295, -1.996413779700876079 ) ) ;
#171852=CARTESIAN_POINT ( 'NONE',  ( 6.163654587501778970, 1.125051486859941718, 1.880622087419632882 ) ) ;
#171857=CARTESIAN_POINT ( 'NONE',  ( -0.02319159430947368566, 6.948789054712430691, -2.406029888528108618 ) ) ;
#171863=CARTESIAN_POINT ( 'NONE',  ( 5.928598010555855780, -1.317819122799672504, 1.596621505246295314 ) ) ;
#171864=CARTESIAN_POINT ( 'NONE',  ( 4.529859951405730278, -1.186268397688082343, -1.517871513682719886 ) ) ;
#171865=CARTESIAN_POINT ( 'NONE',  ( 1.177361486786612899, 1.528755565978222819, 1.314981834344926437 ) ) ;
#171869=CARTESIAN_POINT ( 'NONE',  ( 1.447511513890851864, 0.6336015447323711802, -2.097855558553712196 ) ) ;
#171870=CARTESIAN_POINT ( 'NONE',  ( 5.197797600609998625, -0.6536857159176562293, 1.704833070275885598 ) ) ;
#171879=CARTESIAN_POINT ( 'NONE',  ( 2.630204301513817455, 0.2276190002089127917, 1.827071974840013269 ) ) ;
#171880=CARTESIAN_POINT ( 'NONE',  ( 5.765890645310551399, 0.5801508929094216782, -1.927831218222434195 ) ) ;
#171881=CARTESIAN_POINT ( 'NONE',  ( 2.425563141628499064, 0.9819131520533967983, 2.078181775667542475 ) ) ;
#171882=CARTESIAN_POINT ( 'NONE',  ( 0.3208626164478335374, -1.658663274457260473, -0.8439677346868018626 ) ) ;
#171885=CARTESIAN_POINT ( 'NONE',  ( 3.902528505893249733, -1.892296425594198750, -0.2755589300712790735 ) ) ;
#171887=CARTESIAN_POINT ( 'NONE',  ( 0.6958625912084138720, -1.462932864358768459, -1.465259690088885014 ) ) ;
#171889=CARTESIAN_POINT ( 'NONE',  ( 3.087527064991796077, -0.8449906179068911172, 1.912563079267016297 ) ) ;
#171890=CARTESIAN_POINT ( 'NONE',  ( 1.322894217037654085, -0.04941562205608432401, 1.870173573632450958 ) ) ;
#171891=CARTESIAN_POINT ( 'NONE',  ( 2.495470048217228065, 1.954872899240958972, 0.4925676099705801891 ) ) ;
#171895=CARTESIAN_POINT ( 'NONE',  ( 3.016877700344788416, -1.676514204431644783, 0.4670218299706177523 ) ) ;
#171898=CARTESIAN_POINT ( 'NONE',  ( 2.508071618744921238, -0.6595455166902574051, -1.594007932167235131 ) ) ;
#171899=CARTESIAN_POINT ( 'NONE',  ( 2.648187065138879692, 0.7411268365287645432, 2.062558662443473523 ) ) ;
#171900=CARTESIAN_POINT ( 'NONE',  ( 4.934293700819583073, 1.136511309699510308, -1.891595316245115788 ) ) ;
#171904=CARTESIAN_POINT ( 'NONE',  ( 4.047858276791187038, 1.568658707867241819, 1.501164901757213288 ) ) ;
#171905=CARTESIAN_POINT ( 'NONE',  ( 2.226930044512597906, -0.0006860120723567450030, 1.825872481329051222 ) ) ;
#171907=CARTESIAN_POINT ( 'NONE',  ( 4.874263506423556436, -2.101702868649154343, -0.2561063476108938475 ) ) ;
#171908=CARTESIAN_POINT ( 'NONE',  ( 6.639320575229239019, 3.696696400505532942, 2.511109302898812956 ) ) ;
#171910=CARTESIAN_POINT ( 'NONE',  ( 4.933284685991359275, -1.619851263076008019, -1.622297632854825755 ) ) ;
#171915=CARTESIAN_POINT ( 'NONE',  ( -0.02259406399240069044, -1.896172633340575064, -0.9493637518730788649 ) ) ;
#171919=CARTESIAN_POINT ( 'NONE',  ( 6.825078400183553384, 0.5907600490881077526, 1.908621492364571903 ) ) ;
#171921=CARTESIAN_POINT ( 'NONE',  ( 5.625625018759272677, 0.3960990390993284205, 1.976956468877195894 ) ) ;
#171923=CARTESIAN_POINT ( 'NONE',  ( 3.204023084367659813, 0.7466497159868844546, -1.922840047214324333 ) ) ;
#171925=CARTESIAN_POINT ( 'NONE',  ( -0.1409997244345879974, 2.021982482314553131, -2.415666835770650778 ) ) ;
#171930=CARTESIAN_POINT ( 'NONE',  ( 5.824229312739954700, 2.111140916326431416, 0.5876101183235474812 ) ) ;
#171931=CARTESIAN_POINT ( 'NONE',  ( 3.147111449167848019, 0.9091449406319618287, 1.799922684605055556 ) ) ;
#171932=CARTESIAN_POINT ( 'NONE',  ( 3.227900028218867234, 1.797025815167479390, 0.4004103908350764573 ) ) ;
#171937=CARTESIAN_POINT ( 'NONE',  ( 6.563509198815889789, 0.3086105522638156184, -1.799150958419073909 ) ) ;
#171939=CARTESIAN_POINT ( 'NONE',  ( 6.561402770032070286, 0.3947617697056918784, -2.227681008968500631 ) ) ;
#171940=CARTESIAN_POINT ( 'NONE',  ( 1.664816323125760889, -1.488367931135538891, 1.490329786196037398 ) ) ;
#171950=CARTESIAN_POINT ( 'NONE',  ( 4.359788498249434596, -1.718402401499378840, -1.407797849641032828 ) ) ;
#171951=CARTESIAN_POINT ( 'NONE',  ( 2.589988673929614738, -2.185656584452956075, -0.1600571409424780822 ) ) ;
#171953=CARTESIAN_POINT ( 'NONE',  ( 6.883263157960373135, 2.058310207169287143, 2.252834201749584153 ) ) ;
#171955=CARTESIAN_POINT ( 'NONE',  ( 5.898874287966751950, 0.3812104124719677412, 1.924297140916144233 ) ) ;
#171961=CARTESIAN_POINT ( 'NONE',  ( 4.517907016363444939, -0.5628432189327194912, 2.044499502628312371 ) ) ;
#171964=CARTESIAN_POINT ( 'NONE',  ( 5.735289742212391850, -1.956171686333206816, 0.9202595734885756773 ) ) ;
#171966=CARTESIAN_POINT ( 'NONE',  ( 4.563899478665734755, -1.199029595066217313, 1.397436126395680267 ) ) ;
#171969=CARTESIAN_POINT ( 'NONE',  ( 0.3623613221122607420, 0.1732436440316066917, -1.731762550003753898 ) ) ;
#171970=CARTESIAN_POINT ( 'NONE',  ( 6.727182134110207379, 6.038252846411742425, 2.505853901327475874 ) ) ;
#171973=CARTESIAN_POINT ( 'NONE',  ( 4.434552454296070145, 2.119417814153037316, 0.4246342833542292028 ) ) ;
#171976=CARTESIAN_POINT ( 'NONE',  ( 6.309922681198771421, -1.704675833164914778, 1.076154833852351000 ) ) ;
#171978=CARTESIAN_POINT ( 'NONE',  ( 2.958072429731006370, 2.151414462573512765, -0.2105227563667099733 ) ) ;
#171979=CARTESIAN_POINT ( 'NONE',  ( 4.358636338273668365, -1.462950666040288006, 1.321578431016472654 ) ) ;
#171980=CARTESIAN_POINT ( 'NONE',  ( 3.725721709451996322, -1.528540617003815383, -0.8183948105100163906 ) ) ;
#171981=CARTESIAN_POINT ( 'NONE',  ( 0.7674258922165803076, 2.110627382301712540, -0.5898035449652739848 ) ) ;
#171982=CARTESIAN_POINT ( 'NONE',  ( 0.9566253870459644482, 2.304745586553739400, -0.1165920040033379956 ) ) ;
#171983=CARTESIAN_POINT ( 'NONE',  ( 3.831368270176987334, -1.905513148489059283, 0.7852520889023787420 ) ) ;
#171984=CARTESIAN_POINT ( 'NONE',  ( 6.058146487192490603, -1.370253782545840293, 1.376481248621561182 ) ) ;
#171992=CARTESIAN_POINT ( 'NONE',  ( 3.452368941479638131, 2.206952907609287973, 0.002057427529567057434 ) ) ;
#171994=ORIENTED_EDGE ( 'NONE', *, *, #183399, .T. ) ;
#171995=CARTESIAN_POINT ( 'NONE',  ( 1.023987020198445341, 0.9106972337104453086, 1.622782493823480943 ) ) ;
#171996=CARTESIAN_POINT ( 'NONE',  ( -0.02919842301641033255, 0.7163969788333038879, -2.157531187298274311 ) ) ;
#172002=CARTESIAN_POINT ( 'NONE',  ( 6.122987604524110949, -1.732013368603693593, 0.6248225064409973495 ) ) ;
#172004=CARTESIAN_POINT ( 'NONE',  ( 2.465760480296646850, 2.021364445465044124, -0.4007626210408669620 ) ) ;
#172009=CARTESIAN_POINT ( 'NONE',  ( 1.182575006203628210, -2.010449142642761089, -0.4523898644508434486 ) ) ;
#172011=CARTESIAN_POINT ( 'NONE',  ( 5.179192671508887180, 1.240781939916297372, 1.360553736468192554 ) ) ;
#172016=CARTESIAN_POINT ( 'NONE',  ( 4.002700589841681200, -0.6913439845411989415, -2.095861086919461602 ) ) ;
#172017=CARTESIAN_POINT ( 'NONE',  ( 6.714178486276241919, -1.057601618853749148, -1.999996817866441123 ) ) ;
#172019=CARTESIAN_POINT ( 'NONE',  ( 0.3340484552533556362, -1.024938778295768849, -1.614363347046356756 ) ) ;
#172020=CARTESIAN_POINT ( 'NONE',  ( 0.8840003597419334724, -2.016708404047353742, 0.004841148455551891328 ) ) ;
#172025=CARTESIAN_POINT ( 'NONE',  ( 2.131529507118444133, -1.219933349377068099, -1.418231869465089057 ) ) ;
#172027=CARTESIAN_POINT ( 'NONE',  ( 2.430875351317234756, -1.673853735218135741, 1.124246214196801485 ) ) ;
#172029=CARTESIAN_POINT ( 'NONE',  ( 6.639320575229257670, 3.688898292602959650, 2.617366112374151399 ) ) ;
#172032=CARTESIAN_POINT ( 'NONE',  ( 4.740906146847382985, 0.3592350385927112200, 2.075039481041524247 ) ) ;
#172037=CARTESIAN_POINT ( 'NONE',  ( 4.482678814652188315, -1.316266026504675057, 1.532109124154117596 ) ) ;
#172039=CARTESIAN_POINT ( 'NONE',  ( 6.584441931359013900, 1.190761153509769521, -1.684076666428784064 ) ) ;
#172041=CARTESIAN_POINT ( 'NONE',  ( 4.622454487542248636, 1.333869025858843704, -1.700861402727947391 ) ) ;
#172047=CARTESIAN_POINT ( 'NONE',  ( 2.401036581340802556, 0.4739146800750834165, 2.118683212603386767 ) ) ;
#172050=CARTESIAN_POINT ( 'NONE',  ( 1.329379181053941483, 0.9071106928158387817, -1.602193565413398968 ) ) ;
#172052=CARTESIAN_POINT ( 'NONE',  ( 2.700927432832851860, 1.852951201923001223, 1.169960570980829839 ) ) ;
#172054=CARTESIAN_POINT ( 'NONE',  ( 3.626065245518626412, -1.345661663401491293, -1.818709669598504997 ) ) ;
#172060=CARTESIAN_POINT ( 'NONE',  ( 5.132005351226563761, 0.9095619001311354701, -1.517971549226182715 ) ) ;
#172063=CARTESIAN_POINT ( 'NONE',  ( 1.905437291041052195, 1.750494195096408800, 1.170504954829422850 ) ) ;
#172066=CARTESIAN_POINT ( 'NONE',  ( 0.8011416495431540330, -1.691081937322042483, 1.009368880822520298 ) ) ;
#172068=CARTESIAN_POINT ( 'NONE',  ( 0.1390251588108057101, -0.1389306544097475005, -1.930426113910483688 ) ) ;
#172069=CARTESIAN_POINT ( 'NONE',  ( 5.361500737056818622, -1.433101695931580100, -1.108104203189824277 ) ) ;
#172074=CARTESIAN_POINT ( 'NONE',  ( 4.750782166719051069, -1.502237938222051650, 1.114538048626475986 ) ) ;
#172076=CARTESIAN_POINT ( 'NONE',  ( 4.364170320198999420, -2.065056620294950740, 0.1471644388686063065 ) ) ;
#172086=CARTESIAN_POINT ( 'NONE',  ( 5.248475795274027078, -1.946838731704622072, -0.2419367024937419397 ) ) ;
#172088=CARTESIAN_POINT ( 'NONE',  ( 1.792342068719571468, -1.899328565777322231, 0.6766080823841430503 ) ) ;
#172090=CARTESIAN_POINT ( 'NONE',  ( -0.1108833634136767443, 0.0002062650063822807356, -1.896853557917008271 ) ) ;
#172091=CARTESIAN_POINT ( 'NONE',  ( 6.639320575229276322, 3.701785489019034259, 2.411212692025939131 ) ) ;
#172092=CARTESIAN_POINT ( 'NONE',  ( 6.539320575229249144, 0.007148032025052972194, 1.896977914940492393 ) ) ;
#172093=CARTESIAN_POINT ( 'NONE',  ( 2.055717040066493695, 1.865871300129381183, -0.1328275987748789300 ) ) ;
#172097=CARTESIAN_POINT ( 'NONE',  ( 2.900141384978659698, -1.046112932010187624, -1.840686247649555796 ) ) ;
#172099=CARTESIAN_POINT ( 'NONE',  ( 4.791501694037465953, -1.894250426384593844, 0.8359921707915063394 ) ) ;
#172101=CARTESIAN_POINT ( 'NONE',  ( 1.593426000515285157, -0.7013512306414200204, 1.969750900790192549 ) ) ;
#172102=CARTESIAN_POINT ( 'NONE',  ( 6.620655732516668834, 6.034240673559561507, 2.768629221164942145 ) ) ;
#172103=CARTESIAN_POINT ( 'NONE',  ( 6.352569596097208837, 0.5757234290239590102, 1.732508359437078482 ) ) ;
#172111=CARTESIAN_POINT ( 'NONE',  ( 6.006500814222540008, -1.903516144586704151, -0.1827706444143817055 ) ) ;
#172119=CARTESIAN_POINT ( 'NONE',  ( 5.747672784407955149, 1.986098415631059932, -0.3474865836668520336 ) ) ;
#172122=CARTESIAN_POINT ( 'NONE',  ( 0.1399997263885795484, 5.723012109828673921, -2.593777676649943409 ) ) ;
#172125=CARTESIAN_POINT ( 'NONE',  ( 3.590635625024854338, 1.920399590389043620, 0.4359694148904534328 ) ) ;
#172126=CARTESIAN_POINT ( 'NONE',  ( 4.939077454563308933, -1.704950310733845065, -1.076300583479961048 ) ) ;
#172128=FACE_OUTER_BOUND ( 'NONE', #32655, .T. ) ;
#172129=CARTESIAN_POINT ( 'NONE',  ( 5.085950966588184130, -2.174626929279792176, -0.2704268894557353975 ) ) ;
#172131=CARTESIAN_POINT ( 'NONE',  ( 2.907156789938716290, 1.626457378340099069, 1.032021673995666911 ) ) ;
#172133=CARTESIAN_POINT ( 'NONE',  ( -0.02948999725182511675, 6.948707995275583471, -2.521364601437687369 ) ) ;
#172134=CARTESIAN_POINT ( 'NONE',  ( 0.1357705729100426029, -2.015811560716780360, 0.8986578214904349382 ) ) ;
#172143=CARTESIAN_POINT ( 'NONE',  ( 6.444863656277017405, -1.483217659742748218, -1.090817886357238198 ) ) ;
#172144=CARTESIAN_POINT ( 'NONE',  ( 2.490887342608373078, -1.927107516443892221, -0.5821121120333644372 ) ) ;
#172145=CARTESIAN_POINT ( 'NONE',  ( 4.903846967696810388, 0.3865712588492843937, 2.265520236764162920 ) ) ;
#172147=CARTESIAN_POINT ( 'NONE',  ( 2.975287861635074194, -0.1872683251897942214, 1.851525965346143554 ) ) ;
#172150=CARTESIAN_POINT ( 'NONE',  ( 6.187759705938407073, 1.828009178079874841, -0.5617473972939349691 ) ) ;
#172153=CARTESIAN_POINT ( 'NONE',  ( 6.462449937854951365, -1.911777437574797345, -0.8467615847161328313 ) ) ;
#172158=CARTESIAN_POINT ( 'NONE',  ( 6.674431755534494748, -1.054235620458108702, 1.365612558063566073 ) ) ;
#172160=CARTESIAN_POINT ( 'NONE',  ( 2.092031233620697872, -0.3790036544207425195, 1.692025817237676311 ) ) ;
#172166=CARTESIAN_POINT ( 'NONE',  ( 0.3036855567021545244, -1.598042064648269811, -1.315789336611736138 ) ) ;
#172167=CARTESIAN_POINT ( 'NONE',  ( 5.795480788678070816, 1.385457615097264394, 1.189071861804301466 ) ) ;
#172168=CARTESIAN_POINT ( 'NONE',  ( 2.940231979924610606, -1.012623612260230566, 1.680088604585870060 ) ) ;
#172172=CARTESIAN_POINT ( 'NONE',  ( 3.580828998445852562, -1.422877522674294681, 1.572404880189558485 ) ) ;
#172177=CARTESIAN_POINT ( 'NONE',  ( 1.727480438796034745, 0.1563249218069600044, -2.064440809470533544 ) ) ;
#172180=CARTESIAN_POINT ( 'NONE',  ( 4.055513949679364849, -1.932427950605047018, 1.095304516859375799 ) ) ;
#172182=CARTESIAN_POINT ( 'NONE',  ( 1.706133075696044221, 2.146806223983906747, 0.8221538945956968769 ) ) ;
#172184=CARTESIAN_POINT ( 'NONE',  ( 6.737180511075488987, -0.09540316190201691970, -2.060463472160603882 ) ) ;
#172191=CARTESIAN_POINT ( 'NONE',  ( 3.006014587165442453, -0.7710369221427433306, 1.750240277048662030 ) ) ;
#172192=CARTESIAN_POINT ( 'NONE',  ( -0.2104748580754183529, 0.2283854016844401591, -2.137091067173245929 ) ) ;
#172193=CARTESIAN_POINT ( 'NONE',  ( 4.647282941162062642, -1.334376716645750971, -1.092789356466111972 ) ) ;
#172194=CARTESIAN_POINT ( 'NONE',  ( 2.518767860054324625, 0.2516336668320385828, 2.000731427934741902 ) ) ;
#172195=CARTESIAN_POINT ( 'NONE',  ( 4.342621253679892490, 0.5038326875656545800, -2.242679570940506739 ) ) ;
#172196=CARTESIAN_POINT ( 'NONE',  ( 3.690934243623856581, -0.4369955660583099699, -2.219648300357620396 ) ) ;
#172197=CARTESIAN_POINT ( 'NONE',  ( 5.901026713257129686, 1.722607154707327615, -1.211383145191318400 ) ) ;
#172199=CARTESIAN_POINT ( 'NONE',  ( 4.956192180792302615, 0.6771475221719803761, 1.635265836519818716 ) ) ;
#172202=CARTESIAN_POINT ( 'NONE',  ( 0.4984804791418595560, -0.7777643670432095035, -2.156416217022334436 ) ) ;
#172203=CARTESIAN_POINT ( 'NONE',  ( 5.964778383650899407, 0.1308802983275309528, -1.836551591404868233 ) ) ;
#172205=CARTESIAN_POINT ( 'NONE',  ( 6.193348084369689310, -0.7418380161853587174, 2.062208804312585020 ) ) ;
#172208=CARTESIAN_POINT ( 'NONE',  ( 5.723117673755029777, -1.870111591731966616, -0.8886290660751752224 ) ) ;
#172209=CARTESIAN_POINT ( 'NONE',  ( 0.5500180045474002410, 0.9981291480291035745, 1.752136972055001518 ) ) ;
#172212=CARTESIAN_POINT ( 'NONE',  ( 4.846275584324886587, 1.921458954407113451, 0.1401587531122197583 ) ) ;
#172215=CARTESIAN_POINT ( 'NONE',  ( 1.582608957317205522, 1.147345939325004283, 1.902073548153013327 ) ) ;
#172225=CARTESIAN_POINT ( 'NONE',  ( 1.469116868872882398, 1.728625619535430369, 0.9278086228877155950 ) ) ;
#172228=CARTESIAN_POINT ( 'NONE',  ( 6.830524215763060347, -1.208013408316032322, 1.546442907991877558 ) ) ;
#172232=CARTESIAN_POINT ( 'NONE',  ( 0.5150084580479041829, 1.557691122620246116, -1.641117935488043633 ) ) ;
#172236=CARTESIAN_POINT ( 'NONE',  ( 0.9658262494645246665, 0.9167188063998463754, 1.630421345857439475 ) ) ;
#172237=CARTESIAN_POINT ( 'NONE',  ( 0.7208516900601771304, 1.708106959156988847, 0.2981761063507569198 ) ) ;
#172239=CARTESIAN_POINT ( 'NONE',  ( 4.353197867323560288, 0.4795420089713005041, -2.138300074133951068 ) ) ;
#172240=CARTESIAN_POINT ( 'NONE',  ( 4.612551310933718618, -0.9822873175598394457, -2.088206479280288796 ) ) ;
#172241=CARTESIAN_POINT ( 'NONE',  ( 0.09275324736048547181, -0.4491109574935348014, -2.018345435551980316 ) ) ;
#172242=CARTESIAN_POINT ( 'NONE',  ( 2.501813746025891128, -0.7434988463325925556, -1.794173334931578712 ) ) ;
#172245=CARTESIAN_POINT ( 'NONE',  ( 5.695592476053609410, 1.958610405324921588, -0.8133567297157192622 ) ) ;
#172247=CARTESIAN_POINT ( 'NONE',  ( 3.235000160576475992, 2.016597019841442240, -0.002811030766311505089 ) ) ;
#172251=CARTESIAN_POINT ( 'NONE',  ( 0.5393321728033516615, -1.288848960320065462, -1.293324666950084190 ) ) ;
#172256=CARTESIAN_POINT ( 'NONE',  ( 5.067286680778130936, 0.2040240636430467047, -2.050771057314598966 ) ) ;
#172260=CARTESIAN_POINT ( 'NONE',  ( 6.024083573256426405, -2.004181050114914875, 0.2492093081243785258 ) ) ;
#172261=CARTESIAN_POINT ( 'NONE',  ( 5.901095752275416828, -0.3235219084677161128, -2.197517257070471075 ) ) ;
#172263=AXIS2_PLACEMENT_3D ( 'NONE', #194924, #126818, #159225 ) ;
#172266=CARTESIAN_POINT ( 'NONE',  ( 4.258703985924441326, -1.528322205979601334, 1.382770117495622397 ) ) ;
#172267=CARTESIAN_POINT ( 'NONE',  ( 4.289685514112329123, 1.556909497225898109, -1.281360267751927129 ) ) ;
#172274=CARTESIAN_POINT ( 'NONE',  ( 3.761092154037175117, -2.013677596940225190, -0.1017350580494805479 ) ) ;
#172275=CARTESIAN_POINT ( 'NONE',  ( 3.327899939431624876, 1.796474422365784029, 0.4023406486387756664 ) ) ;
#172277=CARTESIAN_POINT ( 'NONE',  ( 1.296046498377702472, 1.750325484892759409, 1.504033841696296836 ) ) ;
#172279=CARTESIAN_POINT ( 'NONE',  ( 3.796290242343594468, -2.158924006851222988, -0.1102321833298808978 ) ) ;
#172281=AXIS2_PLACEMENT_3D ( 'NONE', #166440, #199988, #144114 ) ;
#172284=CARTESIAN_POINT ( 'NONE',  ( 1.955717210371358483, 1.865846021326333926, -0.1348392221205765851 ) ) ;
#172285=CARTESIAN_POINT ( 'NONE',  ( 6.819227947992137828, -0.1355634432321853045, 1.940828160714276995 ) ) ;
#172289=CARTESIAN_POINT ( 'NONE',  ( 2.086817400036289794, -2.164668306305051804, -0.4287355390964405211 ) ) ;
#172290=CARTESIAN_POINT ( 'NONE',  ( 6.589320575229280053, 7.629137130509070275, 2.496737603865983868 ) ) ;
#172294=CARTESIAN_POINT ( 'NONE',  ( 6.209841870239331207, -1.956602576295646490, 0.2410399859902948028 ) ) ;
#172295=CARTESIAN_POINT ( 'NONE',  ( 5.953837893508783452, 0.6757001976828447276, -2.206575258351393565 ) ) ;
#172296=CARTESIAN_POINT ( 'NONE',  ( 6.707467475981614413, -1.495571456699902546, -1.107353707014941069 ) ) ;
#172297=CARTESIAN_POINT ( 'NONE',  ( 3.028243468416950357, 1.099549687589720826, 1.744862417660711262 ) ) ;
#172304=CARTESIAN_POINT ( 'NONE',  ( 5.231008634329041840, -2.042658762482005841, -0.7362343983412369397 ) ) ;
#172306=CARTESIAN_POINT ( 'NONE',  ( 4.915489835137424102, -0.9894786724786635013, -1.552603174752004600 ) ) ;
#172309=CARTESIAN_POINT ( 'NONE',  ( 0.1747926744264660381, 0.006858446013176254172, -1.855468577918440776 ) ) ;
#172310=CARTESIAN_POINT ( 'NONE',  ( 0.5271418889439123401, 2.165442452462429834, 0.6551351998097357798 ) ) ;
#172315=CARTESIAN_POINT ( 'NONE',  ( 0.1879522776407696050, 1.101030317643518330, 1.563299796079109072 ) ) ;
#172316=CARTESIAN_POINT ( 'NONE',  ( 1.885279724593362793, 1.217781634009064806, 1.284517237999055039 ) ) ;
#172318=CARTESIAN_POINT ( 'NONE',  ( 6.639320575229259447, 0.002292789353198348111, 1.996863816985874118 ) ) ;
#172320=CARTESIAN_POINT ( 'NONE',  ( 3.726117878570588626, 1.906711264527670258, 0.1841570787439601176 ) ) ;
#172322=CARTESIAN_POINT ( 'NONE',  ( 4.351979406267578732, -0.7558620137302939357, 1.818942442720396624 ) ) ;
#172323=CARTESIAN_POINT ( 'NONE',  ( 6.469012451414649867, -1.558587985773008278, 1.284399031846704009 ) ) ;
#172325=CARTESIAN_POINT ( 'NONE',  ( 3.010468980803046257, 1.356049738124785353, -1.288842618233053683 ) ) ;
#172326=CARTESIAN_POINT ( 'NONE',  ( 6.006443931695136129, -0.6276177885309804916, -1.606848298988555301 ) ) ;
#172328=CARTESIAN_POINT ( 'NONE',  ( 2.104404934925046877, -2.206339196854599116, 0.05594281105186085790 ) ) ;
#172332=CARTESIAN_POINT ( 'NONE',  ( 6.180128940399614912, -1.088687182605744042, -1.631870318916525120 ) ) ;
#172340=CARTESIAN_POINT ( 'NONE',  ( 1.697802635435996743, -1.498143435978617877, -1.429203828351800487 ) ) ;
#172344=CARTESIAN_POINT ( 'NONE',  ( 0.3639331001695153001, 0.6315192924679478015, -1.918485960686921565 ) ) ;
#172346=CARTESIAN_POINT ( 'NONE',  ( 0.07479286986305369589, 0.2526433113205875935, -1.890777245541554574 ) ) ;
#172348=CARTESIAN_POINT ( 'NONE',  ( 5.747422657745248742, -1.966344092054626680, -0.4444320411668146731 ) ) ;
#172349=CARTESIAN_POINT ( 'NONE',  ( 5.612480213242726279, 1.848112342440700440, 0.5042863886801035589 ) ) ;
#172350=CARTESIAN_POINT ( 'NONE',  ( 6.639320575229291421, 2.053731943030055795, 2.310327526069462234 ) ) ;
#172351=CARTESIAN_POINT ( 'NONE',  ( 4.089532599075940134, -0.8378280566024614018, 2.025282237563410526 ) ) ;
#172353=CARTESIAN_POINT ( 'NONE',  ( 2.619282413590624525, 1.617716081779559278, 1.019604094833974628 ) ) ;
#172357=CARTESIAN_POINT ( 'NONE',  ( 6.925078400183548588, 0.0006614011395407459748, 1.855452278108092656 ) ) ;
#172358=CARTESIAN_POINT ( 'NONE',  ( 0.3336115229473045618, 0.6298545048411038350, -1.915608025624820909 ) ) ;
#172360=CARTESIAN_POINT ( 'NONE',  ( 5.671465802443460547, 1.304529079428708549, 1.760837017921567771 ) ) ;
#172362=CARTESIAN_POINT ( 'NONE',  ( 3.065164753754692661, 0.2545988855646770244, -1.705743084088023664 ) ) ;
#172368=CARTESIAN_POINT ( 'NONE',  ( 0.2562055958934654210, -1.961350414083770977, -0.05204156388862594962 ) ) ;
#172376=CARTESIAN_POINT ( 'NONE',  ( 3.123486050149349769, -0.3508677868355335461, 1.776971544703136452 ) ) ;
#172380=CARTESIAN_POINT ( 'NONE',  ( 3.264119686811095988, 1.811656971725349896, -0.002766503545040265976 ) ) ;
#172385=CARTESIAN_POINT ( 'NONE',  ( 4.967181581899757781, 1.619035083845013157, 0.9176225028624994673 ) ) ;
#172387=CARTESIAN_POINT ( 'NONE',  ( 2.161615495643732565, 1.180369796089770995, 1.508615382416353290 ) ) ;
#172388=CARTESIAN_POINT ( 'NONE',  ( 1.500715674837904468, 1.494693011815557471, -1.047886037138339166 ) ) ;
#172398=CARTESIAN_POINT ( 'NONE',  ( 0.9551577523512165824, 0.4061005957273036704, -2.050632492140195939 ) ) ;
#172399=CARTESIAN_POINT ( 'NONE',  ( 6.299827777084090918, -0.6482784301091691903, 1.814149458844191320 ) ) ;
#172401=CARTESIAN_POINT ( 'NONE',  ( 1.905030480050071251, 1.515927946353814892, 1.016894063925778635 ) ) ;
#172402=CARTESIAN_POINT ( 'NONE',  ( 3.317197348578094562, 1.995112415077514356, 0.9436014139095407760 ) ) ;
#172403=CARTESIAN_POINT ( 'NONE',  ( 0.5098338327763075606, -0.6861045072398126443, 1.785269576063217567 ) ) ;
#172404=CARTESIAN_POINT ( 'NONE',  ( 1.961320326556061922, 1.635743983707088622, 1.096704005335534138 ) ) ;
#172405=CARTESIAN_POINT ( 'NONE',  ( 3.438947998021203656, -1.472602994093423545, -1.266235326041851961 ) ) ;
#172409=CARTESIAN_POINT ( 'NONE',  ( 6.754761327113334879, -0.4959639348531270642, -1.793591138363290316 ) ) ;
#172414=CARTESIAN_POINT ( 'NONE',  ( 2.402122600552298870, -0.8417629408748151798, -2.023652355447076001 ) ) ;
#172419=CARTESIAN_POINT ( 'NONE',  ( 3.387140609607977026, 1.650079954178599539, -0.7815607168924765258 ) ) ;
#172424=CARTESIAN_POINT ( 'NONE',  ( 4.012460596634464416, 1.323225596166040186, -1.322536486416127977 ) ) ;
#172426=CARTESIAN_POINT ( 'NONE',  ( 2.385270436692279006, 1.761333987333755013, -0.7808530812865380755 ) ) ;
#172433=CARTESIAN_POINT ( 'NONE',  ( 6.456269881894531437, -1.301449686459619226, 1.670992065744638433 ) ) ;
#172436=CARTESIAN_POINT ( 'NONE',  ( 5.348515126027270306, -2.053966340784090239, -0.2589089449258550890 ) ) ;
#172437=ADVANCED_FACE ( 'NONE', ( #11611 ), #170863, .F. ) ;
#172438=CARTESIAN_POINT ( 'NONE',  ( 0.5558949066124979632, -1.334021266253348381, 1.269314063962425854 ) ) ;
#172440=CARTESIAN_POINT ( 'NONE',  ( 4.746898448635796797, 2.273877242543398403, -0.3363112362181965853 ) ) ;
#172444=CARTESIAN_POINT ( 'NONE',  ( 0.5160991691709617690, -1.231265438625952724, -1.933346247471772861 ) ) ;
#172447=CARTESIAN_POINT ( 'NONE',  ( 5.068278781427039803, -1.829183178514147690, -0.6524800764661740082 ) ) ;
#172451=CARTESIAN_POINT ( 'NONE',  ( 6.310809538426106258, -0.5167911955388967415, -1.841158844219364044 ) ) ;
#172452=CARTESIAN_POINT ( 'NONE',  ( 0.5567383370381777663, -1.454440682700371079, -0.9269339563611042054 ) ) ;
#172453=CARTESIAN_POINT ( 'NONE',  ( 5.805875103277515770, -1.124240986939632592, -1.673857227857282082 ) ) ;
#172456=CARTESIAN_POINT ( 'NONE',  ( 2.572312895708084302, -2.000810251872984225, -0.6062274732134291799 ) ) ;
#172457=CARTESIAN_POINT ( 'NONE',  ( 0.7425837709835466649, -1.521049679623546425, 0.9045992453171716186 ) ) ;
#172461=CARTESIAN_POINT ( 'NONE',  ( 4.435649837374885607, 0.9824219174630977047, -2.071190651000577976 ) ) ;
#172462=CARTESIAN_POINT ( 'NONE',  ( 2.202700171921621042, -0.3823900931277899318, 1.697618373880743325 ) ) ;
#172464=CARTESIAN_POINT ( 'NONE',  ( 2.795306286867365486, -0.1602278063087131110, -2.114629986603839829 ) ) ;
#172466=CARTESIAN_POINT ( 'NONE',  ( 2.512703819571511232, 1.733401479428131609, 0.04661458952265155886 ) ) ;
#172468=CARTESIAN_POINT ( 'NONE',  ( 1.222862307070234911, -1.680409034227359211, -0.8001750615637763797 ) ) ;
#172469=CARTESIAN_POINT ( 'NONE',  ( 1.908858375081338377, 0.6798548000985217277, 2.062075944584631504 ) ) ;
#172471=CARTESIAN_POINT ( 'NONE',  ( 3.538296236868877731, 0.7303062672313584969, 1.879804216660937666 ) ) ;
#172472=CARTESIAN_POINT ( 'NONE',  ( 2.906250000000002220, 1.895863743164021509, -0.7852924748301391977 ) ) ;
#172475=CARTESIAN_POINT ( 'NONE',  ( 0.4461525089796612997, 1.920980128883168714, 0.1452595308072956448 ) ) ;
#172477=CARTESIAN_POINT ( 'NONE',  ( 4.377308812845062569, -1.984989629755340435, -0.9973083610524589027 ) ) ;
#172483=CARTESIAN_POINT ( 'NONE',  ( 6.345936316318473658, -1.449877878406122145, -1.683046035897132420 ) ) ;
#172484=CARTESIAN_POINT ( 'NONE',  ( 5.230891786122516152, -1.846674803186045821, -0.6626716404555529349 ) ) ;
#172487=CARTESIAN_POINT ( 'NONE',  ( 5.325545376182048152, -2.150690057981026193, 0.7024452394915041697 ) ) ;
#172490=CARTESIAN_POINT ( 'NONE',  ( 3.139185485588998237, -0.1492200975972737820, -2.057319831125117737 ) ) ;
#172495=CARTESIAN_POINT ( 'NONE',  ( 4.903500725120335524, -0.5004011548357701900, 1.802273645872286334 ) ) ;
#172496=CARTESIAN_POINT ( 'NONE',  ( 3.779676010894826188, 1.462474260537292681, -0.9315460551484288088 ) ) ;
#172497=CARTESIAN_POINT ( 'NONE',  ( 2.893823712666950598, -0.5078125688623453815, -1.664683006417116751 ) ) ;
#172498=CARTESIAN_POINT ( 'NONE',  ( 0.9257723888009254942, -1.459437212925698502, -1.767766894381626486 ) ) ;
#172499=CARTESIAN_POINT ( 'NONE',  ( 1.554063478550568256, 0.6399170599369340406, -2.111937735441645980 ) ) ;
#172500=CARTESIAN_POINT ( 'NONE',  ( 5.091392180243133225, -0.7513228403347729234, 1.951278057808901512 ) ) ;
#172501=CARTESIAN_POINT ( 'NONE',  ( 5.525317926099265087, -1.233401178653690033, -1.499961942869533438 ) ) ;
#172505=CARTESIAN_POINT ( 'NONE',  ( 0.5279704824466545654, -1.728000714500482982, 1.038995864524896673 ) ) ;
#172506=CARTESIAN_POINT ( 'NONE',  ( 0.8266187642571948269, -0.9586779626098644869, -1.891633453305548773 ) ) ;
#172512=CARTESIAN_POINT ( 'NONE',  ( 4.160648861918358143, -1.351394993475165673, 1.227733137840483879 ) ) ;
#172518=CARTESIAN_POINT ( 'NONE',  ( 1.740496097130298958, 1.159487406938706888, -1.653631796535762755 ) ) ;
#172519=CARTESIAN_POINT ( 'NONE',  ( 5.473716482686670659, 2.128106746890707335, -0.5837492795209007213 ) ) ;
#172521=CARTESIAN_POINT ( 'NONE',  ( 2.570971337753673147, 1.659905555536644872, 0.8415416509589612737 ) ) ;
#172528=CARTESIAN_POINT ( 'NONE',  ( 5.320859459983126705, 1.688362619374352613, 0.6951667914897319278 ) ) ;
#172532=CARTESIAN_POINT ( 'NONE',  ( 0.1394461523056798324, 0.009327122704651937685, -1.719853553173174232 ) ) ;
#172533=CARTESIAN_POINT ( 'NONE',  ( -0.02988540731103071432, 0.005807295984020746475, -1.726291166677936362 ) ) ;
#172534=CARTESIAN_POINT ( 'NONE',  ( 5.795647523915807398, 1.743732541305573758, 1.511695197786174782 ) ) ;
#172536=CARTESIAN_POINT ( 'NONE',  ( 0.5443023342626990280, 2.055102546481206272, 0.1540600304409632249 ) ) ;
#172538=CARTESIAN_POINT ( 'NONE',  ( 6.116662973727256869, 0.6756443950356945116, -2.196842021360578823 ) ) ;
#172541=CARTESIAN_POINT ( 'NONE',  ( 5.436355746168001879, 1.843147576875401983, 0.3187000444574567548 ) ) ;
#172542=CARTESIAN_POINT ( 'NONE',  ( 3.076317393561965208, 0.8638369986560844316, 1.706277067364105893 ) ) ;
#172544=CARTESIAN_POINT ( 'NONE',  ( 4.951907052881864502, 0.6945806438464275923, -2.094803410698709900 ) ) ;
#172545=CARTESIAN_POINT ( 'NONE',  ( 4.399685268140280492, -2.075804279169701339, 0.4165508703993703876 ) ) ;
#172547=CARTESIAN_POINT ( 'NONE',  ( 6.983263157960371004, 2.969675876345272858, 2.399270433241917466 ) ) ;
#172550=CARTESIAN_POINT ( 'NONE',  ( 5.760427271636393343, 2.118038551301495875, 0.1041057254967461404 ) ) ;
#172551=CARTESIAN_POINT ( 'NONE',  ( 2.608792587697115639, -0.8827421749361822334, -2.132256252471361524 ) ) ;
#172552=CARTESIAN_POINT ( 'NONE',  ( 4.000408739481801312, 1.952204270133122810, 0.1946113827649766925 ) ) ;
#172554=CARTESIAN_POINT ( 'NONE',  ( 6.561391914609854936, 1.711577788671992062, 1.150682440272139617 ) ) ;
#172558=CARTESIAN_POINT ( 'NONE',  ( 5.419157771004846857, -1.820987890746316173, 0.8666037247077316152 ) ) ;
#172560=( BOUNDED_SURFACE ( )  B_SPLINE_SURFACE ( 3, 3, ( 
 ( #180696, #102659, #16040, #167652, #131996, #19253, #33377, #118968, #85333, #2990 ),
 ( #115756, #198005, #99458, #86406, #39794, #202257, #61100, #189238, #38726, #90695 ),
 ( #173007, #143458, #22442, #87479, #88553, #72262, #193230, #155679, #105901, #187092 ),
 ( #136234, #23521, #209456, #176988, #171925, #156757, #106982, #44877, #123276, #24588 ),
 ( #5114, #40877, #110982, #11268, #77346, #120043, #204387, #127259, #71191, #154614 ),
 ( #28606, #121128, #4053, #94695, #6193, #70123, #104807, #153545, #89627, #170852 ),
 ( #7261, #53908, #186017, #73337, #57107, #188161, #138370, #137308, #56043, #103731 ) ),
 .UNSPECIFIED., .T., .F., .F. ) 
 B_SPLINE_SURFACE_WITH_KNOTS ( ( 4, 3, 4 ),
 ( 4, 1, 1, 1, 1, 1, 1, 4 ),
 ( 0.000000000000000000, 0.5000000000000000000, 1.000000000000000000 ),
 ( 0.000000000000000000, 0.09489293188423997272, 0.1878783894049059211, 0.2584743716234961797, 0.3617987437640678983, 0.5212292184658617877, 0.7337638816394396191, 1.000000000000000000 ),
 .UNSPECIFIED. ) 
 GEOMETRIC_REPRESENTATION_ITEM ( )  RATIONAL_B_SPLINE_SURFACE ( (
 ( 1.000000000000000222, 1.000000000000000222, 1.000000000000000000, 1.000000000000000000, 1.000000000000000000, 1.000000000000000000, 1.000000000000000000, 0.9999999999999997780, 1.000000000000000000, 1.000000000000000000),
 ( 0.3333333333333334259, 0.3333333333333333703, 0.3333333333333334259, 0.3333333333333334259, 0.3333333333333333703, 0.3333333333333333703, 0.3333333333333333703, 0.3333333333333332038, 0.3333333333333333703, 0.3333333333333333703),
 ( 0.3333333333333334259, 0.3333333333333333703, 0.3333333333333334259, 0.3333333333333334259, 0.3333333333333333703, 0.3333333333333333703, 0.3333333333333333703, 0.3333333333333332038, 0.3333333333333333703, 0.3333333333333333703),
 ( 1.000000000000000222, 1.000000000000000222, 1.000000000000000000, 1.000000000000000000, 1.000000000000000000, 1.000000000000000000, 1.000000000000000000, 0.9999999999999997780, 1.000000000000000000, 1.000000000000000000),
 ( 0.3333333333333334259, 0.3333333333333333703, 0.3333333333333334259, 0.3333333333333334259, 0.3333333333333333703, 0.3333333333333333703, 0.3333333333333333703, 0.3333333333333332038, 0.3333333333333333703, 0.3333333333333333703),
 ( 0.3333333333333334259, 0.3333333333333333703, 0.3333333333333334259, 0.3333333333333334259, 0.3333333333333333703, 0.3333333333333333703, 0.3333333333333333703, 0.3333333333333332038, 0.3333333333333333703, 0.3333333333333333703),
 ( 1.000000000000000222, 1.000000000000000222, 1.000000000000000000, 1.000000000000000000, 1.000000000000000000, 1.000000000000000000, 1.000000000000000000, 0.9999999999999997780, 1.000000000000000000, 1.000000000000000000) ) ) 
 REPRESENTATION_ITEM ( '' )  SURFACE ( )  );
#172562=CARTESIAN_POINT ( 'NONE',  ( 2.571331741745811250, 1.937545498039330960, 0.9797267027546376905 ) ) ;
#172563=CARTESIAN_POINT ( 'NONE',  ( 6.539320575229290000, 0.004092658091040673150, 2.003502637948690879 ) ) ;
#172569=CARTESIAN_POINT ( 'NONE',  ( 1.317730169365991522, -2.011166735366700209, 0.4487503453191737934 ) ) ;
#172571=CARTESIAN_POINT ( 'NONE',  ( 6.727182134110205602, 7.053355583909074689, 2.409100679957976165 ) ) ;
#172576=CARTESIAN_POINT ( 'NONE',  ( 3.580628178849315280, -1.282259035790348722, 1.418852674340838060 ) ) ;
#172577=CARTESIAN_POINT ( 'NONE',  ( 4.944116541256327935, 1.765280609655010879, 0.1280878748119110566 ) ) ;
#172580=CARTESIAN_POINT ( 'NONE',  ( 0.2459857770662046417, 0.9310377468562742731, -1.553837941864342875 ) ) ;
#172582=CARTESIAN_POINT ( 'NONE',  ( 0.2510146965912671835, 0.1847738873272772309, -1.906744464555621521 ) ) ;
#172585=CARTESIAN_POINT ( 'NONE',  ( 0.5200892513525963157, 2.048054262204841880, -0.3022008342252607838 ) ) ;
#172587=CARTESIAN_POINT ( 'NONE',  ( 6.368025811218641863, 0.9635043244729593059, 1.603280169136585220 ) ) ;
#172588=CARTESIAN_POINT ( 'NONE',  ( 3.000428103051573814, -0.5303778429210231904, -1.746945217264872507 ) ) ;
#172589=CARTESIAN_POINT ( 'NONE',  ( 6.252570086353132162, 0.6882034672392455255, 2.096894461246688213 ) ) ;
#172593=CARTESIAN_POINT ( 'NONE',  ( 3.156738326643961923, -0.5960753502360670586, -1.974691822637637761 ) ) ;
#172597=CARTESIAN_POINT ( 'NONE',  ( 0.9312127099814873077, 0.1580370610147242560, 2.155845405312675211 ) ) ;
#172598=CARTESIAN_POINT ( 'NONE',  ( 0.2038950025188591975, -1.678810847859620869, -1.376375048264495859 ) ) ;
#172600=CARTESIAN_POINT ( 'NONE',  ( 4.235729478701364847, -1.487246874726022350, -1.568870776130903089 ) ) ;
#172601=CARTESIAN_POINT ( 'NONE',  ( 4.705726078268232193, 1.497967940706146805, 1.354894159888963001 ) ) ;
#172602=CARTESIAN_POINT ( 'NONE',  ( 2.629291921057617554, 0.09916324773191761976, -1.959495597191794225 ) ) ;
#172603=CARTESIAN_POINT ( 'NONE',  ( 6.720655732516649827, 2.940181725866806151, 2.725612257524675730 ) ) ;
#172610=CARTESIAN_POINT ( 'NONE',  ( 3.028530041973789722, 0.4946322284519070189, 1.954779462066410733 ) ) ;
#172614=CARTESIAN_POINT ( 'NONE',  ( 5.502191098127390489, -0.8541586074963626318, 1.711093258865265421 ) ) ;
#172618=CARTESIAN_POINT ( 'NONE',  ( 3.761342352588430860, 1.897692735847063661, -0.6820134568972098243 ) ) ;
#172621=CARTESIAN_POINT ( 'NONE',  ( 5.983370841356476788, 1.591773204597257463, -0.6646525218769030463 ) ) ;
#172625=CARTESIAN_POINT ( 'NONE',  ( 4.130043426961079511, 1.002751595458702738, -1.578879078160302818 ) ) ;
#172627=CARTESIAN_POINT ( 'NONE',  ( 2.676698048161993082, 1.355622082481915847, -1.564734663558226879 ) ) ;
#172634=CARTESIAN_POINT ( 'NONE',  ( 0.08776524826303951088, 1.042983370315919478, 1.480986741271082430 ) ) ;
#172640=CARTESIAN_POINT ( 'NONE',  ( 5.642171489992906075, 0.7808347329528000369, 1.749441798972359408 ) ) ;
#172648=CARTESIAN_POINT ( 'NONE',  ( 2.817419395390472037, -0.2130390993498078311, 2.151187356804876050 ) ) ;
#172652=CARTESIAN_POINT ( 'NONE',  ( 0.4574861729177078229, -1.815669959853306370, 1.095388807130371900 ) ) ;
#172653=CARTESIAN_POINT ( 'NONE',  ( 5.473610661177239933, 1.758888005172161373, -0.4887267171112125164 ) ) ;
#172655=CARTESIAN_POINT ( 'NONE',  ( 1.053909416342192484, 1.969286043147522980, -0.09259992539933233069 ) ) ;
#172656=CARTESIAN_POINT ( 'NONE',  ( 3.006014587165442453, -0.7710369221427433306, 1.750240277048662030 ) ) ;
#172659=CARTESIAN_POINT ( 'NONE',  ( 5.160591359625510854, -0.6618325696593707619, -1.855173450206740071 ) ) ;
#172660=CARTESIAN_POINT ( 'NONE',  ( 0.4451279286748652808, 0.6098585162058448583, -1.843775557458992687 ) ) ;
#172665=CARTESIAN_POINT ( 'NONE',  ( 3.756429630051653312, 1.903336793139896788, 0.1845653119916731144 ) ) ;
#172667=CARTESIAN_POINT ( 'NONE',  ( 1.132168909276673796, -1.401036632855560349, -1.704990472574128502 ) ) ;
#172669=CARTESIAN_POINT ( 'NONE',  ( 6.428391161641624940, -0.9511404050406097044, -1.774240594045069841 ) ) ;
#172672=CARTESIAN_POINT ( 'NONE',  ( 5.823453932400854960, -1.463924103857511039, -1.387103351090559711 ) ) ;
#172673=CARTESIAN_POINT ( 'NONE',  ( 2.383334800519558705, -0.002349189141126820958, 2.070544812199434315 ) ) ;
#172676=CARTESIAN_POINT ( 'NONE',  ( 0.1105426557568081891, -0.9253945370547181914, -1.951590883024490353 ) ) ;
#172683=CARTESIAN_POINT ( 'NONE',  ( 6.825078400183513416, 0.6012913621265563169, 1.809472532188656890 ) ) ;
#172685=CARTESIAN_POINT ( 'NONE',  ( 5.168516884834092551, 1.170641038942145995, 1.279587065987584982 ) ) ;
#172687=CARTESIAN_POINT ( 'NONE',  ( 2.026315959858393967, 1.060668813445601044, 1.777738962378045295 ) ) ;
#172688=CARTESIAN_POINT ( 'NONE',  ( 3.849298028564145380, 0.2572143275579537591, -2.101468238826177615 ) ) ;
#172691=CARTESIAN_POINT ( 'NONE',  ( 1.428490153906246007, -1.253617920133040853, 1.518890472526812419 ) ) ;
#172693=CARTESIAN_POINT ( 'NONE',  ( 0.01762790050853849447, -0.5081247445114078776, 1.843608005305336528 ) ) ;
#172694=CARTESIAN_POINT ( 'NONE',  ( 3.802894434091105946, 1.965436290923015639, 1.179407150283459105 ) ) ;
#172695=CARTESIAN_POINT ( 'NONE',  ( 1.594096589105632011, -1.816728215151931058, -0.1805768397986490248 ) ) ;
#172699=CARTESIAN_POINT ( 'NONE',  ( 2.496342308839387680, -1.031403195114518390, 1.728778584395810114 ) ) ;
#172700=CARTESIAN_POINT ( 'NONE',  ( 3.485159065011545376, 0.04355839926390054490, 1.961427607708134957 ) ) ;
#172703=CARTESIAN_POINT ( 'NONE',  ( 0.07516593201273635838, 7.629137130509072939, -2.644199648255764590 ) ) ;
#172704=CARTESIAN_POINT ( 'NONE',  ( 5.806606243248950250, 1.843357943042901459, 0.9862787698241348711 ) ) ;
#172705=CARTESIAN_POINT ( 'NONE',  ( 4.065142161210800076, 0.2162087174472343276, -1.756520380257739822 ) ) ;
#172708=CARTESIAN_POINT ( 'NONE',  ( 0.5861907285475282947, -2.175377356269320828, -0.2643977408666315365 ) ) ;
#172709=CARTESIAN_POINT ( 'NONE',  ( 5.736210779895188239, 0.3457693788900301768, 1.705448404129115580 ) ) ;
#172713=CARTESIAN_POINT ( 'NONE',  ( 5.818996626390088522, 1.136386364665368687, -1.998068361519554248 ) ) ;
#172715=CARTESIAN_POINT ( 'NONE',  ( 5.167242596723413683, -0.5858957144197572964, -1.632003580468445847 ) ) ;
#172716=CARTESIAN_POINT ( 'NONE',  ( 1.752831059180045115, 0.6944836804415283060, 2.094827981560241970 ) ) ;
#172717=CARTESIAN_POINT ( 'NONE',  ( 5.934065736658769019, 1.288437188380668452, 1.747434731901863936 ) ) ;
#172719=CARTESIAN_POINT ( 'NONE',  ( 0.3744018202470792978, -2.102136181054746089, -0.2526282858289953248 ) ) ;
#172720=CARTESIAN_POINT ( 'NONE',  ( 2.687500000000001332, -1.451031289061010421, 1.451031289061227136 ) ) ;
#172721=CARTESIAN_POINT ( 'NONE',  ( 6.727182134110199385, 1.257034414284210921, 2.204727292504021108 ) ) ;
#172722=CARTESIAN_POINT ( 'NONE',  ( 4.471652382922743030, 1.868735325311605688, -0.4673391499005700722 ) ) ;
#172723=CARTESIAN_POINT ( 'NONE',  ( 1.418920233055203761, -0.8037200727962053870, -2.070967414838392084 ) ) ;
#172728=CARTESIAN_POINT ( 'NONE',  ( 3.686370400671713732, 1.234840205895268328, 1.846255301073204791 ) ) ;
#172736=CARTESIAN_POINT ( 'NONE',  ( 2.039685609654022347, -1.556907966322677472, 1.281362143053674130 ) ) ;
#172738=CARTESIAN_POINT ( 'NONE',  ( 0.2860855845884663351, -1.266418373674676134, -1.628825195542679793 ) ) ;
#172741=CARTESIAN_POINT ( 'NONE',  ( 0.2570343420702363435, 1.821350608449383124, -0.2692129421619017804 ) ) ;
#172745=CARTESIAN_POINT ( 'NONE',  ( 1.387592303909779279, -0.8018289002829273038, 1.577768680615166952 ) ) ;
#172746=CARTESIAN_POINT ( 'NONE',  ( -0.03452862918938356951, -1.956592590566148093, -0.4871966601913205186 ) ) ;
#172747=CARTESIAN_POINT ( 'NONE',  ( 0.3976880421775743635, -0.6195963491163231085, -1.733980255833282191 ) ) ;
#172748=CARTESIAN_POINT ( 'NONE',  ( 3.948992478018618080, -1.906111675684089901, -1.273188117731700597 ) ) ;
#172749=CARTESIAN_POINT ( 'NONE',  ( 2.009460956091331685, -0.8672641894471898594, -1.624084198382821587 ) ) ;
#172752=CARTESIAN_POINT ( 'NONE',  ( 3.451995160207482538, 1.825762228170943136, 0.001041782061617091849 ) ) ;
#172753=CARTESIAN_POINT ( 'NONE',  ( 3.586564705785996843, -0.5826563296015655480, 1.930417576838711957 ) ) ;
#172755=CARTESIAN_POINT ( 'NONE',  ( 3.309705378935084763, -0.4432241279512488807, 2.218521802316391511 ) ) ;
#172757=CARTESIAN_POINT ( 'NONE',  ( 5.667048493276758414, -1.902512422570214357, -0.9033719842039839021 ) ) ;
#172759=CARTESIAN_POINT ( 'NONE',  ( 1.979048004138800998, 1.930994533390210544, 0.7472069620131777112 ) ) ;
#172762=CARTESIAN_POINT ( 'NONE',  ( 5.778019675193696969, 2.089136139637823852, -0.3624112956793351659 ) ) ;
#172765=CARTESIAN_POINT ( 'NONE',  ( 0.8207749864527034145, 1.779613767027238502, 0.7382806748287008558 ) ) ;
#172772=CARTESIAN_POINT ( 'NONE',  ( 0.8268048150999330881, -1.005496690709275720, -1.980927387359689318 ) ) ;
#172773=CARTESIAN_POINT ( 'NONE',  ( 2.116374960856721277, -0.9918371849380368532, -1.857756019195427877 ) ) ;
#172776=CARTESIAN_POINT ( 'NONE',  ( 6.860206125033806224, -1.860540838789390694, 0.04523802485481390190 ) ) ;
#172782=CARTESIAN_POINT ( 'NONE',  ( 0.07077104593807002908, 0.8175350930016941353, 1.956879683024402183 ) ) ;
#172785=CARTESIAN_POINT ( 'NONE',  ( 3.209375601822930690, -1.602329130913646926, -1.131729396966949963 ) ) ;
#172786=CARTESIAN_POINT ( 'NONE',  ( 2.184651956524386041, -2.119909832212972578, -0.4221607449544013679 ) ) ;
#172787=CARTESIAN_POINT ( 'NONE',  ( 3.309780021317248355, -1.205041885261768808, -1.616693488061982098 ) ) ;
#172791=CARTESIAN_POINT ( 'NONE',  ( 3.732115773437282513, 0.2573812008909857618, 1.721053547986243215 ) ) ;
#172794=CARTESIAN_POINT ( 'NONE',  ( 1.006953172832128152, 1.636353683469338183, -1.412668763314451903 ) ) ;
#172796=CARTESIAN_POINT ( 'NONE',  ( 2.565779641467882399, 1.620934753846922982, -1.198676126143098486 ) ) ;
#172798=CARTESIAN_POINT ( 'NONE',  ( 0.5148121308554790554, 1.489681748880047563, -1.566682057046255849 ) ) ;
#172799=CARTESIAN_POINT ( 'NONE',  ( 2.149238863156129220, -1.582378584423797419, -1.175707468242733977 ) ) ;
#172806=CARTESIAN_POINT ( 'NONE',  ( 2.156904581142269350, 0.4447176379400120672, 1.969927323211942083 ) ) ;
#172808=CARTESIAN_POINT ( 'NONE',  ( 5.860475213782774695, 0.9281710514958280145, 2.112872520220021144 ) ) ;
#172810=CARTESIAN_POINT ( 'NONE',  ( 2.623818369222921554, 1.924856029493416276, -0.3778354045670463401 ) ) ;
#172812=CARTESIAN_POINT ( 'NONE',  ( 0.3521856818783953846, 0.1948384997633167970, -2.006960225185448810 ) ) ;
#172814=CARTESIAN_POINT ( 'NONE',  ( 2.747379667311528273, 0.3059357446031922834, -2.094990568135519649 ) ) ;
#172817=CARTESIAN_POINT ( 'NONE',  ( 2.202840038917678545, -0.4038221959529255112, 1.796142596185656526 ) ) ;
#172821=CARTESIAN_POINT ( 'NONE',  ( 4.359710196644346780, -1.641147893522959089, -1.343014508298406628 ) ) ;
#172822=CARTESIAN_POINT ( 'NONE',  ( 0.1461044202776436429, -1.480667811789614596, 1.094048858351577724 ) ) ;
#172826=CARTESIAN_POINT ( 'NONE',  ( 4.587218493272061437, 1.842632243969796413, -0.9228815313185294578 ) ) ;
#172829=CARTESIAN_POINT ( 'NONE',  ( 1.856743374925871715, 0.3135980649527739250, -1.814175028193690808 ) ) ;
#172834=CARTESIAN_POINT ( 'NONE',  ( 1.454063653991678473, 0.6380318336138122159, -2.112638918738508398 ) ) ;
#172835=CARTESIAN_POINT ( 'NONE',  ( 3.374574379025939486, -1.350666858538966064, 1.814832908163630742 ) ) ;
#172837=CARTESIAN_POINT ( 'NONE',  ( 3.427799431637909233, -1.783865866189004556, 0.3147462633073249139 ) ) ;
#172839=CARTESIAN_POINT ( 'NONE',  ( 3.485460621946351534, -0.5511008185722067187, 1.834767741543178676 ) ) ;
#172840=CARTESIAN_POINT ( 'NONE',  ( 3.895033709675084221, 0.3008086390649654662, 2.048262060622765279 ) ) ;
#172842=CARTESIAN_POINT ( 'NONE',  ( 3.116049734078304212, -0.9705229388551097625, -1.715950581178276479 ) ) ;
#172843=CARTESIAN_POINT ( 'NONE',  ( 1.412975430660408538, 1.697568229685364249, 0.9106500277177332903 ) ) ;
#172844=CARTESIAN_POINT ( 'NONE',  ( 3.959713429720784106, 1.856571849420919795, -0.2284545790810637578 ) ) ;
#172846=CARTESIAN_POINT ( 'NONE',  ( 2.579137097422959712, -2.208767019342866345, -0.6684429575241066512 ) ) ;
#172847=CARTESIAN_POINT ( 'NONE',  ( 3.314761293198214887, -1.410806105172614178, 1.213857476866337937 ) ) ;
#172852=CARTESIAN_POINT ( 'NONE',  ( 0.4519647057620000408, 0.6586765168765180700, -2.000488393216502292 ) ) ;
#172857=CARTESIAN_POINT ( 'NONE',  ( 6.819591527820957566, -2.098570527662356522, 0.5178885164088961046 ) ) ;
#172858=CARTESIAN_POINT ( 'NONE',  ( 2.391022662813433453, -2.030629854096975606, -0.6112283555373964061 ) ) ;
#172860=CARTESIAN_POINT ( 'NONE',  ( 1.142838682686732277, 1.947676595115959586, 0.5347052314127549444 ) ) ;
#172865=CARTESIAN_POINT ( 'NONE',  ( 1.282749207608822495, -2.108609127331688260, -0.4749100009155197699 ) ) ;
#172867=CARTESIAN_POINT ( 'NONE',  ( 6.825078400183573812, 7.629137130509070275, 2.455651831298297338 ) ) ;
#172870=CARTESIAN_POINT ( 'NONE',  ( 5.700407750362016301, 1.350738941191354625, -1.497498989668680114 ) ) ;
#172872=CARTESIAN_POINT ( 'NONE',  ( -0.1114211809780316365, -0.4883405756051837354, -2.144353428667714390 ) ) ;
#172874=CARTESIAN_POINT ( 'NONE',  ( 6.614160618316515361, -1.014195557614630205, -1.909021090911746654 ) ) ;
#172878=CARTESIAN_POINT ( 'NONE',  ( 0.6146668332816725977, 0.1418531279011990553, 1.910429497406636479 ) ) ;
#172881=CARTESIAN_POINT ( 'NONE',  ( 2.490480453433571384, -0.2941264275767330183, -1.699438164531028583 ) ) ;
#172883=CARTESIAN_POINT ( 'NONE',  ( 0.4207181242068900873, -0.09552205520973154618, 1.767312625620009126 ) ) ;
#172884=CARTESIAN_POINT ( 'NONE',  ( 1.524088986950965730, -1.997618534301074833, 0.2487294023021668354 ) ) ;
#172886=CARTESIAN_POINT ( 'NONE',  ( 4.296070028909639404, -0.8476096858263427736, 2.037697185916572007 ) ) ;
#172890=CARTESIAN_POINT ( 'NONE',  ( 3.879626234357834047, 0.2581020070546445888, -2.104639248629774251 ) ) ;
#172891=CARTESIAN_POINT ( 'NONE',  ( 4.517203946846011675, -1.842441744247227842, 0.8197884948388590720 ) ) ;
#172892=CARTESIAN_POINT ( 'NONE',  ( 2.935611553675514518, -1.744650271585326484, 0.4875094811955403284 ) ) ;
#172897=CARTESIAN_POINT ( 'NONE',  ( 1.217418975555501826, -1.825842229346545498, 0.4062821374252246764 ) ) ;
#172898=CARTESIAN_POINT ( 'NONE',  ( 6.410779360540267646, 1.349177972556347971, -1.230185023894624141 ) ) ;
#172909=CARTESIAN_POINT ( 'NONE',  ( 4.289387122732970958, -0.003046686910593982868, -2.120778211268215419 ) ) ;
#172910=CARTESIAN_POINT ( 'NONE',  ( -0.02948999725178609935, 2.037268340021273882, -2.343334633859140315 ) ) ;
#172912=CARTESIAN_POINT ( 'NONE',  ( 6.081318999601531772, 1.822420489394786625, -0.7521447986948930353 ) ) ;
#172914=CARTESIAN_POINT ( 'NONE',  ( 6.539320575229249144, 0.007148032025052972194, 1.896977914940492393 ) ) ;
#172916=CARTESIAN_POINT ( 'NONE',  ( 0.2810647479330531939, 1.757583132164267647, -1.180221762011339326 ) ) ;
#172918=CARTESIAN_POINT ( 'NONE',  ( 1.926316106172959230, 1.062450747350886848, 1.776810178100460824 ) ) ;
#172922=CARTESIAN_POINT ( 'NONE',  ( 3.890639641997388765, 1.766133395052928101, -1.118410975085604608 ) ) ;
#172925=CARTESIAN_POINT ( 'NONE',  ( 2.256629077056008015, -1.412982602626071671, 1.155960151518524937 ) ) ;
#172926=CARTESIAN_POINT ( 'NONE',  ( 1.787489318380721448, 1.733277665728020001, -0.5263807565755849183 ) ) ;
#172928=CARTESIAN_POINT ( 'NONE',  ( 5.461621781982892720, 0.4335984126433762853, -2.163701019753036192 ) ) ;
#172930=CARTESIAN_POINT ( 'NONE',  ( 4.665167916288286420, -1.969490514480085164, -0.9956290437203789701 ) ) ;
#172934=CARTESIAN_POINT ( 'NONE',  ( 3.264218543254516103, 1.912461472423478970, -0.002497826895729581952 ) ) ;
#172936=CARTESIAN_POINT ( 'NONE',  ( 4.914543119725925280, 0.7892175071393169317, 1.914236960262293508 ) ) ;
#172939=CARTESIAN_POINT ( 'NONE',  ( 5.618738332679400038, -0.05485954975367920983, 2.191026952110195491 ) ) ;
#172948=CARTESIAN_POINT ( 'NONE',  ( 5.313363446356571984, -1.745981802610725442, -1.112170280247841703 ) ) ;
#172949=CARTESIAN_POINT ( 'NONE',  ( 4.354074215503287881, 1.926045596674738514, -0.04874250487575670227 ) ) ;
#172950=CARTESIAN_POINT ( 'NONE',  ( 6.603150282362637569, -0.1459358296138096867, 2.084196934165093662 ) ) ;
#172955=CARTESIAN_POINT ( 'NONE',  ( 0.7795418844130063141, 1.474435645617519164, 1.621430000501473900 ) ) ;
#172956=CARTESIAN_POINT ( 'NONE',  ( 5.320859459983126705, 1.688362619374352613, 0.6951667914897319278 ) ) ;
#172963=CARTESIAN_POINT ( 'NONE',  ( 2.964219115174483665, -1.702287218311925310, -0.7022057971969236645 ) ) ;
#172964=CARTESIAN_POINT ( 'NONE',  ( -0.005209864377695229073, -1.953240142932886725, -0.4869125064202137199 ) ) ;
#172965=CARTESIAN_POINT ( 'NONE',  ( 1.950936211155746447, 1.584691988697755960, 1.664941613344946836 ) ) ;
#172966=CARTESIAN_POINT ( 'NONE',  ( 6.614115624646348834, 1.956711779489667125, -0.1410536379464824575 ) ) ;
#172972=CARTESIAN_POINT ( 'NONE',  ( 2.542619699696859303, -1.736688010486141520, 1.163783427146478200 ) ) ;
#172973=CARTESIAN_POINT ( 'NONE',  ( 0.6197280442463182215, -0.9970892369244135356, -1.582582228963416160 ) ) ;
#172974=CARTESIAN_POINT ( 'NONE',  ( 2.513045873335068237, 2.015604327017831654, 0.05229110803010171560 ) ) ;
#172978=CARTESIAN_POINT ( 'NONE',  ( 1.856607919947508956, 0.2971036446917668106, -1.714703581143263156 ) ) ;
#172983=CARTESIAN_POINT ( 'NONE',  ( 2.402614999361089243, 1.385809671090399986, -1.026769200382530167 ) ) ;
#172984=CARTESIAN_POINT ( 'NONE',  ( 2.823975127348025804, 1.215230906543849354, -1.823574674616668556 ) ) ;
#172985=CARTESIAN_POINT ( 'NONE',  ( 4.899154391205060577, 1.836108854712194649, -1.224054507610386366 ) ) ;
#172987=CARTESIAN_POINT ( 'NONE',  ( 2.817415258179640336, -1.886890863808653007, -1.073800027038468219 ) ) ;
#172988=CARTESIAN_POINT ( 'NONE',  ( 0.5393321728033516615, -1.288848960320065462, -1.293324666950084190 ) ) ;
#172989=CARTESIAN_POINT ( 'NONE',  ( 4.276635374070654194, -0.4674139498860945263, -2.064944810692950217 ) ) ;
#172992=CARTESIAN_POINT ( 'NONE',  ( 4.265347265089792117, 2.223640956194427254, -0.5566138344911036873 ) ) ;
#172996=CARTESIAN_POINT ( 'NONE',  ( 0.6102159345307588412, -0.7594153588383574238, 1.980023364433493693 ) ) ;
#173003=CARTESIAN_POINT ( 'NONE',  ( 5.045546153961558922, -1.458558117013383892, 1.392544180963309230 ) ) ;
#173005=CARTESIAN_POINT ( 'NONE',  ( 2.957939313049274599, -0.6512127342562739063, 1.957104789517728483 ) ) ;
#173007=CARTESIAN_POINT ( 'NONE',  ( -0.1408020194049781904, -0.005144001661201018025, -2.100147592658160089 ) ) ;
#173011=CARTESIAN_POINT ( 'NONE',  ( 6.421842908546859796, 1.265077015623069512, -1.789241164368003290 ) ) ;
#173012=CARTESIAN_POINT ( 'NONE',  ( 3.410779880581996437, -1.203353552534730309, -1.617818353255597863 ) ) ;
#173013=CARTESIAN_POINT ( 'NONE',  ( 3.368544699895597461, 0.04196216268675251326, -1.840931771443871101 ) ) ;
#173015=CARTESIAN_POINT ( 'NONE',  ( 6.598675984083053336, -0.4903212918116289787, -1.758449130657411263 ) ) ;
#173016=CARTESIAN_POINT ( 'NONE',  ( 0.1593517250534680629, 1.330572521919655360, 1.874314102060254505 ) ) ;
#173018=CARTESIAN_POINT ( 'NONE',  ( 6.772354121900423962, -1.399018086243536407, 1.779017302379340748 ) ) ;
#173019=CARTESIAN_POINT ( 'NONE',  ( 1.717544045074904213, -0.2563126921724939167, 2.090340884163774948 ) ) ;
#173028=CARTESIAN_POINT ( 'NONE',  ( 4.096076364168971473, 1.452574950358286765, 1.680725415074139306 ) ) ;
#173029=CARTESIAN_POINT ( 'NONE',  ( 2.554835828347111093, -1.907293181126702653, -1.079063956894068976 ) ) ;
#173030=CARTESIAN_POINT ( 'NONE',  ( 0.6103625832605160673, -2.195865045534075133, 0.2202409711149767024 ) ) ;
#173032=CARTESIAN_POINT ( 'NONE',  ( 4.176187491914356897, -1.006606191838583131, -1.683785057063936552 ) ) ;
#173039=CARTESIAN_POINT ( 'NONE',  ( 3.164422831683691761, 2.120778211551369807, -0.003951117757632071313 ) ) ;
#173041=CARTESIAN_POINT ( 'NONE',  ( 5.401312781148373432, 1.764888628567516049, 1.247983453017486699 ) ) ;
#173042=CARTESIAN_POINT ( 'NONE',  ( 3.421284184235491743, -1.099380227797893905, -1.476844927387373163 ) ) ;
#173045=CARTESIAN_POINT ( 'NONE',  ( 0.5381063436600447281, -1.494009556959356999, 0.8925505203737462701 ) ) ;
#173046=CARTESIAN_POINT ( 'NONE',  ( 6.827182134110233669, 2.103728865748891508, 2.021873693915546610 ) ) ;
#173051=CARTESIAN_POINT ( 'NONE',  ( 4.680646922328831394, -2.095996545452833981, -0.5284188670612932626 ) ) ;
#173054=CARTESIAN_POINT ( 'NONE',  ( 5.149767453795408123, -0.2439937967673235231, -2.001204641050558397 ) ) ;
#173056=CARTESIAN_POINT ( 'NONE',  ( 3.239309987758617115, -1.907233169736745060, 1.017530501952010447 ) ) ;
#173057=CARTESIAN_POINT ( 'NONE',  ( 4.094965523422711584, 1.667053662060855812, -1.051937181705852931 ) ) ;
#173059=CARTESIAN_POINT ( 'NONE',  ( 1.325685429717119446, -0.05423940138811130657, 2.307114084963398870 ) ) ;
#173060=CARTESIAN_POINT ( 'NONE',  ( 3.128252755821586906, 1.147704512706015922, -1.711389856620056493 ) ) ;
#173061=CARTESIAN_POINT ( 'NONE',  ( 5.355005569747676830, 0.3749256243090701712, -1.905367961469102811 ) ) ;
#173069=CARTESIAN_POINT ( 'NONE',  ( 2.257103711190447282, -1.706036888594957723, 1.399758388914617013 ) ) ;
#173072=CARTESIAN_POINT ( 'NONE',  ( 6.965691013979927959, -0.4331334938386353084, 1.920344510276907890 ) ) ;
#173073=CARTESIAN_POINT ( 'NONE',  ( 6.539320575229256249, 7.052319431262985105, 2.701414634427783845 ) ) ;
#173078=CARTESIAN_POINT ( 'NONE',  ( 5.736236344406846932, 0.3633543575551900773, 1.804753862313414281 ) ) ;
#173080=CARTESIAN_POINT ( 'NONE',  ( 2.606383665309390363, -0.7875068868475536554, -1.904698518741376079 ) ) ;
#173087=CARTESIAN_POINT ( 'NONE',  ( 0.6728171419645075924, -1.940266777691628919, -0.6950667680841491336 ) ) ;
#173089=CARTESIAN_POINT ( 'NONE',  ( 5.020983453748395497, -1.746657797055195305, 0.5827527221545365510 ) ) ;
#173094=CARTESIAN_POINT ( 'NONE',  ( 3.950008152305323428, 0.7444041667201054535, -2.077678867657362538 ) ) ;
#173095=CARTESIAN_POINT ( 'NONE',  ( 0.8257154465432202661, -2.052837714267462754, 0.6772920067378007669 ) ) ;
#173097=CARTESIAN_POINT ( 'NONE',  ( -0.1581436608063293003, -1.178060542814472367, -1.506996232563104776 ) ) ;
#173098=CARTESIAN_POINT ( 'NONE',  ( 0.7961116948485976730, -0.9110139862544311962, -1.799120828532501326 ) ) ;
#173100=CARTESIAN_POINT ( 'NONE',  ( 1.722429217803717938, -1.971362081364759655, -1.181495133065799230 ) ) ;
#173102=CARTESIAN_POINT ( 'NONE',  ( 6.498695769366850783, -1.876353784076413067, -0.3680397143606057853 ) ) ;
#173105=CARTESIAN_POINT ( 'NONE',  ( 0.2681426532152464959, -1.225442487749365483, 1.413462724991432218 ) ) ;
#173106=CARTESIAN_POINT ( 'NONE',  ( 2.870327622459168726, -1.987497926849005836, -0.3399570244180456502 ) ) ;
#173110=CARTESIAN_POINT ( 'NONE',  ( 4.055375990838584244, -1.750834834141304697, -1.170193647660602965 ) ) ;
#173115=CARTESIAN_POINT ( 'NONE',  ( 4.535418805095452477, -0.09482428102505417733, 2.017666594091566346 ) ) ;
#173119=CARTESIAN_POINT ( 'NONE',  ( 4.657600047955182454, 0.4785990281669267876, -2.107782517917502929 ) ) ;
#173125=CARTESIAN_POINT ( 'NONE',  ( 1.574930973106080545, 1.458645925580204006, -1.608354241196547685 ) ) ;
#173128=CARTESIAN_POINT ( 'NONE',  ( 0.3273695209934923689, 0.9472894719858866441, -1.578709817245539604 ) ) ;
#173130=CARTESIAN_POINT ( 'NONE',  ( 3.333693798916517625, 0.9835563995168915552, -1.958507884819527867 ) ) ;
#173132=CARTESIAN_POINT ( 'NONE',  ( 3.467884472470097457, 2.207893551020873257, -0.4935151710872084929 ) ) ;
#173139=CARTESIAN_POINT ( 'NONE',  ( 3.778344457583324711, -1.704853921413415296, -0.4744283172272641957 ) ) ;
#173141=CARTESIAN_POINT ( 'NONE',  ( 0.9210891864466156376, 1.945811402625597486, 0.8060233215861163369 ) ) ;
#173144=CARTESIAN_POINT ( 'NONE',  ( 0.6253724811571198527, 0.1964764651697422093, -1.959740272926189464 ) ) ;
#173147=CARTESIAN_POINT ( 'NONE',  ( 5.291193953664572902, -0.05252268709225348109, -1.811016617013387009 ) ) ;
#173151=CARTESIAN_POINT ( 'NONE',  ( 4.539837415608827698, 0.7997722286730184482, -1.691214532891088362 ) ) ;
#173154=CARTESIAN_POINT ( 'NONE',  ( 4.100488025649267954, 2.059819936833905185, 0.2079151390043249559 ) ) ;
#173156=( BOUNDED_SURFACE ( )  B_SPLINE_SURFACE ( 3, 3, ( 
 ( #142918, #172192, #23781, #109388, #207863, #206798, #76797, #125644, #58431, #89887 ),
 ( #189492, #108316, #155938, #208918, #158081, #59487, #57365, #191606, #10727, #122462 ),
 ( #43268, #60552, #157015, #72530, #175393, #141856, #41136, #173267, #7524, #26979 ),
 ( #110448, #73607, #93084, #159126, #90948, #74683, #139706, #8599, #140784, #188420 ),
 ( #205729, #192672, #126712, #40056, #138627, #174337, #44326, #124584, #22700, #88812 ),
 ( #107246, #154870, #123527, #6453, #25915, #190544, #204651, #42201, #92023, #9668 ),
 ( #56300, #75744, #196953, #147161, #180704, #162336, #211052, #177516, #29129, #32327 ) ),
 .UNSPECIFIED., .T., .F., .T. ) 
 B_SPLINE_SURFACE_WITH_KNOTS ( ( 4, 3, 4 ),
 ( 4, 1, 1, 1, 1, 1, 1, 4 ),
 ( 0.000000000000000000, 0.5000000000000000000, 1.000000000000000000 ),
 ( 0.000000000000000000, 0.09272347919791326665, 0.1850049962306132278, 0.2567072177207115891, 0.3610482009861257779, 0.5209239196176974618, 0.7336689415868371533, 1.000000000000000000 ),
 .UNSPECIFIED. ) 
 GEOMETRIC_REPRESENTATION_ITEM ( )  RATIONAL_B_SPLINE_SURFACE ( (
 ( 1.000000000000000444, 1.000000000000000444, 1.000000000000000222, 1.000000000000000444, 1.000000000000000222, 1.000000000000000444, 1.000000000000000222, 1.000000000000000222, 1.000000000000000222, 1.000000000000000222),
 ( 0.3333333333333334814, 0.3333333333333335369, 0.3333333333333334814, 0.3333333333333334259, 0.3333333333333334259, 0.3333333333333334259, 0.3333333333333334259, 0.3333333333333334259, 0.3333333333333334259, 0.3333333333333334259),
 ( 0.3333333333333334814, 0.3333333333333335369, 0.3333333333333334814, 0.3333333333333334259, 0.3333333333333334259, 0.3333333333333334259, 0.3333333333333334259, 0.3333333333333334259, 0.3333333333333334259, 0.3333333333333334259),
 ( 1.000000000000000444, 1.000000000000000444, 1.000000000000000222, 1.000000000000000444, 1.000000000000000222, 1.000000000000000444, 1.000000000000000222, 1.000000000000000222, 1.000000000000000222, 1.000000000000000222),
 ( 0.3333333333333334814, 0.3333333333333335369, 0.3333333333333334814, 0.3333333333333334259, 0.3333333333333334259, 0.3333333333333334259, 0.3333333333333334259, 0.3333333333333334259, 0.3333333333333334259, 0.3333333333333334259),
 ( 0.3333333333333334814, 0.3333333333333335369, 0.3333333333333334814, 0.3333333333333334259, 0.3333333333333334259, 0.3333333333333334259, 0.3333333333333334259, 0.3333333333333334259, 0.3333333333333334259, 0.3333333333333334259),
 ( 1.000000000000000444, 1.000000000000000444, 1.000000000000000222, 1.000000000000000444, 1.000000000000000222, 1.000000000000000444, 1.000000000000000222, 1.000000000000000222, 1.000000000000000222, 1.000000000000000222) ) ) 
 REPRESENTATION_ITEM ( '' )  SURFACE ( )  );
#173167=CARTESIAN_POINT ( 'NONE',  ( 4.017981030900905637, 1.947309607215493621, -0.2378496960543720617 ) ) ;
#173169=CARTESIAN_POINT ( 'NONE',  ( 2.091172504846372959, 1.163092143266548639, -1.646586049616038494 ) ) ;
#173171=CARTESIAN_POINT ( 'NONE',  ( -0.1290005225502675879, -0.006633637972621592160, -2.173875058097324064 ) ) ;
#173172=CARTESIAN_POINT ( 'NONE',  ( 2.002991962376502233, 1.552455721610061179, 1.043161660468715279 ) ) ;
#173175=CARTESIAN_POINT ( 'NONE',  ( 2.812237032231167611, 1.173781612916646289, -1.761886306039317285 ) ) ;
#173177=CARTESIAN_POINT ( 'NONE',  ( 5.125469573878929097, 0.2063957376101481500, -2.060066405364005426 ) ) ;
#173179=CARTESIAN_POINT ( 'NONE',  ( 0.3102505407175432661, 1.438864707272140775, -1.517118456267575022 ) ) ;
#173180=CARTESIAN_POINT ( 'NONE',  ( 6.620655732516649294, 2.950034989283246478, 2.626075342966327497 ) ) ;
#173181=CARTESIAN_POINT ( 'NONE',  ( 5.368107995252269227, 0.9013511576922846880, 1.587453057759043551 ) ) ;
#173189=CARTESIAN_POINT ( 'NONE',  ( 5.795548653916324788, 1.765151677092157811, -0.7360495477024899813 ) ) ;
#173199=CARTESIAN_POINT ( 'NONE',  ( 5.290638740200859225, 1.525033539048275877, -1.319242139327673424 ) ) ;
#173205=CARTESIAN_POINT ( 'NONE',  ( 2.272252165359678333, -0.9238012212633615050, -1.739302338446031548 ) ) ;
#173206=CARTESIAN_POINT ( 'NONE',  ( 5.009388752257521560, -1.913799287717246500, 0.6352160319311253023 ) ) ;
#173208=CARTESIAN_POINT ( 'NONE',  ( 6.827182134110238110, 0.5514785450725538940, 2.340047124761033714 ) ) ;
#173209=CARTESIAN_POINT ( 'NONE',  ( 5.068408068084750973, -2.062719301109996461, -0.7404068969242217912 ) ) ;
#173211=CARTESIAN_POINT ( 'NONE',  ( 2.942313797947668785, 1.911627860423757097, 0.2376154225440275658 ) ) ;
#173221=CARTESIAN_POINT ( 'NONE',  ( 5.899929530298204661, -0.6689130865737795695, -1.715630562827724637 ) ) ;
#173222=CARTESIAN_POINT ( 'NONE',  ( 2.420566579892877268, -0.7724838186086988578, -1.859170112617714699 ) ) ;
#173223=CARTESIAN_POINT ( 'NONE',  ( 5.765083458594993715, -2.298542321979883507, -0.008455817729055568541 ) ) ;
#173224=CARTESIAN_POINT ( 'NONE',  ( 2.834617457269935414, -1.779228943046967437, -0.5452927797432933765 ) ) ;
#173226=CARTESIAN_POINT ( 'NONE',  ( -0.1290005225502433017, 0.6921039065478848951, -2.255494067288220439 ) ) ;
#173227=CARTESIAN_POINT ( 'NONE',  ( 6.533470333208203584, -0.1312131129157616261, 1.882018712217728318 ) ) ;
#173230=CARTESIAN_POINT ( 'NONE',  ( 6.198786912940476235, 1.738631647849303130, 1.160874564816395615 ) ) ;
#173236=CARTESIAN_POINT ( 'NONE',  ( 6.568995754424670430, -1.580519633186812767, -0.6912669513192554183 ) ) ;
#173240=CARTESIAN_POINT ( 'NONE',  ( 0.9494047574800461575, -1.567277312892487284, -0.7424874142042283687 ) ) ;
#173244=CARTESIAN_POINT ( 'NONE',  ( 5.383699271828307431, -2.063871618437407740, 0.6740922461795120224 ) ) ;
#173245=CARTESIAN_POINT ( 'NONE',  ( 4.705575438601840688, -0.4840451379145363497, 1.760283039881085809 ) ) ;
#173246=CARTESIAN_POINT ( 'NONE',  ( 2.166782468979636000, 1.457124453068344039, -1.313723524322525815 ) ) ;
#173250=CARTESIAN_POINT ( 'NONE',  ( 3.352298257493666167, 0.9517314053594098100, -1.894962337767625904 ) ) ;
#173254=CARTESIAN_POINT ( 'NONE',  ( 2.043885321627556095, 1.424625833772466210, 1.502381739045772546 ) ) ;
#173257=CARTESIAN_POINT ( 'NONE',  ( 3.387547421374631273, 0.05309406834838430178, -2.220816570709438498 ) ) ;
#173259=CARTESIAN_POINT ( 'NONE',  ( 2.250986472945924355, 2.253575863342609065, -0.4525425749238082829 ) ) ;
#173261=CARTESIAN_POINT ( 'NONE',  ( 6.948098685450462497, -0.8862217868219750549, 1.860397500250488001 ) ) ;
#173267=CARTESIAN_POINT ( 'NONE',  ( -0.1102773484823963285, 5.719690680991945442, -2.797532285072940272 ) ) ;
#173268=CARTESIAN_POINT ( 'NONE',  ( 2.959633327367673150, 1.716642837065301519, -0.1670560860976433859 ) ) ;
#173269=CARTESIAN_POINT ( 'NONE',  ( 2.255092540634635156, 0.09411513195021346811, -2.014433103604281960 ) ) ;
#173270=CARTESIAN_POINT ( 'NONE',  ( 2.989241104188970155, -2.295904969233518500, 0.1156830036863568528 ) ) ;
#173271=CARTESIAN_POINT ( 'NONE',  ( 3.813984095001612395, -2.229740912845196377, 0.3821933647679372492 ) ) ;
#173272=CARTESIAN_POINT ( 'NONE',  ( 5.637368906844186789, -1.904612104999114708, 0.8991850809280316215 ) ) ;
#173274=CARTESIAN_POINT ( 'NONE',  ( 3.268565602506213974, -1.633896335792903054, -0.6804537918285047393 ) ) ;
#173276=CARTESIAN_POINT ( 'NONE',  ( 6.497627784488766878, -2.291974509058695375, 0.05125074467529803363 ) ) ;
#173277=CARTESIAN_POINT ( 'NONE',  ( 5.279192629422701621, 1.239228542960477242, 1.361826556748657602 ) ) ;
#173279=CARTESIAN_POINT ( 'NONE',  ( 5.490230790444213582, -0.5297859672059505032, -2.126319610106224278 ) ) ;
#173282=CARTESIAN_POINT ( 'NONE',  ( 5.582505937350194181, 1.236201877336528643, -1.660625051266072960 ) ) ;
#173283=CARTESIAN_POINT ( 'NONE',  ( -0.2234322562767385167, -0.4468160588090731022, -1.973564571300358228 ) ) ;
#173285=CARTESIAN_POINT ( 'NONE',  ( 3.861874329138580197, 1.911805356762337205, -0.2370204922254297297 ) ) ;
#173288=CARTESIAN_POINT ( 'NONE',  ( -0.06965283525045895541, -2.176852707449424607, 0.4419662969857121038 ) ) ;
#173297=CARTESIAN_POINT ( 'NONE',  ( 0.9241798626423224361, 0.9638202082158978667, 1.708698881219716137 ) ) ;
#173302=CARTESIAN_POINT ( 'NONE',  ( 5.564887814092526419, 1.486691789297951871, -1.280227714881218892 ) ) ;
#173306=CARTESIAN_POINT ( 'NONE',  ( 0.2513181340676704512, -1.814898432050582766, 1.350810986113021750 ) ) ;
#173310=CARTESIAN_POINT ( 'NONE',  ( 1.967826412060974084, 0.9573937279930484490, 1.606809688844474726 ) ) ;
#173311=CARTESIAN_POINT ( 'NONE',  ( 0.5099215751255279372, -1.647279052675547861, 0.5420907402255652485 ) ) ;
#173313=CARTESIAN_POINT ( 'NONE',  ( 4.054362073078698891, -1.623213109359676443, 1.472610181411204922 ) ) ;
#173314=CARTESIAN_POINT ( 'NONE',  ( 3.962222562901392742, 2.290579029535879219, -0.2790985642298955405 ) ) ;
#173315=CARTESIAN_POINT ( 'NONE',  ( 6.919229409281150822, -0.1609914934341447335, 2.026046322553672674 ) ) ;
#173316=CARTESIAN_POINT ( 'NONE',  ( 2.308448745193259821, 1.734665721750632938, 0.8731161087585439518 ) ) ;
#173320=CARTESIAN_POINT ( 'NONE',  ( 5.537388447972660721, -0.05000006065614125139, 2.120159173171487055 ) ) ;
#173323=CARTESIAN_POINT ( 'NONE',  ( 3.621720349255663773, 0.2986264320336135536, 1.994071497604548382 ) ) ;
#173327=CARTESIAN_POINT ( 'NONE',  ( 1.400715809426569702, 1.493624456287694358, -1.049586478250638999 ) ) ;
#173332=CARTESIAN_POINT ( 'NONE',  ( 5.348532861604016198, 0.5962098156395375659, 1.972770010162463228 ) ) ;
#173337=CARTESIAN_POINT ( 'NONE',  ( 4.108072977939541737, -0.7709450260172491243, 1.866947522544240901 ) ) ;
#173338=CARTESIAN_POINT ( 'NONE',  ( 6.252596820807392319, 2.196675488376065744, 0.3289990992049235397 ) ) ;
#173342=CARTESIAN_POINT ( 'NONE',  ( 4.012614562483146408, 1.458688259485216854, -1.456115939812257620 ) ) ;
#173343=CARTESIAN_POINT ( 'NONE',  ( 4.500625067706437221, -1.976956227568788638, 0.3961002554062897918 ) ) ;
#173351=CARTESIAN_POINT ( 'NONE',  ( 3.725935337077026510, -1.776739457207517248, -0.9528653653038119398 ) ) ;
#173352=CARTESIAN_POINT ( 'NONE',  ( 2.273173984786102775, 1.132353773513800510, 1.451651336590239927 ) ) ;
#173353=CARTESIAN_POINT ( 'NONE',  ( 1.348709242277994269, 2.305235852375675076, 0.1091458774659745806 ) ) ;
#173355=CARTESIAN_POINT ( 'NONE',  ( 3.497504216883956296, 1.701635573755799324, 1.332874705691905248 ) ) ;
#173360=CARTESIAN_POINT ( 'NONE',  ( 2.149089010626914931, -1.500894351328721621, -1.116326037436713881 ) ) ;
#173361=CARTESIAN_POINT ( 'NONE',  ( 5.313337694394675736, -0.2901137614541632881, 1.949896409304814116 ) ) ;
#173365=CARTESIAN_POINT ( 'NONE',  ( 0.2236267563471248943, -0.1037379595543522215, 2.204571545119632603 ) ) ;
#173370=CARTESIAN_POINT ( 'NONE',  ( 6.192255011402767018, -1.961924197356275323, -0.1938383548326528261 ) ) ;
#173371=CARTESIAN_POINT ( 'NONE',  ( 5.672612835131308984, -1.468196381517340665, 1.780430754307258390 ) ) ;
#173372=CARTESIAN_POINT ( 'NONE',  ( 6.812964112091245639, -1.437450002374938585, 1.181853997439401116 ) ) ;
#173373=CARTESIAN_POINT ( 'NONE',  ( 3.116140835343351956, 2.053043485406472080, -0.1977005638095686579 ) ) ;
#173375=EDGE_CURVE ( 'NONE', #90486, #157709, #55963, .T. ) ;
#173381=CARTESIAN_POINT ( 'NONE',  ( 5.529782829607038153, 2.093976201882574273, -0.5736635526294631138 ) ) ;
#173382=CARTESIAN_POINT ( 'NONE',  ( 3.028530041973789722, 0.4946322284519070189, 1.954779462066410733 ) ) ;
#173384=CARTESIAN_POINT ( 'NONE',  ( 5.390138975101268493, -0.4531076923771395482, -1.784498753146485539 ) ) ;
#173386=CARTESIAN_POINT ( 'NONE',  ( 6.720655732516684466, 7.052972427687314472, 2.524416814197846914 ) ) ;
#173387=CARTESIAN_POINT ( 'NONE',  ( 6.444889499930222421, -1.758869480593090673, -1.307235502039267860 ) ) ;
#173389=CARTESIAN_POINT ( 'NONE',  ( 6.789870067575622947, -0.9739125386618008307, 2.039881742057749303 ) ) ;
#173394=CARTESIAN_POINT ( 'NONE',  ( 0.3637282827039616251, 0.5997036651611362679, -1.815894722023647656 ) ) ;
#173396=CARTESIAN_POINT ( 'NONE',  ( 1.938023551401172773, 1.750023271871611996, 0.2632672158595899536 ) ) ;
#173398=CARTESIAN_POINT ( 'NONE',  ( 5.953776513178359764, -1.459723235216038750, -1.386512712134661207 ) ) ;
#173399=CARTESIAN_POINT ( 'NONE',  ( 5.579168075997259280, -0.04836659121091852614, -2.105573489274599197 ) ) ;
#173401=CARTESIAN_POINT ( 'NONE',  ( 3.356958492073054412, 0.04375785802200299335, -1.915270648069177462 ) ) ;
#173404=CARTESIAN_POINT ( 'NONE',  ( 3.824621415324851892, -1.324631885467566716, 1.457714561274085163 ) ) ;
#173405=CARTESIAN_POINT ( 'NONE',  ( 0.08834397731360790762, 1.226219587655341448, 1.729930300845914815 ) ) ;
#173407=CARTESIAN_POINT ( 'NONE',  ( 2.395189659270926086, 1.444574673180216706, 1.188490415850687265 ) ) ;
#173408=CARTESIAN_POINT ( 'NONE',  ( 5.338411986983877533, 1.700291985010034201, 0.2892061366746317419 ) ) ;
#173409=ORIENTED_EDGE ( 'NONE', *, *, #3142, .F. ) ;
#173410=CARTESIAN_POINT ( 'NONE',  ( 2.174722684859807575, -1.356406721008751814, 1.740749382485320407 ) ) ;
#173413=CARTESIAN_POINT ( 'NONE',  ( 6.584431417889404337, 1.130572321132311098, -1.603143135845342515 ) ) ;
#173420=CARTESIAN_POINT ( 'NONE',  ( 1.504437137538238600, 2.067909592606699487, 0.1035681241481553605 ) ) ;
#173424=CARTESIAN_POINT ( 'NONE',  ( 0.1178396879437521028, -0.5365784638422869124, 1.947031292057841645 ) ) ;
#173431=CARTESIAN_POINT ( 'NONE',  ( 5.870470189955956819, -0.4925641237488035395, 1.954873771647095415 ) ) ;
#173432=CARTESIAN_POINT ( 'NONE',  ( 4.364398177449787752, -1.859642558872817375, -0.4596742015197906595 ) ) ;
#173434=CARTESIAN_POINT ( 'NONE',  ( 2.665787806004876970, 1.174844384069907655, 1.849873475113596566 ) ) ;
#173437=CARTESIAN_POINT ( 'NONE',  ( 2.689602200614676697, 1.814610489020528350, -0.6038049036062518304 ) ) ;
#173441=CARTESIAN_POINT ( 'NONE',  ( 6.362923164919582319, -0.1041218986313949546, -2.114803170081226646 ) ) ;
#173443=CARTESIAN_POINT ( 'NONE',  ( 5.601184584505256581, -0.5335315006234629953, 2.125516261704554211 ) ) ;
#173445=CARTESIAN_POINT ( 'NONE',  ( 2.713528120726243831, -1.706327644498882634, 0.2505720552260106149 ) ) ;
#173449=DIRECTION ( 'NONE',  ( -0.9999980456341538426, 0.000000000000000000, -0.001977050295958626691 ) ) ;
#173457=CARTESIAN_POINT ( 'NONE',  ( 3.228980503213836339, 1.638859372766150679, 0.7719998214037685491 ) ) ;
#173461=CARTESIAN_POINT ( 'NONE',  ( 4.143061475816012695, 0.09292765117045087564, 1.809223169447377710 ) ) ;
#173467=CARTESIAN_POINT ( 'NONE',  ( 4.685918305224146430, -1.144368955370359098, -1.467557204495354872 ) ) ;
#173469=CARTESIAN_POINT ( 'NONE',  ( 1.476048981871850518, -1.906537803873010084, -0.1858940877890648546 ) ) ;
#173470=CARTESIAN_POINT ( 'NONE',  ( 1.219449367515994309, -1.782015241123528826, 0.3957228718986585680 ) ) ;
#173480=CARTESIAN_POINT ( 'NONE',  ( 5.559413648769178096, 1.607788300429791262, 1.137107417019854072 ) ) ;
#173483=CARTESIAN_POINT ( 'NONE',  ( 0.9375778709549039691, 0.8456052968917522339, -1.912177616049218098 ) ) ;
#173484=CARTESIAN_POINT ( 'NONE',  ( 0.2526013166088726392, -1.469656019175567208, 1.082793315970068004 ) ) ;
#173486=CARTESIAN_POINT ( 'NONE',  ( 1.553431815599433108, 0.5335803070953272220, -1.745854899344486233 ) ) ;
#173487=CARTESIAN_POINT ( 'NONE',  ( 2.877765823869771644, 2.095344539500657799, -0.6929138170133213315 ) ) ;
#173489=CARTESIAN_POINT ( 'NONE',  ( 1.336036003918249948, -1.064896177285217016, -1.588262137521757822 ) ) ;
#173491=CARTESIAN_POINT ( 'NONE',  ( 1.469134468336911192, 1.735519167469494084, 0.9312130504785380847 ) ) ;
#173492=CARTESIAN_POINT ( 'NONE',  ( 2.560020840168964806, -1.337455066581024976, 1.408356088163305042 ) ) ;
#173496=CARTESIAN_POINT ( 'NONE',  ( 6.227394082031683986, 0.1379007965640146050, -1.855924616290964169 ) ) ;
#173501=CARTESIAN_POINT ( 'NONE',  ( 2.648187065138879692, 0.7411268365287645432, 2.062558662443473523 ) ) ;
#173505=CARTESIAN_POINT ( 'NONE',  ( 3.000428103051573814, -0.5303778429210231904, -1.746945217264872507 ) ) ;
#173506=CARTESIAN_POINT ( 'NONE',  ( 5.876185452347599814, -2.007255679753978228, -0.1928398672442974138 ) ) ;
#173512=CARTESIAN_POINT ( 'NONE',  ( 1.963383859451812041, 0.3296633872902128282, -1.897934821152784446 ) ) ;
#173513=CARTESIAN_POINT ( 'NONE',  ( 5.700043108275813175, 0.7984002208856562088, -1.792138013221859394 ) ) ;
#173522=CARTESIAN_POINT ( 'NONE',  ( 5.717656431054087385, 0.4094431674900833595, -2.029196096928844284 ) ) ;
#173526=CARTESIAN_POINT ( 'NONE',  ( 4.992985585870878928, -2.287786813913486039, 0.2239274308311194894 ) ) ;
#173530=CARTESIAN_POINT ( 'NONE',  ( 6.515150198369638268, -2.224820657066893137, 0.5519656782505685255 ) ) ;
#173533=CARTESIAN_POINT ( 'NONE',  ( 5.455005553751488989, 0.3768678912985870544, -1.904869181234331910 ) ) ;
#173537=CARTESIAN_POINT ( 'NONE',  ( 6.029550621839829816, -0.2273517531893587407, 1.898748578088353733 ) ) ;
#173538=CARTESIAN_POINT ( 'NONE',  ( 6.176716277887216222, -1.639393978788429740, -0.5360894954027517478 ) ) ;
#173539=CARTESIAN_POINT ( 'NONE',  ( 5.876185452347599814, -2.007255679753978228, -0.1928398672442974138 ) ) ;
#173543=CARTESIAN_POINT ( 'NONE',  ( 1.728581982081365265, 0.2060769881795926906, 2.080452860985905428 ) ) ;
#173544=CARTESIAN_POINT ( 'NONE',  ( 0.09216213259799833912, -0.3764253007602496592, -1.735191564994809976 ) ) ;
#173547=CARTESIAN_POINT ( 'NONE',  ( 3.820531118927258607, 2.176299813863972865, 0.7200661129266039406 ) ) ;
#173548=CARTESIAN_POINT ( 'NONE',  ( 2.097218849865792212, -1.740012409040556429, 0.04131442251954255129 ) ) ;
#173549=CARTESIAN_POINT ( 'NONE',  ( 2.900754761704402274, -2.089926006748676457, -0.3584049868644647585 ) ) ;
#173551=CARTESIAN_POINT ( 'NONE',  ( 2.301686711942134256, -1.551025276819127496, 0.7750448480700108389 ) ) ;
#173553=CARTESIAN_POINT ( 'NONE',  ( 6.333220217719927270, -1.622483202430196725, -1.197309987464048486 ) ) ;
#173554=CARTESIAN_POINT ( 'NONE',  ( 1.978732740145513480, 1.735006779315110492, 0.6737207639663128633 ) ) ;
#173555=CARTESIAN_POINT ( 'NONE',  ( 2.682273331476907607, -1.248350377418592672, -1.776241996044833238 ) ) ;
#173557=CARTESIAN_POINT ( 'NONE',  ( 3.731657894805060938, 0.6748485617756972976, -1.900415309456899182 ) ) ;
#173558=CARTESIAN_POINT ( 'NONE',  ( 3.312500000000002220, 1.451031289061251339, 1.451031289060983998 ) ) ;
#173561=CARTESIAN_POINT ( 'NONE',  ( 0.9031967280443575774, 1.573137106080691572, 1.111599351221918663 ) ) ;
#173563=CARTESIAN_POINT ( 'NONE',  ( 4.324628213192062809, -0.9515899357304625772, -2.007430035002121471 ) ) ;
#173570=CARTESIAN_POINT ( 'NONE',  ( 5.783471039277606529, 0.1639875503032099946, -2.215378355603670357 ) ) ;
#173571=CARTESIAN_POINT ( 'NONE',  ( 5.072687121480487171, 1.354251660176824856, -1.419695456575476689 ) ) ;
#173577=CARTESIAN_POINT ( 'NONE',  ( 5.870491743106223126, -1.441790217864300283, 1.743476569090945061 ) ) ;
#173579=CARTESIAN_POINT ( 'NONE',  ( 3.227062719040986405, -1.904794013395166186, -0.7919108894221676964 ) ) ;
#173584=CARTESIAN_POINT ( 'NONE',  ( 4.938664768831325880, 0.3182328507864223277, 1.843102042236575588 ) ) ;
#173585=CARTESIAN_POINT ( 'NONE',  ( 3.164447786964882603, 1.103041557463914524, 1.338080049202054145 ) ) ;
#173586=CARTESIAN_POINT ( 'NONE',  ( 1.979654113181174901, -1.706931329119738772, -0.3388794841660112689 ) ) ;
#173587=CARTESIAN_POINT ( 'NONE',  ( 0.7852321044731135347, 2.018311417075705272, -1.086964541883679303 ) ) ;
#173588=CARTESIAN_POINT ( 'NONE',  ( 1.395868886378356821, 1.671639904693554168, 1.440724375100350008 ) ) ;
#173589=CARTESIAN_POINT ( 'NONE',  ( 4.159774813393120496, 0.9870934738810345221, 1.843074783240926884 ) ) ;
#173590=CARTESIAN_POINT ( 'NONE',  ( 6.105412738798914773, -1.926975682693391700, 0.2402159021005992046 ) ) ;
#173594=CARTESIAN_POINT ( 'NONE',  ( 0.08851783505585240908, -0.5350849913869708541, 1.944072358963434555 ) ) ;
#173600=CARTESIAN_POINT ( 'NONE',  ( 4.283705427790140519, 1.194290084605063251, 1.380960126487425166 ) ) ;
#173601=CARTESIAN_POINT ( 'NONE',  ( 1.747397587315655088, -1.864034986486883039, 1.180896971623420999 ) ) ;
#173607=CARTESIAN_POINT ( 'NONE',  ( 1.248313549685893475, 0.9916667988653109500, -1.759473928524292630 ) ) ;
#173610=CARTESIAN_POINT ( 'NONE',  ( 2.676407432925419272, 1.219717815897247259, -1.405545362062944559 ) ) ;
#173616=CARTESIAN_POINT ( 'NONE',  ( 4.318856058802469811, 1.670182456744148336, 0.7377305746401884301 ) ) ;
#173620=CARTESIAN_POINT ( 'NONE',  ( 1.053531109644106678, 1.532759392139435128, -0.8104334526845609066 ) ) ;
#173621=CARTESIAN_POINT ( 'NONE',  ( 5.788959344212086577, 1.397023377451442228, 1.199316859253784839 ) ) ;
#173622=CARTESIAN_POINT ( 'NONE',  ( 4.828937647557053126, 2.207305988086407655, 0.6732806465959675357 ) ) ;
#173624=CARTESIAN_POINT ( 'NONE',  ( 6.819591527820957566, -2.098570527662356522, 0.5178885164088961046 ) ) ;
#173626=CARTESIAN_POINT ( 'NONE',  ( 5.571695488097110349, 1.745893177897942738, -1.494929824115182937 ) ) ;
#173629=CARTESIAN_POINT ( 'NONE',  ( 6.227412191919261986, -1.760757567598171480, 0.6321290105378990498 ) ) ;
#173631=CARTESIAN_POINT ( 'NONE',  ( 2.091926199050548441, 1.179367891222588005, 1.505316542580182659 ) ) ;
#173633=CARTESIAN_POINT ( 'NONE',  ( 4.336686996305870068, 2.164023489887345164, 0.4319772483800735086 ) ) ;
#173634=CARTESIAN_POINT ( 'NONE',  ( 4.645784029343587918, 2.093824292288968270, -0.3141051717527267861 ) ) ;
#173636=CARTESIAN_POINT ( 'NONE',  ( 6.883263157960391787, -0.001104538646235289417, 1.946037152736757925 ) ) ;
#173639=CARTESIAN_POINT ( 'NONE',  ( 2.643975807074511408, -1.709602402607094396, -1.550068159870971574 ) ) ;
#173640=CARTESIAN_POINT ( 'NONE',  ( 4.017981030900905637, 1.947309607215493621, -0.2378496960543720617 ) ) ;
#173642=CARTESIAN_POINT ( 'NONE',  ( 6.121949867982135807, 2.033011618171334245, -0.3470327977990442792 ) ) ;
#173646=CARTESIAN_POINT ( 'NONE',  ( 6.192592252150040721, 1.490973663936447258, -1.357864438797616868 ) ) ;
#173651=CARTESIAN_POINT ( 'NONE',  ( 1.885821443427546207, -2.045346407173433967, 0.7285060392495151804 ) ) ;
#173656=CARTESIAN_POINT ( 'NONE',  ( 1.388040899126226302, -0.9290452130323262336, 1.839580399304826752 ) ) ;
#173659=CARTESIAN_POINT ( 'NONE',  ( 6.727182134110164746, 4.698490487241143043, 2.473633340027088678 ) ) ;
#173663=CARTESIAN_POINT ( 'NONE',  ( 3.440010667329951310, -1.141173813254949820, -1.534285795567114974 ) ) ;
#173664=CARTESIAN_POINT ( 'NONE',  ( 4.908955397393719444, 1.540865433829426090, 0.8705488387463419242 ) ) ;
#173668=CARTESIAN_POINT ( 'NONE',  ( 6.222283718431360633, 1.895538691748376081, 0.2756032664797089526 ) ) ;
#173670=CARTESIAN_POINT ( 'NONE',  ( 1.012269475826784060, 2.068064858651061932, -0.09981174449213289779 ) ) ;
#173672=CARTESIAN_POINT ( 'NONE',  ( 6.737182200980119440, -1.669782060861616291, 0.8434366901180423426 ) ) ;
#173673=CARTESIAN_POINT ( 'NONE',  ( 3.387140609607977026, 1.650079954178599539, -0.7815607168924765258 ) ) ;
#173674=CARTESIAN_POINT ( 'NONE',  ( 5.918643953348324160, 1.484978324971843566, -1.632713241052483832 ) ) ;
#173677=CARTESIAN_POINT ( 'NONE',  ( 2.699736158553706300, -1.526808845971421968, -1.387057796406083732 ) ) ;
#173681=CARTESIAN_POINT ( 'NONE',  ( 0.6323695665565836066, 1.111747700424435159, -1.853661729306683936 ) ) ;
#173683=CARTESIAN_POINT ( 'NONE',  ( 5.424307079040114665, 1.017280057988108499, 1.803113764695261523 ) ) ;
#173685=CARTESIAN_POINT ( 'NONE',  ( 4.095124908492456584, 1.828510582809875107, -1.152538879107746439 ) ) ;
#173687=CARTESIAN_POINT ( 'NONE',  ( 2.631515421131935817, -0.1955963300145530936, 2.010161875231412765 ) ) ;
#173688=CARTESIAN_POINT ( 'NONE',  ( 2.137090596337941406, -0.09316805448006218460, -1.959763546484971197 ) ) ;
#173689=CARTESIAN_POINT ( 'NONE',  ( 6.620655732516625314, 7.629137130509059617, 2.773739711112707340 ) ) ;
#173694=CARTESIAN_POINT ( 'NONE',  ( 1.270720652900014791, -0.3006520276036573902, -1.993892820393451615 ) ) ;
#173696=CARTESIAN_POINT ( 'NONE',  ( 6.163654587501778970, 1.125051486859941718, 1.880622087419632882 ) ) ;
#173698=CARTESIAN_POINT ( 'NONE',  ( 5.449440537890919423, -1.726199344983204043, 0.8234401749890254418 ) ) ;
#173703=CARTESIAN_POINT ( 'NONE',  ( 3.515250061227533696, -1.862011288300661871, 0.7743320027404425598 ) ) ;
#173706=CARTESIAN_POINT ( 'NONE',  ( 6.633849695589691287, -1.131556152058693865, -1.301821263952767316 ) ) ;
#173710=CARTESIAN_POINT ( 'NONE',  ( 4.850782132498069998, -1.503350029756752804, 1.112868480285071460 ) ) ;
#173712=CARTESIAN_POINT ( 'NONE',  ( 2.694261129275489886, 0.9798316074655871732, -1.823736424811234658 ) ) ;
#173717=CARTESIAN_POINT ( 'NONE',  ( 0.3338568476279568653, -0.9693210200989417213, -1.530242633214883963 ) ) ;
#173721=CARTESIAN_POINT ( 'NONE',  ( 1.855835942623608181, -0.6640040153468586004, 1.846199708051485811 ) ) ;
#173723=CARTESIAN_POINT ( 'NONE',  ( 5.747645016999404888, 1.886384853835708642, -0.3323884645628824019 ) ) ;
#173730=CARTESIAN_POINT ( 'NONE',  ( 2.729541802387557059, -2.017400560480298033, 0.7770373237434914371 ) ) ;
#173733=CARTESIAN_POINT ( 'NONE',  ( -0.06985027309261250539, -2.078401542846250116, 0.4200961532789050379 ) ) ;
#173734=CARTESIAN_POINT ( 'NONE',  ( 5.280226139177822908, -1.012770463184736736, 1.518683248463777113 ) ) ;
#173736=CARTESIAN_POINT ( 'NONE',  ( 1.405477211469996934, -0.4828617686813937993, 1.911177332403845464 ) ) ;
#173737=CARTESIAN_POINT ( 'NONE',  ( 3.445477555875466891, -1.765175379189663607, 0.7362804355328657069 ) ) ;
#173741=CARTESIAN_POINT ( 'NONE',  ( 5.037540015474098354, 1.838441386810828693, -0.7070908002782918533 ) ) ;
#173743=CARTESIAN_POINT ( 'NONE',  ( 6.321825213571911739, 1.114395046473240392, -1.590342819258899532 ) ) ;
#173747=CARTESIAN_POINT ( 'NONE',  ( 6.433838290133602200, -2.056603270127650429, 0.5165238393732355382 ) ) ;
#173749=CARTESIAN_POINT ( 'NONE',  ( 4.090413894173472009, -1.098427525215146749, 1.565146720495188104 ) ) ;
#173751=CARTESIAN_POINT ( 'NONE',  ( 0.8860939741733677710, 1.483344945610004073, 1.634051305214024641 ) ) ;
#173754=CARTESIAN_POINT ( 'NONE',  ( 6.024093331079843239, -1.997604944964962437, 0.2488386476607491182 ) ) ;
#173756=CARTESIAN_POINT ( 'NONE',  ( 5.988856447087389512, -0.2726756491404982441, -1.805090154579996442 ) ) ;
#173757=CARTESIAN_POINT ( 'NONE',  ( 2.418496320782090869, 0.8830982243829659240, 1.872697815963566992 ) ) ;
#173761=CARTESIAN_POINT ( 'NONE',  ( 6.737182200980119440, -1.669782060861616291, 0.8434366901180423426 ) ) ;
#173768=CARTESIAN_POINT ( 'NONE',  ( 6.925078400183550364, 2.979478345347879031, 2.309228228758605450 ) ) ;
#173770=CARTESIAN_POINT ( 'NONE',  ( 5.150864522821732017, 0.8611363216781149355, 1.505151585408972981 ) ) ;
#173774=CARTESIAN_POINT ( 'NONE',  ( 2.483334644719075168, -0.004358110040847408898, 2.070434559716929357 ) ) ;
#173775=CARTESIAN_POINT ( 'NONE',  ( 3.585668865097063840, -0.6122912394212923770, 2.026781372153120930 ) ) ;
#173778=CARTESIAN_POINT ( 'NONE',  ( 1.182395473146230946, 1.177546377092754337, -1.578453288034264990 ) ) ;
#173781=CARTESIAN_POINT ( 'NONE',  ( -0.1054227091227821350, -1.855472971956134920, -0.4628026090111520552 ) ) ;
#173782=CARTESIAN_POINT ( 'NONE',  ( 3.240441643373017211, 0.5569673610456173929, 2.223450396423230391 ) ) ;
#173783=CARTESIAN_POINT ( 'NONE',  ( 1.330379832379691818, 1.758967509726565792, 0.4888242021733391618 ) ) ;
#173787=CARTESIAN_POINT ( 'NONE',  ( 2.865492421389451039, -1.648320183868864364, -1.155634683092461978 ) ) ;
#173788=CARTESIAN_POINT ( 'NONE',  ( 3.625789200213443753, 1.914935786268581852, -0.4253726038727227432 ) ) ;
#173792=CARTESIAN_POINT ( 'NONE',  ( 5.613254157830992241, -2.039858995719573631, 0.4571984828403846124 ) ) ;
#173793=CARTESIAN_POINT ( 'NONE',  ( 4.768267862989370443, -1.154894395163852616, 1.341171105668465646 ) ) ;
#173795=CARTESIAN_POINT ( 'NONE',  ( 0.7092355107721182161, -0.3178641103029449799, 2.168156088950490723 ) ) ;
#173796=CARTESIAN_POINT ( 'NONE',  ( 5.577983363897286218, -1.699187140184825751, -0.3753857801653339710 ) ) ;
#173798=CARTESIAN_POINT ( 'NONE',  ( 6.188148266813070286, 1.908752161701723571, 1.280650486962619627 ) ) ;
#173799=CARTESIAN_POINT ( 'NONE',  ( 0.1333692844072802142, 0.2389375359408679178, -2.087895146362698906 ) ) ;
#173800=CARTESIAN_POINT ( 'NONE',  ( 5.800041802258188106, -1.566351721726914725, 0.7437187281235900782 ) ) ;
#173801=CARTESIAN_POINT ( 'NONE',  ( 5.898927382237683759, 0.4177183949424836396, 2.130464630886391486 ) ) ;
#173803=CARTESIAN_POINT ( 'NONE',  ( 0.4623062725150044461, -1.170719190667910414, 1.764065175548671593 ) ) ;
#173804=CARTESIAN_POINT ( 'NONE',  ( 3.093750000000001776, -1.895863743164152071, -0.7852924748298234503 ) ) ;
#173805=CARTESIAN_POINT ( 'NONE',  ( 6.727182134110234024, 0.5746707207614526469, 2.142055518182262475 ) ) ;
#173806=CARTESIAN_POINT ( 'NONE',  ( 4.155238220467009747, -1.601147421941846227, -1.070839854175157813 ) ) ;
#173808=CARTESIAN_POINT ( 'NONE',  ( 0.9970955524637573619, -2.168350899310825586, -0.4814931055744512411 ) ) ;
#173813=CARTESIAN_POINT ( 'NONE',  ( 3.123905467589927820, -0.4314640245299468657, 2.178836924841739631 ) ) ;
#173815=CARTESIAN_POINT ( 'NONE',  ( -0.02900071798683095947, 5.719935618195115978, -2.767867108847458901 ) ) ;
#173820=CARTESIAN_POINT ( 'NONE',  ( 0.7037502660087076034, 1.864169469917423161, 0.7691187473759173443 ) ) ;
#173822=CARTESIAN_POINT ( 'NONE',  ( 6.549293068304288923, 1.796493013226226232, -1.013385894242497809 ) ) ;
#173826=CARTESIAN_POINT ( 'NONE',  ( 0.9129390864682377371, -0.2673504635808711671, 1.749312949811430373 ) ) ;
#173827=CARTESIAN_POINT ( 'NONE',  ( 0.3521856818783953846, 0.1948384997633167970, -2.006960225185448810 ) ) ;
#173828=CARTESIAN_POINT ( 'NONE',  ( 6.093256065386793985, -0.5776499228958801302, 1.641946315008017576 ) ) ;
#173829=CARTESIAN_POINT ( 'NONE',  ( 3.738036193864560541, 2.281383974799616521, 0.2239769770701737495 ) ) ;
#173831=CARTESIAN_POINT ( 'NONE',  ( 2.062219658421380775, -1.683061746929171321, -0.7467898329211534181 ) ) ;
#173833=CARTESIAN_POINT ( 'NONE',  ( 3.575057022766346737, 0.04566639709948847742, -1.825179878808772305 ) ) ;
#173834=CARTESIAN_POINT ( 'NONE',  ( 3.832657856672664565, 0.6767144645295587457, -1.899618369658891748 ) ) ;
#173836=CARTESIAN_POINT ( 'NONE',  ( 2.114515676104791186, -1.066955051536956356, -1.995125387583786214 ) ) ;
#173838=CARTESIAN_POINT ( 'NONE',  ( 4.893641883129576264, 1.558557130586870398, 1.416501212539149845 ) ) ;
#173840=CARTESIAN_POINT ( 'NONE',  ( 2.840353284027045344, -1.066491845456703835, 1.774417039089710935 ) ) ;
#173843=CARTESIAN_POINT ( 'NONE',  ( 5.004590575528129470, -2.104527602236761386, -0.2589986953433416894 ) ) ;
#173846=CARTESIAN_POINT ( 'NONE',  ( 1.189925737956001095, -0.8670580458889056708, 1.720419655784347412 ) ) ;
#173853=CARTESIAN_POINT ( 'NONE',  ( 0.7037666293719077037, 1.955508453885120401, -1.053950084065604864 ) ) ;
#173854=CARTESIAN_POINT ( 'NONE',  ( 1.712088352014268899, -2.090129137712465557, 0.2570578816783394283 ) ) ;
#173857=CARTESIAN_POINT ( 'NONE',  ( 6.491040186595096628, 0.1814514006053032646, 1.852032668777810587 ) ) ;
#173866=CARTESIAN_POINT ( 'NONE',  ( 2.910546574502240968, 0.6583626327048962557, 1.848246418561696913 ) ) ;
#173867=CARTESIAN_POINT ( 'NONE',  ( 1.674925575805393585, -2.052671086741376882, -0.6780288057936025847 ) ) ;
#173873=CARTESIAN_POINT ( 'NONE',  ( 3.116877616926060135, -1.676954032530679761, 0.4650628940853319682 ) ) ;
#173877=CARTESIAN_POINT ( 'NONE',  ( 2.794295885581669747, -1.882186412485300719, 0.7230279869864174591 ) ) ;
#173878=CARTESIAN_POINT ( 'NONE',  ( 6.825078400183546279, 2.419143596098617621, 2.525240329153962904 ) ) ;
#173880=CARTESIAN_POINT ( 'NONE',  ( 2.395336953769642729, 1.522948423943527363, 1.251906274522778251 ) ) ;
#173888=CARTESIAN_POINT ( 'NONE',  ( 1.928384432292037598, -0.9539229595667864103, -1.780212580967098335 ) ) ;
#173890=CARTESIAN_POINT ( 'NONE',  ( 5.280430876874616430, -1.287285901688420608, 1.914989055045878352 ) ) ;
#173891=CARTESIAN_POINT ( 'NONE',  ( 6.795372052238223048, -1.752927774724974297, 0.8811163259476795240 ) ) ;
#173892=CARTESIAN_POINT ( 'NONE',  ( 2.483191118468269565, -0.005009705968514814069, 1.961936380092830223 ) ) ;
#173894=CARTESIAN_POINT ( 'NONE',  ( 1.072888940501380839, -0.9041080511620370741, 1.802418165037560138 ) ) ;
#173896=CARTESIAN_POINT ( 'NONE',  ( 2.097004163592118164, 1.893647498693065589, 0.9473067498170744116 ) ) ;
#173899=CARTESIAN_POINT ( 'NONE',  ( 2.220424023188283247, -0.0004634451795330202239, 1.841320589463534052 ) ) ;
#173901=CARTESIAN_POINT ( 'NONE',  ( 3.116422982138194353, 1.968445132739887748, 0.4370783100892047801 ) ) ;
#173904=CARTESIAN_POINT ( 'NONE',  ( 3.340189922722580196, -1.266226476691566738, -1.700888996046201029 ) ) ;
#173905=CARTESIAN_POINT ( 'NONE',  ( 0.6910384644343779970, -0.6650364481293036256, 1.717017257891314097 ) ) ;
#173910=CARTESIAN_POINT ( 'NONE',  ( 4.464173201700037730, 0.9678196394932538915, 1.819351253882226516 ) ) ;
#173913=CARTESIAN_POINT ( 'NONE',  ( 1.188719773494644860, 1.394467456127197025, 1.202481090285527632 ) ) ;
#173919=CARTESIAN_POINT ( 'NONE',  ( 1.155211076828046579, -1.737760091701185505, 1.360235214042208263 ) ) ;
#173920=CARTESIAN_POINT ( 'NONE',  ( 3.269090859574837804, -2.088958473869072741, -0.8692115097446629912 ) ) ;
#173922=CARTESIAN_POINT ( 'NONE',  ( 3.339928375916663139, -1.083189831351333954, -1.451890931963683684 ) ) ;
#173923=CARTESIAN_POINT ( 'NONE',  ( 2.712013535993620383, 1.060242027361221862, -1.595356271853585195 ) ) ;
#173924=CARTESIAN_POINT ( 'NONE',  ( 4.404779037558821386, 0.5491149005726041477, 1.996164414091922135 ) ) ;
#173926=CARTESIAN_POINT ( 'NONE',  ( 2.377750047251852017, 1.211369778508808448, 1.555330764497768303 ) ) ;
#173927=CARTESIAN_POINT ( 'NONE',  ( 1.026247228566424363, 1.149774913616221417, -1.545494133055951069 ) ) ;
#173928=CARTESIAN_POINT ( 'NONE',  ( 4.381629165553334815, 1.221847395770376377, 1.416585496670008659 ) ) ;
#173929=CARTESIAN_POINT ( 'NONE',  ( 1.981525833354264243, -0.1160811445666837666, -2.304894087891403487 ) ) ;
#173930=CARTESIAN_POINT ( 'NONE',  ( 3.824516763807362274, -1.251359258362509497, 1.377693585838150936 ) ) ;
#173936=CARTESIAN_POINT ( 'NONE',  ( 0.8386649464857205416, 2.075244960028700181, 0.3580382472886770584 ) ) ;
#173939=CARTESIAN_POINT ( 'NONE',  ( 6.696550776676711614, -0.5693818166121329405, -2.085215994158528208 ) ) ;
#173940=CARTESIAN_POINT ( 'NONE',  ( 2.232824136269210502, 1.381628265877183903, -1.608862310199298928 ) ) ;
#173941=CARTESIAN_POINT ( 'NONE',  ( 1.248313549685893475, 0.9916667988653109500, -1.759473928524292630 ) ) ;
#173945=CARTESIAN_POINT ( 'NONE',  ( 1.335488691732108046, -1.954760257947166568, 0.9229496955955732718 ) ) ;
#173949=CARTESIAN_POINT ( 'NONE',  ( 6.210172754313918908, 1.157103754073171675, -1.651340222398114843 ) ) ;
#173953=CARTESIAN_POINT ( 'NONE',  ( 0.2161854901324336276, -2.218109922327567318, 0.4452641707137113825 ) ) ;
#173958=CARTESIAN_POINT ( 'NONE',  ( 0.1224727961543301408, 0.3280879897031144798, 1.887133295268013766 ) ) ;
#173962=CARTESIAN_POINT ( 'NONE',  ( 3.035487670047633202, -1.158914029964135395, -1.277714875195012700 ) ) ;
#173965=CARTESIAN_POINT ( 'NONE',  ( 1.264531387369687065, -1.596916444607907382, -0.7631234423778727738 ) ) ;
#173966=CARTESIAN_POINT ( 'NONE',  ( 1.453772141523026251, -1.459646937795316068, -1.386592938616920678 ) ) ;
#173968=CARTESIAN_POINT ( 'NONE',  ( 4.401547605996741552, 1.770323140634282311, 1.317293360403009927 ) ) ;
#173971=CARTESIAN_POINT ( 'NONE',  ( 3.791739704763209318, 1.996120715041304061, -0.7158466834289513026 ) ) ;
#173972=CARTESIAN_POINT ( 'NONE',  ( 3.216422893352603563, 1.967893637826668263, 0.4390085219014849827 ) ) ;
#173973=CARTESIAN_POINT ( 'NONE',  ( 3.322321318109163979, -0.7387318680696324247, -1.654322230785286063 ) ) ;
#173977=CARTESIAN_POINT ( 'NONE',  ( 1.832664747978371533, 0.1804508633567840359, 1.861920966532565336 ) ) ;
#173980=CARTESIAN_POINT ( 'NONE',  ( 6.006453938882227561, -0.6616566355047011072, -1.701761020394356283 ) ) ;
#173982=CARTESIAN_POINT ( 'NONE',  ( 2.676846564686267804, 1.640678131122888406, -0.9888057999517668728 ) ) ;
#173991=CARTESIAN_POINT ( 'NONE',  ( 3.357788437482766675, -1.608272433257527556, -1.382313803475518244 ) ) ;
#173992=CARTESIAN_POINT ( 'NONE',  ( -0.02968770228140017037, 2.049257630910449990, -2.243713227073070637 ) ) ;
#173994=CARTESIAN_POINT ( 'NONE',  ( 3.866447834861338695, -1.326295688514609550, 1.458626262776492544 ) ) ;
#173995=CARTESIAN_POINT ( 'NONE',  ( -0.1403655429255863119, -1.558841978801903894, -1.273620833657141072 ) ) ;
#173997=CARTESIAN_POINT ( 'NONE',  ( 6.385961957380775544, -2.116826826188836552, 0.05405687909286471110 ) ) ;
#173999=CARTESIAN_POINT ( 'NONE',  ( 1.522023487246677798, 2.040062638832959241, -0.3519594530456415793 ) ) ;
#174004=CARTESIAN_POINT ( 'NONE',  ( 4.101575158799015242, -2.085053422979638693, 0.1536182331017873492 ) ) ;
#174007=CARTESIAN_POINT ( 'NONE',  ( 0.1174177504974990710, -0.4853618992130321885, 1.745175170155540245 ) ) ;
#174009=CARTESIAN_POINT ( 'NONE',  ( 5.619807753665406302, -2.153844256707802440, 0.4802137346974973409 ) ) ;
#174011=CARTESIAN_POINT ( 'NONE',  ( 4.753059971535213535, -1.774748228059085164, 1.311344899593884561 ) ) ;
#174014=CARTESIAN_POINT ( 'NONE',  ( 2.789602095257078584, 1.815147277589121533, -0.6018686165152677958 ) ) ;
#174017=CARTESIAN_POINT ( 'NONE',  ( 5.477033855465498924, 1.911541192706748715, 0.7957256658025003704 ) ) ;
#174020=CARTESIAN_POINT ( 'NONE',  ( 3.098656953246520906, -0.6260995091542166380, -2.069055637940686143 ) ) ;
#174021=CARTESIAN_POINT ( 'NONE',  ( 5.214472588068230330, 2.024700573814151028, 0.8392323156421463981 ) ) ;
#174029=CARTESIAN_POINT ( 'NONE',  ( 5.647352632913819726, 1.828451368696734747, -0.9708816006866529680 ) ) ;
#174030=CARTESIAN_POINT ( 'NONE',  ( 4.371652425709642742, 1.868346805267994570, -0.4693074334855638630 ) ) ;
#174031=CARTESIAN_POINT ( 'NONE',  ( 0.2105648349144396136, 1.930425396462841725, 0.5826343419270895163 ) ) ;
#174035=CARTESIAN_POINT ( 'NONE',  ( 0.6916816545035618935, -0.7852976098030055585, 2.046091368998310678 ) ) ;
#174036=CARTESIAN_POINT ( 'NONE',  ( 5.566980414702134894, -1.652319403193935887, -0.7768266693391965294 ) ) ;
#174042=CARTESIAN_POINT ( 'NONE',  ( 2.612652284633736777, -0.1782932461553646819, 1.832575692395449485 ) ) ;
#174043=CARTESIAN_POINT ( 'NONE',  ( 6.363545146358847937, -1.619577101098391925, -1.195656717203520403 ) ) ;
#174044=CARTESIAN_POINT ( 'NONE',  ( 1.353307579497017965, -1.032721833433938530, 2.053394521917959015 ) ) ;
#174045=CARTESIAN_POINT ( 'NONE',  ( 6.192239757033616065, 0.9699301198475211994, -1.705161095427814466 ) ) ;
#174051=CARTESIAN_POINT ( 'NONE',  ( 2.243796185194739223, 2.090353954619321275, 0.04827919579214814960 ) ) ;
#174052=CARTESIAN_POINT ( 'NONE',  ( 1.393192293617943944, 1.414286473764417185, 1.224485199485196629 ) ) ;
#174053=CARTESIAN_POINT ( 'NONE',  ( 2.337267334706777611, -1.242538083881424837, 1.587593183769491878 ) ) ;
#174056=CARTESIAN_POINT ( 'NONE',  ( 2.419155098189431641, -1.003372571555812831, -1.421874531148322740 ) ) ;
#174061=CARTESIAN_POINT ( 'NONE',  ( 2.806937704738516448, 1.457146550840708210, 0.9226662414157487113 ) ) ;
#174062=CARTESIAN_POINT ( 'NONE',  ( 2.349409277133751139, 0.5813161652389825518, -2.113004480973964760 ) ) ;
#174063=CARTESIAN_POINT ( 'NONE',  ( 4.688207069967821106, -1.042061291317699423, 1.945354640606362873 ) ) ;
#174065=CARTESIAN_POINT ( 'NONE',  ( 2.641674518982541020, 1.986514366401496590, -0.8763142005700165216 ) ) ;
#174066=CARTESIAN_POINT ( 'NONE',  ( 1.347985785199314668, 1.823511463271022093, 0.09156768404049858701 ) ) ;
#174067=CARTESIAN_POINT ( 'NONE',  ( 3.116528361068672481, 2.066776279341679956, 0.4593686614828630943 ) ) ;
#174071=CARTESIAN_POINT ( 'NONE',  ( 3.632637656275085281, 0.3374270351050281946, 2.267304333945507011 ) ) ;
#174075=CARTESIAN_POINT ( 'NONE',  ( 6.463560548549353690, -1.782115098378980855, -1.325830300435285825 ) ) ;
#174082=CARTESIAN_POINT ( 'NONE',  ( 4.078750125433938223, -0.7691220382576718917, 1.864168106189521890 ) ) ;
#174084=CARTESIAN_POINT ( 'NONE',  ( 2.834894798709301611, -1.972450601023918448, -0.6029180858937719378 ) ) ;
#174089=CARTESIAN_POINT ( 'NONE',  ( 6.087848540548081999, -2.180536604488235941, -0.2183335821156970336 ) ) ;
#174090=CARTESIAN_POINT ( 'NONE',  ( 3.498672800139957406, -1.986100699840901651, 0.3474671148789992836 ) ) ;
#174091=CARTESIAN_POINT ( 'NONE',  ( 2.823586671956069605, 1.020774559177588081, -1.532180179759069283 ) ) ;
#174094=CARTESIAN_POINT ( 'NONE',  ( 6.229513028222847026, -1.717969363144413952, 0.6179237509907066217 ) ) ;
#174097=CARTESIAN_POINT ( 'NONE',  ( 0.4919812829822337030, 1.677557865031731765, 1.518126404548009178 ) ) ;
#174098=CARTESIAN_POINT ( 'NONE',  ( 1.840588936376737372, 2.083348874589638466, 0.3076409294043966902 ) ) ;
#174109=CARTESIAN_POINT ( 'NONE',  ( 4.166425639909420831, 2.220860392705526820, -0.05667459126444325535 ) ) ;
#174110=CARTESIAN_POINT ( 'NONE',  ( 1.623246906879351581, -2.062630869249089116, 0.7406334225198917265 ) ) ;
#174111=CARTESIAN_POINT ( 'NONE',  ( 0.2763675079364875664, 1.274320874971252460, 1.801605125401319007 ) ) ;
#174113=CARTESIAN_POINT ( 'NONE',  ( 4.773855682050706761, -1.924389145058275963, 0.3807478752155256663 ) ) ;
#174121=CARTESIAN_POINT ( 'NONE',  ( 3.955424862866574021, -1.843446357660895041, 1.048082435718917571 ) ) ;
#174123=CARTESIAN_POINT ( 'NONE',  ( 5.243122039519461097, -1.856066598825537373, 1.107904190987746063 ) ) ;
#174124=CARTESIAN_POINT ( 'NONE',  ( 4.265079090171526310, 1.784866007061826298, -0.4516350764028759235 ) ) ;
#174128=CARTESIAN_POINT ( 'NONE',  ( -0.006821830062568761018, -1.739981233400577088, -0.04623622425214619219 ) ) ;
#174129=CARTESIAN_POINT ( 'NONE',  ( 6.727182134110205602, 7.053355583909074689, 2.409100679957976165 ) ) ;
#174132=CARTESIAN_POINT ( 'NONE',  ( 4.399409362686744096, 1.734418756986338295, 1.290045131933370781 ) ) ;
#174133=CARTESIAN_POINT ( 'NONE',  ( 5.272814466252145671, -2.006652483137221665, 0.1948127969565379425 ) ) ;
#174135=CARTESIAN_POINT ( 'NONE',  ( 3.538091169922503276, 0.9737216987566952309, -1.930062384640649054 ) ) ;
#174136=CARTESIAN_POINT ( 'NONE',  ( 3.760970446608974171, -1.736958583363076736, -0.9323722252271587907 ) ) ;
#174138=CARTESIAN_POINT ( 'NONE',  ( 1.062054608305310177, 0.4471719227481777414, -2.263690193671878514 ) ) ;
#174139=CARTESIAN_POINT ( 'NONE',  ( 2.688805810584052658, -0.3489404079633807165, -2.030846992095108217 ) ) ;
#174140=CARTESIAN_POINT ( 'NONE',  ( 5.653840721119872903, 0.7909470656678599942, 1.773883556849734644 ) ) ;
#174149=CARTESIAN_POINT ( 'NONE',  ( 1.887996149947854807, 1.521953097117642706, 1.598203399828190152 ) ) ;
#174151=CARTESIAN_POINT ( 'NONE',  ( 6.825062041929172985, -1.792332737533608666, -0.7979697884207545000 ) ) ;
#174152=CARTESIAN_POINT ( 'NONE',  ( 6.539320575229278454, 2.035006821797652687, 2.408631514295301645 ) ) ;
#174156=CARTESIAN_POINT ( 'NONE',  ( 4.874869531740305462, 1.716800804850382223, -0.6655867697097292979 ) ) ;
#174159=CARTESIAN_POINT ( 'NONE',  ( 2.114203836804037007, -0.9703286663178596338, -1.818149309968750016 ) ) ;
#174161=UNCERTAINTY_MEASURE_WITH_UNIT (LENGTH_MEASURE( 1.000000000000000082E-05 ), #185150, 'distance_accuracy_value', 'NONE');
#174166=CARTESIAN_POINT ( 'NONE',  ( 0.4618819262211275034, 2.038552468250200533, -0.3016747405163843765 ) ) ;
#174168=CARTESIAN_POINT ( 'NONE',  ( 4.476008884455379366, -1.787108923542475525, -0.4427587100873929815 ) ) ;
#174172=CARTESIAN_POINT ( 'NONE',  ( 6.610000000000008313, 7.629137130509070275, 2.600000000000001421 ) ) ;
#174175=CARTESIAN_POINT ( 'NONE',  ( 4.301547675229603129, 1.771612934706376707, 1.315755017190944676 ) ) ;
#174176=CARTESIAN_POINT ( 'NONE',  ( 0.8433209000573947955, -1.854398715148808385, 1.110445933987347367 ) ) ;
#174178=CARTESIAN_POINT ( 'NONE',  ( 0.2110004604562870645, 1.588762659912812403, -1.064147093309028680 ) ) ;
#174179=CARTESIAN_POINT ( 'NONE',  ( 6.491422787562372676, -0.4091076066058823013, 1.878265147811091662 ) ) ;
#174182=CARTESIAN_POINT ( 'NONE',  ( 5.707647354773449422, 1.450964518888698596, 1.245719642194928589 ) ) ;
#174184=CARTESIAN_POINT ( 'NONE',  ( 0.4791068267422092797, 1.747065859276742072, -0.6691465683838908607 ) ) ;
#174186=CARTESIAN_POINT ( 'NONE',  ( 2.694546298722868549, 1.457235452327232395, -1.394086077981852911 ) ) ;
#174188=CARTESIAN_POINT ( 'NONE',  ( 4.389357127182037743, 1.881541760944308139, -0.9463713395347850277 ) ) ;
#174193=CARTESIAN_POINT ( 'NONE',  ( 3.779560859189102562, 0.2429267963163626032, -2.005027992008329818 ) ) ;
#174196=CARTESIAN_POINT ( 'NONE',  ( 4.112696061561730509, 1.531809107248631507, -1.525399859652858847 ) ) ;
#174202=CARTESIAN_POINT ( 'NONE',  ( 2.260437933566094681, -2.170709518246512815, 0.05174924654302060639 ) ) ;
#174205=CARTESIAN_POINT ( 'NONE',  ( 1.206327419354651820, 1.623952629372883427, 0.8676893986077349741 ) ) ;
#174207=CARTESIAN_POINT ( 'NONE',  ( 2.911879292414458309, -1.082406496695037301, -1.905547650945007776 ) ) ;
#174209=CARTESIAN_POINT ( 'NONE',  ( 3.766728628225763043, -1.521468805364207144, 1.674700015324230407 ) ) ;
#174211=CARTESIAN_POINT ( 'NONE',  ( 4.663296154398564042, 1.879804967172087782, -0.7303043177912388328 ) ) ;
#174216=CARTESIAN_POINT ( 'NONE',  ( 4.657331418887999064, 0.3884847549131437705, -1.726375946583807774 ) ) ;
#174218=CARTESIAN_POINT ( 'NONE',  ( 1.237491679122425969, -1.904027454836676014, 0.9001316648933003206 ) ) ;
#174221=CARTESIAN_POINT ( 'NONE',  ( 0.9241884870439884825, 0.9676023207046909880, 1.715383555584276909 ) ) ;
#174223=CARTESIAN_POINT ( 'NONE',  ( 5.800407700000974387, 1.352143934286989868, -1.496062775417882129 ) ) ;
#174226=CARTESIAN_POINT ( 'NONE',  ( 4.381629165553334815, 1.221847395770376377, 1.416585496670008659 ) ) ;
#174228=CARTESIAN_POINT ( 'NONE',  ( 4.047765473330780850, 1.496028175931501947, 1.431257568052332729 ) ) ;
#174239=CARTESIAN_POINT ( 'NONE',  ( 4.141029529442549872, -0.1900441490861082827, -1.952618137025011746 ) ) ;
#174240=CARTESIAN_POINT ( 'NONE',  ( 1.862657450031137474, -0.6818942500997280387, 1.897406292459068222 ) ) ;
#174243=CARTESIAN_POINT ( 'NONE',  ( 6.639320575229252341, 2.457876053485750223, 2.280608551775892501 ) ) ;
#174244=CARTESIAN_POINT ( 'NONE',  ( 1.387741975113141235, -0.8460221195879283895, 1.668388151239764028 ) ) ;
#174246=CARTESIAN_POINT ( 'NONE',  ( 3.093996842688331750, 1.280297628565935097, 1.553616095213964154 ) ) ;
#174248=CARTESIAN_POINT ( 'NONE',  ( 3.902059883959855924, -1.090250183479730461, -1.814828101457645060 ) ) ;
#174250=CARTESIAN_POINT ( 'NONE',  ( 5.230950013807261101, -1.948248037745937022, -0.7008574099531189594 ) ) ;
#174252=CARTESIAN_POINT ( 'NONE',  ( 0.2399332258718233080, 2.085444179493881389, 0.1495565104911322774 ) ) ;
#174254=CARTESIAN_POINT ( 'NONE',  ( 5.526323803393728085, 1.085782926936417425, -1.467421699745217412 ) ) ;
#174261=CARTESIAN_POINT ( 'NONE',  ( 6.481121912432155519, -1.750430003815309998, -0.7703581994758443852 ) ) ;
#174265=DIRECTION ( 'NONE',  ( 1.014813233446432150E-15, 1.000000000000000000, -4.583713267641621330E-32 ) ) ;
#174270=CARTESIAN_POINT ( 'NONE',  ( 5.325796065338770369, 0.8146125389149364571, -1.844717355016491478 ) ) ;
#174275=CARTESIAN_POINT ( 'NONE',  ( 2.711712322018722698, 0.5300763513187057852, -1.896665901777684127 ) ) ;
#174276=CARTESIAN_POINT ( 'NONE',  ( 3.761342352588430860, 1.897692735847063661, -0.6820134568972098243 ) ) ;
#174278=CARTESIAN_POINT ( 'NONE',  ( 6.827182134110224787, 2.015384445464900587, 2.492173930675382731 ) ) ;
#174279=CARTESIAN_POINT ( 'NONE',  ( 3.820431320580887302, 2.080737768064028437, 0.6879518193209921417 ) ) ;
#174281=CARTESIAN_POINT ( 'NONE',  ( 2.291906413246731944, -0.8257142216546548008, 1.740595036569925647 ) ) ;
#174283=CARTESIAN_POINT ( 'NONE',  ( -0.1296875068447916890, 6.948706544289747988, -2.421546651465163347 ) ) ;
#174284=CARTESIAN_POINT ( 'NONE',  ( 0.2329586101569892376, 6.948071080078905837, -2.440796105365902857 ) ) ;
#174291=CARTESIAN_POINT ( 'NONE',  ( 5.565905774130330386, -1.163279849954502287, 1.427249551226833502 ) ) ;
#174292=CARTESIAN_POINT ( 'NONE',  ( 3.018229385809416687, -2.010681777978724494, 0.1011178238035769505 ) ) ;
#174293=CARTESIAN_POINT ( 'NONE',  ( 4.710533686004090725, -1.772996550310073971, -1.462542180504990075 ) ) ;
#174294=CARTESIAN_POINT ( 'NONE',  ( -0.1290005225502398323, 0.2247172878383028038, -2.207197350255707402 ) ) ;
#174295=CARTESIAN_POINT ( 'NONE',  ( 2.729178580549945110, 0.09652143117058623045, -1.858595261477024918 ) ) ;
#174298=FACE_OUTER_BOUND ( 'NONE', #193968, .T. ) ;
#174301=CARTESIAN_POINT ( 'NONE',  ( 6.023005994326640078, -1.968326514718239828, 0.7052485104920204195 ) ) ;
#174303=EDGE_LOOP ( 'NONE', ( #149557, #63565, #97657, #109465 ) ) ;
#174306=CARTESIAN_POINT ( 'NONE',  ( 6.721331452548120922, -0.1233026559786208343, 1.696394328608492819 ) ) ;
#174309=CARTESIAN_POINT ( 'NONE',  ( 1.459138885926267504, -1.646488293146914472, -0.5446327844310631106 ) ) ;
#174313=CARTESIAN_POINT ( 'NONE',  ( 6.368071955308375998, -2.155667716570781156, 0.2575352064990812928 ) ) ;
#174314=CARTESIAN_POINT ( 'NONE',  ( 4.195794211080963620, -0.6966935528937777677, 1.687730213881050600 ) ) ;
#174315=CARTESIAN_POINT ( 'NONE',  ( 2.360140415366945188, -1.961439503465340239, 0.04308618615556784187 ) ) ;
#174319=CARTESIAN_POINT ( 'NONE',  ( 3.211701520346501582, 1.672844727185973657, 1.303009041611735030 ) ) ;
#174323=CARTESIAN_POINT ( 'NONE',  ( 0.8837443060279138729, -1.967007789996034095, 0.6459356165888497925 ) ) ;
#174326=CARTESIAN_POINT ( 'NONE',  ( 3.686370400671713732, 1.234840205895268328, 1.846255301073204791 ) ) ;
#174328=CARTESIAN_POINT ( 'NONE',  ( 1.653414166010831243, 1.186659091926351106, 1.968620417403597944 ) ) ;
#174330=CARTESIAN_POINT ( 'NONE',  ( 6.596538677256176264, 2.039275035945103731, 0.3085339683557372092 ) ) ;
#174337=CARTESIAN_POINT ( 'NONE',  ( -0.1106727585415837045, 2.871245121144291090, -2.491938459964110120 ) ) ;
#174338=CARTESIAN_POINT ( 'NONE',  ( 2.766273355629506714, -1.191139867243676598, 1.247637197061921555 ) ) ;
#174339=CARTESIAN_POINT ( 'NONE',  ( 2.800017839408690090, -0.9981255096969069429, -1.752139039461996006 ) ) ;
#174340=CARTESIAN_POINT ( 'NONE',  ( 3.270466940867942984, 2.077131924838520050, -0.9849289250120364381 ) ) ;
#174341=CARTESIAN_POINT ( 'NONE',  ( 3.058202344463755828, 2.251794067479270911, -0.2186341555679652271 ) ) ;
#174342=CARTESIAN_POINT ( 'NONE',  ( 4.828798294617491216, 2.015104956129540881, 0.6122756557535751210 ) ) ;
#174344=CARTESIAN_POINT ( 'NONE',  ( 3.848697245170757508, -1.448060206101034808, 1.017097547381773159 ) ) ;
#174346=CARTESIAN_POINT ( 'NONE',  ( 5.864811835480173485, 0.1724426041235416485, -2.285918041817245783 ) ) ;
#174347=CARTESIAN_POINT ( 'NONE',  ( 5.191278274421009975, -0.6593680717656666967, 1.719199333795925710 ) ) ;
#174351=CARTESIAN_POINT ( 'NONE',  ( 4.945371362016416583, 0.6893947036107104243, -2.080263006054481334 ) ) ;
#174355=CARTESIAN_POINT ( 'NONE',  ( 5.898901817742318698, 0.4001337562283372451, 2.031160294743330486 ) ) ;
#174356=CARTESIAN_POINT ( 'NONE',  ( -0.06521966986864842497, -1.616690375843790051, 1.205047459138554045 ) ) ;
#174358=CARTESIAN_POINT ( 'NONE',  ( 3.018101299323606046, -0.9500872288037317537, -1.675862364343786215 ) ) ;
#174361=CARTESIAN_POINT ( 'NONE',  ( 6.486587849989844834, -1.303813291173651301, 1.673118453357678392 ) ) ;
#174370=CARTESIAN_POINT ( 'NONE',  ( 1.012071980069820132, 1.959787197952606252, -0.09269708818125663163 ) ) ;
#174373=CARTESIAN_POINT ( 'NONE',  ( 5.969191311310417802, 1.729517061547349632, 0.9261464158661563140 ) ) ;
#174376=CARTESIAN_POINT ( 'NONE',  ( 0.09312846265441956928, -0.5046389715205062965, -2.214118724221309620 ) ) ;
#174380=CARTESIAN_POINT ( 'NONE',  ( 0.3681424317822541425, -1.226883886190757611, 1.412057460252094554 ) ) ;
#174381=CARTESIAN_POINT ( 'NONE',  ( 5.641838915941918664, -0.04494510194943436565, -1.733422878500885167 ) ) ;
#174385=CARTESIAN_POINT ( 'NONE',  ( 3.263397454411249399, 2.137687552337414587, -0.4822058812353549606 ) ) ;
#174386=CARTESIAN_POINT ( 'NONE',  ( 4.296143005555221883, -0.8870401112092487494, 2.130475988740585080 ) ) ;
#174387=CARTESIAN_POINT ( 'NONE',  ( 6.520785525839065677, 1.921145329286999326, 0.7461220883302563944 ) ) ;
#174388=CARTESIAN_POINT ( 'NONE',  ( 1.956878712445113244, 0.3320500349934927820, -1.913199751371328361 ) ) ;
#174392=CARTESIAN_POINT ( 'NONE',  ( 4.658503719480325600, 2.115088938745744329, 0.1532479335744421078 ) ) ;
#174393=CARTESIAN_POINT ( 'NONE',  ( 3.147111449167848019, 0.9091449406319618287, 1.799922684605055556 ) ) ;
#174397=CARTESIAN_POINT ( 'NONE',  ( 1.172165686010542274, -1.159919637379997814, 1.409874495853599141 ) ) ;
#174402=CARTESIAN_POINT ( 'NONE',  ( 6.139539385720709674, -1.490912338237950108, -1.423074965643542411 ) ) ;
#174408=CARTESIAN_POINT ( 'NONE',  ( 4.354169037430507316, 0.8614980693376246279, -1.826848373156648497 ) ) ;
#174409=CARTESIAN_POINT ( 'NONE',  ( 5.268325480127796112, 2.218825861875061811, -0.1076023827350883894 ) ) ;
#174414=CARTESIAN_POINT ( 'NONE',  ( 4.434483769945627429, 2.020730376925969018, 0.4039503012724340869 ) ) ;
#174415=CARTESIAN_POINT ( 'NONE',  ( 2.426407915648312930, -1.496052118593782287, -1.352154011671408362 ) ) ;
#174416=ORIENTED_EDGE ( 'NONE', *, *, #199668, .T. ) ;
#174422=CARTESIAN_POINT ( 'NONE',  ( 3.128279665134887644, 0.2985813455266342342, -1.993766061640166232 ) ) ;
#174423=CARTESIAN_POINT ( 'NONE',  ( 2.220424023188283247, -0.0004634451795330202239, 1.841320589463534052 ) ) ;
#174424=CARTESIAN_POINT ( 'NONE',  ( 0.9620547613307988133, 0.4452262838200848893, -2.264189643979396482 ) ) ;
#174426=CARTESIAN_POINT ( 'NONE',  ( 3.989662644735529451, 1.562606173494068829, 1.493797087085822595 ) ) ;
#174430=CARTESIAN_POINT ( 'NONE',  ( 1.199835987674138460, -1.870836310881810682, -0.003643258294119822160 ) ) ;
#174431=EDGE_LOOP ( 'NONE', ( #110981, #133542 ) ) ;
#174433=CARTESIAN_POINT ( 'NONE',  ( 5.823112234018508637, -0.04902082458170010926, 1.971020750367402430 ) ) ;
#174438=CARTESIAN_POINT ( 'NONE',  ( 0.7509353727821498348, 0.6442623716619542140, 2.110749664216593047 ) ) ;
#174443=CARTESIAN_POINT ( 'NONE',  ( 5.049669536805332370, 0.6190787695102616395, -1.871797661314599015 ) ) ;
#174444=CARTESIAN_POINT ( 'NONE',  ( 5.373738807407080209, 2.225351779437909183, -0.6107155785605354881 ) ) ;
#174445=CARTESIAN_POINT ( 'NONE',  ( 5.600015889513015210, 0.7539677941885476464, -1.701683582386106952 ) ) ;
#174446=CARTESIAN_POINT ( 'NONE',  ( 3.520431386055590917, 0.9232258726861832798, 1.844449542969233358 ) ) ;
#174453=CARTESIAN_POINT ( 'NONE',  ( 5.301315566676442437, -1.864821911710778490, 1.111730659606048111 ) ) ;
#174455=CARTESIAN_POINT ( 'NONE',  ( 4.511176471348508521, -1.804767551675333204, 0.3638508048048467169 ) ) ;
#174457=CARTESIAN_POINT ( 'NONE',  ( 6.620655732516673275, 1.290356161719278028, 1.942653802560645460 ) ) ;
#174458=CARTESIAN_POINT ( 'NONE',  ( 6.339412547452306868, 0.8406370108028878851, -2.024118718474729128 ) ) ;
#174460=CARTESIAN_POINT ( 'NONE',  ( 0.5095019425028306514, 1.969206903598280212, 1.113800330609107103 ) ) ;
#174466=CARTESIAN_POINT ( 'NONE',  ( 0.2503970875498504056, -1.425519035090598852, 1.048718885610238294 ) ) ;
#174467=CARTESIAN_POINT ( 'NONE',  ( 5.584640334855505373, -1.275214923639787834, 1.557698558565046243 ) ) ;
#174469=CARTESIAN_POINT ( 'NONE',  ( 4.542079205076994697, 0.9026690382304535243, -1.902845716346044158 ) ) ;
#174470=CARTESIAN_POINT ( 'NONE',  ( 3.480013654308728555, -1.913576260228011749, -0.09060460826773930609 ) ) ;
#174473=CARTESIAN_POINT ( 'NONE',  ( 4.510180775305682843, 1.969176117969779982, -0.04608634298608124680 ) ) ;
#174474=CARTESIAN_POINT ( 'NONE',  ( 5.379167904621746210, -1.827783419154908273, -0.8597544005511729148 ) ) ;
#174475=CARTESIAN_POINT ( 'NONE',  ( 3.028041890241763401, 1.040506211802554981, -1.554362669439563360 ) ) ;
#174476=CARTESIAN_POINT ( 'NONE',  ( 4.881344157179084320, 1.607756147011094150, -0.6252594192169037557 ) ) ;
#174477=CARTESIAN_POINT ( 'NONE',  ( 0.7735182334044669039, 0.3705173918269571431, -1.875978362188877036 ) ) ;
#174479=CARTESIAN_POINT ( 'NONE',  ( 2.631697372267821855, -2.058793095894187353, 0.7952504953367269813 ) ) ;
#174482=CARTESIAN_POINT ( 'NONE',  ( 0.1392228125525768467, -0.1412503886474673342, -2.030206775815279308 ) ) ;
#174487=CLOSED_SHELL ( 'NONE', ( #197236, #12593, #124848, #104589, #131806, #140035, #177268, #94801 ) ) ;
#174490=CARTESIAN_POINT ( 'NONE',  ( 2.137250951388528275, -0.09934309608320915363, -2.068088366144354318 ) ) ;
#174495=CARTESIAN_POINT ( 'NONE',  ( 6.270199134133584096, 2.114857618286110075, -0.1555134818699496213 ) ) ;
#174498=CARTESIAN_POINT ( 'NONE',  ( 0.07479286986302942364, 7.629137130509078268, -2.455503679634089220 ) ) ;
#174501=CARTESIAN_POINT ( 'NONE',  ( 5.589220178194088895, 1.203167956798111060, -1.617571559180859486 ) ) ;
#174502=CARTESIAN_POINT ( 'NONE',  ( 5.067565384200278800, 1.291559945344708638, 1.415018661930996569 ) ) ;
#174504=CARTESIAN_POINT ( 'NONE',  ( 2.366952063387484095, 0.1042156695447923470, -2.189191704635709890 ) ) ;
#174507=CARTESIAN_POINT ( 'NONE',  ( 5.765890645310551399, 0.5801508929094216782, -1.927831218222434195 ) ) ;
#174508=CARTESIAN_POINT ( 'NONE',  ( 0.7383556378116812313, 1.137082172773289379, -1.537495029474859276 ) ) ;
#174511=CARTESIAN_POINT ( 'NONE',  ( 0.3511856949766634095, 0.1948183440376727305, -2.006963311255556714 ) ) ;
#174513=CARTESIAN_POINT ( 'NONE',  ( 3.966417678127855950, -1.951510144350139919, -0.7507201541567410930 ) ) ;
#174515=CARTESIAN_POINT ( 'NONE',  ( 2.045521581634631048, 0.6637456736250256784, -1.592148833096140192 ) ) ;
#174517=CARTESIAN_POINT ( 'NONE',  ( 5.976833544478475702, -1.498421880457675215, 1.500811427713820478 ) ) ;
#174520=CARTESIAN_POINT ( 'NONE',  ( 0.2737812321212430566, -1.924752420120953822, 0.3788971555385572954 ) ) ;
#174525=CARTESIAN_POINT ( 'NONE',  ( 3.264119686811095988, 1.811656971725349896, -0.002766503545040265976 ) ) ;
#174529=CARTESIAN_POINT ( 'NONE',  ( 3.457467740999135231, -1.373635607365558453, -1.181027286383716124 ) ) ;
#174534=CARTESIAN_POINT ( 'NONE',  ( 4.545250530879026307, 1.662896905596674468, -0.8357390809586220382 ) ) ;
#174536=CARTESIAN_POINT ( 'NONE',  ( 2.073720586576404568, -0.8169873708120840572, 1.732773573125611088 ) ) ;
#174537=CARTESIAN_POINT ( 'NONE',  ( 1.078802750678783395, -0.04027803099338270881, -1.825304540826321542 ) ) ;
#174547=CARTESIAN_POINT ( 'NONE',  ( 5.278159644759479185, -1.050164822159710853, -1.665878549478349013 ) ) ;
#174550=CARTESIAN_POINT ( 'NONE',  ( 0.04111360010001801485, -1.617408405202691135, -1.324400026677017728 ) ) ;
#174551=CARTESIAN_POINT ( 'NONE',  ( 5.702155557734973179, -1.926566265495327723, 0.0002483051060025303638 ) ) ;
#174553=CARTESIAN_POINT ( 'NONE',  ( 0.9205982885796895054, 1.684962172289593996, 0.7030880920091547859 ) ) ;
#174554=CARTESIAN_POINT ( 'NONE',  ( 2.543839704335303153, -1.636039663378138886, -1.481301067789652537 ) ) ;
#174556=CARTESIAN_POINT ( 'NONE',  ( 1.072351618572921605, 0.7776387867773439933, 1.747342548420704800 ) ) ;
#174559=CARTESIAN_POINT ( 'NONE',  ( 0.3968417698968416674, 0.3330189415953662690, 1.941018003364772593 ) ) ;
#174560=CARTESIAN_POINT ( 'NONE',  ( 2.841277192181762334, 0.6965426786647112012, -1.813031058463436818 ) ) ;
#174562=CARTESIAN_POINT ( 'NONE',  ( 1.159529582462547781, -0.4871260124716703110, -1.956262300040665814 ) ) ;
#174564=CARTESIAN_POINT ( 'NONE',  ( 6.772303520102497920, -0.8766781706108403016, -1.641457522745570996 ) ) ;
#174569=CARTESIAN_POINT ( 'NONE',  ( 2.806388347806953121, 1.585463108415147149, -1.513251884624075672 ) ) ;
#174573=CARTESIAN_POINT ( 'NONE',  ( 2.683998146737070378, -0.9385614705539682134, 1.565816405032012470 ) ) ;
#174580=CARTESIAN_POINT ( 'NONE',  ( 1.541497387563552479, -1.395045264726347600, -1.328863961831990181 ) ) ;
#174581=CARTESIAN_POINT ( 'NONE',  ( 5.594571816639393624, 1.932094781187740917, 0.3390067100078468232 ) ) ;
#174585=CARTESIAN_POINT ( 'NONE',  ( 4.634432875810733599, 0.3748786239917039631, 2.159109584303263940 ) ) ;
#174587=CARTESIAN_POINT ( 'NONE',  ( 5.489151832033660305, 0.1466973765328460355, 2.065091666743318122 ) ) ;
#174591=CARTESIAN_POINT ( 'NONE',  ( 4.694093285409329575, 1.999278280869060342, 1.134256664920972213 ) ) ;
#174594=CARTESIAN_POINT ( 'NONE',  ( 0.4984804791418595560, -0.7777643670432095035, -2.156416217022334436 ) ) ;
#174597=CARTESIAN_POINT ( 'NONE',  ( 4.787022420419578594, 1.440143517293355879, 1.302930595787118895 ) ) ;
#174603=CARTESIAN_POINT ( 'NONE',  ( 4.693567934957057375, 1.782326746607498791, -0.6936623114904352239 ) ) ;
#174604=CARTESIAN_POINT ( 'NONE',  ( 6.475633750228043439, 1.648727237068832396, -0.5065655092456061714 ) ) ;
#174605=CARTESIAN_POINT ( 'NONE',  ( 5.313685493615880162, -1.282986534165726944, -1.555701818360885280 ) ) ;
#174609=CARTESIAN_POINT ( 'NONE',  ( 1.570382428225084226, -1.985578813138744403, -0.6546124938694962703 ) ) ;
#174610=CARTESIAN_POINT ( 'NONE',  ( 0.5492016079408028606, 0.5613503750152969429, -1.678537049539428727 ) ) ;
#174611=CARTESIAN_POINT ( 'NONE',  ( 5.449842333688053486, -1.824117940560719298, -0.8596331684956670660 ) ) ;
#174613=CARTESIAN_POINT ( 'NONE',  ( 3.152547991667663307, -1.735656589536422212, 1.497406435017712756 ) ) ;
#174614=CARTESIAN_POINT ( 'NONE',  ( 1.868729199028572596, 1.665863247900209121, -0.5035742270650641617 ) ) ;
#174615=CARTESIAN_POINT ( 'NONE',  ( 2.918346969001627045, -2.117983955170518851, 0.1081942149789016649 ) ) ;
#174617=CARTESIAN_POINT ( 'NONE',  ( 2.161130077686782336, -0.4579326675830681093, -1.672196941802698733 ) ) ;
#174619=CARTESIAN_POINT ( 'NONE',  ( 2.066652149400012295, 1.381653119961171239, -1.247030302550973468 ) ) ;
#174620=CARTESIAN_POINT ( 'NONE',  ( 2.418641202038225302, 0.9268156738743680290, 1.963535311701142483 ) ) ;
#174621=CARTESIAN_POINT ( 'NONE',  ( 3.186732694495420848, 1.586669336078951664, -1.244385354607212335 ) ) ;
#174622=CARTESIAN_POINT ( 'NONE',  ( 4.125000000000001776, -2.052068128417945392, 2.349217982248014418E-13 ) ) ;
#174624=CARTESIAN_POINT ( 'NONE',  ( 1.289925581193847925, -0.8688078642279849495, 1.719429354455022096 ) ) ;
#174626=CARTESIAN_POINT ( 'NONE',  ( 3.832468605949594043, -1.144296635937601669, -1.903904886208422909 ) ) ;
#174632=CARTESIAN_POINT ( 'NONE',  ( 5.660436988733716035, 2.218808146451553220, 0.1093606849192785280 ) ) ;
#174633=CARTESIAN_POINT ( 'NONE',  ( 4.457442142980160504, 1.574409630067734156, 1.170308293268598643 ) ) ;
#174636=CARTESIAN_POINT ( 'NONE',  ( 6.063815651355930036, 2.230472738441360292, -0.3779872977145922741 ) ) ;
#174638=CARTESIAN_POINT ( 'NONE',  ( 2.313000242259897199, -1.596077997345384247, 1.306617308116851062 ) ) ;
#174643=CARTESIAN_POINT ( 'NONE',  ( 4.235518730357812345, -1.288231833625707701, -1.356488508162751128 ) ) ;
#174644=CARTESIAN_POINT ( 'NONE',  ( 2.443678673881148011, -1.509841515647825094, -0.8527992262679043867 ) ) ;
#174646=CARTESIAN_POINT ( 'NONE',  ( 0.09973926083830295108, -0.6030689337076476919, 2.211586693686658389 ) ) ;
#174647=CARTESIAN_POINT ( 'NONE',  ( 1.589210545419886378, -0.3244246349418925535, -2.182665228674217861 ) ) ;
#174648=CARTESIAN_POINT ( 'NONE',  ( 4.089459622424143070, -0.7983975988373869237, 1.932503512935821011 ) ) ;
#174649=CARTESIAN_POINT ( 'NONE',  ( 5.314377360232536596, 1.795021767651948208, 0.7414505486388212052 ) ) ;
#174651=CARTESIAN_POINT ( 'NONE',  ( 0.4062500000042400528, 1.895863743059760909, -0.7852924748300097457 ) ) ;
#174653=CARTESIAN_POINT ( 'NONE',  ( 0.4576579978108759050, -1.899619568183811058, -0.6767110947205197125 ) ) ;
#174658=CARTESIAN_POINT ( 'NONE',  ( 4.441915170580639227, 0.7783198120194650960, -1.651611053696280695 ) ) ;
#174660=CARTESIAN_POINT ( 'NONE',  ( 2.468050989216635127, 2.164326253657654853, -0.4298898877757306725 ) ) ;
#174666=CARTESIAN_POINT ( 'NONE',  ( 1.177996693904998615, 1.989173073321507612, -0.3494277517126374577 ) ) ;
#174670=CARTESIAN_POINT ( 'NONE',  ( 3.467479172597370596, -0.3673618142193516012, 1.824136687861827921 ) ) ;
#174677=CARTESIAN_POINT ( 'NONE',  ( 4.143042835627613663, -1.587387879459275286, 0.9017181768668989239 ) ) ;
#174681=CARTESIAN_POINT ( 'NONE',  ( 0.5789038866980666942, 1.201919051685101270, -1.249903294292388667 ) ) ;
#174682=CARTESIAN_POINT ( 'NONE',  ( 5.718664505737725001, -0.04093049815006092468, 1.840854889930729765 ) ) ;
#174683=CARTESIAN_POINT ( 'NONE',  ( 3.879734811474966794, 2.173438607767137043, -0.7759833549572618949 ) ) ;
#174685=CARTESIAN_POINT ( 'NONE',  ( 0.1927530690809010350, -0.4471281949963988867, -2.018758496260419921 ) ) ;
#174686=CARTESIAN_POINT ( 'NONE',  ( 5.413504136812340661, 0.6594720349357428013, 2.201770641885878899 ) ) ;
#174691=CARTESIAN_POINT ( 'NONE',  ( 5.963714631206167738, 1.842656449598079060, -0.3214700631931910468 ) ) ;
#174694=CARTESIAN_POINT ( 'NONE',  ( 2.320441991784210067, -0.7354482596747033973, -1.765520077574176394 ) ) ;
#174696=CARTESIAN_POINT ( 'NONE',  ( 3.774219598512587037, 1.225428716765289749, 1.835190637982798023 ) ) ;
#174698=CARTESIAN_POINT ( 'NONE',  ( 6.983263157960370116, 7.052597238847845063, 2.544342084569085838 ) ) ;
#174701=CARTESIAN_POINT ( 'NONE',  ( 2.626355190031507192, -1.328241637659173247, -1.886819894403545028 ) ) ;
#174702=CARTESIAN_POINT ( 'NONE',  ( 2.646866301197240645, -0.3325320220872363675, -1.933311746529025266 ) ) ;
#174704=CARTESIAN_POINT ( 'NONE',  ( 6.385603471572667722, -1.944119864917488893, 0.6893456996763939193 ) ) ;
#174706=CARTESIAN_POINT ( 'NONE',  ( 3.925017756809038527, -1.752140073516525565, 0.9981236898717813499 ) ) ;
#174709=CARTESIAN_POINT ( 'NONE',  ( 5.014861385384292269, 0.1531656238677771009, 2.010801456750747285 ) ) ;
#174715=CARTESIAN_POINT ( 'NONE',  ( 1.464000922811282468, -0.5298712919106687291, 2.105275420227727956 ) ) ;
#174719=CARTESIAN_POINT ( 'NONE',  ( 2.301827437220682171, -1.870247568056710774, 0.04138213060620592881 ) ) ;
#174720=CARTESIAN_POINT ( 'NONE',  ( 0.1809649437218979473, -0.1514441579043615538, -2.027393396774066936 ) ) ;
#174721=CARTESIAN_POINT ( 'NONE',  ( -0.02244404828157658613, 7.629137130509074716, -2.789100637983293662 ) ) ;
#174722=CARTESIAN_POINT ( 'NONE',  ( 6.727182134110201162, 1.271184308336456015, 2.025152302351560518 ) ) ;
#174726=CARTESIAN_POINT ( 'NONE',  ( 2.982959643696237784, -1.767753630637520779, -0.7297678730374329570 ) ) ;
#174728=CARTESIAN_POINT ( 'NONE',  ( 4.662845455860040289, -1.581648675543185334, -0.7943582009959786472 ) ) ;
#174729=CARTESIAN_POINT ( 'NONE',  ( 1.453610327690219473, -1.385809040371610346, -1.317956379189986871 ) ) ;
#174732=CARTESIAN_POINT ( 'NONE',  ( 0.02247297916271525850, 0.3300846716227764932, 1.886903735308493424 ) ) ;
#174734=CARTESIAN_POINT ( 'NONE',  ( 0.8892259839063383353, 0.1505779921940515187, 2.064926437897919964 ) ) ;
#174736=CARTESIAN_POINT ( 'NONE',  ( 5.770339134078734666, -1.185559297855027561, 1.446973003893243348 ) ) ;
#174737=CARTESIAN_POINT ( 'NONE',  ( 1.558932953716257730, -1.564965500463588732, -0.9399777662534372080 ) ) ;
#174738=CARTESIAN_POINT ( 'NONE',  ( 5.567066847960510323, -1.993696164035433371, -0.9465883713010987410 ) ) ;
#174741=CARTESIAN_POINT ( 'NONE',  ( 3.051292873657907023, 1.770411945740796966, -1.058192539780268282 ) ) ;
#174745=CARTESIAN_POINT ( 'NONE',  ( 0.4390364970160882119, 0.3691015439823106536, 2.129678967336546602 ) ) ;
#174748=CARTESIAN_POINT ( 'NONE',  ( 4.914543119725925280, 0.7892175071393169317, 1.914236960262293508 ) ) ;
#174750=CARTESIAN_POINT ( 'NONE',  ( 3.093221446634909721, 1.855696356685032633, -1.108285163885482039 ) ) ;
#174752=CARTESIAN_POINT ( 'NONE',  ( 3.563153132451855054, -1.649810593967064865, 1.164694042050371303 ) ) ;
#174753=CARTESIAN_POINT ( 'NONE',  ( 1.996468121258226924, 1.940055844723225009, 0.2909814450420752929 ) ) ;
#174754=CARTESIAN_POINT ( 'NONE',  ( 6.620655732516684822, 7.052296306484477029, 2.671890196246820004 ) ) ;
#174761=CARTESIAN_POINT ( 'NONE',  ( 0.9894706735516716201, -0.4852629857438545691, 1.957171443305204761 ) ) ;
#174763=CARTESIAN_POINT ( 'NONE',  ( 5.812113132715003516, 1.472855484078567923, -1.623034594306454137 ) ) ;
#174765=CARTESIAN_POINT ( 'NONE',  ( 5.713130151434068438, 1.559639147136464343, -1.106415316399149473 ) ) ;
#174768=CARTESIAN_POINT ( 'NONE',  ( 3.023064714212614135, -1.777003028299545484, 0.9530295004822467719 ) ) ;
#174770=CARTESIAN_POINT ( 'NONE',  ( 4.823137214860290456, -0.08221903636504260260, 1.722948775904736385 ) ) ;
#174773=CARTESIAN_POINT ( 'NONE',  ( 4.112460492241882370, 1.324567223757302292, -1.321038939096484066 ) ) ;
#174775=CARTESIAN_POINT ( 'NONE',  ( 0.7431355771655088205, -0.2497938498803170537, -2.055034051290441255 ) ) ;
#174776=CARTESIAN_POINT ( 'NONE',  ( 6.602015318333181781, 0.7961593463888805289, -1.911361562896146671 ) ) ;
#174780=CARTESIAN_POINT ( 'NONE',  ( -0.03528172390533482194, -1.455059732361897895, 1.078909735853793794 ) ) ;
#174786=CARTESIAN_POINT ( 'NONE',  ( 0.5550359226569913096, 1.633180182981083028, -1.086726831054436682 ) ) ;
#174789=CARTESIAN_POINT ( 'NONE',  ( 4.991753579581297728, -1.905966813954384387, 0.1920618708746626713 ) ) ;
#174796=CARTESIAN_POINT ( 'NONE',  ( 2.114359756454447847, -1.018641858927371135, -1.906637348776268004 ) ) ;
#174800=CARTESIAN_POINT ( 'NONE',  ( 4.788025880137685597, -0.8597811773201522456, 1.610451283527076116 ) ) ;
#174803=CARTESIAN_POINT ( 'NONE',  ( 0.8781228960479293688, -1.098726114091676198, 1.636593336376483743 ) ) ;
#174804=CARTESIAN_POINT ( 'NONE',  ( 3.779479514802902340, 0.2291398179169491789, -1.898525689255560422 ) ) ;
#174807=CARTESIAN_POINT ( 'NONE',  ( 4.703538277703087189, -1.521029056438701232, -1.251204274914043957 ) ) ;
#174809=CARTESIAN_POINT ( 'NONE',  ( 5.987830644705256056, -1.933104919717167025, -0.1861817195589876295 ) ) ;
#174813=CARTESIAN_POINT ( 'NONE',  ( 6.099870585610251084, 1.463495690422533579, 1.534846084132005961 ) ) ;
#174815=CARTESIAN_POINT ( 'NONE',  ( 4.055252259792781366, -1.662250449027093735, 0.9452659147194606426 ) ) ;
#174818=CARTESIAN_POINT ( 'NONE',  ( 0.08333923026508995024, -0.1592477204843331384, -2.171661519566956855 ) ) ;
#174820=CARTESIAN_POINT ( 'NONE',  ( 4.934244218189309805, -1.078892596291732398, -1.699401429059212765 ) ) ;
#174822=CARTESIAN_POINT ( 'NONE',  ( 6.147073579019600054, -1.539581890156189292, 0.9809480439507823890 ) ) ;
#174823=CARTESIAN_POINT ( 'NONE',  ( 6.727182134110202050, 0.5964276595885747989, 1.864301751488647962 ) ) ;
#174824=CARTESIAN_POINT ( 'NONE',  ( 1.522023487246677798, 2.040062638832959241, -0.3519594530456415793 ) ) ;
#174832=CARTESIAN_POINT ( 'NONE',  ( 6.925078400183531713, 7.629137130509067610, 2.355651831298340326 ) ) ;
#174835=CARTESIAN_POINT ( 'NONE',  ( 4.605968593894432139, -0.07825817699743177480, 1.732511586087708499 ) ) ;
#174837=CARTESIAN_POINT ( 'NONE',  ( 2.940353189855488658, -1.068159618217549234, 1.773299548953041871 ) ) ;
#174838=CARTESIAN_POINT ( 'NONE',  ( 3.075892445452293344, -0.8556518723831849638, 1.936791289764336010 ) ) ;
#174842=CARTESIAN_POINT ( 'NONE',  ( 1.621857603371698708, 1.941177911247515375, -0.3314221829187612989 ) ) ;
#174847=CARTESIAN_POINT ( 'NONE',  ( 3.873197071204284914, 2.158828169701370037, -0.7710026823131793661 ) ) ;
#174848=CARTESIAN_POINT ( 'NONE',  ( 2.015964598666186269, -0.8597642540715648707, -1.610575774528985704 ) ) ;
#174853=CARTESIAN_POINT ( 'NONE',  ( 2.760023647720879492, 0.7205980239477025595, -1.880007780590841282 ) ) ;
#174854=CARTESIAN_POINT ( 'NONE',  ( 2.131626046773547500, 1.878804184644796926, -0.5645400877590660560 ) ) ;
#174857=CARTESIAN_POINT ( 'NONE',  ( 0.07536363704233400851, 2.864322694550157866, -2.632457840217194089 ) ) ;
#174858=CARTESIAN_POINT ( 'NONE',  ( 5.208965158259858619, -0.3072975092734456237, 2.067794563079519143 ) ) ;
#174859=CARTESIAN_POINT ( 'NONE',  ( 3.010364070732887143, 1.283045204736869671, -1.219329851163194922 ) ) ;
#174861=CARTESIAN_POINT ( 'NONE',  ( 6.087847202767847854, -2.280615992951875448, -0.2307264670357595804 ) ) ;
#174862=CARTESIAN_POINT ( 'NONE',  ( 5.929613673486688441, 0.8517357041802063877, -1.517590187452934281 ) ) ;
#174864=CARTESIAN_POINT ( 'NONE',  ( 5.801499429514798578, 1.546190052965769057, -1.701143905309614679 ) ) ;
#174865=CARTESIAN_POINT ( 'NONE',  ( 0.1333692844072559003, 2.872395615372814515, -2.542035612928101873 ) ) ;
#174866=CARTESIAN_POINT ( 'NONE',  ( 5.272643526055802887, -1.725312034932389382, 0.1713184177872198732 ) ) ;
#174867=CARTESIAN_POINT ( 'NONE',  ( 5.371592247264787900, -0.3238957681546798528, 2.146784808600268324 ) ) ;
#174869=CARTESIAN_POINT ( 'NONE',  ( 0.3216855292715998793, -1.502087118449943137, -1.492529068308690920 ) ) ;
#174870=CARTESIAN_POINT ( 'NONE',  ( 5.875000000000001776, 2.052068128417940951, -3.214650538869141380E-13 ) ) ;
#174872=CARTESIAN_POINT ( 'NONE',  ( 4.067344539004444037, 0.2368424065766552566, -1.911724265930745847 ) ) ;
#174874=CARTESIAN_POINT ( 'NONE',  ( 6.240512348869785342, 1.279970183950808860, -1.815422973897186543 ) ) ;
#174879=CARTESIAN_POINT ( 'NONE',  ( 2.789914007569836318, 2.108506539658880907, -0.6989939510357189301 ) ) ;
#174885=CARTESIAN_POINT ( 'NONE',  ( 0.4400775573648734174, -1.704940109561555950, -1.076314675215600314 ) ) ;
#174887=CARTESIAN_POINT ( 'NONE',  ( 5.002416047594211435, 2.056911163480923843, 0.1552035700525862538 ) ) ;
#174892=CARTESIAN_POINT ( 'NONE',  ( 1.563349520526525538, 1.744638119327382553, -0.2959517217632592900 ) ) ;
#174893=CARTESIAN_POINT ( 'NONE',  ( 0.1060925565549031974, -0.09613213100253051313, 2.014232862735332308 ) ) ;
#174894=CARTESIAN_POINT ( 'NONE',  ( 5.741712943377584644, 1.738890731700697412, 0.07666446624409603561 ) ) ;
#174896=CARTESIAN_POINT ( 'NONE',  ( 3.615000845857639256, -0.1676676331447447266, 2.286275989141072440 ) ) ;
#174898=CARTESIAN_POINT ( 'NONE',  ( 1.868857239601273923, 1.762127240619456803, -0.5335365013287919345 ) ) ;
#174901=CARTESIAN_POINT ( 'NONE',  ( 2.871877888313049354, 0.9750061419492547232, 1.543211660213184899 ) ) ;
#174902=CARTESIAN_POINT ( 'NONE',  ( 3.709611425391425854, 1.915599900965975433, 0.6298755557959597740 ) ) ;
#174905=CARTESIAN_POINT ( 'NONE',  ( 5.139724016738759005, -1.487180916556319454, -1.491360876250556800 ) ) ;
#174908=CARTESIAN_POINT ( 'NONE',  ( 2.559107912120599071, 1.664280205102614429, -1.231313097332722872 ) ) ;
#174911=CARTESIAN_POINT ( 'NONE',  ( 5.074906250706387567, -1.535530725987072298, 1.462626433913247093 ) ) ;
#174912=CARTESIAN_POINT ( 'NONE',  ( 1.102032671262738850, -1.926676517669764443, -0.0008590682252854196007 ) ) ;
#174919=CARTESIAN_POINT ( 'NONE',  ( 5.783468009189684622, 0.1541500780414573890, -2.115021274163720211 ) ) ;
#174920=CARTESIAN_POINT ( 'NONE',  ( 2.010898292529788467, 1.560970962663108752, -1.413861550561988922 ) ) ;
#174923=CARTESIAN_POINT ( 'NONE',  ( 6.192234700126073577, 0.9181466042854893317, -1.618627059862162376 ) ) ;
#174928=CARTESIAN_POINT ( 'NONE',  ( 0.2641366190093488164, 0.6592694798918593557, -2.015615888626711705 ) ) ;
#174931=CARTESIAN_POINT ( 'NONE',  ( 3.455471728117681440, 1.544996161402897528, 1.208956721487665087 ) ) ;
#174932=CARTESIAN_POINT ( 'NONE',  ( 0.4972265960483426284, 1.796464302094663346, -1.202062886709959422 ) ) ;
#174936=CARTESIAN_POINT ( 'NONE',  ( 2.448798285840974476, 0.4648185774855151942, -1.677030037339591217 ) ) ;
#174939=CARTESIAN_POINT ( 'NONE',  ( 2.741564358335503382, -1.928455994415989139, -0.5879317209081732498 ) ) ;
#174940=CARTESIAN_POINT ( 'NONE',  ( 6.825078400183572036, 2.942104585519232263, 2.696255528691358982 ) ) ;
#174943=CARTESIAN_POINT ( 'NONE',  ( 2.430492692261185805, 1.911874441976011640, 0.4805678379448170001 ) ) ;
#174944=CARTESIAN_POINT ( 'NONE',  ( 6.222915752822945734, 1.412394824171304908, -1.289504995239741714 ) ) ;
#174949=CARTESIAN_POINT ( 'NONE',  ( 0.9088601047923352549, -0.4930153254206064428, -1.958433058913966018 ) ) ;
#174951=CARTESIAN_POINT ( 'NONE',  ( 5.491387719013633983, 2.038315193044057505, -1.081779828593228521 ) ) ;
#174953=CARTESIAN_POINT ( 'NONE',  ( 2.711707638535421960, 0.5279276851305572116, -1.889291386287835550 ) ) ;
#174955=CARTESIAN_POINT ( 'NONE',  ( 0.1236729436712938751, 0.3474707636354073537, 1.986100063511665237 ) ) ;
#174957=CARTESIAN_POINT ( 'NONE',  ( 0.7611333729100393519, -0.05844121263920940695, -2.116714853662078344 ) ) ;
#174960=CARTESIAN_POINT ( 'NONE',  ( 1.675478281319711549, -0.9859397310463119402, 1.554705294492392254 ) ) ;
#174963=CARTESIAN_POINT ( 'NONE',  ( 3.498385214435925317, -1.041973313016024472, 1.846846941210858351 ) ) ;
#174967=CARTESIAN_POINT ( 'NONE',  ( 4.218082229858637788, -1.055972844705153291, -1.769506188133779467 ) ) ;
#174969=CARTESIAN_POINT ( 'NONE',  ( 0.8371598888798935656, 0.7463826720714299423, -1.683355135116317847 ) ) ;
#174974=CARTESIAN_POINT ( 'NONE',  ( 1.489210700298746692, -0.3264265768355456010, -2.182489157894373033 ) ) ;
#174975=CARTESIAN_POINT ( 'NONE',  ( 2.460583821258513382, 0.9655243699240693145, 2.046139933455006776 ) ) ;
#174977=CARTESIAN_POINT ( 'NONE',  ( 1.915983733309385872, -1.811150802387480274, 0.04719988836864030118 ) ) ;
#174978=CARTESIAN_POINT ( 'NONE',  ( 2.536237933002471134, 0.6498936893539140058, 1.802224345963408192 ) ) ;
#174979=CARTESIAN_POINT ( 'NONE',  ( 4.527825515032589898, 2.008996319933327612, -0.4998958796476050681 ) ) ;
#174981=CARTESIAN_POINT ( 'NONE',  ( 3.133621081638960693, -1.322844378366348606, -1.461937730511401190 ) ) ;
#174982=CARTESIAN_POINT ( 'NONE',  ( 6.358035567807713839, 1.921127907539350810, -0.1446545421508997620 ) ) ;
#174983=CARTESIAN_POINT ( 'NONE',  ( 4.293723057671197552, -0.7160966649314598476, 1.728361679364013748 ) ) ;
#174984=CARTESIAN_POINT ( 'NONE',  ( 1.911159365042811809, 1.708073263224022975, -1.551933148444275989 ) ) ;
#174986=CARTESIAN_POINT ( 'NONE',  ( 3.490524873212813795, 1.815147244032933038, 0.4099927795770376693 ) ) ;
#174991=CARTESIAN_POINT ( 'NONE',  ( 0.5222713366250474332, -1.128438999127111098, -1.778050165696586360 ) ) ;
#174994=CARTESIAN_POINT ( 'NONE',  ( 5.677088005223024147, -0.04676544374488526834, -2.161250967910962828 ) ) ;
#174995=CARTESIAN_POINT ( 'NONE',  ( 2.531617689938488791, -0.2033970545941807817, 2.110794199748195599 ) ) ;
#174996=CARTESIAN_POINT ( 'NONE',  ( 6.182287216677275765, 1.039997956529638889, 1.731187096421077376 ) ) ;
#174999=CARTESIAN_POINT ( 'NONE',  ( 1.229993901927586286, -1.370328181169593096, -1.671761099108048265 ) ) ;
#175004=CARTESIAN_POINT ( 'NONE',  ( 5.208220363674559650, 1.197307938467083055, -1.622483861274232719 ) ) ;
#175008=CARTESIAN_POINT ( 'NONE',  ( 6.209879897626497502, -2.145988306206991325, 0.2596296833028768347 ) ) ;
#175011=CARTESIAN_POINT ( 'NONE',  ( -0.08845379458875551881, -1.178863245278682026, -1.510317944339079732 ) ) ;
#175013=CARTESIAN_POINT ( 'NONE',  ( 6.883263157960364254, 2.431740398616466070, 2.435552827938294751 ) ) ;
#175015=CARTESIAN_POINT ( 'NONE',  ( 3.123388959964632949, -1.662097631915793183, 0.4608284732507839654 ) ) ;
#175019=CARTESIAN_POINT ( 'NONE',  ( 1.088686764528872919, 1.564356141470560679, -0.8274751086292527757 ) ) ;
#175020=CARTESIAN_POINT ( 'NONE',  ( 2.033841672972019676, -1.952135521142538854, 0.4911360252713212193 ) ) ;
#175022=CARTESIAN_POINT ( 'NONE',  ( 4.612475435721691497, -0.9401552641563456492, -1.996616816212187340 ) ) ;
#175024=CARTESIAN_POINT ( 'NONE',  ( 4.997030173247643425, 0.3645372836193886967, 2.140096573681660619 ) ) ;
#175028=CARTESIAN_POINT ( 'NONE',  ( 3.739029402251158984, 2.014021593674422572, 0.6637135986873595739 ) ) ;
#175029=CARTESIAN_POINT ( 'NONE',  ( 2.390250109419411295, -0.7743331304885041622, -1.862010821188607945 ) ) ;
#175030=CARTESIAN_POINT ( 'NONE',  ( 3.761794061002172729, 0.6050747832711267371, -1.707706662339498749 ) ) ;
#175036=CARTESIAN_POINT ( 'NONE',  ( 5.883392091387671385, 1.685093539698417242, -0.7030590484573000509 ) ) ;
#175038=CARTESIAN_POINT ( 'NONE',  ( 1.833070758936614864, -1.541008679516321589, -1.137915016233618015 ) ) ;
#175047=CARTESIAN_POINT ( 'NONE',  ( 2.514065211524143084, -0.6609878990531635745, 2.015050547854141172 ) ) ;
#175050=CARTESIAN_POINT ( 'NONE',  ( 4.182859841474963147, -0.1902271694152017079, -1.962134583082324024 ) ) ;
#175051=CARTESIAN_POINT ( 'NONE',  ( 6.222915752822945734, 1.412394824171304908, -1.289504995239741714 ) ) ;
#175053=CARTESIAN_POINT ( 'NONE',  ( 6.139883455347572294, 2.111525295599859575, -0.1581134299761654260 ) ) ;
#175055=CARTESIAN_POINT ( 'NONE',  ( 1.820844063133007396, -1.465591517063179028, 1.462601037713284535 ) ) ;
#175056=CARTESIAN_POINT ( 'NONE',  ( 3.169799299931614911, -1.156099248863748485, 1.560184043245048890 ) ) ;
#175060=CARTESIAN_POINT ( 'NONE',  ( 3.240259679068544507, 0.5084995621511109176, 2.027717503869540749 ) ) ;
#175063=CARTESIAN_POINT ( 'NONE',  ( 0.5042037957796470238, -1.797571035118279870, -0.2231917716723781087 ) ) ;
#175065=CARTESIAN_POINT ( 'NONE',  ( 5.356176587289051660, 2.204499490778097481, -0.1052899746726426722 ) ) ;
#175067=CARTESIAN_POINT ( 'NONE',  ( 2.995379075007987613, 1.893430763284314811, -1.133229021217339483 ) ) ;
#175069=CARTESIAN_POINT ( 'NONE',  ( 1.998553653897700011, -1.875654816251038248, -0.3715787057524469472 ) ) ;
#175071=CARTESIAN_POINT ( 'NONE',  ( 5.090316257491098284, 1.067296284200716983, -1.773933887923849984 ) ) ;
#175073=CARTESIAN_POINT ( 'NONE',  ( 2.413140945657660907, 1.930630709398067246, 0.9725960170764782475 ) ) ;
#175074=CARTESIAN_POINT ( 'NONE',  ( 5.108995794240286159, -0.3219066699026683631, 2.167653318578148358 ) ) ;
#175077=CARTESIAN_POINT ( 'NONE',  ( -0.1294898018152357277, -0.0008549345193623123906, -1.926395771554182179 ) ) ;
#175085=CARTESIAN_POINT ( 'NONE',  ( 6.244996659533327943, -0.2978818936431072983, -2.048576297084458098 ) ) ;
#175086=CARTESIAN_POINT ( 'NONE',  ( 4.002502541323429419, -0.6052661472178870739, -1.829015351804675005 ) ) ;
#175087=CARTESIAN_POINT ( 'NONE',  ( 6.521125090989952078, -1.891168486443073116, 0.9521521135891182208 ) ) ;
#175091=CARTESIAN_POINT ( 'NONE',  ( 5.541845313694261144, 1.319919544752303331, 1.461889559981154108 ) ) ;
#175092=CARTESIAN_POINT ( 'NONE',  ( 0.3049557181189038180, 1.908793570626087455, 1.076422248949958638 ) ) ;
#175093=CARTESIAN_POINT ( 'NONE',  ( 5.690036971771410101, -0.8169618954828453683, 1.632782195682795257 ) ) ;
#175100=CARTESIAN_POINT ( 'NONE',  ( 2.155570461979210428, 0.7887370375637430264, 1.663910549085621415 ) ) ;
#175101=CARTESIAN_POINT ( 'NONE',  ( 5.871345457035325843, -1.728819661934883678, -1.031334786431532313 ) ) ;
#175102=CARTESIAN_POINT ( 'NONE',  ( 0.4744793627779358980, 2.001106834215804042, 1.130494720166761891 ) ) ;
#175103=CARTESIAN_POINT ( 'NONE',  ( 6.016451032921247055, 0.7918200671565789328, 1.795022358689958963 ) ) ;
#175108=CARTESIAN_POINT ( 'NONE',  ( 0.8892259839063383353, 0.1505779921940515187, 2.064926437897919964 ) ) ;
#175110=CARTESIAN_POINT ( 'NONE',  ( 1.874669627338154454, -0.1056657526060876956, -2.088216114563210102 ) ) ;
#175111=CARTESIAN_POINT ( 'NONE',  ( 0.3911966820569385828, 1.383097094795827209, 1.259704262696823118 ) ) ;
#175112=CARTESIAN_POINT ( 'NONE',  ( 1.405624810022429561, 0.3905361843517705100, 1.977748161624798939 ) ) ;
#175113=CARTESIAN_POINT ( 'NONE',  ( -0.2104748580754166321, -0.006608320950486632102, -2.103482951484026309 ) ) ;
#175114=CARTESIAN_POINT ( 'NONE',  ( 2.278492620635372390, 1.590801041788017178, -0.7064735415249421280 ) ) ;
#175118=CARTESIAN_POINT ( 'NONE',  ( 3.017853972043908151, -0.8504761986376055960, -1.500546066986796490 ) ) ;
#175120=CARTESIAN_POINT ( 'NONE',  ( 2.507599501126521524, -2.167277876680247850, 0.3246147914140809498 ) ) ;
#175121=CARTESIAN_POINT ( 'NONE',  ( 5.637410271038987730, -1.996576301129053377, 0.9405272304151901519 ) ) ;
#175123=CARTESIAN_POINT ( 'NONE',  ( 2.799877792657178066, -1.606015216909290277, -1.461049007858437054 ) ) ;
#175124=CARTESIAN_POINT ( 'NONE',  ( 0.7502976729042536430, 0.5272139720400963459, 1.747899773703022408 ) ) ;
#175125=CARTESIAN_POINT ( 'NONE',  ( 3.591103737854687061, 1.818103999434977025, 1.084929287856269742 ) ) ;
#175128=CARTESIAN_POINT ( 'NONE',  ( 3.316269524717931017, 1.452881069417772730, -1.773186822121583184 ) ) ;
#175132=CARTESIAN_POINT ( 'NONE',  ( 6.340512354315207766, 1.281540423541355223, -1.814176132805396691 ) ) ;
#175140=CARTESIAN_POINT ( 'NONE',  ( 4.412732527109735514, -1.242725882911545510, -1.587838301257207041 ) ) ;
#175142=CARTESIAN_POINT ( 'NONE',  ( 3.485269120655315689, 0.04592427588026624929, 2.062205569330832766 ) ) ;
#175147=CARTESIAN_POINT ( 'NONE',  ( 6.228506716250251429, 0.2110190803071687604, 2.181275323772186692 ) ) ;
#175148=CARTESIAN_POINT ( 'NONE',  ( 4.043592392309851569, -1.492256208629010761, 1.356298961253152413 ) ) ;
#175149=CARTESIAN_POINT ( 'NONE',  ( 2.296224312773272658, 1.477747569344042278, -1.098160524033331642 ) ) ;
#175151=CARTESIAN_POINT ( 'NONE',  ( 5.877927443470423619, 1.089437568142386015, 1.464738158297604453 ) ) ;
#175152=CARTESIAN_POINT ( 'NONE',  ( 0.3000039258060793745, 1.578900123410318823, -1.670874907869798864 ) ) ;
#175154=CARTESIAN_POINT ( 'NONE',  ( 6.209908689894510836, -2.246332978858367468, 0.2696892186580777673 ) ) ;
#175156=CARTESIAN_POINT ( 'NONE',  ( 1.682391906368089662, -1.125439293035620292, 1.779948400507038953 ) ) ;
#175166=CARTESIAN_POINT ( 'NONE',  ( 3.252379014334851437, 0.9957207747773239026, -1.985791214296761087 ) ) ;
#175167=CARTESIAN_POINT ( 'NONE',  ( 0.2236267563471248943, -0.1037379595543522215, 2.204571545119632603 ) ) ;
#175170=CARTESIAN_POINT ( 'NONE',  ( 4.193769882565239193, -1.351282707657221582, -1.422545440481419510 ) ) ;
#175179=CARTESIAN_POINT ( 'NONE',  ( 3.972980863544761654, -1.569110274459505350, 1.426624754300914510 ) ) ;
#175181=CARTESIAN_POINT ( 'NONE',  ( 4.434552454296070145, 2.119417814153037316, 0.4246342833542292028 ) ) ;
#175182=CARTESIAN_POINT ( 'NONE',  ( 4.528748383445759806, -1.681502307688139908, 0.7506017836093890061 ) ) ;
#175185=CARTESIAN_POINT ( 'NONE',  ( 6.158121301954061266, -1.225565299391921936, 1.235896697784558906 ) ) ;
#175186=CARTESIAN_POINT ( 'NONE',  ( 6.727182134110198497, 4.703735537933666500, 2.273690654489219032 ) ) ;
#175189=CARTESIAN_POINT ( 'NONE',  ( 3.608425205800522839, -0.8741791752944136906, -1.977237025433141504 ) ) ;
#175190=CARTESIAN_POINT ( 'NONE',  ( 5.220077296912079667, -1.701688162634030999, -1.080898591909580597 ) ) ;
#175192=CARTESIAN_POINT ( 'NONE',  ( 2.307699607974790901, -0.4742087202370263155, 2.108885336910087283 ) ) ;
#175194=CARTESIAN_POINT ( 'NONE',  ( 3.796128654474308028, -1.968949637145664955, -0.1001596523246932047 ) ) ;
#175195=CARTESIAN_POINT ( 'NONE',  ( 2.852750215419812108, -1.865046845876184189, -0.7672916333427428626 ) ) ;
#175197=CARTESIAN_POINT ( 'NONE',  ( 1.255362601414770296, -1.817582055312426004, 1.421667062125511860 ) ) ;
#175198=CARTESIAN_POINT ( 'NONE',  ( 4.054194213510796452, -1.436945492307143635, 1.306602268835421077 ) ) ;
#175208=CARTESIAN_POINT ( 'NONE',  ( 2.661379449941482012, -1.919611247835448342, -1.088434722066232485 ) ) ;
#175210=CARTESIAN_POINT ( 'NONE',  ( 6.016451032921247055, 0.7918200671565789328, 1.795022358689958963 ) ) ;
#175216=CARTESIAN_POINT ( 'NONE',  ( 5.859284738525260217, 1.813109059707292747, -0.3191327317438249489 ) ) ;
#175221=CARTESIAN_POINT ( 'NONE',  ( 6.258074605086497932, 0.8102346573028992305, -1.959903593942226685 ) ) ;
#175224=CARTESIAN_POINT ( 'NONE',  ( 0.3739917644934092067, 1.186169308094830344, 1.685110605438163045 ) ) ;
#175226=CARTESIAN_POINT ( 'NONE',  ( 2.312761410774709425, -1.440873624601293423, 1.177899742917737358 ) ) ;
#175227=CARTESIAN_POINT ( 'NONE',  ( 4.300242120186610784, 1.420457692841030850, -1.171515996850613694 ) ) ;
#175232=VERTEX_POINT ( 'NONE', #23809 ) ;
#175233=CARTESIAN_POINT ( 'NONE',  ( 4.319099500008596770, 2.017107695584336557, 0.8957252843501888329 ) ) ;
#175234=CARTESIAN_POINT ( 'NONE',  ( 6.028679731477588177, 2.178036183261321757, 0.6118574502519974478 ) ) ;
#175236=CARTESIAN_POINT ( 'NONE',  ( 0.1055216070770526038, 1.418477292093557329, 1.282857148695019989 ) ) ;
#175237=CARTESIAN_POINT ( 'NONE',  ( 6.174997428096934193, 1.663181612469267101, -0.9506077395253130780 ) ) ;
#175240=CARTESIAN_POINT ( 'NONE',  ( 5.373660369522260005, 0.3689257714810100230, -1.876182517032434438 ) ) ;
#175242=CARTESIAN_POINT ( 'NONE',  ( 0.4439547499465161251, 1.865322535695708606, 0.1421067652795371117 ) ) ;
#175243=CARTESIAN_POINT ( 'NONE',  ( 1.956267901341804283, -1.236798062192035363, 1.592663274815858676 ) ) ;
#175245=CARTESIAN_POINT ( 'NONE',  ( 4.195997148085639061, -0.8063668458072065226, 1.945788449171739876 ) ) ;
#175250=CARTESIAN_POINT ( 'NONE',  ( 2.549087187268097576, 0.2513027392179004171, 2.004046050866041817 ) ) ;
#175253=CARTESIAN_POINT ( 'NONE',  ( 4.903692054014650026, -0.5817465652163296141, 2.081756923971528117 ) ) ;
#175259=CARTESIAN_POINT ( 'NONE',  ( 1.697964449562241018, -1.571978469985369831, -1.497844480664213052 ) ) ;
#175262=CARTESIAN_POINT ( 'NONE',  ( 1.012948470060770934, -1.796336717620912626, 0.4034172393945419377 ) ) ;
#175264=CARTESIAN_POINT ( 'NONE',  ( 1.558417602779540889, -1.546676288433556756, 1.552911753681482487 ) ) ;
#175265=CARTESIAN_POINT ( 'NONE',  ( 6.883263157960364254, 4.694764272337425659, 2.516417202187768432 ) ) ;
#175266=CARTESIAN_POINT ( 'NONE',  ( 3.204270770158343939, -2.259979215032235977, 0.1094169825565076415 ) ) ;
#175272=CARTESIAN_POINT ( 'NONE',  ( 4.376060336092471026, -1.020005645217741064, 1.445989269263460386 ) ) ;
#175274=CARTESIAN_POINT ( 'NONE',  ( 0.3937647135470741522, 1.560644430845319119, 1.414193795423605904 ) ) ;
#175278=CARTESIAN_POINT ( 'NONE',  ( 6.011342256177333532, -1.897693555989588887, 0.6820111564242032909 ) ) ;
#175284=CARTESIAN_POINT ( 'NONE',  ( 3.660894226558962128, -1.649352935060313552, -0.8826137995501317501 ) ) ;
#175285=CARTESIAN_POINT ( 'NONE',  ( 4.205968427668831389, 0.7022645179026367757, -1.947615878368731623 ) ) ;
#175294=CARTESIAN_POINT ( 'NONE',  ( 3.982823771651412770, 1.862158852298421152, 0.6176278068941787325 ) ) ;
#175295=CARTESIAN_POINT ( 'NONE',  ( 2.249374845261054467, -1.976652949091894707, -0.3960421909960794018 ) ) ;
#175298=CARTESIAN_POINT ( 'NONE',  ( 1.000990332655056436, 1.525750722454706443, 1.081861512215509524 ) ) ;
#175300=CARTESIAN_POINT ( 'NONE',  ( 3.340093095703601023, -1.202498264213421209, -1.614455356613291093 ) ) ;
#175302=CARTESIAN_POINT ( 'NONE',  ( 3.427469813117941744, -1.604901852541072760, -1.381049200617268102 ) ) ;
#175303=CARTESIAN_POINT ( 'NONE',  ( 4.967269779104159788, 1.799668380515653920, 1.023422521214325309 ) ) ;
#175305=CARTESIAN_POINT ( 'NONE',  ( 0.4157161284131759005, -1.121801286243618190, -1.764121917367883263 ) ) ;
#175307=CARTESIAN_POINT ( 'NONE',  ( 5.702125722003772879, -1.825762228975034596, 0.002264948092654816680 ) ) ;
#175314=CARTESIAN_POINT ( 'NONE',  ( 6.463533315534490065, -1.538886664202097965, -1.134999244291827747 ) ) ;
#175329=CARTESIAN_POINT ( 'NONE',  ( 0.1394461523057501928, 1.435241935670927171, -1.984817279021661829 ) ) ;
#175332=CARTESIAN_POINT ( 'NONE',  ( 2.448051270322794348, -0.8465065455745772738, 1.778409512993859076 ) ) ;
#175334=CARTESIAN_POINT ( 'NONE',  ( 3.163685574146878565, 1.281377625384312324, 1.556896677758594416 ) ) ;
#175336=CARTESIAN_POINT ( 'NONE',  ( 6.827182134110198142, 3.677047352536796154, 2.802821765677898203 ) ) ;
#175338=CARTESIAN_POINT ( 'NONE',  ( 3.205210054081304438, -0.4271916898582402422, 2.149238826137919389 ) ) ;
#175340=CARTESIAN_POINT ( 'NONE',  ( 2.397378046164869936, 1.487928659643242169, 1.223526803071661950 ) ) ;
#175344=CARTESIAN_POINT ( 'NONE',  ( 0.2331563151865486683, 7.629137130509099585, -2.545728013813946422 ) ) ;
#175351=CARTESIAN_POINT ( 'NONE',  ( 6.462460624273299814, -1.686435539877573220, -0.7394478613861471539 ) ) ;
#175352=CARTESIAN_POINT ( 'NONE',  ( 2.912746486309669258, -0.5863433081114779455, -1.925794048158388394 ) ) ;
#175353=CARTESIAN_POINT ( 'NONE',  ( 4.394144163123720581, 0.1076087731387373875, 2.295966082354545801 ) ) ;
#175354=CARTESIAN_POINT ( 'NONE',  ( -0.02900071798685525254, 1.326456003635017922, -2.425894103910302135 ) ) ;
#175355=CARTESIAN_POINT ( 'NONE',  ( 2.483057756668010541, -0.005615179255674587061, 1.861131632832468963 ) ) ;
#175358=CARTESIAN_POINT ( 'NONE',  ( 6.293217207623316156, -0.1008467329366956045, -1.909883259500498198 ) ) ;
#175361=CARTESIAN_POINT ( 'NONE',  ( 6.339408610606328764, 0.7995911543839243629, -1.932009116241965252 ) ) ;
#175366=CARTESIAN_POINT ( 'NONE',  ( 5.725168984891365831, -0.03570264050535218447, 1.724697241110892509 ) ) ;
#175368=CARTESIAN_POINT ( 'NONE',  ( 2.004178618920505972, -1.681731546479984463, 0.4224366712483189623 ) ) ;
#175371=CARTESIAN_POINT ( 'NONE',  ( 5.471592230178073279, -0.3258623020658823477, 2.146390899824067056 ) ) ;
#175372=CARTESIAN_POINT ( 'NONE',  ( 4.002439121739418404, -0.5745171773131328985, -1.733004836422600725 ) ) ;
#175373=CARTESIAN_POINT ( 'NONE',  ( 1.780054392102415672, -1.085390340960286082, -1.633940563308281968 ) ) ;
#175376=CARTESIAN_POINT ( 'NONE',  ( 1.998837940877351116, -2.080155006269391205, -0.4107514010402503746 ) ) ;
#175380=CARTESIAN_POINT ( 'NONE',  ( 1.077107760077404830, 1.911388382048292645, 0.7958064784282170567 ) ) ;
#175383=CARTESIAN_POINT ( 'NONE',  ( 3.194184678167404368, 1.410462778303589015, 1.716012817976236171 ) ) ;
#175385=CARTESIAN_POINT ( 'NONE',  ( 1.073308018423566823, -1.027821916426611581, 2.056166664744577321 ) ) ;
#175387=CARTESIAN_POINT ( 'NONE',  ( 6.983263157960404754, -0.005959781318053481922, 2.045923054782183392 ) ) ;
#175391=CARTESIAN_POINT ( 'NONE',  ( 5.864778394761136049, 0.1288883805774850844, -1.836796581567698539 ) ) ;
#175393=CARTESIAN_POINT ( 'NONE',  ( -0.1102773484823937195, 1.994803768489497031, -2.617422746694163749 ) ) ;
#175394=CARTESIAN_POINT ( 'NONE',  ( 3.100334465813825435, -0.4993057154734497072, -1.650917527159057707 ) ) ;
#175395=CARTESIAN_POINT ( 'NONE',  ( 1.288296401830712368, -0.7303101666344159471, -1.879802715551846859 ) ) ;
#175396=CARTESIAN_POINT ( 'NONE',  ( 2.778317543532899947, 1.969881296151472894, -1.184559908770227432 ) ) ;
#175397=CARTESIAN_POINT ( 'NONE',  ( 1.862946185591638049, -1.600570176636705089, 1.599199478044037059 ) ) ;
#175398=CARTESIAN_POINT ( 'NONE',  ( 5.408848747418643299, 1.595474064493606514, -1.374861248814135628 ) ) ;
#175400=CARTESIAN_POINT ( 'NONE',  ( 3.971743243459349149, 0.9813984145389564873, 1.472460009610305320 ) ) ;
#175403=CARTESIAN_POINT ( 'NONE',  ( 0.1118211671861284034, -2.246746504121981403, 0.4537721782011410188 ) ) ;
#175404=CARTESIAN_POINT ( 'NONE',  ( 4.716662652015527257, -0.08744826293657045890, 1.839185557975311358 ) ) ;
#175409=CARTESIAN_POINT ( 'NONE',  ( 4.822331674454460426, 2.096538211656114647, 0.6379635903819569354 ) ) ;
#175412=CARTESIAN_POINT ( 'NONE',  ( 4.826661161267837841, -1.354893614093263254, 1.565527137264411728 ) ) ;
#175413=CARTESIAN_POINT ( 'NONE',  ( 0.2336117360935245635, 0.6279853779636718203, -1.916355031878452797 ) ) ;
#175415=CARTESIAN_POINT ( 'NONE',  ( 3.650929903551769939, -1.574478333125122864, 1.109889904662264115 ) ) ;
#175418=CARTESIAN_POINT ( 'NONE',  ( 0.4225341819744453664, -2.209939313495157265, 0.2258247597332131984 ) ) ;
#175426=CARTESIAN_POINT ( 'NONE',  ( 1.521847698614446687, 1.933392594956625521, -0.3320675068423510345 ) ) ;
#175429=CARTESIAN_POINT ( 'NONE',  ( 5.142999638377217408, -0.2383176028181442918, -1.947251298587366231 ) ) ;
#175433=CARTESIAN_POINT ( 'NONE',  ( 6.350466702034289312, 0.6732396885240909956, 2.054270918568662729 ) ) ;
#175434=CARTESIAN_POINT ( 'NONE',  ( -0.2104748580754391973, 0.7011259924453935310, -2.185273273056092425 ) ) ;
#175437=CARTESIAN_POINT ( 'NONE',  ( 6.661403070661808812, 0.3393488462513394310, -1.941789718247180607 ) ) ;
#175438=CARTESIAN_POINT ( 'NONE',  ( 6.661516750719080449, -0.4673772157907078451, -1.669595843636323185 ) ) ;
#175440=CARTESIAN_POINT ( 'NONE',  ( 2.700927432832851860, 1.852951201923001223, 1.169960570980829839 ) ) ;
#175441=CARTESIAN_POINT ( 'NONE',  ( 4.348838485402671594, 0.6111939248801941948, 2.225120539556017629 ) ) ;
#175442=CARTESIAN_POINT ( 'NONE',  ( 5.764934849280819229, -1.861221615537820728, -0.8850300128313455250 ) ) ;
#175443=CARTESIAN_POINT ( 'NONE',  ( 1.798672962244704410, 1.614485480382701565, 1.078883064099228628 ) ) ;
#175445=EDGE_CURVE ( 'NONE', #88459, #160735, #139142, .T. ) ;
#175447=CARTESIAN_POINT ( 'NONE',  ( 5.414351406770180120, -2.120778210838507150, 0.002142078463891750485 ) ) ;
#175449=CARTESIAN_POINT ( 'NONE',  ( 2.479138880926802901, -2.011204309026824344, -0.1455328587063598189 ) ) ;
#175459=CARTESIAN_POINT ( 'NONE',  ( 6.121960869219821966, -1.142753529713343763, -1.714830629803126616 ) ) ;
#175464=CARTESIAN_POINT ( 'NONE',  ( 4.283856624473350472, 1.958454427565621048, -0.4929297443572661641 ) ) ;
#175470=CARTESIAN_POINT ( 'NONE',  ( 3.836836124264888959, 0.3005266716369097701, 2.038723765318616099 ) ) ;
#175471=CARTESIAN_POINT ( 'NONE',  ( 2.373672848961404735, -0.3474683332905931232, -1.986100487175908258 ) ) ;
#175478=CARTESIAN_POINT ( 'NONE',  ( 3.251327214347735861, -1.985796489957316391, -0.3474142817363470304 ) ) ;
#175479=CARTESIAN_POINT ( 'NONE',  ( 2.413779523973126118, 1.202770565240804279, -1.394052804434331216 ) ) ;
#175480=CARTESIAN_POINT ( 'NONE',  ( 0.7159568421808035765, -0.3331041906398305441, 2.283425790780469811 ) ) ;
#175482=CARTESIAN_POINT ( 'NONE',  ( 3.216266648612066792, -1.062311135343798618, -1.882447817163131587 ) ) ;
#175487=CARTESIAN_POINT ( 'NONE',  ( 3.023178501820302344, 2.287506772329782390, -0.2231754551033394429 ) ) ;
#175490=CARTESIAN_POINT ( 'NONE',  ( 0.7955152940811484052, -0.6771210053572243037, 1.743984199989514927 ) ) ;
#175491=CARTESIAN_POINT ( 'NONE',  ( 5.524284814141814159, 1.174771371627521876, -1.583071389104006244 ) ) ;
#175495=CARTESIAN_POINT ( 'NONE',  ( 0.5224629442122545875, -1.184049029929446828, -1.862174541895257995 ) ) ;
#175498=CARTESIAN_POINT ( 'NONE',  ( 6.539320575229236709, 1.252639605590207150, 2.218328189723097754 ) ) ;
#175499=CARTESIAN_POINT ( 'NONE',  ( 5.207875265678946874, -1.962022031532301369, 0.1926216461900862598 ) ) ;
#175500=CARTESIAN_POINT ( 'NONE',  ( 5.039818274408326637, -1.629004898613298558, -1.634814698366208185 ) ) ;
#175501=CARTESIAN_POINT ( 'NONE',  ( 2.887610015510627459, -1.926180996541780877, 0.7380674418178012619 ) ) ;
#175508=CARTESIAN_POINT ( 'NONE',  ( 4.844266001044335468, -1.027726779992131023, 1.912555630771580084 ) ) ;
#175510=CARTESIAN_POINT ( 'NONE',  ( 3.632213977189250098, 0.2737156317273430894, 1.820677940640710979 ) ) ;
#175513=CARTESIAN_POINT ( 'NONE',  ( 5.214472588068230330, 2.024700573814151028, 0.8392323156421463981 ) ) ;
#175515=CARTESIAN_POINT ( 'NONE',  ( 6.772354121900423962, -1.399018086243536407, 1.779017302379340748 ) ) ;
#175522=CARTESIAN_POINT ( 'NONE',  ( 0.4261447845913856614, 1.691672268694037307, 0.5201907349937917591 ) ) ;
#175523=CARTESIAN_POINT ( 'NONE',  ( 5.760407631487725055, 2.010880845746499279, 0.09660876809274536459 ) ) ;
#175525=CARTESIAN_POINT ( 'NONE',  ( 4.524511627872906061, 1.297711147994727865, -1.658517390945497549 ) ) ;
#175526=CARTESIAN_POINT ( 'NONE',  ( 2.847180372343278254, 0.2781937080071684720, -1.895151957576347579 ) ) ;
#175528=CARTESIAN_POINT ( 'NONE',  ( 4.369560876907440772, -0.3388413995694672387, 1.940020671193002810 ) ) ;
#175530=CARTESIAN_POINT ( 'NONE',  ( 5.660417604421997595, 2.017665076342503916, 0.09485465564632548918 ) ) ;
#175531=CARTESIAN_POINT ( 'NONE',  ( 1.639302681421180852, -1.352760811461351187, -1.292285834730775074 ) ) ;
#175532=CARTESIAN_POINT ( 'NONE',  ( 4.617633504863215776, -1.690751803285206245, 0.3404669814689939011 ) ) ;
#175533=CARTESIAN_POINT ( 'NONE',  ( 1.828231037913151447, -0.9045423626323212396, -1.684975973026317408 ) ) ;
#175534=CARTESIAN_POINT ( 'NONE',  ( 2.649284799151204073, -1.834272514977531632, 1.226802785254533568 ) ) ;
#175537=CARTESIAN_POINT ( 'NONE',  ( 6.268018250734934682, -1.947192974725008963, 0.2387856323943157166 ) ) ;
#175545=CARTESIAN_POINT ( 'NONE',  ( 1.908725956546155178, 0.6474277305483535638, 1.966616875269424192 ) ) ;
#175550=CARTESIAN_POINT ( 'NONE',  ( 0.1881566102324930545, 1.164766123054150837, 1.649759867427439186 ) ) ;
#175556=CARTESIAN_POINT ( 'NONE',  ( 5.852888695852590750, -0.9090035733541059759, 1.799648235488074732 ) ) ;
#175557=CARTESIAN_POINT ( 'NONE',  ( 4.540194369826378029, 0.7389084316076138803, 1.767693002002197034 ) ) ;
#175558=CARTESIAN_POINT ( 'NONE',  ( 3.052458795248469414, -1.657928338269051505, 1.433322580492613296 ) ) ;
#175561=CARTESIAN_POINT ( 'NONE',  ( 5.836195099138038245, -1.121959161234881819, -1.671398195203987136 ) ) ;
#175562=CARTESIAN_POINT ( 'NONE',  ( 1.810667312839256304, -0.5133170510521027907, -1.842115474350584980 ) ) ;
#175565=CARTESIAN_POINT ( 'NONE',  ( 6.468375645409351726, -2.076397406075684682, -0.4129765506453788038 ) ) ;
#175567=CARTESIAN_POINT ( 'NONE',  ( 3.825792374969799514, 1.116656699807290432, -1.767364921024146218 ) ) ;
#175569=CARTESIAN_POINT ( 'NONE',  ( 1.869703332329395895, 0.8828569656042523084, 1.481527559500251501 ) ) ;
#175574=CARTESIAN_POINT ( 'NONE',  ( 0.1683002474503410839, -0.8351952195557797998, -1.773497582445908938 ) ) ;
#175579=CARTESIAN_POINT ( 'NONE',  ( 3.369578772036628145, 0.4373610723380080834, -1.757749666579068171 ) ) ;
#175584=CARTESIAN_POINT ( 'NONE',  ( 3.299258901807587741, 1.636513117289538188, -0.7770104639905143218 ) ) ;
#175585=CARTESIAN_POINT ( 'NONE',  ( 6.639320575229255006, 4.696066290934245657, 2.559399261709224049 ) ) ;
#175589=CARTESIAN_POINT ( 'NONE',  ( 3.947575701020007877, 1.346737928234511106, 1.284688856454605732 ) ) ;
#175590=CARTESIAN_POINT ( 'NONE',  ( 1.704550880262687640, 1.788078052428695219, 0.6877594758711459422 ) ) ;
#175591=CARTESIAN_POINT ( 'NONE',  ( 0.5865807246496178573, -0.2182756592755269454, -1.812417144444453232 ) ) ;
#175599=CARTESIAN_POINT ( 'NONE',  ( 5.629738194587773137, 1.899041559284548208, -0.5217042529989719402 ) ) ;
#175603=CARTESIAN_POINT ( 'NONE',  ( 6.615165563918417924, -2.126712762998611783, 0.5283135293715838232 ) ) ;
#175605=CARTESIAN_POINT ( 'NONE',  ( 5.456054696845579421, 1.924170334762603574, -0.09472988109167354565 ) ) ;
#175608=CARTESIAN_POINT ( 'NONE',  ( 1.272165501999738435, -1.161393580401563375, 1.408505525491813515 ) ) ;
#175609=CARTESIAN_POINT ( 'NONE',  ( 2.174722684859807575, -1.356406721008751814, 1.740749382485320629 ) ) ;
#175611=CARTESIAN_POINT ( 'NONE',  ( 0.6153073421325053749, 1.564839666810373231, 1.099065937236625157 ) ) ;
#175613=CARTESIAN_POINT ( 'NONE',  ( 0.5902130973520075541, 1.015489506344388282, -1.687439782384107634 ) ) ;
#175614=CARTESIAN_POINT ( 'NONE',  ( 2.243606950041766357, 1.941679294436208680, 0.04551257769231514122 ) ) ;
#175616=CARTESIAN_POINT ( 'NONE',  ( 0.4915642615439493879, 1.928455281639355867, 0.5879340682083398217 ) ) ;
#175618=CARTESIAN_POINT ( 'NONE',  ( 6.684420909863875160, 1.071953792136259187, -1.520962823361602601 ) ) ;
#175624=CARTESIAN_POINT ( 'NONE',  ( 2.314256413632868714, 1.428969747754246233, -1.661726224907192684 ) ) ;
#175628=CARTESIAN_POINT ( 'NONE',  ( 2.367563199519676420, 1.790531440309536926, -0.3556685536310541518 ) ) ;
#175635=CARTESIAN_POINT ( 'NONE',  ( 0.9086680563264810662, 1.459560178543020559, -1.257504221390127519 ) ) ;
#175636=CARTESIAN_POINT ( 'NONE',  ( 5.190269257085567745, 1.011813749630154691, -1.680575076195559792 ) ) ;
#175637=CIRCLE ( 'NONE', #57958, 0.04999999999999883010 ) ;
#175641=CARTESIAN_POINT ( 'NONE',  ( 5.337503337980974649, 0.8888059580158399475, -2.003405333693850654 ) ) ;
#175643=CARTESIAN_POINT ( 'NONE',  ( 3.995033623311712301, 0.2988084191791628985, 2.048438004591215389 ) ) ;
#175646=CARTESIAN_POINT ( 'NONE',  ( 3.762538640753902097, 2.164199696370266324, -0.7750164773838670307 ) ) ;
#175650=CARTESIAN_POINT ( 'NONE',  ( 6.620655732516623537, 7.629137130509068498, 2.426260288887295058 ) ) ;
#175652=CARTESIAN_POINT ( 'NONE',  ( 4.997963218837587540, -0.6557800786283998207, -1.827999027568379509 ) ) ;
#175656=CARTESIAN_POINT ( 'NONE',  ( 5.537344615273096515, -0.04053095765194079242, 1.912125305397804009 ) ) ;
#175657=CARTESIAN_POINT ( 'NONE',  ( 6.633849695589691287, -1.131556152058693865, -1.301821263952767316 ) ) ;
#175658=CARTESIAN_POINT ( 'NONE',  ( 4.065638850954083061, 1.320825628876612257, 1.523796413913918624 ) ) ;
#175662=CARTESIAN_POINT ( 'NONE',  ( 1.201248573238463235, -0.5064915201186767080, 2.028225233004859351 ) ) ;
#175663=CARTESIAN_POINT ( 'NONE',  ( 0.4964904254905980197, 1.474999729349553590, -0.9777959528048956184 ) ) ;
#175664=CARTESIAN_POINT ( 'NONE',  ( 5.959611329766300258, -1.915599147091971544, -0.6298778581111733610 ) ) ;
#175666=CARTESIAN_POINT ( 'NONE',  ( 2.519810532312277473, -1.321113963755312870, -1.873090484924363697 ) ) ;
#175667=CARTESIAN_POINT ( 'NONE',  ( 1.657743431332364681, -1.232332549506355290, 1.229129442381997395 ) ) ;
#175668=CARTESIAN_POINT ( 'NONE',  ( 6.559000000000036579, 7.629137130509070275, 2.600000000000001421 ) ) ;
#175669=CARTESIAN_POINT ( 'NONE',  ( 0.5965333524920403141, 0.8982759108043871787, -1.482850294500896560 ) ) ;
#175671=CARTESIAN_POINT ( 'NONE',  ( 1.416206177014844192, 0.7498276349873562729, 1.703500622989342572 ) ) ;
#175672=CARTESIAN_POINT ( 'NONE',  ( 2.699877945841188343, -1.607453219145397849, -1.459642119406568739 ) ) ;
#175673=CARTESIAN_POINT ( 'NONE',  ( 3.925017756809038527, -1.752140073516525565, 0.9981236898717813499 ) ) ;
#175674=CARTESIAN_POINT ( 'NONE',  ( 4.218750000000001776, -0.7852924748297752666, 1.895863743164170057 ) ) ;
#175676=CARTESIAN_POINT ( 'NONE',  ( 6.340456170274588743, 1.905924810476855580, 0.2800546826549690782 ) ) ;
#175678=CARTESIAN_POINT ( 'NONE',  ( 3.217226816143878398, 1.749018536054181672, -1.369387470038183396 ) ) ;
#175684=CARTESIAN_POINT ( 'NONE',  ( -0.07508257667859614959, -0.9546805890920804227, -2.003339222774684458 ) ) ;
#175685=CARTESIAN_POINT ( 'NONE',  ( 4.387127823891323608, 0.09410986116351567621, 1.959716250186482434 ) ) ;
#175689=CARTESIAN_POINT ( 'NONE',  ( 6.134080777514242300, 1.123080384508338136, -1.963935940973794869 ) ) ;
#175690=CARTESIAN_POINT ( 'NONE',  ( 2.400897505987206415, 0.4495084874868838232, 2.012960725780033489 ) ) ;
#175695=CARTESIAN_POINT ( 'NONE',  ( 3.514787476322968285, 1.689724804184733253, 0.8026845837263293371 ) ) ;
#175696=CARTESIAN_POINT ( 'NONE',  ( 2.197566421822871874, 1.549772363009613407, 0.7782106121714903457 ) ) ;
#175697=CARTESIAN_POINT ( 'NONE',  ( 6.392125918040960642, -0.5824770489515176397, -2.112646119873210271 ) ) ;
#175698=CARTESIAN_POINT ( 'NONE',  ( 1.026743138268666922, 1.313310656681260680, -1.773271738842125300 ) ) ;
#175699=CARTESIAN_POINT ( 'NONE',  ( 4.047864428982482110, 0.7307185629543844207, -2.034579650689218866 ) ) ;
#175700=CARTESIAN_POINT ( 'NONE',  ( 5.718683143142158087, -0.04558518807709806275, 1.941574535162658544 ) ) ;
#175710=CARTESIAN_POINT ( 'NONE',  ( 2.982817717652554101, -0.1347461720548545627, -1.820777111243766733 ) ) ;
#175711=CARTESIAN_POINT ( 'NONE',  ( 1.817678338065799704, -0.2697497798337232244, 2.190168480848574628 ) ) ;
#175716=CARTESIAN_POINT ( 'NONE',  ( 1.564719475598770337, 0.6377593443319184985, 1.916497437154760508 ) ) ;
#175717=CARTESIAN_POINT ( 'NONE',  ( 1.119968162728638417, -0.5116716972351254000, 2.057716464106795318 ) ) ;
#175721=CARTESIAN_POINT ( 'NONE',  ( 3.133497910287503796, 1.768579976953125632, -0.5793101531420452588 ) ) ;
#175723=CARTESIAN_POINT ( 'NONE',  ( 5.994767569012836361, -2.000857541758268354, 0.2496038112331094849 ) ) ;
#175724=EDGE_LOOP ( 'NONE', ( #51593, #103523, #129192, #86289 ) ) ;
#175727=CARTESIAN_POINT ( 'NONE',  ( 3.756323439517950558, 0.6585720284536450420, 1.702948436616057881 ) ) ;
#175733=CARTESIAN_POINT ( 'NONE',  ( 6.661482485103542572, -0.5350097378542042481, -1.943772860543022230 ) ) ;
#175734=CARTESIAN_POINT ( 'NONE',  ( 6.017501326166345699, -1.026660802952833240, -1.528114487065170390 ) ) ;
#175735=CARTESIAN_POINT ( 'NONE',  ( -0.02319159430949970999, 0.003959926571647092407, -1.810968101872318714 ) ) ;
#175736=CARTESIAN_POINT ( 'NONE',  ( 4.407023800010228420, 1.785630936674869274, -1.461832730142158088 ) ) ;
#175738=CARTESIAN_POINT ( 'NONE',  ( 6.872347393157318685, -1.336039616365672700, 1.699942530728588919 ) ) ;
#175740=CARTESIAN_POINT ( 'NONE',  ( 2.366656106817651040, 0.09313060749883492195, -1.939932752287050199 ) ) ;
#175742=CARTESIAN_POINT ( 'NONE',  ( 5.870575887392723402, -0.5666052741825926553, 2.227357739769205924 ) ) ;
#175745=CARTESIAN_POINT ( 'NONE',  ( 4.065207594588423845, 0.2294239933214488880, -1.856472568989680161 ) ) ;
#175746=ORIENTED_EDGE ( 'NONE', *, *, #161141, .T. ) ;
#175748=CIRCLE ( 'NONE', #110088, 0.1399999999999995970 ) ;
#175749=CARTESIAN_POINT ( 'NONE',  ( 2.918110517850933672, -1.910018876965378309, 0.09814724848770939314 ) ) ;
#175752=CARTESIAN_POINT ( 'NONE',  ( 3.651171877326536030, -1.804458330144659950, 1.270265763067345066 ) ) ;
#175754=CARTESIAN_POINT ( 'NONE',  ( 6.983263157960370116, 6.036630394911544073, 2.541087343977180613 ) ) ;
#175757=CARTESIAN_POINT ( 'NONE',  ( 1.827351761895773530, -1.857630472158870116, 0.6603073207397982536 ) ) ;
#175758=CARTESIAN_POINT ( 'NONE',  ( 2.151827808644761308, -1.853761708218491178, -1.374033529217959515 ) ) ;
#175759=CARTESIAN_POINT ( 'NONE',  ( 2.295295855072278624, -1.753792786583353580, 0.8793850528211948347 ) ) ;
#175761=CARTESIAN_POINT ( 'NONE',  ( 6.034046607691841757, 1.223980295139483809, 1.660032098485002994 ) ) ;
#175763=CARTESIAN_POINT ( 'NONE',  ( 3.872279980006509970, -1.995268062538615883, -0.2910826752766728642 ) ) ;
#175769=CARTESIAN_POINT ( 'NONE',  ( 2.219799714087321796, 0.3745715905324221162, -2.138378345340052444 ) ) ;
#175773=CARTESIAN_POINT ( 'NONE',  ( 2.002991962376502233, 1.552455721610061179, 1.043161660468715279 ) ) ;
#175774=CARTESIAN_POINT ( 'NONE',  ( 6.116527240895272222, 1.456737685447502262, -1.597155580871166602 ) ) ;
#175775=CARTESIAN_POINT ( 'NONE',  ( -0.02224634325196597762, 0.2233488839939681836, -2.322587069611138144 ) ) ;
#175776=CARTESIAN_POINT ( 'NONE',  ( 6.727182134110202050, 0.5964276595885747989, 1.864301751488647962 ) ) ;
#175779=CARTESIAN_POINT ( 'NONE',  ( 1.787617358713189386, 1.829539840090635749, -0.5563488465884156575 ) ) ;
#175782=CARTESIAN_POINT ( 'NONE',  ( 3.942089010115860326, 1.761346036062165332, 0.1732582469678861092 ) ) ;
#175783=CARTESIAN_POINT ( 'NONE',  ( 1.717294761138322912, 1.590556852780611097, 1.061263400373997134 ) ) ;
#175785=CARTESIAN_POINT ( 'NONE',  ( 6.591422782704708716, -0.4110296003016626898, 1.877638232857116174 ) ) ;
#175787=CARTESIAN_POINT ( 'NONE',  ( 0.8189040078958352842, -1.500748464528355974, 1.426492703164506937 ) ) ;
#175790=CARTESIAN_POINT ( 'NONE',  ( 5.506679003988666388, 1.415762158562785533, -1.222804595763474333 ) ) ;
#175791=CARTESIAN_POINT ( 'NONE',  ( 2.139018802738294589, -1.631172329757241801, 0.8201644002571031322 ) ) ;
#175792=CARTESIAN_POINT ( 'NONE',  ( 5.461621781982892720, 0.4335984126433762853, -2.163701019753036192 ) ) ;
#175795=CARTESIAN_POINT ( 'NONE',  ( 2.646997546006967905, -0.3502154465670388461, -2.032575613165943818 ) ) ;
#175800=CARTESIAN_POINT ( 'NONE',  ( 0.7378453340087381962, -1.528073262844112268, -1.529135702860604074 ) ) ;
#175803=CARTESIAN_POINT ( 'NONE',  ( 5.072747062355987602, 1.430223858385268665, -1.497173470029027120 ) ) ;
#175805=CARTESIAN_POINT ( 'NONE',  ( 2.548304106926166490, 2.161049004374314464, 0.05582717182670697553 ) ) ;
#175807=CARTESIAN_POINT ( 'NONE',  ( 3.334632977657724151, 1.279679970181834436, -1.562544408365494686 ) ) ;
#175808=CARTESIAN_POINT ( 'NONE',  ( 6.720655732516647163, 1.258879151752972048, 2.189434846530075252 ) ) ;
#175814=CARTESIAN_POINT ( 'NONE',  ( 0.9367328597341374463, -1.586666764284098807, 1.244388658875786424 ) ) ;
#175816=CARTESIAN_POINT ( 'NONE',  ( 6.427279137517246888, -1.429865906218323435, -1.660902671979214595 ) ) ;
#175818=CARTESIAN_POINT ( 'NONE',  ( 4.341997288149157086, -1.180789491531178292, -1.504210074635865757 ) ) ;
#175822=CARTESIAN_POINT ( 'NONE',  ( 2.952750085323506024, -1.864176452196796507, -0.7691048347045483791 ) ) ;
#175825=CARTESIAN_POINT ( 'NONE',  ( 5.297747862459361912, -0.6177129893134482019, 1.610538751920454592 ) ) ;
#175829=CARTESIAN_POINT ( 'NONE',  ( 3.919104170388473030, -0.1403237101727794756, 1.865361397874479632 ) ) ;
#175833=CARTESIAN_POINT ( 'NONE',  ( 0.9013344411078340057, -1.777497804657724334, 1.061070337243313455 ) ) ;
#175836=CARTESIAN_POINT ( 'NONE',  ( 6.270143006926431006, 1.806086713848788161, -0.1406222877055433862 ) ) ;
#175838=CARTESIAN_POINT ( 'NONE',  ( 0.4217375466794699435, -1.802849824360297060, 0.1778772001973498718 ) ) ;
#175843=CARTESIAN_POINT ( 'NONE',  ( 0.8890225878602634468, 0.1407106197201784259, 1.956863499422318631 ) ) ;
#175845=CARTESIAN_POINT ( 'NONE',  ( 4.815990648786471873, 0.9809511849332609446, -1.645218558792021613 ) ) ;
#175854=CARTESIAN_POINT ( 'NONE',  ( 1.973706723050288936, 2.068691090354588091, -0.6273066937243013674 ) ) ;
#175859=CARTESIAN_POINT ( 'NONE',  ( 4.981388616008130654, 1.702979688329594676, -0.6582044668519275721 ) ) ;
#175861=CARTESIAN_POINT ( 'NONE',  ( 0.7550724807275938089, -1.663022853828221681, -1.058333363951379003 ) ) ;
#175862=CARTESIAN_POINT ( 'NONE',  ( 3.216961742616857745, 1.504763323797538410, -1.180078671740567131 ) ) ;
#175865=CARTESIAN_POINT ( 'NONE',  ( 4.316829372628319561, -1.460888098903726728, 1.321172513512254065 ) ) ;
#175867=CARTESIAN_POINT ( 'NONE',  ( 6.392136499528294102, -0.5222240449473265489, -1.870457282704639290 ) ) ;
#175871=CARTESIAN_POINT ( 'NONE',  ( 6.451439665316073935, -1.893653415279672902, 0.9546920624979161607 ) ) ;
#175873=CARTESIAN_POINT ( 'NONE',  ( 3.932203299393256302, -0.9856607118853939475, -1.638553295466014248 ) ) ;
#175876=FILL_AREA_STYLE ('',( #109862 ) ) ;
#175877=CARTESIAN_POINT ( 'NONE',  ( 4.617841973404108735, -0.5345865524139911118, 1.940763608534997520 ) ) ;
#175879=CARTESIAN_POINT ( 'NONE',  ( 5.883392091387671385, 1.685093539698417242, -0.7030590484573000509 ) ) ;
#175880=CARTESIAN_POINT ( 'NONE',  ( 1.381394743813993964, -0.05274132383669553892, 2.069866178704110382 ) ) ;
#175891=SURFACE_SIDE_STYLE ('',( #109879 ) ) ;
#175893=CARTESIAN_POINT ( 'NONE',  ( 3.498401880895495086, -1.707742140280370746, 0.3003691301488361498 ) ) ;
#175896=CARTESIAN_POINT ( 'NONE',  ( 2.659107809384615884, 1.665393510391148801, -1.229642267604726058 ) ) ;
#175897=CARTESIAN_POINT ( 'NONE',  ( 3.779011003814860548, 1.787463462570267447, -1.134484337778138174 ) ) ;
#175900=CARTESIAN_POINT ( 'NONE',  ( 0.9011414689646871645, -1.692011168669171672, 1.007586202480597048 ) ) ;
#175905=CARTESIAN_POINT ( 'NONE',  ( 3.609589514692018053, -2.258491968568816066, 0.3911977494595666460 ) ) ;
#175906=CARTESIAN_POINT ( 'NONE',  ( 0.9260630535584664091, 1.089557764695957554, -1.464779044915397455 ) ) ;
#175907=CARTESIAN_POINT ( 'NONE',  ( 3.691585721427274258, 1.799035686688513325, -0.6489376663148455071 ) ) ;
#175911=CARTESIAN_POINT ( 'NONE',  ( 1.775641216270260170, 0.3400756789797795832, -1.984116031292797677 ) ) ;
#175912=CARTESIAN_POINT ( 'NONE',  ( 1.920681792755131845, -1.391007931628859939, 1.383589105726056756 ) ) ;
#175916=CARTESIAN_POINT ( 'NONE',  ( 5.472635741755179417, -0.05041999219103148605, -2.090201512065153366 ) ) ;
#175917=CARTESIAN_POINT ( 'NONE',  ( 3.045496301383675330, 0.6385914081092295413, -1.650799995714345325 ) ) ;
#175919=CARTESIAN_POINT ( 'NONE',  ( 6.562434020506859866, -2.092894318229638895, -0.9354203566987564500 ) ) ;
#175920=CARTESIAN_POINT ( 'NONE',  ( 5.120954501598782294, -1.650910780824323298, 0.5508982476954398244 ) ) ;
#175923=CARTESIAN_POINT ( 'NONE',  ( 5.307816166741994302, -1.486200299559970128, 0.8926388968444918248 ) ) ;
#175924=CARTESIAN_POINT ( 'NONE',  ( 6.303213947599001443, -1.837614076384209261, 1.156103312670229810 ) ) ;
#175926=CARTESIAN_POINT ( 'NONE',  ( 6.350795928397162449, -1.845624747684541989, -0.8128223418941012968 ) ) ;
#175927=CARTESIAN_POINT ( 'NONE',  ( 5.406250000000002665, 1.895863743163962223, -0.7852924748302683167 ) ) ;
#175929=CARTESIAN_POINT ( 'NONE',  ( 3.522408793619712153, 1.222923848883204156, -1.488421986030899591 ) ) ;
#175931=CARTESIAN_POINT ( 'NONE',  ( 0.1357878378635381522, -0.1024811726445598314, 2.219055157331132566 ) ) ;
#175936=CARTESIAN_POINT ( 'NONE',  ( 2.807538669062619174, 1.903917518177394630, -1.144040067606937550 ) ) ;
#175937=CARTESIAN_POINT ( 'NONE',  ( -0.02900071798685524560, 0.6937575422599016051, -2.255700163050919471 ) ) ;
#175941=CARTESIAN_POINT ( 'NONE',  ( 0.5807041986926939625, -0.7231374404764076003, 1.882475062126743204 ) ) ;
#175943=CARTESIAN_POINT ( 'NONE',  ( 5.986801016505616246, 1.986937900772387078, 0.5535461689152029185 ) ) ;
#175948=CARTESIAN_POINT ( 'NONE',  ( 0.3503969169679886919, -1.426633182142377443, 1.047046497418676392 ) ) ;
#175949=CARTESIAN_POINT ( 'NONE',  ( 5.959525138608227302, -1.649545596257080637, -0.5353374286216765476 ) ) ;
#175950=CARTESIAN_POINT ( 'NONE',  ( 6.040530583712122592, -1.465329908677007742, 0.9388326107527265041 ) ) ;
#175951=CARTESIAN_POINT ( 'NONE',  ( 2.595625714788946770, -0.7159257691751429453, 2.177794363412302481 ) ) ;
#175953=CARTESIAN_POINT ( 'NONE',  ( 2.114959233223293822, -1.785989328681826027, 0.4467204754193611627 ) ) ;
#175956=CARTESIAN_POINT ( 'NONE',  ( 2.520284954824199453, 1.194270260598716771, -1.380820861806408617 ) ) ;
#175958=CARTESIAN_POINT ( 'NONE',  ( 4.289685514112329123, 1.556909497225898109, -1.281360267751927129 ) ) ;
#175961=CARTESIAN_POINT ( 'NONE',  ( 5.385806172021708527, 1.412131043145675280, 1.562536384088798691 ) ) ;
#175965=CARTESIAN_POINT ( 'NONE',  ( 2.541538742049511246, 1.893869637037654208, -0.8368498079355383146 ) ) ;
#175968=CARTESIAN_POINT ( 'NONE',  ( 5.127636373287420390, -0.3106611864900838960, 2.097473367668806876 ) ) ;
#175969=CARTESIAN_POINT ( 'NONE',  ( 0.9614038661405551744, 0.3767496340168969837, -1.889141571593662805 ) ) ;
#175977=CARTESIAN_POINT ( 'NONE',  ( -0.2044637419536878831, -0.1604900674421188000, -2.186121014245277383 ) ) ;
#175978=CARTESIAN_POINT ( 'NONE',  ( 1.958176110230916755, 2.100372442369624171, -0.1540336313638566157 ) ) ;
#175981=CARTESIAN_POINT ( 'NONE',  ( 6.877813048773076865, -1.805165420234026818, 0.4518952398848713470 ) ) ;
#175986=CARTESIAN_POINT ( 'NONE',  ( 0.1234922912959918878, 1.848187084301698757, 1.039613981531524400 ) ) ;
#175989=CARTESIAN_POINT ( 'NONE',  ( 1.820681965693775162, -1.389665069980907441, 1.385087887197037571 ) ) ;
#175990=CARTESIAN_POINT ( 'NONE',  ( 0.9366540776252421097, 2.129889809250965271, 0.3686189752144660714 ) ) ;
#175994=CARTESIAN_POINT ( 'NONE',  ( 3.075252150474018009, 1.257817891742564642, -1.193625562640305615 ) ) ;
#175995=CARTESIAN_POINT ( 'NONE',  ( 1.991783209624857331, -0.4627563367010344986, -1.677588981799936541 ) ) ;
#176000=CARTESIAN_POINT ( 'NONE',  ( 1.827499746633702182, -1.427720486614523221, 1.423741782973136694 ) ) ;
#176001=CARTESIAN_POINT ( 'NONE',  ( 6.925078400183550364, 3.684205305355064297, 2.658256427561227486 ) ) ;
#176003=CARTESIAN_POINT ( 'NONE',  ( 0.7781230576423033840, -1.097119503657293382, 1.637799472441689996 ) ) ;
#176004=CARTESIAN_POINT ( 'NONE',  ( 6.082274476537278041, 0.9889857280602430967, 1.636697341158253272 ) ) ;
#176009=CARTESIAN_POINT ( 'NONE',  ( 1.277996545170931197, 1.989402420072207800, -0.3474319251903742467 ) ) ;
#176011=CARTESIAN_POINT ( 'NONE',  ( 5.878008146920711496, 1.368277704907730374, 1.858044196986943675 ) ) ;
#176012=CARTESIAN_POINT ( 'NONE',  ( 5.687936657224680559, -1.243353266631580523, -1.517579924814119074 ) ) ;
#176013=EDGE_CURVE ( 'NONE', #87871, #117162, #170798, .T. ) ;
#176014=CARTESIAN_POINT ( 'NONE',  ( 2.817183829107517745, -1.704460984269993817, -0.9711623693852902139 ) ) ;
#176016=CARTESIAN_POINT ( 'NONE',  ( 0.5103889644224939293, -1.913802852362624929, 0.6352017490645139874 ) ) ;
#176018=CARTESIAN_POINT ( 'NONE',  ( 1.745463160119866686, 0.3564436455325488695, -2.086969855494016368 ) ) ;
#176021=CARTESIAN_POINT ( 'NONE',  ( 2.466542765887615563, 0.09048117372523720170, -1.839033023284454060 ) ) ;
#176024=CARTESIAN_POINT ( 'NONE',  ( 3.111701630267147412, 1.674174984267240429, 1.301503359413098249 ) ) ;
#176028=CARTESIAN_POINT ( 'NONE',  ( 2.776696059289599283, -1.970994871289712069, -0.6015693623636628740 ) ) ;
#176030=CARTESIAN_POINT ( 'NONE',  ( 0.01093749962182561514, -1.805946196879631094, 0.3578947576599255664 ) ) ;
#176032=CARTESIAN_POINT ( 'NONE',  ( -0.02244404828160087226, 0.2256878572204877031, -2.222431841814066278 ) ) ;
#176035=CARTESIAN_POINT ( 'NONE',  ( 0.06543086261080394150, -1.973449318085427340, -0.9880335165917543128 ) ) ;
#176036=CARTESIAN_POINT ( 'NONE',  ( 2.442968603456824095, 0.4936193734879111283, 2.207763252559187261 ) ) ;
#176038=CARTESIAN_POINT ( 'NONE',  ( 2.970771795020191064, -1.368765343908146415, 1.186782720094860855 ) ) ;
#176039=CARTESIAN_POINT ( 'NONE',  ( 3.573361294032686430, 1.391295603808204051, 1.317194196901736669 ) ) ;
#176040=CARTESIAN_POINT ( 'NONE',  ( 3.807136610393092813, -1.694265131726957252, 1.189645435975445809 ) ) ;
#176042=CARTESIAN_POINT ( 'NONE',  ( 2.325019196037684477, -0.001775356835979901692, 1.971640592446997298 ) ) ;
#176043=CARTESIAN_POINT ( 'NONE',  ( 6.621714856310891406, -1.867994803139013005, 0.4708039761674199797 ) ) ;
#176044=CARTESIAN_POINT ( 'NONE',  ( 2.500682550815761740, 1.503739811390795378, -1.112508705057350999 ) ) ;
#176045=CARTESIAN_POINT ( 'NONE',  ( 2.790017796326722532, 1.632578265707486098, 1.631241332076227346 ) ) ;
#176047=CARTESIAN_POINT ( 'NONE',  ( 2.629178708315405455, 0.09452080204645990635, -1.858793618116144186 ) ) ;
#176049=CARTESIAN_POINT ( 'NONE',  ( 6.391093295415360309, 0.1985076180841711668, 2.053089703019762791 ) ) ;
#176053=CARTESIAN_POINT ( 'NONE',  ( 0.9968619785027620361, -0.5136065205212798634, -2.042351051948914531 ) ) ;
#176055=CARTESIAN_POINT ( 'NONE',  ( 5.747404748698970778, -1.700087083557629386, -1.334863535946126500 ) ) ;
#176056=CARTESIAN_POINT ( 'NONE',  ( 0.1584709747761771925, 2.014675524564497167, 0.1441611394625528231 ) ) ;
#176064=CARTESIAN_POINT ( 'NONE',  ( 4.329314735043091389, -1.561880650076686861, -1.275557594027726394 ) ) ;
#176067=CARTESIAN_POINT ( 'NONE',  ( 5.875883356151954118, 1.283970044810868849, 1.738936680771227206 ) ) ;
#176072=CARTESIAN_POINT ( 'NONE',  ( -0.07089544441234334193, -1.481030113823898375, -1.214736957437832832 ) ) ;
#176076=CARTESIAN_POINT ( 'NONE',  ( 2.297083607218278978, 1.332544580598886252, 1.095227982430951208 ) ) ;
#176080=CARTESIAN_POINT ( 'NONE',  ( 0.5086179708909451813, 1.535567861042252957, 0.8796773807029609760 ) ) ;
#176081=CARTESIAN_POINT ( 'NONE',  ( 2.174478567003877316, 0.8628565524405201748, 1.818940509527650295 ) ) ;
#176083=CARTESIAN_POINT ( 'NONE',  ( 3.803933094734159415, -0.6430795383850876901, 2.110982628114480786 ) ) ;
#176084=CARTESIAN_POINT ( 'NONE',  ( 5.436453865645980876, -1.212139536413152197, 1.801006579369943239 ) ) ;
#176088=CARTESIAN_POINT ( 'NONE',  ( 3.492942606646631809, -2.044086983709763050, -0.5638711869686771072 ) ) ;
#176089=CARTESIAN_POINT ( 'NONE',  ( 2.689077551358230789, 1.704951624378052033, 1.076298511635757738 ) ) ;
#176090=CARTESIAN_POINT ( 'NONE',  ( 3.586021145937230870, 1.010873021915110748, 1.503094931805592394 ) ) ;
#176094=CARTESIAN_POINT ( 'NONE',  ( 0.2681426532152464959, -1.225442487749365483, 1.413462724991432218 ) ) ;
#176096=CARTESIAN_POINT ( 'NONE',  ( 6.147073579019600054, -1.539581890156189292, 0.9809480439507823890 ) ) ;
#176098=CARTESIAN_POINT ( 'NONE',  ( 1.956118367686721538, -1.175378340988470827, 1.512710158094223933 ) ) ;
#176105=CARTESIAN_POINT ( 'NONE',  ( 5.647404790089923132, -1.701416311724871067, -1.333359258283283166 ) ) ;
#176108=CARTESIAN_POINT ( 'NONE',  ( 2.883181758455736432, -1.960942133159260692, -0.8077274430827171559 ) ) ;
#176111=CARTESIAN_POINT ( 'NONE',  ( 4.130118527232538028, 1.057347662480428108, -1.663647784685320818 ) ) ;
#176112=CARTESIAN_POINT ( 'NONE',  ( -0.2047996464942871964, -0.1441562275304847374, -1.980932652848297115 ) ) ;
#176114=CARTESIAN_POINT ( 'NONE',  ( 5.665271214873143890, 1.955333520279872506, -0.8127364881663766694 ) ) ;
#176116=CARTESIAN_POINT ( 'NONE',  ( 0.5024991115675537801, 2.064720838319131779, 0.1538615064654233477 ) ) ;
#176117=CARTESIAN_POINT ( 'NONE',  ( 2.958853767740171392, 0.2844919188511252917, -1.920881014358867489 ) ) ;
#176121=CARTESIAN_POINT ( 'NONE',  ( 4.083990600187762610, -2.067889708199427190, -0.3066597852425279047 ) ) ;
#176124=CARTESIAN_POINT ( 'NONE',  ( 0.2756360753965527155, 1.792041154956749871, -0.2637626551888968551 ) ) ;
#176125=VERTEX_POINT ( 'NONE', #121057 ) ;
#176126=CARTESIAN_POINT ( 'NONE',  ( 5.795608111622330583, 1.668732747960173235, 1.444295198399044855 ) ) ;
#176129=CARTESIAN_POINT ( 'NONE',  ( 2.925073249431627165, 2.077443920948469192, 0.7446974470129497092 ) ) ;
#176132=CARTESIAN_POINT ( 'NONE',  ( 2.174333686202088334, 0.8191313854410250395, 1.728107290330855639 ) ) ;
#176134=CARTESIAN_POINT ( 'NONE',  ( 5.863751307568212390, -0.5067217619753560109, 2.007263066363853987 ) ) ;
#176136=CARTESIAN_POINT ( 'NONE',  ( 3.274459119871219848, -1.289031633699176949, 1.735169069618908821 ) ) ;
#176137=CARTESIAN_POINT ( 'NONE',  ( 4.528971853086540378, -2.003544689622422936, 0.8885388601788182239 ) ) ;
#176148=CARTESIAN_POINT ( 'NONE',  ( 5.436411051413860385, -1.154718516627372127, 1.718110687276501958 ) ) ;
#176149=CARTESIAN_POINT ( 'NONE',  ( 4.336495953379083446, 1.889596944713485049, 0.3744603196194126182 ) ) ;
#176150=CARTESIAN_POINT ( 'NONE',  ( 6.345324880664913181, 0.3618513607092630480, -2.085922816363374288 ) ) ;
#176154=CARTESIAN_POINT ( 'NONE',  ( 4.645333151331359822, 1.761124666023382579, -0.8816396696852289994 ) ) ;
#176155=CARTESIAN_POINT ( 'NONE',  ( 0.7443833103580773658, 0.6396484562771963533, 2.096019810003430184 ) ) ;
#176156=CARTESIAN_POINT ( 'NONE',  ( 4.547361323050268744, -1.413013347330991598, -1.156083184146582177 ) ) ;
#176162=CARTESIAN_POINT ( 'NONE',  ( 2.682954136603598272, 1.303717545168959990, 1.300458928786947688 ) ) ;
#176163=CARTESIAN_POINT ( 'NONE',  ( 5.291276029577359985, -0.05376236717486576611, -2.012660120947160181 ) ) ;
#176164=CARTESIAN_POINT ( 'NONE',  ( 1.388484499181727561, -0.05552238045265603383, 2.297868740670248044 ) ) ;
#176165=CARTESIAN_POINT ( 'NONE',  ( 5.752778578519474273, -0.4731148833870613690, -1.903749215227706015 ) ) ;
#176169=CARTESIAN_POINT ( 'NONE',  ( 0.9595327444568906294, 1.691550050060253829, 1.193477315110213599 ) ) ;
#176171=CARTESIAN_POINT ( 'NONE',  ( 1.048509228467583876, -1.645825662996244443, 1.289236127856315139 ) ) ;
#176172=CARTESIAN_POINT ( 'NONE',  ( 0.1978467685152424937, -1.870139902624564865, -0.05068021481659244765 ) ) ;
#176175=CARTESIAN_POINT ( 'NONE',  ( 1.628031597684251208, 0.1703553616784689029, 1.732092769550299227 ) ) ;
#176179=CARTESIAN_POINT ( 'NONE',  ( 2.701417116451056533, -0.5414251306648624196, 1.637772108618321454 ) ) ;
#176180=CARTESIAN_POINT ( 'NONE',  ( 2.208753784402537335, 1.959192758111829136, 0.9821998110004714899 ) ) ;
#176181=CARTESIAN_POINT ( 'NONE',  ( 0.1055823559395060729, -0.08803060671099156853, 1.732021048141555220 ) ) ;
#176182=CARTESIAN_POINT ( 'NONE',  ( 4.653060005753134831, -1.773635849817876586, 1.313014255023836618 ) ) ;
#176184=CARTESIAN_POINT ( 'NONE',  ( 2.676840970354518845, 1.421027823260514911, -1.641450307487320792 ) ) ;
#176185=CARTESIAN_POINT ( 'NONE',  ( 0.8908993799596062191, 1.611356928563783208, -0.8583080905386344384 ) ) ;
#176186=CARTESIAN_POINT ( 'NONE',  ( 2.993478482863177081, -0.4084587893785693868, 2.077413892881809776 ) ) ;
#176187=CARTESIAN_POINT ( 'NONE',  ( 6.639320575229259447, 2.978120323461688201, 2.350396677589302374 ) ) ;
#176189=CARTESIAN_POINT ( 'NONE',  ( 3.228363206396630769, 2.236961789864226002, 0.5003539455325100027 ) ) ;
#176193=CARTESIAN_POINT ( 'NONE',  ( 5.549557930969759134, -2.008940618436024117, 0.9481178722350207533 ) ) ;
#176199=CARTESIAN_POINT ( 'NONE',  ( 3.902970337090125863, -1.038992709432768891, -1.728002613881730598 ) ) ;
#176201=CARTESIAN_POINT ( 'NONE',  ( 1.639586372526161684, 1.907294469559306815, -0.7855861486642725655 ) ) ;
#176206=CARTESIAN_POINT ( 'NONE',  ( 4.910206770677443266, 1.512653250323254817, -1.585896273577400706 ) ) ;
#176207=CARTESIAN_POINT ( 'NONE',  ( 2.725232599228684993, 2.001511357256777313, 0.2440295182731533341 ) ) ;
#176208=CARTESIAN_POINT ( 'NONE',  ( 1.786409390178132162, 1.601450680722369846, -0.9084932335857234253 ) ) ;
#176210=CARTESIAN_POINT ( 'NONE',  ( 6.299803673773761936, -0.6120917497752301761, 1.720027978493202436 ) ) ;
#176211=CARTESIAN_POINT ( 'NONE',  ( 0.001177798100650446610, -2.252613640939280515, 0.4573402144308849615 ) ) ;
#176213=CARTESIAN_POINT ( 'NONE',  ( 6.086863830973287648, -0.3249354738291005407, -2.238958312302678610 ) ) ;
#176215=CARTESIAN_POINT ( 'NONE',  ( 1.436301726765435438, 1.036571610867568216, -1.833232669937171266 ) ) ;
#176224=CARTESIAN_POINT ( 'NONE',  ( 1.617596980227502756, 1.765956010477184535, 1.173731981927571555 ) ) ;
#176225=CARTESIAN_POINT ( 'NONE',  ( 3.375417215397161552, -1.960608319544883793, -1.044296844735680185 ) ) ;
#176230=CARTESIAN_POINT ( 'NONE',  ( 4.105873170248697690, 0.6631157982108953908, -1.846516426336957784 ) ) ;
#176238=CARTESIAN_POINT ( 'NONE',  ( 3.691739789689612472, 1.995538565534977549, -0.7177698711837015022 ) ) ;
#176240=CARTESIAN_POINT ( 'NONE',  ( 3.872077330825273389, 1.198917189070296541, 1.798566189592496034 ) ) ;
#176241=CARTESIAN_POINT ( 'NONE',  ( 3.966218424140379728, -1.719484690100345325, -0.6589542199007536460 ) ) ;
#176244=CARTESIAN_POINT ( 'NONE',  ( 5.876847675788273939, 1.605460876287589045, -0.6722632963065499068 ) ) ;
#176245=CARTESIAN_POINT ( 'NONE',  ( 6.727182134110202050, 0.5964276595885747989, 1.864301751488647962 ) ) ;
#176249=CARTESIAN_POINT ( 'NONE',  ( 2.870174731959000525, 1.155358403710282866, 1.826860881501219280 ) ) ;
#176251=CARTESIAN_POINT ( 'NONE',  ( 6.098982473628085543, 0.9961464269193781584, -1.752763620266280187 ) ) ;
#176253=CARTESIAN_POINT ( 'NONE',  ( 2.342841879718413622, 0.4729757327756216601, 2.109170662781891359 ) ) ;
#176254=CARTESIAN_POINT ( 'NONE',  ( 3.884019131438942285, -0.9746410142534560617, 1.713524893406521699 ) ) ;
#176255=CARTESIAN_POINT ( 'NONE',  ( -0.05867695357848409787, -1.698172713885632401, -1.384993232510664640 ) ) ;
#176256=CARTESIAN_POINT ( 'NONE',  ( 4.317874670498635048, 1.191976824791032064, -1.533171632797071693 ) ) ;
#176265=CARTESIAN_POINT ( 'NONE',  ( 2.081372155488591780, -0.1082299263688718260, -2.204229314041641352 ) ) ;
#176267=CARTESIAN_POINT ( 'NONE',  ( 6.930524233185829885, -1.209519613549964845, 1.545115813350018241 ) ) ;
#176273=CARTESIAN_POINT ( 'NONE',  ( 5.050657991863417351, -1.557144343216086968, -0.9820927893566462341 ) ) ;
#176278=CARTESIAN_POINT ( 'NONE',  ( 5.888958097455845753, -2.014202512972632420, -0.6635655960139997811 ) ) ;
#176281=CARTESIAN_POINT ( 'NONE',  ( 6.134070664438048048, 1.019536383099900245, -1.790854842558225801 ) ) ;
#176283=CARTESIAN_POINT ( 'NONE',  ( 2.330303589177587398, -1.147911989558418222, 1.464751052146954224 ) ) ;
#176284=CARTESIAN_POINT ( 'NONE',  ( 4.897927690869709139, -0.6253142351902387652, -1.731941863025769246 ) ) ;
#176290=CARTESIAN_POINT ( 'NONE',  ( 4.987059637548557411, -0.2676712469649074055, -2.190530366034774801 ) ) ;
#176291=CARTESIAN_POINT ( 'NONE',  ( 5.589262808440923713, 1.998987879104210608, -1.059483486058722779 ) ) ;
#176293=CARTESIAN_POINT ( 'NONE',  ( 5.677939507029830857, 1.783257022268599723, -0.3182440143107477248 ) ) ;
#176294=CARTESIAN_POINT ( 'NONE',  ( 0.1281391398850126040, 2.011452084832816123, 0.1435147193784985509 ) ) ;
#176297=CARTESIAN_POINT ( 'NONE',  ( 6.649288223980674317, -1.503899034092892162, -1.112267350887645945 ) ) ;
#176298=CARTESIAN_POINT ( 'NONE',  ( 5.320932177894995618, 1.445329238430465013, -1.252218921613167169 ) ) ;
#176300=CARTESIAN_POINT ( 'NONE',  ( 0.9713206009373563932, 1.803875226702996049, -0.4951341686536685494 ) ) ;
#176301=CARTESIAN_POINT ( 'NONE',  ( 0.7961116948485976730, -0.9110139862544311962, -1.799120828532501326 ) ) ;
#176303=CARTESIAN_POINT ( 'NONE',  ( 4.266313661023513504, 0.9922932564179194337, 1.857654695958657953 ) ) ;
#176308=CARTESIAN_POINT ( 'NONE',  ( 2.970967976831692781, -1.526577591334898454, 1.322595846222093030 ) ) ;
#176311=CARTESIAN_POINT ( 'NONE',  ( 4.886082254767631916, -1.023713625618065004, 1.903838226609423590 ) ) ;
#176317=CARTESIAN_POINT ( 'NONE',  ( 0.9245737983274513461, 1.070221580302813891, 1.888989948743382552 ) ) ;
#176321=CARTESIAN_POINT ( 'NONE',  ( 1.980270094416748394, -2.150034404144373301, -0.4237573071887782983 ) ) ;
#176323=CARTESIAN_POINT ( 'NONE',  ( 2.114515676104791186, -1.066955051536956356, -1.995125387583786214 ) ) ;
#176329=CARTESIAN_POINT ( 'NONE',  ( 3.989309445023786704, 1.280397443517577782, 1.221928027103141634 ) ) ;
#176331=CARTESIAN_POINT ( 'NONE',  ( 0.4640741377587159211, 2.083006155408675397, -0.3091503547662070583 ) ) ;
#176335=CARTESIAN_POINT ( 'NONE',  ( 5.976185453469534892, -2.006962702346287930, -0.1948244327795861652 ) ) ;
#176336=CARTESIAN_POINT ( 'NONE',  ( 5.009926431283926895, -0.6449355957302944642, 1.693101296380158383 ) ) ;
#176339=CARTESIAN_POINT ( 'NONE',  ( 3.168673215318769110, -1.727878594304607995, -0.7172629358194044791 ) ) ;
#176340=CARTESIAN_POINT ( 'NONE',  ( 4.891501605334720004, -1.894957309059261297, 0.8341102180390786991 ) ) ;
#176349=CARTESIAN_POINT ( 'NONE',  ( 3.613678190204441254, 0.4790664972640528152, -1.902336835828049244 ) ) ;
#176350=CARTESIAN_POINT ( 'NONE',  ( 0.8958609827393304581, 0.1455075039201655374, 2.010896580075637541 ) ) ;
#176353=CARTESIAN_POINT ( 'NONE',  ( 0.9658262494645246665, 0.9167188063998463754, 1.630421345857439475 ) ) ;
#176355=CARTESIAN_POINT ( 'NONE',  ( 2.953388010686915255, -1.773442693046624496, 0.9528950618205129786 ) ) ;
#176357=CARTESIAN_POINT ( 'NONE',  ( 2.390374844762462203, -0.8132668539616545456, -1.954994498336021458 ) ) ;
#176360=CARTESIAN_POINT ( 'NONE',  ( 4.686024408448190570, -1.271122505372159539, -1.634150330299996012 ) ) ;
#176362=CARTESIAN_POINT ( 'NONE',  ( 6.509723796436136745, -0.9841294377065135102, -1.844520550012812565 ) ) ;
#176364=CARTESIAN_POINT ( 'NONE',  ( 4.805575371506604299, -0.4859443722219913830, 1.759630929660048526 ) ) ;
#176370=CARTESIAN_POINT ( 'NONE',  ( 6.036183878773405453, 1.092744051193066834, -1.917163762461614240 ) ) ;
#176373=CARTESIAN_POINT ( 'NONE',  ( 4.758414378865199801, 1.907420806491459064, 0.1369992607160031295 ) ) ;
#176389=CARTESIAN_POINT ( 'NONE',  ( 1.990998161727207449, 0.1877779126488627881, 1.960439330322023999 ) ) ;
#176390=CARTESIAN_POINT ( 'NONE',  ( 3.146111402376899235, 0.9091623069825971459, 1.799915193831227889 ) ) ;
#176393=CARTESIAN_POINT ( 'NONE',  ( 6.827182134110224787, 2.426453598513299337, 2.470348285387702347 ) ) ;
#176394=CARTESIAN_POINT ( 'NONE',  ( 3.187623232016934871, -0.8878212517344568067, 2.003729935572157839 ) ) ;
#176396=CARTESIAN_POINT ( 'NONE',  ( 2.520427876150105995, 1.259661825572227167, -1.457548065151576200 ) ) ;
#176399=CARTESIAN_POINT ( 'NONE',  ( 0.2331563151865729544, 6.948071805571808035, -2.540803835148666145 ) ) ;
#176404=CARTESIAN_POINT ( 'NONE',  ( 6.198766299729112639, 1.534709720371667308, 1.016988835930050739 ) ) ;
#176405=CARTESIAN_POINT ( 'NONE',  ( 2.561191855132368467, -1.672464352163150147, 1.120165047906955147 ) ) ;
#176406=CARTESIAN_POINT ( 'NONE',  ( 3.972236164830291738, 1.968842830503451991, 1.185689330230592642 ) ) ;
#176407=CARTESIAN_POINT ( 'NONE',  ( -0.02880301295727759683, -0.006976478922920535501, -2.273770288744044521 ) ) ;
#176408=CARTESIAN_POINT ( 'NONE',  ( 2.553354172538614630, 1.434905519572576171, 1.184926768776579431 ) ) ;
#176411=CARTESIAN_POINT ( 'NONE',  ( 5.695548698317931091, 1.764485844685494742, -0.7379451211212140205 ) ) ;
#176414=CARTESIAN_POINT ( 'NONE',  ( 4.827721544939969966, 1.073412050285113661, -1.793994897088858176 ) ) ;
#176415=CARTESIAN_POINT ( 'NONE',  ( 3.696050037196423332, -1.868490534004090931, -0.09263902202472777681 ) ) ;
#176420=CARTESIAN_POINT ( 'NONE',  ( 6.006443931695136129, -0.6276177885309804916, -1.606848298988555301 ) ) ;
#176422=CARTESIAN_POINT ( 'NONE',  ( 1.582203977811939000, -0.5845794355729941882, 1.632800797419992955 ) ) ;
#176426=CARTESIAN_POINT ( 'NONE',  ( 5.682552277248558603, 1.299237613850280360, -1.739252610423980938 ) ) ;
#176427=CARTESIAN_POINT ( 'NONE',  ( 4.125493313500066428, -1.746467973620144942, 0.5319596651164605339 ) ) ;
#176428=CARTESIAN_POINT ( 'NONE',  ( 1.955835763735654487, -0.6658547638305843952, 1.845409454533278648 ) ) ;
#176429=CARTESIAN_POINT ( 'NONE',  ( 6.280470216940358341, -0.5666190470481970998, -2.040018813895160044 ) ) ;
#176433=CARTESIAN_POINT ( 'NONE',  ( 2.367978261241600713, 0.5630001329197281690, -2.044326955284565539 ) ) ;
#176436=CARTESIAN_POINT ( 'NONE',  ( 6.965710887581792576, -0.4882203796070741508, 2.123536573467856403 ) ) ;
#176439=CARTESIAN_POINT ( 'NONE',  ( 3.106314965395097438, -0.8985160938580877277, 2.031629072759451926 ) ) ;
#176441=CARTESIAN_POINT ( 'NONE',  ( 0.8448572530952251913, 0.4413087945813984336, -2.255810399402935484 ) ) ;
#176443=CARTESIAN_POINT ( 'NONE',  ( 5.032111728107424575, 1.183179145130999643, 1.689302184701612086 ) ) ;
#176446=CARTESIAN_POINT ( 'NONE',  ( 0.2329586101569553480, 1.399178205689523224, -2.105666472772389941 ) ) ;
#176447=CARTESIAN_POINT ( 'NONE',  ( 5.390138975101268493, -0.4531076923771395482, -1.784498753146485539 ) ) ;
#176450=CARTESIAN_POINT ( 'NONE',  ( 3.469487465715580310, 1.682841854137674398, -0.3771888234031828824 ) ) ;
#176451=CARTESIAN_POINT ( 'NONE',  ( 1.200408080392855181, 1.350732740426639822, -1.497504596960941958 ) ) ;
#176452=CARTESIAN_POINT ( 'NONE',  ( 3.024404714233555946, -2.025920917938589749, 1.086156575756046294 ) ) ;
#176453=CARTESIAN_POINT ( 'NONE',  ( 2.759333473672697767, -1.967098484071924558, -1.117512413888957612 ) ) ;
#176454=CARTESIAN_POINT ( 'NONE',  ( 5.022148466640797615, -1.125808720090130111, -1.779717422886097244 ) ) ;
#176456=CARTESIAN_POINT ( 'NONE',  ( 3.215802288110910290, -0.8691132097216300867, -1.541513200001721540 ) ) ;
#176458=CARTESIAN_POINT ( 'NONE',  ( 0.1294186239076781653, -2.093018298938463140, 0.9351526010841960668 ) ) ;
#176459=CARTESIAN_POINT ( 'NONE',  ( 4.628748294741646951, -1.682209325509572473, 0.7487199040775437409 ) ) ;
#176463=CARTESIAN_POINT ( 'NONE',  ( 4.505938053128990539, -0.9357023767473917619, -1.981784127816770935 ) ) ;
#176466=CARTESIAN_POINT ( 'NONE',  ( 4.738769824615551407, -2.007376682328159134, -0.5062664373569197851 ) ) ;
#176470=CARTESIAN_POINT ( 'NONE',  ( 3.035679594228014810, -1.294101122711612151, -1.427291446562365618 ) ) ;
#176472=CARTESIAN_POINT ( 'NONE',  ( 0.1764466950717893667, 2.196028898142581731, -0.3343166089466164115 ) ) ;
#176481=CARTESIAN_POINT ( 'NONE',  ( 0.9944974185457016169, 1.932217576897478528, 0.3389098420027157332 ) ) ;
#176484=CARTESIAN_POINT ( 'NONE',  ( 6.649309733611729278, -1.732918351142084035, -1.292073167451508686 ) ) ;
#176485=CARTESIAN_POINT ( 'NONE',  ( 5.986763597034562068, 1.890319730748804439, 0.5246630281777532323 ) ) ;
#176488=CARTESIAN_POINT ( 'NONE',  ( 5.717692609583751029, -2.109997883074541392, 0.4692839721026839661 ) ) ;
#176492=CARTESIAN_POINT ( 'NONE',  ( 0.4911964603225346115, 1.381658100223854380, 1.261112594198803061 ) ) ;
#176493=CARTESIAN_POINT ( 'NONE',  ( 6.116466030266402676, 0.5002120791919911769, -1.660072079997718442 ) ) ;
#176495=CARTESIAN_POINT ( 'NONE',  ( 3.474349307649237328, -2.112600797985896950, -0.5827812199917583591 ) ) ;
#176496=CARTESIAN_POINT ( 'NONE',  ( 4.137936126805092485, -1.588447180316322260, -1.674080592224574504 ) ) ;
#176497=CARTESIAN_POINT ( 'NONE',  ( 6.221960870361377793, -1.141027836104959281, -1.715851070140647527 ) ) ;
#176498=CARTESIAN_POINT ( 'NONE',  ( 1.306472565299764410, 1.712382563992039586, 0.9159111323687963990 ) ) ;
#176502=CARTESIAN_POINT ( 'NONE',  ( 5.361630242575341931, -1.673063676233761621, -1.302930760576012092 ) ) ;
#176503=CARTESIAN_POINT ( 'NONE',  ( 1.986954140179174155, -2.015912935764123670, 0.05229865529512293942 ) ) ;
#176505=CARTESIAN_POINT ( 'NONE',  ( 5.174942826180319422, -2.076333920960464763, -0.7478091396579674699 ) ) ;
#176508=CARTESIAN_POINT ( 'NONE',  ( 0.04711308451243316486, -1.408776630263553375, -1.161003007932148501 ) ) ;
#176514=CARTESIAN_POINT ( 'NONE',  ( 4.452062314400541787, 2.060485596604546110, -0.04854883430290175134 ) ) ;
#176519=CARTESIAN_POINT ( 'NONE',  ( 5.004559639922408820, -2.004681531738555123, -0.2449335584770311880 ) ) ;
#176525=CARTESIAN_POINT ( 'NONE',  ( 4.135659164760732587, -1.419885373862592726, -1.493960738838293389 ) ) ;
#176526=CARTESIAN_POINT ( 'NONE',  ( 2.918592439375994552, -1.356299846568160827, -1.492255409411529898 ) ) ;
#176528=CARTESIAN_POINT ( 'NONE',  ( 6.727182134110201162, 1.237345558575109861, 2.302850971298702643 ) ) ;
#176532=CARTESIAN_POINT ( 'NONE',  ( 2.811874868751465417, -1.677748492350576770, 1.117661080827489606 ) ) ;
#176533=CARTESIAN_POINT ( 'NONE',  ( 2.765369989423609454, 0.9851603262180377296, 1.555203531693909680 ) ) ;
#176535=CARTESIAN_POINT ( 'NONE',  ( 1.173011757359025520, -1.460375281577396489, 1.786833355454720884 ) ) ;
#176537=CARTESIAN_POINT ( 'NONE',  ( 2.038557401052975671, 2.137775048120754029, 0.3193135401893046899 ) ) ;
#176541=CARTESIAN_POINT ( 'NONE',  ( 1.375632740723360836, 1.111493989511678881, 1.504490780774490499 ) ) ;
#176543=CARTESIAN_POINT ( 'NONE',  ( 5.998895389381466714, 1.612053949438954303, -1.134635204971563782 ) ) ;
#176548=CARTESIAN_POINT ( 'NONE',  ( 0.3994152196779980346, 1.832435997337564348, -1.229551327501000380 ) ) ;
#176549=CARTESIAN_POINT ( 'NONE',  ( 6.707487347292075519, -1.660346423639452951, -1.236579608897829363 ) ) ;
#176552=CARTESIAN_POINT ( 'NONE',  ( 6.539320575229278454, 2.035006821797652687, 2.408631514295301645 ) ) ;
#176553=CARTESIAN_POINT ( 'NONE',  ( 5.102397915883716273, -0.6633297369818305089, -1.856656708325474581 ) ) ;
#176554=CARTESIAN_POINT ( 'NONE',  ( -0.01710467543277957581, -1.380256469788909035, 1.610041658517608054 ) ) ;
#176556=CARTESIAN_POINT ( 'NONE',  ( 5.057380973065424001, -1.947307563149714316, -1.238062830034118988 ) ) ;
#176557=CARTESIAN_POINT ( 'NONE',  ( 1.428664617098963863, -1.311459235982143534, 1.591897985181329966 ) ) ;
#176561=( BOUNDED_SURFACE ( )  B_SPLINE_SURFACE ( 3, 3, ( 
 ( #40860, #26713, #106966, #24571, #154598, #124315, #122180, #191333, #105883, #10456, #76529 ),
 ( #8329, #58156, #207593, #142642, #208650, #190274, #187076, #157805, #38709, #59212, #170835 ),
 ( #41931, #204369, #89610, #22426, #171908, #6176, #138352, #56027, #23504, #155661, #7243 ),
 ( #112308, #110176, #180434, #209713, #163132, #176187, #78657, #15775, #60281, #28858, #97079 ),
 ( #144785, #210793, #113378, #29931, #14716, #27787, #126438, #12585, #98140, #178323, #93885 ),
 ( #62416, #159925, #45131, #179384, #192401, #11528, #13657, #80807, #128580, #193489, #44057 ),
 ( #147945, #77598, #143721, #96015, #111241, #160993, #177246, #61358, #127517, #194546, #94945 ) ),
 .UNSPECIFIED., .T., .F., .T. ) 
 B_SPLINE_SURFACE_WITH_KNOTS ( ( 4, 3, 4 ),
 ( 4, 1, 1, 1, 1, 1, 1, 1, 4 ),
 ( 0.000000000000000000, 0.5000000000000000000, 1.000000000000000000 ),
 ( 0.000000000000000000, 0.2255234228546724728, 0.3973271701647976828, 0.5245128843546777997, 0.6161923999872991331, 0.6815320185768301009, 0.7298552812456317040, 0.7704940248801678271, 1.000000000000000000 ),
 .UNSPECIFIED. ) 
 GEOMETRIC_REPRESENTATION_ITEM ( )  RATIONAL_B_SPLINE_SURFACE ( (
 ( 1.000000000000000222, 1.000000000000000222, 1.000000000000000666, 0.9999999999999996669, 1.000000000000000222, 0.9999999999999997780, 1.000000000000000000, 1.000000000000000222, 1.000000000000000000, 1.000000000000000000, 1.000000000000000000),
 ( 0.3333333333333334259, 0.3333333333333334259, 0.3333333333333335369, 0.3333333333333333148, 0.3333333333333333148, 0.3333333333333333703, 0.3333333333333333703, 0.3333333333333334814, 0.3333333333333333148, 0.3333333333333334259, 0.3333333333333333703),
 ( 0.3333333333333334259, 0.3333333333333334259, 0.3333333333333335369, 0.3333333333333333148, 0.3333333333333333148, 0.3333333333333333703, 0.3333333333333333703, 0.3333333333333334814, 0.3333333333333333148, 0.3333333333333334259, 0.3333333333333333703),
 ( 1.000000000000000222, 1.000000000000000222, 1.000000000000000666, 0.9999999999999996669, 1.000000000000000222, 0.9999999999999997780, 1.000000000000000000, 1.000000000000000222, 1.000000000000000000, 1.000000000000000000, 1.000000000000000000),
 ( 0.3333333333333334259, 0.3333333333333334259, 0.3333333333333335369, 0.3333333333333333148, 0.3333333333333333148, 0.3333333333333333703, 0.3333333333333333703, 0.3333333333333334814, 0.3333333333333333148, 0.3333333333333334259, 0.3333333333333333703),
 ( 0.3333333333333334259, 0.3333333333333334259, 0.3333333333333335369, 0.3333333333333333148, 0.3333333333333333148, 0.3333333333333333703, 0.3333333333333333703, 0.3333333333333334814, 0.3333333333333333148, 0.3333333333333334259, 0.3333333333333333703),
 ( 1.000000000000000222, 1.000000000000000222, 1.000000000000000666, 0.9999999999999996669, 1.000000000000000222, 0.9999999999999997780, 1.000000000000000000, 1.000000000000000222, 1.000000000000000000, 1.000000000000000000, 1.000000000000000000) ) ) 
 REPRESENTATION_ITEM ( '' )  SURFACE ( )  );
#176565=CARTESIAN_POINT ( 'NONE',  ( 4.809118753965334392, -1.746635306876740401, 1.289517135737711540 ) ) ;
#176567=CARTESIAN_POINT ( 'NONE',  ( 4.317794123949899365, 1.129187743159822288, -1.454283868005897151 ) ) ;
#176570=CARTESIAN_POINT ( 'NONE',  ( 5.442994344319362021, -1.727133847215430729, -1.348975639928217118 ) ) ;
#176572=CARTESIAN_POINT ( 'NONE',  ( 5.998944898715565799, 1.853732409352136568, -1.296943227565182877 ) ) ;
#176579=CARTESIAN_POINT ( 'NONE',  ( 1.059032582198644601, 0.3505281480379630610, -1.734596922625891713 ) ) ;
#176580=CARTESIAN_POINT ( 'NONE',  ( 5.092444288794719220, -1.116435683446183713, 1.674956235503543889 ) ) ;
#176582=CARTESIAN_POINT ( 'NONE',  ( 3.962026973360888604, 2.090321222856437178, -0.2555144258320155015 ) ) ;
#176583=CARTESIAN_POINT ( 'NONE',  ( 2.056118223505171372, -1.176884799952466087, 1.511379468370318113 ) ) ;
#176584=CARTESIAN_POINT ( 'NONE',  ( -0.02244404828157658613, 5.719765766439059540, -2.783169749654360814 ) ) ;
#176585=CARTESIAN_POINT ( 'NONE',  ( 3.490635713810024132, 1.920951117756137583, 0.4340392168088512692 ) ) ;
#176586=CARTESIAN_POINT ( 'NONE',  ( 5.238538122511118722, 1.199862898965612823, -1.624631798562142793 ) ) ;
#176587=CARTESIAN_POINT ( 'NONE',  ( 2.078771448894382701, -0.08914341469279044028, -1.868647664167771616 ) ) ;
#176588=CARTESIAN_POINT ( 'NONE',  ( 5.355954780876127863, 1.722648150766812103, -0.09025627888907016005 ) ) ;
#176589=CARTESIAN_POINT ( 'NONE',  ( 1.248149539447914735, 0.9399939672071171426, -1.665319807275446706 ) ) ;
#176591=CARTESIAN_POINT ( 'NONE',  ( 1.647397727484143592, -1.863059487452220386, 1.182652941231487453 ) ) ;
#176596=CARTESIAN_POINT ( 'NONE',  ( 6.526239545637954720, 1.075124705556152138, -1.530631868311462362 ) ) ;
#176601=CARTESIAN_POINT ( 'NONE',  ( 2.119664376568120012, 0.3561266789769075292, -2.039353370234835872 ) ) ;
#176606=CARTESIAN_POINT ( 'NONE',  ( 6.147156607449644206, 0.2074554230099104890, 2.110329589018632657 ) ) ;
#176611=CARTESIAN_POINT ( 'NONE',  ( 4.130232389481975908, 0.2495678132241747615, -2.000550906993769473 ) ) ;
#176612=CARTESIAN_POINT ( 'NONE',  ( 4.997249278368244951, -0.2745004324337502744, 1.895803710022869959 ) ) ;
#176614=CARTESIAN_POINT ( 'NONE',  ( 3.157961424266928052, 0.9873743524775533409, 1.956624655947765357 ) ) ;
#176615=FACE_OUTER_BOUND ( 'NONE', #152642, .T. ) ;
#176617=CARTESIAN_POINT ( 'NONE',  ( 5.519794446587845016, -0.4848760706452569513, 1.953846845731139759 ) ) ;
#176620=CARTESIAN_POINT ( 'NONE',  ( -0.01795374796791787686, -2.016030408028956167, -0.04665595434990427171 ) ) ;
#176623=CARTESIAN_POINT ( 'NONE',  ( 3.069954157378000925, -1.243473088950231675, 1.680628819622100423 ) ) ;
#176625=CARTESIAN_POINT ( 'NONE',  ( 1.518105509412637444, 1.162241833864360974, -1.274548180342775838 ) ) ;
#176627=CARTESIAN_POINT ( 'NONE',  ( 6.099870585610251972, 1.463495690422533579, 1.534846084132005961 ) ) ;
#176635=CARTESIAN_POINT ( 'NONE',  ( 1.471055694106305101, -1.553634009935511484, -0.9311844293155254748 ) ) ;
#176641=CARTESIAN_POINT ( 'NONE',  ( 2.842218536208180435, 1.004546245467073717, -1.507189720918320486 ) ) ;
#176642=CARTESIAN_POINT ( 'NONE',  ( 6.639320575229255006, 7.629137130509086262, 2.596737603865982624 ) ) ;
#176645=CARTESIAN_POINT ( 'NONE',  ( 3.560865204049929122, 1.468383728701172064, -1.143307097947023010 ) ) ;
#176646=CARTESIAN_POINT ( 'NONE',  ( 1.563933522115690922, -1.023182376180698849, 1.619245466209729756 ) ) ;
#176647=CARTESIAN_POINT ( 'NONE',  ( 0.9030137451815029026, 1.489685209907613439, 1.054989265776705709 ) ) ;
#176654=CARTESIAN_POINT ( 'NONE',  ( 5.313322838536244319, -1.661678602684885986, -1.056841482759300233 ) ) ;
#176657=CARTESIAN_POINT ( 'NONE',  ( 0.02354010051478470922, -1.288079656314411459, -1.647238045112088267 ) ) ;
#176659=CARTESIAN_POINT ( 'NONE',  ( 4.911117597291495329, 1.675855952751242883, 0.9498910403669177382 ) ) ;
#176661=CARTESIAN_POINT ( 'NONE',  ( 1.166719304534512558, -1.648536928579244165, -0.7845717211837842653 ) ) ;
#176662=CARTESIAN_POINT ( 'NONE',  ( 2.051678093609669240, -1.773579625386853875, -1.313098587465796774 ) ) ;
#176665=CARTESIAN_POINT ( 'NONE',  ( 0.6253724811571198527, 0.1964764651697422093, -1.959740272926189464 ) ) ;
#176666=CARTESIAN_POINT ( 'NONE',  ( 2.735803960117746403, 1.927664933923057600, 0.2353960755621438972 ) ) ;
#176667=CARTESIAN_POINT ( 'NONE',  ( 1.212267286723569981, -1.587592435625035270, -1.242539042498117086 ) ) ;
#176669=CARTESIAN_POINT ( 'NONE',  ( 5.260548175522302472, -0.6249328720258572334, -1.753037815340392935 ) ) ;
#176675=CARTESIAN_POINT ( 'NONE',  ( 1.488088480104592826, -2.181432686776756391, -0.2102995727721947705 ) ) ;
#176679=CARTESIAN_POINT ( 'NONE',  ( 3.299243935302543118, 1.439784963707075649, 1.122460502641378755 ) ) ;
#176683=DIRECTION ( 'NONE',  ( 2.949029909160572061E-17, 1.000000000000000000, -8.673600428462353400E-15 ) ) ;
#176685=CARTESIAN_POINT ( 'NONE',  ( 1.242661541247750856, 0.3750627104036097781, 1.889477121596821352 ) ) ;
#176686=CARTESIAN_POINT ( 'NONE',  ( 5.102378460580520247, 1.956245014681293970, 0.1482201060269832671 ) ) ;
#176690=CARTESIAN_POINT ( 'NONE',  ( 5.495707582769355781, -2.191739722525353429, -0.0009102486706394352645 ) ) ;
#176692=CARTESIAN_POINT ( 'NONE',  ( 3.502843950909264592, 0.4983820457637299639, 2.009271733256080772 ) ) ;
#176693=CARTESIAN_POINT ( 'NONE',  ( 0.1331565106231328843, 0.003911343561965873426, -1.946049565259087455 ) ) ;
#176696=CARTESIAN_POINT ( 'NONE',  ( 3.780169564947546856, 1.941421826978003251, -1.230584599089700637 ) ) ;
#176698=ORIENTED_EDGE ( 'NONE', *, *, #150667, .F. ) ;
#176703=CARTESIAN_POINT ( 'NONE',  ( 3.785046133934614865, 1.407330997726879973, 1.338362524258763786 ) ) ;
#176707=CARTESIAN_POINT ( 'NONE',  ( 5.414289803398987466, -1.912571729023364364, 0.006307610287324683096 ) ) ;
#176708=CARTESIAN_POINT ( 'NONE',  ( 5.948237010872538200, 1.723075781188963207, 0.07969437682242562493 ) ) ;
#176709=CARTESIAN_POINT ( 'NONE',  ( 4.768767694835816862, -0.2516295123269947642, -2.000731945836851544 ) ) ;
#176711=CARTESIAN_POINT ( 'NONE',  ( 2.209865124170300898, -0.4819264253047173541, 2.153463223375853719 ) ) ;
#176714=CARTESIAN_POINT ( 'NONE',  ( 2.132869701138325969, -1.867042483574256728, 0.9408474824332532238 ) ) ;
#176715=CARTESIAN_POINT ( 'NONE',  ( 6.485617131683707903, 1.222450955268041373, 1.279935727357548458 ) ) ;
#176716=CARTESIAN_POINT ( 'NONE',  ( 5.854138739207011888, 0.1455364397412381439, -2.011204036175239018 ) ) ;
#176718=CARTESIAN_POINT ( 'NONE',  ( 3.486539624822242889, -0.4467316994782115636, -2.248153690150441975 ) ) ;
#176719=CARTESIAN_POINT ( 'NONE',  ( 0.8490573499697011695, 1.738566659290440963, -0.08130723561216267326 ) ) ;
#176721=CARTESIAN_POINT ( 'NONE',  ( 2.988655875014298857, -1.259908772670719657, 1.705623289672608678 ) ) ;
#176723=CARTESIAN_POINT ( 'NONE',  ( 1.493026163575939425, 1.669116110853157808, 0.4689669769783275100 ) ) ;
#176726=CARTESIAN_POINT ( 'NONE',  ( 0.8894206616707257540, 0.1598827910747530057, 2.165323314709698632 ) ) ;
#176727=CARTESIAN_POINT ( 'NONE',  ( 3.380092458137720968, -2.014432998692190058, -0.09411721906785883163 ) ) ;
#176728=CARTESIAN_POINT ( 'NONE',  ( 5.093750000000003553, -1.895863743164187376, -0.7852924748297283042 ) ) ;
#176730=CARTESIAN_POINT ( 'NONE',  ( 0.1297406284284522426, -1.182532350666727128, -1.521449160436913584 ) ) ;
#176732=CARTESIAN_POINT ( 'NONE',  ( 3.006315081767933606, -0.8967225907310495403, 2.032537921011686954 ) ) ;
#176737=EDGE_CURVE ( 'NONE', #88820, #8341, #165408, .T. ) ;
#176738=CARTESIAN_POINT ( 'NONE',  ( 4.915436192723389830, -0.9368120511010556983, -1.466610992562596527 ) ) ;
#176739=CARTESIAN_POINT ( 'NONE',  ( 4.123457186961496213, 0.2424046295769199388, -1.946780420294342617 ) ) ;
#176743=CARTESIAN_POINT ( 'NONE',  ( 4.411571241670419141, -0.3925092328114428986, 2.227967001921112633 ) ) ;
#176744=CARTESIAN_POINT ( 'NONE',  ( 1.979039114045421988, 1.923815945824264073, 0.7444423131674202665 ) ) ;
#176748=CARTESIAN_POINT ( 'NONE',  ( 3.356579238971897805, -1.418645411611328067, 1.219307012350186126 ) ) ;
#176749=CARTESIAN_POINT ( 'NONE',  ( 2.092031233620697872, -0.3790036544207425195, 1.692025817237676311 ) ) ;
#176750=CARTESIAN_POINT ( 'NONE',  ( 6.585463931165095985, -0.9389328202267492873, 1.978239266594773671 ) ) ;
#176751=CARTESIAN_POINT ( 'NONE',  ( 0.7455094363101981703, -1.891729906373079029, 1.136061337225414913 ) ) ;
#176752=CARTESIAN_POINT ( 'NONE',  ( 4.135729569369491543, -1.488772398488470872, -1.567562023322838671 ) ) ;
#176753=CARTESIAN_POINT ( 'NONE',  ( 4.347558855881414885, 1.941490382076584975, -0.04909019101095174475 ) ) ;
#176754=EDGE_CURVE ( 'NONE', #112905, #21324, #121792, .T. ) ;
#176757=CARTESIAN_POINT ( 'NONE',  ( 0.1762450972803019933, 2.096614079038420897, -0.3174041833761130360 ) ) ;
#176759=CARTESIAN_POINT ( 'NONE',  ( 5.625625018759272677, 0.3960990390993284205, 1.976956468877195894 ) ) ;
#176763=CARTESIAN_POINT ( 'NONE',  ( 2.947667120405720986, 0.6567698719579934119, -1.703645827024417914 ) ) ;
#176764=CARTESIAN_POINT ( 'NONE',  ( 2.714145368365259436, -2.182908968410116834, 0.3227909207665635716 ) ) ;
#176770=CARTESIAN_POINT ( 'NONE',  ( 0.9670638486888746277, -1.589497524861957611, 1.246053474203263178 ) ) ;
#176771=CARTESIAN_POINT ( 'NONE',  ( 0.8211285067932658777, 1.603129840700336706, -1.388046135824993366 ) ) ;
#176775=CARTESIAN_POINT ( 'NONE',  ( 2.061162768541408230, 1.543764177570670970, 1.038864413082870142 ) ) ;
#176777=CARTESIAN_POINT ( 'NONE',  ( 1.129994055010040022, -1.371941552271437770, -1.670562328977095445 ) ) ;
#176778=CARTESIAN_POINT ( 'NONE',  ( 5.942029771888944545, -1.730864577151491890, -1.034168155301495862 ) ) ;
#176782=CARTESIAN_POINT ( 'NONE',  ( 3.668406916800326822, -1.225078373119499187, 1.353803248016255178 ) ) ;
#176788=CARTESIAN_POINT ( 'NONE',  ( 5.975935433960425591, 1.776740614516297390, 0.9528632009266968517 ) ) ;
#176789=CARTESIAN_POINT ( 'NONE',  ( 6.316338248019477852, 1.719745045379994286, 0.6579504788090041467 ) ) ;
#176791=CARTESIAN_POINT ( 'NONE',  ( 4.635575047956096206, -2.111140572116900316, 0.9323621513206108435 ) ) ;
#176793=CARTESIAN_POINT ( 'NONE',  ( 5.501312752317830679, 1.763641270444433307, 1.249554385337700024 ) ) ;
#176795=CARTESIAN_POINT ( 'NONE',  ( 1.768985407559420020, 1.857901784229658793, -0.5654475766003872472 ) ) ;
#176796=CARTESIAN_POINT ( 'NONE',  ( 4.692867332335362462, -1.408920786844407802, -1.815866644984363232 ) ) ;
#176799=CARTESIAN_POINT ( 'NONE',  ( 5.119927267529915227, -1.001353885182048931, -1.579878405157906673 ) ) ;
#176801=CARTESIAN_POINT ( 'NONE',  ( 2.812653035604309348, -0.5591599321941118639, -1.828790038765286452 ) ) ;
#176805=CARTESIAN_POINT ( 'NONE',  ( 3.862124860921032354, 2.190326239153097543, -0.2693113811002012525 ) ) ;
#176806=CARTESIAN_POINT ( 'NONE',  ( 6.983263157960402090, -0.0002233252893329463486, 1.845923184817334084 ) ) ;
#176807=CARTESIAN_POINT ( 'NONE',  ( -0.2108831679770959699, 2.036692374882024037, -2.313561348563981657 ) ) ;
#176810=CARTESIAN_POINT ( 'NONE',  ( 1.317580156568556538, -1.924246910545416522, 0.4277698889081028577 ) ) ;
#176812=CARTESIAN_POINT ( 'NONE',  ( 1.431196836673795936, 2.224535207900823153, 0.6132342015414853353 ) ) ;
#176813=CARTESIAN_POINT ( 'NONE',  ( 3.033595934319989418, 1.863777508880835487, -0.6128360024686765328 ) ) ;
#176815=CARTESIAN_POINT ( 'NONE',  ( 5.910998778867512016, -1.629530645011644463, 1.264396865911474821 ) ) ;
#176822=CARTESIAN_POINT ( 'NONE',  ( 1.903425830921786188, -1.835712436893768063, 1.158886079418340875 ) ) ;
#176828=CARTESIAN_POINT ( 'NONE',  ( 2.460033746253722065, 0.7958763861501785275, 1.692906160045657860 ) ) ;
#176829=CARTESIAN_POINT ( 'NONE',  ( 6.538358481810655043, 2.137031053877674225, 0.3242996077847115632 ) ) ;
#176830=CARTESIAN_POINT ( 'NONE',  ( -0.02244404828160087226, 1.323617703852699057, -2.440988974267483957 ) ) ;
#176831=CARTESIAN_POINT ( 'NONE',  ( 6.827182134110225675, 7.053278108740402175, 2.409100297097351184 ) ) ;
#176834=CARTESIAN_POINT ( 'NONE',  ( 2.455592584850064153, -1.418247937500687561, -1.282927761235647335 ) ) ;
#176835=CARTESIAN_POINT ( 'NONE',  ( 4.170580646280578563, -1.651567487535645640, -0.6365977468129493388 ) ) ;
#176836=CARTESIAN_POINT ( 'NONE',  ( 2.033716200607054159, -1.854476301366870805, 0.4660679227486630438 ) ) ;
#176839=CARTESIAN_POINT ( 'NONE',  ( 0.07520289192196588646, 1.421326540713454323, 1.284674935297628773 ) ) ;
#176841=CARTESIAN_POINT ( 'NONE',  ( 0.7134375191242479097, -1.748147108003229810, -1.108949491591210146 ) ) ;
#176844=CARTESIAN_POINT ( 'NONE',  ( 5.594569530875262764, -0.4557361262383100020, -1.814172972432124720 ) ) ;
#176845=CARTESIAN_POINT ( 'NONE',  ( 1.805030607383810715, 1.517133602069477893, 1.015288170653723343 ) ) ;
#176846=CARTESIAN_POINT ( 'NONE',  ( 4.846401659255799466, 2.200796399388889935, 0.1645688927329121420 ) ) ;
#176849=CARTESIAN_POINT ( 'NONE',  ( 3.561030563730323006, 1.627881067681248073, -1.266672197246907494 ) ) ;
#176857=CARTESIAN_POINT ( 'NONE',  ( 5.687960312649480876, -1.310561514506687564, -1.602779375087557412 ) ) ;
#176859=CARTESIAN_POINT ( 'NONE',  ( 2.196749789412206333, -0.5742421066207163971, -2.083876772215712325 ) ) ;
#176862=CARTESIAN_POINT ( 'NONE',  ( 2.965494806321045562, -1.652366046825021417, -1.161084516292823832 ) ) ;
#176869=CARTESIAN_POINT ( 'NONE',  ( 1.393767942625488532, -2.000731169080074423, 0.2516357431460446992 ) ) ;
#176871=CARTESIAN_POINT ( 'NONE',  ( 5.864808805604325492, 0.1626094438406736342, -2.185560445749204828 ) ) ;
#176873=CARTESIAN_POINT ( 'NONE',  ( 4.799029005866479736, -0.2398712174674077491, -1.897248949554980024 ) ) ;
#176877=CARTESIAN_POINT ( 'NONE',  ( 3.831657784458125438, 0.6766976527424087839, -1.899625577706779422 ) ) ;
#176880=CARTESIAN_POINT ( 'NONE',  ( 5.245002492778637837, -1.477622881800463306, 0.8893561077145789584 ) ) ;
#176886=CARTESIAN_POINT ( 'NONE',  ( 1.164989683304976875, 1.570165760251106990, -1.349419213858449318 ) ) ;
#176889=CARTESIAN_POINT ( 'NONE',  ( 5.760388245948376174, 1.809740711040405348, 0.08207984589548086851 ) ) ;
#176891=CARTESIAN_POINT ( 'NONE',  ( 0.05236148938883232462, -1.314980595004966002, 1.528755779884483523 ) ) ;
#176892=CARTESIAN_POINT ( 'NONE',  ( 0.3514446173804542939, -1.281351489097491303, -1.280874292944272685 ) ) ;
#176895=CARTESIAN_POINT ( 'NONE',  ( 3.416156609664961152, 1.390242785425911620, -1.694013327489252152 ) ) ;
#176898=CARTESIAN_POINT ( 'NONE',  ( 1.117545225965112188, 0.3861695934333775337, -1.923310697798483293 ) ) ;
#176900=CARTESIAN_POINT ( 'NONE',  ( 5.273012193977356432, 1.687281682853270848, -0.9070163062135666587 ) ) ;
#176907=CARTESIAN_POINT ( 'NONE',  ( 2.307699607974790901, -0.4742087202370263155, 2.108885336910087283 ) ) ;
#176910=CARTESIAN_POINT ( 'NONE',  ( 1.641335390984842491, -1.319735721761399638, -1.261605215524951085 ) ) ;
#176912=CARTESIAN_POINT ( 'NONE',  ( 4.506759567000420574, 1.410888988908312047, -1.158519065656477220 ) ) ;
#176914=CARTESIAN_POINT ( 'NONE',  ( 3.076317393561965208, 0.8638369986560844316, 1.706277067364105893 ) ) ;
#176916=CARTESIAN_POINT ( 'NONE',  ( 3.578522297727056767, 1.251517597477384447, -1.520772613757546354 ) ) ;
#176918=CARTESIAN_POINT ( 'NONE',  ( 6.427294056597427918, -1.271908742016104821, -1.467670737461545860 ) ) ;
#176924=CARTESIAN_POINT ( 'NONE',  ( 3.650944405621194377, 0.2833616294029631111, 1.891055170903446658 ) ) ;
#176928=CARTESIAN_POINT ( 'NONE',  ( 5.127594652646677353, -0.2932247039480195827, 1.991498814599843792 ) ) ;
#176930=CARTESIAN_POINT ( 'NONE',  ( 5.971303284387838417, 0.1295235881030691594, -1.821162830480331563 ) ) ;
#176931=CARTESIAN_POINT ( 'NONE',  ( 0.6255436495894195481, 0.2045281481408110225, -2.060252820462626477 ) ) ;
#176936=FACE_OUTER_BOUND ( 'NONE', #47871, .T. ) ;
#176941=CARTESIAN_POINT ( 'NONE',  ( 0.1333692844072559280, 0.001398348041498076455, -2.053671342968105051 ) ) ;
#176946=CARTESIAN_POINT ( 'NONE',  ( 4.254371668973718990, 1.680547194560323643, -0.4271837243535313022 ) ) ;
#176948=CARTESIAN_POINT ( 'NONE',  ( 0.9189038144036645317, -1.502058968113138437, 1.424965263859011122 ) ) ;
#176949=( BOUNDED_SURFACE ( )  B_SPLINE_SURFACE ( 3, 3, ( 
 ( #118946, #85308, #67953, #170829, #2964, #133028, #53884, #202232, #34417, #199027, #150327, #168692, #185994, #83162, #1894, #5092, #149242, #52808, #50674, #18153, #134098, #69035, #201168, #817, #200106, #66886, #71167, #166564, #84240, #183870, #135152, #184925, #137284, #120018, #151394, #101561, #51758, #35484, #117879, #20296, #167629, #152450, #36549, #37628, #102635, #203303, #86382, #4028, #103708, #169759, #54950, #70098, #21347, #121103, #187070, #26707, #139417, #124310, #141580, #91747, #60276, #126433, #138346, #175121, #123250, #74408, #207588, #154591, #208644, #189214, #72238, #24564, #89604, #157800, #25635, #8324, #90670, #40854, #192396, #6170, #206519, #188139, #158853, #122173, #88530, #204363, #190269, #191327, #106960, #155655, #56019, #59207, #9396, #44051, #10451, #92810, #39771, #41926, #75468, #105876, #58151, #205452, #125364, #171900, #23498, #172985, #76524, #156733, #142635, #7237, #73314, #109106, #110171, #140508, #57085, #108037, #22420, #174063, #42993, #176182, #62411, #162062, #13651, #15771, #212913, #178317, #194539, #93880, #128575, #27781, #47259, #46186, #30999, #193482, #64547, #209708, #164185, #45126, #127512, #196681, #146893, #180430, #79724, #210788, #177239, #28853, #32047, #78652, #63483, #80803, #97074, #213954, #65575, #77593, #114431, #112302, #145840, #130690, #159918, #147939, #29926, #11523, #96009, #94940, #163127, #179379, #211845, #129637, #195624, #131722, #143716, #113372, #111236, #98135, #61352, #160988, #12580, #14710, #48319, #81856, #144780, #197727, #49366, #184665, #153246, #37361, #119749, #132771, #68775, #168433, #99185, #85047, #17890, #36284, #181478, #66625, #199851, #103436, #117617, #21079, #50424, #116543, #201960, #137012, #169497, #87181, #182534, #1635, #166300, #20030, #560, #4821, #198775, #185728, #70901, #86118, #3758, #34162, #152189, #151135, #51493, #100233, #203039, #35217, #165235, #69834, #135943, #83976, #16829, #150064, #200900, #53616, #115485, #67694, #33108, #82912, #2701, #148985, #133841, #183610, #101293, #167374, #18962, #134894, #52549, #118679, #102362, #194014, #29403, #121902, #155384, #105596, #110711, #154324, #111781, #71970, #128058, #13129, #176711, #160459, #138080, #28324, #90398, #205176, #39498, #79207, #188946, #104514, #94420, #12067, #5898, #170557, #187869, #143193, #78136, #145324, #171629, #61897, #54679, #24292, #22141, #204093, #23224, #40586, #172716, #186805, #89336, #120829, #45664, #55746, #38434, #6968, #106691, #156468, #177787, #144266, #56818, #73049, #88255, #139148, #122988, #209184, #8055, #126985, #77063, #210259, #60824, #95495, #192944, #44596, #161542, #182015, #1125, #197212, #31538, #212386, #64028, #67187, #113920, #98665, #116029, #66115, #34707, #100776, #112845, #149539, #97614, #48852, #33646, #129119, #183095, #163671, #46733, #213445, #130174, #132258, #52, #114966, #65068, #15254, #166858, #195096, #180966, #162604, #133324, #96557, #62950, #178861, #164720, #165792, #81341, #196166, #30472, #99720, #198265, #18454, #199327, #50973, #14180, #16309, #49908, #80273, #32588, #179916, #17375, #146371, #47807, #147420, #117095, #131224, #82394, #148483, #83459, #84531, #211325, #36836, #5378, #167920, #38989, #184153, #138633, #19517, #101851, #171113, #121386, #154875, #136500 ),
 ( #88818, #102919, #202521, #55239, #68257, #122467, #168980, #200393, #152731, #3252, #71457, #153807, #54170, #4313, #20580, #188426, #134390, #120309, #85594, #72535, #35776, #2181, #118167, #103995, #105074, #86664, #69320, #52041, #187359, #137570, #40061, #204656, #6458, #151682, #170039, #203587, #135430, #186284, #53095, #22705, #201452, #119229, #70384, #56305, #37921, #106171, #185212, #21625, #172197, #23786, #150620, #87733, #157019, #190549, #140789, #142923, #189497, #143998, #107251, #160198, #45400, #208923, #192677, #173272, #60558, #125649, #25920, #74688, #111516, #9673, #139711, #126717, #44331, #41141, #205735, #8605, #175398, #110453, #177522, #206803, #94159, #89892, #59492, #57369, #24852, #58436, #75750, #207868, #7529, #124589, #155943, #77876, #90954, #73612, #42205, #141860, #191611, #209990, #176454, #127798, #28066, #26983, #43273, #108322, #109393, #11801, #61632, #93090, #159131, #174342, #123532, #92028, #158085, #10732, #76802, #193753, #180710, #12858, #113654, #198018, #48597, #33392, #179658, #178593, #81080, #96290, #14986, #13925, #99470, #80005, #46459, #162342, #165529, #161272, #146110, #50713, #212121, #49646, #115769, #63759, #78933, #129919, #30202, #164466, #17121, #31278, #195905, #47541, #97353, #181758, #163410, #147167, #83198, #64821, #145055, #213194, #148228, #130967, #194823, #196959, #114715, #82136, #32333, #98401, #16052, #214230, #149280, #65858, #132008, #861, #66927, #133069, #199067, #116839, #29134, #95222, #211058, #62683, #128842, #112581, #18193, #138385, #35520, #51798, #187105, #118981, #67995, #38739, #186033, #87494, #152486, #120058, #85348, #137321, #203337, #151429, #19266, #54990, #204403, #121142, #37669, #104821, #88569, #200144, #135191, #1935, #167665, #201207, #4068, #103745, #3002, #100529, #182840, #134137, #202270, #153559, #36586, #183909, #168731, #117916, #101597, #102673, #71205, #154627, #70138, #184960, #53921, #69071, #170867, #20333, #52846, #22457, #169796, #5130, #136250, #21385, #86419, #6207, #72276, #56056, #34457, #166604, #84278, #150365, #191364, #208680, #27817, #139454, #74441, #155691, #106994, #140543, #157835, #43031, #90709, #39809, #122213, #7274, #141613, #92845, #190301, #123287, #108070, #205486, #189250, #41958, #10485, #93914, #9432, #58185, #207623, #159955, #158889, #59240, #91778, #73351, #125399, #126468, #192431, #174098, #109143, #57120, #188175, #77629, #40889, #156771, #173019, #105915, #175156, #171940, #206557, #76559, #26742, #44086, #124343, #24600, #25671, #8357, #75502, #142669, #110205, #60309, #176215, #11559, #143751, #23531, #209746, #89639, #46223, #81892, #15806, #112340, #45159, #178352, #62447, #196715, #49401, #63523, #13688, #29960, #96046, #147978, #129675, #179415, #197763, #97110, #111273, #162099, #180467, #195660, #12617, #163162, #146929, #114467, #79758, #47294, #212946, #211882, #213988, #32083, #98171, #145874, #130724, #115520, #65608, #113409, #164219, #31036, #131758, #181515, #33144, #128610, #177276, #16869, #194577, #99224, #78690, #14747, #165274, #28892, #80839, #64583, #48356, #127547, #144815, #82949, #149023, #61388, #193518, #210822, #94976, #161022, #22183, #137051, #186844, #67730, #101331, #51533, #53654, #100272, #54721, #17929, #70941, #170597, #119786, #103474, #84013 ),
 ( #133881, #86156, #169536, #88299, #199888, #4862, #598, #184702, #116580, #150104, #117658, #200938, #118714, #132811, #183651, #66664, #203077, #166337, #198815, #167412, #52586, #36323, #120870, #37399, #2740, #19004, #50461, #85085, #182575, #152227, #151169, #69872, #1676, #21116, #34197, #38476, #35255, #68811, #87222, #185767, #104553, #102401, #134933, #168469, #20067, #3798, #135981, #201996, #153286, #9172, #192174, #43835, #55785, #92594, #40627, #206298, #58993, #72010, #126212, #106730, #204132, #156508, #7008, #75247, #157579, #140279, #8097, #172757, #109951, #138123, #124088, #105639, #76308, #39538, #5939, #121942, #107813, #108882, #24332, #73085, #187908, #125149, #141359, #175961, #142415, #171667, #90440, #23263, #25415, #74186, #207373, #89375, #42775, #155424, #208423, #139186, #205216, #174905, #191107, #158636, #57923, #188983, #56858, #123032, #10233, #190051, #41703, #26484, #60057, #27556, #154360, #173838, #91520, #144558, #29708, #179156, #11294, #114220, #210568, #143488, #45968, #28634, #129422, #63260, #95789, #112089, #128358, #180219, #77373, #161846, #127286, #130475, #193257, #159695, #209485, #79510, #162907, #62202, #94721, #61126, #30780, #195405, #31841, #64334, #212692, #44904, #145628, #113150, #111012, #13434, #12359, #47035, #177017, #160764, #194326, #196466, #178090, #48108, #78438, #211625, #80579, #97917, #163976, #93652, #96859, #14489, #146677, #22201, #119803, #66679, #149035, #182590, #168485, #185782, #2756, #150119, #134947, #17943, #1692, #68825, #37416, #54737, #36339, #85099, #20084, #186861, #103492, #86172, #118731, #34213, #152242, #153303, #4878, #200953, #3814, #166352, #611, #104569, #100286, #117673, #84030, #132826, #69886, #198830, #19019, #169553, #135999, #70957, #151184, #67746, #52602, #133896, #21134, #87238, #137067, #184715, #183666, #199903, #51549, #203092, #35270, #102417, #53671, #202012, #38491, #170614, #50475, #120887, #101348, #116596, #167427, #5955, #60072, #189000, #138138, #90457, #155440, #157595, #91536, #74202, #156523, #106746, #126228, #72026, #57939, #39554, #10248, #187924, #154378, #55802, #41719, #42788, #40643, #7025, #204147, #59007, #9190, #192189, #76324, #92607, #105655, #107829, #141375, #121957, #124104, #205232, #75261, #171683, #23280, #172773, #142429, #8114, #208438, #89392, #73101, #174920, #109967, #43853, #175978, #139202, #190067, #56873, #26500, #24347, #88314, #123049, #158650, #140296, #207386, #191122, #206315, #125163, #173854, #25430, #108897, #197528, #161861, #77388, #212708, #146692, #193274, #143504, #94736, #113167, #130495, #115290, #160782, #31857, #27571, #211640, #209501, #177032, #12375, #13451, #145645, #159711, #144573, #49172, #15566, #44919, #93669, #128374, #79527, #63276, #81653, #64349, #29723, #45983, #11310, #194341, #61141, #179171, #112104, #96874, #111027, #196482, #127303, #147740, #28649, #78455, #48124, #95805, #210587, #129438, #30795, #80596, #62217, #195421, #162924, #178107, #180234, #114236, #97933, #47051, #14504, #163991, #213756, #65379, #131525, #1438, #201775, #135751, #119552, #33965, #16631, #136816, #100042, #50227, #185538, #117420, #66434, #37166, #184471, #85924, #150941, #118487, #83777, #53415, #103244, #149870, #17691, #169304, #202843, #20888, #36088, #86985, #153055 ),
 ( #151997, #69643, #198580, #3569, #2504, #183417, #166105, #54492, #101091, #82715, #4631, #70703, #132577, #148792, #67503, #52359, #181281, #32907, #133649, #98985, #165038, #68576, #362, #116346, #199648, #167178, #84851, #182337, #51295, #35020, #18767, #134703, #200708, #102172, #168239, #19838, #177577, #160251, #122791, #138960, #38240, #6778, #186614, #208976, #72853, #192729, #137892, #11852, #154129, #111569, #203911, #71776, #144050, #94211, #127854, #106493, #155197, #121713, #187675, #193804, #23028, #10781, #28117, #44383, #161328, #12912, #55558, #76856, #89143, #104313, #60612, #170362, #204981, #77930, #142975, #45453, #56626, #39305, #172519, #105400, #24104, #171438, #29190, #188750, #40389, #93143, #95280, #21947, #159180, #145108, #126771, #210046, #61685, #110505, #88057, #176505, #78992, #211114, #120636, #5699, #15042, #47595, #31330, #149335, #131021, #80062, #146163, #212178, #16105, #179713, #181814, #64875, #13975, #164520, #148282, #115827, #113709, #197013, #214281, #213245, #915, #33446, #99523, #147220, #132061, #199119, #83251, #48649, #165582, #97407, #66982, #17176, #133120, #129973, #112638, #18245, #195960, #63813, #50762, #114766, #162399, #116892, #65914, #182891, #32390, #198071, #163462, #34508, #100581, #81134, #180763, #166655, #84329, #150415, #49699, #62738, #128898, #98455, #82189, #96344, #194879, #46515, #178647, #30258, #187157, #134183, #1982, #35569, #21432, #38786, #70186, #3051, #202321, #85395, #69120, #136298, #104867, #122263, #103795, #152532, #87540, #39861, #170912, #153609, #186086, #101649, #5180, #6257, #72328, #53970, #71256, #19319, #68046, #171992, #167716, #185011, #151481, #4117, #22507, #36638, #88617, #154672, #138434, #135241, #51845, #23584, #201255, #52895, #204452, #120107, #119029, #56106, #137369, #121188, #37717, #203386, #102722, #188221, #105970, #168779, #20384, #89691, #200192, #117964, #55039, #183958, #86468, #169845, #108122, #189297, #140596, #25722, #57171, #28940, #126522, #73404, #155742, #40937, #175208, #192483, #9482, #156818, #141665, #24650, #8405, #75554, #44135, #61432, #43083, #91831, #26790, #193565, #110256, #92895, #125454, #107042, #158940, #160004, #11605, #207676, #10536, #173069, #7327, #111322, #90757, #124393, #74490, #139507, #76609, #205534, #157890, #176265, #142723, #77679, #59295, #206607, #191416, #58236, #109196, #190351, #143800, #42013, #174149, #208732, #209797, #123333, #60359, #177326, #27866, #93963, #127599, #45208, #78739, #211933, #96094, #15857, #82998, #97159, #47343, #79809, #63567, #181565, #163214, #112386, #178398, #30010, #48409, #129724, #214037, #14796, #46269, #196766, #180516, #148027, #145921, #80887, #32136, #31086, #33193, #65662, #131810, #179462, #164268, #16918, #115569, #99276, #195708, #113457, #165325, #50512, #49450, #81944, #149074, #651, #162149, #146977, #128660, #212995, #64632, #210870, #182629, #197819, #12665, #95024, #194626, #114521, #66717, #130771, #13736, #98217, #132861, #198865, #116634, #161074, #144863, #62495, #184752, #119843, #72064, #4915, #185821, #3852, #133935, #53710, #38528, #104605, #168524, #37452, #51588, #34252, #204184, #199940, #2793, #117713, #100324, #103531, #17982, #118768, #203134, #169590, #170652, #36380, #183703, #86208, #101388, #20122, #19059 ),
 ( #85137, #84071, #151224, #35311, #21172, #22240, #102458, #200994, #68864, #134983, #120923, #152279, #167463, #52639, #69926, #202050, #136037, #153344, #87275, #70992, #137105, #54776, #186896, #88350, #154414, #5993, #138174, #55840, #121996, #166391, #150160, #1728, #67785, #208470, #124137, #76355, #8151, #60106, #142462, #126265, #40677, #23319, #143540, #106780, #56909, #192222, #190099, #73134, #43885, #191157, #92640, #157625, #125194, #90493, #109999, #176011, #172808, #89427, #209534, #24380, #123082, #27603, #41752, #139238, #93704, #42824, #158682, #9222, #108930, #156556, #159744, #11342, #74235, #140328, #77423, #61176, #187961, #174951, #39589, #105693, #205269, #206346, #7061, #57974, #107864, #155478, #171720, #10281, #189040, #173890, #25465, #207417, #91573, #75294, #141410, #59036, #26533, #194373, #47082, #15600, #32944, #14536, #63309, #212744, #165075, #97967, #64378, #96906, #12408, #146725, #131560, #197561, #113200, #130523, #144605, #127336, #82750, #78488, #95839, #210620, #193306, #196514, #111059, #211673, #81688, #48157, #49205, #129471, #62246, #179206, #46017, #30830, #112136, #115325, #178140, #128406, #29754, #181315, #44951, #161895, #148823, #13482, #147772, #213788, #79557, #177066, #145676, #195453, #114269, #99017, #162958, #80633, #180266, #31890, #65411, #164025, #16666, #396, #28682, #94768, #160816, #185571, #68610, #17721, #168271, #152031, #119588, #51326, #134734, #3601, #2535, #4665, #37201, #103275, #150970, #135783, #202875, #87017, #200742, #169337, #101123, #153090, #20922, #52391, #118519, #120668, #70738, #184503, #84883, #198615, #167211, #132608, #69679, #18799, #201807, #83809, #136851, #100072, #54523, #149902, #1469, #186646, #38272, #104349, #36122, #102206, #67536, #133678, #170393, #183448, #19872, #21982, #53449, #85956, #88091, #154165, #66467, #50261, #116380, #182368, #33998, #166134, #199683, #117454, #35052, #72888, #75041, #8968, #206092, #7887, #24136, #43633, #137920, #189850, #171471, #142208, #105436, #71809, #187710, #173639, #174701, #172551, #138995, #203940, #190906, #141158, #109748, #208222, #10030, #23061, #25212, #58789, #55588, #41495, #122825, #207165, #121743, #89177, #90238, #59854, #73974, #126006, #155229, #6810, #92392, #27350, #191967, #175758, #205016, #107608, #56662, #158428, #156304, #93453, #188787, #76104, #5730, #124944, #108673, #40422, #42570, #91316, #140069, #106525, #39338, #57727, #123884, #26276, #157373, #110806, #209278, #12166, #30576, #47912, #32688, #78238, #163774, #159490, #129226, #60925, #94520, #144360, #145427, #63058, #77166, #62001, #115074, #147523, #176812, #11089, #45768, #197315, #143287, #195199, #28427, #81446, #44699, #127082, #193045, #112950, #114022, #111885, #210361, #160558, #130277, #14282, #48956, #213544, #15352, #128157, #178961, #212492, #194117, #46836, #177889, #80377, #29502, #95595, #161643, #65167, #13238, #131322, #79311, #211428, #31639, #181070, #96657, #162710, #146472, #64133, #196265, #97716, #180018, #152841, #116131, #169080, #54276, #3357, #201557, #182119, #69428, #134493, #34804, #83561, #120413, #18556, #148582, #135533, #53203, #50007, #151, #165892, #184252, #119334, #186388, #17477, #103025, #98768, #68360, #66217, #33749, #149643, #84633, #2284, #16415, #1225, #164825 ),
 ( #199433, #82495, #35879, #51075, #168021, #99826, #185321, #132365, #86769, #67287, #133426, #36944, #20679, #4415, #150724, #117201, #183198, #100879, #70486, #166966, #200497, #136602, #19625, #52140, #202626, #198367, #118268, #101954, #85696, #151784, #170145, #9777, #138737, #87841, #40160, #105177, #107349, #41242, #23883, #106274, #56406, #38025, #71563, #57474, #8707, #172295, #39090, #89989, #121490, #171213, #156040, #140893, #158184, #139812, #188530, #123633, #75849, #74791, #189596, #7629, #137670, #173371, #42307, #108422, #73714, #24955, #55338, #104096, #207968, #203691, #6560, #187462, #21732, #91057, #153912, #122567, #206903, #157118, #174444, #205840, #22807, #58534, #88922, #124689, #154975, #26020, #72640, #204755, #190647, #92130, #5482, #141956, #59594, #125751, #212229, #146211, #176556, #175500, #94262, #192779, #112685, #179759, #193854, #144101, #28166, #160301, #63862, #45504, #209022, #60658, #126822, #145157, #11904, #96394, #111620, #143027, #79042, #62787, #30309, #77978, #177632, #128950, #127903, #130018, #162445, #14020, #61735, #46565, #113755, #196009, #29240, #80107, #210096, #47644, #31376, #97452, #44437, #27089, #147260, #110554, #95332, #163507, #161381, #76903, #15091, #194928, #81181, #12965, #178695, #211163, #213292, #64918, #191713, #43371, #109493, #93197, #159228, #10829, #6032, #39624, #148324, #83293, #164563, #115870, #3889, #32433, #7099, #104641, #48693, #69959, #88384, #153379, #138212, #136071, #65955, #185856, #198113, #119878, #181855, #204224, #33492, #214323, #49743, #55876, #114808, #99565, #155518, #165629, #154454, #72101, #17217, #180807, #149378, #132104, #54814, #122033, #202086, #53744, #37488, #103566, #187999, #169625, #21208, #87310, #4950, #71028, #137142, #38566, #203169, #82233, #120963, #186934, #170688, #22275, #105729, #171759, #23355, #89464, #131067, #197055, #98499, #16148, #209566, #93738, #9259, #176045, #107903, #159777, #27638, #11377, #140363, #123118, #28715, #206382, #156592, #77456, #75329, #172846, #143574, #76389, #192255, #42857, #10315, #190136, #61212, #127369, #41790, #124172, #193340, #94802, #44985, #142498, #111094, #177100, #90530, #25502, #106816, #58008, #157661, #189078, #160850, #43918, #205309, #73171, #24417, #92673, #110033, #141446, #74271, #59072, #8186, #173929, #207453, #139277, #56946, #174984, #125232, #158717, #40711, #91610, #208504, #108964, #191190, #60139, #26568, #126296, #146759, #15638, #29789, #12442, #182406, #112170, #195485, #95874, #78521, #164059, #210653, #14573, #132642, #161929, #13519, #99053, #34035, #148858, #198648, #79592, #48191, #145711, #165108, #179240, #66503, #211709, #82786, #100108, #131595, #115359, #63345, #197597, #114303, #162992, #129504, #144638, #212777, #62281, #49240, #181351, #178174, #128441, #47119, #98002, #32977, #194407, #113236, #16700, #46049, #196548, #30864, #96942, #80668, #64412, #130558, #180301, #31923, #81725, #432, #147808, #213827, #65444, #50297, #116415, #5766, #202913, #168308, #184535, #83846, #52428, #17757, #37239, #118554, #20956, #183480, #54558, #199720, #154199, #35089, #117489, #186679, #136886, #170431, #152065, #200776, #167245, #18833, #22018, #68645, #53485, #70773, #87054, #119623, #120704, #71847, #201841, #36158, #3635, #38307, #149935, #137955 ),
 ( #88128, #104384, #102237, #203975, #19906, #55622, #121779, #187746, #84917, #1504, #39374, #151005, #101159, #166169, #85991, #51366, #67570, #169372, #133714, #135817, #103310, #134768, #2575, #69714, #185607, #153126, #4697, #122863, #172589, #27383, #23097, #7925, #127116, #90271, #126038, #59889, #156340, #89212, #74011, #106562, #26311, #93484, #107642, #57760, #140103, #206130, #192001, #173674, #188824, #40458, #24168, #58825, #123921, #10064, #25249, #56696, #207200, #190939, #158464, #189889, #91349, #42603, #41530, #43666, #76140, #142243, #157411, #174738, #159523, #109783, #9002, #208255, #75077, #175792, #11122, #77199, #141190, #155265, #60959, #124978, #108710, #143318, #92424, #205054, #209312, #193083, #105471, #171504, #6846, #72924, #139030, #65199, #13271, #95627, #131351, #183, #213577, #114057, #197347, #164856, #62037, #211457, #78268, #29535, #129261, #160591, #132399, #15384, #176846, #44733, #144394, #64166, #81478, #112982, #45800, #30608, #128191, #111921, #178993, #147555, #16447, #146508, #195231, #130309, #82528, #48989, #196296, #14317, #210395, #47943, #115107, #181105, #96696, #180050, #194152, #110840, #66251, #177921, #79344, #161677, #28459, #31672, #94553, #46869, #32720, #97749, #98802, #162744, #145462, #80410, #63092, #212525, #163808, #148614, #12198, #70518, #52174, #1259, #67317, #133461, #151818, #100910, #103060, #200528, #149678, #85733, #69461, #36977, #183230, #118300, #135566, #134524, #136633, #169114, #20710, #68395, #53237, #120447, #4448, #184286, #86804, #18590, #202660, #152870, #54309, #51107, #33782, #153944, #117232, #199465, #186421, #35912, #83596, #38059, #201590, #104130, #168056, #119367, #166999, #170176, #21764, #84668, #34836, #87872, #5512, #71593, #185355, #198401, #50043, #150757, #2319, #17508, #101987, #19658, #99861, #116166, #182152, #165923, #3391, #171244, #157154, #108459, #205874, #138770, #123667, #6593, #204788, #57508, #26055, #43405, #24991, #73750, #8746, #175534, #174479, #74827, #107387, #22840, #140927, #141991, #208005, #189630, #206941, #155008, #137702, #93230, #88954, #106306, #72673, #203722, #58570, #121524, #7665, #92168, #124724, #59630, #139845, #56441, #41278, #122600, #173410, #188563, #125788, #40194, #172328, #23917, #191750, #55370, #90022, #159262, #156079, #158220, #9809, #91094, #187494, #190685, #42344, #75884, #109528, #27124, #10863, #39124, #105207, #144137, #212262, #81215, #63896, #112719, #130051, #31411, #176591, #193892, #192815, #210130, #111654, #126857, #147295, #14054, #209057, #76936, #110589, #194965, #80143, #161416, #11941, #13000, #94297, #78013, #79076, #146246, #97485, #62826, #29274, #46601, #163542, #196044, #178731, #211200, #28203, #30346, #47678, #113789, #145194, #96431, #160337, #143062, #60693, #61772, #95366, #127940, #45540, #179791, #177666, #128986, #15127, #162482, #44473, #206570, #205498, #108082, #123298, #41971, #40900, #60320, #107005, #73364, #189261, #192444, #188186, #173030, #77641, #24612, #76571, #10498, #90721, #39821, #156783, #57131, #191376, #44099, #58197, #8369, #74452, #140556, #142683, #124355, #139469, #190313, #174111, #9442, #25683, #175167, #91792, #7286, #157848, #141624, #109155, #75513, #207634, #59252, #125410, #208693, #26754, #92855, #43042, #158901, #110219 ) ),
 .UNSPECIFIED., .T., .F., .T. ) 
 B_SPLINE_SURFACE_WITH_KNOTS ( ( 4, 3, 4 ),
 ( 4, 1, 1, 1, 1, 1, 1, 1, 1, 1, 1, 1, 1, 1, 1, 1, 1, 1, 1, 1, 1, 1, 1, 1, 1, 1, 1, 1, 1, 1, 1, 1, 1, 1, 1, 1, 1, 1, 1, 1, 1, 1, 1, 1, 1, 1, 1, 1, 1, 1, 1, 1, 1, 1, 1, 1, 1, 1, 1, 1, 1, 1, 1, 1, 1, 1, 1, 1, 1, 1, 1, 1, 1, 1, 1, 1, 1, 1, 1, 1, 1, 1, 1, 1, 1, 1, 1, 1, 1, 1, 1, 1, 1, 1, 1, 1, 1, 1, 1, 1, 1, 1, 1, 1, 1, 1, 1, 1, 1, 1, 1, 1, 1, 1, 1, 1, 1, 1, 1, 1, 1, 1, 1, 1, 1, 1, 1, 1, 1, 1, 1, 1, 1, 1, 1, 1, 1, 1, 1, 1, 1, 1, 1, 1, 1, 1, 1, 1, 1, 1, 1, 1, 1, 1, 1, 1, 1, 1, 1, 1, 1, 1, 1, 1, 1, 1, 1, 1, 1, 1, 1, 1, 1, 1, 1, 1, 1, 1, 1, 1, 1, 1, 1, 1, 1, 1, 1, 1, 1, 1, 1, 1, 1, 1, 1, 1, 1, 1, 1, 1, 1, 1, 1, 1, 1, 1, 1, 1, 1, 1, 1, 1, 1, 1, 1, 1, 1, 1, 1, 1, 1, 1, 1, 1, 1, 1, 1, 1, 1, 1, 1, 1, 1, 1, 1, 1, 1, 1, 1, 1, 1, 1, 1, 1, 1, 1, 1, 1, 1, 1, 1, 1, 1, 1, 1, 1, 1, 1, 1, 1, 1, 1, 1, 1, 1, 1, 1, 1, 1, 1, 1, 1, 1, 1, 1, 1, 1, 1, 1, 1, 1, 1, 1, 1, 1, 1, 1, 1, 1, 1, 1, 1, 1, 1, 1, 1, 1, 1, 1, 1, 1, 1, 1, 1, 1, 1, 1, 1, 1, 1, 1, 1, 1, 1, 1, 1, 1, 1, 1, 1, 1, 1, 1, 1, 1, 1, 1, 1, 1, 1, 1, 1, 1, 1, 1, 1, 1, 1, 1, 1, 1, 1, 1, 1, 1, 1, 1, 1, 1, 1, 1, 1, 1, 1, 1, 1, 1, 1, 1, 1, 1, 1, 1, 1, 1, 1, 1, 1, 1, 1, 1, 1, 1, 1, 1, 1, 1, 1, 1, 1, 1, 1, 1, 1, 4 ),
 ( 0.000000000000000000, 0.5000000000000000000, 1.000000000000000000 ),
 ( 0.000000000000000000, 0.002599878613971510263, 0.005208762566300055921, 0.007813076245110234588, 0.01041697056762492211, 0.01302017924898362516, 0.01562522799165661294, 0.01822895742955179393, 0.02083332403451576206, 0.02343772221867868391, 0.02604143078293654281, 0.02864626161639613477, 0.03124961764961396021, 0.03385452714844047750, 0.03645799780571232912, 0.03906266225314121432, 0.04166671052383312535, 0.04427076094224517699, 0.04687542278318937439, 0.04947889361195772356, 0.05208380280015859759, 0.05468715921365963767, 0.05729198803509916865, 0.05989568673917144287, 0.06250009379223495087, 0.06510449848632135494, 0.06770819839843210397, 0.07031302545632363288, 0.07291638160390327694, 0.07552129054917994244, 0.07812475961953217751, 0.08072942239586503033, 0.08333346963797970408, 0.08593751866472883194, 0.08854217935802578821, 0.09114564884740632145, 0.09375055680876714925, 0.09635391199924973893, 0.09895873945611717570, 0.1015624370353711836, 0.1041668426700886191, 0.1067712463110160465, 0.1093749448896196713, 0.1119797708301935452, 0.1145831257515418783, 0.1171880334468678037, 0.1197915013940491491, 0.1223961628153678316, 0.1250002090321265524, 0.1276042567216372492, 0.1302089163955687523, 0.1328123846563000476, 0.1354172914881497103, 0.1380206455552074885, 0.1406254717515977581, 0.1432291683081768907, 0.1458335726268597532, 0.1484379753169847160, 0.1510416726638619811, 0.1536464975900906083, 0.1562498513865758776, 0.1588547579349887939, 0.1614582248604825021, 0.1640628850295551278, 0.1666669303230295940, 0.1692709767774011609, 0.1718756355346959253, 0.1744791026682601387, 0.1770840084736199360, 0.1796873615186004858, 0.1822921865574477218, 0.1848958821930496710, 0.1875002852981585977, 0.1901046871399069693, 0.1927083833567690418, 0.1953132073715553307, 0.1979165601445126987, 0.2005214656490191816, 0.2031249316542690642, 0.2057295906738217384, 0.2083336351460475244, 0.2109376804673406547, 0.2135423384106908962, 0.2161458045185324639, 0.2187507094003866837, 0.2213540615246011867, 0.2239588855088016361, 0.2265625803250888304, 0.2291669823190463362, 0.2317713834148095453, 0.2343750786033309830, 0.2369799018095430365, 0.2395832536602726381, 0.2421881582238437913, 0.2447916234102597566, 0.2473962813829825302, 0.2500003251359625422, 0.2526043694262022354, 0.2552090266582678346, 0.2578124918417971090, 0.2604173959030967600, 0.2630207472078238129, 0.2656255702402394725, 0.2682292643388430320, 0.2708336653240377978, 0.2734380657761767419, 0.2760417600379992398, 0.2786465825384744077, 0.2812499335682448476, 0.2838548372938197173, 0.2864583017627815864, 0.2890629587913320364, 0.2916670019270400371, 0.2942710452882197347, 0.2968757019116316509, 0.2994791662722288139, 0.3020840696158954564, 0.3046874202023847622, 0.3072922423858477359, 0.3098959358683710530, 0.3125003359471613118, 0.3151047358580104651, 0.3177084292947467969, 0.3203132511922952008, 0.3229166015023476888, 0.3255215044928377321, 0.3281249683456989308, 0.3307296245327063788, 0.3333336671530912065, 0.3359377096871765112, 0.3385423658045411677, 0.3411458294435600336, 0.3437507321724898035, 0.3463540821419661686, 0.3489589035792820537, 0.3515625965473047621, 0.3541669958220223235, 0.3567713952938928457, 0.3593750880071304721, 0.3619799094045394461, 0.3645832590960911834, 0.3671881614543835437, 0.3697916247924753486, 0.3723962802405443862, 0.3750003224475334518, 0.3776043642564660408, 0.3802090199703688222, 0.3828124829891406122, 0.3854173852062082184, 0.3880207346598750218, 0.3906255554538268782, 0.3932292480089087938, 0.3958336465818629857, 0.3984380457170473289, 0.4010417378083525053, 0.4036465588083897882, 0.4062499079826380477, 0.4088548098116001062, 0.4114582727362346981, 0.4140629275479489335, 0.4166669694434522730, 0.4192710106291533956, 0.4218756660421624782, 0.4244791285419997062, 0.4270840303500617607, 0.4296873793891050619, 0.4322921996424575197, 0.4348958918861421385, 0.4375002898596233591, 0.4401046887603987101, 0.4427083803313200949, 0.4453132010367379379, 0.4479165497948640051, 0.4505214511973463787, 0.4531249138098211726, 0.4557295680877478938, 0.4583336097736617210, 0.4609376504380365280, 0.4635423056527069874, 0.4661457677349071238, 0.4687506692368063055, 0.4713540179623986193, 0.4739588377779012651, 0.4765625298117197040, 0.4791669272880037522, 0.4817713260566358624, 0.4843750172087082362, 0.4869798377222476216, 0.4895831861654201811, 0.4921880872442612742, 0.4947915496458628049, 0.4973962034925555886, 0.5000002450707665691, 0.5026042853157074441, 0.5052089404345847523, 0.5078124022004342208, 0.5104173034990032720, 0.5130206520123070657, 0.5156254714926987726, 0.5182291634181735995, 0.5208335604995248946, 0.5234379592382720769, 0.5260416500730202838, 0.5286464704974140894, 0.5312498187267931105, 0.5338547195848227789, 0.5364581818768299204, 0.5390628353948335727, 0.5416668769672219330, 0.5442709168946127107, 0.5468755720202369552, 0.5494790335710144635, 0.5520839347690799093, 0.5546872831712518215, 0.5572921024192640793, 0.5598957943379132551, 0.5625001911265891108, 0.5651045899377058479, 0.5677082805566486812, 0.5703131009946261765, 0.5729164491113668545, 0.5755213498514099024, 0.5781248121350983649, 0.5807294654269519185, 0.5833335070953961088, 0.5859375468071157389, 0.5885422020420250089, 0.5911456634790059894, 0.5937505646793920233, 0.5963539130715860281, 0.5989587321899475514, 0.6015624242032879820, 0.6041668208015419372, 0.6067712197872831004, 0.6093749102919370220, 0.6119797308462270324, 0.6145830789514836745, 0.6171879796763642956, 0.6197914420530098445, 0.6223960952212510556, 0.6250001370876311357, 0.6276041766855571247, 0.6302088321322918407, 0.6328122935567517260, 0.6354171948622837629, 0.6380205433456558328, 0.6406253624370956690, 0.6432290546466469250, 0.6458334511567334069, 0.6484378504193577530, 0.6510415409112403351, 0.6536463616845760161, 0.6562497098795055939, 0.6588546106920506462, 0.6614580732629331550, 0.6640627264101022220, 0.6666667685763031370, 0.6692708081623160998, 0.6718754639234225667, 0.6744789254366408970, 0.6770838269501499029, 0.6796871756258610064, 0.6822919947931124218, 0.6848956873004010681, 0.6875000838245786117, 0.6901044834663523364, 0.6927081740469867022, 0.6953129951421085364, 0.6979163435278744609, 0.7005212445309179081, 0.7031247073973251327, 0.7057293606259679164, 0.7083334031938842701, 0.7109374428698714832, 0.7135420990479055536, 0.7161455607511696408, 0.7187504625754957965, 0.7213538115447158949, 0.7239586308905210377, 0.7265623237970838533, 0.7291667204376187650, 0.7317711205608201652, 0.7343748113317387638, 0.7369796328513985584, 0.7395829815291747877, 0.7421878828255610294, 0.7447913460887924941, 0.7473959995014650692, 0.7500000425730045661, 0.7526040824408628538, 0.7552087391383944803, 0.7578122011330034047, 0.7604171033709996586, 0.7630204527349119248, 0.7656252723620247114, 0.7682289657694127971, 0.7708333626285834850, 0.7734377633355060677, 0.7760414543982535607, 0.7786462764452187768, 0.7812496255161931469, 0.7838545272087811266, 0.7864579909701516769, 0.7890626446694239959, 0.7916666883465109938, 0.7942707285081521684, 0.7968753858277685120, 0.7994788482150362308, 0.8020837509695725176, 0.8046871008293766669, 0.8072919208405671121, 0.8098956148503495545, 0.8125000120304503026, 0.8151044134234068927, 0.8177081048795449281, 0.8203129275566022338, 0.8229162771219805661, 0.8255211793136476572, 0.8281246436744912343, 0.8307292977629509023, 0.8333333421475307423, 0.8359373827048843797, 0.8385420407491936956, 0.8411455036304537058, 0.8437504070044209437, 0.8463537574613370085, 0.8489585779593948889, 0.8515622726731627568, 0.8541666702765071673, 0.8567710724578335713, 0.8593747644089445581, 0.8619795878189033811, 0.8645829379799131464, 0.8671878407735589267, 0.8697913058352330085, 0.8723959604154888359, 0.8750000056095312839, 0.8776040466645483873, 0.8802087055361843548, 0.8828121690127931354, 0.8854170731091063340, 0.8880204242643787715, 0.8906252453521178447, 0.8932289408714879642, 0.8958333390004131758, 0.8984377420724726226, 0.9010414346201626179, 0.9036462588658594752, 0.9062496097237539017, 0.9088545132223035949, 0.9114579790861923048, 0.9140626342608790811, 0.9166666803663815477, 0.9192707220210388774, 0.9218753818226663732, 0.9244788459960084914, 0.9270837509176034219, 0.9296871028724987829, 0.9322919246527909820, 0.9348956210794385768, 0.9375000198362011261, 0.9401044239011964176, 0.9427081171475072408, 0.9453129423329229564, 0.9479162939871883520, 0.9505211982878988275, 0.9531246650646376661, 0.9557293209618126228, 0.9583333680330715643, 0.9609374102905526849, 0.9635420713365114853, 0.9661455366701111602, 0.9687504417289087844, 0.9713537931426093897, 0.9739586182492501187, 0.9765623229037746489, 0.9791667147516245340, 0.9817710778420317697, 0.9843748014325267581, 0.9869798465897002826, 0.9895830499482988207, 0.9921869381715581193, 0.9947912477285243416, 0.9974001254724073062, 1.000000000000000000 ),
 .UNSPECIFIED. ) 
 GEOMETRIC_REPRESENTATION_ITEM ( )  RATIONAL_B_SPLINE_SURFACE ( (
 ( 1.000000000000000222, 1.000000000000000222, 1.000000000000000222, 1.000000000000000222, 1.000000000000000444, 1.000000000000000000, 1.000000000000000666, 0.9999999999999997780, 1.000000000000000444, 1.000000000000000000, 1.000000000000000444, 1.000000000000000444, 1.000000000000000000, 1.000000000000000444, 1.000000000000000000, 1.000000000000000444, 1.000000000000000222, 1.000000000000000222, 1.000000000000000222, 1.000000000000000444, 1.000000000000000444, 1.000000000000000000, 1.000000000000000444, 1.000000000000000000, 1.000000000000000222, 1.000000000000000222, 1.000000000000000444, 1.000000000000000222, 1.000000000000000222, 1.000000000000000444, 1.000000000000000444, 1.000000000000000444, 1.000000000000000000, 1.000000000000000444, 1.000000000000000444, 1.000000000000000000, 1.000000000000000444, 1.000000000000000444, 1.000000000000000000, 1.000000000000000444, 1.000000000000000444, 1.000000000000000000, 1.000000000000000222, 1.000000000000000444, 1.000000000000000222, 1.000000000000000222, 1.000000000000000000, 1.000000000000000444, 1.000000000000000222, 1.000000000000000222, 1.000000000000000222, 1.000000000000000222, 1.000000000000000222, 1.000000000000000222, 1.000000000000000444, 1.000000000000000000, 1.000000000000000444, 0.9999999999999997780, 1.000000000000000666, 1.000000000000000444, 1.000000000000000444, 1.000000000000000000, 1.000000000000000444, 1.000000000000000222, 1.000000000000000222, 1.000000000000000444, 1.000000000000000222, 1.000000000000000444, 1.000000000000000000, 1.000000000000000444, 1.000000000000000222, 1.000000000000000444, 1.000000000000000444, 1.000000000000000222, 1.000000000000000222, 1.000000000000000222, 1.000000000000000444, 0.9999999999999997780, 1.000000000000000444, 1.000000000000000000, 1.000000000000000444, 1.000000000000000000, 1.000000000000000444, 0.9999999999999997780, 1.000000000000000444, 0.9999999999999997780, 1.000000000000000444, 1.000000000000000222, 1.000000000000000444, 1.000000000000000000, 1.000000000000000222, 1.000000000000000444, 1.000000000000000444, 1.000000000000000222, 1.000000000000000444, 1.000000000000000444, 1.000000000000000222, 1.000000000000000222, 1.000000000000000222, 1.000000000000000222, 1.000000000000000000, 1.000000000000000222, 1.000000000000000222, 1.000000000000000222, 1.000000000000000444, 1.000000000000000000, 1.000000000000000444, 0.9999999999999997780, 1.000000000000000666, 1.000000000000000222, 1.000000000000000444, 1.000000000000000000, 1.000000000000000444, 1.000000000000000222, 1.000000000000000222, 1.000000000000000444, 1.000000000000000000, 1.000000000000000000, 1.000000000000000444, 1.000000000000000000, 1.000000000000000444, 1.000000000000000000, 1.000000000000000444, 1.000000000000000222, 1.000000000000000444, 1.000000000000000222, 1.000000000000000444, 1.000000000000000222, 1.000000000000000444, 1.000000000000000000, 1.000000000000000444, 1.000000000000000222, 1.000000000000000444, 1.000000000000000000, 1.000000000000000444, 1.000000000000000000, 1.000000000000000444, 1.000000000000000000, 1.000000000000000444, 1.000000000000000222, 1.000000000000000444, 1.000000000000000222, 1.000000000000000444, 0.9999999999999997780, 1.000000000000000444, 1.000000000000000000, 1.000000000000000444, 1.000000000000000222, 1.000000000000000222, 1.000000000000000222, 1.000000000000000222, 1.000000000000000444, 0.9999999999999997780, 1.000000000000000444, 1.000000000000000000, 1.000000000000000000, 1.000000000000000222, 1.000000000000000222, 1.000000000000000666, 0.9999999999999997780, 1.000000000000000000, 1.000000000000000444, 1.000000000000000222, 1.000000000000000444, 1.000000000000000000, 1.000000000000000222, 1.000000000000000444, 1.000000000000000222, 1.000000000000000000, 1.000000000000000444, 1.000000000000000222, 1.000000000000000222, 1.000000000000000444, 1.000000000000000222, 1.000000000000000000, 1.000000000000000444, 1.000000000000000000, 1.000000000000000444, 1.000000000000000222, 1.000000000000000222, 1.000000000000000444, 0.9999999999999997780, 1.000000000000000444, 0.9999999999999997780, 1.000000000000000444, 1.000000000000000222, 1.000000000000000444, 1.000000000000000222, 1.000000000000000222, 1.000000000000000444, 1.000000000000000000, 1.000000000000000222, 1.000000000000000444, 1.000000000000000000, 1.000000000000000444, 1.000000000000000000, 1.000000000000000222, 1.000000000000000444, 1.000000000000000000, 1.000000000000000444, 0.9999999999999997780, 1.000000000000000444, 1.000000000000000222, 1.000000000000000444, 1.000000000000000000, 1.000000000000000000, 1.000000000000000444, 1.000000000000000000, 1.000000000000000222, 1.000000000000000444, 1.000000000000000222, 1.000000000000000444, 1.000000000000000222, 1.000000000000000444, 1.000000000000000444, 1.000000000000000444, 1.000000000000000000, 1.000000000000000444, 1.000000000000000222, 1.000000000000000444, 1.000000000000000222, 1.000000000000000000, 1.000000000000000222, 1.000000000000000444, 1.000000000000000222, 1.000000000000000444, 1.000000000000000000, 1.000000000000000222, 1.000000000000000000, 1.000000000000000444, 1.000000000000000000, 1.000000000000000444, 1.000000000000000444, 1.000000000000000444, 1.000000000000000444, 1.000000000000000000, 1.000000000000000222, 1.000000000000000444, 1.000000000000000000, 1.000000000000000444, 1.000000000000000444, 1.000000000000000444, 1.000000000000000222, 1.000000000000000222, 1.000000000000000222, 0.9999999999999997780, 1.000000000000000444, 1.000000000000000222, 1.000000000000000222, 1.000000000000000000, 1.000000000000000444, 1.000000000000000000, 1.000000000000000444, 1.000000000000000000, 1.000000000000000000, 1.000000000000000666, 1.000000000000000000, 1.000000000000000444, 1.000000000000000000, 1.000000000000000444, 1.000000000000000222, 0.9999999999999997780, 1.000000000000000444, 1.000000000000000000, 1.000000000000000444, 1.000000000000000222, 1.000000000000000444, 1.000000000000000222, 1.000000000000000222, 1.000000000000000444, 1.000000000000000000, 1.000000000000000222, 1.000000000000000444, 1.000000000000000222, 1.000000000000000000, 1.000000000000000444, 0.9999999999999997780, 1.000000000000000444, 1.000000000000000222, 1.000000000000000222, 1.000000000000000222, 1.000000000000000000, 1.000000000000000444, 1.000000000000000222, 1.000000000000000666, 0.9999999999999997780, 1.000000000000000444, 1.000000000000000222, 1.000000000000000000, 1.000000000000000222, 1.000000000000000444, 1.000000000000000222, 1.000000000000000000, 1.000000000000000444, 1.000000000000000222, 1.000000000000000444, 1.000000000000000000, 1.000000000000000444, 1.000000000000000222, 1.000000000000000444, 1.000000000000000222, 1.000000000000000222, 1.000000000000000444, 1.000000000000000222, 1.000000000000000444, 1.000000000000000000, 1.000000000000000444, 1.000000000000000222, 1.000000000000000222, 1.000000000000000000, 1.000000000000000666, 0.9999999999999997780, 1.000000000000000444, 1.000000000000000222, 1.000000000000000444, 1.000000000000000222, 1.000000000000000444, 1.000000000000000000, 1.000000000000000444, 1.000000000000000222, 1.000000000000000222, 1.000000000000000444, 1.000000000000000222, 1.000000000000000444, 1.000000000000000000, 1.000000000000000444, 1.000000000000000444, 0.9999999999999997780, 1.000000000000000444, 1.000000000000000000, 1.000000000000000444, 1.000000000000000444, 1.000000000000000222, 1.000000000000000000, 1.000000000000000444, 1.000000000000000222, 1.000000000000000444, 1.000000000000000000, 1.000000000000000444, 1.000000000000000222, 1.000000000000000444, 1.000000000000000222, 1.000000000000000444, 1.000000000000000222, 1.000000000000000222, 1.000000000000000444, 1.000000000000000444, 1.000000000000000000, 1.000000000000000444, 0.9999999999999997780, 1.000000000000000444, 1.000000000000000222, 1.000000000000000222, 1.000000000000000222, 1.000000000000000444, 1.000000000000000222, 1.000000000000000222, 1.000000000000000444, 1.000000000000000000, 1.000000000000000444, 1.000000000000000000, 1.000000000000000444, 1.000000000000000222, 1.000000000000000000, 1.000000000000000222, 1.000000000000000444, 1.000000000000000000, 1.000000000000000444, 1.000000000000000000, 1.000000000000000444, 1.000000000000000444, 1.000000000000000000, 1.000000000000000444, 1.000000000000000000, 1.000000000000000444, 1.000000000000000000, 1.000000000000000444, 1.000000000000000000, 1.000000000000000444, 1.000000000000000000, 1.000000000000000444, 1.000000000000000000, 1.000000000000000444, 1.000000000000000222, 1.000000000000000222, 1.000000000000000222, 1.000000000000000222),
 ( 0.3333333333333334259, 0.3333333333333334259, 0.3333333333333333703, 0.3333333333333334259, 0.3333333333333334814, 0.3333333333333333148, 0.3333333333333335924, 0.3333333333333333148, 0.3333333333333334259, 0.3333333333333333703, 0.3333333333333334814, 0.3333333333333334814, 0.3333333333333333148, 0.3333333333333334814, 0.3333333333333333703, 0.3333333333333334259, 0.3333333333333334259, 0.3333333333333333703, 0.3333333333333334814, 0.3333333333333334259, 0.3333333333333335369, 0.3333333333333333148, 0.3333333333333335369, 0.3333333333333333703, 0.3333333333333333703, 0.3333333333333334259, 0.3333333333333334814, 0.3333333333333334814, 0.3333333333333333148, 0.3333333333333335369, 0.3333333333333335924, 0.3333333333333334259, 0.3333333333333333703, 0.3333333333333335369, 0.3333333333333334259, 0.3333333333333334259, 0.3333333333333334814, 0.3333333333333335369, 0.3333333333333333703, 0.3333333333333334259, 0.3333333333333335369, 0.3333333333333333148, 0.3333333333333334259, 0.3333333333333335369, 0.3333333333333333703, 0.3333333333333334259, 0.3333333333333333703, 0.3333333333333335369, 0.3333333333333333703, 0.3333333333333334814, 0.3333333333333333703, 0.3333333333333334259, 0.3333333333333333703, 0.3333333333333333703, 0.3333333333333334259, 0.3333333333333333703, 0.3333333333333334259, 0.3333333333333333148, 0.3333333333333336479, 0.3333333333333334259, 0.3333333333333334814, 0.3333333333333333703, 0.3333333333333335369, 0.3333333333333334259, 0.3333333333333334259, 0.3333333333333334259, 0.3333333333333334259, 0.3333333333333333703, 0.3333333333333333703, 0.3333333333333335369, 0.3333333333333333703, 0.3333333333333335369, 0.3333333333333334259, 0.3333333333333333703, 0.3333333333333334814, 0.3333333333333334259, 0.3333333333333333703, 0.3333333333333333148, 0.3333333333333335369, 0.3333333333333333703, 0.3333333333333335369, 0.3333333333333333703, 0.3333333333333334814, 0.3333333333333333703, 0.3333333333333334259, 0.3333333333333333148, 0.3333333333333335369, 0.3333333333333333703, 0.3333333333333334814, 0.3333333333333333148, 0.3333333333333334814, 0.3333333333333334259, 0.3333333333333335369, 0.3333333333333334259, 0.3333333333333334814, 0.3333333333333334259, 0.3333333333333334259, 0.3333333333333334259, 0.3333333333333334259, 0.3333333333333333703, 0.3333333333333333703, 0.3333333333333334814, 0.3333333333333333703, 0.3333333333333333703, 0.3333333333333335369, 0.3333333333333332593, 0.3333333333333335369, 0.3333333333333332593, 0.3333333333333335924, 0.3333333333333334259, 0.3333333333333334814, 0.3333333333333333703, 0.3333333333333334814, 0.3333333333333334259, 0.3333333333333334259, 0.3333333333333334814, 0.3333333333333333703, 0.3333333333333333703, 0.3333333333333334814, 0.3333333333333333703, 0.3333333333333334814, 0.3333333333333333703, 0.3333333333333334259, 0.3333333333333334259, 0.3333333333333335369, 0.3333333333333333703, 0.3333333333333335369, 0.3333333333333334259, 0.3333333333333335369, 0.3333333333333334259, 0.3333333333333334259, 0.3333333333333334814, 0.3333333333333334814, 0.3333333333333333703, 0.3333333333333334814, 0.3333333333333333148, 0.3333333333333335369, 0.3333333333333333148, 0.3333333333333335369, 0.3333333333333334259, 0.3333333333333334259, 0.3333333333333334814, 0.3333333333333334814, 0.3333333333333333703, 0.3333333333333335369, 0.3333333333333333703, 0.3333333333333334259, 0.3333333333333334814, 0.3333333333333334814, 0.3333333333333334259, 0.3333333333333334259, 0.3333333333333335369, 0.3333333333333333148, 0.3333333333333335924, 0.3333333333333333703, 0.3333333333333333703, 0.3333333333333335369, 0.3333333333333333703, 0.3333333333333335924, 0.3333333333333333148, 0.3333333333333333703, 0.3333333333333334814, 0.3333333333333333703, 0.3333333333333335369, 0.3333333333333333703, 0.3333333333333334259, 0.3333333333333334814, 0.3333333333333333703, 0.3333333333333334259, 0.3333333333333334259, 0.3333333333333334259, 0.3333333333333334814, 0.3333333333333333703, 0.3333333333333334259, 0.3333333333333333703, 0.3333333333333335369, 0.3333333333333333703, 0.3333333333333334259, 0.3333333333333334259, 0.3333333333333333703, 0.3333333333333334814, 0.3333333333333333703, 0.3333333333333334259, 0.3333333333333333703, 0.3333333333333334814, 0.3333333333333335369, 0.3333333333333334259, 0.3333333333333334259, 0.3333333333333333703, 0.3333333333333335369, 0.3333333333333333703, 0.3333333333333333703, 0.3333333333333335369, 0.3333333333333333703, 0.3333333333333335924, 0.3333333333333332593, 0.3333333333333335369, 0.3333333333333334259, 0.3333333333333333703, 0.3333333333333335369, 0.3333333333333333703, 0.3333333333333333703, 0.3333333333333334259, 0.3333333333333335369, 0.3333333333333333148, 0.3333333333333333703, 0.3333333333333335369, 0.3333333333333334259, 0.3333333333333333703, 0.3333333333333335369, 0.3333333333333333703, 0.3333333333333335924, 0.3333333333333333703, 0.3333333333333335369, 0.3333333333333334259, 0.3333333333333334814, 0.3333333333333334259, 0.3333333333333334259, 0.3333333333333334814, 0.3333333333333334259, 0.3333333333333334259, 0.3333333333333333148, 0.3333333333333333703, 0.3333333333333334814, 0.3333333333333334814, 0.3333333333333334259, 0.3333333333333333703, 0.3333333333333334259, 0.3333333333333333148, 0.3333333333333335369, 0.3333333333333333703, 0.3333333333333334814, 0.3333333333333335369, 0.3333333333333335369, 0.3333333333333335369, 0.3333333333333333703, 0.3333333333333334259, 0.3333333333333334259, 0.3333333333333333148, 0.3333333333333335369, 0.3333333333333334259, 0.3333333333333334259, 0.3333333333333334259, 0.3333333333333334814, 0.3333333333333334259, 0.3333333333333333148, 0.3333333333333334814, 0.3333333333333334259, 0.3333333333333333703, 0.3333333333333333703, 0.3333333333333334814, 0.3333333333333333703, 0.3333333333333334814, 0.3333333333333334814, 0.3333333333333333148, 0.3333333333333335924, 0.3333333333333333148, 0.3333333333333335369, 0.3333333333333333148, 0.3333333333333335924, 0.3333333333333333703, 0.3333333333333333148, 0.3333333333333334259, 0.3333333333333334259, 0.3333333333333334259, 0.3333333333333333703, 0.3333333333333334814, 0.3333333333333333703, 0.3333333333333334814, 0.3333333333333334814, 0.3333333333333333703, 0.3333333333333334259, 0.3333333333333334259, 0.3333333333333334814, 0.3333333333333333703, 0.3333333333333333703, 0.3333333333333334259, 0.3333333333333334259, 0.3333333333333333703, 0.3333333333333334259, 0.3333333333333333703, 0.3333333333333334259, 0.3333333333333334259, 0.3333333333333333703, 0.3333333333333335924, 0.3333333333333332593, 0.3333333333333335369, 0.3333333333333334259, 0.3333333333333333703, 0.3333333333333333148, 0.3333333333333335924, 0.3333333333333333148, 0.3333333333333333703, 0.3333333333333334259, 0.3333333333333334814, 0.3333333333333335369, 0.3333333333333333703, 0.3333333333333334259, 0.3333333333333333703, 0.3333333333333335369, 0.3333333333333333703, 0.3333333333333334259, 0.3333333333333334814, 0.3333333333333333703, 0.3333333333333335369, 0.3333333333333333148, 0.3333333333333335369, 0.3333333333333334259, 0.3333333333333334259, 0.3333333333333333703, 0.3333333333333335369, 0.3333333333333333703, 0.3333333333333335369, 0.3333333333333334814, 0.3333333333333333703, 0.3333333333333334814, 0.3333333333333333703, 0.3333333333333333703, 0.3333333333333335369, 0.3333333333333333703, 0.3333333333333334259, 0.3333333333333334814, 0.3333333333333333703, 0.3333333333333334259, 0.3333333333333333148, 0.3333333333333335369, 0.3333333333333334259, 0.3333333333333333703, 0.3333333333333334814, 0.3333333333333334259, 0.3333333333333334814, 0.3333333333333334259, 0.3333333333333333703, 0.3333333333333333703, 0.3333333333333334259, 0.3333333333333334259, 0.3333333333333334259, 0.3333333333333334259, 0.3333333333333333703, 0.3333333333333334814, 0.3333333333333334814, 0.3333333333333333703, 0.3333333333333335369, 0.3333333333333333703, 0.3333333333333334814, 0.3333333333333334814, 0.3333333333333335369, 0.3333333333333333148, 0.3333333333333335369, 0.3333333333333333703, 0.3333333333333333148, 0.3333333333333334814, 0.3333333333333333703, 0.3333333333333334814, 0.3333333333333333703, 0.3333333333333334814, 0.3333333333333333703, 0.3333333333333335369, 0.3333333333333333703, 0.3333333333333334814, 0.3333333333333334259, 0.3333333333333334814, 0.3333333333333334259, 0.3333333333333333703, 0.3333333333333333703, 0.3333333333333334814, 0.3333333333333334259, 0.3333333333333334814, 0.3333333333333334259, 0.3333333333333334259, 0.3333333333333334259, 0.3333333333333333703, 0.3333333333333334259, 0.3333333333333333703, 0.3333333333333334814, 0.3333333333333333148, 0.3333333333333335369, 0.3333333333333333703, 0.3333333333333334814, 0.3333333333333333703, 0.3333333333333335369, 0.3333333333333334259, 0.3333333333333334259, 0.3333333333333334259, 0.3333333333333334259, 0.3333333333333334259, 0.3333333333333334259),
 ( 0.3333333333333334259, 0.3333333333333334259, 0.3333333333333333703, 0.3333333333333334259, 0.3333333333333334814, 0.3333333333333333148, 0.3333333333333335924, 0.3333333333333333148, 0.3333333333333334259, 0.3333333333333333703, 0.3333333333333334814, 0.3333333333333334814, 0.3333333333333333148, 0.3333333333333334814, 0.3333333333333333703, 0.3333333333333334259, 0.3333333333333334259, 0.3333333333333333703, 0.3333333333333334814, 0.3333333333333334259, 0.3333333333333335369, 0.3333333333333333148, 0.3333333333333335369, 0.3333333333333333703, 0.3333333333333333703, 0.3333333333333334259, 0.3333333333333334814, 0.3333333333333334814, 0.3333333333333333148, 0.3333333333333335369, 0.3333333333333335924, 0.3333333333333334259, 0.3333333333333333703, 0.3333333333333335369, 0.3333333333333334259, 0.3333333333333334259, 0.3333333333333334814, 0.3333333333333335369, 0.3333333333333333703, 0.3333333333333334259, 0.3333333333333335369, 0.3333333333333333148, 0.3333333333333334259, 0.3333333333333335369, 0.3333333333333333703, 0.3333333333333334259, 0.3333333333333333703, 0.3333333333333335369, 0.3333333333333333703, 0.3333333333333334814, 0.3333333333333333703, 0.3333333333333334259, 0.3333333333333333703, 0.3333333333333333703, 0.3333333333333334259, 0.3333333333333333703, 0.3333333333333334259, 0.3333333333333333148, 0.3333333333333336479, 0.3333333333333334259, 0.3333333333333334814, 0.3333333333333333703, 0.3333333333333335369, 0.3333333333333334259, 0.3333333333333334259, 0.3333333333333334259, 0.3333333333333334259, 0.3333333333333333703, 0.3333333333333333703, 0.3333333333333335369, 0.3333333333333333703, 0.3333333333333335369, 0.3333333333333334259, 0.3333333333333333703, 0.3333333333333334814, 0.3333333333333334259, 0.3333333333333333703, 0.3333333333333333148, 0.3333333333333335369, 0.3333333333333333703, 0.3333333333333335369, 0.3333333333333333703, 0.3333333333333334814, 0.3333333333333333703, 0.3333333333333334259, 0.3333333333333333148, 0.3333333333333335369, 0.3333333333333333703, 0.3333333333333334814, 0.3333333333333333148, 0.3333333333333334814, 0.3333333333333334259, 0.3333333333333335369, 0.3333333333333334259, 0.3333333333333334814, 0.3333333333333334259, 0.3333333333333334259, 0.3333333333333334259, 0.3333333333333334259, 0.3333333333333333703, 0.3333333333333333703, 0.3333333333333334814, 0.3333333333333333703, 0.3333333333333333703, 0.3333333333333335369, 0.3333333333333332593, 0.3333333333333335369, 0.3333333333333332593, 0.3333333333333335924, 0.3333333333333334259, 0.3333333333333334814, 0.3333333333333333703, 0.3333333333333334814, 0.3333333333333334259, 0.3333333333333334259, 0.3333333333333334814, 0.3333333333333333703, 0.3333333333333333703, 0.3333333333333334814, 0.3333333333333333703, 0.3333333333333334814, 0.3333333333333333703, 0.3333333333333334259, 0.3333333333333334259, 0.3333333333333335369, 0.3333333333333333703, 0.3333333333333335369, 0.3333333333333334259, 0.3333333333333335369, 0.3333333333333334259, 0.3333333333333334259, 0.3333333333333334814, 0.3333333333333334814, 0.3333333333333333703, 0.3333333333333334814, 0.3333333333333333148, 0.3333333333333335369, 0.3333333333333333148, 0.3333333333333335369, 0.3333333333333334259, 0.3333333333333334259, 0.3333333333333334814, 0.3333333333333334814, 0.3333333333333333703, 0.3333333333333335369, 0.3333333333333333703, 0.3333333333333334259, 0.3333333333333334814, 0.3333333333333334814, 0.3333333333333334259, 0.3333333333333334259, 0.3333333333333335369, 0.3333333333333333148, 0.3333333333333335924, 0.3333333333333333703, 0.3333333333333333703, 0.3333333333333335369, 0.3333333333333333703, 0.3333333333333335924, 0.3333333333333333148, 0.3333333333333333703, 0.3333333333333334814, 0.3333333333333333703, 0.3333333333333335369, 0.3333333333333333703, 0.3333333333333334259, 0.3333333333333334814, 0.3333333333333333703, 0.3333333333333334259, 0.3333333333333334259, 0.3333333333333334259, 0.3333333333333334814, 0.3333333333333333703, 0.3333333333333334259, 0.3333333333333333703, 0.3333333333333335369, 0.3333333333333333703, 0.3333333333333334259, 0.3333333333333334259, 0.3333333333333333703, 0.3333333333333334814, 0.3333333333333333703, 0.3333333333333334259, 0.3333333333333333703, 0.3333333333333334814, 0.3333333333333335369, 0.3333333333333334259, 0.3333333333333334259, 0.3333333333333333703, 0.3333333333333335369, 0.3333333333333333703, 0.3333333333333333703, 0.3333333333333335369, 0.3333333333333333703, 0.3333333333333335924, 0.3333333333333332593, 0.3333333333333335369, 0.3333333333333334259, 0.3333333333333333703, 0.3333333333333335369, 0.3333333333333333703, 0.3333333333333333703, 0.3333333333333334259, 0.3333333333333335369, 0.3333333333333333148, 0.3333333333333333703, 0.3333333333333335369, 0.3333333333333334259, 0.3333333333333333703, 0.3333333333333335369, 0.3333333333333333703, 0.3333333333333335924, 0.3333333333333333703, 0.3333333333333335369, 0.3333333333333334259, 0.3333333333333334814, 0.3333333333333334259, 0.3333333333333334259, 0.3333333333333334814, 0.3333333333333334259, 0.3333333333333334259, 0.3333333333333333148, 0.3333333333333333703, 0.3333333333333334814, 0.3333333333333334814, 0.3333333333333334259, 0.3333333333333333703, 0.3333333333333334259, 0.3333333333333333148, 0.3333333333333335369, 0.3333333333333333703, 0.3333333333333334814, 0.3333333333333335369, 0.3333333333333335369, 0.3333333333333335369, 0.3333333333333333703, 0.3333333333333334259, 0.3333333333333334259, 0.3333333333333333148, 0.3333333333333335369, 0.3333333333333334259, 0.3333333333333334259, 0.3333333333333334259, 0.3333333333333334814, 0.3333333333333334259, 0.3333333333333333148, 0.3333333333333334814, 0.3333333333333334259, 0.3333333333333333703, 0.3333333333333333703, 0.3333333333333334814, 0.3333333333333333703, 0.3333333333333334814, 0.3333333333333334814, 0.3333333333333333148, 0.3333333333333335924, 0.3333333333333333148, 0.3333333333333335369, 0.3333333333333333148, 0.3333333333333335924, 0.3333333333333333703, 0.3333333333333333148, 0.3333333333333334259, 0.3333333333333334259, 0.3333333333333334259, 0.3333333333333333703, 0.3333333333333334814, 0.3333333333333333703, 0.3333333333333334814, 0.3333333333333334814, 0.3333333333333333703, 0.3333333333333334259, 0.3333333333333334259, 0.3333333333333334814, 0.3333333333333333703, 0.3333333333333333703, 0.3333333333333334259, 0.3333333333333334259, 0.3333333333333333703, 0.3333333333333334259, 0.3333333333333333703, 0.3333333333333334259, 0.3333333333333334259, 0.3333333333333333703, 0.3333333333333335924, 0.3333333333333332593, 0.3333333333333335369, 0.3333333333333334259, 0.3333333333333333703, 0.3333333333333333148, 0.3333333333333335924, 0.3333333333333333148, 0.3333333333333333703, 0.3333333333333334259, 0.3333333333333334814, 0.3333333333333335369, 0.3333333333333333703, 0.3333333333333334259, 0.3333333333333333703, 0.3333333333333335369, 0.3333333333333333703, 0.3333333333333334259, 0.3333333333333334814, 0.3333333333333333703, 0.3333333333333335369, 0.3333333333333333148, 0.3333333333333335369, 0.3333333333333334259, 0.3333333333333334259, 0.3333333333333333703, 0.3333333333333335369, 0.3333333333333333703, 0.3333333333333335369, 0.3333333333333334814, 0.3333333333333333703, 0.3333333333333334814, 0.3333333333333333703, 0.3333333333333333703, 0.3333333333333335369, 0.3333333333333333703, 0.3333333333333334259, 0.3333333333333334814, 0.3333333333333333703, 0.3333333333333334259, 0.3333333333333333148, 0.3333333333333335369, 0.3333333333333334259, 0.3333333333333333703, 0.3333333333333334814, 0.3333333333333334259, 0.3333333333333334814, 0.3333333333333334259, 0.3333333333333333703, 0.3333333333333333703, 0.3333333333333334259, 0.3333333333333334259, 0.3333333333333334259, 0.3333333333333334259, 0.3333333333333333703, 0.3333333333333334814, 0.3333333333333334814, 0.3333333333333333703, 0.3333333333333335369, 0.3333333333333333703, 0.3333333333333334814, 0.3333333333333334814, 0.3333333333333335369, 0.3333333333333333148, 0.3333333333333335369, 0.3333333333333333703, 0.3333333333333333148, 0.3333333333333334814, 0.3333333333333333703, 0.3333333333333334814, 0.3333333333333333703, 0.3333333333333334814, 0.3333333333333333703, 0.3333333333333335369, 0.3333333333333333703, 0.3333333333333334814, 0.3333333333333334259, 0.3333333333333334814, 0.3333333333333334259, 0.3333333333333333703, 0.3333333333333333703, 0.3333333333333334814, 0.3333333333333334259, 0.3333333333333334814, 0.3333333333333334259, 0.3333333333333334259, 0.3333333333333334259, 0.3333333333333333703, 0.3333333333333334259, 0.3333333333333333703, 0.3333333333333334814, 0.3333333333333333148, 0.3333333333333335369, 0.3333333333333333703, 0.3333333333333334814, 0.3333333333333333703, 0.3333333333333335369, 0.3333333333333334259, 0.3333333333333334259, 0.3333333333333334259, 0.3333333333333334259, 0.3333333333333334259, 0.3333333333333334259),
 ( 1.000000000000000222, 1.000000000000000222, 1.000000000000000222, 1.000000000000000222, 1.000000000000000444, 1.000000000000000000, 1.000000000000000666, 0.9999999999999997780, 1.000000000000000444, 1.000000000000000000, 1.000000000000000444, 1.000000000000000444, 1.000000000000000000, 1.000000000000000444, 1.000000000000000000, 1.000000000000000444, 1.000000000000000222, 1.000000000000000222, 1.000000000000000222, 1.000000000000000444, 1.000000000000000444, 1.000000000000000000, 1.000000000000000444, 1.000000000000000000, 1.000000000000000222, 1.000000000000000222, 1.000000000000000444, 1.000000000000000222, 1.000000000000000222, 1.000000000000000444, 1.000000000000000444, 1.000000000000000444, 1.000000000000000000, 1.000000000000000444, 1.000000000000000444, 1.000000000000000000, 1.000000000000000444, 1.000000000000000444, 1.000000000000000000, 1.000000000000000444, 1.000000000000000444, 1.000000000000000000, 1.000000000000000222, 1.000000000000000444, 1.000000000000000222, 1.000000000000000222, 1.000000000000000000, 1.000000000000000444, 1.000000000000000222, 1.000000000000000222, 1.000000000000000222, 1.000000000000000222, 1.000000000000000222, 1.000000000000000222, 1.000000000000000444, 1.000000000000000000, 1.000000000000000444, 0.9999999999999997780, 1.000000000000000666, 1.000000000000000444, 1.000000000000000444, 1.000000000000000000, 1.000000000000000444, 1.000000000000000222, 1.000000000000000222, 1.000000000000000444, 1.000000000000000222, 1.000000000000000444, 1.000000000000000000, 1.000000000000000444, 1.000000000000000222, 1.000000000000000444, 1.000000000000000444, 1.000000000000000222, 1.000000000000000222, 1.000000000000000222, 1.000000000000000444, 0.9999999999999997780, 1.000000000000000444, 1.000000000000000000, 1.000000000000000444, 1.000000000000000000, 1.000000000000000444, 0.9999999999999997780, 1.000000000000000444, 0.9999999999999997780, 1.000000000000000444, 1.000000000000000222, 1.000000000000000444, 1.000000000000000000, 1.000000000000000222, 1.000000000000000444, 1.000000000000000444, 1.000000000000000222, 1.000000000000000444, 1.000000000000000444, 1.000000000000000222, 1.000000000000000222, 1.000000000000000222, 1.000000000000000222, 1.000000000000000000, 1.000000000000000222, 1.000000000000000222, 1.000000000000000222, 1.000000000000000444, 1.000000000000000000, 1.000000000000000444, 0.9999999999999997780, 1.000000000000000666, 1.000000000000000222, 1.000000000000000444, 1.000000000000000000, 1.000000000000000444, 1.000000000000000222, 1.000000000000000222, 1.000000000000000444, 1.000000000000000000, 1.000000000000000000, 1.000000000000000444, 1.000000000000000000, 1.000000000000000444, 1.000000000000000000, 1.000000000000000444, 1.000000000000000222, 1.000000000000000444, 1.000000000000000222, 1.000000000000000444, 1.000000000000000222, 1.000000000000000444, 1.000000000000000000, 1.000000000000000444, 1.000000000000000222, 1.000000000000000444, 1.000000000000000000, 1.000000000000000444, 1.000000000000000000, 1.000000000000000444, 1.000000000000000000, 1.000000000000000444, 1.000000000000000222, 1.000000000000000444, 1.000000000000000222, 1.000000000000000444, 0.9999999999999997780, 1.000000000000000444, 1.000000000000000000, 1.000000000000000444, 1.000000000000000222, 1.000000000000000222, 1.000000000000000222, 1.000000000000000222, 1.000000000000000444, 0.9999999999999997780, 1.000000000000000444, 1.000000000000000000, 1.000000000000000000, 1.000000000000000222, 1.000000000000000222, 1.000000000000000666, 0.9999999999999997780, 1.000000000000000000, 1.000000000000000444, 1.000000000000000222, 1.000000000000000444, 1.000000000000000000, 1.000000000000000222, 1.000000000000000444, 1.000000000000000222, 1.000000000000000000, 1.000000000000000444, 1.000000000000000222, 1.000000000000000222, 1.000000000000000444, 1.000000000000000222, 1.000000000000000000, 1.000000000000000444, 1.000000000000000000, 1.000000000000000444, 1.000000000000000222, 1.000000000000000222, 1.000000000000000444, 0.9999999999999997780, 1.000000000000000444, 0.9999999999999997780, 1.000000000000000444, 1.000000000000000222, 1.000000000000000444, 1.000000000000000222, 1.000000000000000222, 1.000000000000000444, 1.000000000000000000, 1.000000000000000222, 1.000000000000000444, 1.000000000000000000, 1.000000000000000444, 1.000000000000000000, 1.000000000000000222, 1.000000000000000444, 1.000000000000000000, 1.000000000000000444, 0.9999999999999997780, 1.000000000000000444, 1.000000000000000222, 1.000000000000000444, 1.000000000000000000, 1.000000000000000000, 1.000000000000000444, 1.000000000000000000, 1.000000000000000222, 1.000000000000000444, 1.000000000000000222, 1.000000000000000444, 1.000000000000000222, 1.000000000000000444, 1.000000000000000444, 1.000000000000000444, 1.000000000000000000, 1.000000000000000444, 1.000000000000000222, 1.000000000000000444, 1.000000000000000222, 1.000000000000000000, 1.000000000000000222, 1.000000000000000444, 1.000000000000000222, 1.000000000000000444, 1.000000000000000000, 1.000000000000000222, 1.000000000000000000, 1.000000000000000444, 1.000000000000000000, 1.000000000000000444, 1.000000000000000444, 1.000000000000000444, 1.000000000000000444, 1.000000000000000000, 1.000000000000000222, 1.000000000000000444, 1.000000000000000000, 1.000000000000000444, 1.000000000000000444, 1.000000000000000444, 1.000000000000000222, 1.000000000000000222, 1.000000000000000222, 0.9999999999999997780, 1.000000000000000444, 1.000000000000000222, 1.000000000000000222, 1.000000000000000000, 1.000000000000000444, 1.000000000000000000, 1.000000000000000444, 1.000000000000000000, 1.000000000000000000, 1.000000000000000666, 1.000000000000000000, 1.000000000000000444, 1.000000000000000000, 1.000000000000000444, 1.000000000000000222, 0.9999999999999997780, 1.000000000000000444, 1.000000000000000000, 1.000000000000000444, 1.000000000000000222, 1.000000000000000444, 1.000000000000000222, 1.000000000000000222, 1.000000000000000444, 1.000000000000000000, 1.000000000000000222, 1.000000000000000444, 1.000000000000000222, 1.000000000000000000, 1.000000000000000444, 0.9999999999999997780, 1.000000000000000444, 1.000000000000000222, 1.000000000000000222, 1.000000000000000222, 1.000000000000000000, 1.000000000000000444, 1.000000000000000222, 1.000000000000000666, 0.9999999999999997780, 1.000000000000000444, 1.000000000000000222, 1.000000000000000000, 1.000000000000000222, 1.000000000000000444, 1.000000000000000222, 1.000000000000000000, 1.000000000000000444, 1.000000000000000222, 1.000000000000000444, 1.000000000000000000, 1.000000000000000444, 1.000000000000000222, 1.000000000000000444, 1.000000000000000222, 1.000000000000000222, 1.000000000000000444, 1.000000000000000222, 1.000000000000000444, 1.000000000000000000, 1.000000000000000444, 1.000000000000000222, 1.000000000000000222, 1.000000000000000000, 1.000000000000000666, 0.9999999999999997780, 1.000000000000000444, 1.000000000000000222, 1.000000000000000444, 1.000000000000000222, 1.000000000000000444, 1.000000000000000000, 1.000000000000000444, 1.000000000000000222, 1.000000000000000222, 1.000000000000000444, 1.000000000000000222, 1.000000000000000444, 1.000000000000000000, 1.000000000000000444, 1.000000000000000444, 0.9999999999999997780, 1.000000000000000444, 1.000000000000000000, 1.000000000000000444, 1.000000000000000444, 1.000000000000000222, 1.000000000000000000, 1.000000000000000444, 1.000000000000000222, 1.000000000000000444, 1.000000000000000000, 1.000000000000000444, 1.000000000000000222, 1.000000000000000444, 1.000000000000000222, 1.000000000000000444, 1.000000000000000222, 1.000000000000000222, 1.000000000000000444, 1.000000000000000444, 1.000000000000000000, 1.000000000000000444, 0.9999999999999997780, 1.000000000000000444, 1.000000000000000222, 1.000000000000000222, 1.000000000000000222, 1.000000000000000444, 1.000000000000000222, 1.000000000000000222, 1.000000000000000444, 1.000000000000000000, 1.000000000000000444, 1.000000000000000000, 1.000000000000000444, 1.000000000000000222, 1.000000000000000000, 1.000000000000000222, 1.000000000000000444, 1.000000000000000000, 1.000000000000000444, 1.000000000000000000, 1.000000000000000444, 1.000000000000000444, 1.000000000000000000, 1.000000000000000444, 1.000000000000000000, 1.000000000000000444, 1.000000000000000000, 1.000000000000000444, 1.000000000000000000, 1.000000000000000444, 1.000000000000000000, 1.000000000000000444, 1.000000000000000000, 1.000000000000000444, 1.000000000000000222, 1.000000000000000222, 1.000000000000000222, 1.000000000000000222),
 ( 0.3333333333333334259, 0.3333333333333334259, 0.3333333333333333703, 0.3333333333333334259, 0.3333333333333334814, 0.3333333333333333148, 0.3333333333333335924, 0.3333333333333333148, 0.3333333333333334259, 0.3333333333333333703, 0.3333333333333334814, 0.3333333333333334814, 0.3333333333333333148, 0.3333333333333334814, 0.3333333333333333703, 0.3333333333333334259, 0.3333333333333334259, 0.3333333333333333703, 0.3333333333333334814, 0.3333333333333334259, 0.3333333333333335369, 0.3333333333333333148, 0.3333333333333335369, 0.3333333333333333703, 0.3333333333333333703, 0.3333333333333334259, 0.3333333333333334814, 0.3333333333333334814, 0.3333333333333333148, 0.3333333333333335369, 0.3333333333333335924, 0.3333333333333334259, 0.3333333333333333703, 0.3333333333333335369, 0.3333333333333334259, 0.3333333333333334259, 0.3333333333333334814, 0.3333333333333335369, 0.3333333333333333703, 0.3333333333333334259, 0.3333333333333335369, 0.3333333333333333148, 0.3333333333333334259, 0.3333333333333335369, 0.3333333333333333703, 0.3333333333333334259, 0.3333333333333333703, 0.3333333333333335369, 0.3333333333333333703, 0.3333333333333334814, 0.3333333333333333703, 0.3333333333333334259, 0.3333333333333333703, 0.3333333333333333703, 0.3333333333333334259, 0.3333333333333333703, 0.3333333333333334259, 0.3333333333333333148, 0.3333333333333336479, 0.3333333333333334259, 0.3333333333333334814, 0.3333333333333333703, 0.3333333333333335369, 0.3333333333333334259, 0.3333333333333334259, 0.3333333333333334259, 0.3333333333333334259, 0.3333333333333333703, 0.3333333333333333703, 0.3333333333333335369, 0.3333333333333333703, 0.3333333333333335369, 0.3333333333333334259, 0.3333333333333333703, 0.3333333333333334814, 0.3333333333333334259, 0.3333333333333333703, 0.3333333333333333148, 0.3333333333333335369, 0.3333333333333333703, 0.3333333333333335369, 0.3333333333333333703, 0.3333333333333334814, 0.3333333333333333703, 0.3333333333333334259, 0.3333333333333333148, 0.3333333333333335369, 0.3333333333333333703, 0.3333333333333334814, 0.3333333333333333148, 0.3333333333333334814, 0.3333333333333334259, 0.3333333333333335369, 0.3333333333333334259, 0.3333333333333334814, 0.3333333333333334259, 0.3333333333333334259, 0.3333333333333334259, 0.3333333333333334259, 0.3333333333333333703, 0.3333333333333333703, 0.3333333333333334814, 0.3333333333333333703, 0.3333333333333333703, 0.3333333333333335369, 0.3333333333333332593, 0.3333333333333335369, 0.3333333333333332593, 0.3333333333333335924, 0.3333333333333334259, 0.3333333333333334814, 0.3333333333333333703, 0.3333333333333334814, 0.3333333333333334259, 0.3333333333333334259, 0.3333333333333334814, 0.3333333333333333703, 0.3333333333333333703, 0.3333333333333334814, 0.3333333333333333703, 0.3333333333333334814, 0.3333333333333333703, 0.3333333333333334259, 0.3333333333333334259, 0.3333333333333335369, 0.3333333333333333703, 0.3333333333333335369, 0.3333333333333334259, 0.3333333333333335369, 0.3333333333333334259, 0.3333333333333334259, 0.3333333333333334814, 0.3333333333333334814, 0.3333333333333333703, 0.3333333333333334814, 0.3333333333333333148, 0.3333333333333335369, 0.3333333333333333148, 0.3333333333333335369, 0.3333333333333334259, 0.3333333333333334259, 0.3333333333333334814, 0.3333333333333334814, 0.3333333333333333703, 0.3333333333333335369, 0.3333333333333333703, 0.3333333333333334259, 0.3333333333333334814, 0.3333333333333334814, 0.3333333333333334259, 0.3333333333333334259, 0.3333333333333335369, 0.3333333333333333148, 0.3333333333333335924, 0.3333333333333333703, 0.3333333333333333703, 0.3333333333333335369, 0.3333333333333333703, 0.3333333333333335924, 0.3333333333333333148, 0.3333333333333333703, 0.3333333333333334814, 0.3333333333333333703, 0.3333333333333335369, 0.3333333333333333703, 0.3333333333333334259, 0.3333333333333334814, 0.3333333333333333703, 0.3333333333333334259, 0.3333333333333334259, 0.3333333333333334259, 0.3333333333333334814, 0.3333333333333333703, 0.3333333333333334259, 0.3333333333333333703, 0.3333333333333335369, 0.3333333333333333703, 0.3333333333333334259, 0.3333333333333334259, 0.3333333333333333703, 0.3333333333333334814, 0.3333333333333333703, 0.3333333333333334259, 0.3333333333333333703, 0.3333333333333334814, 0.3333333333333335369, 0.3333333333333334259, 0.3333333333333334259, 0.3333333333333333703, 0.3333333333333335369, 0.3333333333333333703, 0.3333333333333333703, 0.3333333333333335369, 0.3333333333333333703, 0.3333333333333335924, 0.3333333333333332593, 0.3333333333333335369, 0.3333333333333334259, 0.3333333333333333703, 0.3333333333333335369, 0.3333333333333333703, 0.3333333333333333703, 0.3333333333333334259, 0.3333333333333335369, 0.3333333333333333148, 0.3333333333333333703, 0.3333333333333335369, 0.3333333333333334259, 0.3333333333333333703, 0.3333333333333335369, 0.3333333333333333703, 0.3333333333333335924, 0.3333333333333333703, 0.3333333333333335369, 0.3333333333333334259, 0.3333333333333334814, 0.3333333333333334259, 0.3333333333333334259, 0.3333333333333334814, 0.3333333333333334259, 0.3333333333333334259, 0.3333333333333333148, 0.3333333333333333703, 0.3333333333333334814, 0.3333333333333334814, 0.3333333333333334259, 0.3333333333333333703, 0.3333333333333334259, 0.3333333333333333148, 0.3333333333333335369, 0.3333333333333333703, 0.3333333333333334814, 0.3333333333333335369, 0.3333333333333335369, 0.3333333333333335369, 0.3333333333333333703, 0.3333333333333334259, 0.3333333333333334259, 0.3333333333333333148, 0.3333333333333335369, 0.3333333333333334259, 0.3333333333333334259, 0.3333333333333334259, 0.3333333333333334814, 0.3333333333333334259, 0.3333333333333333148, 0.3333333333333334814, 0.3333333333333334259, 0.3333333333333333703, 0.3333333333333333703, 0.3333333333333334814, 0.3333333333333333703, 0.3333333333333334814, 0.3333333333333334814, 0.3333333333333333148, 0.3333333333333335924, 0.3333333333333333148, 0.3333333333333335369, 0.3333333333333333148, 0.3333333333333335924, 0.3333333333333333703, 0.3333333333333333148, 0.3333333333333334259, 0.3333333333333334259, 0.3333333333333334259, 0.3333333333333333703, 0.3333333333333334814, 0.3333333333333333703, 0.3333333333333334814, 0.3333333333333334814, 0.3333333333333333703, 0.3333333333333334259, 0.3333333333333334259, 0.3333333333333334814, 0.3333333333333333703, 0.3333333333333333703, 0.3333333333333334259, 0.3333333333333334259, 0.3333333333333333703, 0.3333333333333334259, 0.3333333333333333703, 0.3333333333333334259, 0.3333333333333334259, 0.3333333333333333703, 0.3333333333333335924, 0.3333333333333332593, 0.3333333333333335369, 0.3333333333333334259, 0.3333333333333333703, 0.3333333333333333148, 0.3333333333333335924, 0.3333333333333333148, 0.3333333333333333703, 0.3333333333333334259, 0.3333333333333334814, 0.3333333333333335369, 0.3333333333333333703, 0.3333333333333334259, 0.3333333333333333703, 0.3333333333333335369, 0.3333333333333333703, 0.3333333333333334259, 0.3333333333333334814, 0.3333333333333333703, 0.3333333333333335369, 0.3333333333333333148, 0.3333333333333335369, 0.3333333333333334259, 0.3333333333333334259, 0.3333333333333333703, 0.3333333333333335369, 0.3333333333333333703, 0.3333333333333335369, 0.3333333333333334814, 0.3333333333333333703, 0.3333333333333334814, 0.3333333333333333703, 0.3333333333333333703, 0.3333333333333335369, 0.3333333333333333703, 0.3333333333333334259, 0.3333333333333334814, 0.3333333333333333703, 0.3333333333333334259, 0.3333333333333333148, 0.3333333333333335369, 0.3333333333333334259, 0.3333333333333333703, 0.3333333333333334814, 0.3333333333333334259, 0.3333333333333334814, 0.3333333333333334259, 0.3333333333333333703, 0.3333333333333333703, 0.3333333333333334259, 0.3333333333333334259, 0.3333333333333334259, 0.3333333333333334259, 0.3333333333333333703, 0.3333333333333334814, 0.3333333333333334814, 0.3333333333333333703, 0.3333333333333335369, 0.3333333333333333703, 0.3333333333333334814, 0.3333333333333334814, 0.3333333333333335369, 0.3333333333333333148, 0.3333333333333335369, 0.3333333333333333703, 0.3333333333333333148, 0.3333333333333334814, 0.3333333333333333703, 0.3333333333333334814, 0.3333333333333333703, 0.3333333333333334814, 0.3333333333333333703, 0.3333333333333335369, 0.3333333333333333703, 0.3333333333333334814, 0.3333333333333334259, 0.3333333333333334814, 0.3333333333333334259, 0.3333333333333333703, 0.3333333333333333703, 0.3333333333333334814, 0.3333333333333334259, 0.3333333333333334814, 0.3333333333333334259, 0.3333333333333334259, 0.3333333333333334259, 0.3333333333333333703, 0.3333333333333334259, 0.3333333333333333703, 0.3333333333333334814, 0.3333333333333333148, 0.3333333333333335369, 0.3333333333333333703, 0.3333333333333334814, 0.3333333333333333703, 0.3333333333333335369, 0.3333333333333334259, 0.3333333333333334259, 0.3333333333333334259, 0.3333333333333334259, 0.3333333333333334259, 0.3333333333333334259),
 ( 0.3333333333333334259, 0.3333333333333334259, 0.3333333333333333703, 0.3333333333333334259, 0.3333333333333334814, 0.3333333333333333148, 0.3333333333333335924, 0.3333333333333333148, 0.3333333333333334259, 0.3333333333333333703, 0.3333333333333334814, 0.3333333333333334814, 0.3333333333333333148, 0.3333333333333334814, 0.3333333333333333703, 0.3333333333333334259, 0.3333333333333334259, 0.3333333333333333703, 0.3333333333333334814, 0.3333333333333334259, 0.3333333333333335369, 0.3333333333333333148, 0.3333333333333335369, 0.3333333333333333703, 0.3333333333333333703, 0.3333333333333334259, 0.3333333333333334814, 0.3333333333333334814, 0.3333333333333333148, 0.3333333333333335369, 0.3333333333333335924, 0.3333333333333334259, 0.3333333333333333703, 0.3333333333333335369, 0.3333333333333334259, 0.3333333333333334259, 0.3333333333333334814, 0.3333333333333335369, 0.3333333333333333703, 0.3333333333333334259, 0.3333333333333335369, 0.3333333333333333148, 0.3333333333333334259, 0.3333333333333335369, 0.3333333333333333703, 0.3333333333333334259, 0.3333333333333333703, 0.3333333333333335369, 0.3333333333333333703, 0.3333333333333334814, 0.3333333333333333703, 0.3333333333333334259, 0.3333333333333333703, 0.3333333333333333703, 0.3333333333333334259, 0.3333333333333333703, 0.3333333333333334259, 0.3333333333333333148, 0.3333333333333336479, 0.3333333333333334259, 0.3333333333333334814, 0.3333333333333333703, 0.3333333333333335369, 0.3333333333333334259, 0.3333333333333334259, 0.3333333333333334259, 0.3333333333333334259, 0.3333333333333333703, 0.3333333333333333703, 0.3333333333333335369, 0.3333333333333333703, 0.3333333333333335369, 0.3333333333333334259, 0.3333333333333333703, 0.3333333333333334814, 0.3333333333333334259, 0.3333333333333333703, 0.3333333333333333148, 0.3333333333333335369, 0.3333333333333333703, 0.3333333333333335369, 0.3333333333333333703, 0.3333333333333334814, 0.3333333333333333703, 0.3333333333333334259, 0.3333333333333333148, 0.3333333333333335369, 0.3333333333333333703, 0.3333333333333334814, 0.3333333333333333148, 0.3333333333333334814, 0.3333333333333334259, 0.3333333333333335369, 0.3333333333333334259, 0.3333333333333334814, 0.3333333333333334259, 0.3333333333333334259, 0.3333333333333334259, 0.3333333333333334259, 0.3333333333333333703, 0.3333333333333333703, 0.3333333333333334814, 0.3333333333333333703, 0.3333333333333333703, 0.3333333333333335369, 0.3333333333333332593, 0.3333333333333335369, 0.3333333333333332593, 0.3333333333333335924, 0.3333333333333334259, 0.3333333333333334814, 0.3333333333333333703, 0.3333333333333334814, 0.3333333333333334259, 0.3333333333333334259, 0.3333333333333334814, 0.3333333333333333703, 0.3333333333333333703, 0.3333333333333334814, 0.3333333333333333703, 0.3333333333333334814, 0.3333333333333333703, 0.3333333333333334259, 0.3333333333333334259, 0.3333333333333335369, 0.3333333333333333703, 0.3333333333333335369, 0.3333333333333334259, 0.3333333333333335369, 0.3333333333333334259, 0.3333333333333334259, 0.3333333333333334814, 0.3333333333333334814, 0.3333333333333333703, 0.3333333333333334814, 0.3333333333333333148, 0.3333333333333335369, 0.3333333333333333148, 0.3333333333333335369, 0.3333333333333334259, 0.3333333333333334259, 0.3333333333333334814, 0.3333333333333334814, 0.3333333333333333703, 0.3333333333333335369, 0.3333333333333333703, 0.3333333333333334259, 0.3333333333333334814, 0.3333333333333334814, 0.3333333333333334259, 0.3333333333333334259, 0.3333333333333335369, 0.3333333333333333148, 0.3333333333333335924, 0.3333333333333333703, 0.3333333333333333703, 0.3333333333333335369, 0.3333333333333333703, 0.3333333333333335924, 0.3333333333333333148, 0.3333333333333333703, 0.3333333333333334814, 0.3333333333333333703, 0.3333333333333335369, 0.3333333333333333703, 0.3333333333333334259, 0.3333333333333334814, 0.3333333333333333703, 0.3333333333333334259, 0.3333333333333334259, 0.3333333333333334259, 0.3333333333333334814, 0.3333333333333333703, 0.3333333333333334259, 0.3333333333333333703, 0.3333333333333335369, 0.3333333333333333703, 0.3333333333333334259, 0.3333333333333334259, 0.3333333333333333703, 0.3333333333333334814, 0.3333333333333333703, 0.3333333333333334259, 0.3333333333333333703, 0.3333333333333334814, 0.3333333333333335369, 0.3333333333333334259, 0.3333333333333334259, 0.3333333333333333703, 0.3333333333333335369, 0.3333333333333333703, 0.3333333333333333703, 0.3333333333333335369, 0.3333333333333333703, 0.3333333333333335924, 0.3333333333333332593, 0.3333333333333335369, 0.3333333333333334259, 0.3333333333333333703, 0.3333333333333335369, 0.3333333333333333703, 0.3333333333333333703, 0.3333333333333334259, 0.3333333333333335369, 0.3333333333333333148, 0.3333333333333333703, 0.3333333333333335369, 0.3333333333333334259, 0.3333333333333333703, 0.3333333333333335369, 0.3333333333333333703, 0.3333333333333335924, 0.3333333333333333703, 0.3333333333333335369, 0.3333333333333334259, 0.3333333333333334814, 0.3333333333333334259, 0.3333333333333334259, 0.3333333333333334814, 0.3333333333333334259, 0.3333333333333334259, 0.3333333333333333148, 0.3333333333333333703, 0.3333333333333334814, 0.3333333333333334814, 0.3333333333333334259, 0.3333333333333333703, 0.3333333333333334259, 0.3333333333333333148, 0.3333333333333335369, 0.3333333333333333703, 0.3333333333333334814, 0.3333333333333335369, 0.3333333333333335369, 0.3333333333333335369, 0.3333333333333333703, 0.3333333333333334259, 0.3333333333333334259, 0.3333333333333333148, 0.3333333333333335369, 0.3333333333333334259, 0.3333333333333334259, 0.3333333333333334259, 0.3333333333333334814, 0.3333333333333334259, 0.3333333333333333148, 0.3333333333333334814, 0.3333333333333334259, 0.3333333333333333703, 0.3333333333333333703, 0.3333333333333334814, 0.3333333333333333703, 0.3333333333333334814, 0.3333333333333334814, 0.3333333333333333148, 0.3333333333333335924, 0.3333333333333333148, 0.3333333333333335369, 0.3333333333333333148, 0.3333333333333335924, 0.3333333333333333703, 0.3333333333333333148, 0.3333333333333334259, 0.3333333333333334259, 0.3333333333333334259, 0.3333333333333333703, 0.3333333333333334814, 0.3333333333333333703, 0.3333333333333334814, 0.3333333333333334814, 0.3333333333333333703, 0.3333333333333334259, 0.3333333333333334259, 0.3333333333333334814, 0.3333333333333333703, 0.3333333333333333703, 0.3333333333333334259, 0.3333333333333334259, 0.3333333333333333703, 0.3333333333333334259, 0.3333333333333333703, 0.3333333333333334259, 0.3333333333333334259, 0.3333333333333333703, 0.3333333333333335924, 0.3333333333333332593, 0.3333333333333335369, 0.3333333333333334259, 0.3333333333333333703, 0.3333333333333333148, 0.3333333333333335924, 0.3333333333333333148, 0.3333333333333333703, 0.3333333333333334259, 0.3333333333333334814, 0.3333333333333335369, 0.3333333333333333703, 0.3333333333333334259, 0.3333333333333333703, 0.3333333333333335369, 0.3333333333333333703, 0.3333333333333334259, 0.3333333333333334814, 0.3333333333333333703, 0.3333333333333335369, 0.3333333333333333148, 0.3333333333333335369, 0.3333333333333334259, 0.3333333333333334259, 0.3333333333333333703, 0.3333333333333335369, 0.3333333333333333703, 0.3333333333333335369, 0.3333333333333334814, 0.3333333333333333703, 0.3333333333333334814, 0.3333333333333333703, 0.3333333333333333703, 0.3333333333333335369, 0.3333333333333333703, 0.3333333333333334259, 0.3333333333333334814, 0.3333333333333333703, 0.3333333333333334259, 0.3333333333333333148, 0.3333333333333335369, 0.3333333333333334259, 0.3333333333333333703, 0.3333333333333334814, 0.3333333333333334259, 0.3333333333333334814, 0.3333333333333334259, 0.3333333333333333703, 0.3333333333333333703, 0.3333333333333334259, 0.3333333333333334259, 0.3333333333333334259, 0.3333333333333334259, 0.3333333333333333703, 0.3333333333333334814, 0.3333333333333334814, 0.3333333333333333703, 0.3333333333333335369, 0.3333333333333333703, 0.3333333333333334814, 0.3333333333333334814, 0.3333333333333335369, 0.3333333333333333148, 0.3333333333333335369, 0.3333333333333333703, 0.3333333333333333148, 0.3333333333333334814, 0.3333333333333333703, 0.3333333333333334814, 0.3333333333333333703, 0.3333333333333334814, 0.3333333333333333703, 0.3333333333333335369, 0.3333333333333333703, 0.3333333333333334814, 0.3333333333333334259, 0.3333333333333334814, 0.3333333333333334259, 0.3333333333333333703, 0.3333333333333333703, 0.3333333333333334814, 0.3333333333333334259, 0.3333333333333334814, 0.3333333333333334259, 0.3333333333333334259, 0.3333333333333334259, 0.3333333333333333703, 0.3333333333333334259, 0.3333333333333333703, 0.3333333333333334814, 0.3333333333333333148, 0.3333333333333335369, 0.3333333333333333703, 0.3333333333333334814, 0.3333333333333333703, 0.3333333333333335369, 0.3333333333333334259, 0.3333333333333334259, 0.3333333333333334259, 0.3333333333333334259, 0.3333333333333334259, 0.3333333333333334259),
 ( 1.000000000000000222, 1.000000000000000222, 1.000000000000000222, 1.000000000000000222, 1.000000000000000444, 1.000000000000000000, 1.000000000000000666, 0.9999999999999997780, 1.000000000000000444, 1.000000000000000000, 1.000000000000000444, 1.000000000000000444, 1.000000000000000000, 1.000000000000000444, 1.000000000000000000, 1.000000000000000444, 1.000000000000000222, 1.000000000000000222, 1.000000000000000222, 1.000000000000000444, 1.000000000000000444, 1.000000000000000000, 1.000000000000000444, 1.000000000000000000, 1.000000000000000222, 1.000000000000000222, 1.000000000000000444, 1.000000000000000222, 1.000000000000000222, 1.000000000000000444, 1.000000000000000444, 1.000000000000000444, 1.000000000000000000, 1.000000000000000444, 1.000000000000000444, 1.000000000000000000, 1.000000000000000444, 1.000000000000000444, 1.000000000000000000, 1.000000000000000444, 1.000000000000000444, 1.000000000000000000, 1.000000000000000222, 1.000000000000000444, 1.000000000000000222, 1.000000000000000222, 1.000000000000000000, 1.000000000000000444, 1.000000000000000222, 1.000000000000000222, 1.000000000000000222, 1.000000000000000222, 1.000000000000000222, 1.000000000000000222, 1.000000000000000444, 1.000000000000000000, 1.000000000000000444, 0.9999999999999997780, 1.000000000000000666, 1.000000000000000444, 1.000000000000000444, 1.000000000000000000, 1.000000000000000444, 1.000000000000000222, 1.000000000000000222, 1.000000000000000444, 1.000000000000000222, 1.000000000000000444, 1.000000000000000000, 1.000000000000000444, 1.000000000000000222, 1.000000000000000444, 1.000000000000000444, 1.000000000000000222, 1.000000000000000222, 1.000000000000000222, 1.000000000000000444, 0.9999999999999997780, 1.000000000000000444, 1.000000000000000000, 1.000000000000000444, 1.000000000000000000, 1.000000000000000444, 0.9999999999999997780, 1.000000000000000444, 0.9999999999999997780, 1.000000000000000444, 1.000000000000000222, 1.000000000000000444, 1.000000000000000000, 1.000000000000000222, 1.000000000000000444, 1.000000000000000444, 1.000000000000000222, 1.000000000000000444, 1.000000000000000444, 1.000000000000000222, 1.000000000000000222, 1.000000000000000222, 1.000000000000000222, 1.000000000000000000, 1.000000000000000222, 1.000000000000000222, 1.000000000000000222, 1.000000000000000444, 1.000000000000000000, 1.000000000000000444, 0.9999999999999997780, 1.000000000000000666, 1.000000000000000222, 1.000000000000000444, 1.000000000000000000, 1.000000000000000444, 1.000000000000000222, 1.000000000000000222, 1.000000000000000444, 1.000000000000000000, 1.000000000000000000, 1.000000000000000444, 1.000000000000000000, 1.000000000000000444, 1.000000000000000000, 1.000000000000000444, 1.000000000000000222, 1.000000000000000444, 1.000000000000000222, 1.000000000000000444, 1.000000000000000222, 1.000000000000000444, 1.000000000000000000, 1.000000000000000444, 1.000000000000000222, 1.000000000000000444, 1.000000000000000000, 1.000000000000000444, 1.000000000000000000, 1.000000000000000444, 1.000000000000000000, 1.000000000000000444, 1.000000000000000222, 1.000000000000000444, 1.000000000000000222, 1.000000000000000444, 0.9999999999999997780, 1.000000000000000444, 1.000000000000000000, 1.000000000000000444, 1.000000000000000222, 1.000000000000000222, 1.000000000000000222, 1.000000000000000222, 1.000000000000000444, 0.9999999999999997780, 1.000000000000000444, 1.000000000000000000, 1.000000000000000000, 1.000000000000000222, 1.000000000000000222, 1.000000000000000666, 0.9999999999999997780, 1.000000000000000000, 1.000000000000000444, 1.000000000000000222, 1.000000000000000444, 1.000000000000000000, 1.000000000000000222, 1.000000000000000444, 1.000000000000000222, 1.000000000000000000, 1.000000000000000444, 1.000000000000000222, 1.000000000000000222, 1.000000000000000444, 1.000000000000000222, 1.000000000000000000, 1.000000000000000444, 1.000000000000000000, 1.000000000000000444, 1.000000000000000222, 1.000000000000000222, 1.000000000000000444, 0.9999999999999997780, 1.000000000000000444, 0.9999999999999997780, 1.000000000000000444, 1.000000000000000222, 1.000000000000000444, 1.000000000000000222, 1.000000000000000222, 1.000000000000000444, 1.000000000000000000, 1.000000000000000222, 1.000000000000000444, 1.000000000000000000, 1.000000000000000444, 1.000000000000000000, 1.000000000000000222, 1.000000000000000444, 1.000000000000000000, 1.000000000000000444, 0.9999999999999997780, 1.000000000000000444, 1.000000000000000222, 1.000000000000000444, 1.000000000000000000, 1.000000000000000000, 1.000000000000000444, 1.000000000000000000, 1.000000000000000222, 1.000000000000000444, 1.000000000000000222, 1.000000000000000444, 1.000000000000000222, 1.000000000000000444, 1.000000000000000444, 1.000000000000000444, 1.000000000000000000, 1.000000000000000444, 1.000000000000000222, 1.000000000000000444, 1.000000000000000222, 1.000000000000000000, 1.000000000000000222, 1.000000000000000444, 1.000000000000000222, 1.000000000000000444, 1.000000000000000000, 1.000000000000000222, 1.000000000000000000, 1.000000000000000444, 1.000000000000000000, 1.000000000000000444, 1.000000000000000444, 1.000000000000000444, 1.000000000000000444, 1.000000000000000000, 1.000000000000000222, 1.000000000000000444, 1.000000000000000000, 1.000000000000000444, 1.000000000000000444, 1.000000000000000444, 1.000000000000000222, 1.000000000000000222, 1.000000000000000222, 0.9999999999999997780, 1.000000000000000444, 1.000000000000000222, 1.000000000000000222, 1.000000000000000000, 1.000000000000000444, 1.000000000000000000, 1.000000000000000444, 1.000000000000000000, 1.000000000000000000, 1.000000000000000666, 1.000000000000000000, 1.000000000000000444, 1.000000000000000000, 1.000000000000000444, 1.000000000000000222, 0.9999999999999997780, 1.000000000000000444, 1.000000000000000000, 1.000000000000000444, 1.000000000000000222, 1.000000000000000444, 1.000000000000000222, 1.000000000000000222, 1.000000000000000444, 1.000000000000000000, 1.000000000000000222, 1.000000000000000444, 1.000000000000000222, 1.000000000000000000, 1.000000000000000444, 0.9999999999999997780, 1.000000000000000444, 1.000000000000000222, 1.000000000000000222, 1.000000000000000222, 1.000000000000000000, 1.000000000000000444, 1.000000000000000222, 1.000000000000000666, 0.9999999999999997780, 1.000000000000000444, 1.000000000000000222, 1.000000000000000000, 1.000000000000000222, 1.000000000000000444, 1.000000000000000222, 1.000000000000000000, 1.000000000000000444, 1.000000000000000222, 1.000000000000000444, 1.000000000000000000, 1.000000000000000444, 1.000000000000000222, 1.000000000000000444, 1.000000000000000222, 1.000000000000000222, 1.000000000000000444, 1.000000000000000222, 1.000000000000000444, 1.000000000000000000, 1.000000000000000444, 1.000000000000000222, 1.000000000000000222, 1.000000000000000000, 1.000000000000000666, 0.9999999999999997780, 1.000000000000000444, 1.000000000000000222, 1.000000000000000444, 1.000000000000000222, 1.000000000000000444, 1.000000000000000000, 1.000000000000000444, 1.000000000000000222, 1.000000000000000222, 1.000000000000000444, 1.000000000000000222, 1.000000000000000444, 1.000000000000000000, 1.000000000000000444, 1.000000000000000444, 0.9999999999999997780, 1.000000000000000444, 1.000000000000000000, 1.000000000000000444, 1.000000000000000444, 1.000000000000000222, 1.000000000000000000, 1.000000000000000444, 1.000000000000000222, 1.000000000000000444, 1.000000000000000000, 1.000000000000000444, 1.000000000000000222, 1.000000000000000444, 1.000000000000000222, 1.000000000000000444, 1.000000000000000222, 1.000000000000000222, 1.000000000000000444, 1.000000000000000444, 1.000000000000000000, 1.000000000000000444, 0.9999999999999997780, 1.000000000000000444, 1.000000000000000222, 1.000000000000000222, 1.000000000000000222, 1.000000000000000444, 1.000000000000000222, 1.000000000000000222, 1.000000000000000444, 1.000000000000000000, 1.000000000000000444, 1.000000000000000000, 1.000000000000000444, 1.000000000000000222, 1.000000000000000000, 1.000000000000000222, 1.000000000000000444, 1.000000000000000000, 1.000000000000000444, 1.000000000000000000, 1.000000000000000444, 1.000000000000000444, 1.000000000000000000, 1.000000000000000444, 1.000000000000000000, 1.000000000000000444, 1.000000000000000000, 1.000000000000000444, 1.000000000000000000, 1.000000000000000444, 1.000000000000000000, 1.000000000000000444, 1.000000000000000000, 1.000000000000000444, 1.000000000000000222, 1.000000000000000222, 1.000000000000000222, 1.000000000000000222) ) ) 
 REPRESENTATION_ITEM ( '' )  SURFACE ( )  );
#176950=CARTESIAN_POINT ( 'NONE',  ( 3.796581652666820350, 1.495729193744433028, -1.498731062137735437 ) ) ;
#176954=CARTESIAN_POINT ( 'NONE',  ( 0.5495732465782035003, 1.455460699200894270, 1.326940832280040450 ) ) ;
#176959=CARTESIAN_POINT ( 'NONE',  ( 3.205313226950608385, -0.4470181708258395004, 2.248096707283386841 ) ) ;
#176960=CARTESIAN_POINT ( 'NONE',  ( 0.8733498553583609603, 1.760202786292342170, -0.4843115980177821744 ) ) ;
#176961=CARTESIAN_POINT ( 'NONE',  ( 3.463059065379545221, -1.560675823418774533, 1.104941681961457256 ) ) ;
#176965=CARTESIAN_POINT ( 'NONE',  ( 2.056891478215248981, 0.4451058530966587323, 1.963224067645082949 ) ) ;
#176966=CARTESIAN_POINT ( 'NONE',  ( 2.606241817087478374, 1.961221450604538008, 0.05310280016677935283 ) ) ;
#176970=CARTESIAN_POINT ( 'NONE',  ( 5.578101482107681974, -2.039469400243614672, -0.4589526871568836430 ) ) ;
#176971=CARTESIAN_POINT ( 'NONE',  ( 3.115802406598367824, -0.8709184464271730874, -1.540630773470308190 ) ) ;
#176974=CARTESIAN_POINT ( 'NONE',  ( 6.070342170859510667, -2.174803699615239783, -0.7246130948556377405 ) ) ;
#176975=CARTESIAN_POINT ( 'NONE',  ( 3.907932343763017347, 1.228949333998660798, -1.232512660115521408 ) ) ;
#176978=CARTESIAN_POINT ( 'NONE',  ( 3.883936887208380373, -0.1284340723075507729, 1.729154583330833272 ) ) ;
#176979=CARTESIAN_POINT ( 'NONE',  ( 4.703694880604158968, -1.675542544088706620, -1.380765677988102791 ) ) ;
#176981=CARTESIAN_POINT ( 'NONE',  ( 6.298064597363540074, -0.9548514761729166578, -1.776169100128288658 ) ) ;
#176982=CARTESIAN_POINT ( 'NONE',  ( 5.593750000000004441, -1.895863743164200921, -0.7852924748296893354 ) ) ;
#176984=CARTESIAN_POINT ( 'NONE',  ( 2.907156789938716290, 1.626457378340099069, 1.032021673995666911 ) ) ;
#176986=CARTESIAN_POINT ( 'NONE',  ( 0.2588218971089132348, 2.215798623493638875, 0.1571155685827912152 ) ) ;
#176988=CARTESIAN_POINT ( 'NONE',  ( -0.1409997244346088141, 1.357410162930408504, -2.254437325861287533 ) ) ;
#176991=CARTESIAN_POINT ( 'NONE',  ( 2.491161192834326688, -2.126536535197431022, -0.6419364700022185399 ) ) ;
#176997=CARTESIAN_POINT ( 'NONE',  ( 0.8619541869999207684, -0.05229984143813663777, -2.015912905633105101 ) ) ;
#176999=CARTESIAN_POINT ( 'NONE',  ( 5.881316448893678661, -0.05433346072863074611, 2.062130925675903725 ) ) ;
#177004=CARTESIAN_POINT ( 'NONE',  ( 0.2273421782777407807, -1.081390543313685226, -1.401283913643845969 ) ) ;
#177005=CARTESIAN_POINT ( 'NONE',  ( 5.590364566445758854, -0.4131642248683431440, 1.684076740667529881 ) ) ;
#177006=CARTESIAN_POINT ( 'NONE',  ( 5.917484386527373630, -0.9743193633129590969, -1.441955756940280997 ) ) ;
#177007=CARTESIAN_POINT ( 'NONE',  ( 3.474455725741688372, -2.209678783342132746, -0.6099929035564675139 ) ) ;
#177009=CARTESIAN_POINT ( 'NONE',  ( 2.325889007780062023, 1.785771638016835361, 0.4476198290149570602 ) ) ;
#177013=CARTESIAN_POINT ( 'NONE',  ( 2.168725436055967570, -1.667931858681595880, -0.7425449061374129744 ) ) ;
#177014=CARTESIAN_POINT ( 'NONE',  ( 2.373672848961404735, -0.3474683332905931232, -1.986100487175908258 ) ) ;
#177017=CARTESIAN_POINT ( 'NONE',  ( 4.172956468465331525, -1.964154803760146617, -0.7601757144085323770 ) ) ;
#177020=CARTESIAN_POINT ( 'NONE',  ( 2.928250347896840022, 1.105370970781336837, 1.750397071514836478 ) ) ;
#177023=CARTESIAN_POINT ( 'NONE',  ( 4.793665170694914046, 1.978287127071875151, -0.7638792978137476375 ) ) ;
#177024=CARTESIAN_POINT ( 'NONE',  ( 6.340460056601358474, 1.806591233369018834, 0.2625940548972791611 ) ) ;
#177031=CARTESIAN_POINT ( 'NONE',  ( 6.469000917296717112, -1.638331675554663747, 1.346054232038436105 ) ) ;
#177032=CARTESIAN_POINT ( 'NONE',  ( 1.378104160372157994, 1.254256560567709622, 1.691567388252762649 ) ) ;
#177035=CARTESIAN_POINT ( 'NONE',  ( 5.190230013454653069, 0.9586131782086585451, -1.594917819662385883 ) ) ;
#177045=CARTESIAN_POINT ( 'NONE',  ( 2.418345249890076154, 0.8361516037145629854, 1.774881043358336630 ) ) ;
#177046=CARTESIAN_POINT ( 'NONE',  ( 1.006953172832128152, 1.636353683469338183, -1.412668763314451903 ) ) ;
#177050=CARTESIAN_POINT ( 'NONE',  ( 2.477566078851959563, 1.547001316009195548, 0.7831083592614047628 ) ) ;
#177051=CARTESIAN_POINT ( 'NONE',  ( 2.378492463385312394, 1.591508763844831531, -0.7045900751257595518 ) ) ;
#177054=CARTESIAN_POINT ( 'NONE',  ( 1.018907413236518789, 2.013924516646655949, -0.09611688112247382398 ) ) ;
#177055=CARTESIAN_POINT ( 'NONE',  ( 6.825078400183550720, 7.629137130509051623, 2.644348168701659674 ) ) ;
#177057=CARTESIAN_POINT ( 'NONE',  ( 1.428526753364509627, 1.899469058273341338, 0.5276583995704342556 ) ) ;
#177058=CARTESIAN_POINT ( 'NONE',  ( 5.467032840998240495, -1.503656711810175350, 1.181500457595338505 ) ) ;
#177064=CARTESIAN_POINT ( 'NONE',  ( 1.611979286579327431, -0.6784349324776539625, 1.902464779174169562 ) ) ;
#177066=CARTESIAN_POINT ( 'NONE',  ( 4.296143005555221883, -0.8870401112092487494, 2.130475988740585080 ) ) ;
#177067=CARTESIAN_POINT ( 'NONE',  ( 5.652778587040098834, -0.4750822840141955550, -1.903360745478323679 ) ) ;
#177068=CARTESIAN_POINT ( 'NONE',  ( 2.975390029205774223, -0.1970676810524821243, 1.951864085487287959 ) ) ;
#177072=CARTESIAN_POINT ( 'NONE',  ( 1.640021805331920213, 2.111262888970814267, -0.1616085204505824935 ) ) ;
#177075=CARTESIAN_POINT ( 'NONE',  ( 2.255570300226293234, 0.7868700230135963203, 1.664660379391752043 ) ) ;
#177078=CARTESIAN_POINT ( 'NONE',  ( 2.760144723603759065, 0.7592700852765141839, -1.980205354017528840 ) ) ;
#177082=CARTESIAN_POINT ( 'NONE',  ( 3.391920509712963661, -0.8384013316644415292, 1.882726026762149285 ) ) ;
#177084=CARTESIAN_POINT ( 'NONE',  ( 0.1867156058280826092, 1.363667594142993877, 1.237386390646778578 ) ) ;
#177086=CARTESIAN_POINT ( 'NONE',  ( -0.02224634325196857970, 6.946779003630102700, -2.884187630258818302 ) ) ;
#177089=CARTESIAN_POINT ( 'NONE',  ( 0.1181803206181560040, -2.163391993613572151, 0.4351206515559591370 ) ) ;
#177090=CARTESIAN_POINT ( 'NONE',  ( 2.302381833152538082, -2.261912932826372735, 0.05377845686085034466 ) ) ;
#177093=CARTESIAN_POINT ( 'NONE',  ( 2.847713089995526303, -1.219902489354685038, -1.339422833384727118 ) ) ;
#177094=CARTESIAN_POINT ( 'NONE',  ( 2.835059001918965649, -1.568902116443865236, -1.099054045514812117 ) ) ;
#177095=CARTESIAN_POINT ( 'NONE',  ( 4.703616579153604427, -1.598285800263723910, -1.315984976451072930 ) ) ;
#177097=CARTESIAN_POINT ( 'NONE',  ( 1.639464495141579770, -1.426599704724445861, -1.360921036830293307 ) ) ;
#177098=CARTESIAN_POINT ( 'NONE',  ( 0.2000540296341560831, -1.925883223908849251, -0.05090804828828016798 ) ) ;
#177099=CARTESIAN_POINT ( 'NONE',  ( 3.344469905398727239, 0.4532862802011444758, 1.814783984445811127 ) ) ;
#177100=CARTESIAN_POINT ( 'NONE',  ( 2.297912027771050081, 1.785232721601331507, 1.462330537539487496 ) ) ;
#177102=CARTESIAN_POINT ( 'NONE',  ( 2.998338655031260735, 1.846661096025622228, 0.2305314943511579950 ) ) ;
#177104=CARTESIAN_POINT ( 'NONE',  ( 6.707491137888100141, -1.654371308887558234, -1.231747576844913539 ) ) ;
#177108=CARTESIAN_POINT ( 'NONE',  ( 6.036178822307518566, 1.040974378708346526, -1.830621892639591630 ) ) ;
#177110=CARTESIAN_POINT ( 'NONE',  ( 6.116527240895272222, 1.456737685447502262, -1.597155580871166602 ) ) ;
#177111=CARTESIAN_POINT ( 'NONE',  ( 6.322916996384010169, 1.495059732148263487, -1.358068445443241457 ) ) ;
#177118=CARTESIAN_POINT ( 'NONE',  ( 4.733611406029458735, 0.6279933214467496860, -1.916352419866963697 ) ) ;
#177123=CARTESIAN_POINT ( 'NONE',  ( 5.559502693676295237, 0.4258712887980077300, -2.119171757835013548 ) ) ;
#177128=CARTESIAN_POINT ( 'NONE',  ( 0.05214973123207015254, -1.250902960675448483, 1.450897702916327248 ) ) ;
#177131=CARTESIAN_POINT ( 'NONE',  ( 1.717014342725260656, -0.2134408525867482198, 1.711538560699257916 ) ) ;
#177136=CARTESIAN_POINT ( 'NONE',  ( 0.8601951712396675997, -1.287299901140761316, 1.214705651989380852 ) ) ;
#177139=CARTESIAN_POINT ( 'NONE',  ( 3.786314268594536347, -1.089870966172037825, 1.918795532666245363 ) ) ;
#177140=CARTESIAN_POINT ( 'NONE',  ( 5.506739464099510428, 0.6230791789904217559, 2.079776831526482628 ) ) ;
#177144=CARTESIAN_POINT ( 'NONE',  ( 2.824977599723184074, 1.534285384246200090, -1.463936014953904463 ) ) ;
#177145=CARTESIAN_POINT ( 'NONE',  ( 2.706657832681820697, 1.899625987897411772, 0.6766965020792228280 ) ) ;
#177146=CARTESIAN_POINT ( 'NONE',  ( 2.847713089995526303, -1.219902489354685038, -1.339422833384727118 ) ) ;
#177150=CARTESIAN_POINT ( 'NONE',  ( 0.5670072068131201126, 0.1877032549213939472, -1.861219751863735672 ) ) ;
#177154=CARTESIAN_POINT ( 'NONE',  ( 1.639701460626964868, 1.910339084310968660, -0.1447352371885517186 ) ) ;
#177159=CARTESIAN_POINT ( 'NONE',  ( 4.803922858132807505, -1.082837210388952309, -1.700963621564715700 ) ) ;
#177160=CARTESIAN_POINT ( 'NONE',  ( 4.961884481312108797, 2.138711985806662330, -0.3135959325617638238 ) ) ;
#177163=CARTESIAN_POINT ( 'NONE',  ( 3.094099843433151253, 1.348383549611749332, 1.636666742212993686 ) ) ;
#177167=CARTESIAN_POINT ( 'NONE',  ( 4.815676612163926507, -1.933897303736350270, 0.3816649536505806184 ) ) ;
#177168=CARTESIAN_POINT ( 'NONE',  ( 6.258066496116281741, 0.7254575739856858885, -1.769658340881982816 ) ) ;
#177170=CARTESIAN_POINT ( 'NONE',  ( 6.069547426979996274, 1.461697874074740389, 1.532048495917796016 ) ) ;
#177172=CARTESIAN_POINT ( 'NONE',  ( 0.4321921490204432281, 1.190796696626210682, 1.693455153822187587 ) ) ;
#177173=CARTESIAN_POINT ( 'NONE',  ( 2.501813746025891128, -0.7434988463325925556, -1.794173334931578712 ) ) ;
#177178=CARTESIAN_POINT ( 'NONE',  ( 3.064484987736408872, -1.931880230092865025, -0.7996142226951181708 ) ) ;
#177181=CARTESIAN_POINT ( 'NONE',  ( 0.4163052458206939477, -0.6087807487058238820, -1.706225765549937545 ) ) ;
#177183=CARTESIAN_POINT ( 'NONE',  ( 5.901041445831935128, 1.806360628843254768, -1.267562117129708454 ) ) ;
#177187=CARTESIAN_POINT ( 'NONE',  ( 2.802037382575186975, -0.6933082239683820980, 2.095089865402133267 ) ) ;
#177188=CARTESIAN_POINT ( 'NONE',  ( 1.910667195161031007, -0.5113573046386342691, -1.842555643073694238 ) ) ;
#177190=CARTESIAN_POINT ( 'NONE',  ( 4.861816338261779613, -0.5554421346023461492, 1.994381909410049891 ) ) ;
#177192=CARTESIAN_POINT ( 'NONE',  ( 3.292016909520224743, -0.8776455207864016783, 1.975710135277891633 ) ) ;
#177193=CARTESIAN_POINT ( 'NONE',  ( 4.564136437409766600, -1.431273618155091576, 1.659743667367798103 ) ) ;
#177203=CARTESIAN_POINT ( 'NONE',  ( 0.2818752512256904597, 1.674885806461807958, -1.122501178855893400 ) ) ;
#177206=CARTESIAN_POINT ( 'NONE',  ( 5.049704560591026237, 1.530381825397047812, 1.394388655583590042 ) ) ;
#177207=CARTESIAN_POINT ( 'NONE',  ( 3.422408909100621344, 1.221451249705886477, -1.489789856891531761 ) ) ;
#177208=CARTESIAN_POINT ( 'NONE',  ( 6.556269899348222907, -1.302956475595556496, 1.669668561148303976 ) ) ;
#177211=CARTESIAN_POINT ( 'NONE',  ( 4.416829296269289884, -1.462161721869711384, 1.319618631580289581 ) ) ;
#177212=CARTESIAN_POINT ( 'NONE',  ( 0.7268461993804631316, 0.1648446022758827123, 2.185306563462440899 ) ) ;
#177213=CARTESIAN_POINT ( 'NONE',  ( 3.545350327189537687, -1.383302465072188792, -1.191577590537174158 ) ) ;
#177220=CARTESIAN_POINT ( 'NONE',  ( 1.839159199666509981, 0.7036077657225293658, -1.701706503975081830 ) ) ;
#177221=CARTESIAN_POINT ( 'NONE',  ( 4.588143835816930860, 1.162566388618992308, 1.643413508355499708 ) ) ;
#177222=CARTESIAN_POINT ( 'NONE',  ( 1.441203352352852463, 1.369654091668540241, 1.845602877388529572 ) ) ;
#177223=CARTESIAN_POINT ( 'NONE',  ( 4.996903459272755477, 0.3314677610860050083, 1.933379042443456486 ) ) ;
#177225=CARTESIAN_POINT ( 'NONE',  ( 0.2333690889706717397, 6.947499272388762748, -2.648434294982876303 ) ) ;
#177229=CARTESIAN_POINT ( 'NONE',  ( 1.821934285652214935, 1.201201420651318630, -1.711045060523497030 ) ) ;
#177230=CARTESIAN_POINT ( 'NONE',  ( 0.3736316133628528879, 1.073300769168658908, 1.531925686032776124 ) ) ;
#177232=CARTESIAN_POINT ( 'NONE',  ( -0.1104750535120268828, 4.084583917300320444, -2.658209514912849514 ) ) ;
#177233=CARTESIAN_POINT ( 'NONE',  ( 2.331276520414362174, 0.8190846186081652824, -1.535621120930601213 ) ) ;
#177237=CARTESIAN_POINT ( 'NONE',  ( 2.174029202910219283, -1.062355927555928226, 1.358808029953484597 ) ) ;
#177238=CARTESIAN_POINT ( 'NONE',  ( 1.681448347407452193, 1.514353137444489406, 1.584415833815432162 ) ) ;
#177239=CARTESIAN_POINT ( 'NONE',  ( 4.213639274598267370, -0.3785452818781535611, 2.174016619501429215 ) ) ;
#177242=CARTESIAN_POINT ( 'NONE',  ( 2.571331741745811250, 1.937545498039330960, 0.9797267027546376905 ) ) ;
#177243=CARTESIAN_POINT ( 'NONE',  ( 0.6799654140086827114, -1.016662149479659494, 1.516215539243186639 ) ) ;
#177244=CARTESIAN_POINT ( 'NONE',  ( 3.292305547686771305, -0.8622227623886582482, -1.934024985413025810 ) ) ;
#177246=CARTESIAN_POINT ( 'NONE',  ( 6.539320575229245591, 2.459069921018588900, 2.280790101157427419 ) ) ;
#177248=CARTESIAN_POINT ( 'NONE',  ( 3.597495906037956992, -0.6642907406799610781, 2.194031518130711067 ) ) ;
#177252=CARTESIAN_POINT ( 'NONE',  ( 6.375645204974608404, 0.3829637424261604361, -2.187886986038441339 ) ) ;
#177258=CARTESIAN_POINT ( 'NONE',  ( 3.815077410725797424, 1.076317812134291119, -1.704938119663282903 ) ) ;
#177260=CARTESIAN_POINT ( 'NONE',  ( 2.641531011850445143, 1.887532825382558066, -0.8318756707885038848 ) ) ;
#177265=CARTESIAN_POINT ( 'NONE',  ( 5.437503290160631941, 0.8905978969957989433, -2.002497223260243153 ) ) ;
#177266=CARTESIAN_POINT ( 'NONE',  ( 2.883435573726996548, -0.5880205015329244000, -1.928751729079546173 ) ) ;
#177267=CARTESIAN_POINT ( 'NONE',  ( 1.698526806778306586, 1.531337151408303621, 1.022036240780115346 ) ) ;
#177268=ADVANCED_FACE ( 'NONE', ( #25077 ), #38142, .T. ) ;
#177271=CARTESIAN_POINT ( 'NONE',  ( 5.438443955714742373, 1.798867289239113987, 0.3102399082220568816 ) ) ;
#177272=CARTESIAN_POINT ( 'NONE',  ( 5.889296118903345700, -0.7283762112263308941, -1.880435897373772258 ) ) ;
#177274=CARTESIAN_POINT ( 'NONE',  ( 5.858358025671378755, 0.9108227554960802719, 2.071263147418811013 ) ) ;
#177276=CARTESIAN_POINT ( 'NONE',  ( 0.5574226275508349371, -1.780365264567655759, -1.124781644112993417 ) ) ;
#177287=CARTESIAN_POINT ( 'NONE',  ( 1.670341986359990205, 2.114562342887704283, -0.1611296783964668855 ) ) ;
#177288=CARTESIAN_POINT ( 'NONE',  ( 2.935994361307178391, -2.139806239105252583, 0.5962572732955830901 ) ) ;
#177293=CARTESIAN_POINT ( 'NONE',  ( 3.894932841003693191, 0.2855096342280309396, 1.940843471192068570 ) ) ;
#177300=CARTESIAN_POINT ( 'NONE',  ( 3.480829117359967917, -1.421471314662653196, 1.573842340227212366 ) ) ;
#177302=CARTESIAN_POINT ( 'NONE',  ( 4.364260218091946975, 1.016419123106377276, 1.907829002176253175 ) ) ;
#177303=CARTESIAN_POINT ( 'NONE',  ( 3.632213977189250098, 0.2737156317273430894, 1.820677940640710979 ) ) ;
#177306=CARTESIAN_POINT ( 'NONE',  ( 5.296709758707953242, 1.425846067417353868, 0.9975513609157842243 ) ) ;
#177309=CARTESIAN_POINT ( 'NONE',  ( 3.309602206082487008, -0.4233974974612622066, 2.119663826602156131 ) ) ;
#177311=CARTESIAN_POINT ( 'NONE',  ( 5.167342215279058237, -0.6766115767681828430, -1.899327316215810857 ) ) ;
#177313=CARTESIAN_POINT ( 'NONE',  ( 2.852577672069932735, 0.7271573612388192442, 2.035869728763760378 ) ) ;
#177315=CARTESIAN_POINT ( 'NONE',  ( 3.778557292509187260, -1.899022758751211182, -0.5288098451153611101 ) ) ;
#177316=CARTESIAN_POINT ( 'NONE',  ( 4.915543477551369556, -1.042145293856342914, -1.638595356941417114 ) ) ;
#177326=CARTESIAN_POINT ( 'NONE',  ( 1.800138458411651765, -0.7431416638853625134, 2.077998897882806784 ) ) ;
#177328=CARTESIAN_POINT ( 'NONE',  ( 6.491066726104213203, 0.1889763263339637456, 1.952597990788194959 ) ) ;
#177332=CARTESIAN_POINT ( 'NONE',  ( 0.07479286986305369589, 1.387406912293275729, -2.112587013352088317 ) ) ;
#177333=CARTESIAN_POINT ( 'NONE',  ( 5.085823778388903982, -1.827637283562512538, -0.2220107604927607503 ) ) ;
#177343=CARTESIAN_POINT ( 'NONE',  ( 6.063760116591036642, 2.031045510622536909, -0.3477994121598385613 ) ) ;
#177345=CARTESIAN_POINT ( 'NONE',  ( 1.802945237480069407, -1.574492340324705753, 0.9918895310334940874 ) ) ;
#177346=CARTESIAN_POINT ( 'NONE',  ( 3.333393596924072444, 0.8250370302015205271, -1.646115572170883112 ) ) ;
#177352=CARTESIAN_POINT ( 'NONE',  ( 3.598431038176507002, -2.204323482753521635, -0.1086902067785888437 ) ) ;
#177353=CARTESIAN_POINT ( 'NONE',  ( 6.063815651355930036, 2.230472738441360292, -0.3779872977145922741 ) ) ;
#177355=CARTESIAN_POINT ( 'NONE',  ( 5.572461477490294968, 0.7419763400571472989, 1.652881490725614189 ) ) ;
#177356=CARTESIAN_POINT ( 'NONE',  ( 6.210162240821837543, 1.096913934394160517, -1.570407731631766390 ) ) ;
#177358=CARTESIAN_POINT ( 'NONE',  ( 6.192256348250350761, -1.861847689568534081, -0.1814220289034565448 ) ) ;
#177359=CARTESIAN_POINT ( 'NONE',  ( 5.725241913846256914, 1.688569718951500986, 0.8975008795490190261 ) ) ;
#177362=CARTESIAN_POINT ( 'NONE',  ( 0.5142528298564854605, 1.293200884458247657, -1.351890787750304135 ) ) ;
#177363=CARTESIAN_POINT ( 'NONE',  ( 1.675017921984035096, 1.752138005693338441, -0.9981273289914743829 ) ) ;
#177365=CARTESIAN_POINT ( 'NONE',  ( 3.369845833479632180, 2.054674681345913800, -0.4616683548303905926 ) ) ;
#177370=CARTESIAN_POINT ( 'NONE',  ( 2.953383392634020943, -1.779389778202213446, 0.9557246442400985087 ) ) ;
#177373=CARTESIAN_POINT ( 'NONE',  ( 3.198656860129048152, -0.6241516536032962748, -2.069545307505623821 ) ) ;
#177379=CARTESIAN_POINT ( 'NONE',  ( 1.117902646172004522, 0.4237721370383492059, -2.129260471988907000 ) ) ;
#177383=CARTESIAN_POINT ( 'NONE',  ( 2.331793494658142230, 1.030094174309360344, -1.934364310732391345 ) ) ;
#177384=CARTESIAN_POINT ( 'NONE',  ( 6.883263157960362477, -0.004191378316371896506, 2.053658919477070910 ) ) ;
#177385=CARTESIAN_POINT ( 'NONE',  ( 2.835161494786802461, 0.2760463380651246856, 2.245541603805699005 ) ) ;
#177392=CARTESIAN_POINT ( 'NONE',  ( 4.112378888775404917, 1.252788995219549895, -1.250258383314418520 ) ) ;
#177395=CARTESIAN_POINT ( 'NONE',  ( 0.7804679756576750060, -1.169858290841051307, 1.750926281551241415 ) ) ;
#177399=CARTESIAN_POINT ( 'NONE',  ( 5.941029844038744123, -1.730876725876070221, -1.034150010194856417 ) ) ;
#177402=CARTESIAN_POINT ( 'NONE',  ( 3.344469905398726794, 0.4532862802011444203, 1.814783984445810905 ) ) ;
#177403=CARTESIAN_POINT ( 'NONE',  ( 2.817306709214098870, -1.799057772339835548, -1.024303335033532658 ) ) ;
#177409=CARTESIAN_POINT ( 'NONE',  ( 6.368072262247213899, 1.106822706796772193, 1.856716078747308263 ) ) ;
#177411=CARTESIAN_POINT ( 'NONE',  ( 2.471086628630547288, 1.751123931924388089, 0.8847596551376719631 ) ) ;
#177412=CARTESIAN_POINT ( 'NONE',  ( 1.475935241056694380, 1.776738309990203213, 0.9528675108748105860 ) ) ;
#177416=CARTESIAN_POINT ( 'NONE',  ( 1.299835797595794151, -1.870726058509405210, -0.005653028302576856845 ) ) ;
#177418=CARTESIAN_POINT ( 'NONE',  ( 3.427992945418765203, -1.982693224445150060, 0.3483943456095982549 ) ) ;
#177420=CARTESIAN_POINT ( 'NONE',  ( 1.898220681748989280, -1.001352587523595128, -1.865485677531570685 ) ) ;
#177422=CARTESIAN_POINT ( 'NONE',  ( 4.211429588753928144, -1.719575573843846072, -1.152724658989822348 ) ) ;
#177424=CARTESIAN_POINT ( 'NONE',  ( 6.439408583351804438, 0.8014019654560710082, -1.931139719275380084 ) ) ;
#177426=CARTESIAN_POINT ( 'NONE',  ( 5.016531207907320322, 1.258010867292450152, -1.323153095230594989 ) ) ;
#177429=CARTESIAN_POINT ( 'NONE',  ( 6.539320575229233157, 0.001224430076711413356, 2.103502572931112091 ) ) ;
#177432=CARTESIAN_POINT ( 'NONE',  ( 5.930760676324510428, 2.125237774816424619, 0.5940772278362898007 ) ) ;
#177434=CARTESIAN_POINT ( 'NONE',  ( 5.004515039866801906, -1.898294113557968510, -0.2302225566794338651 ) ) ;
#177444=CARTESIAN_POINT ( 'NONE',  ( 5.008994926481016741, 1.626754543590884561, 0.9232732976792233925 ) ) ;
#177452=CARTESIAN_POINT ( 'NONE',  ( 1.287880319801449902, -1.245359047439015932, -1.525745898539744516 ) ) ;
#177453=CARTESIAN_POINT ( 'NONE',  ( 3.339470413395662085, 0.4871825726840799398, -1.956567533273507964 ) ) ;
#177456=CARTESIAN_POINT ( 'NONE',  ( 6.827182134110235445, 7.051404648315344303, 2.887205390314013354 ) ) ;
#177457=CARTESIAN_POINT ( 'NONE',  ( 3.486445073788289051, -0.4274320362823453290, -2.149191018322317515 ) ) ;
#177459=CARTESIAN_POINT ( 'NONE',  ( 1.993070439633041424, 1.677129747370089019, -0.9476047394562473469 ) ) ;
#177461=CARTESIAN_POINT ( 'NONE',  ( 0.1331565106231363538, 0.2470099659030860484, -1.980838409567912572 ) ) ;
#177470=CARTESIAN_POINT ( 'NONE',  ( 5.442854017605395889, -1.455216020186438364, -1.127989967910733915 ) ) ;
#177471=CARTESIAN_POINT ( 'NONE',  ( 1.594390828295478402, -1.075120693119306692, 1.701777395020438899 ) ) ;
#177472=CARTESIAN_POINT ( 'NONE',  ( 4.692867332335362462, -1.408920786844407802, -1.815866644984363232 ) ) ;
#177473=CARTESIAN_POINT ( 'NONE',  ( -0.1290005225502433017, 0.6921039065478848951, -2.255494067288220439 ) ) ;
#177474=CARTESIAN_POINT ( 'NONE',  ( 2.236936919162732629, -0.08530413586980757634, -1.859100468073461965 ) ) ;
#177476=CARTESIAN_POINT ( 'NONE',  ( 5.959226163113887864, -1.611951592244726950, 1.028742869173946861 ) ) ;
#177479=CARTESIAN_POINT ( 'NONE',  ( 4.687105897418362588, 1.550225779131916726, 1.403071992899749931 ) ) ;
#177480=CARTESIAN_POINT ( 'NONE',  ( 3.045614982896325262, 0.6747646648952825288, -1.744891315567910439 ) ) ;
#177485=CARTESIAN_POINT ( 'NONE',  ( 5.338411986983877533, 1.700291985010034201, 0.2892061366746317419 ) ) ;
#177487=CARTESIAN_POINT ( 'NONE',  ( 0.9669347054478127923, -1.691490974053434959, -0.3813910478582624441 ) ) ;
#177490=CARTESIAN_POINT ( 'NONE',  ( 6.298064597363540074, -0.9548514761729166578, -1.776169100128288658 ) ) ;
#177492=CARTESIAN_POINT ( 'NONE',  ( 5.612245307067635025, 2.168910047263863827, -0.09915484274719725544 ) ) ;
#177493=CARTESIAN_POINT ( 'NONE',  ( 4.248545464119923842, 0.4890907236730773766, 1.758887239191930796 ) ) ;
#177494=CARTESIAN_POINT ( 'NONE',  ( 2.289831844592318255, -1.277571413231039399, -1.488851726829775846 ) ) ;
#177495=CARTESIAN_POINT ( 'NONE',  ( 6.438674896094000566, -1.635394517905249145, 1.344423162301669361 ) ) ;
#177499=CARTESIAN_POINT ( 'NONE',  ( 2.649219347560148208, 0.2619616101627724736, 2.104190563435456518 ) ) ;
#177503=CARTESIAN_POINT ( 'NONE',  ( 1.024380955673375393, 1.017105081308821379, 1.803069775380027995 ) ) ;
#177506=CARTESIAN_POINT ( 'NONE',  ( 2.825082509308895151, 1.607285200359307886, -1.533455307168646975 ) ) ;
#177508=CARTESIAN_POINT ( 'NONE',  ( 0.3351808223112633933, 0.7127874033420987798, -2.185478155228081754 ) ) ;
#177510=CARTESIAN_POINT ( 'NONE',  ( 5.946154108440814490, -0.9325515945646453142, 1.839819606017919718 ) ) ;
#177513=CARTESIAN_POINT ( 'NONE',  ( 0.1329588055935396196, 0.006246367379872731426, -1.846049620084761367 ) ) ;
#177514=CARTESIAN_POINT ( 'NONE',  ( 5.056134578334451568, -1.329838508726857382, 1.273713382018211382 ) ) ;
#177516=CARTESIAN_POINT ( 'NONE',  ( -0.2104748580754201015, 5.720428293583295520, -2.697747842008205943 ) ) ;
#177517=CARTESIAN_POINT ( 'NONE',  ( 3.205755162861756435, -1.722880287277430478, 0.08319854473674663520 ) ) ;
#177518=CARTESIAN_POINT ( 'NONE',  ( 1.393767942625488532, -2.000731169080074423, 0.2516357431460446992 ) ) ;
#177519=CARTESIAN_POINT ( 'NONE',  ( 2.813438166105670657, 1.274540910030600216, -1.912834453734891804 ) ) ;
#177521=CARTESIAN_POINT ( 'NONE',  ( 2.513255990918183524, 2.019876067157271748, 1.019300669498679479 ) ) ;
#177522=CARTESIAN_POINT ( 'NONE',  ( 5.373694187740483130, 2.029982003570539817, -0.5606972681787207868 ) ) ;
#177524=CARTESIAN_POINT ( 'NONE',  ( 3.602599932655100812, 1.396742099285839256, -1.086680525292152977 ) ) ;
#177527=CARTESIAN_POINT ( 'NONE',  ( 0.2524361811976470471, 0.8832210619409311958, 2.115471854006613750 ) ) ;
#177528=CARTESIAN_POINT ( 'NONE',  ( 4.154132678086497776, -1.362845063541193946, 1.238102162693654584 ) ) ;
#177532=CARTESIAN_POINT ( 'NONE',  ( 2.514065211524143084, -0.6609878990531635745, 2.015050547854141172 ) ) ;
#177533=CARTESIAN_POINT ( 'NONE',  ( 4.295009486468337023, 1.759388067201245187, 1.306329983072423984 ) ) ;
#177539=CARTESIAN_POINT ( 'NONE',  ( 3.070836455255634423, -1.780209531678895729, -0.7368423699729318432 ) ) ;
#177542=CARTESIAN_POINT ( 'NONE',  ( 0.2467152807458715680, 1.134915856054707906, -1.909484979926486137 ) ) ;
#177552=CARTESIAN_POINT ( 'NONE',  ( 2.173056921186319546, 1.071630648972416333, 1.371277206274525096 ) ) ;
#177554=CARTESIAN_POINT ( 'NONE',  ( 0.4495626703563437299, 1.451167377975391304, 1.320406988977901985 ) ) ;
#177556=CARTESIAN_POINT ( 'NONE',  ( 5.911032513020411550, 1.904272706209766630, 1.023102869888978583 ) ) ;
#177559=CARTESIAN_POINT ( 'NONE',  ( 5.911032513020411550, 1.904272706209766630, 1.023102869888978583 ) ) ;
#177563=CARTESIAN_POINT ( 'NONE',  ( 0.7548939078372005618, -1.576849831105286537, -1.005952255950369301 ) ) ;
#177564=CARTESIAN_POINT ( 'NONE',  ( 6.591143254762334536, 0.9945565086073978600, -1.419977980273220863 ) ) ;
#177566=CARTESIAN_POINT ( 'NONE',  ( 3.122796855005858241, 0.05607861761174406934, 2.191015320347329709 ) ) ;
#177567=CARTESIAN_POINT ( 'NONE',  ( 3.645846906810937149, -1.745625206895658810, -1.509303248858377966 ) ) ;
#177568=CARTESIAN_POINT ( 'NONE',  ( 5.835248319207797074, -1.864956875241881251, 0.8770506743334179900 ) ) ;
#177569=CARTESIAN_POINT ( 'NONE',  ( 0.7615419678954943317, 0.9566914028362738520, 1.689878795569139891 ) ) ;
#177573=CARTESIAN_POINT ( 'NONE',  ( 3.709332143218791789, 1.789599998243587731, -1.137392358348317201 ) ) ;
#177575=CARTESIAN_POINT ( 'NONE',  ( 2.391250195717840477, -0.7743161457766101208, -1.862016636315230844 ) ) ;
#177577=CARTESIAN_POINT ( 'NONE',  ( 6.211994372536747022, -2.190858219723303080, 0.2640275128017176565 ) ) ;
#177583=CARTESIAN_POINT ( 'NONE',  ( 6.825078400183518745, 4.686743419949856104, 2.806861564458093650 ) ) ;
#177586=CARTESIAN_POINT ( 'NONE',  ( 4.188392892783887156, -2.038203232304033108, -0.3041262925047826249 ) ) ;
#177593=CARTESIAN_POINT ( 'NONE',  ( 4.037763967290787903, -1.932009543340426072, 0.5885129382087511685 ) ) ;
#177598=CARTESIAN_POINT ( 'NONE',  ( 2.817317228389113470, -0.2032538945386449802, 2.050847873933867138 ) ) ;
#177599=CARTESIAN_POINT ( 'NONE',  ( 2.988907892087853124, -2.013985899409028946, 0.1017507309580278629 ) ) ;
#177605=CARTESIAN_POINT ( 'NONE',  ( 3.427111092251767133, 0.9039706872599994059, 1.802141633730186543 ) ) ;
#177606=CARTESIAN_POINT ( 'NONE',  ( 2.536835285771392279, -1.364265644482412609, -1.236541980112846550 ) ) ;
#177607=CARTESIAN_POINT ( 'NONE',  ( 6.252570086353132162, 0.6882034672392455255, 2.096894461246688213 ) ) ;
#177609=CARTESIAN_POINT ( 'NONE',  ( 2.196749789412206333, -0.5742421066207163971, -2.083876772215712325 ) ) ;
#177611=CARTESIAN_POINT ( 'NONE',  ( 5.085217855557687905, 1.732777129288827656, 1.216576597717359931 ) ) ;
#177612=CARTESIAN_POINT ( 'NONE',  ( 2.882471369727876542, -0.2278316040762885242, 2.287086785078895179 ) ) ;
#177616=CARTESIAN_POINT ( 'NONE',  ( 1.234984068473435892, -1.692697435815498919, 0.7966027930108383615 ) ) ;
#177619=CARTESIAN_POINT ( 'NONE',  ( 5.155133900154169169, -1.665016652684460530, -1.055383500247959461 ) ) ;
#177623=CARTESIAN_POINT ( 'NONE',  ( 0.4873205249028254027, -0.2742316277877173691, -2.189713876267186166 ) ) ;
#177625=CARTESIAN_POINT ( 'NONE',  ( 6.039524589772497620, 1.914416561877980261, -0.7887839105886890190 ) ) ;
#177628=CARTESIAN_POINT ( 'NONE',  ( 6.639320575229255894, 6.035237531390704291, 2.698156163645454964 ) ) ;
#177629=CARTESIAN_POINT ( 'NONE',  ( 5.348493512783888626, 0.5714336785274246600, 1.886844506308351210 ) ) ;
#177630=CARTESIAN_POINT ( 'NONE',  ( -0.03470293633787284449, -1.699275230904277789, 1.268407768021381221 ) ) ;
#177632=CARTESIAN_POINT ( 'NONE',  ( 4.635575047956096206, -2.111140572116900316, 0.9323621513206108435 ) ) ;
#177633=CARTESIAN_POINT ( 'NONE',  ( 2.430602512062591369, -1.272252061732727091, 1.623331442124707591 ) ) ;
#177641=CARTESIAN_POINT ( 'NONE',  ( 4.545498338918555703, 1.941281163200560878, -0.9724488383844475115 ) ) ;
#177643=CARTESIAN_POINT ( 'NONE',  ( 4.335397732480402055, 0.7831895168094182846, -1.666506522714307437 ) ) ;
#177644=CARTESIAN_POINT ( 'NONE',  ( 6.720655732516681802, 2.481091636469245021, 2.111593894264688132 ) ) ;
#177645=CARTESIAN_POINT ( 'NONE',  ( 5.232042516939362287, 2.159042084939459816, 0.3751777721049884273 ) ) ;
#177647=CARTESIAN_POINT ( 'NONE',  ( 5.682586732044571320, -2.206005490488979426, -0.5019008842952320526 ) ) ;
#177654=CARTESIAN_POINT ( 'NONE',  ( 0.9535335928906017999, 1.768114364327963539, -0.08115213312524624523 ) ) ;
#177655=CARTESIAN_POINT ( 'NONE',  ( 4.776043607066285723, 1.990852085817075068, -0.2977186459587366496 ) ) ;
#177657=CARTESIAN_POINT ( 'NONE',  ( 3.997179113411051254, 1.780275165862042153, -1.124711807175354350 ) ) ;
#177658=CARTESIAN_POINT ( 'NONE',  ( 2.425271589312021359, -1.421058436811825754, -1.284788359014801706 ) ) ;
#177660=CARTESIAN_POINT ( 'NONE',  ( 3.455474441396837904, 1.550956523109302543, 1.213803446622195636 ) ) ;
#177661=CARTESIAN_POINT ( 'NONE',  ( 5.097918204798724595, 1.359643563815411405, 1.493766824747685185 ) ) ;
#177662=CARTESIAN_POINT ( 'NONE',  ( 1.832664747978371533, 0.1804508633567840359, 1.861920966532565336 ) ) ;
#177663=CARTESIAN_POINT ( 'NONE',  ( 5.074679841287068172, -1.625846828454122983, -0.5764380256386961721 ) ) ;
#177664=CARTESIAN_POINT ( 'NONE',  ( 1.705181254219298115, 1.662258477346746588, -0.9455041445245655485 ) ) ;
#177666=CARTESIAN_POINT ( 'NONE',  ( 0.9091299924109221831, 1.668792687453458878, -1.444214864661397035 ) ) ;
#177672=CARTESIAN_POINT ( 'NONE',  ( 0.4849360239999983557, 1.980737741294085419, 0.6024896509310638804 ) ) ;
#177677=CARTESIAN_POINT ( 'NONE',  ( 6.375647721065083928, 0.3630326626483972308, -2.089014862189771726 ) ) ;
#177682=CARTESIAN_POINT ( 'NONE',  ( 4.675157572021750418, -0.8594996001172333644, -1.823839583407538267 ) ) ;
#177683=CARTESIAN_POINT ( 'NONE',  ( 4.715990674440117658, 0.9792849278024118309, -1.646335200727979897 ) ) ;
#177685=CARTESIAN_POINT ( 'NONE',  ( 2.331793494658142230, 1.030094174309360344, -1.934364310732391345 ) ) ;
#177688=CARTESIAN_POINT ( 'NONE',  ( 5.203390118303760303, 1.773417465902687562, -0.9529421280250712778 ) ) ;
#177691=CARTESIAN_POINT ( 'NONE',  ( 5.536746206892352085, -1.668647081869235826, 1.303048207008510317 ) ) ;
#177693=CARTESIAN_POINT ( 'NONE',  ( 3.808215996505484036, 1.477046120823837683, -1.479981065426434483 ) ) ;
#177695=CARTESIAN_POINT ( 'NONE',  ( 1.430204257492089903, 1.660765249891223316, 0.4652242431656942179 ) ) ;
#177697=CARTESIAN_POINT ( 'NONE',  ( 4.763993809689464065, 0.6627061821620899851, -2.014485251161435286 ) ) ;
#177707=CARTESIAN_POINT ( 'NONE',  ( 1.699580558467077118, 1.249458034614457702, 1.311817296177042902 ) ) ;
#177714=CARTESIAN_POINT ( 'NONE',  ( 2.560951022220711248, -1.505102882618135629, 1.007669420338821675 ) ) ;
#177715=CARTESIAN_POINT ( 'NONE',  ( 6.639320575229255894, 7.053084031878349869, 2.494893166485531388 ) ) ;
#177719=CARTESIAN_POINT ( 'NONE',  ( 4.562867621930529971, 1.439169320343157921, -1.179982364782502069 ) ) ;
#177720=CARTESIAN_POINT ( 'NONE',  ( 1.774859612008858667, 1.665787454739732221, -0.9457685036825744795 ) ) ;
#177721=CARTESIAN_POINT ( 'NONE',  ( 6.299827777084090918, -0.6482784301091691903, 1.814149458844191320 ) ) ;
#177727=CARTESIAN_POINT ( 'NONE',  ( 5.875830846898042914, -1.922239612846994294, 0.4278824943488717114 ) ) ;
#177730=CARTESIAN_POINT ( 'NONE',  ( 0.4454078864507329816, 0.6539998520847762897, -1.985780399853773526 ) ) ;
#177731=CARTESIAN_POINT ( 'NONE',  ( 5.895520149318425496, 1.459072380863110530, 1.257889585189754023 ) ) ;
#177733=CARTESIAN_POINT ( 'NONE',  ( 0.8151338971811080691, -0.2727355552937099636, 1.804975678908596226 ) ) ;
#177734=CARTESIAN_POINT ( 'NONE',  ( 1.840723031453334935, 2.183200880077686978, 0.3216222850719457349 ) ) ;
#177735=CARTESIAN_POINT ( 'NONE',  ( 0.1758378621803426134, 1.891278220088285833, -0.2826890867150752551 ) ) ;
#177737=CARTESIAN_POINT ( 'NONE',  ( 0.3265233526151562482, -1.289390354768883862, 1.488895225407897538 ) ) ;
#177738=CARTESIAN_POINT ( 'NONE',  ( 2.507286712376335824, -1.920573583173491139, 0.2874136252781610001 ) ) ;
#177740=CARTESIAN_POINT ( 'NONE',  ( 0.5970295589228531430, 1.038836743281198238, -1.727736137786803461 ) ) ;
#177742=CARTESIAN_POINT ( 'NONE',  ( 5.207777014082533462, 0.5861155943000575519, -1.766266804033526094 ) ) ;
#177745=CARTESIAN_POINT ( 'NONE',  ( 6.509000000000038533, 4.695815278351551214, 2.562658139094180942 ) ) ;
#177748=CARTESIAN_POINT ( 'NONE',  ( 1.628746693258641853, 0.2190750365392846177, 2.180598679842937759 ) ) ;
#177752=CARTESIAN_POINT ( 'NONE',  ( 3.281694405262673087, 1.158851912627656189, 1.410738560442346801 ) ) ;
#177756=CARTESIAN_POINT ( 'NONE',  ( 6.609000000000047947, 7.629137130509099585, 2.699999999999993516 ) ) ;
#177758=CARTESIAN_POINT ( 'NONE',  ( 0.7504602152685091454, 0.5580118324238073635, 1.843911685078497120 ) ) ;
#177759=CARTESIAN_POINT ( 'NONE',  ( 5.823093080589802462, -1.771997608643091304, -0.8420800316405114838 ) ) ;
#177762=CARTESIAN_POINT ( 'NONE',  ( 4.862908538974716421, 0.2148362657848035262, -2.180980218048253150 ) ) ;
#177766=CARTESIAN_POINT ( 'NONE',  ( 3.977443466873982203, -0.1572589350618114057, 2.064370724987254047 ) ) ;
#177771=CARTESIAN_POINT ( 'NONE',  ( 3.815287691547566418, 1.229174737571071541, -1.942296044024049761 ) ) ;
#177778=CARTESIAN_POINT ( 'NONE',  ( 4.294824717068760123, 1.560567246164183519, 1.155581451937383930 ) ) ;
#177782=CARTESIAN_POINT ( 'NONE',  ( 4.781465250580236415, 0.1816826923375300662, -1.903719681147630016 ) ) ;
#177784=CARTESIAN_POINT ( 'NONE',  ( 5.790025292147505276, -0.7713913475298206368, 1.542752225890047679 ) ) ;
#177785=CARTESIAN_POINT ( 'NONE',  ( 4.276577519141481432, -0.4465006364167342645, -1.966305148836451577 ) ) ;
#177787=CARTESIAN_POINT ( 'NONE',  ( 1.577102763248950046, -2.096353118739826993, -0.6898709473643764856 ) ) ;
#177790=CARTESIAN_POINT ( 'NONE',  ( 2.027394857466585432, -1.366561296588153063, -1.582253647643002914 ) ) ;
#177791=CARTESIAN_POINT ( 'NONE',  ( 0.5668360377511200143, 0.1796360565177144708, -1.760708420565498589 ) ) ;
#177792=CARTESIAN_POINT ( 'NONE',  ( 5.379529795981254914, -0.4926393568372189335, -1.955173248319847845 ) ) ;
#177794=CARTESIAN_POINT ( 'NONE',  ( 3.117397163603967680, -2.209095822378583929, 0.6116082133489489925 ) ) ;
#177795=CARTESIAN_POINT ( 'NONE',  ( 1.604977476713872697, -1.727474156022209328, 0.2105546776469246206 ) ) ;
#177797=CARTESIAN_POINT ( 'NONE',  ( 1.264529683829066498, -1.734034291683920426, -0.006956266631255938158 ) ) ;
#177800=CARTESIAN_POINT ( 'NONE',  ( 1.750661792711872611, -2.160631921778751519, -0.2139166996905516871 ) ) ;
#177801=CARTESIAN_POINT ( 'NONE',  ( 1.850796360583713884, -1.845628094615419768, -0.8128149310912060610 ) ) ;
#177802=CARTESIAN_POINT ( 'NONE',  ( 4.656250000000003553, -1.895863743163975101, 0.7852924748302414493 ) ) ;
#177805=CARTESIAN_POINT ( 'NONE',  ( 0.1473221176215748218, -1.486828977120215001, -1.224531343831699592 ) ) ;
#177807=CARTESIAN_POINT ( 'NONE',  ( 3.621504738650199950, 1.906737781736141280, 1.139490138724685853 ) ) ;
#177813=CARTESIAN_POINT ( 'NONE',  ( 5.548340067360077121, -1.366870494764490296, 1.077293122972399431 ) ) ;
#177814=CARTESIAN_POINT ( 'NONE',  ( 3.982823771651412770, 1.862158852298421152, 0.6176278068941787325 ) ) ;
#177818=CARTESIAN_POINT ( 'NONE',  ( 4.235799883310053637, -1.556133899351975103, -1.642472060615452589 ) ) ;
#177819=CARTESIAN_POINT ( 'NONE',  ( 1.750508186522087062, -2.052535545683041196, -0.2044793282457678107 ) ) ;
#177821=CARTESIAN_POINT ( 'NONE',  ( 2.167197484064213420, -2.068651741926224474, -0.9167319039211866416 ) ) ;
#177824=CARTESIAN_POINT ( 'NONE',  ( 3.919104170388473030, -0.1403237101727794756, 1.865361397874479632 ) ) ;
#177825=CARTESIAN_POINT ( 'NONE',  ( 2.830371795882984820, 0.6218406304432465559, -1.619021885657184745 ) ) ;
#177826=CARTESIAN_POINT ( 'NONE',  ( 6.093348126157794198, -0.7399906200981146709, 2.062998119606203939 ) ) ;
#177827=CARTESIAN_POINT ( 'NONE',  ( 0.2884678563945877738, -1.037960011796670523, 1.947446179978419512 ) ) ;
#177828=CARTESIAN_POINT ( 'NONE',  ( 4.012696165952275962, 1.530467462299599513, -1.526897427004340280 ) ) ;
#177829=CARTESIAN_POINT ( 'NONE',  ( 4.787022420419578594, 1.440143517293355879, 1.302930595787118895 ) ) ;
#177839=CARTESIAN_POINT ( 'NONE',  ( 5.309220276109914316, 1.198862193007979471, -1.621181151826488254 ) ) ;
#177844=CARTESIAN_POINT ( 'NONE',  ( 2.789462663364688844, 1.291185895303394116, 1.290987730777813702 ) ) ;
#177845=CARTESIAN_POINT ( 'NONE',  ( 2.098912041516465266, -0.5885267676426220174, -2.126790307141281033 ) ) ;
#177851=CARTESIAN_POINT ( 'NONE',  ( 0.9143263792395848188, -2.019972748253701322, 0.004280675582559247648 ) ) ;
#177852=CARTESIAN_POINT ( 'NONE',  ( 1.260569961473339440, 2.118219532560499996, 0.1004958096475216667 ) ) ;
#177854=CARTESIAN_POINT ( 'NONE',  ( 1.990827601993300666, 0.1760917813397035736, 1.852568099299256366 ) ) ;
#177856=CARTESIAN_POINT ( 'NONE',  ( 6.649297902391459125, -1.653525193404258742, -1.229868563883255828 ) ) ;
#177862=CARTESIAN_POINT ( 'NONE',  ( 4.477060521952030747, -0.002618581577289170060, -1.825872481161804561 ) ) ;
#177866=CARTESIAN_POINT ( 'NONE',  ( 6.011092252151500226, 2.013677719867816851, 0.1017325769363253418 ) ) ;
#177867=CARTESIAN_POINT ( 'NONE',  ( 5.876868881424701208, 1.699447150514224125, -0.7087742222662285485 ) ) ;
#177868=CARTESIAN_POINT ( 'NONE',  ( 0.07680821025393863577, 2.892152076732486421, -2.299782885777381658 ) ) ;
#177869=CARTESIAN_POINT ( 'NONE',  ( 4.617980755673473325, -2.263821322725892315, 0.4470779566097658475 ) ) ;
#177871=CARTESIAN_POINT ( 'NONE',  ( 6.327428285124779173, -2.037722512857220725, 0.7216720553550812767 ) ) ;
#177872=CARTESIAN_POINT ( 'NONE',  ( 1.136160399770862250, 0.3804006922196729867, 1.904278901077125052 ) ) ;
#177875=CARTESIAN_POINT ( 'NONE',  ( 4.569826555773855326, 1.780639694173843823, -1.453273832002010213 ) ) ;
#177878=CARTESIAN_POINT ( 'NONE',  ( 4.293723057671197552, -0.7160966649314598476, 1.728361679364013748 ) ) ;
#177879=CARTESIAN_POINT ( 'NONE',  ( 2.355592738034977263, -1.419685808644566949, -1.281520755053264571 ) ) ;
#177882=CARTESIAN_POINT ( 'NONE',  ( 3.791807063958370971, 1.597966631936774684, 1.522356218736670153 ) ) ;
#177883=CARTESIAN_POINT ( 'NONE',  ( 6.883263157960370471, 7.053006342242538196, 2.444342378444531949 ) ) ;
#177888=CARTESIAN_POINT ( 'NONE',  ( 1.159376733683295191, 0.3886980088604417016, -1.932498344103703136 ) ) ;
#177889=CARTESIAN_POINT ( 'NONE',  ( 0.9741375256873509025, 2.223107509294399264, -0.6184994596578182735 ) ) ;
#177890=CARTESIAN_POINT ( 'NONE',  ( 2.242563829109287088, -1.923402688547710904, -0.3857071251459272543 ) ) ;
#177892=CARTESIAN_POINT ( 'NONE',  ( 4.750865691763131338, -0.4467450692671371959, -2.013472809446889666 ) ) ;
#177899=CARTESIAN_POINT ( 'NONE',  ( 1.165147980530324201, 1.645521545068162617, -1.416405498411864583 ) ) ;
#177903=CARTESIAN_POINT ( 'NONE',  ( 2.319419987651088810, -1.815478447740950685, 0.4500915571382518854 ) ) ;
#177904=CARTESIAN_POINT ( 'NONE',  ( 6.661405305706385782, 0.3767857563467743032, -2.128362917677539379 ) ) ;
#177906=PRESENTATION_STYLE_ASSIGNMENT (( #111903 ) ) ;
#177908=CARTESIAN_POINT ( 'NONE',  ( 2.613799471529183460, -0.5979904443059110841, 1.816458080996792068 ) ) ;
#177909=CARTESIAN_POINT ( 'NONE',  ( 4.697990591988738807, -1.769527177957382680, -0.04185004791794690038 ) ) ;
#177910=CARTESIAN_POINT ( 'NONE',  ( 1.998553653897700011, -1.875654816251038248, -0.3715787057524469472 ) ) ;
#177913=CARTESIAN_POINT ( 'NONE',  ( 5.483970141128155618, -1.915793143390194242, 0.004843307671191510178 ) ) ;
#177915=CARTESIAN_POINT ( 'NONE',  ( 6.619592842669682398, 0.3380432134332654881, -1.940159576567195288 ) ) ;
#177918=CARTESIAN_POINT ( 'NONE',  ( 5.453920962983416665, 1.868457504587007545, -0.09292587778651077712 ) ) ;
#177919=CARTESIAN_POINT ( 'NONE',  ( 2.244514701088017539, 0.3993153960501935051, 1.781317584591130432 ) ) ;
#177921=CARTESIAN_POINT ( 'NONE',  ( 4.336686996305870068, 2.164023489887345164, 0.4319772483800735086 ) ) ;
#177924=CARTESIAN_POINT ( 'NONE',  ( 1.873554394494097997, -0.2548139927673950256, 2.046832928722150058 ) ) ;
#177932=CARTESIAN_POINT ( 'NONE',  ( 5.002425025097493538, 2.064580399062130311, 0.1557331365308264881 ) ) ;
#177935=CARTESIAN_POINT ( 'NONE',  ( 2.214359598146302677, -1.016813397907929239, -1.907474440234188995 ) ) ;
#177937=CARTESIAN_POINT ( 'NONE',  ( 3.264323853713008816, 2.019862492602925386, -0.002211735406987268802 ) ) ;
#177944=CARTESIAN_POINT ( 'NONE',  ( 1.675017921984035096, 1.752138005693338441, -0.9981273289914743829 ) ) ;
#177945=CARTESIAN_POINT ( 'NONE',  ( 6.409741707328596938, -1.031184584194230647, -1.933826218581576439 ) ) ;
#177947=CARTESIAN_POINT ( 'NONE',  ( 4.429883728109570207, -1.874397765517330061, 0.3784635845696313061 ) ) ;
#177951=CARTESIAN_POINT ( 'NONE',  ( 1.687125285987755019, 1.678019391100945779, 1.117813378161469418 ) ) ;
#177954=CARTESIAN_POINT ( 'NONE',  ( 4.735197965344590365, -1.576124854778211626, 0.7008788178320748408 ) ) ;
#177960=CARTESIAN_POINT ( 'NONE',  ( 0.4970418144054839504, 0.3504251219754518365, 2.040211723117946629 ) ) ;
#177963=CARTESIAN_POINT ( 'NONE',  ( 5.602179418825736334, -0.8085942178241835032, 1.621059995222628780 ) ) ;
#177966=CARTESIAN_POINT ( 'NONE',  ( 6.890000000000009450, -0.01081285896028029957, 2.279840171838914298 ) ) ;
#177967=CARTESIAN_POINT ( 'NONE',  ( 6.481129863841750272, -1.659422710288318115, -0.7269172754736009656 ) ) ;
#177970=CARTESIAN_POINT ( 'NONE',  ( 2.923975034273151419, 1.216836049711809586, -1.822369523680394066 ) ) ;
#177971=ORIENTED_EDGE ( 'NONE', *, *, #133575, .T. ) ;
#177973=CARTESIAN_POINT ( 'NONE',  ( 0.6077679335219284829, 0.6189715888181289705, -1.861716921216026055 ) ) ;
#177975=CARTESIAN_POINT ( 'NONE',  ( 5.149962951811881240, 0.9480454039230011842, 1.664493911490998679 ) ) ;
#177982=CARTESIAN_POINT ( 'NONE',  ( 1.622176833581047806, -1.201014165160016356, -1.797165035535647659 ) ) ;
#177987=CARTESIAN_POINT ( 'NONE',  ( 2.063248287022978467, 0.3151258922809499485, -1.798016661460503984 ) ) ;
#177989=CARTESIAN_POINT ( 'NONE',  ( 4.559475717982610199, 0.3993622990657343941, -1.781190812766835441 ) ) ;
#177992=CARTESIAN_POINT ( 'NONE',  ( 3.842214238857721842, -0.9727578572899638898, 1.712498773813153408 ) ) ;
#177994=CARTESIAN_POINT ( 'NONE',  ( 5.847205921155025798, 0.5594960185140216424, -1.859740419532672773 ) ) ;
#177998=CARTESIAN_POINT ( 'NONE',  ( 5.396778611113259849, -2.069399493756381769, -0.4625044129713885011 ) ) ;
#178004=CARTESIAN_POINT ( 'NONE',  ( 5.320952465583661528, 1.522972439820569956, -1.316545952364375438 ) ) ;
#178006=CARTESIAN_POINT ( 'NONE',  ( 6.006453938882227561, -0.6616566355047011072, -1.701761020394356283 ) ) ;
#178007=CARTESIAN_POINT ( 'NONE',  ( 1.363825363374836286, -0.5049007678423790280, 2.007717453658082629 ) ) ;
#178010=CARTESIAN_POINT ( 'NONE',  ( 6.262560305340551636, -1.321439916381482060, 1.324322166508178356 ) ) ;
#178013=FILL_AREA_STYLE_COLOUR ( '', #162695 ) ;
#178017=CARTESIAN_POINT ( 'NONE',  ( 3.691823404346205706, 1.489760995587570358, 0.8873103889329400085 ) ) ;
#178020=CARTESIAN_POINT ( 'NONE',  ( 1.674760025662187735, 1.393346669028448392, -1.531324272915953744 ) ) ;
#178021=CARTESIAN_POINT ( 'NONE',  ( 2.320046401798322222, 0.9952771033397389555, -1.868693074688542843 ) ) ;
#178026=CARTESIAN_POINT ( 'NONE',  ( 0.6550501802922055195, 1.640498656168420943, -1.089389633329050033 ) ) ;
#178031=CARTESIAN_POINT ( 'NONE',  ( 2.607731988003787915, -2.267127051869659571, 0.3377934734241551662 ) ) ;
#178032=CARTESIAN_POINT ( 'NONE',  ( 0.7326872660318054509, 0.1314506862302306234, 1.821024990000128296 ) ) ;
#178033=CARTESIAN_POINT ( 'NONE',  ( 2.953266587970606150, -1.684550232849800544, 0.9053361341156559439 ) ) ;
#178034=EDGE_CURVE ( 'NONE', #46524, #190431, #106014, .T. ) ;
#178038=CARTESIAN_POINT ( 'NONE',  ( 1.986589674187682064, -1.235133946311824049, 1.589746892572386994 ) ) ;
#178039=CARTESIAN_POINT ( 'NONE',  ( 2.500770564479499303, 0.4249116886347775179, 1.915039037836663738 ) ) ;
#178043=CARTESIAN_POINT ( 'NONE',  ( 5.314434061427068201, 1.931386623266003078, 0.8008058956679960927 ) ) ;
#178044=CARTESIAN_POINT ( 'NONE',  ( 3.344378923012015115, 0.4290688666262321149, 1.716912437317794415 ) ) ;
#178046=CARTESIAN_POINT ( 'NONE',  ( 6.685440801012543233, -0.9854850593251741619, 2.067252628450669594 ) ) ;
#178048=CARTESIAN_POINT ( 'NONE',  ( 4.259493880088534468, 0.8231460567260719952, 1.533345966155388540 ) ) ;
#178050=CARTESIAN_POINT ( 'NONE',  ( 4.059675810253587258, 1.465203325174119664, -0.9266335502581940498 ) ) ;
#178051=CARTESIAN_POINT ( 'NONE',  ( 5.231008634329041840, -2.042658762482005841, -0.7362343983412369397 ) ) ;
#178053=CARTESIAN_POINT ( 'NONE',  ( 5.594935472981866553, 1.780666063871166882, 0.9463038388278843804 ) ) ;
#178054=CARTESIAN_POINT ( 'NONE',  ( 5.062500000000005329, -1.451031289061317064, -1.451031289060909168 ) ) ;
#178055=DIRECTION ( 'NONE',  ( 2.949029909160572061E-17, 1.000000000000000000, -8.673600428462354978E-15 ) ) ;
#178056=CARTESIAN_POINT ( 'NONE',  ( 2.766527970621732724, -1.329674337952547303, 1.394112488825666851 ) ) ;
#178058=CARTESIAN_POINT ( 'NONE',  ( 6.433822955411669930, -2.155103329387221933, 0.5382066023030105395 ) ) ;
#178060=CARTESIAN_POINT ( 'NONE',  ( 6.883263157960371359, 7.052674735402435502, 2.544342468817725855 ) ) ;
#178063=CARTESIAN_POINT ( 'NONE',  ( 3.018465837578692579, -2.218647833171137673, 0.1111532960578337226 ) ) ;
#178064=CARTESIAN_POINT ( 'NONE',  ( -0.02900071798685524560, -0.004641455105012376459, -2.173770343569726649 ) ) ;
#178069=CARTESIAN_POINT ( 'NONE',  ( 1.143204175302305670, 0.8197749522141674072, 1.842446510343001442 ) ) ;
#178071=CARTESIAN_POINT ( 'NONE',  ( 5.652800580869365099, -0.4976084531597444460, -2.001653870753268283 ) ) ;
#178077=CARTESIAN_POINT ( 'NONE',  ( 0.3152201331171593512, -1.737291786998166332, 0.3363950369540784080 ) ) ;
#178078=CARTESIAN_POINT ( 'NONE',  ( 5.520041967268690897, -1.564255855279505836, 0.7489400339724672229 ) ) ;
#178079=CARTESIAN_POINT ( 'NONE',  ( 6.110887277445514520, -0.2035749799894230883, 1.728432721540203998 ) ) ;
#178081=CARTESIAN_POINT ( 'NONE',  ( 3.316269524717931017, 1.452881069417772730, -1.773186822121583184 ) ) ;
#178083=CARTESIAN_POINT ( 'NONE',  ( 1.200829095903386046, -0.4490931065196464012, 1.785404219219708377 ) ) ;
#178086=CARTESIAN_POINT ( 'NONE',  ( 1.694096453153286497, -1.816434584207878622, -0.1825648128309723117 ) ) ;
#178087=CARTESIAN_POINT ( 'NONE',  ( 2.971327447312217984, -1.987046587055636637, -0.3419355124290662240 ) ) ;
#178088=CARTESIAN_POINT ( 'NONE',  ( 0.9025786099917804117, 1.657183926254527595, -1.434042119274607563 ) ) ;
#178090=CARTESIAN_POINT ( 'NONE',  ( 4.102637100452250607, -0.6586339671014628250, -2.000395093806975222 ) ) ;
#178094=CARTESIAN_POINT ( 'NONE',  ( 1.662640112210824306, -0.7432673875312334477, -1.932532381715674097 ) ) ;
#178097=CARTESIAN_POINT ( 'NONE',  ( 4.354221869268804390, 0.9056986662851628234, -1.917456963280273818 ) ) ;
#178098=CARTESIAN_POINT ( 'NONE',  ( 0.04732232356348483465, -1.488192626783080952, -1.223051670295220994 ) ) ;
#178106=CARTESIAN_POINT ( 'NONE',  ( -0.1575499713504755483, -1.374138184231291415, -1.746309953600865716 ) ) ;
#178107=CARTESIAN_POINT ( 'NONE',  ( 0.7101633350218137242, -2.095805943121428427, 0.2063731196077517871 ) ) ;
#178110=CARTESIAN_POINT ( 'NONE',  ( 4.821077630544555070, -1.661119493813640657, -0.8391380156763434961 ) ) ;
#178117=CARTESIAN_POINT ( 'NONE',  ( 2.488659587246494276, 1.902222718079676689, 0.4795239450603656084 ) ) ;
#178118=CARTESIAN_POINT ( 'NONE',  ( 1.059701713109785670, 0.4209238396889224965, -2.120155868012041811 ) ) ;
#178122=CARTESIAN_POINT ( 'NONE',  ( 2.442404235307413796, 1.063479746408531046, 1.369289251230455751 ) ) ;
#178123=CARTESIAN_POINT ( 'NONE',  ( 2.642201187982503363, -1.446964261146063802, 0.9666251106823405825 ) ) ;
#178126=CARTESIAN_POINT ( 'NONE',  ( 2.020846523693183627, 1.921700534952670791, 0.7446803044362272361 ) ) ;
#178127=CARTESIAN_POINT ( 'NONE',  ( 1.440779594245532369, 1.198675164295496920, 1.620935466883965503 ) ) ;
#178128=CARTESIAN_POINT ( 'NONE',  ( 6.925078400183534377, -0.01048729610059369148, 2.244148362790527429 ) ) ;
#178130=CARTESIAN_POINT ( 'NONE',  ( 1.129686040349969556, -1.248873030102001902, -1.525460987127578605 ) ) ;
#178132=CARTESIAN_POINT ( 'NONE',  ( 5.396708386617175890, -1.867154475869851504, -0.4128305108781898936 ) ) ;
#178137=CARTESIAN_POINT ( 'NONE',  ( 1.313155450441779726, 1.649776782055782709, -1.164742093282441937 ) ) ;
#178140=CARTESIAN_POINT ( 'NONE',  ( 4.489522129203258771, 2.063289974401757654, -1.033470928033096037 ) ) ;
#178141=CARTESIAN_POINT ( 'NONE',  ( 5.740667459973674447, -1.913685094937540132, -0.4313615418530327150 ) ) ;
#178142=CARTESIAN_POINT ( 'NONE',  ( 1.903102209365503894, -1.660057620245494636, 1.045011325395063251 ) ) ;
#178144=CARTESIAN_POINT ( 'NONE',  ( -0.08726289061519039436, -1.242903867559573161, -1.588418431006669351 ) ) ;
#178146=CARTESIAN_POINT ( 'NONE',  ( 1.393934723748765814, -2.100642827862955198, 0.2651745403093440090 ) ) ;
#178149=CARTESIAN_POINT ( 'NONE',  ( 0.7965151530783078915, 1.503791256141374211, 1.061989520254283281 ) ) ;
#178152=CARTESIAN_POINT ( 'NONE',  ( 2.707414796094851361, 1.816601298730673220, -1.093838055662835096 ) ) ;
#178153=B_SPLINE_CURVE_WITH_KNOTS ( 'NONE', 3,
 ( #184162, #35783, #180974, #101859, #199335, #19526, #83467, #66122, #151691, #167927, #50981, #3260, #117103, #69328, #49915, #116036, #135439, #201460, #17383, #149546, #53104, #81348, #119237, #185220, #163679, #147428, #106180, #40069, #139721, #121394, #6467, #172205, #124599, #154883, #71464, #8614, #37929, #152740, #23795, #168988, #88828, #123540, #72543, #137577, #89900, #104003, #157028, #155952, #170047, #153816, #203595, #21632, #120317, #70391, #7537, #73621, #55247, #36844, #20587, #204664, #205744, #87740, #5387, #57376, #74696, #188435, #189504, #41150, #202528, #107259, #138641, #173279, #22714, #54177, #24861, #90962, #56313, #122474, #140800, #38997, #206811, #105082, #58445, #102926, #187367, #86673, #171120, #136508, #4321, #186292, #92038, #45410, #190559, #80016, #42215, #208933, #111527, #158095, #108331, #46469, #12869, #207878, #174351, #44341, #60567, #191620, #194835, #109403, #28076, #175409, #59501, #30213, #128854, #43282, #161283, #10742, #94170, #110463, #145067, #146119, #212132, #78942, #211070, #112592, #126726, #125658, #192687, #176463, #162353, #127810, #26992, #25930, #93099, #9683, #141869, #63768, #159140, #193764, #76813, #177533, #142932, #61642, #29145, #178604, #160210, #11811, #75760, #95234, #77887, #62693, #144008, #210000, #96298, #13933, #18204, #134146, #130977, #98410, #166614, #101608, #66937, #164474, #14995, #167675, #183920, #16061, #81088, #34468, #82145, #84288, #33402, #1944, #179667, #148237, #147176, #133079, #198028, #99481, #149291, #114723, #31286, #151440, #196968, #100539, #199077, #68006, #51808, #35532, #150374, #200154, #872, #48605, #115780, #50723, #214239, #116848, #213202, #129927, #49657, #65869, #180720, #132018, #83208, #117926, #181769, #97362, #163420, #182849, #19276, #165539, #17132, #113663, #85358, #3011, #195915, #32344, #47552, #64831, #205497, #87506, #152495, #23540, #104831, #73361, #170876, #69081, #71215, #137332, #139467, #20344, #203348, #118992, #107004, #38749, #55001, #121152, #171951, #22468, #173029, #56067, #120069, #136260, #202280, #204413, #153570, #138395, #72287, #89649, #5139, #88579, #122224, #156782, #187117, #103757, #40899, #70149, #184971, #188184, #201218, #154637, #39819, #6218, #105927, #155703, #7284, #57130, #123297, #36596, #102683, #189260, #24611, #90719, #135201, #52859, #168741, #86430, #4078, #186045, #53933, #37680, #169806, #21395, #210566, #180217, #47033, #15550, #113148, #8368, #13432, #79508, #81637, #174110, #145626, #58196, #49156, #195403, #211623, #63258, #114218, #179154, #115272, #196464, #31839, #128356, #78436, #25682, #129420, #30778, #96857, #97915, #147722, #74451, #146675, #181265, #62200, #162905, #45966, #144556, #157847, #14487, #163974, #80577, #212690, #12357, #194324, #213739, #65362, #140555, #64332, #130473, #131509, #112087, #178088, #32891, #48106, #29706, #197512, #206569, #91791, #108081, #98969, #124354, #190312, #41970, #95787, #161844, #68563, #134690, #133633, #50213, #136803, #4618, #51281, #116332, #69629, #199635, #119539, #200694, #37149, #347, #117406, #52345, #135738, #83763, #167166, #38226, #16615, #53401, #186599, #166089, #201760, #19824, #103229, #86973, #70690, #185524, #169289, #184458, #17677, #150927, #36076, #20874, #85909, #118473, #165021, #66420, #18753 ),
 .UNSPECIFIED., .F., .F.,
 ( 4, 1, 1, 1, 1, 1, 1, 1, 1, 1, 1, 1, 1, 1, 1, 1, 1, 1, 1, 1, 1, 1, 1, 1, 1, 1, 1, 1, 1, 1, 1, 1, 1, 1, 1, 1, 1, 1, 1, 1, 1, 1, 1, 1, 1, 1, 1, 1, 1, 1, 1, 1, 1, 1, 1, 1, 1, 1, 1, 1, 1, 1, 1, 1, 1, 1, 1, 1, 1, 1, 1, 1, 1, 1, 1, 1, 1, 1, 1, 1, 1, 1, 1, 1, 1, 1, 1, 1, 1, 1, 1, 1, 1, 1, 1, 1, 1, 1, 1, 1, 1, 1, 1, 1, 1, 1, 1, 1, 1, 1, 1, 1, 1, 1, 1, 1, 1, 1, 1, 1, 1, 1, 1, 1, 1, 1, 1, 1, 1, 1, 1, 1, 1, 1, 1, 1, 1, 1, 1, 1, 1, 1, 1, 1, 1, 1, 1, 1, 1, 1, 1, 1, 1, 1, 1, 1, 1, 1, 1, 1, 1, 1, 1, 1, 1, 1, 1, 1, 1, 1, 1, 1, 1, 1, 1, 1, 1, 1, 1, 1, 1, 1, 1, 1, 1, 1, 1, 1, 1, 1, 1, 1, 1, 1, 1, 1, 1, 1, 1, 1, 1, 1, 1, 1, 1, 1, 1, 1, 1, 1, 1, 1, 1, 1, 1, 1, 1, 1, 1, 1, 1, 1, 1, 1, 1, 1, 1, 1, 1, 1, 1, 1, 1, 1, 1, 1, 1, 1, 1, 1, 1, 1, 1, 1, 1, 1, 1, 1, 1, 1, 1, 1, 1, 1, 1, 1, 1, 1, 1, 1, 1, 1, 1, 1, 1, 1, 1, 1, 1, 1, 1, 1, 1, 1, 1, 1, 1, 1, 1, 1, 1, 1, 1, 1, 1, 1, 1, 1, 1, 1, 1, 1, 1, 1, 1, 1, 1, 1, 1, 1, 1, 1, 1, 1, 1, 1, 1, 1, 1, 1, 1, 1, 1, 1, 1, 1, 1, 1, 1, 1, 1, 1, 1, 1, 1, 1, 1, 1, 1, 1, 1, 1, 1, 1, 1, 1, 1, 1, 1, 1, 1, 1, 1, 1, 1, 1, 1, 1, 1, 1, 1, 1, 1, 1, 1, 1, 1, 1, 1, 1, 1, 1, 1, 1, 1, 1, 1, 1, 1, 1, 1, 1, 1, 1, 1, 1, 1, 1, 1, 1, 1, 1, 1, 1, 4 ),
 ( 0.000000000000000000, 0.002599888508634240914, 0.005208754120092145765, 0.007813069968323356138, 0.01041690100177071650, 0.01302019566086259385, 0.01562517182793091500, 0.01822893254318404960, 0.02083328139698771564, 0.02343764900838959594, 0.02604139750447371365, 0.02864615928571910553, 0.03124958462592061434, 0.03385442086835698666, 0.03645794792899405279, 0.03906256697173399878, 0.04166661757251870907, 0.04427067912273281725, 0.04687528696281444140, 0.04947881815967773017, 0.05208365228821221909, 0.05468707701066444909, 0.05729184299815447134, 0.05989557646906591704, 0.06249996333325048142, 0.06510433798480201595, 0.06770807906337909798, 0.07031283757201339801, 0.07291626355048291819, 0.07552109983967189577, 0.07812462590386089201, 0.08072924387304455940, 0.08333329402460390445, 0.08593735478041557296, 0.08854196204427712547, 0.09114549249794960672, 0.09375032597506528786, 0.09635375006294695510, 0.09895851527076646170, 0.1015622481948881828, 0.1041666342325376776, 0.1067710083972730206, 0.1093747487337090180, 0.1119795066911244419, 0.1145829320296284648, 0.1171877676425944481, 0.1197912931610935483, 0.1223959103579086161, 0.1249999600491941698, 0.1276040200539713398, 0.1302086268569593308, 0.1328121566649932417, 0.1354169895755736042, 0.1380204131161003600, 0.1406251776355303407, 0.1432289101024236955, 0.1458332954032181272, 0.1484376691708411133, 0.1510414088543486633, 0.1536461663508109643, 0.1562495911381983071, 0.1588544261652600487, 0.1614579512270202244, 0.1640625677415503691, 0.1666666170620310916, 0.1692706764052687440, 0.1718752828374313091, 0.1744788120887783289, 0.1770836445231302458, 0.1796870676051354199, 0.1822918315264069888, 0.1848955636252137269, 0.1874999482789682093, 0.1901043217392619777, 0.1927080608589964439, 0.1953128179847096746, 0.1979162423098047296, 0.2005210768412587219, 0.2031246015352002054, 0.2057292174574958665, 0.2083332664966131842, 0.2109373252677763377, 0.2135419314191336626, 0.2161454602027163274, 0.2187502922511180836, 0.2213537149634070833, 0.2239584783767220588, 0.2265622101965570623, 0.2291665942930569411, 0.2317709675357785548, 0.2343747061808670040, 0.2369794630260087243, 0.2395828869776091552, 0.2421877211037245237, 0.2447912455187418734, 0.2473958609388257068, 0.2499999097859964270, 0.2526039680745227334, 0.2552085740350705789, 0.2578121024397855843, 0.2604169341924902348, 0.2630203566238439872, 0.2656251196193780695, 0.2682288512493328225, 0.2708332348783377697, 0.2734376079932215875, 0.2760413462527663842, 0.2786461029074911444, 0.2812495265743710227, 0.2838543603853929120, 0.2864578846103582599, 0.2890624996182282747, 0.2916665483628478883, 0.2942706062581511572, 0.2968752121178640513, 0.2994787402325856385, 0.3020835717798243114, 0.3046869940190023440, 0.3072917566869088346, 0.3098954882160545599, 0.3124998714673014044, 0.3151042445440625506, 0.3177079825071445485, 0.3203127390615869707, 0.3229161625325003282, 0.3255209961186533163, 0.3281245202424198926, 0.3307291349280532256, 0.3333331836594992104, 0.3359372412509727956, 0.3385418470998076690, 0.3411453750133909280, 0.3437502064453764050, 0.3463536285811206206, 0.3489583910115333087, 0.3515621225289245477, 0.3541665054921307454, 0.3567708786204680238, 0.3593746163761498691, 0.3619793729204284771, 0.3645827962841124981, 0.3671876297356038710, 0.3697911538470093351, 0.3723957683003653041, 0.3749998171080005105, 0.3776038744850206963, 0.3802084804129200468, 0.3828120082142042468, 0.3854168396211344327, 0.3880202617421720235, 0.3906250240252089334, 0.3932287556198868494, 0.3958331383847540352, 0.3984375116543538153, 0.4010412492916836102, 0.4036460059159037717, 0.4062494292610819846, 0.4088542626681055392, 0.4114577868559751161, 0.4140624011669984950, 0.4166664501401745602, 0.4192705073921035863, 0.4218751134889988097, 0.4244786412668108966, 0.4270834727388717056, 0.4296868949339185950, 0.4322916571596854274, 0.4348953889206810253, 0.4374997715768980666, 0.4401041450774376140, 0.4427078826854516369, 0.4453126394797092824, 0.4479160628950952239, 0.4505208963478340434, 0.4531244207009840763, 0.4557290349596088697, 0.4583330841876695483, 0.4609371414038593850, 0.4635417477596745495, 0.4661452756028321986, 0.4687501072302013849, 0.4713535295879656695, 0.4739582918465587991, 0.4765620238628961447, 0.4791664065001429718, 0.4817707803212932793, 0.4843745179890200370, 0.4869792750434049911, 0.4895826986177053142, 0.4921875322063354874, 0.4947910568135764908, 0.4973956711097291539, 0.4999997206820134821, 0.5026037779518089943, 0.5052083846564635605, 0.5078119126537786743, 0.5104167445266291070, 0.5130201671358142201, 0.5156249295173244152, 0.5182286618780244103, 0.5208330445859747915, 0.5234374188174044651, 0.5260411566338674128, 0.5286459140384663913, 0.5312493378603841965, 0.5338541716750782040, 0.5364576966252184720, 0.5390623110488209635, 0.5416663610546670338, 0.5442704184674093115, 0.5468750256108222407, 0.5494785538511040013, 0.5520833860596070508, 0.5546868090089153158, 0.5572915716034309019, 0.5598953043975141153, 0.5624996872658396541, 0.5651040619972180767, 0.5677078000514395040, 0.5703125578963399445, 0.5729159820545779436, 0.5755208161855079885, 0.5781243415673570363, 0.5807289562083304268, 0.5833330067370782190, 0.5859370643821081304, 0.5885416720542003821, 0.5911452006262593040, 0.5937500332605881725, 0.5963534566387238556, 0.5989582195363342132, 0.6015619528528246551, 0.6041663359711972880, 0.6067707112921981727, 0.6093744496732020899, 0.6119792080484952601, 0.6145826326317597177, 0.6171874671691013337, 0.6197909930714722293, 0.6223956080197403651, 0.6249996591607356322, 0.6276037171273963766, 0.6302083254180952387, 0.6328118544107458332, 0.6354166875610788301, 0.6380201114567515264, 0.6406248747475506988, 0.6432286086754787080, 0.6458329921335752566, 0.6484373681338796436, 0.6510411069306952792, 0.6536458659264798854, 0.6562492910234830612, 0.6588541260574176661, 0.6614576525691320263, 0.6640622679146246377, 0.6666663197572214594, 0.6692703781348633418, 0.6718749871341050950, 0.6744785166361690898, 0.6770833503926931840, 0.6796867748946214816, 0.6822915386687108397, 0.6848952732971168578, 0.6874996571846213600, 0.6901040339539210589, 0.6927077732555863010, 0.6953125329619718187, 0.6979159586614360755, 0.7005207942821553013, 0.7031243214920454010, 0.7057289373247008779, 0.7083329899582661016, 0.7109370488362486418, 0.7135416586339821121, 0.7161451887342924483, 0.7187500231872065992, 0.7213534483841206324, 0.7239582127316128712, 0.7265619481495508847, 0.7291663325561579256, 0.7317707101841592898, 0.7343744500797240171, 0.7369792105868335774, 0.7395826369774940456, 0.7421874732752028470, 0.7447910012721150608, 0.7473956176818850050, 0.7499996711958007989, 0.7526037306634962842, 0.7552083413496862851, 0.7578118721370898925, 0.7604167073766084917, 0.7630201333572542710, 0.7656248983682768516, 0.7682286346648167230, 0.7708330196802359868, 0.7734373982566630223, 0.7760411388351919904, 0.7786459002331664880, 0.7812493274037752844, 0.7838541644686951582, 0.7864576933414935134, 0.7890623104183455139, 0.7916663649020125870, 0.7942704250488100692, 0.7968750367134410650, 0.7994785682768023038, 0.8020834043931583945, 0.8046868312463003603, 0.8072915970109983963, 0.8098953342752303053, 0.8124997199891885735, 0.8151040996037859365, 0.8177078409543626636, 0.8203126033333638656, 0.8229160313726919806, 0.8255208692950642968, 0.8281243991326340259, 0.8307290169665545454, 0.8333330725093962554, 0.8359371334247044372, 0.8385417461577832077, 0.8411452785859873105, 0.8437501156694361404, 0.8463535434838604932, 0.8489583100924004144, 0.8515620484134380774, 0.8541664349156833369, 0.8567708156582201084, 0.8593745578699503174, 0.8619793213201638604, 0.8645827503170061545, 0.8671875891870957087, 0.8697911200783463581, 0.8723957387593448409, 0.8749997954508100806, 0.8776038572240605351, 0.8802084711156200614, 0.8828120044975765746, 0.8854168426383988155, 0.8880202715029178462, 0.8906250390454908406, 0.8932287785124739532, 0.8958331658927787267, 0.8984375478530519654, 0.9010412910150662480, 0.9036460556267057465, 0.9062494856698833923, 0.9088543255779816255, 0.9114578576118502751, 0.9140624772299625889, 0.9166665351595286726, 0.9192705978801787303, 0.9218752130202838568, 0.9244787474449313036, 0.9270835867334279445, 0.9296870167368762594, 0.9322917853037333558, 0.9348955260058576799, 0.9374999143539141100, 0.9401042976215825409, 0.9427080418234272674, 0.9453128076877782560, 0.9479162388645026027, 0.9505210798953250828, 0.9531246131693177359, 0.9557292338404025367, 0.9583332930514818493, 0.9609373567081632705, 0.9635419734050364449, 0.9661455093234165847, 0.9687503490003109841, 0.9713537788664922124, 0.9739585512809396661, 0.9765622998769101226, 0.9791666815729623830, 0.9817710277688282972, 0.9843747994658795797, 0.9869797739623470401, 0.9895830763955310028, 0.9921869177308453303, 0.9947912343601759133, 0.9974001139318913189, 1.000000000000000000 ),
 .UNSPECIFIED. ) ;
#178157=CARTESIAN_POINT ( 'NONE',  ( 3.180987545930415106, -0.1479678519747235910, -2.055505606019301990 ) ) ;
#178159=DIRECTION ( 'NONE',  ( 1.214306433183764966E-17, 1.000000000000000000, 5.200010849845536803E-32 ) ) ;
#178164=CARTESIAN_POINT ( 'NONE',  ( 2.548426268707996822, 2.261836392764454473, 0.05785012348054861114 ) ) ;
#178166=CARTESIAN_POINT ( 'NONE',  ( 2.074188967152798657, 0.7772732722058082189, 1.636524323399509928 ) ) ;
#178167=CARTESIAN_POINT ( 'NONE',  ( 2.008866915445167045, 0.004233813517278902337, 1.915903396628533706 ) ) ;
#178168=CARTESIAN_POINT ( 'NONE',  ( 2.893098739488662030, 0.2508700648995808025, 2.055025655848155886 ) ) ;
#178170=CARTESIAN_POINT ( 'NONE',  ( 1.903138372489954655, 1.638015138609005383, 1.096796735940619660 ) ) ;
#178171=CARTESIAN_POINT ( 'NONE',  ( 6.164670984062957437, -1.360496472042394656, 1.364235590486153837 ) ) ;
#178172=CARTESIAN_POINT ( 'NONE',  ( 3.309304339999539657, -0.3661640501408692794, 1.834289908569000538 ) ) ;
#178174=CARTESIAN_POINT ( 'NONE',  ( 1.014821436393667398, -1.042085040243752481, -2.059081925104982336 ) ) ;
#178176=CARTESIAN_POINT ( 'NONE',  ( 2.611566863951066519, 0.4996721132001956112, -1.792629727676842144 ) ) ;
#178178=CARTESIAN_POINT ( 'NONE',  ( 5.863753151201884783, -0.5045919461894343705, 1.999881752496771359 ) ) ;
#178183=CARTESIAN_POINT ( 'NONE',  ( 5.930723256393157783, 2.028624516890007445, 0.5651790528119063906 ) ) ;
#178185=CARTESIAN_POINT ( 'NONE',  ( 5.764953170560049855, -1.951456690425241947, -0.9300186209130756332 ) ) ;
#178186=CARTESIAN_POINT ( 'NONE',  ( 5.971354884044596467, -1.733367664992270685, -1.036320259733174209 ) ) ;
#178193=CARTESIAN_POINT ( 'NONE',  ( 4.663296154398564042, 1.879804967172087782, -0.7303043177912388328 ) ) ;
#178199=CARTESIAN_POINT ( 'NONE',  ( 5.594645800149128156, -0.5210773734287167391, -2.097845705497362712 ) ) ;
#178204=CARTESIAN_POINT ( 'NONE',  ( 0.3334082175802362547, 0.6002418569295930872, -1.819223357073847636 ) ) ;
#178207=CARTESIAN_POINT ( 'NONE',  ( 6.639320575229286092, 4.689090874229541406, 2.765823994384248419 ) ) ;
#178208=CARTESIAN_POINT ( 'NONE',  ( 1.435739417030171605, 0.8527202394775310612, -1.499263083578871836 ) ) ;
#178212=CARTESIAN_POINT ( 'NONE',  ( 6.485618507650338316, 1.290063292742931633, 1.354747167150817333 ) ) ;
#178213=CARTESIAN_POINT ( 'NONE',  ( 1.102198380138383449, -0.9033151347564006839, 1.799099544393264472 ) ) ;
#178216=CARTESIAN_POINT ( 'NONE',  ( 3.487540646120320442, 1.995909124301387116, -0.9416478298167814120 ) ) ;
#178217=CARTESIAN_POINT ( 'NONE',  ( 5.840740439281987051, -2.116473627201011620, -0.4831736825232531007 ) ) ;
#178221=CARTESIAN_POINT ( 'NONE',  ( 3.475340844119988226, -1.870931441966826148, -0.9980012987173056960 ) ) ;
#178222=CARTESIAN_POINT ( 'NONE',  ( 2.425407844734633223, -1.496065234337567329, -1.352141214786584777 ) ) ;
#178223=CARTESIAN_POINT ( 'NONE',  ( 1.898416112216103624, -1.777124406008349533, -0.3506645682890742743 ) ) ;
#178230=CARTESIAN_POINT ( 'NONE',  ( 1.340887447446635017, -1.644988140609974225, -0.9815275998622545739 ) ) ;
#178237=CARTESIAN_POINT ( 'NONE',  ( 4.873979933848565871, 1.241796773192262116, 1.769252301715443565 ) ) ;
#178241=CARTESIAN_POINT ( 'NONE',  ( 2.672263739372262137, 2.109986773948614225, -0.2121620573234672125 ) ) ;
#178244=CARTESIAN_POINT ( 'NONE',  ( 3.585193993258027678, 1.783571249345828003, -0.8399556444593555549 ) ) ;
#178245=( BOUNDED_SURFACE ( )  B_SPLINE_SURFACE ( 3, 3, ( 
 ( #175113, #10443, #46179, #113366, #14703, #110163, #93871, #143709, #45119, #47252 ),
 ( #146887, #142627, #130684, #127504, #212907, #64540, #159909, #79716, #78645, #179371 ),
 ( #209701, #211837, #196673, #112293, #30993, #178309, #11515, #60269, #77586, #126426 ),
 ( #61345, #192389, #193475, #160982, #94933, #111229, #177232, #28845, #144771, #29918 ),
 ( #96000, #12573, #62404, #162054, #13644, #63475, #129629, #195616, #160235, #159166 ),
 ( #94195, #92062, #157054, #76840, #192712, #140827, #211097, #127836, #191644, #29172 ),
 ( #111551, #78973, #175434, #145093, #8643, #77912, #46496, #12894, #10765, #45437 ) ),
 .UNSPECIFIED., .T., .F., .F. ) 
 B_SPLINE_SURFACE_WITH_KNOTS ( ( 4, 3, 4 ),
 ( 4, 1, 1, 1, 1, 1, 1, 4 ),
 ( 0.000000000000000000, 0.5000000000000000000, 1.000000000000000000 ),
 ( 0.000000000000000000, 0.09272347919791326665, 0.1850049962306132278, 0.2567072177207115891, 0.3610482009861257779, 0.5209239196176974618, 0.7336689415868371533, 1.000000000000000000 ),
 .UNSPECIFIED. ) 
 GEOMETRIC_REPRESENTATION_ITEM ( )  RATIONAL_B_SPLINE_SURFACE ( (
 ( 1.000000000000000444, 1.000000000000000444, 1.000000000000000222, 1.000000000000000444, 1.000000000000000222, 1.000000000000000444, 1.000000000000000222, 1.000000000000000222, 1.000000000000000222, 1.000000000000000222),
 ( 0.3333333333333334814, 0.3333333333333335369, 0.3333333333333334814, 0.3333333333333334259, 0.3333333333333334259, 0.3333333333333334259, 0.3333333333333334259, 0.3333333333333334259, 0.3333333333333334259, 0.3333333333333334259),
 ( 0.3333333333333334814, 0.3333333333333335369, 0.3333333333333334814, 0.3333333333333334259, 0.3333333333333334259, 0.3333333333333334259, 0.3333333333333334259, 0.3333333333333334259, 0.3333333333333334259, 0.3333333333333334259),
 ( 1.000000000000000444, 1.000000000000000444, 1.000000000000000222, 1.000000000000000444, 1.000000000000000222, 1.000000000000000444, 1.000000000000000222, 1.000000000000000222, 1.000000000000000222, 1.000000000000000222),
 ( 0.3333333333333334814, 0.3333333333333335369, 0.3333333333333334814, 0.3333333333333334259, 0.3333333333333334259, 0.3333333333333334259, 0.3333333333333334259, 0.3333333333333334259, 0.3333333333333334259, 0.3333333333333334259),
 ( 0.3333333333333334814, 0.3333333333333335369, 0.3333333333333334814, 0.3333333333333334259, 0.3333333333333334259, 0.3333333333333334259, 0.3333333333333334259, 0.3333333333333334259, 0.3333333333333334259, 0.3333333333333334259),
 ( 1.000000000000000444, 1.000000000000000444, 1.000000000000000222, 1.000000000000000444, 1.000000000000000222, 1.000000000000000444, 1.000000000000000222, 1.000000000000000222, 1.000000000000000222, 1.000000000000000222) ) ) 
 REPRESENTATION_ITEM ( '' )  SURFACE ( )  );
#178246=CARTESIAN_POINT ( 'NONE',  ( 5.326388512780113160, -0.8654452107222168067, -1.705464787417856787 ) ) ;
#178249=CARTESIAN_POINT ( 'NONE',  ( 0.6079806153083644471, 0.6509857562557037625, -1.965403638620793147 ) ) ;
#178250=CARTESIAN_POINT ( 'NONE',  ( 3.134642302965468641, -1.712256071497103349, 0.9161664635699683368 ) ) ;
#178255=CARTESIAN_POINT ( 'NONE',  ( 3.029325995398450821, -1.404573224648179242, -1.548692548079745546 ) ) ;
#178258=CARTESIAN_POINT ( 'NONE',  ( -0.07596920688733227456, -0.7732221873907207943, -1.636987988057141852 ) ) ;
#178260=CARTESIAN_POINT ( 'NONE',  ( 4.002700589841681200, -0.6913439845411989415, -2.095861086919461602 ) ) ;
#178261=CARTESIAN_POINT ( 'NONE',  ( 3.311752114541001379, -0.4323003076652854326, 2.163846791405985570 ) ) ;
#178264=( BOUNDED_SURFACE ( )  B_SPLINE_SURFACE ( 3, 3, ( 
 ( #146169, #45459, #212184, #180767, #98461, #95286, #149342, #111575, #164525, #82194, #49705 ),
 ( #181820, #921, #66989, #177583, #211120, #62744, #194885, #112644, #178653, #30264, #96350 ),
 ( #70194, #101656, #199126, #167724, #119036, #20391, #182899, #38794, #36645, #104875, #35576 ),
 ( #153616, #121196, #3057, #68052, #69127, #52902, #170918, #136306, #152539, #18252, #150424 ),
 ( #1989, #88625, #51852, #202328, #103803, #19325, #84336, #137377, #87548, #100588, #200199 ),
 ( #4125, #71263, #53978, #187165, #135249, #102729, #120114, #5188, #201262, #168786, #186094 ),
 ( #37724, #169852, #134190, #34515, #117972, #22514, #50770, #154680, #183965, #86475, #85402 ) ),
 .UNSPECIFIED., .T., .F., .F. ) 
 B_SPLINE_SURFACE_WITH_KNOTS ( ( 4, 3, 4 ),
 ( 4, 1, 1, 1, 1, 1, 1, 1, 4 ),
 ( 0.000000000000000000, 0.5000000000000000000, 1.000000000000000000 ),
 ( 0.000000000000000000, 0.2256337125576066971, 0.3978389261578171299, 0.5257960283851228489, 0.6187025735204009225, 0.6856790771877526725, 0.7354782194756434022, 0.7762620033627533056, 0.9999999999999998890 ),
 .UNSPECIFIED. ) 
 GEOMETRIC_REPRESENTATION_ITEM ( )  RATIONAL_B_SPLINE_SURFACE ( (
 ( 1.000000000000000000, 1.000000000000000000, 1.000000000000000222, 1.000000000000000000, 0.9999999999999997780, 1.000000000000000222, 0.9999999999999997780, 1.000000000000000222, 0.9999999999999992228, 1.000000000000000000, 1.000000000000000000),
 ( 0.3333333333333333703, 0.3333333333333334259, 0.3333333333333334259, 0.3333333333333333703, 0.3333333333333333148, 0.3333333333333334259, 0.3333333333333333703, 0.3333333333333334259, 0.3333333333333330928, 0.3333333333333333703, 0.3333333333333333703),
 ( 0.3333333333333333703, 0.3333333333333334259, 0.3333333333333334259, 0.3333333333333333703, 0.3333333333333333148, 0.3333333333333334259, 0.3333333333333333703, 0.3333333333333334259, 0.3333333333333330928, 0.3333333333333333703, 0.3333333333333333703),
 ( 1.000000000000000000, 1.000000000000000000, 1.000000000000000222, 1.000000000000000000, 0.9999999999999997780, 1.000000000000000222, 0.9999999999999997780, 1.000000000000000222, 0.9999999999999992228, 1.000000000000000000, 1.000000000000000000),
 ( 0.3333333333333333703, 0.3333333333333334259, 0.3333333333333334259, 0.3333333333333333703, 0.3333333333333333148, 0.3333333333333334259, 0.3333333333333333703, 0.3333333333333334259, 0.3333333333333330928, 0.3333333333333333703, 0.3333333333333333703),
 ( 0.3333333333333333703, 0.3333333333333334259, 0.3333333333333334259, 0.3333333333333333703, 0.3333333333333333148, 0.3333333333333334259, 0.3333333333333333703, 0.3333333333333334259, 0.3333333333333330928, 0.3333333333333333703, 0.3333333333333333703),
 ( 1.000000000000000000, 1.000000000000000000, 1.000000000000000222, 1.000000000000000000, 0.9999999999999997780, 1.000000000000000222, 0.9999999999999997780, 1.000000000000000222, 0.9999999999999992228, 1.000000000000000000, 1.000000000000000000) ) ) 
 REPRESENTATION_ITEM ( '' )  SURFACE ( )  );
#178266=CARTESIAN_POINT ( 'NONE',  ( 1.559083858985313542, -1.614856622157490929, 1.023943737511850083 ) ) ;
#178268=CARTESIAN_POINT ( 'NONE',  ( 4.281733463571851139, -1.982135700070002615, 0.5980053909793591194 ) ) ;
#178271=CARTESIAN_POINT ( 'NONE',  ( 3.327187652246216931, 0.05129554954072869377, 2.161254785723889515 ) ) ;
#178272=CARTESIAN_POINT ( 'NONE',  ( 4.862908538974716421, 0.2148362657848035262, -2.180980218048253150 ) ) ;
#178279=CARTESIAN_POINT ( 'NONE',  ( 0.2994542103806375200, 1.388483683912977495, -1.462447666687356485 ) ) ;
#178282=CARTESIAN_POINT ( 'NONE',  ( 4.170806909802426965, 1.467596682293986765, -1.460439952253207663 ) ) ;
#178283=CARTESIAN_POINT ( 'NONE',  ( 2.807156881705831442, 1.627618881652561411, 1.030384643589934646 ) ) ;
#178284=CARTESIAN_POINT ( 'NONE',  ( 5.466459189643565253, -2.065842013452086956, -0.4630074653421185071 ) ) ;
#178288=CARTESIAN_POINT ( 'NONE',  ( 3.432427499664345127, -1.176894005904068896, 1.578936197102176031 ) ) ;
#178289=CARTESIAN_POINT ( 'NONE',  ( 6.351568543859240634, 2.286598795830016684, -0.1622092447367465551 ) ) ;
#178290=CARTESIAN_POINT ( 'NONE',  ( 4.230939532379584200, 0.09184734775685020336, 1.823503176236190404 ) ) ;
#178298=CARTESIAN_POINT ( 'NONE',  ( 2.085277916773973228, -0.7859315772556186852, 1.665205719185464561 ) ) ;
#178299=CARTESIAN_POINT ( 'NONE',  ( 5.431894621915298593, -1.963206642400895374, 0.4451836139030879713 ) ) ;
#178300=CARTESIAN_POINT ( 'NONE',  ( 6.592461167385279097, -0.5184713896582182624, 2.248443398875634269 ) ) ;
#178301=CARTESIAN_POINT ( 'NONE',  ( 5.119951393648711324, 1.940949770148656661, -0.2839766199017114690 ) ) ;
#178306=CARTESIAN_POINT ( 'NONE',  ( 1.259447021655529797, 2.059213905598542116, -0.3608319165549890295 ) ) ;
#178307=CARTESIAN_POINT ( 'NONE',  ( 6.350471991779750525, 0.5597436608810264502, 1.679089333223187985 ) ) ;
#178309=CARTESIAN_POINT ( 'NONE',  ( -0.1102773484824119410, 2.860927498608015984, -2.691535809252169731 ) ) ;
#178310=CARTESIAN_POINT ( 'NONE',  ( 1.065484398342542383, -1.105240684350906610, 1.344476687319878794 ) ) ;
#178312=DIRECTION ( 'NONE',  ( -1.000000000000000000, 0.000000000000000000, 0.000000000000000000 ) ) ;
#178314=CARTESIAN_POINT ( 'NONE',  ( 1.910387937834428174, 1.279409190829815746, -1.157040217339623034 ) ) ;
#178315=CARTESIAN_POINT ( 'NONE',  ( 1.663894474538109236, 1.130263417742288112, 1.877492182091732076 ) ) ;
#178316=CARTESIAN_POINT ( 'NONE',  ( -0.07027205189932134166, -1.338084538058325279, -1.103043951268277478 ) ) ;
#178317=CARTESIAN_POINT ( 'NONE',  ( 4.547634279845023109, -1.704780727694398479, -1.401453192282381188 ) ) ;
#178320=CARTESIAN_POINT ( 'NONE',  ( 1.077284259287077495, 2.005170101804130578, 0.8328141809181826005 ) ) ;
#178321=CARTESIAN_POINT ( 'NONE',  ( 0.2229205655521030172, -0.09321834626660817358, 1.823428419517532983 ) ) ;
#178322=CARTESIAN_POINT ( 'NONE',  ( 3.380171168471556520, -2.115091482053657934, -0.09962960183704583361 ) ) ;
#178323=CARTESIAN_POINT ( 'NONE',  ( 6.639320575229255006, 0.6011172813700341733, 1.850849092781511107 ) ) ;
#178325=CARTESIAN_POINT ( 'NONE',  ( 3.720531229262864947, 2.177046216224611364, 0.7181995365407625176 ) ) ;
#178329=CARTESIAN_POINT ( 'NONE',  ( 6.498696386931579028, -2.177790866848747342, -0.4366942510913833231 ) ) ;
#178335=CARTESIAN_POINT ( 'NONE',  ( 3.604138833494671346, -0.1455340571130462057, 2.011204217620660817 ) ) ;
#178337=CARTESIAN_POINT ( 'NONE',  ( 1.762625871119470000, -0.7384422231204194054, -1.926036706659232323 ) ) ;
#178342=CARTESIAN_POINT ( 'NONE',  ( 4.962908505822443139, 0.2168217322565080263, -2.180687389885840322 ) ) ;
#178343=CARTESIAN_POINT ( 'NONE',  ( 2.514296259408643319, -1.880434619097739013, 0.7283795345095490648 ) ) ;
#178344=CARTESIAN_POINT ( 'NONE',  ( 2.173174093899932657, 1.133995793187540180, 1.450494936146892622 ) ) ;
#178347=CARTESIAN_POINT ( 'NONE',  ( 5.016531207907320322, 1.258010867292450152, -1.323153095230594989 ) ) ;
#178348=CARTESIAN_POINT ( 'NONE',  ( 6.240861317752083970, 2.010826688392798101, -0.1511364921914087889 ) ) ;
#178350=CARTESIAN_POINT ( 'NONE',  ( 5.524405971769074775, 1.352560167130362867, -1.813582142078016712 ) ) ;
#178352=CARTESIAN_POINT ( 'NONE',  ( 1.242952776902699785, 0.4124841525564198474, 2.065099357090140586 ) ) ;
#178361=CARTESIAN_POINT ( 'NONE',  ( 2.571500236035813902, 1.429449181443824823, 1.422607194786096541 ) ) ;
#178363=CARTESIAN_POINT ( 'NONE',  ( 2.637233524875877588, 2.093239256532848369, 0.7440790952397638991 ) ) ;
#178367=CARTESIAN_POINT ( 'NONE',  ( 3.560947883890089649, 1.548132398191165882, -1.204989647596923508 ) ) ;
#178373=CARTESIAN_POINT ( 'NONE',  ( 2.848016566918720294, -1.427295477286108394, -1.568503593382633454 ) ) ;
#178375=CARTESIAN_POINT ( 'NONE',  ( 4.012696165952275962, 1.530467462299599513, -1.526897427004340280 ) ) ;
#178376=CARTESIAN_POINT ( 'NONE',  ( 2.384105128782065819, -0.3166398734758494315, -1.813660976904336808 ) ) ;
#178379=CARTESIAN_POINT ( 'NONE',  ( 6.140530580581591735, -1.466303750465405065, 0.9370796520578956734 ) ) ;
#178382=CARTESIAN_POINT ( 'NONE',  ( 2.817419395390472037, -0.2130390993498078311, 2.151187356804876050 ) ) ;
#178383=CARTESIAN_POINT ( 'NONE',  ( 4.552111140598270822, 1.802141083034415781, -0.9039717811075360654 ) ) ;
#178385=CARTESIAN_POINT ( 'NONE',  ( 2.360439101503517101, 0.9236781337260314695, 1.954550705658316456 ) ) ;
#178386=CARTESIAN_POINT ( 'NONE',  ( 2.846899755239293839, -1.641009487379685217, 1.092116875444639090 ) ) ;
#178388=CARTESIAN_POINT ( 'NONE',  ( 6.509000000000014552, 2.444259026362519904, 2.383015625331697862 ) ) ;
#178389=CARTESIAN_POINT ( 'NONE',  ( 4.177243316516196181, 1.270932653052879502, 1.468510540936379671 ) ) ;
#178398=CARTESIAN_POINT ( 'NONE',  ( 1.501302152069685425, 1.803625081967351829, -1.271268654958551014 ) ) ;
#178400=CARTESIAN_POINT ( 'NONE',  ( 5.823093080589802462, -1.771997608643091304, -0.8420800316405114838 ) ) ;
#178405=CARTESIAN_POINT ( 'NONE',  ( 3.855264089065893351, 1.827008581971893530, -0.2271198879545410221 ) ) ;
#178410=CARTESIAN_POINT ( 'NONE',  ( 6.533471381225442798, -0.1521382079053348602, 2.086446650026114735 ) ) ;
#178414=CARTESIAN_POINT ( 'NONE',  ( 0.2509463769419334467, -1.655472276559850853, 1.227265982703225511 ) ) ;
#178416=CARTESIAN_POINT ( 'NONE',  ( 1.486513762117396498, 1.792272468715813138, 0.5009694556475997596 ) ) ;
#178417=CARTESIAN_POINT ( 'NONE',  ( 3.386116603743833497, -0.3623624896987759914, -1.805063595765175499 ) ) ;
#178423=CARTESIAN_POINT ( 'NONE',  ( 3.018423772948013006, -1.088090592406821155, -1.919924466345590108 ) ) ;
#178424=CARTESIAN_POINT ( 'NONE',  ( 6.081380179524085605, 2.093784091706856199, -0.8575614380509981594 ) ) ;
#178426=CARTESIAN_POINT ( 'NONE',  ( 5.853729002925880387, -1.318332981873654441, -1.242799640730863464 ) ) ;
#178427=CARTESIAN_POINT ( 'NONE',  ( 5.911341210168471250, -1.801345639624308381, 0.6523577827844198040 ) ) ;
#178428=ADVANCED_FACE ( 'NONE', ( #206525 ), #176561, .F. ) ;
#178430=CARTESIAN_POINT ( 'NONE',  ( 6.596569749568344854, -0.5012203084251048990, -1.802199723311518786 ) ) ;
#178432=CARTESIAN_POINT ( 'NONE',  ( 6.443805748662878585, 1.284351271648530357, 1.347085863211768819 ) ) ;
#178434=CARTESIAN_POINT ( 'NONE',  ( 0.07479286986305370977, 0.004866263145587856019, -1.855573292446038414 ) ) ;
#178436=CARTESIAN_POINT ( 'NONE',  ( 1.165250339122084533, 1.861343190080061882, -0.7762330495894869120 ) ) ;
#178438=CARTESIAN_POINT ( 'NONE',  ( 3.404997959543601294, 1.660052132133410296, -1.295932331351705935 ) ) ;
#178442=CARTESIAN_POINT ( 'NONE',  ( 2.461199802766162570, -1.676885983773316990, 1.125551603727361627 ) ) ;
#178445=CARTESIAN_POINT ( 'NONE',  ( 3.550220938608072085, 2.161773192003491495, 0.003901938047633223515 ) ) ;
#178450=CARTESIAN_POINT ( 'NONE',  ( 1.293694231370069891, -1.962959732339657259, 0.9280293838552654551 ) ) ;
#178454=CARTESIAN_POINT ( 'NONE',  ( 2.226364491882920404, 2.126620374013419301, 0.5291077681483095096 ) ) ;
#178456=CARTESIAN_POINT ( 'NONE',  ( 2.694485044408474916, -2.256396476877442492, -0.1672753843019215703 ) ) ;
#178463=CARTESIAN_POINT ( 'NONE',  ( 3.092752268530512438, 1.519777622694931773, -0.9064811718217934411 ) ) ;
#178465=CARTESIAN_POINT ( 'NONE',  ( 6.493228066955544442, 1.923254169853494178, -1.081975473724585690 ) ) ;
#178468=CARTESIAN_POINT ( 'NONE',  ( 6.591432905763006111, -0.4393008961055907546, 1.975236973087670878 ) ) ;
#178470=CARTESIAN_POINT ( 'NONE',  ( 3.502682687546424312, 1.475339254275360279, -1.149998991230333223 ) ) ;
#178471=CARTESIAN_POINT ( 'NONE',  ( 2.782155020660907141, -1.188329515115684076, -1.695063343828225877 ) ) ;
#178475=FILL_AREA_STYLE ('',( #61516 ) ) ;
#178476=CARTESIAN_POINT ( 'NONE',  ( 6.596550757224428629, -0.5713381284546023009, -2.084776384472402100 ) ) ;
#178478=CARTESIAN_POINT ( 'NONE',  ( 2.383191274269541360, -0.003000794896521400724, 1.962046632024143866 ) ) ;
#178479=CARTESIAN_POINT ( 'NONE',  ( 0.4388270972612972609, 1.158508728638860230, 1.649830871073371119 ) ) ;
#178484=CARTESIAN_POINT ( 'NONE',  ( 0.9482695043977107385, 0.5371953702461745861, 1.791772314883005146 ) ) ;
#178486=CARTESIAN_POINT ( 'NONE',  ( 2.654543897082308312, 1.998474955683330334, 0.2423782132614532570 ) ) ;
#178488=CARTESIAN_POINT ( 'NONE',  ( 1.986098615764248398, -2.116669865667855088, 0.05555418577087371801 ) ) ;
#178490=CARTESIAN_POINT ( 'NONE',  ( 3.701679681979888503, -1.565833156357125278, -1.354537944502069102 ) ) ;
#178492=CARTESIAN_POINT ( 'NONE',  ( 5.455056007322736100, 0.4086298902603173744, -2.050129383449701415 ) ) ;
#178494=CARTESIAN_POINT ( 'NONE',  ( 4.506759567000420574, 1.410888988908312047, -1.158519065656477220 ) ) ;
#178499=CARTESIAN_POINT ( 'NONE',  ( 6.581111309608331794, -0.1016299978719436697, -2.204559905201553427 ) ) ;
#178502=CARTESIAN_POINT ( 'NONE',  ( 5.250612361737760025, 1.884661702551674534, 0.3228764834103393100 ) ) ;
#178507=CARTESIAN_POINT ( 'NONE',  ( 0.7668492355173107677, 1.774547462407764842, -0.4907661837717376407 ) ) ;
#178510=CARTESIAN_POINT ( 'NONE',  ( 5.255093269098372488, -1.579555527043162488, -1.001684657140684775 ) ) ;
#178511=CARTESIAN_POINT ( 'NONE',  ( 0.07700591528351108384, 2.887024434135841755, -2.399578936219012082 ) ) ;
#178519=CARTESIAN_POINT ( 'NONE',  ( 0.8308272516417656295, -1.852502698908803591, -0.6688572162713811720 ) ) ;
#178520=CARTESIAN_POINT ( 'NONE',  ( 3.444935562074178392, -1.779636981393231565, -0.9480232565319337557 ) ) ;
#178523=EDGE_CURVE ( 'NONE', #8531, #71735, #142054, .T. ) ;
#178524=CARTESIAN_POINT ( 'NONE',  ( 3.117305861062225958, -2.111875107304355570, 0.5849144002756587746 ) ) ;
#178528=CARTESIAN_POINT ( 'NONE',  ( 0.2331563151865694850, 5.724144821786467219, -2.539778028485844441 ) ) ;
#178535=CARTESIAN_POINT ( 'NONE',  ( 4.511176471348508521, -1.804767551675333204, 0.3638508048048467169 ) ) ;
#178536=CARTESIAN_POINT ( 'NONE',  ( 1.735022414761304921, 1.879166562360615966, 0.7224556781355166990 ) ) ;
#178537=CARTESIAN_POINT ( 'NONE',  ( 4.728017916497640805, -2.050086588643835750, -1.039272215941482225 ) ) ;
#178538=CARTESIAN_POINT ( 'NONE',  ( -0.1291982275798781443, -0.004298614154785855221, -2.073875112923003083 ) ) ;
#178539=CARTESIAN_POINT ( 'NONE',  ( 1.727181476345755806, 0.1432717513335572956, -1.855521175285803182 ) ) ;
#178542=CARTESIAN_POINT ( 'NONE',  ( 5.924064563541377559, -1.897137492723115049, 0.2407653536913647030 ) ) ;
#178545=CARTESIAN_POINT ( 'NONE',  ( 5.161704669080129371, 1.031500688015974054, 1.818515148517543034 ) ) ;
#178546=CARTESIAN_POINT ( 'NONE',  ( 2.869827659178546764, 0.9992216309704025079, 1.581230272166146644 ) ) ;
#178548=CARTESIAN_POINT ( 'NONE',  ( 5.390138975101268493, -0.4531076923771395482, -1.784498753146485539 ) ) ;
#178551=CARTESIAN_POINT ( 'NONE',  ( 5.232891500378062943, 0.1322050776780703540, 1.719872175869048947 ) ) ;
#178553=CARTESIAN_POINT ( 'NONE',  ( 0.4747597223977735315, -1.720734514737034093, -0.2143409017008046646 ) ) ;
#178556=CARTESIAN_POINT ( 'NONE',  ( 4.961888193860729324, -0.5853885669280403103, 2.090577497978749477 ) ) ;
#178557=CARTESIAN_POINT ( 'NONE',  ( 3.703562413045482060, -0.5285312144065814621, 1.747510042522756990 ) ) ;
#178558=CARTESIAN_POINT ( 'NONE',  ( 1.076917802502619592, 1.810449747239597951, 0.7559744942375112853 ) ) ;
#178559=CARTESIAN_POINT ( 'NONE',  ( -0.05292715583045219663, -1.893440308637056146, -0.9475653277955156106 ) ) ;
#178561=CARTESIAN_POINT ( 'NONE',  ( 0.1997390566700393277, -0.6049713359795177992, 2.210933144166931985 ) ) ;
#178564=ADVANCED_FACE ( 'NONE', ( #152196 ), #199944, .F. ) ;
#178567=CARTESIAN_POINT ( 'NONE',  ( 2.737105750116640923, 1.997451989420237606, 0.7121958652205606644 ) ) ;
#178572=CARTESIAN_POINT ( 'NONE',  ( 0.4091448426733998445, -1.664836780672280803, 1.230395522420650201 ) ) ;
#178575=CARTESIAN_POINT ( 'NONE',  ( 2.772393654007713870, 2.210366155326251025, -0.2202761458626761870 ) ) ;
#178577=CARTESIAN_POINT ( 'NONE',  ( 1.161203735943004300, 1.374334461307982425, 1.842484299438088557 ) ) ;
#178579=CARTESIAN_POINT ( 'NONE',  ( 5.190308500716538376, 1.065014321051664048, -1.766232332728798538 ) ) ;
#178584=CARTESIAN_POINT ( 'NONE',  ( 5.337399561049260832, 0.7408347518493042516, -1.685818907712175019 ) ) ;
#178588=CARTESIAN_POINT ( 'NONE',  ( 2.326796526899118422, -0.003300274434325441240, 1.724958192180660044 ) ) ;
#178589=CARTESIAN_POINT ( 'NONE',  ( 1.657435761918718331, 1.928256795251210631, -0.5899901959932272177 ) ) ;
#178590=CARTESIAN_POINT ( 'NONE',  ( 1.952162490553134955, -2.103507816325803415, -0.9273050526804761384 ) ) ;
#178592=CARTESIAN_POINT ( 'NONE',  ( 2.478104529052836291, 1.390129537188329101, 1.784895063601476428 ) ) ;
#178593=CARTESIAN_POINT ( 'NONE',  ( 4.582709122986449835, -2.042650070554121733, -0.5124292222106421324 ) ) ;
#178595=CARTESIAN_POINT ( 'NONE',  ( 2.248939020346378381, -1.418119551073221851, -1.058484587410456701 ) ) ;
#178598=CARTESIAN_POINT ( 'NONE',  ( 4.915721525821019178, -1.224934246408443839, -1.937497040551818150 ) ) ;
#178599=CARTESIAN_POINT ( 'NONE',  ( 4.681507052731401330, -0.8653998779965512700, 1.625073734443114759 ) ) ;
#178604=CARTESIAN_POINT ( 'NONE',  ( 4.224703044441734612, 0.1064595904514322594, 2.188988589495489911 ) ) ;
#178609=CARTESIAN_POINT ( 'NONE',  ( 3.105993306306195301, -1.924270352051945299, 0.09518456514568535143 ) ) ;
#178612=CARTESIAN_POINT ( 'NONE',  ( 6.011998765391792787, -0.7129019540204998284, 1.997330473063135381 ) ) ;
#178618=CARTESIAN_POINT ( 'NONE',  ( 6.409700764581637067, -0.8744420883355051854, -1.620376909479949390 ) ) ;
#178621=CARTESIAN_POINT ( 'NONE',  ( 1.821426705348125230, 1.001848811563336605, -1.422965107008233643 ) ) ;
#178623=CARTESIAN_POINT ( 'NONE',  ( 0.2210476084268316321, -1.750679471464357873, -0.8856473702157914296 ) ) ;
#178626=CARTESIAN_POINT ( 'NONE',  ( 5.981359018292748075, 1.999130597612966742, -0.8229454869796914984 ) ) ;
#178629=CARTESIAN_POINT ( 'NONE',  ( 6.157120911006636277, -1.851533521339579380, -1.115484332758958974 ) ) ;
#178633=CARTESIAN_POINT ( 'NONE',  ( 0.4384654110765589530, 0.3132546388123040870, 1.843968665737522050 ) ) ;
#178634=CARTESIAN_POINT ( 'NONE',  ( 6.169268014014505752, -0.6277043665407368023, -1.616433383845305105 ) ) ;
#178636=CARTESIAN_POINT ( 'NONE',  ( 3.087623348389135547, -0.8860277256741244667, 2.004638750299721828 ) ) ;
#178637=CARTESIAN_POINT ( 'NONE',  ( 3.804037270277782490, -0.6727452520632947186, 2.207335857111696331 ) ) ;
#178638=CARTESIAN_POINT ( 'NONE',  ( 6.011025214932095295, 1.815421535059216662, 0.9752673143463059802 ) ) ;
#178639=CARTESIAN_POINT ( 'NONE',  ( 1.534995247775998939, -1.406442930887800813, -1.339296560326202146 ) ) ;
#178644=CARTESIAN_POINT ( 'NONE',  ( 3.568700945156903614, 0.7666329941097769218, 1.977337035738421900 ) ) ;
#178645=CARTESIAN_POINT ( 'NONE',  ( 2.795546247670523954, 1.458556481301529706, -1.392545902517070111 ) ) ;
#178647=CARTESIAN_POINT ( 'NONE',  ( 3.997267248050282884, 1.865803599355109421, -1.178106810156675843 ) ) ;
#178653=CARTESIAN_POINT ( 'NONE',  ( 6.825078400183548943, 1.222324429417048330, 2.356141576552318817 ) ) ;
#178656=CARTESIAN_POINT ( 'NONE',  ( 4.258703985924441326, -1.528322205979601334, 1.382770117495622397 ) ) ;
#178661=CARTESIAN_POINT ( 'NONE',  ( 3.510419912045096069, -2.017469964673058946, -0.09679370177045029666 ) ) ;
#178666=CARTESIAN_POINT ( 'NONE',  ( 3.485278940986863638, 1.863876800102952203, -0.8796150190680316339 ) ) ;
#178667=CARTESIAN_POINT ( 'NONE',  ( 2.567029916978436077, -1.034165006014248211, 1.730866473406714068 ) ) ;
#178671=CARTESIAN_POINT ( 'NONE',  ( 0.9195641160042143936, 1.098457714822091091, -1.477412082521646575 ) ) ;
#178672=CARTESIAN_POINT ( 'NONE',  ( 6.568967528192747096, -2.015767819289843388, -0.8987472251835016968 ) ) ;
#178674=CARTESIAN_POINT ( 'NONE',  ( 2.653791512158054200, 0.5793167894731532375, -2.082426382048585101 ) ) ;
#178676=CARTESIAN_POINT ( 'NONE',  ( 4.593022152086825294, 1.843820828628543129, 1.040707789177892861 ) ) ;
#178680=CARTESIAN_POINT ( 'NONE',  ( 1.358040219746913024, 0.7549631825471068147, 1.711723683848711985 ) ) ;
#178681=CARTESIAN_POINT ( 'NONE',  ( 5.032083864297879572, 1.014306426666331529, -1.690397665970795105 ) ) ;
#178683=CARTESIAN_POINT ( 'NONE',  ( 4.118375227313908482, 1.978554835517082555, 0.3886342876525810119 ) ) ;
#178687=CARTESIAN_POINT ( 'NONE',  ( 6.586557477600968546, -2.065026496990796101, -0.4128237726619687353 ) ) ;
#178688=CARTESIAN_POINT ( 'NONE',  ( 6.338344951546218908, -1.110931056888088353, 1.746890944850580052 ) ) ;
#178692=CARTESIAN_POINT ( 'NONE',  ( 4.715676653857135747, -1.933614719187324082, 0.3836508851736331605 ) ) ;
#178693=CARTESIAN_POINT ( 'NONE',  ( 5.994400513263062891, -1.076938050528394308, 1.708516719617196422 ) ) ;
#178695=CARTESIAN_POINT ( 'NONE',  ( 4.143447727350758392, -2.008842960899869912, 1.135675674892607345 ) ) ;
#178696=CARTESIAN_POINT ( 'NONE',  ( 2.342701370759682433, -2.021932799725610241, -0.4066214432158538616 ) ) ;
#178704=CARTESIAN_POINT ( 'NONE',  ( 4.527882006162959883, 2.107076143796441592, -0.5232759588417631447 ) ) ;
#178706=CARTESIAN_POINT ( 'NONE',  ( 3.509164994824386596, -1.813400730843343966, 0.3181347684400454012 ) ) ;
#178709=CARTESIAN_POINT ( 'NONE',  ( 5.302338810847701644, 1.659911028786088538, -1.431018553749352051 ) ) ;
#178711=CARTESIAN_POINT ( 'NONE',  ( 5.418922386936855240, 2.088194672119690676, 0.8713435986696310698 ) ) ;
#178712=EDGE_LOOP ( 'NONE', ( #191242, #155752, #61027, #202588 ) ) ;
#178717=CARTESIAN_POINT ( 'NONE',  ( 0.4789242711138582687, 1.653723610832663393, -0.6310274585415026616 ) ) ;
#178719=CARTESIAN_POINT ( 'NONE',  ( 5.074862666803740652, -1.456563189067984876, 1.389812660683345191 ) ) ;
#178721=CARTESIAN_POINT ( 'NONE',  ( 3.786240212431398966, -1.039621666623831597, 1.831390154885542243 ) ) ;
#178722=CARTESIAN_POINT ( 'NONE',  ( 1.739701290322914540, 1.910364143156467298, -0.1427236045144583687 ) ) ;
#178724=CARTESIAN_POINT ( 'NONE',  ( 3.613681597605075346, 0.4810616251548325284, -1.909752186315590405 ) ) ;
#178725=CARTESIAN_POINT ( 'NONE',  ( 5.590105174118587428, 1.206514928144377441, 1.619649990711173215 ) ) ;
#178726=CARTESIAN_POINT ( 'NONE',  ( 2.113927203836548419, -0.8795192785214582809, -1.650985937663045577 ) ) ;
#178727=CARTESIAN_POINT ( 'NONE',  ( 1.750371521623844462, -1.952110535733902585, -0.1955497077021361163 ) ) ;
#178728=CARTESIAN_POINT ( 'NONE',  ( 4.336358584672225902, 1.692218828317056278, 0.3330917469099390904 ) ) ;
#178729=CARTESIAN_POINT ( 'NONE',  ( 0.8438408207818194340, -1.215224102361469161, -1.476598726422105656 ) ) ;
#178731=CARTESIAN_POINT ( 'NONE',  ( 1.190363680384380229, -0.9894552095768920363, 1.972713631218452557 ) ) ;
#178740=CARTESIAN_POINT ( 'NONE',  ( 6.912946559606852226, -1.604190412254998810, 1.308348183162249434 ) ) ;
#178741=CARTESIAN_POINT ( 'NONE',  ( 1.064989848632340363, 1.568927673159369762, -1.351003706900590018 ) ) ;
#178746=CARTESIAN_POINT ( 'NONE',  ( 5.971359625099014856, -1.818578809777360972, -1.090262957368436147 ) ) ;
#178751=CARTESIAN_POINT ( 'NONE',  ( 5.828557447170540584, -1.245780601409246957, 1.515539014345569147 ) ) ;
#178753=CARTESIAN_POINT ( 'NONE',  ( 3.796249832574852601, -1.863883295361246084, 0.7690029265580224926 ) ) ;
#178755=CARTESIAN_POINT ( 'NONE',  ( 4.030425823177123057, 0.5166280748541264289, 1.844641390986961671 ) ) ;
#178757=CARTESIAN_POINT ( 'NONE',  ( 1.417800074541092137, -1.221294057239637576, -1.819523406426680090 ) ) ;
#178758=CARTESIAN_POINT ( 'NONE',  ( -0.1405533004718755308, 0.003749010675345022196, -1.720146753850456234 ) ) ;
#178760=CARTESIAN_POINT ( 'NONE',  ( 5.590095194574172588, 1.202541018705102660, 1.614423701025817115 ) ) ;
#178763=CARTESIAN_POINT ( 'NONE',  ( 5.694942756591524713, 1.867452007164069672, 0.9975914146606623678 ) ) ;
#178765=CARTESIAN_POINT ( 'NONE',  ( 2.595357119365874432, -0.6533576199754445035, 1.986123937679643348 ) ) ;
#178767=CARTESIAN_POINT ( 'NONE',  ( 2.063112832053456636, 0.2986308487272717471, -1.698545238003341673 ) ) ;
#178769=CARTESIAN_POINT ( 'NONE',  ( 5.818629517237746462, -0.7649446623404360102, -1.977987144599784086 ) ) ;
#178779=CARTESIAN_POINT ( 'NONE',  ( 2.209342481274043646, 1.400903122447524796, 1.148441741360214152 ) ) ;
#178784=CARTESIAN_POINT ( 'NONE',  ( 2.297251093426439628, 1.655750149966995544, -0.7352264245090130990 ) ) ;
#178785=CARTESIAN_POINT ( 'NONE',  ( 6.539320575229279342, 6.038407674219216759, 2.491644695858772796 ) ) ;
#178789=CARTESIAN_POINT ( 'NONE',  ( 4.404655029226283602, 0.4953248787317258706, 1.793866421858918869 ) ) ;
#178790=CARTESIAN_POINT ( 'NONE',  ( 0.1752026701883572513, 1.419887415397131925, 1.286083148499452600 ) ) ;
#178791=CARTESIAN_POINT ( 'NONE',  ( 0.3580656308817787292, 0.6935259069400134813, 1.688922952486398454 ) ) ;
#178797=CARTESIAN_POINT ( 'NONE',  ( 4.364079147461279895, -1.964463519307905193, 0.1404744649011815116 ) ) ;
#178801=CARTESIAN_POINT ( 'NONE',  ( 0.1817335109410072314, -0.9834369453871127931, 1.844881371607492326 ) ) ;
#178802=CARTESIAN_POINT ( 'NONE',  ( 5.368162667233546514, 0.9496366811117643580, 1.675975028240711540 ) ) ;
#178804=CARTESIAN_POINT ( 'NONE',  ( 0.6041866639863550104, -0.6101368697832668664, -1.720745249832649870 ) ) ;
#178805=CARTESIAN_POINT ( 'NONE',  ( 2.016531038934398445, -1.041976349804032642, -1.945408382319254503 ) ) ;
#178807=CARTESIAN_POINT ( 'NONE',  ( -0.1054227091227821350, -1.855472971956134920, -0.4628026090111520552 ) ) ;
#178810=CARTESIAN_POINT ( 'NONE',  ( 0.6429344911094649895, -0.2373986304471594755, -1.955105650238073478 ) ) ;
#178811=CARTESIAN_POINT ( 'NONE',  ( 1.188897196845212445, 1.471763766255501427, 1.267211023470141695 ) ) ;
#178814=CARTESIAN_POINT ( 'NONE',  ( 1.124374798274978104, 0.3960433595797500095, -1.976652716225081097 ) ) ;
#178816=CARTESIAN_POINT ( 'NONE',  ( 5.401151054173385369, -1.597185415876556158, 0.9547389691558528790 ) ) ;
#178823=CARTESIAN_POINT ( 'NONE',  ( 1.189316404147572337, 1.662717542896676504, 1.427817766309902314 ) ) ;
#178828=CARTESIAN_POINT ( 'NONE',  ( 2.121465551170404140, -1.771062468586531047, 0.4427346646293239818 ) ) ;
#178830=CARTESIAN_POINT ( 'NONE',  ( 6.609000000000012420, 4.697979799133416456, 2.462673521647487540 ) ) ;
#178832=CARTESIAN_POINT ( 'NONE',  ( 1.172347479525590375, -1.222655876604409553, 1.488804252732379485 ) ) ;
#178833=CARTESIAN_POINT ( 'NONE',  ( 4.926587646396720643, -1.284401507782207963, 1.482881906352449874 ) ) ;
#178837=CARTESIAN_POINT ( 'NONE',  ( 4.581673536070863584, -1.032772929490553215, 1.932928240684625099 ) ) ;
#178838=EDGE_CURVE ( 'NONE', #194636, #165662, #181033, .T. ) ;
#178841=CARTESIAN_POINT ( 'NONE',  ( 4.293848342403890683, -1.423947089648310849, -1.503027170334819029 ) ) ;
#178845=CARTESIAN_POINT ( 'NONE',  ( 4.166792231569245608, 1.501215554499458982, 1.740835934941728169 ) ) ;
#178847=ORIENTED_EDGE ( 'NONE', *, *, #32535, .T. ) ;
#178850=CARTESIAN_POINT ( 'NONE',  ( 6.620655732516679493, 2.454579131793722002, 2.310038015908893350 ) ) ;
#178852=CARTESIAN_POINT ( 'NONE',  ( 3.310425057758420664, 1.755882755489517999, 0.8297573096471222431 ) ) ;
#178855=CARTESIAN_POINT ( 'NONE',  ( 4.746305163667582150, 0.9781546018433548983, -1.643150005489722787 ) ) ;
#178857=CARTESIAN_POINT ( 'NONE',  ( 5.420820933352582749, 1.595050213381223214, 0.6567411224575621098 ) ) ;
#178858=CARTESIAN_POINT ( 'NONE',  ( 4.434779938697545276, -1.616694733667634942, 1.205040202231236091 ) ) ;
#178859=CARTESIAN_POINT ( 'NONE',  ( 5.045646660657260973, -1.666335398280174074, 1.583644221457411794 ) ) ;
#178861=CARTESIAN_POINT ( 'NONE',  ( 0.6455096168876961471, -1.890800792967793686, 1.137844069391671820 ) ) ;
#178864=CARTESIAN_POINT ( 'NONE',  ( 5.747242073547443653, -1.395821259116083013, -1.087781934379092874 ) ) ;
#178865=CARTESIAN_POINT ( 'NONE',  ( 6.363907750917786821, -0.1017471579566435469, -2.013986097687201049 ) ) ;
#178867=CARTESIAN_POINT ( 'NONE',  ( 1.939794425703120995, 0.8746495868690505882, -2.119022276272637839 ) ) ;
#178868=CARTESIAN_POINT ( 'NONE',  ( 0.9897393536978270623, -0.4193350815317981040, -1.688907716811594240 ) ) ;
#178871=CARTESIAN_POINT ( 'NONE',  ( 1.405166929871915604, 0.3316955492517637549, 1.701605581617445129 ) ) ;
#178874=CARTESIAN_POINT ( 'NONE',  ( 1.293694231370069891, -1.962959732339657259, 0.9280293838552654551 ) ) ;
#178875=CARTESIAN_POINT ( 'NONE',  ( 2.202361591730035428, 1.313542931311746598, -1.530159205979222170 ) ) ;
#178877=CARTESIAN_POINT ( 'NONE',  ( 0.3582593949469566885, 0.7340744485371183403, 1.781236698655277895 ) ) ;
#178879=CARTESIAN_POINT ( 'NONE',  ( 3.726986581234917661, 1.568921747024876634, -1.572872013324580154 ) ) ;
#178880=ORIENTED_EDGE ( 'NONE', *, *, #45059, .F. ) ;
#178885=CARTESIAN_POINT ( 'NONE',  ( 5.724081574600810463, 1.679587015112851578, 0.4559996917168698261 ) ) ;
#178887=CARTESIAN_POINT ( 'NONE',  ( 3.385159196556942085, 0.04556868695702701727, 1.961494628812537444 ) ) ;
#178890=CARTESIAN_POINT ( 'NONE',  ( 4.288523069895104456, -2.236996925053718055, -0.3375187357864944393 ) ) ;
#178892=CARTESIAN_POINT ( 'NONE',  ( 2.506364121320878713, 2.062161341495666100, 0.05312637652370164748 ) ) ;
#178894=CARTESIAN_POINT ( 'NONE',  ( 2.132027182898531326, -1.478040878648724465, -1.713098503734461708 ) ) ;
#178897=CARTESIAN_POINT ( 'NONE',  ( 4.147608549738549755, 0.6325110726591242072, -1.760471310998643624 ) ) ;
#178898=CARTESIAN_POINT ( 'NONE',  ( 2.250263858207638634, 1.700335624809163004, -0.3396627995243851061 ) ) ;
#178899=CARTESIAN_POINT ( 'NONE',  ( -0.04093971525966337566, -2.051586291785143512, -1.022954789973041123 ) ) ;
#178900=CARTESIAN_POINT ( 'NONE',  ( 6.510760317505348560, 1.716126801009032032, -1.542884448788630625 ) ) ;
#178901=CARTESIAN_POINT ( 'NONE',  ( 3.678741886385179072, -2.082744454470350615, -0.5786317199799119182 ) ) ;
#178902=CARTESIAN_POINT ( 'NONE',  ( 4.453030731839799472, 0.4239971928432215154, -1.894948383050964580 ) ) ;
#178904=CARTESIAN_POINT ( 'NONE',  ( 6.397708313642382905, -0.6301307688901837123, 1.761319926792910495 ) ) ;
#178906=CARTESIAN_POINT ( 'NONE',  ( -0.1224325501351306023, -0.4448023855274513272, -1.973852191825019364 ) ) ;
#178909=CARTESIAN_POINT ( 'NONE',  ( 6.276017556857773627, 1.753032240926259311, -0.9962986157117934560 ) ) ;
#178913=CARTESIAN_POINT ( 'NONE',  ( 3.475057130574196407, 0.04366187338752242769, -1.825333387291371512 ) ) ;
#178920=CARTESIAN_POINT ( 'NONE',  ( 6.322916996384010169, 1.495059732148263487, -1.358068445443241457 ) ) ;
#178921=CARTESIAN_POINT ( 'NONE',  ( 0.8387270772249322270, 1.259995426201226953, -1.705408266269872630 ) ) ;
#178924=CARTESIAN_POINT ( 'NONE',  ( 2.236936919162732629, -0.08530413586980757634, -1.859100468073461965 ) ) ;
#178926=CARTESIAN_POINT ( 'NONE',  ( 6.227427239534573999, -1.941376443541954488, 0.6920112976290059281 ) ) ;
#178927=CARTESIAN_POINT ( 'NONE',  ( 6.082657761774012961, -0.6767167302549758068, 1.899617564980569773 ) ) ;
#178937=CARTESIAN_POINT ( 'NONE',  ( 6.028672669474048007, 1.986741788447304646, -0.3418859329693338944 ) ) ;
#178938=CARTESIAN_POINT ( 'NONE',  ( 4.224425198852012286, 0.09258891237720960621, 1.838934309869838968 ) ) ;
#178939=CARTESIAN_POINT ( 'NONE',  ( 0.07700591528354226722, 2.040803078245361224, -2.328119179575589559 ) ) ;
#178940=CARTESIAN_POINT ( 'NONE',  ( 3.475486094516122115, 0.05728489528775136674, -2.307140494302026390 ) ) ;
#178942=CARTESIAN_POINT ( 'NONE',  ( 5.764953170560049855, -1.951456690425241947, -0.9300186209130756332 ) ) ;
#178944=CARTESIAN_POINT ( 'NONE',  ( 0.8197486350577835035, 1.155594189952107609, -1.560708653158059622 ) ) ;
#178948=CARTESIAN_POINT ( 'NONE',  ( 4.622621100999918298, 0.5092349069827777353, -2.241135911243127055 ) ) ;
#178951=CARTESIAN_POINT ( 'NONE',  ( 4.715616592392388284, -1.834479983729628616, 0.3652084810651031743 ) ) ;
#178952=CARTESIAN_POINT ( 'NONE',  ( 1.845825534506392085, -1.251752223804462272, -1.445855903880132631 ) ) ;
#178955=CARTESIAN_POINT ( 'NONE',  ( 3.158999515626020216, -1.670948785577108797, 1.441709373268922123 ) ) ;
#178960=CARTESIAN_POINT ( 'NONE',  ( 1.633988421434044325, 0.9753176276560069358, -1.713140426071022349 ) ) ;
#178961=CARTESIAN_POINT ( 'NONE',  ( 1.044460364342413072, 0.9324277726035223868, -2.110995228001291579 ) ) ;
#178962=CARTESIAN_POINT ( 'NONE',  ( 2.910546574502240968, 0.6583626327048962557, 1.848246418561696913 ) ) ;
#178963=CARTESIAN_POINT ( 'NONE',  ( 5.190308500716538376, 1.065014321051664048, -1.766232332728798538 ) ) ;
#178970=CARTESIAN_POINT ( 'NONE',  ( 0.7081837076810155729, 0.6824709381345904768, -2.061040276042750641 ) ) ;
#178976=CARTESIAN_POINT ( 'NONE',  ( 2.530351333283612281, 1.813318468827030072, 0.4585936022679508728 ) ) ;
#178977=CARTESIAN_POINT ( 'NONE',  ( 6.555963963954187790, 2.156316573842661732, -0.1517529999496904924 ) ) ;
#178978=CARTESIAN_POINT ( 'NONE',  ( -0.02264175331115856130, 5.720791440175713838, -2.683188945093956335 ) ) ;
#178979=CARTESIAN_POINT ( 'NONE',  ( 6.827182134110200806, 7.053609659044731472, 2.309100207511079805 ) ) ;
#178981=CARTESIAN_POINT ( 'NONE',  ( 2.191926089937683564, 1.177725938178806997, 1.506473034612793693 ) ) ;
#178982=CARTESIAN_POINT ( 'NONE',  ( 3.695971326421595204, -1.767833007231565334, -0.08711813594433276409 ) ) ;
#178983=CARTESIAN_POINT ( 'NONE',  ( 2.350135150926917493, 0.8998847150011926033, -1.687291145760522859 ) ) ;
#178986=CARTESIAN_POINT ( 'NONE',  ( 5.079654255714375566, -0.6853159911496645718, 1.789018848640187231 ) ) ;
#178987=CARTESIAN_POINT ( 'NONE',  ( 6.877413706903859669, -0.1509731808640407125, 1.936391978998742269 ) ) ;
#178989=CARTESIAN_POINT ( 'NONE',  ( 1.933984528066152953, -2.055706711753771287, 0.5200354980386610038 ) ) ;
#178990=CARTESIAN_POINT ( 'NONE',  ( 4.627732503263369601, -1.150995203733524930, -1.474563928533303869 ) ) ;
#178991=CARTESIAN_POINT ( 'NONE',  ( 2.103868193876055503, -1.825329726703457833, 0.04394198290156441783 ) ) ;
#178993=CARTESIAN_POINT ( 'NONE',  ( 4.670673364294657404, -1.443042178620690841, 1.669811033208345341 ) ) ;
#178996=CARTESIAN_POINT ( 'NONE',  ( 1.469262158920743966, 1.818092299969736425, 0.9742969159239748267 ) ) ;
#179005=CARTESIAN_POINT ( 'NONE',  ( 4.615722581382986967, 0.4567890626981512270, -2.019179087418949692 ) ) ;
#179007=CARTESIAN_POINT ( 'NONE',  ( 2.460438939752376708, 0.9218109643280817389, 1.955300211207489980 ) ) ;
#179009=CARTESIAN_POINT ( 'NONE',  ( 1.682291859507994092, 1.040098842697153136, 1.731126528333865933 ) ) ;
#179015=CARTESIAN_POINT ( 'NONE',  ( 0.4093891192313535710, -1.913260280790154866, 0.6371585790938688598 ) ) ;
#179016=CARTESIAN_POINT ( 'NONE',  ( 4.599289333468261631, -0.5842463895667610041, 2.112197083089427885 ) ) ;
#179018=CARTESIAN_POINT ( 'NONE',  ( 4.183787391381143195, 1.853651273288700718, -0.4697857328580385960 ) ) ;
#179022=CARTESIAN_POINT ( 'NONE',  ( 2.671500097371417137, 1.427951006967288272, 1.423949442620517702 ) ) ;
#179025=CARTESIAN_POINT ( 'NONE',  ( 5.368053323270940425, 0.8530656342727646058, 1.498931087277301843 ) ) ;
#179031=CARTESIAN_POINT ( 'NONE',  ( 0.8837443060279138729, -1.967007789996034095, 0.6459356165888497925 ) ) ;
#179033=CARTESIAN_POINT ( 'NONE',  ( 4.547391301494094762, -1.654308909395687310, 0.7384720232115218330 ) ) ;
#179035=DIRECTION ( 'NONE',  ( -3.451266460341926649E-31, -5.200009205990155575E-32, 1.000000000000000000 ) ) ;
#179036=CARTESIAN_POINT ( 'NONE',  ( 6.147087800311862971, 0.1847020338378597137, 1.802040927518679281 ) ) ;
#179039=CARTESIAN_POINT ( 'NONE',  ( 3.310656966840678894, 1.981231107410564851, 0.9368519390955745152 ) ) ;
#179042=CARTESIAN_POINT ( 'NONE',  ( 0.9417639971489067952, 1.314929008279978495, 1.456166070238865018 ) ) ;
#179044=CARTESIAN_POINT ( 'NONE',  ( 5.185127790529111991, 1.568658432645179124, 1.099198482053822534 ) ) ;
#179050=CARTESIAN_POINT ( 'NONE',  ( 2.149508875876861236, -1.735919364271593546, -1.288018159417112729 ) ) ;
#179053=CARTESIAN_POINT ( 'NONE',  ( 1.992912282819898850, 1.589903476415389871, -0.8970392876451321884 ) ) ;
#179055=CARTESIAN_POINT ( 'NONE',  ( 4.383705365265609721, 1.192707349210776036, 1.382196219385352309 ) ) ;
#179057=CARTESIAN_POINT ( 'NONE',  ( 2.882959773793275726, -1.768624019741386277, -0.7279546805132871556 ) ) ;
#179059=CARTESIAN_POINT ( 'NONE',  ( 3.754321382136751595, -1.967203782747016128, -0.09899598954335629697 ) ) ;
#179061=CARTESIAN_POINT ( 'NONE',  ( 4.915543477551369556, -1.042145293856342914, -1.638595356941417114 ) ) ;
#179065=CARTESIAN_POINT ( 'NONE',  ( 5.256147377898004791, 0.8573370980917979223, -1.939729252509444279 ) ) ;
#179067=CARTESIAN_POINT ( 'NONE',  ( 3.211475575234080004, 1.509012206799903666, 1.174515185244667581 ) ) ;
#179070=CARTESIAN_POINT ( 'NONE',  ( 6.983263157960373668, 7.629137130509066722, 2.546189081643289942 ) ) ;
#179072=CARTESIAN_POINT ( 'NONE',  ( 4.951819039462027838, -1.425199631963388391, -1.421988410718623586 ) ) ;
#179074=CARTESIAN_POINT ( 'NONE',  ( 4.811078068098579408, 1.589968679568127596, 0.8971634079883783475 ) ) ;
#179075=CARTESIAN_POINT ( 'NONE',  ( 1.240778115703184303, -2.019486815914430355, -0.4554155650244652853 ) ) ;
#179079=CARTESIAN_POINT ( 'NONE',  ( 5.928550619183988957, 1.803260976426118489, 0.4972845834502263584 ) ) ;
#179087=CARTESIAN_POINT ( 'NONE',  ( 1.077107760077404830, 1.911388382048292645, 0.7958064784282170567 ) ) ;
#179089=CARTESIAN_POINT ( 'NONE',  ( 2.337658655405081110, 0.5614262474852428353, -2.041391482465891194 ) ) ;
#179092=CARTESIAN_POINT ( 'NONE',  ( 0.2683110675134177669, -0.8374301267611580224, -1.781048649993026700 ) ) ;
#179096=CARTESIAN_POINT ( 'NONE',  ( 6.670655732516626912, 7.629137130509076492, 2.426260288887295502 ) ) ;
#179097=CARTESIAN_POINT ( 'NONE',  ( 2.554944377107245757, -1.995129818168206226, -1.128553997664314412 ) ) ;
#179098=CARTESIAN_POINT ( 'NONE',  ( 0.3811277156573149583, 1.704729334087114578, -0.6539457117896372296 ) ) ;
#179099=CARTESIAN_POINT ( 'NONE',  ( 1.880979024232478425, -1.749874716401520036, -0.7718601483891265325 ) ) ;
#179103=CARTESIAN_POINT ( 'NONE',  ( 2.021741635325131625, -0.4369018484469379682, 1.965087169840364245 ) ) ;
#179104=CARTESIAN_POINT ( 'NONE',  ( 0.9538670997781794059, -0.7113550649951918547, 1.828410001767373450 ) ) ;
#179108=CARTESIAN_POINT ( 'NONE',  ( 4.558587588987070838, -1.867386427489168055, -0.9401465391167336261 ) ) ;
#179109=CARTESIAN_POINT ( 'NONE',  ( 4.029968384200533826, 0.9465192177370416182, -1.495271383057869441 ) ) ;
#179112=CARTESIAN_POINT ( 'NONE',  ( 6.210887435761151210, -0.2868632742878024500, 2.274177813689901573 ) ) ;
#179113=CARTESIAN_POINT ( 'NONE',  ( 4.839680888265717407, 1.736017449284636527, 0.1234091131117609486 ) ) ;
#179116=CARTESIAN_POINT ( 'NONE',  ( 4.288270029534011485, -1.659180151977168283, 0.5033209731903751649 ) ) ;
#179117=CARTESIAN_POINT ( 'NONE',  ( 4.439989079487234314, 1.414935287217274684, 1.646911713943682409 ) ) ;
#179119=CARTESIAN_POINT ( 'NONE',  ( 5.471888747823221877, -0.9023485654677811940, 1.803414228490702209 ) ) ;
#179120=CARTESIAN_POINT ( 'NONE',  ( 5.437500000000002665, 1.451031289060892737, -1.451031289061332608 ) ) ;
#179123=CARTESIAN_POINT ( 'NONE',  ( 3.329043352767379282, 0.04595412404927168293, 1.925998307505512486 ) ) ;
#179125=CARTESIAN_POINT ( 'NONE',  ( 0.04794026018281431767, -2.028123841075918588, 0.9064578031776747702 ) ) ;
#179127=CARTESIAN_POINT ( 'NONE',  ( 6.883263157960382905, 3.691751545928231959, 2.560365603790202282 ) ) ;
#179130=CARTESIAN_POINT ( 'NONE',  ( 6.602011099637477010, 0.7519813002578833450, -1.812223124677159181 ) ) ;
#179138=CARTESIAN_POINT ( 'NONE',  ( 5.670399732568969675, -0.9243551164253935859, -1.844019960785907797 ) ) ;
#179143=CARTESIAN_POINT ( 'NONE',  ( 0.1745949693968693039, 0.009193469831081376581, -1.755468632744116686 ) ) ;
#179144=CARTESIAN_POINT ( 'NONE',  ( 5.924387396467542644, -1.262448726827345435, -1.189203582418095761 ) ) ;
#179145=CARTESIAN_POINT ( 'NONE',  ( 4.968161617874263136, -1.641142972212021656, -0.5799033918824270106 ) ) ;
#179147=CARTESIAN_POINT ( 'NONE',  ( 3.017397247018727580, -2.208655522623126366, 0.6135670354654331193 ) ) ;
#179149=CARTESIAN_POINT ( 'NONE',  ( 1.148114065366242498, -1.452583890646602205, 1.131155481815901753 ) ) ;
#179152=CARTESIAN_POINT ( 'NONE',  ( 2.274178591966895091, -1.125271047149905890, 1.437439779654096750 ) ) ;
#179153=CARTESIAN_POINT ( 'NONE',  ( 2.988907892087853568, -2.013985899409028946, 0.1017507309580278629 ) ) ;
#179154=CARTESIAN_POINT ( 'NONE',  ( 1.482659311839970684, -0.3241159351022730450, -2.167229700873399612 ) ) ;
#179156=CARTESIAN_POINT ( 'NONE',  ( 4.823321527849568469, -0.1059641466341002675, 2.103426968240690087 ) ) ;
#179159=CARTESIAN_POINT ( 'NONE',  ( 1.838419004579601834, -1.109345826794335688, 1.747895861591180156 ) ) ;
#179162=CARTESIAN_POINT ( 'NONE',  ( 3.774183692772983267, 2.104302197123971485, -0.2610650231627819062 ) ) ;
#179163=CARTESIAN_POINT ( 'NONE',  ( 6.375623774462673587, 1.745513195383348926, -0.5351242734627087438 ) ) ;
#179170=CARTESIAN_POINT ( 'NONE',  ( 3.797132494115144308, -0.2020087959641834463, -2.009684039814496170 ) ) ;
#179171=CARTESIAN_POINT ( 'NONE',  ( 1.026558790958994383, 1.254618057004111886, -1.691278660206218420 ) ) ;
#179174=CARTESIAN_POINT ( 'NONE',  ( 4.856225966575771658, -1.860502807761035715, -0.04838197303517684927 ) ) ;
#179181=CARTESIAN_POINT ( 'NONE',  ( 2.646866301197240645, -0.3325320220872363675, -1.933311746529025266 ) ) ;
#179182=CARTESIAN_POINT ( 'NONE',  ( 1.323354039402934390, -0.05256100377049736927, 2.161234000603563299 ) ) ;
#179186=CARTESIAN_POINT ( 'NONE',  ( 3.057622914094188626, 1.488722154369751083, -0.8884403576015533766 ) ) ;
#179187=CARTESIAN_POINT ( 'NONE',  ( 1.974151807821213245, -0.08369685440555743594, -1.738446472377056740 ) ) ;
#179188=CARTESIAN_POINT ( 'NONE',  ( 0.3765545373161778286, 1.332373789618445770, 1.883912488508274752 ) ) ;
#179191=CARTESIAN_POINT ( 'NONE',  ( 2.723961130741957781, -1.183836802208296568, -1.686624133856133412 ) ) ;
#179194=CARTESIAN_POINT ( 'NONE',  ( 0.6146109705059289441, 0.6351056948852469297, -1.913509406280079705 ) ) ;
#179195=CARTESIAN_POINT ( 'NONE',  ( 6.925078400183548588, 3.689301810296021777, 2.558360072861276979 ) ) ;
#179197=CARTESIAN_POINT ( 'NONE',  ( 1.604304721248978494, -0.7076282383621353977, -1.840268529672415498 ) ) ;
#179198=CARTESIAN_POINT ( 'NONE',  ( 4.834190613173367623, -1.027981871586785889, -1.612434056610718480 ) ) ;
#179204=CARTESIAN_POINT ( 'NONE',  ( 1.647134723225437636, 0.2000593722277475561, 2.009751748981201569 ) ) ;
#179206=CARTESIAN_POINT ( 'NONE',  ( 4.577368073103933455, 0.004851830007264032810, -2.307758714736147798 ) ) ;
#179207=CARTESIAN_POINT ( 'NONE',  ( 5.951606347324345236, 1.484592722905058393, 1.282605414028796353 ) ) ;
#179208=CARTESIAN_POINT ( 'NONE',  ( 2.377722661024490147, -1.904092233959910896, 0.4717398701708991893 ) ) ;
#179211=CARTESIAN_POINT ( 'NONE',  ( 0.9193374879241524855, -1.911445915896703207, 0.9111208566532496000 ) ) ;
#179214=CARTESIAN_POINT ( 'NONE',  ( 0.4976878544296211571, -0.6176706345307935164, -1.734562967469073014 ) ) ;
#179216=CARTESIAN_POINT ( 'NONE',  ( 3.854478708947015164, -2.168323188329326801, -0.1120144502513506779 ) ) ;
#179218=CARTESIAN_POINT ( 'NONE',  ( 2.180079139336263516, 2.078761533942363737, -0.4183221158333137457 ) ) ;
#179222=CARTESIAN_POINT ( 'NONE',  ( 2.917317126705867736, -0.2052410828034083035, 2.050554836033135597 ) ) ;
#179224=CARTESIAN_POINT ( 'NONE',  ( 0.4679805871025365382, -1.733519288248483559, -0.6209854868195128219 ) ) ;
#179226=CARTESIAN_POINT ( 'NONE',  ( 0.07735805125223639556, 7.629137130509110243, -2.688903128390319530 ) ) ;
#179228=CARTESIAN_POINT ( 'NONE',  ( 0.4170028235400899397, 1.518763190251697370, -1.601383572969114599 ) ) ;
#179229=CARTESIAN_POINT ( 'NONE',  ( 2.864839704461724867, -1.562160111903969417, 1.636705750015782224 ) ) ;
#179231=CARTESIAN_POINT ( 'NONE',  ( 2.144508837627901343, 1.757922920557394519, 0.4371675498636724000 ) ) ;
#179233=CARTESIAN_POINT ( 'NONE',  ( 1.797909001537282503, -0.9065369449853509787, -1.687681949719927577 ) ) ;
#179235=CARTESIAN_POINT ( 'NONE',  ( 3.314952806421948672, -1.569539724514938950, 1.350292352848787569 ) ) ;
#179237=CARTESIAN_POINT ( 'NONE',  ( 1.305477374917118016, -0.4809445013957516779, 1.911780493352131183 ) ) ;
#179238=CARTESIAN_POINT ( 'NONE',  ( 0.4109946218407485308, 1.674316264148696165, 0.9526004100348076653 ) ) ;
#179239=CARTESIAN_POINT ( 'NONE',  ( 2.483090063216564669, 1.711211315118581711, -0.7561169667836544761 ) ) ;
#179240=CARTESIAN_POINT ( 'NONE',  ( 1.313548042387347348, 2.037171730821058624, 1.084164666379479502 ) ) ;
#179242=CARTESIAN_POINT ( 'NONE',  ( 3.086215985183130339, 1.036139677906501300, -1.545717422611452729 ) ) ;
#179244=CARTESIAN_POINT ( 'NONE',  ( 5.107907679073590224, 0.6501100083472023394, -1.957599679411163196 ) ) ;
#179248=CARTESIAN_POINT ( 'NONE',  ( -0.02264175331115856477, -0.002534049983802035520, -2.089079740194145440 ) ) ;
#179251=CARTESIAN_POINT ( 'NONE',  ( 6.327428285124779173, -2.037722512857220725, 0.7216720553550812767 ) ) ;
#179252=CARTESIAN_POINT ( 'NONE',  ( 0.7492455685023796663, 1.839184785914184994, -0.09005233288367914257 ) ) ;
#179253=CARTESIAN_POINT ( 'NONE',  ( 5.110023566311792997, -0.7249756751233800145, 1.885263354437803240 ) ) ;
#179258=CARTESIAN_POINT ( 'NONE',  ( 6.825078400183548055, 2.475450427997231362, 2.140471860334830279 ) ) ;
#179261=CARTESIAN_POINT ( 'NONE',  ( 5.102750050473856547, 1.865045247124358818, 0.7672954931761333253 ) ) ;
#179266=CARTESIAN_POINT ( 'NONE',  ( 6.104392421991035711, -0.7735064434604683736, -2.018760209060527888 ) ) ;
#179271=CARTESIAN_POINT ( 'NONE',  ( 5.343375128634678006, 0.3905785925618041610, -1.978055652833633271 ) ) ;
#179273=B_SPLINE_CURVE_WITH_KNOTS ( 'NONE', 3,
 ( #194732, #14894, #112489, #159048, #161181, #12767, #80988, #110365, #78842, #60469, #196866, #128758, #144962, #210968, #47445, #178499, #114624, #146019, #95132, #30109, #31185, #209901, #62596, #147077, #11713, #96200, #213098, #10640, #63673, #180614, #143908, #13836, #193666, #61539, #94070, #195809, #179564, #44244, #113561, #126626, #32239, #97258, #64728, #76716, #130871, #192589, #176370, #127705, #27977, #160111, #45309, #111427, #177432, #98310, #49548, #119961, #99379, #68977, #167574, #36496, #20237, #202173, #164374, #116743, #182743, #34361, #200054, #168634, #135096, #19173, #1841, #185936, #214137, #100434, #134044, #166505, #51703, #201110, #18096, #183816, #761, #184870, #52750, #132971, #150272, #84184, #118884, #53831, #15959, #83105, #65765, #115673, #131911, #67900, #149186, #102574, #117826, #86322, #35426, #82042, #101504, #197920, #181668, #148136, #165432, #85247, #2905, #198973, #33295, #152394, #3973, #17028, #66828, #70040, #50618, #136156, #151336, #88474, #23438, #174011, #104725, #140456, #122116, #7185, #172930, #125314, #155600, #72184, #9343, #38647, #153464, #40799, #169702, #87397, #189160, #206467, #6113, #190213, #25582, #103652, #123199, #73257, #154533, #5037, #171845, #121047, #71112, #8268, #90618, #138292, #37571, #21292, #205394, #137229, #124255, #74352, #41873, #204307, #188081, #107984, #156675, #39710, #89549, #105819, #203250, #54894, #187015, #55964, #91693, #139363, #106905, #57032, #24507, #58094, #157746, #170773, #75416, #22362, #141529, #207537, #59156, #127457, #144724, #63431, #210736, #179328, #209655, #94885, #194491, #79675, #61296, #160937, #112250, #64496, #12532, #11466, #163077, #192340, #92755, #46134, #109048, #178261, #158800, #212860, #43999, #29874, #110117, #97023, #95958, #78604, #93823, #10397, #111183, #60222, #76471, #162012, #13602, #77539, #191273, #175067, #62361, #193428, #145790, #176129, #211794, #26654, #129584, #195570, #80752, #45072, #177187, #28800, #142581, #42939, #208587, #143661, #47206, #128522, #113321, #30949, #14659, #146840, #27728, #126381, #159864, #196630, #18912, #152143, #131676, #101244, #199801, #68724, #52499, #36234, #84996, #184617, #168386, #118632, #100186, #1585, #16781, #51446, #34114, #3710, #32003, #132723, #166251, #66581, #83926, #167326, #198728, #67646, #33060, #130638, #99138, #50374, #17841, #114384, #102312, #182486, #19982, #115439, #98084, #147891, #164139, #150015, #181430, #151087, #133793, #134846, #117566, #48271, #116497, #183560, #200850, #81809, #35167, #180379, #86066, #2651, #15723, #213907, #65530, #197678, #49323, #165188, #82865, #148941, #514, #70851, #74093, #202993, #121851, #54632, #40536, #135895, #139100, #156414, #106639, #104463, #187823, #123996, #39449, #189963, #120779, #172667, #24244, #206206, #88205, #153203, #154277, #138032, #41613, #6921, #136965, #53566, #4773, #185683, #21033, #173751, #186758, #107725, #105544, #71923, #204046, #90345, #171578, #25329, #56771, #5852, #23174, #8002, #89288, #57834, #55696, #155338, #72998, #140185, #205128, #122937, #188894, #38382, #91429, #170511, #22093, #157491, #69787, #201913, #169448, #119700, #37312, #103386, #87131, #210477, #76217, #129339, #62115, #127200, #126122, #191017, #143398, #12273, #10141, #78349, #9085, #174818, #108792 ),
 .UNSPECIFIED., .F., .F.,
 ( 4, 1, 1, 1, 1, 1, 1, 1, 1, 1, 1, 1, 1, 1, 1, 1, 1, 1, 1, 1, 1, 1, 1, 1, 1, 1, 1, 1, 1, 1, 1, 1, 1, 1, 1, 1, 1, 1, 1, 1, 1, 1, 1, 1, 1, 1, 1, 1, 1, 1, 1, 1, 1, 1, 1, 1, 1, 1, 1, 1, 1, 1, 1, 1, 1, 1, 1, 1, 1, 1, 1, 1, 1, 1, 1, 1, 1, 1, 1, 1, 1, 1, 1, 1, 1, 1, 1, 1, 1, 1, 1, 1, 1, 1, 1, 1, 1, 1, 1, 1, 1, 1, 1, 1, 1, 1, 1, 1, 1, 1, 1, 1, 1, 1, 1, 1, 1, 1, 1, 1, 1, 1, 1, 1, 1, 1, 1, 1, 1, 1, 1, 1, 1, 1, 1, 1, 1, 1, 1, 1, 1, 1, 1, 1, 1, 1, 1, 1, 1, 1, 1, 1, 1, 1, 1, 1, 1, 1, 1, 1, 1, 1, 1, 1, 1, 1, 1, 1, 1, 1, 1, 1, 1, 1, 1, 1, 1, 1, 1, 1, 1, 1, 1, 1, 1, 1, 1, 1, 1, 1, 1, 1, 1, 1, 1, 1, 1, 1, 1, 1, 1, 1, 1, 1, 1, 1, 1, 1, 1, 1, 1, 1, 1, 1, 1, 1, 1, 1, 1, 1, 1, 1, 1, 1, 1, 1, 1, 1, 1, 1, 1, 1, 1, 1, 1, 1, 1, 1, 1, 1, 1, 1, 1, 1, 1, 1, 1, 1, 1, 1, 1, 1, 1, 1, 1, 1, 1, 1, 1, 1, 1, 1, 1, 1, 1, 1, 1, 1, 1, 1, 1, 1, 1, 1, 1, 1, 1, 1, 1, 1, 1, 1, 1, 1, 1, 1, 1, 1, 1, 1, 1, 1, 1, 1, 1, 1, 1, 1, 1, 1, 1, 1, 1, 1, 1, 1, 1, 1, 1, 1, 1, 1, 1, 1, 1, 1, 1, 1, 1, 1, 1, 1, 1, 1, 1, 1, 1, 1, 1, 1, 1, 1, 1, 1, 1, 1, 1, 1, 1, 1, 1, 1, 1, 1, 1, 1, 1, 1, 1, 1, 1, 1, 1, 1, 1, 1, 1, 1, 1, 1, 1, 1, 1, 1, 1, 1, 1, 1, 1, 1, 1, 1, 1, 1, 1, 1, 1, 1, 1, 1, 1, 1, 1, 1, 4 ),
 ( 0.000000000000000000, 0.002599878613971510263, 0.005208762566300055921, 0.007813076245110234588, 0.01041697056762492211, 0.01302017924898362516, 0.01562522799165661294, 0.01822895742955179393, 0.02083332403451576206, 0.02343772221867868391, 0.02604143078293654281, 0.02864626161639613477, 0.03124961764961396021, 0.03385452714844047750, 0.03645799780571232912, 0.03906266225314121432, 0.04166671052383312535, 0.04427076094224517699, 0.04687542278318937439, 0.04947889361195772356, 0.05208380280015859759, 0.05468715921365963767, 0.05729198803509916865, 0.05989568673917144287, 0.06250009379223495087, 0.06510449848632135494, 0.06770819839843210397, 0.07031302545632363288, 0.07291638160390327694, 0.07552129054917994244, 0.07812475961953217751, 0.08072942239586503033, 0.08333346963797970408, 0.08593751866472883194, 0.08854217935802578821, 0.09114564884740632145, 0.09375055680876714925, 0.09635391199924973893, 0.09895873945611717570, 0.1015624370353711836, 0.1041668426700886191, 0.1067712463110160465, 0.1093749448896196713, 0.1119797708301935452, 0.1145831257515418783, 0.1171880334468678037, 0.1197915013940491491, 0.1223961628153678316, 0.1250002090321265524, 0.1276042567216372492, 0.1302089163955687523, 0.1328123846563000476, 0.1354172914881497103, 0.1380206455552074885, 0.1406254717515977581, 0.1432291683081768907, 0.1458335726268597532, 0.1484379753169847160, 0.1510416726638619811, 0.1536464975900906083, 0.1562498513865758776, 0.1588547579349887939, 0.1614582248604825021, 0.1640628850295551278, 0.1666669303230295940, 0.1692709767774011609, 0.1718756355346959253, 0.1744791026682601387, 0.1770840084736199360, 0.1796873615186004858, 0.1822921865574477218, 0.1848958821930496710, 0.1875002852981585977, 0.1901046871399069693, 0.1927083833567690418, 0.1953132073715553307, 0.1979165601445126987, 0.2005214656490191816, 0.2031249316542690642, 0.2057295906738217384, 0.2083336351460475244, 0.2109376804673406547, 0.2135423384106908962, 0.2161458045185324639, 0.2187507094003866837, 0.2213540615246011867, 0.2239588855088016361, 0.2265625803250888304, 0.2291669823190463362, 0.2317713834148095453, 0.2343750786033309830, 0.2369799018095430365, 0.2395832536602726381, 0.2421881582238437913, 0.2447916234102597566, 0.2473962813829825302, 0.2500003251359625422, 0.2526043694262022354, 0.2552090266582678346, 0.2578124918417971090, 0.2604173959030967600, 0.2630207472078238129, 0.2656255702402394725, 0.2682292643388430320, 0.2708336653240377978, 0.2734380657761767419, 0.2760417600379992398, 0.2786465825384744077, 0.2812499335682448476, 0.2838548372938197173, 0.2864583017627815864, 0.2890629587913320364, 0.2916670019270400371, 0.2942710452882197347, 0.2968757019116316509, 0.2994791662722288139, 0.3020840696158954564, 0.3046874202023847622, 0.3072922423858477359, 0.3098959358683710530, 0.3125003359471613118, 0.3151047358580104651, 0.3177084292947467969, 0.3203132511922952008, 0.3229166015023476888, 0.3255215044928377321, 0.3281249683456989308, 0.3307296245327063788, 0.3333336671530912065, 0.3359377096871765112, 0.3385423658045411677, 0.3411458294435600336, 0.3437507321724898035, 0.3463540821419661686, 0.3489589035792820537, 0.3515625965473047621, 0.3541669958220223235, 0.3567713952938928457, 0.3593750880071304721, 0.3619799094045394461, 0.3645832590960911834, 0.3671881614543835437, 0.3697916247924753486, 0.3723962802405443862, 0.3750003224475334518, 0.3776043642564660408, 0.3802090199703688222, 0.3828124829891406122, 0.3854173852062082184, 0.3880207346598750218, 0.3906255554538268782, 0.3932292480089087938, 0.3958336465818629857, 0.3984380457170473289, 0.4010417378083525053, 0.4036465588083897882, 0.4062499079826380477, 0.4088548098116001062, 0.4114582727362346981, 0.4140629275479489335, 0.4166669694434522730, 0.4192710106291533956, 0.4218756660421624782, 0.4244791285419997062, 0.4270840303500617607, 0.4296873793891050619, 0.4322921996424575197, 0.4348958918861421385, 0.4375002898596233591, 0.4401046887603987101, 0.4427083803313200949, 0.4453132010367379379, 0.4479165497948640051, 0.4505214511973463787, 0.4531249138098211726, 0.4557295680877478938, 0.4583336097736617210, 0.4609376504380365280, 0.4635423056527069874, 0.4661457677349071238, 0.4687506692368063055, 0.4713540179623986193, 0.4739588377779012651, 0.4765625298117197040, 0.4791669272880037522, 0.4817713260566358624, 0.4843750172087082362, 0.4869798377222476216, 0.4895831861654201811, 0.4921880872442612742, 0.4947915496458628049, 0.4973962034925555886, 0.5000002450707665691, 0.5026042853157074441, 0.5052089404345847523, 0.5078124022004342208, 0.5104173034990032720, 0.5130206520123070657, 0.5156254714926987726, 0.5182291634181735995, 0.5208335604995248946, 0.5234379592382720769, 0.5260416500730202838, 0.5286464704974140894, 0.5312498187267931105, 0.5338547195848227789, 0.5364581818768299204, 0.5390628353948335727, 0.5416668769672219330, 0.5442709168946127107, 0.5468755720202369552, 0.5494790335710144635, 0.5520839347690799093, 0.5546872831712518215, 0.5572921024192640793, 0.5598957943379132551, 0.5625001911265891108, 0.5651045899377058479, 0.5677082805566486812, 0.5703131009946261765, 0.5729164491113668545, 0.5755213498514099024, 0.5781248121350983649, 0.5807294654269519185, 0.5833335070953961088, 0.5859375468071157389, 0.5885422020420250089, 0.5911456634790059894, 0.5937505646793920233, 0.5963539130715860281, 0.5989587321899475514, 0.6015624242032879820, 0.6041668208015419372, 0.6067712197872831004, 0.6093749102919370220, 0.6119797308462270324, 0.6145830789514836745, 0.6171879796763642956, 0.6197914420530098445, 0.6223960952212510556, 0.6250001370876311357, 0.6276041766855571247, 0.6302088321322918407, 0.6328122935567517260, 0.6354171948622837629, 0.6380205433456558328, 0.6406253624370956690, 0.6432290546466469250, 0.6458334511567334069, 0.6484378504193577530, 0.6510415409112403351, 0.6536463616845760161, 0.6562497098795055939, 0.6588546106920506462, 0.6614580732629331550, 0.6640627264101022220, 0.6666667685763031370, 0.6692708081623160998, 0.6718754639234225667, 0.6744789254366408970, 0.6770838269501499029, 0.6796871756258610064, 0.6822919947931124218, 0.6848956873004010681, 0.6875000838245786117, 0.6901044834663523364, 0.6927081740469867022, 0.6953129951421085364, 0.6979163435278744609, 0.7005212445309179081, 0.7031247073973251327, 0.7057293606259679164, 0.7083334031938842701, 0.7109374428698714832, 0.7135420990479055536, 0.7161455607511696408, 0.7187504625754957965, 0.7213538115447158949, 0.7239586308905210377, 0.7265623237970838533, 0.7291667204376187650, 0.7317711205608201652, 0.7343748113317387638, 0.7369796328513985584, 0.7395829815291747877, 0.7421878828255610294, 0.7447913460887924941, 0.7473959995014650692, 0.7500000425730045661, 0.7526040824408628538, 0.7552087391383944803, 0.7578122011330034047, 0.7604171033709996586, 0.7630204527349119248, 0.7656252723620247114, 0.7682289657694127971, 0.7708333626285834850, 0.7734377633355060677, 0.7760414543982535607, 0.7786462764452187768, 0.7812496255161931469, 0.7838545272087811266, 0.7864579909701516769, 0.7890626446694239959, 0.7916666883465109938, 0.7942707285081521684, 0.7968753858277685120, 0.7994788482150362308, 0.8020837509695725176, 0.8046871008293766669, 0.8072919208405671121, 0.8098956148503495545, 0.8125000120304503026, 0.8151044134234068927, 0.8177081048795449281, 0.8203129275566022338, 0.8229162771219805661, 0.8255211793136476572, 0.8281246436744912343, 0.8307292977629509023, 0.8333333421475307423, 0.8359373827048843797, 0.8385420407491936956, 0.8411455036304537058, 0.8437504070044209437, 0.8463537574613370085, 0.8489585779593948889, 0.8515622726731627568, 0.8541666702765071673, 0.8567710724578335713, 0.8593747644089445581, 0.8619795878189033811, 0.8645829379799131464, 0.8671878407735589267, 0.8697913058352330085, 0.8723959604154888359, 0.8750000056095312839, 0.8776040466645483873, 0.8802087055361843548, 0.8828121690127931354, 0.8854170731091063340, 0.8880204242643787715, 0.8906252453521178447, 0.8932289408714879642, 0.8958333390004131758, 0.8984377420724726226, 0.9010414346201626179, 0.9036462588658594752, 0.9062496097237539017, 0.9088545132223035949, 0.9114579790861923048, 0.9140626342608790811, 0.9166666803663815477, 0.9192707220210388774, 0.9218753818226663732, 0.9244788459960084914, 0.9270837509176034219, 0.9296871028724987829, 0.9322919246527909820, 0.9348956210794385768, 0.9375000198362011261, 0.9401044239011964176, 0.9427081171475072408, 0.9453129423329229564, 0.9479162939871883520, 0.9505211982878988275, 0.9531246650646376661, 0.9557293209618126228, 0.9583333680330715643, 0.9609374102905526849, 0.9635420713365114853, 0.9661455366701111602, 0.9687504417289087844, 0.9713537931426093897, 0.9739586182492501187, 0.9765623229037746489, 0.9791667147516245340, 0.9817710778420317697, 0.9843748014325267581, 0.9869798465897002826, 0.9895830499482988207, 0.9921869381715581193, 0.9947912477285243416, 0.9974001254724073062, 1.000000000000000000 ),
 .UNSPECIFIED. ) ;
#179274=CARTESIAN_POINT ( 'NONE',  ( 2.226796682701466246, -0.001291377463900899485, 1.725068445404242201 ) ) ;
#179279=CARTESIAN_POINT ( 'NONE',  ( 0.3152201331171593512, -1.737291786998166332, 0.3363950369540784080 ) ) ;
#179280=CARTESIAN_POINT ( 'NONE',  ( 0.3463400477153228407, 1.033117966650568986, -1.727632672016335080 ) ) ;
#179282=CARTESIAN_POINT ( 'NONE',  ( 2.819571115601596123, -0.2173934082839618642, 2.196046946737562511 ) ) ;
#179284=CARTESIAN_POINT ( 'NONE',  ( 5.032167298026094748, 1.244454833084396306, 1.778855100471810280 ) ) ;
#179288=CARTESIAN_POINT ( 'NONE',  ( 3.334745777049468618, 1.343786929377327466, -1.640352557257473309 ) ) ;
#179289=CARTESIAN_POINT ( 'NONE',  ( 1.651970485933237143, 1.039013645561959853, 1.727991324714774013 ) ) ;
#179290=CARTESIAN_POINT ( 'NONE',  ( 2.566445574732978407, 0.6140501124722294035, 1.704450811836472734 ) ) ;
#179296=CARTESIAN_POINT ( 'NONE',  ( 0.8838324889288513564, -1.915903395820263366, 0.003361870754229472590 ) ) ;
#179305=CARTESIAN_POINT ( 'NONE',  ( 5.418883921851007202, 1.995750516393671514, 0.8311057252617033431 ) ) ;
#179308=CARTESIAN_POINT ( 'NONE',  ( 2.443736651115399283, -1.977012053918187906, 0.7674769708189137507 ) ) ;
#179311=CARTESIAN_POINT ( 'NONE',  ( 3.813711686511447763, -1.942732367404787830, 0.3338136033803756342 ) ) ;
#179312=CARTESIAN_POINT ( 'NONE',  ( 5.291234991620994421, -0.05314252713351996088, -1.911838368980276925 ) ) ;
#179315=CARTESIAN_POINT ( 'NONE',  ( 6.848121164528643945, -0.8440317545377834518, 1.778091661420333702 ) ) ;
#179316=CARTESIAN_POINT ( 'NONE',  ( 1.499837725185527049, -0.6986378101729547874, -1.812093905146118233 ) ) ;
#179321=CARTESIAN_POINT ( 'NONE',  ( 2.888710413438722924, 1.792813287458893790, -1.075199139784080771 ) ) ;
#179325=CARTESIAN_POINT ( 'NONE',  ( 5.654919265238161685, 0.3773621422162172223, 1.874504418562010999 ) ) ;
#179327=CARTESIAN_POINT ( 'NONE',  ( 4.582781371344160526, -2.140174514510746029, -0.5380331057033281850 ) ) ;
#179328=CARTESIAN_POINT ( 'NONE',  ( 3.592985822966657583, -0.4282699184722462693, -2.164648485658649868 ) ) ;
#179331=CARTESIAN_POINT ( 'NONE',  ( 1.928230879603441750, -0.9027140558476205445, -1.685813393195116694 ) ) ;
#179334=CARTESIAN_POINT ( 'NONE',  ( 4.404779037558821386, 0.5491149005726041477, 1.996164414091922135 ) ) ;
#179336=CARTESIAN_POINT ( 'NONE',  ( 1.745224485312408813, -1.826185749030174499, 1.156423465944363294 ) ) ;
#179337=CARTESIAN_POINT ( 'NONE',  ( 3.316156725143477146, 1.388770557483296697, -1.695381604771596606 ) ) ;
#179344=CARTESIAN_POINT ( 'NONE',  ( 0.0006249722829775038483, -1.976948959267275541, 0.3961041280396286890 ) ) ;
#179346=CARTESIAN_POINT ( 'NONE',  ( 5.137584473783054051, 1.933663220787355419, -0.7400441640052906056 ) ) ;
#179347=CARTESIAN_POINT ( 'NONE',  ( 2.895051130818243834, 1.652057846050537515, -0.9908002393040680200 ) ) ;
#179348=CARTESIAN_POINT ( 'NONE',  ( 6.257425474675967436, 2.026018168931587482, -0.6146651352928398371 ) ) ;
#179351=CARTESIAN_POINT ( 'NONE',  ( 4.100420354389649802, 1.959567862165834562, 0.1972540966053982214 ) ) ;
#179352=CARTESIAN_POINT ( 'NONE',  ( 6.333931935734662844, 2.266371222927834772, 0.3428166536569366984 ) ) ;
#179353=CARTESIAN_POINT ( 'NONE',  ( 4.125493313500066428, -1.746467973620144720, 0.5319596651164605339 ) ) ;
#179359=CARTESIAN_POINT ( 'NONE',  ( 1.083273795380396143, -0.8277460070302902206, 1.644747122058511035 ) ) ;
#179360=CARTESIAN_POINT ( 'NONE',  ( 5.537363252524067470, -0.04518311473342268708, 2.012845415592057208 ) ) ;
#179361=CARTESIAN_POINT ( 'NONE',  ( 6.363951117287210302, -0.1083456013219602776, -2.296273276487709847 ) ) ;
#179362=CARTESIAN_POINT ( 'NONE',  ( 5.963715375765575644, -0.4800653121489819042, 1.901962685674676301 ) ) ;
#179367=CARTESIAN_POINT ( 'NONE',  ( 1.312182373965790072, 1.401635355298202379, -1.551525349546636123 ) ) ;
#179368=CARTESIAN_POINT ( 'NONE',  ( 0.2154177506630133854, -1.835460468737951878, 0.3602540799089171131 ) ) ;
#179370=CARTESIAN_POINT ( 'NONE',  ( 5.578056150152780113, -1.895089194937165100, -0.4233685073328739557 ) ) ;
#179371=CARTESIAN_POINT ( 'NONE',  ( -0.2102771530458225069, 7.629137130509110243, -2.803678522703976661 ) ) ;
#179372=CARTESIAN_POINT ( 'NONE',  ( 0.7139227764019463462, 1.607345104371117772, 0.6680024673673248259 ) ) ;
#179376=CARTESIAN_POINT ( 'NONE',  ( 1.875234852168044641, 1.651158054356154148, -0.4988350824523117844 ) ) ;
#179377=CARTESIAN_POINT ( 'NONE',  ( 1.909981697816802049, -1.036543071415759298, -1.930953618257096993 ) ) ;
#179378=CARTESIAN_POINT ( 'NONE',  ( 6.884150274805287850, -0.1404709382532287054, 1.702994612897957394 ) ) ;
#179379=CARTESIAN_POINT ( 'NONE',  ( 3.844505992619148937, 2.196175933995975438, 0.2170506636963928093 ) ) ;
#179381=CARTESIAN_POINT ( 'NONE',  ( 1.235490768065301337, -0.05108008202716606688, -2.170608684345101125 ) ) ;
#179382=CARTESIAN_POINT ( 'NONE',  ( 0.09986456629675066754, -1.825204794925545881, -0.04862044751281074939 ) ) ;
#179383=CARTESIAN_POINT ( 'NONE',  ( 2.026704517097451586, 0.4691240347775883501, 2.064561701657470660 ) ) ;
#179384=CARTESIAN_POINT ( 'NONE',  ( 6.539320575229250032, 4.701774335136183147, 2.359470009949143243 ) ) ;
#179387=CARTESIAN_POINT ( 'NONE',  ( 2.613130667218881431, -0.2215951064345271782, 2.281621536969838271 ) ) ;
#179391=CARTESIAN_POINT ( 'NONE',  ( 4.670683837814712192, 0.8496151569591952057, 2.052583376702998397 ) ) ;
#179398=CARTESIAN_POINT ( 'NONE',  ( 2.479138880926802901, -2.011204309026824344, -0.1455328587063598189 ) ) ;
#179400=CARTESIAN_POINT ( 'NONE',  ( 2.377848133335142222, -2.001750602163259174, 0.4968105773679451498 ) ) ;
#179405=CARTESIAN_POINT ( 'NONE',  ( 4.628971764384363752, -2.004251508290517680, 0.8866568735110615940 ) ) ;
#179406=CARTESIAN_POINT ( 'NONE',  ( 2.461564753630896440, -1.930417925741171103, -0.5826551686555282439 ) ) ;
#179407=CARTESIAN_POINT ( 'NONE',  ( 2.313779677144182312, 1.201330555204615180, -1.395457044143719072 ) ) ;
#179410=CARTESIAN_POINT ( 'NONE',  ( 5.104447739783800841, -0.6163660037172628003, -1.718524672285254740 ) ) ;
#179411=CARTESIAN_POINT ( 'NONE',  ( 5.537732479266092689, -1.587839044716709669, 1.242724925242834066 ) ) ;
#179413=CARTESIAN_POINT ( 'NONE',  ( 6.174757231500850096, -2.146110616029934803, -0.7165941539545512828 ) ) ;
#179415=CARTESIAN_POINT ( 'NONE',  ( 1.067171494879548987, -1.904794536548588546, -0.8987870243707897222 ) ) ;
#179426=CARTESIAN_POINT ( 'NONE',  ( 3.287547529179511319, 0.05108950329585186523, -2.220969887641692342 ) ) ;
#179430=CARTESIAN_POINT ( 'NONE',  ( 2.787496613063783713, -1.831585881375777713, 0.7034878451678548972 ) ) ;
#179437=CARTESIAN_POINT ( 'NONE',  ( 1.898838059644195386, -2.080654286433290867, -0.4088066060855889972 ) ) ;
#179439=CARTESIAN_POINT ( 'NONE',  ( 3.889662759143839299, 1.564074849111227516, 1.492423382767386730 ) ) ;
#179440=CARTESIAN_POINT ( 'NONE',  ( 2.559893532628489954, -1.268187297466142338, 1.335118840784771166 ) ) ;
#179443=CARTESIAN_POINT ( 'NONE',  ( 5.349435159262297290, 1.738085940734758639, -0.09086515553361101949 ) ) ;
#179446=CARTESIAN_POINT ( 'NONE',  ( 3.133815226704575796, -1.450665623810345473, -1.602838778681405785 ) ) ;
#179447=CARTESIAN_POINT ( 'NONE',  ( 4.358749857130030492, -0.7741967591250037417, 1.861731939633674893 ) ) ;
#179450=CARTESIAN_POINT ( 'NONE',  ( 2.254944280175336324, -1.671361177491991201, 1.370965666894090385 ) ) ;
#179451=CARTESIAN_POINT ( 'NONE',  ( 2.987526725409937800, 1.391544230491305933, 1.396620715705886084 ) ) ;
#179452=CARTESIAN_POINT ( 'NONE',  ( 6.509000000000012776, 0.5843741663743782233, 2.053293374786519188 ) ) ;
#179453=CARTESIAN_POINT ( 'NONE',  ( 4.528815305949091652, -1.774144813887452266, 0.7903587577767021699 ) ) ;
#179462=CARTESIAN_POINT ( 'NONE',  ( 1.202499378025536636, -2.206952907257493823, 0.001246274542086866404 ) ) ;
#179464=CARTESIAN_POINT ( 'NONE',  ( 4.698074428120575519, 0.8425069249109422564, -1.771795133841248981 ) ) ;
#179468=CARTESIAN_POINT ( 'NONE',  ( 0.07479286986305545837, 0.7422478802248284602, -1.939684878352589070 ) ) ;
#179470=CARTESIAN_POINT ( 'NONE',  ( 3.732213890823964597, 0.2717154217161937280, 1.820854149191558635 ) ) ;
#179475=CARTESIAN_POINT ( 'NONE',  ( 5.396778611113259849, -2.069399493756381769, -0.4625044129713885011 ) ) ;
#179479=CARTESIAN_POINT ( 'NONE',  ( 6.397740692956204178, -0.6987371234766488470, 1.938827229339795455 ) ) ;
#179482=CARTESIAN_POINT ( 'NONE',  ( 1.504125588540955683, 1.858726126767410669, 0.09586466133617438379 ) ) ;
#179483=CARTESIAN_POINT ( 'NONE',  ( 3.280630368989821743, 1.663260157205956880, -0.7901080472864712156 ) ) ;
#179488=CARTESIAN_POINT ( 'NONE',  ( 2.860232119962682784, 2.196193069775736362, -0.2169517147150926140 ) ) ;
#179489=CARTESIAN_POINT ( 'NONE',  ( 6.204402397823557180, -0.8056473179405240215, -2.114295379420629839 ) ) ;
#179491=CARTESIAN_POINT ( 'NONE',  ( 6.381129877538572970, -1.660329982341423705, -0.7251259014357125388 ) ) ;
#179492=CARTESIAN_POINT ( 'NONE',  ( 5.137857799264941683, 1.913235287650059790, -0.1005462703686579862 ) ) ;
#179494=CARTESIAN_POINT ( 'NONE',  ( 6.420764531294745225, 1.746252128813120086, 0.6712297951826234899 ) ) ;
#179496=CARTESIAN_POINT ( 'NONE',  ( 5.723074792265875566, -1.682715607417185399, -0.7953119777529999990 ) ) ;
#179498=CARTESIAN_POINT ( 'NONE',  ( 6.719637426148988624, -1.715392417075599196, 0.4352852820774539833 ) ) ;
#179499=CARTESIAN_POINT ( 'NONE',  ( 1.411342602523330214, -1.897109289313268166, 0.6839406069230756779 ) ) ;
#179501=CARTESIAN_POINT ( 'NONE',  ( 2.947987317136715468, 0.7576180897185936791, -1.965265766029665295 ) ) ;
#179507=CARTESIAN_POINT ( 'NONE',  ( 2.883074275722704360, -1.867829236092366951, -0.7691044946091238899 ) ) ;
#179511=CARTESIAN_POINT ( 'NONE',  ( 3.181113218772323226, -0.1555236193923059951, -2.156033859764289407 ) ) ;
#179516=CARTESIAN_POINT ( 'NONE',  ( 0.6608746330511162670, -0.7316962540516893654, -2.044312434917434640 ) ) ;
#179521=CARTESIAN_POINT ( 'NONE',  ( 1.769323484426460480, 2.095969018468134770, -0.6401429536977767398 ) ) ;
#179522=CARTESIAN_POINT ( 'NONE',  ( 2.395744609331447172, 1.748901261223069437, 1.435362524944477025 ) ) ;
#179531=CARTESIAN_POINT ( 'NONE',  ( 2.653260118625869080, 0.4764888685691510140, -1.704286641089979959 ) ) ;
#179532=CARTESIAN_POINT ( 'NONE',  ( 6.598651186688741177, -0.5821561243712966016, -2.128545807824663960 ) ) ;
#179535=CARTESIAN_POINT ( 'NONE',  ( 4.692982559244565088, 1.755779632255444422, 0.9913831279167032440 ) ) ;
#179537=CARTESIAN_POINT ( 'NONE',  ( 3.819104250046548632, -0.1383300533824398659, 1.865606469731183825 ) ) ;
#179538=CARTESIAN_POINT ( 'NONE',  ( 3.748938768049938197, -0.3990674421511587466, -2.031259957477090428 ) ) ;
#179543=CARTESIAN_POINT ( 'NONE',  ( 1.195406425308798148, 1.765864799226088744, -0.7346160280939582066 ) ) ;
#179544=CARTESIAN_POINT ( 'NONE',  ( 2.435929278166943490, 1.204617592564939166, 1.548422000036096202 ) ) ;
#179545=CARTESIAN_POINT ( 'NONE',  ( 1.352888501574830205, -0.9090079681693465918, 1.799646022210943386 ) ) ;
#179549=CARTESIAN_POINT ( 'NONE',  ( 6.362572844203587152, -1.395794784517788045, 1.392370165595870679 ) ) ;
#179551=CARTESIAN_POINT ( 'NONE',  ( 2.390887483786011014, -1.927808053674067823, -0.5802275739894193762 ) ) ;
#179553=CARTESIAN_POINT ( 'NONE',  ( 2.372804174479496986, -0.3651721903723912921, -2.085361659519912259 ) ) ;
#179555=CARTESIAN_POINT ( 'NONE',  ( 3.420434311836465291, 0.9283866757503267397, 1.850595421526677775 ) ) ;
#179557=CARTESIAN_POINT ( 'NONE',  ( 6.228480176075449570, 0.2035102421588113053, 2.080708833908810451 ) ) ;
#179559=CARTESIAN_POINT ( 'NONE',  ( 4.014527796464135712, 1.291161025869846712, -1.290856679043244970 ) ) ;
#179564=CARTESIAN_POINT ( 'NONE',  ( 6.211994372536747022, -2.190858219723303524, 0.2640275128017176565 ) ) ;
#179567=CARTESIAN_POINT ( 'NONE',  ( 5.356085673312771966, 0.7711821229579116643, -1.750063228584404440 ) ) ;
#179575=CARTESIAN_POINT ( 'NONE',  ( 0.9426144736941791669, -1.451487892885485742, -1.132780452900377099 ) ) ;
#179577=CARTESIAN_POINT ( 'NONE',  ( 4.973830807571049561, 1.075732564348480746, 1.530087412091485799 ) ) ;
#179584=CARTESIAN_POINT ( 'NONE',  ( 1.375766793938013821, -1.922594530582939942, 0.4262983161763284623 ) ) ;
#179585=CARTESIAN_POINT ( 'NONE',  ( 2.038685622454153190, -1.556895902704044765, 1.281378572682637218 ) ) ;
#179589=CARTESIAN_POINT ( 'NONE',  ( 2.677880624963273171, -1.125664371729949265, 1.880105217535378959 ) ) ;
#179599=CARTESIAN_POINT ( 'NONE',  ( 4.440845869443198701, -1.426288408191313639, -1.164454570719307469 ) ) ;
#179600=CARTESIAN_POINT ( 'NONE',  ( 2.315091943819780340, 1.615584347832084600, -1.200805960377361981 ) ) ;
#179601=CARTESIAN_POINT ( 'NONE',  ( 2.900137762625193183, 0.2794712830477152354, 2.281260185934708140 ) ) ;
#179603=CARTESIAN_POINT ( 'NONE',  ( 1.815070623055618615, -1.592837743320011601, -0.9620759905232498799 ) ) ;
#179606=CARTESIAN_POINT ( 'NONE',  ( 5.220932206144772714, 1.444093599275039885, -1.253800916539760113 ) ) ;
#179609=CARTESIAN_POINT ( 'NONE',  ( 4.862875367868015886, 0.2033134212856284595, -2.080814050062954390 ) ) ;
#179610=CARTESIAN_POINT ( 'NONE',  ( 3.379631771358857950, 1.185797501207178861, 1.446808710765794315 ) ) ;
#179612=CARTESIAN_POINT ( 'NONE',  ( 5.724118993814841794, 1.776208094789998304, 0.4848738846057951135 ) ) ;
#179617=CARTESIAN_POINT ( 'NONE',  ( 4.881344157179084320, 1.607756147011094150, -0.6252594192169037557 ) ) ;
#179622=CARTESIAN_POINT ( 'NONE',  ( 4.276368498475341617, -1.111101898244113872, -1.865058090000100366 ) ) ;
#179623=CARTESIAN_POINT ( 'NONE',  ( 3.721172816245840842, -0.1328194893376876962, 1.820914920514608459 ) ) ;
#179624=CARTESIAN_POINT ( 'NONE',  ( 1.358172466202983042, -1.961936380284023063, -0.005482119489134959674 ) ) ;
#179625=CARTESIAN_POINT ( 'NONE',  ( 5.700440484604645697, 1.420036636931173657, -1.570746850784213056 ) ) ;
#179627=CARTESIAN_POINT ( 'NONE',  ( 6.181209693220585777, 1.577568176048673720, 1.663411239723869173 ) ) ;
#179631=CARTESIAN_POINT ( 'NONE',  ( 2.069135417989849568, -1.637292086295978111, 1.347470637625711731 ) ) ;
#179637=CARTESIAN_POINT ( 'NONE',  ( 6.104372708633159839, 2.168188666507598228, 0.1146961476086311021 ) ) ;
#179638=CARTESIAN_POINT ( 'NONE',  ( 6.883263157960349155, 7.052567563008111051, 2.551962282169925711 ) ) ;
#179640=CARTESIAN_POINT ( 'NONE',  ( 2.579030809547431247, -1.529751724882743247, 1.610829425214066246 ) ) ;
#179641=ORIENTED_EDGE ( 'NONE', *, *, #143420, .T. ) ;
#179642=CARTESIAN_POINT ( 'NONE',  ( 0.5636314131802122596, -1.270468259257762966, 1.915555708879124852 ) ) ;
#179644=CARTESIAN_POINT ( 'NONE',  ( 5.559457797297955750, 1.683061182826322666, 1.192002683324727252 ) ) ;
#179650=CARTESIAN_POINT ( 'NONE',  ( 5.794452930745782382, 1.501506822132542718, -1.065412412061928160 ) ) ;
#179653=CARTESIAN_POINT ( 'NONE',  ( 1.535739282219195978, 0.8544175402723229729, -1.498188246372294863 ) ) ;
#179654=CARTESIAN_POINT ( 'NONE',  ( 1.551970632248239612, 1.040795554343958429, 1.727062486439542965 ) ) ;
#179655=CARTESIAN_POINT ( 'NONE',  ( 1.547921954348607354, -1.621480451111120047, 1.629585861659810009 ) ) ;
#179657=CARTESIAN_POINT ( 'NONE',  ( 2.284789498180723744, -2.218439058979736700, -0.4430748376489759832 ) ) ;
#179658=CARTESIAN_POINT ( 'NONE',  ( 4.600280035732231987, -2.105589688358105782, -0.05227242994678206467 ) ) ;
#179660=CARTESIAN_POINT ( 'NONE',  ( 2.108344674345350445, 1.315072395666099236, -1.184512757523252358 ) ) ;
#179666=CARTESIAN_POINT ( 'NONE',  ( 5.924141181918635368, -2.204746212865996480, 0.2713366554644781603 ) ) ;
#179667=CARTESIAN_POINT ( 'NONE',  ( 3.714928722721734911, -0.1615716889580356697, 2.185543052782303874 ) ) ;
#179670=CARTESIAN_POINT ( 'NONE',  ( 6.498696114369957755, -2.079444522786470184, -0.4142970760486197612 ) ) ;
#179674=CARTESIAN_POINT ( 'NONE',  ( 6.029554895997981667, -0.2579198037528374066, 2.104758538420265168 ) ) ;
#179679=CARTESIAN_POINT ( 'NONE',  ( 5.847170753249844033, 0.5281823367668266878, -1.763884204139199330 ) ) ;
#179684=CARTESIAN_POINT ( 'NONE',  ( 2.190578792945916842, 1.345991196328416573, 1.103389618610579381 ) ) ;
#179690=CARTESIAN_POINT ( 'NONE',  ( 6.807524309086420367, -0.4794501827766698421, 2.115671360755105646 ) ) ;
#179694=CARTESIAN_POINT ( 'NONE',  ( 6.034075718726629844, 1.069613854859407631, -1.878468107683453514 ) ) ;
#179699=CARTESIAN_POINT ( 'NONE',  ( 5.905538618093676639, -0.4813517389176332206, 1.911553968036589390 ) ) ;
#179700=CARTESIAN_POINT ( 'NONE',  ( 4.850818353276647343, -0.8162368348260983231, 1.529697846671844941 ) ) ;
#179702=CARTESIAN_POINT ( 'NONE',  ( 2.349409277133751139, 0.5813161652389825518, -2.113004480973964760 ) ) ;
#179703=CARTESIAN_POINT ( 'NONE',  ( 3.470030448073280205, 2.251904571161921442, -0.5032320387977330389 ) ) ;
#179704=CARTESIAN_POINT ( 'NONE',  ( 5.430957059787441032, 0.1471976826952873518, 2.055563341089384988 ) ) ;
#179705=CARTESIAN_POINT ( 'NONE',  ( 0.9197484630441244979, 1.157134895311136669, -1.559417598425276719 ) ) ;
#179710=CARTESIAN_POINT ( 'NONE',  ( 3.498385214435925317, -1.041973313016024472, 1.846846941210858351 ) ) ;
#179711=CARTESIAN_POINT ( 'NONE',  ( 1.934220422044398813, -1.621183349045727473, -1.198859219795316955 ) ) ;
#179713=CARTESIAN_POINT ( 'NONE',  ( 4.928867898441261275, 2.110505041808665716, 0.6446608841527908806 ) ) ;
#179716=CARTESIAN_POINT ( 'NONE',  ( 0.09986456629675066754, -1.825204794925545881, -0.04862044751281074939 ) ) ;
#179722=CARTESIAN_POINT ( 'NONE',  ( 4.768464766973178115, -1.347833537202504317, 1.559116658007191347 ) ) ;
#179724=CARTESIAN_POINT ( 'NONE',  ( 6.620655732516624425, 7.629137130509072051, 2.773739711112707784 ) ) ;
#179727=CARTESIAN_POINT ( 'NONE',  ( 3.721357204503534355, 1.733397938510993885, 1.036269837853747378 ) ) ;
#179731=CARTESIAN_POINT ( 'NONE',  ( 3.063408159219972227, 0.3037436250956357386, -2.038260327603860222 ) ) ;
#179736=CARTESIAN_POINT ( 'NONE',  ( -0.2411972340275969906, 1.382285239182699854, -2.157708601731861187 ) ) ;
#179737=CARTESIAN_POINT ( 'NONE',  ( 1.446930991382020748, 0.5358794165791405106, -1.761430032344503349 ) ) ;
#179738=CARTESIAN_POINT ( 'NONE',  ( 6.287735281038357549, 1.518688880046001444, 1.601449620450722700 ) ) ;
#179740=CARTESIAN_POINT ( 'NONE',  ( 2.354944161360218224, -1.672559397656541824, 1.369352967626968898 ) ) ;
#179742=CARTESIAN_POINT ( 'NONE',  ( 1.727750297885573882, 0.7672897036171549834, -1.865047645237365215 ) ) ;
#179744=CARTESIAN_POINT ( 'NONE',  ( 0.3209005354254980680, -0.09642172165634513292, 1.868300368337752815 ) ) ;
#179745=CARTESIAN_POINT ( 'NONE',  ( 5.014510501881845883, 1.360076575639699081, -1.427402630902480762 ) ) ;
#179746=CARTESIAN_POINT ( 'NONE',  ( 4.733611406029458735, 0.6279933214467496860, -1.916352419866963697 ) ) ;
#179750=CARTESIAN_POINT ( 'NONE',  ( 6.393207918867057415, 1.833407501889987357, -1.036277073347695588 ) ) ;
#179752=CARTESIAN_POINT ( 'NONE',  ( 6.162566008723842081, -0.7415158119226210598, -1.933206815039355320 ) ) ;
#179756=CARTESIAN_POINT ( 'NONE',  ( 4.065273027966066266, 0.2426392691956253123, -1.956424757721614949 ) ) ;
#179757=CARTESIAN_POINT ( 'NONE',  ( 6.222917004181202749, 1.493787235515126044, -1.359621011941100743 ) ) ;
#179759=CARTESIAN_POINT ( 'NONE',  ( 4.969473931871945638, 0.2302171888925855225, -2.296178194122914018 ) ) ;
#179761=CARTESIAN_POINT ( 'NONE',  ( 1.885666897375902096, -1.943580278752204515, 0.6908589954031388869 ) ) ;
#179768=CARTESIAN_POINT ( 'NONE',  ( 3.947858391199970285, 1.570127341852745273, 1.499791163327832466 ) ) ;
#179770=CARTESIAN_POINT ( 'NONE',  ( 2.665370095338463585, 0.9869154847663293983, 1.554228294351194473 ) ) ;
#179772=CARTESIAN_POINT ( 'NONE',  ( 5.636325218313963603, 0.4264374063192889475, 2.149501299143250055 ) ) ;
#179774=CARTESIAN_POINT ( 'NONE',  ( 6.438354578037611908, 2.236760482230481184, 0.3397759937929164531 ) ) ;
#179778=CARTESIAN_POINT ( 'NONE',  ( 0.08049558579637566824, -0.1306036352819762714, -1.740669940395103366 ) ) ;
#179780=CARTESIAN_POINT ( 'NONE',  ( 4.547525146836687959, -1.839596654198237369, 0.8179813495266550216 ) ) ;
#179782=CARTESIAN_POINT ( 'NONE',  ( 3.030406611367501224, 1.171151514522270398, -1.750062178063223506 ) ) ;
#179783=CARTESIAN_POINT ( 'NONE',  ( 2.618635445852790511, 0.2369565241663183774, 1.900835938982778472 ) ) ;
#179785=CARTESIAN_POINT ( 'NONE',  ( 2.611712457634679296, 0.5281755657932221126, -1.897318813625125777 ) ) ;
#179786=CARTESIAN_POINT ( 'NONE',  ( 1.481098450213329976, 1.729700800547562478, -0.7128637423776186255 ) ) ;
#179787=CARTESIAN_POINT ( 'NONE',  ( 1.574581288703358339, 1.320057194528483135, -1.451483715152704246 ) ) ;
#179788=CARTESIAN_POINT ( 'NONE',  ( 4.494587217144647262, -0.3816326207147257010, -1.681953545215847168 ) ) ;
#179789=CARTESIAN_POINT ( 'NONE',  ( -0.1405747822309927342, -1.479430311965252542, -1.211566217618691210 ) ) ;
#179791=CARTESIAN_POINT ( 'NONE',  ( 0.9267433102794273569, 1.311770220233858586, -1.774563083084364834 ) ) ;
#179795=CARTESIAN_POINT ( 'NONE',  ( 6.578970801323708706, -0.09418725797194843485, -1.868394071727994321 ) ) ;
#179798=CARTESIAN_POINT ( 'NONE',  ( 6.596543124887806364, 2.046857425119428697, 0.3097440254393943881 ) ) ;
#179799=CARTESIAN_POINT ( 'NONE',  ( 0.6958625912084138720, -1.462932864358768459, -1.465259690088885014 ) ) ;
#179804=CARTESIAN_POINT ( 'NONE',  ( 5.725269513181780567, 1.870077439114096629, 0.9995941271150191598 ) ) ;
#179809=CARTESIAN_POINT ( 'NONE',  ( 6.672321430365630412, -0.9237476215336395402, -1.730755693189582667 ) ) ;
#179811=CARTESIAN_POINT ( 'NONE',  ( 4.288435361214689046, -1.930121902525683053, 0.5825675424541224556 ) ) ;
#179812=CARTESIAN_POINT ( 'NONE',  ( 3.766719225569253204, -0.1932013629946625344, -1.905979854919868988 ) ) ;
#179814=CARTESIAN_POINT ( 'NONE',  ( 1.628746693258641853, 0.2190750365392846177, 2.180598679842937759 ) ) ;
#179816=CARTESIAN_POINT ( 'NONE',  ( 2.864352374448192240, -1.292745417840788003, 1.352161534859085412 ) ) ;
#179820=CARTESIAN_POINT ( 'NONE',  ( 5.343409318383084639, 0.4121200312635669993, -2.076573192147526115 ) ) ;
#179822=CARTESIAN_POINT ( 'NONE',  ( 2.823863332701610940, 1.159264052448713889, -1.739707760033171180 ) ) ;
#179824=CARTESIAN_POINT ( 'NONE',  ( 0.5688600258280833710, 0.1761389027815796759, -1.715759018540372827 ) ) ;
#179835=CARTESIAN_POINT ( 'NONE',  ( 1.523755425131537278, -1.797796875034236797, 0.2216367714752715545 ) ) ;
#179839=CARTESIAN_POINT ( 'NONE',  ( 6.639320575229252341, 0.005161017367553630275, 1.896863882003448021 ) ) ;
#179844=CARTESIAN_POINT ( 'NONE',  ( 2.998338655031260735, 1.846661096025622228, 0.2305314943511579950 ) ) ;
#179845=CARTESIAN_POINT ( 'NONE',  ( 0.8607750341611281053, -0.04820650858186093651, -1.915179348411770954 ) ) ;
#179846=CARTESIAN_POINT ( 'NONE',  ( 6.563506682682211490, 0.3285509523427312950, -1.898022546839329472 ) ) ;
#179853=CARTESIAN_POINT ( 'NONE',  ( 4.909022984592102290, -1.584153972474154459, 1.169931220002416339 ) ) ;
#179854=CARTESIAN_POINT ( 'NONE',  ( 1.682450335255514240, 1.092831414372618326, 1.817064408815848964 ) ) ;
#179857=CARTESIAN_POINT ( 'NONE',  ( 6.246043798300164873, 0.6838514278588082584, 2.082077653496945402 ) ) ;
#179859=CARTESIAN_POINT ( 'NONE',  ( 4.770489386553291133, -1.258480429039417592, 1.458564191902473661 ) ) ;
#179861=CARTESIAN_POINT ( 'NONE',  ( 0.2350025537052654601, -1.671451849548213797, 0.7345932495873632728 ) ) ;
#179862=CARTESIAN_POINT ( 'NONE',  ( 1.172829962703396456, -1.397616723802884708, 1.707921395779465890 ) ) ;
#179868=CARTESIAN_POINT ( 'NONE',  ( 6.473500209388782345, -0.2444377345085078923, 1.954170833970412913 ) ) ;
#179869=CARTESIAN_POINT ( 'NONE',  ( 1.962350597898457671, -1.776395552165145997, -0.7852436748517297449 ) ) ;
#179870=CARTESIAN_POINT ( 'NONE',  ( 6.556073970538053075, 2.004588421764907036, -1.124284452974108950 ) ) ;
#179872=CARTESIAN_POINT ( 'NONE',  ( 5.910971410920907942, -1.467885462018687415, 1.143791174867914373 ) ) ;
#179878=CARTESIAN_POINT ( 'NONE',  ( 1.962683346935737205, -2.005255389829229351, -0.8846387633431598285 ) ) ;
#179883=CARTESIAN_POINT ( 'NONE',  ( 1.541335573940459058, -1.321205422867760548, -1.260230113935792318 ) ) ;
#179888=CARTESIAN_POINT ( 'NONE',  ( 0.3285744372712772199, 1.843197283691574873, 0.5604049541020996728 ) ) ;
#179889=CARTESIAN_POINT ( 'NONE',  ( 4.030091663008243508, 1.086175826233202857, 1.633415718976807263 ) ) ;
#179893=CARTESIAN_POINT ( 'NONE',  ( 4.019203527901527018, -2.096847714747759106, 0.6372333828079318474 ) ) ;
#179895=CARTESIAN_POINT ( 'NONE',  ( 6.609000000000037289, 1.265604115953523401, 2.115306440354140172 ) ) ;
#179896=CARTESIAN_POINT ( 'NONE',  ( 4.276279003695676373, -1.059865903354087813, -1.778221194881628220 ) ) ;
#179900=CARTESIAN_POINT ( 'NONE',  ( 3.832918613053246659, 0.7734572015929435107, -2.164792806810557746 ) ) ;
#179906=CARTESIAN_POINT ( 'NONE',  ( 3.732312008210575627, 0.2860496425412931143, 1.920654750396868726 ) ) ;
#179910=CARTESIAN_POINT ( 'NONE',  ( 4.412309042748480792, -1.912102599942141268, -0.04143165621695726192 ) ) ;
#179912=CARTESIAN_POINT ( 'NONE',  ( 5.051616488536272875, 0.5384910649316194675, -1.638604462054549238 ) ) ;
#179913=CARTESIAN_POINT ( 'NONE',  ( 4.012907874177486178, 0.1037781579101039742, 2.014008197856680393 ) ) ;
#179914=CARTESIAN_POINT ( 'NONE',  ( 4.623847096394516853, 0.3921523929481546267, 2.264879156731691712 ) ) ;
#179916=CARTESIAN_POINT ( 'NONE',  ( 0.3642759247451561322, 2.182245240920151375, -0.3280614795862640820 ) ) ;
#179919=CARTESIAN_POINT ( 'NONE',  ( 6.309784262603465699, -1.756040378898944043, 0.2188775834443684731 ) ) ;
#179921=CARTESIAN_POINT ( 'NONE',  ( 1.887097267728707894, 1.992918150068530014, -1.132464722766779675 ) ) ;
#179922=CARTESIAN_POINT ( 'NONE',  ( 1.007268549873532981, -0.7791258169532075950, -1.556267712415648763 ) ) ;
#179924=CARTESIAN_POINT ( 'NONE',  ( 0.6843859445029027988, -0.9204285295532282918, -1.469136994349945047 ) ) ;
#179927=CARTESIAN_POINT ( 'NONE',  ( 1.785821596895339702, -2.044763721651895239, 0.7304308730638265912 ) ) ;
#179928=CARTESIAN_POINT ( 'NONE',  ( 2.255092540634635156, 0.09411513195021348199, -2.014433103604281960 ) ) ;
#179930=CARTESIAN_POINT ( 'NONE',  ( 0.07700591528353968596, 0.003617085621422307627, -1.910863332519038282 ) ) ;
#179932=CARTESIAN_POINT ( 'NONE',  ( 1.775925898354186572, 0.3739997881802308299, -2.189552662180799913 ) ) ;
#179939=CARTESIAN_POINT ( 'NONE',  ( 5.372502291033079302, -0.05049805449116586548, -1.739898325138872215 ) ) ;
#179940=CARTESIAN_POINT ( 'NONE',  ( 3.156644782993088150, -0.5669402238272451822, -1.878178299617596192 ) ) ;
#179945=CARTESIAN_POINT ( 'NONE',  ( 5.167352989974902222, 0.2290589858122368538, -2.250810084452478765 ) ) ;
#179946=CARTESIAN_POINT ( 'NONE',  ( 1.223174996406689585, -1.863865272486511460, -0.8838528460363299644 ) ) ;
#179948=CARTESIAN_POINT ( 'NONE',  ( 1.973834762636607509, 2.164947816325224039, -0.6572921511966890451 ) ) ;
#179951=CARTESIAN_POINT ( 'NONE',  ( 2.354581831802166736, -1.448805955455864769, 1.183207591018392568 ) ) ;
#179952=CARTESIAN_POINT ( 'NONE',  ( 1.599856272741075447, -0.2119130288822292651, 1.721036989116639493 ) ) ;
#179954=CARTESIAN_POINT ( 'NONE',  ( 5.355090213057959403, 0.4282289882464126451, -2.149144931432686256 ) ) ;
#179955=CARTESIAN_POINT ( 'NONE',  ( 0.4642757356001780966, 2.182421439735841684, -0.3260586787675948117 ) ) ;
#179956=CARTESIAN_POINT ( 'NONE',  ( 4.030267251519312310, 1.158562084521784108, -1.824840551714689507 ) ) ;
#179957=CARTESIAN_POINT ( 'NONE',  ( 4.576081071864527061, -1.884036987645235417, -0.4702585519323047025 ) ) ;
#179960=CARTESIAN_POINT ( 'NONE',  ( 2.031250000000000888, -0.7852924748300881275, -1.895863743164043491 ) ) ;
#179966=CARTESIAN_POINT ( 'NONE',  ( 5.414685466650038137, -1.281359335986744341, -1.556910257834144051 ) ) ;
#179970=CARTESIAN_POINT ( 'NONE',  ( 3.088313589057069208, -1.798746773638896457, -0.3115406389907551810 ) ) ;
#179977=CARTESIAN_POINT ( 'NONE',  ( 6.445964431295706731, -1.320945465521980555, -1.527872228271543342 ) ) ;
#179978=CARTESIAN_POINT ( 'NONE',  ( 1.225412164737609055, 1.871785320780447792, 0.9964087003688710809 ) ) ;
#179982=CARTESIAN_POINT ( 'NONE',  ( 6.737187473210400235, -1.842164534206979676, 0.9240717516781959961 ) ) ;
#179983=CARTESIAN_POINT ( 'NONE',  ( 6.557263107265463020, -1.238491779027944162, 1.591905563659588907 ) ) ;
#179992=CARTESIAN_POINT ( 'NONE',  ( 5.729842239849809893, -1.821464125411855761, -0.8645900286049985617 ) ) ;
#179993=CARTESIAN_POINT ( 'NONE',  ( 4.927609005033061429, 0.9437523325564222132, -1.580719041474540010 ) ) ;
#179994=CARTESIAN_POINT ( 'NONE',  ( -0.02319159430947542733, 0.7471999394491578572, -1.895068635927643630 ) ) ;
#179995=CARTESIAN_POINT ( 'NONE',  ( 2.948224681477436881, 0.8299853515197992415, -2.153443412361542020 ) ) ;
#179997=CARTESIAN_POINT ( 'NONE',  ( 5.958325562381369345, 0.8699925256120243366, 1.978967057501494820 ) ) ;
#179999=CARTESIAN_POINT ( 'NONE',  ( 1.171315778946733888, 1.157996810922466313, 1.558895349155087873 ) ) ;
#180003=CARTESIAN_POINT ( 'NONE',  ( 4.446792056507931079, 1.496784378905056334, 1.744297655265887537 ) ) ;
#180006=CARTESIAN_POINT ( 'NONE',  ( 4.258574955689950592, -1.386304660245713860, 1.256184814050688603 ) ) ;
#180007=CARTESIAN_POINT ( 'NONE',  ( 1.230557176020010912, 1.282188879665364656, -1.419081615486268433 ) ) ;
#180010=CARTESIAN_POINT ( 'NONE',  ( 2.262606014870732096, 0.9450075053254001212, 1.994452002680577429 ) ) ;
#180012=CARTESIAN_POINT ( 'NONE',  ( 0.1405533004714107914, -0.003749010675423137661, -2.279853246149381896 ) ) ;
#180017=CARTESIAN_POINT ( 'NONE',  ( 1.704304553464238703, -0.7057161435466070554, -1.840894384558971808 ) ) ;
#180018=CARTESIAN_POINT ( 'NONE',  ( 0.6577796130948220243, -1.951556776833747620, -1.231164357708439017 ) ) ;
#180019=CARTESIAN_POINT ( 'NONE',  ( 1.855835942623608181, -0.6640040153468586004, 1.846199708051485811 ) ) ;
#180020=CARTESIAN_POINT ( 'NONE',  ( 5.278211761479340680, -1.098870959053561469, -1.745292714083917174 ) ) ;
#180027=CARTESIAN_POINT ( 'NONE',  ( 1.411231479646192222, -1.713112901771263630, 1.333658509791965097 ) ) ;
#180032=CARTESIAN_POINT ( 'NONE',  ( 1.844777716111935861, -1.582881869529973562, 0.9963996312925410548 ) ) ;
#180033=CARTESIAN_POINT ( 'NONE',  ( 5.501312752317830679, 1.763641270444433307, 1.249554385337700024 ) ) ;
#180035=CARTESIAN_POINT ( 'NONE',  ( 0.07735805125223117751, 5.721077998510399887, -2.682987299736539377 ) ) ;
#180037=CARTESIAN_POINT ( 'NONE',  ( 1.910667195161031007, -0.5113573046386342691, -1.842555643073694238 ) ) ;
#180039=CARTESIAN_POINT ( 'NONE',  ( 3.537761123354207893, 0.7962651652904990662, -1.580685414113996545 ) ) ;
#180040=CARTESIAN_POINT ( 'NONE',  ( 0.9438406676962156627, -1.213610516764839664, -1.477797202995428938 ) ) ;
#180042=CARTESIAN_POINT ( 'NONE',  ( 5.677321882007140275, 1.453744714618950606, 1.247594701790984306 ) ) ;
#180043=CARTESIAN_POINT ( 'NONE',  ( 6.777801591175982132, -1.910752814866881089, 0.4773036857264860156 ) ) ;
#180045=CARTESIAN_POINT ( 'NONE',  ( 0.6859744409541921328, 2.042103856186634925, -0.5713114342573709648 ) ) ;
#180047=CARTESIAN_POINT ( 'NONE',  ( 4.557402362779487959, 0.4096945884842878582, -1.825068887194372991 ) ) ;
#180048=CARTESIAN_POINT ( 'NONE',  ( 0.8205984872286451459, 1.685833220154912881, 0.7012733028506010768 ) ) ;
#180050=CARTESIAN_POINT ( 'NONE',  ( 4.406973378220558679, 1.706932345810768359, -1.398813476408675260 ) ) ;
#180053=CARTESIAN_POINT ( 'NONE',  ( 1.522013433763437895, 2.032506561856410876, -0.3506121680386958261 ) ) ;
#180059=CARTESIAN_POINT ( 'NONE',  ( 0.1753634416057497647, 4.084635187426246539, -2.698744815386323381 ) ) ;
#180061=CARTESIAN_POINT ( 'NONE',  ( 3.736834853878097107, -1.994506513866915576, -0.5549897870569252545 ) ) ;
#180063=CARTESIAN_POINT ( 'NONE',  ( 2.038557401052975671, 2.137775048120754029, 0.3193135401893046899 ) ) ;
#180065=CARTESIAN_POINT ( 'NONE',  ( 2.086587641237521495, -1.240871089896943280, 1.593450946908819832 ) ) ;
#180072=CARTESIAN_POINT ( 'NONE',  ( -0.01248194115436446205, -0.5331630387654020531, 1.944732228473695868 ) ) ;
#180073=CARTESIAN_POINT ( 'NONE',  ( 4.950807510372833065, -1.851323926424643274, -1.172527737679923465 ) ) ;
#180075=CARTESIAN_POINT ( 'NONE',  ( 4.693567934957057375, 1.782326746607498791, -0.6936623114904352239 ) ) ;
#180079=CARTESIAN_POINT ( 'NONE',  ( 2.636342400811112707, 0.6820146075395253638, 1.897692325672148073 ) ) ;
#180081=CARTESIAN_POINT ( 'NONE',  ( 0.7148891103036036920, 2.120809155261915713, 0.8706237914077943341 ) ) ;
#180083=CARTESIAN_POINT ( 'NONE',  ( 4.700069144524660736, -1.724479993061514449, -0.04023236952926077803 ) ) ;
#180084=CARTESIAN_POINT ( 'NONE',  ( -0.1394461523060987751, 0.6550469493228279205, -2.357635998629922902 ) ) ;
#180088=CARTESIAN_POINT ( 'NONE',  ( 0.07680821025394038437, 7.629137130509076492, -2.410791881123967695 ) ) ;
#180090=CARTESIAN_POINT ( 'NONE',  ( 5.496671973222438723, -1.768653292081886708, -0.3907654940887676509 ) ) ;
#180095=CARTESIAN_POINT ( 'NONE',  ( 6.463521484642490655, -1.459484751789320134, -1.072804587801470921 ) ) ;
#180098=CARTESIAN_POINT ( 'NONE',  ( 2.695491272475036837, -0.6865090956127660737, 2.081212476921667776 ) ) ;
#180100=CARTESIAN_POINT ( 'NONE',  ( 6.760206150924522817, -1.860609546209352372, 0.04724569877399482920 ) ) ;
#180102=CARTESIAN_POINT ( 'NONE',  ( 3.585460515032745210, -0.5529844701629010872, 1.834067302312661241 ) ) ;
#180104=( BOUNDED_SURFACE ( )  B_SPLINE_SURFACE ( 3, 3, ( 
 ( #153797, #204647, #58429, #8597, #75742, #23778, #72527, #38979, #22695, #141854, #154867, #139704, #74679, #24846, #123525, #206796, #125643, #140782, #71449, #88809, #6449, #138622, #56297, #190543, #122457, #188416, #40052, #106162, #89883, #155935, #193745, #209981, #14977, #109385, #161263, #142916, #113645, #76795, #43266, #159124, #145047, #146103, #143989, #110445, #175391, #162332, #46452, #81073, #179650, #195895, #208916, #211049, #30192, #26977, #12850, #94152, #112574, #93082, #60550, #61622, #31270, #45392, #97345, #126708, #192670, #63751, #213184, #163402, #147159, #44323, #78924, #176447, #129910, #96282, #178584, #62675, #212114, #64814, #128834, #191604, #10725, #28059, #160192, #11792, #194816, #77866, #127791, #111508, #13917, #79998, #177514, #29127, #95214, #47532, #48590, #100522, #82127, #52838, #16044, #196950, #98393, #84271, #85340, #83190, #49637, #114706, #101590, #200138, #168723, #118974, #135183, #148221, #150357, #183901, #180701, #166596, #33382, #51791, #32325, #214222, #853, #184952, #133059, #36579, #65851, #132000, #2995, #152479, #102665, #20326, #198009, #18185, #115761, #69063, #149273, #86412, #181751, #201198, #4059, #130960, #99463, #164457, #35512, #19258, #34447, #165520, #167658, #50706, #17113, #151422, #66918, #199060, #116830, #182832, #1927, #67986, #134129, #117908, #74436, #70129, #39800, #186023, #5121, #203329, #56049, #188167, #202263, #187098, #25663, #58177, #21377, #136242, #170858, #122205, #105907, #124337, #106988, #72268, #88560, #53913, #22448, #120049, #155685, #154620, #139446, #87485, #173013, #71197, #24594, #37660, #6199, #90701, #40883, #140536, #171932, #104813, #137313, #54982, #206548, #38732, #23526, #156763, #138376, #121135, #8351, #91772, #190295, #205481, #41953, #108065, #153551, #204394, #103737, #89633, #7267, #169788, #157829, #174091, #73344, #57113, #123282, #189243, #97103, #59233, #26735, #47287, #75495, #78681, #93907, #194568, #129665, #111264, #159947, #94966, #113399, #46214, #161014, #193511, #109136, #28883, #13680, #79751, #143744, #12609, #92837, #9425, #179407, #175149, #192425, #158881, #141607, #144808, #207615, #11551, #178344, #210814, #145867, #77621, #10477, #61382, #76552, #209738, #208672, #211874, #60303, #142662, #126461, #63513, #125391, #44079, #62439, #127539, #112330, #128602, #110198, #191357, #176208, #27809, #29953, #195652, #45152, #177267, #96038, #162090, #31027, #43022, #180459, #32076, #98164, #116570, #101321, #197755, #133872, #67721, #164211, #80831, #114459, #81884, #16859, #34187, #99215, #167403, #199879, #1665, #33135, #17918, #85075, #183640, #165264, #51522, #49394, #35246, #117647, #18993, #15798, #212938, #118705, #147969, #213981, #151160, #82940, #48348, #2729, #166328, #68802, #132801, #100261, #65601, #134922, #131750, #115513, #149013, #84004, #589, #200928, #52576, #184693, #66655, #150094, #36313, #163155, #198804, #14739, #181506, #146920, #64575, #130717, #50452, #196708, #182564, #169527, #185757, #106720, #38466, #201987, #172747, #105627, #6997, #72001, #39529, #4852, #56849, #123021, #70931, #153275, #188972, #57911, #40616, #171656, #24322, #8086, #119777, #54710, #135971, #87211, #186834, #3787, #190040, #73075, #20057, #102392, #53644, #121932, #168459, #152218, #37390, #140267 ),
 ( #138112, #103465, #187899, #90428, #156497, #22172, #23253, #21107, #86147, #124076, #137040, #203067, #120861, #69862, #89366, #104542, #170587, #74175, #155414, #206287, #88287, #154351, #5929, #204123, #55775, #139176, #205207, #92584, #58982, #108871, #178079, #173828, #158626, #44895, #175950, #144550, #94711, #26474, #25405, #10223, #42764, #177006, #29697, #43824, #208413, #76297, #142405, #128349, #109941, #125138, #191095, #174894, #209474, #194316, #60047, #12348, #160753, #126202, #91507, #77364, #145617, #79498, #13423, #157568, #192164, #193248, #107803, #95779, #27546, #111001, #28623, #93641, #159684, #11285, #211613, #9161, #143478, #207362, #161835, #141347, #75237, #61116, #127276, #210557, #78428, #62193, #45957, #112078, #63249, #129410, #41692, #199626, #212680, #148769, #33942, #179145, #165011, #97905, #50204, #47023, #146666, #65353, #117396, #197504, #101070, #130465, #196455, #67478, #2479, #183393, #167157, #48098, #16606, #114210, #133624, #147712, #34998, #64321, #51272, #150917, #18744, #180208, #30768, #100017, #83755, #98960, #31830, #166081, #115263, #96848, #17669, #149847, #163966, #162895, #15542, #66411, #1416, #68555, #81627, #84829, #195393, #82687, #14478, #213730, #131500, #181256, #338, #113138, #49147, #80567, #32883, #132556, #198555, #116322, #182313, #120614, #188730, #171415, #136796, #153035, #52336, #20867, #200685, #5675, #86966, #203889, #151976, #23003, #69620, #89121, #134682, #4609, #155175, #105376, #138937, #186591, #169281, #135730, #201752, #204958, #37140, #21925, #39281, #55533, #88034, #6759, #122770, #137869, #3550, #118464, #90188, #19815, #103221, #53393, #184450, #71753, #36068, #70683, #72834, #154106, #56606, #202821, #119530, #38219, #185516, #104292, #54470, #40368, #170340, #121688, #187655, #106470, #102150, #172497, #24083, #156251, #7829, #168216, #85902, #57673, #193780, #74988, #212150, #64848, #78963, #29161, #61659, #45427, #163436, #145085, #91257, #157317, #8908, #30231, #15016, #111543, #47569, #195931, #141096, #206039, #25156, #210017, #211088, #162371, #12886, #81105, #113680, #129944, #161301, #146137, #213218, #97379, #62711, #179684, #177552, #147193, #31304, #130994, #127827, #123831, #32363, #95252, #128872, #196984, #194855, #173586, #48623, #80034, #114738, #46487, #13951, #112610, #180736, #98427, #178621, #96316, #164492, #73921, #140014, #63786, #189793, #41444, #107552, #182866, #49673, #888, #100556, #132034, #103774, #201233, #148254, #16078, #115798, #35547, #82161, #65886, #33420, #53948, #214255, #85375, #166627, #52874, #136277, #117942, #18219, #101625, #120087, #119010, #167692, #200170, #181786, #19293, #20362, #86446, #150390, #99498, #151457, #152511, #4096, #1959, #3029, #165555, #198044, #186062, #17148, #199092, #83224, #149307, #69097, #66955, #84305, #184988, #135221, #70166, #68022, #133094, #134161, #50738, #51824, #116864, #202297, #34482, #183935, #36614, #37698, #102701, #168758, #173045, #89668, #58214, #8385, #154652, #153587, #72306, #170892, #90735, #157867, #171969, #122243, #6234, #138411, #41991, #23560, #187136, #38765, #104846, #123312, #108099, #204432, #140572, #74467, #22484, #87522, #121167, #88595, #155719, #40915, #105945, #174128, #206585, #124372, #39838, #24628, #91809, #190330, #7304, #25701 ),
 ( #55018, #9460, #156798, #75532, #139486, #107021, #56085, #141643, #207652, #188201, #73380, #59273, #125429, #191394, #43059, #169826, #21412, #205514, #57146, #203366, #189276, #5157, #71233, #137348, #79788, #26772, #109172, #142701, #128640, #196746, #158919, #126498, #146957, #175185, #178379, #193546, #145902, #14776, #210851, #45188, #194605, #212972, #211911, #46249, #78719, #143780, #112367, #92873, #97139, #176244, #29988, #96074, #95005, #111303, #127578, #64613, #10515, #144845, #60338, #31064, #208710, #76590, #192462, #62477, #63548, #61415, #27846, #44115, #129704, #162127, #130752, #163193, #113436, #110236, #13715, #195686, #93944, #47323, #11586, #179443, #159984, #77658, #177306, #80867, #28920, #209775, #161051, #12647, #134963, #69905, #184730, #20100, #115550, #84049, #181546, #200971, #631, #102433, #65641, #118747, #3831, #86188, #131790, #98199, #167444, #151201, #166370, #197795, #101365, #182608, #164247, #19037, #85115, #214019, #15835, #33174, #133914, #2772, #136015, #99255, #52619, #48387, #17962, #81921, #49430, #165303, #34231, #150137, #180497, #16898, #114500, #36356, #82979, #32114, #149052, #67763, #66696, #132842, #100304, #198846, #1709, #50493, #168501, #116614, #199920, #51567, #152257, #148008, #117692, #183684, #35290, #68843, #40661, #186876, #185800, #104586, #203109, #123065, #190083, #204164, #154394, #38508, #170631, #74217, #55819, #4895, #70973, #137083, #155458, #140312, #22217, #172791, #106762, #187940, #121976, #5972, #25446, #119820, #171699, #153320, #124120, #87256, #53688, #169569, #7041, #156541, #72043, #120903, #37432, #24363, #56890, #91553, #41735, #206330, #54754, #73117, #90475, #103510, #23298, #88330, #189019, #21150, #138156, #39570, #107844, #105672, #173873, #89408, #139218, #57955, #9206, #157610, #75278, #205248, #8131, #202028, #79542, #93687, #195437, #158667, #211656, #96890, #113183, #10265, #191140, #46001, #29738, #44936, #76340, #194358, #61159, #42806, #112120, #178123, #92625, #108914, #208455, #12392, #95820, #14520, #60087, #145660, #141393, #111044, #174936, #142447, #126247, #127321, #177051, #59022, #43869, #162939, #129454, #192207, #26517, #78471, #161879, #193291, #47066, #13466, #143523, #159729, #125178, #27589, #207403, #144590, #11328, #210604, #109985, #63294, #175995, #179187, #77406, #209519, #30810, #28668, #94753, #160801, #62233, #128391, #81667, #84864, #197541, #182350, #199661, #149885, #33979, #35031, #68589, #116360, #184483, #118501, #52372, #212723, #115305, #17703, #146707, #134714, #147753, #1450, #83790, #31871, #165053, #2516, #82729, #200721, #15580, #213771, #167191, #102185, #36100, #168252, #65392, #100054, #131539, #18778, #32922, #80614, #97950, #150952, #64362, #130508, #164004, #196495, #51307, #183430, #198593, #49186, #133660, #375, #48137, #117432, #101105, #181295, #114251, #98998, #166118, #180247, #16645, #148806, #66449, #132591, #50240, #67515, #169317, #153070, #5712, #137904, #152010, #136830, #189829, #7868, #185552, #135765, #105414, #40404, #154144, #73956, #56641, #21963, #38254, #3582, #120648, #85938, #171452, #186627, #89157, #37181, #122805, #20901, #188764, #19851, #104328, #106506, #204997, #24117, #71789, #54504, #86997, #4647, #90220, #202856, #121725, #138974, #155210, #187690, #172533 ),
 ( #23041, #170376, #156284, #140048, #72868, #88071, #6791, #206073, #57707, #203923, #123864, #55571, #41478, #107588, #69657, #70717, #201788, #53428, #39319, #103256, #119565, #109727, #58769, #29479, #176789, #78215, #143267, #110787, #76085, #128131, #193023, #46811, #8944, #190885, #211404, #25193, #28404, #43609, #144338, #79286, #60902, #175734, #44675, #63034, #210338, #94498, #209257, #124923, #160536, #177867, #95570, #93429, #12142, #42551, #173621, #129201, #108654, #142186, #174682, #91297, #61977, #157355, #27327, #75024, #59834, #194094, #125987, #26255, #11067, #92372, #159468, #158409, #161620, #10009, #208201, #191944, #13213, #141136, #77146, #45744, #127061, #111862, #145404, #195178, #207146, #15328, #113998, #33725, #100856, #115049, #65143, #97691, #81418, #199408, #181047, #130251, #196242, #47885, #66194, #51053, #147499, #83538, #17454, #179993, #30552, #64109, #31616, #32663, #198345, #48930, #117176, #149620, #165868, #197290, #182094, #34782, #133403, #98742, #1202, #213520, #183178, #67264, #166941, #163749, #162685, #68338, #131299, #164800, #18534, #16392, #212465, #84611, #116103, #150700, #82471, #49985, #148561, #2262, #134470, #127, #132339, #200473, #112925, #178938, #99803, #96631, #14259, #80350, #146450, #85676, #36919, #136581, #167998, #139791, #22783, #184230, #52120, #151764, #53181, #187439, #40138, #54254, #4393, #103002, #20655, #138716, #120391, #69403, #135510, #201533, #5459, #204733, #86745, #88900, #171193, #119309, #35854, #3333, #185295, #186366, #137649, #202601, #56383, #154954, #105153, #38001, #121469, #188507, #72617, #104073, #6539, #152815, #122546, #106251, #172275, #169058, #101932, #7609, #70464, #170120, #23862, #21706, #87818, #89969, #55318, #156021, #153890, #203669, #71539, #73693, #118248, #39067, #19604, #11881, #161357, #160279, #60639, #77957, #111597, #8686, #158163, #24933, #190627, #75830, #107327, #79019, #176533, #123611, #205818, #91037, #10809, #57450, #41222, #74768, #29218, #189574, #126801, #141937, #28145, #177606, #93173, #207950, #76884, #95308, #94240, #143004, #175479, #157097, #209002, #210074, #61713, #125730, #192757, #140871, #173352, #12940, #206883, #174423, #58515, #124670, #44414, #42287, #59572, #108399, #92108, #110533, #9754, #25999, #43351, #191691, #109471, #27066, #127881, #159208, #144078, #193831, #45481, #62764, #47619, #148303, #64897, #33467, #198092, #129996, #128926, #113731, #194905, #96371, #63838, #213268, #16126, #81156, #83269, #49719, #115847, #15066, #214302, #67004, #165605, #147241, #99542, #179737, #17195, #149357, #938, #212202, #46542, #100601, #195986, #14000, #133141, #131044, #30286, #199141, #65933, #181833, #114786, #82210, #31354, #50785, #116914, #97429, #163483, #182914, #166677, #34530, #132082, #18268, #145136, #162423, #197034, #178671, #48669, #180785, #112663, #211142, #80084, #146187, #32409, #98475, #164540, #157639, #134205, #186911, #173905, #84351, #40691, #187977, #90506, #107879, #73149, #39603, #56924, #25481, #156571, #123097, #7076, #120940, #205286, #57988, #124151, #23332, #189054, #38543, #150440, #2003, #104620, #55854, #22255, #200214, #106794, #54792, #105707, #170668, #122010, #172822, #171735, #88365, #139254, #6009, #155493, #138190, #190112, #204200, #154431, #72079, #41766 ),
 ( #91587, #89441, #24394, #8165, #74249, #68068, #140343, #206361, #146886, #212906, #19770, #4562, #98128, #37093, #185471, #64539, #164179, #135682, #80796, #169233, #130683, #20823, #63474, #15764, #86920, #103171, #70637, #52288, #81849, #196672, #48312, #136748, #180423, #168171, #152988, #201707, #85852, #202775, #54426, #102101, #170292, #104246, #38174, #195614, #150869, #3502, #129628, #120567, #114423, #53350, #69572, #118417, #68508, #2433, #21880, #47251, #36023, #14702, #186544, #163120, #113365, #30992, #151928, #87986, #134635, #32041, #179370, #154062, #119484, #97067, #200640, #184403, #22958, #173533, #58687, #203840, #189742, #122720, #74939, #71708, #171364, #90137, #142107, #7780, #125908, #155130, #6712, #92290, #27239, #208120, #191865, #72788, #41394, #138889, #158334, #172447, #59748, #89073, #76002, #175652, #43526, #204908, #55486, #124835, #108570, #123783, #56561, #190801, #139966, #121640, #42461, #174597, #188683, #187608, #40318, #91208, #26174, #93346, #106424, #9928, #5627, #107505, #39235, #24034, #156204, #205989, #25106, #137821, #73872, #105327, #109649, #57625, #157270, #8860, #141050, #207056, #213436, #196157, #161533, #177778, #77055, #45654, #10981, #30463, #212377, #79198, #209176, #130165, #64017, #110703, #60815, #12058, #96548, #47798, #32579, #78126, #163662, #159382, #129111, #126976, #94412, #144256, #145315, #62942, #143185, #61887, #114956, #147410, #176703, #192935, #162595, #179906, #211318, #65059, #113911, #13119, #29393, #44589, #111771, #28316, #14170, #95487, #80264, #160451, #31529, #210249, #97604, #128050, #195086, #15244, #81331, #131215, #46723, #194005, #112836, #178852, #197203, #146363, #48842, #180957, #93811, #42927, #109037, #175056, #193417, #178250, #60209, #210725, #144713, #26643, #157736, #191262, #158788, #159852, #111172, #176117, #29863, #62351, #78593, #110106, #94873, #162001, #46123, #27717, #128512, #126370, #112240, #194480, #95946, #92744, #75405, #195559, #10385, #76461, #13590, #11455, #125303, #79664, #28790, #145779, #209644, #177173, #142569, #211782, #63420, #208576, #192329, #129572, #47195, #113310, #160926, #25572, #91683, #43988, #77528, #59145, #143649, #61285, #141518, #9333, #207526, #127446, #45061, #12520, #198717, #52490, #14647, #196619, #2641, #30937, #34104, #49310, #98072, #165175, #82853, #97013, #81796, #134836, #167315, #130627, #80741, #50363, #199790, #99126, #18902, #1574, #181418, #197666, #163066, #65518, #146829, #116486, #131663, #100175, #48258, #67635, #114372, #133782, #179316, #115427, #51435, #150004, #183549, #16769, #213895, #180367, #31991, #35156, #64485, #33048, #212848, #15711, #132712, #117555, #84986, #502, #68714, #200839, #151077, #164127, #148929, #182475, #147879, #66570, #166240, #17830, #83913, #101233, #120771, #136957, #156406, #36224, #88195, #69778, #40527, #3702, #184607, #86057, #71914, #72990, #70841, #37304, #102303, #89281, #187814, #7993, #106631, #122929, #135886, #138023, #171568, #168376, #154269, #21025, #39440, #19973, #201905, #202983, #172660, #186751, #24235, #53557, #119690, #205120, #140176, #90337, #74085, #185675, #5843, #103378, #56763, #54624, #206198, #169440, #188886, #118620, #152134, #87122, #153192, #23165, #6913, #22084, #4764, #155329, #38373, #104454, #139093 ),
 ( #170501, #204038, #55687, #121843, #105534, #111992, #75151, #128264, #13339, #29607, #141261, #107716, #176918, #160668, #175867, #207269, #110912, #192074, #173743, #28533, #94625, #9077, #25320, #125053, #143388, #12263, #145531, #191008, #62105, #57826, #27455, #91421, #58900, #42675, #43740, #93553, #189955, #174809, #79414, #45870, #108783, #157482, #209386, #78340, #109853, #177994, #144463, #59959, #76208, #41605, #158536, #123988, #61030, #10133, #127191, #26385, #210467, #92497, #194226, #142318, #208328, #95693, #161748, #126114, #159597, #11195, #77276, #193158, #44808, #96763, #15458, #84742, #48011, #164927, #165996, #199541, #32800, #100981, #34909, #183302, #129330, #31745, #148687, #63164, #51183, #64237, #66327, #256, #197418, #213646, #81545, #167070, #195306, #181175, #162814, #133534, #14391, #46937, #179061, #16519, #17581, #163883, #130381, #113055, #182229, #132472, #18662, #117306, #1332, #80482, #82602, #50119, #30680, #98874, #114128, #198474, #146582, #212599, #147628, #211529, #65272, #196371, #180120, #97819, #83664, #131418, #49060, #115180, #116240, #33853, #99934, #149755, #67393, #54385, #68471, #53311, #106382, #138846, #102065, #52246, #21837, #171320, #70594, #204863, #187567, #152945, #169191, #134598, #37050, #2392, #87945, #103133, #5585, #168130, #39193, #85811, #105284, #150830, #20783, #22915, #121595, #155086, #136709, #185430, #151890, #3464, #6672, #35984, #86878, #23993, #201663, #104205, #89031, #56518, #186502, #40271, #188641, #122678, #200599, #4521, #154019, #118374, #172405, #69534, #71665, #137779, #202734, #120523, #38133, #184362, #19732, #170252, #135641, #72749, #119443, #203797, #55443, #43489, #44550, #42425, #8824, #73829, #60777, #159343, #128014, #12017, #94372, #107466, #109608, #143144, #139925, #59707, #207017, #10940, #156161, #41356, #174560, #78090, #92248, #210211, #25068, #91170, #176666, #111731, #144215, #61847, #157229, #125867, #74900, #28278, #108530, #193967, #173492, #160412, #45615, #177738, #141009, #205952, #209138, #192894, #208080, #58648, #126936, #9887, #57584, #110665, #90096, #124802, #123742, #190761, #175614, #7742, #189703, #26136, #158296, #75963, #191826, #142066, #27201, #93308, #77015, #82346, #113874, #98616, #165742, #49857, #179869, #132212, #63979, #115984, #198221, #181972, #96511, #79157, #199282, #162561, #112799, #33602, #31494, #129073, #99673, #32541, #148437, #213401, #180920, #146324, #17329, #83410, #212339, #80225, #149492, #50924, #1075, #164677, #67140, #133274, #46681, #196121, #62903, #14133, #97569, #145273, #117050, #5, #161497, #29353, #195044, #48804, #95448, #211280, #178811, #13077, #30426, #16261, #163626, #66070, #130133, #131178, #15207, #114921, #47760, #81298, #147375, #65023, #197168, #202470, #187310, #38937, #102871, #186235, #200345, #183047, #138581, #68208, #151635, #51994, #34662, #120259, #166811, #53044, #100732, #69270, #54123, #135384, #118120, #20533, #35725, #168930, #167870, #105020, #19468, #184105, #101801, #171059, #18405, #85544, #37869, #86615, #71405, #21575, #3201, #84481, #201405, #119177, #103947, #22655, #185163, #36787, #152683, #204604, #4265, #70335, #136452, #169989, #87681, #153754, #121334, #5325, #137517, #203534, #55187, #150571, #134340, #88766, #154823, #6408, #72480 ),
 ( #56255, #2133, #106120, #93039, #191560, #160149, #44279, #126662, #139661, #75698, #175351, #172143, #91976, #24800, #43224, #188371, #73560, #206753, #110400, #124540, #28010, #57318, #123483, #208872, #143942, #176404, #94108, #189446, #158034, #41088, #60502, #74635, #11746, #205682, #192627, #77821, #209938, #107196, #23735, #26931, #10678, #25866, #173221, #159081, #42155, #89841, #76749, #142870, #90902, #155890, #156965, #207815, #122412, #40009, #8556, #7478, #140742, #9621, #58384, #190497, #108270, #174291, #141812, #59443, #125600, #109341, #49587, #12804, #177470, #147111, #82078, #195845, #115711, #98344, #63705, #79950, #193701, #162284, #127744, #213137, #13872, #130909, #78877, #164409, #211005, #15993, #61576, #146053, #148171, #32278, #65800, #47486, #96234, #62628, #128788, #131947, #161217, #212067, #149220, #112522, #14928, #214173, #181701, #97294, #165467, #99413, #33331, #45345, #129862, #64767, #111464, #17063, #194769, #196901, #48540, #197958, #83142, #29084, #95168, #46406, #163353, #178535, #145000, #113596, #30145, #179599, #31220, #81023, #114659, #180653, #50653, #119996, #103687, #118923, #84218, #53863, #135129, #116779, #185973, #37606, #166541, #182776, #67932, #86357, #169736, #88508, #134077, #5070, #795, #184903, #34394, #150306, #200085, #201146, #36527, #133008, #117857, #170808, #203282, #18129, #100466, #152428, #21325, #52784, #54929, #87432, #2940, #19206, #199008, #101539, #66863, #4007, #167608, #70077, #1872, #153500, #51734, #71145, #183849, #85285, #137262, #121081, #187048, #102614, #35461, #151371, #69012, #38680, #168669, #20273, #136191, #202209, #104759, #22399, #142614, #190247, #44031, #192376, #126413, #72216, #189194, #91727, #6146, #208622, #7217, #9376, #157778, #140487, #156711, #172963, #110149, #138323, #124288, #105852, #76503, #39747, #204339, #122148, #108016, #109085, #106940, #73291, #55997, #125344, #75447, #176162, #60256, #158834, #171879, #174042, #207568, #188116, #41905, #57065, #141560, #23476, #89583, #24542, #27762, #8302, #154570, #155632, #139394, #205427, #25615, #92789, #40831, #191307, #59189, #123229, #90650, #74386, #206498, #58129, #42975, #175100, #10431, #26687, #149788, #178298, #166029, #18693, #117341, #29905, #199573, #128555, #183338, #51217, #34943, #160970, #143697, #52281, #12560, #177220, #101015, #95990, #193463, #167106, #97056, #1362, #63463, #30981, #210770, #84775, #150862, #62390, #144759, #2424, #118408, #68501, #17614, #134629, #200633, #111217, #46168, #127492, #78634, #162043, #209689, #184394, #67424, #11503, #93858, #45107, #113354, #159896, #61333, #28833, #77574, #94921, #83700, #13633, #133567, #194520, #195604, #79706, #179359, #112282, #145821, #211826, #129617, #47239, #55476, #40307, #106415, #170283, #39226, #53341, #36014, #205980, #135673, #4554, #119475, #102093, #187599, #19761, #120556, #168163, #136739, #121630, #202765, #185463, #87977, #103162, #21871, #20815, #172438, #86911, #37083, #169223, #24025, #85843, #152979, #105317, #154051, #138879, #89063, #70628, #151920, #54415, #186535, #171355, #90127, #38164, #104237, #5618, #57615, #71700, #137812, #203831, #22949, #156194, #3493, #155121, #69563, #6703, #72780, #204897, #56550, #201698, #122711, #123773, #7770, #188674, #73861, #139955, #210238 ) ),
 .UNSPECIFIED., .T., .F., .T. ) 
 B_SPLINE_SURFACE_WITH_KNOTS ( ( 4, 3, 4 ),
 ( 4, 1, 1, 1, 1, 1, 1, 1, 1, 1, 1, 1, 1, 1, 1, 1, 1, 1, 1, 1, 1, 1, 1, 1, 1, 1, 1, 1, 1, 1, 1, 1, 1, 1, 1, 1, 1, 1, 1, 1, 1, 1, 1, 1, 1, 1, 1, 1, 1, 1, 1, 1, 1, 1, 1, 1, 1, 1, 1, 1, 1, 1, 1, 1, 1, 1, 1, 1, 1, 1, 1, 1, 1, 1, 1, 1, 1, 1, 1, 1, 1, 1, 1, 1, 1, 1, 1, 1, 1, 1, 1, 1, 1, 1, 1, 1, 1, 1, 1, 1, 1, 1, 1, 1, 1, 1, 1, 1, 1, 1, 1, 1, 1, 1, 1, 1, 1, 1, 1, 1, 1, 1, 1, 1, 1, 1, 1, 1, 1, 1, 1, 1, 1, 1, 1, 1, 1, 1, 1, 1, 1, 1, 1, 1, 1, 1, 1, 1, 1, 1, 1, 1, 1, 1, 1, 1, 1, 1, 1, 1, 1, 1, 1, 1, 1, 1, 1, 1, 1, 1, 1, 1, 1, 1, 1, 1, 1, 1, 1, 1, 1, 1, 1, 1, 1, 1, 1, 1, 1, 1, 1, 1, 1, 1, 1, 1, 1, 1, 1, 1, 1, 1, 1, 1, 1, 1, 1, 1, 1, 1, 1, 1, 1, 1, 1, 1, 1, 1, 1, 1, 1, 1, 1, 1, 1, 1, 1, 1, 1, 1, 1, 1, 1, 1, 1, 1, 1, 1, 1, 1, 1, 1, 1, 1, 1, 1, 1, 1, 1, 1, 1, 1, 1, 1, 1, 1, 1, 1, 1, 1, 1, 1, 1, 1, 1, 1, 1, 1, 1, 1, 1, 1, 1, 1, 1, 1, 1, 1, 1, 1, 1, 1, 1, 1, 1, 1, 1, 1, 1, 1, 1, 1, 1, 1, 1, 1, 1, 1, 1, 1, 1, 1, 1, 1, 1, 1, 1, 1, 1, 1, 1, 1, 1, 1, 1, 1, 1, 1, 1, 1, 1, 1, 1, 1, 1, 1, 1, 1, 1, 1, 1, 1, 1, 1, 1, 1, 1, 1, 1, 1, 1, 1, 1, 1, 1, 1, 1, 1, 1, 1, 1, 1, 1, 1, 1, 1, 1, 1, 1, 1, 1, 1, 1, 1, 1, 1, 1, 1, 1, 1, 1, 1, 1, 1, 1, 1, 1, 1, 1, 1, 1, 1, 1, 1, 4 ),
 ( 0.000000000000000000, 0.5000000000000000000, 1.000000000000000000 ),
 ( 0.000000000000000000, 0.002600209826155936224, 0.005208878553436857226, 0.007813350965615119270, 0.01041570154746907992, 0.01302155883015148306, 0.01562460066207539862, 0.01822947720112986364, 0.02083337797298438765, 0.02343721533725894035, 0.02604213897589890969, 0.02864525980212044229, 0.03125073504456635232, 0.03385369766904555017, 0.03645898980682723417, 0.03906240375024701977, 0.04166680464497042602, 0.04427120869897264999, 0.04687461886132015393, 0.04947991130494613921, 0.05208287402783655373, 0.05468834688957619622, 0.05729146186993632622, 0.05989639238693608009, 0.06250023923939096449, 0.06510408216679804128, 0.06770901469741306966, 0.07031212675311915294, 0.07291759917081726272, 0.07552056149378454097, 0.07812585104223603027, 0.08072926279340975064, 0.08333366149866272554, 0.08593806365491549193, 0.08854147146176674643, 0.09114676191340240208, 0.09374972248801059782, 0.09635519323906190092, 0.09895830628708340848, 0.1015632345865536273, 0.1041670796237980645, 0.1067709202568039306, 0.1093758509056654005, 0.1119789607794838548, 0.1145844312107493490, 0.1171873915655986947, 0.1197926790194954738, 0.1223960889855860712, 0.1250004854864837645, 0.1276048858798866925, 0.1302082914968497596, 0.1328135800830011481, 0.1354165386474412147, 0.1380220074263333041, 0.1406251186789811980, 0.1432300448973659046, 0.1458338882574615747, 0.1484377267335943440, 0.1510426556371624596, 0.1536457634674935069, 0.1562512320483212536, 0.1588541905735017246, 0.1614594760690261366, 0.1640628843880489185, 0.1666672788216651824, 0.1692716775892487424, 0.1718750811543677814, 0.1744803680111783883, 0.1770833247038955116, 0.1796887916465979840, 0.1822919012421508056, 0.1848968255159594287, 0.1875006673364670307, 0.1901045037933276616, 0.1927094310880738681, 0.1953125370132051675, 0.1979180038795354257, 0.2005209607134520455, 0.2031262443867272172, 0.2057296511966431873, 0.2083340436999963075, 0.2109384409787386505, 0.2135418426300015604, 0.2161471278935624962, 0.2187500828529475860, 0.2213555480953768861, 0.2239586561720615654, 0.2265635786377499516, 0.2291674190561798496, 0.2317712536313151217, 0.2343761794536610432, 0.2369792836118274071, 0.2395847488995502261, 0.2421877041805577391, 0.2447929861676560459, 0.2473963916063780244, 0.2500007823164346887, 0.2526051782432667259, 0.2552085781186103075, 0.2578138619249652486, 0.2604168152893601151, 0.2630222789673848927, 0.2656253856633817301, 0.2682303064573571261, 0.2708341456111751366, 0.2734379784420828963, 0.2760429029284052760, 0.2786460054577940548, 0.2812514693027542978, 0.2838544231691620401, 0.2864597036061101165, 0.2890631078115080133, 0.2916674968651886135, 0.2942718915769991783, 0.2968752898143142138, 0.2994805722994643427, 0.3020835242071668869, 0.3046889864566129091, 0.3072920919100609050, 0.3098970111686871198, 0.3125008491953192857, 0.3151046804194536644, 0.3177096037060897493, 0.3203127047448455222, 0.3229181672828482230, 0.3255211198729257016, 0.3281263988957095479, 0.3307298020056156362, 0.3333341895397992083, 0.3359385831734401084, 0.3385419799105768290, 0.3411472612104861635, 0.3437502117997557338, 0.3463556727564109927, 0.3489587771054129539, 0.3515636949650152721, 0.3541675320018531359, 0.3567713617566292128, 0.3593762839798815834, 0.3619793836661120978, 0.3645848450329270407, 0.3671877964849088460, 0.3697930742294792128, 0.3723964763816929868, 0.3750008625332226786, 0.3776052552255140804, 0.3802086506002868016, 0.3828139308508870520, 0.3854168802599494681, 0.3880223400595693151, 0.3906254434421968513, 0.3932303600390676390, 0.3958341962234732669, 0.3984380246462727593, 0.4010429459424146859, 0.4036460444141952153, 0.4062515047455624306, 0.4088544551976535102, 0.4114597317999305615, 0.4140631331322238151, 0.4166675180379114662, 0.4192719099256467796, 0.4218753040758395079, 0.4244805834130354061, 0.4270835317800880659, 0.4296889905584002634, 0.4322920931126992272, 0.4348970085831024290, 0.4375008440524135733, 0.4401046712805898320, 0.4427095917858701601, 0.4453126891812490551, 0.4479181486128839262, 0.4505210982032648026, 0.4531263737991432228, 0.4557297744492659897, 0.4583341582458977381, 0.4609385494658484461, 0.4635419425292200413, 0.4661472210888942258, 0.4687501685521111572, 0.4713556264448209299, 0.4739587283088163017, 0.4765636427889929916, 0.4791674776805284197, 0.4817713038514113699, 0.4843762237020596273, 0.4869793201590638665, 0.4895847788266616818, 0.4921877276934932821, 0.4947930024188478271, 0.4973964025245324327, 0.5000007853488734888, 0.5026051760377950872, 0.5052085681520839255, 0.5078138460701020485, 0.5104167927676396266, 0.5130222499104345468, 0.5156253512221359303, 0.5182302648483090302, 0.5208340992993732987, 0.5234379245502747136, 0.5260428438825063280, 0.5286459395391455152, 0.5312513975783873521, 0.5338543458598166147, 0.5364596198505067193, 0.5390630195494738874, 0.5416674015382738627, 0.5442717918329101900, 0.5468751831358398263, 0.5494804605480556603, 0.5520834066180569932, 0.5546888631466128095, 0.5572919640440190392, 0.5598968769523987588, 0.5625007111002878757, 0.5651045355685063720, 0.5677094545185276120, 0.5703125495128006373, 0.5729180070593572482, 0.5755209548935220631, 0.5781262282853970591, 0.5807296277153600750, 0.5833340090053582561, 0.5859383990424469335, 0.5885417896717308750, 0.5911470667139914204, 0.5937500122945923442, 0.5963554683445766447, 0.5989585689656815592, 0.6015634812924701702, 0.6041673152744758690, 0.6067711390973024033, 0.6093760578013157625, 0.6119791522712144660, 0.6145846094607528842, 0.6171875569857874222, 0.6197928299146914233, 0.6223962292133623508, 0.6250006099412922511, 0.6276049998575695676, 0.6302083899509167697, 0.6328136667590675835, 0.6354166119884008257, 0.6380220676954796444, 0.6406251681782773044, 0.6432300800596744139, 0.6458339140130902045, 0.6484377373278128465, 0.6510426559220214848, 0.6536457500055372627, 0.6562512069737248543, 0.6588541543277639523, 0.6614594269295416273, 0.6640628262346358612, 0.6666672065372305500, 0.6692715964694370134, 0.6718749861645568755, 0.6744802628744462902, 0.6770832078906477980, 0.6796886633904898334, 0.6822917638729786294, 0.6848966754451861760, 0.6875005095073121186, 0.6901043324512210475, 0.6927092510718347862, 0.6953123449069624762, 0.6979178017894718256, 0.7005207491106575368, 0.7031260215211581066, 0.7057294209703992571, 0.7083338009843969107, 0.7109381910692819107, 0.7135415805038890502, 0.7161468572513741693, 0.7187498021925872171, 0.7213552576208688283, 0.7239583582410578089, 0.7265632696402853918, 0.7291671039484327599, 0.7317709266588259265, 0.7343758454420658000, 0.7369789391668094547, 0.7395843960993241373, 0.7421873435258099505, 0.7447926158808931829, 0.7473960156120186271, 0.7500003954741673029, 0.7526047858484943287, 0.7552081751603144655, 0.7578134520812660480, 0.7604163970856469001, 0.7630218525780576577, 0.7656249534739711926, 0.7682298648364407345, 0.7708336995279378989, 0.7734375221421257995, 0.7760424412242287184, 0.7786455349766069345, 0.7812509920948264019, 0.7838539397647821261, 0.7864592122003229990, 0.7890626123510894319, 0.7916669921981516200, 0.7942713829987035901, 0.7968747723254782089, 0.7994800495557851105, 0.8020829947615083499, 0.8046884504537559213, 0.8072915517634385862, 0.8098964632253897733, 0.8125002984375870874, 0.8151041210928977598, 0.8177090406101226172, 0.8203121345281733090, 0.8229175919678175521, 0.8255205400194353116, 0.8281258126713292311, 0.8307292133795166622, 0.8333335933482756142, 0.8359379847118599827, 0.8385413741913512187, 0.8411466518669262760, 0.8437495974121898001, 0.8463550534400045011, 0.8489581553015269622, 0.8515630669992224622, 0.8541669028694969246, 0.8567707257032814994, 0.8593756457919137226, 0.8619787400136992295, 0.8645841979105142183, 0.8671871464820134490, 0.8697924194861808012, 0.8723958208895988831, 0.8750002011168627192, 0.8776045931803160283, 0.8802079829503125508, 0.8828132612070975771, 0.8854162072301272612, 0.8880216637292678294, 0.8906247662807315058, 0.8932296783504612980, 0.8958335150162225480, 0.8984373381658604663, 0.9010422589622166800, 0.9036453536258294283, 0.9062508121155921081, 0.9088537613452241093, 0.9114590348376164775, 0.9140624370741091687, 0.9166668176967164294, 0.9192712105969091940, 0.9218746007952320909, 0.9244798797692056480, 0.9270828264082496828, 0.9296882835145078294, 0.9322913868941045124, 0.9348962994721256026, 0.9375001370706889103, 0.9401039606740361210, 0.9427088823143441321, 0.9453119775565693717, 0.9479174367776000976, 0.9505203868030935865, 0.9531256609099927335, 0.9557290641454977420, 0.9583334452981105978, 0.9609378390199675435, 0.9635412300619400350, 0.9661465102466426647, 0.9687494557931184413, 0.9713549143510965544, 0.9739580252604012056, 0.9765629275426017664, 0.9791667581373608709, 0.9817706348486141543, 0.9843755007711335603, 0.9869785191422796311, 0.9895843624858681187, 0.9921867025132995455, 0.9947911529560371502, 0.9973998138561904758, 1.000000000000000000 ),
 .UNSPECIFIED. ) 
 GEOMETRIC_REPRESENTATION_ITEM ( )  RATIONAL_B_SPLINE_SURFACE ( (
 ( 1.000000000000000222, 1.000000000000000222, 0.9999999999999997780, 1.000000000000000222, 1.000000000000000000, 1.000000000000000000, 0.9999999999999997780, 1.000000000000000000, 1.000000000000000000, 1.000000000000000000, 1.000000000000000000, 1.000000000000000222, 1.000000000000000000, 1.000000000000000000, 1.000000000000000222, 0.9999999999999994449, 1.000000000000000222, 1.000000000000000000, 0.9999999999999997780, 1.000000000000000444, 1.000000000000000000, 1.000000000000000222, 1.000000000000000000, 1.000000000000000000, 0.9999999999999996669, 1.000000000000000000, 1.000000000000000222, 0.9999999999999996669, 1.000000000000000222, 1.000000000000000000, 1.000000000000000222, 1.000000000000000000, 1.000000000000000222, 0.9999999999999997780, 1.000000000000000444, 1.000000000000000000, 1.000000000000000222, 0.9999999999999997780, 1.000000000000000222, 1.000000000000000000, 1.000000000000000000, 0.9999999999999997780, 1.000000000000000000, 0.9999999999999997780, 1.000000000000000000, 0.9999999999999997780, 1.000000000000000000, 1.000000000000000000, 0.9999999999999997780, 1.000000000000000000, 1.000000000000000222, 0.9999999999999996669, 1.000000000000000000, 1.000000000000000000, 1.000000000000000222, 0.9999999999999997780, 1.000000000000000444, 1.000000000000000000, 0.9999999999999997780, 1.000000000000000000, 1.000000000000000000, 1.000000000000000000, 1.000000000000000222, 1.000000000000000000, 1.000000000000000000, 1.000000000000000222, 1.000000000000000000, 1.000000000000000000, 0.9999999999999997780, 1.000000000000000222, 1.000000000000000000, 0.9999999999999997780, 1.000000000000000000, 1.000000000000000000, 1.000000000000000000, 1.000000000000000000, 1.000000000000000222, 0.9999999999999996669, 1.000000000000000444, 0.9999999999999996669, 1.000000000000000000, 0.9999999999999996669, 1.000000000000000444, 1.000000000000000000, 1.000000000000000000, 1.000000000000000222, 1.000000000000000000, 1.000000000000000000, 1.000000000000000222, 0.9999999999999997780, 1.000000000000000000, 1.000000000000000444, 0.9999999999999997780, 1.000000000000000444, 0.9999999999999997780, 1.000000000000000000, 1.000000000000000222, 1.000000000000000000, 0.9999999999999997780, 1.000000000000000222, 1.000000000000000222, 0.9999999999999997780, 1.000000000000000000, 1.000000000000000222, 0.9999999999999997780, 1.000000000000000444, 0.9999999999999997780, 1.000000000000000444, 0.9999999999999997780, 1.000000000000000000, 1.000000000000000222, 0.9999999999999996669, 1.000000000000000000, 1.000000000000000000, 1.000000000000000444, 1.000000000000000222, 0.9999999999999997780, 1.000000000000000222, 1.000000000000000222, 1.000000000000000000, 1.000000000000000222, 0.9999999999999997780, 1.000000000000000000, 1.000000000000000222, 0.9999999999999996669, 1.000000000000000000, 1.000000000000000000, 1.000000000000000000, 1.000000000000000000, 1.000000000000000000, 1.000000000000000000, 1.000000000000000000, 0.9999999999999997780, 1.000000000000000222, 0.9999999999999997780, 1.000000000000000000, 0.9999999999999997780, 1.000000000000000222, 1.000000000000000000, 1.000000000000000000, 1.000000000000000000, 1.000000000000000222, 0.9999999999999997780, 0.9999999999999997780, 1.000000000000000222, 1.000000000000000222, 1.000000000000000000, 1.000000000000000444, 0.9999999999999996669, 1.000000000000000444, 0.9999999999999997780, 1.000000000000000222, 1.000000000000000000, 1.000000000000000000, 1.000000000000000000, 1.000000000000000222, 0.9999999999999997780, 0.9999999999999997780, 1.000000000000000444, 1.000000000000000444, 0.9999999999999997780, 1.000000000000000000, 1.000000000000000000, 1.000000000000000000, 1.000000000000000222, 1.000000000000000000, 1.000000000000000000, 1.000000000000000222, 1.000000000000000222, 1.000000000000000000, 1.000000000000000444, 1.000000000000000000, 1.000000000000000222, 1.000000000000000000, 1.000000000000000000, 1.000000000000000444, 1.000000000000000000, 1.000000000000000222, 1.000000000000000000, 1.000000000000000222, 0.9999999999999997780, 1.000000000000000222, 1.000000000000000222, 1.000000000000000000, 0.9999999999999996669, 1.000000000000000222, 1.000000000000000000, 1.000000000000000000, 1.000000000000000222, 1.000000000000000222, 1.000000000000000222, 0.9999999999999997780, 1.000000000000000000, 1.000000000000000222, 1.000000000000000000, 1.000000000000000000, 1.000000000000000000, 0.9999999999999996669, 1.000000000000000444, 1.000000000000000222, 0.9999999999999996669, 1.000000000000000444, 1.000000000000000000, 1.000000000000000000, 1.000000000000000222, 0.9999999999999997780, 1.000000000000000444, 0.9999999999999997780, 0.9999999999999997780, 1.000000000000000444, 0.9999999999999997780, 1.000000000000000222, 1.000000000000000000, 1.000000000000000000, 1.000000000000000000, 0.9999999999999997780, 1.000000000000000000, 1.000000000000000222, 0.9999999999999996669, 1.000000000000000222, 1.000000000000000000, 1.000000000000000222, 0.9999999999999996669, 0.9999999999999997780, 1.000000000000000444, 0.9999999999999997780, 0.9999999999999997780, 1.000000000000000000, 1.000000000000000222, 1.000000000000000000, 1.000000000000000000, 0.9999999999999996669, 1.000000000000000222, 1.000000000000000000, 0.9999999999999997780, 1.000000000000000000, 1.000000000000000000, 0.9999999999999997780, 1.000000000000000444, 0.9999999999999996669, 1.000000000000000444, 0.9999999999999997780, 1.000000000000000000, 1.000000000000000222, 0.9999999999999997780, 1.000000000000000222, 1.000000000000000222, 0.9999999999999997780, 1.000000000000000000, 1.000000000000000000, 1.000000000000000000, 1.000000000000000222, 1.000000000000000000, 1.000000000000000000, 1.000000000000000222, 1.000000000000000222, 1.000000000000000000, 1.000000000000000000, 1.000000000000000222, 0.9999999999999997780, 1.000000000000000000, 1.000000000000000222, 1.000000000000000000, 1.000000000000000222, 0.9999999999999997780, 1.000000000000000222, 0.9999999999999997780, 1.000000000000000222, 0.9999999999999997780, 1.000000000000000222, 1.000000000000000000, 1.000000000000000000, 1.000000000000000444, 0.9999999999999996669, 1.000000000000000222, 0.9999999999999997780, 1.000000000000000000, 1.000000000000000222, 1.000000000000000000, 1.000000000000000222, 0.9999999999999997780, 0.9999999999999997780, 1.000000000000000000, 0.9999999999999997780, 1.000000000000000000, 1.000000000000000000, 1.000000000000000222, 1.000000000000000000, 1.000000000000000000, 1.000000000000000222, 1.000000000000000000, 1.000000000000000000, 1.000000000000000000, 1.000000000000000000, 0.9999999999999997780, 1.000000000000000222, 1.000000000000000222, 0.9999999999999997780, 1.000000000000000444, 1.000000000000000444, 0.9999999999999997780, 1.000000000000000000, 0.9999999999999997780, 1.000000000000000000, 1.000000000000000000, 1.000000000000000000, 1.000000000000000000, 0.9999999999999997780, 1.000000000000000222, 1.000000000000000000, 0.9999999999999997780, 1.000000000000000222, 1.000000000000000000, 1.000000000000000000, 1.000000000000000000, 1.000000000000000444, 1.000000000000000000, 0.9999999999999997780, 0.9999999999999997780, 0.9999999999999997780, 1.000000000000000222, 1.000000000000000222, 0.9999999999999996669, 1.000000000000000222, 0.9999999999999997780, 1.000000000000000222, 1.000000000000000000, 1.000000000000000000, 0.9999999999999996669, 1.000000000000000222, 1.000000000000000222, 1.000000000000000000, 1.000000000000000000, 1.000000000000000222, 0.9999999999999997780, 1.000000000000000000, 1.000000000000000222, 0.9999999999999994449, 1.000000000000000222, 1.000000000000000000, 1.000000000000000222, 0.9999999999999997780, 1.000000000000000000, 1.000000000000000000, 0.9999999999999997780, 1.000000000000000000, 1.000000000000000222, 0.9999999999999997780, 1.000000000000000000, 1.000000000000000000, 1.000000000000000000, 1.000000000000000000, 1.000000000000000222, 1.000000000000000000, 0.9999999999999996669, 0.9999999999999996669, 1.000000000000000222, 0.9999999999999997780, 1.000000000000000222, 1.000000000000000000, 0.9999999999999997780, 1.000000000000000222, 0.9999999999999997780, 1.000000000000000444, 1.000000000000000222, 1.000000000000000000, 1.000000000000000222, 1.000000000000000222, 1.000000000000000000, 1.000000000000000000, 1.000000000000000000, 1.000000000000000000, 1.000000000000000000, 1.000000000000000000, 1.000000000000000000, 0.9999999999999997780, 1.000000000000000000, 0.9999999999999996669, 1.000000000000000444, 0.9999999999999996669, 1.000000000000000000, 1.000000000000000000, 0.9999999999999997780, 1.000000000000000444, 1.000000000000000000, 1.000000000000000000, 1.000000000000000000),
 ( 0.3333333333333334259, 0.3333333333333334259, 0.3333333333333333703, 0.3333333333333333703, 0.3333333333333334259, 0.3333333333333333703, 0.3333333333333333703, 0.3333333333333334259, 0.3333333333333333148, 0.3333333333333334814, 0.3333333333333332593, 0.3333333333333335369, 0.3333333333333333148, 0.3333333333333333703, 0.3333333333333334259, 0.3333333333333332593, 0.3333333333333333703, 0.3333333333333333703, 0.3333333333333334259, 0.3333333333333334814, 0.3333333333333333148, 0.3333333333333334259, 0.3333333333333333703, 0.3333333333333333703, 0.3333333333333333148, 0.3333333333333333703, 0.3333333333333334259, 0.3333333333333332038, 0.3333333333333334259, 0.3333333333333333703, 0.3333333333333334259, 0.3333333333333333703, 0.3333333333333333148, 0.3333333333333334259, 0.3333333333333334259, 0.3333333333333333703, 0.3333333333333334814, 0.3333333333333332593, 0.3333333333333334259, 0.3333333333333334259, 0.3333333333333333148, 0.3333333333333333703, 0.3333333333333333148, 0.3333333333333333703, 0.3333333333333333148, 0.3333333333333333703, 0.3333333333333333703, 0.3333333333333333703, 0.3333333333333333148, 0.3333333333333333148, 0.3333333333333334259, 0.3333333333333332593, 0.3333333333333333703, 0.3333333333333333703, 0.3333333333333333703, 0.3333333333333332593, 0.3333333333333334259, 0.3333333333333333148, 0.3333333333333333148, 0.3333333333333333703, 0.3333333333333333703, 0.3333333333333333703, 0.3333333333333334259, 0.3333333333333333148, 0.3333333333333334259, 0.3333333333333334259, 0.3333333333333333703, 0.3333333333333333703, 0.3333333333333333148, 0.3333333333333333703, 0.3333333333333333703, 0.3333333333333333148, 0.3333333333333333703, 0.3333333333333332593, 0.3333333333333334814, 0.3333333333333333148, 0.3333333333333333703, 0.3333333333333332593, 0.3333333333333335369, 0.3333333333333333703, 0.3333333333333333703, 0.3333333333333333703, 0.3333333333333334259, 0.3333333333333334259, 0.3333333333333333148, 0.3333333333333334259, 0.3333333333333333148, 0.3333333333333333703, 0.3333333333333335369, 0.3333333333333333148, 0.3333333333333334259, 0.3333333333333334814, 0.3333333333333333148, 0.3333333333333335369, 0.3333333333333332593, 0.3333333333333333703, 0.3333333333333333148, 0.3333333333333334259, 0.3333333333333333148, 0.3333333333333334814, 0.3333333333333333703, 0.3333333333333333148, 0.3333333333333333703, 0.3333333333333334259, 0.3333333333333333703, 0.3333333333333334259, 0.3333333333333332593, 0.3333333333333335924, 0.3333333333333333148, 0.3333333333333333148, 0.3333333333333334259, 0.3333333333333332593, 0.3333333333333333703, 0.3333333333333333148, 0.3333333333333335369, 0.3333333333333333703, 0.3333333333333333703, 0.3333333333333334259, 0.3333333333333334259, 0.3333333333333333703, 0.3333333333333333703, 0.3333333333333333703, 0.3333333333333333703, 0.3333333333333334259, 0.3333333333333333703, 0.3333333333333333703, 0.3333333333333333703, 0.3333333333333334259, 0.3333333333333333148, 0.3333333333333333703, 0.3333333333333333703, 0.3333333333333334259, 0.3333333333333333148, 0.3333333333333333703, 0.3333333333333333703, 0.3333333333333333703, 0.3333333333333333148, 0.3333333333333334259, 0.3333333333333333148, 0.3333333333333333703, 0.3333333333333334259, 0.3333333333333333703, 0.3333333333333333703, 0.3333333333333333703, 0.3333333333333333703, 0.3333333333333334259, 0.3333333333333334259, 0.3333333333333334259, 0.3333333333333333148, 0.3333333333333334259, 0.3333333333333333148, 0.3333333333333334259, 0.3333333333333334259, 0.3333333333333333703, 0.3333333333333333148, 0.3333333333333333703, 0.3333333333333333703, 0.3333333333333333148, 0.3333333333333334259, 0.3333333333333335369, 0.3333333333333333148, 0.3333333333333332593, 0.3333333333333334814, 0.3333333333333332593, 0.3333333333333333703, 0.3333333333333333703, 0.3333333333333333703, 0.3333333333333334259, 0.3333333333333334259, 0.3333333333333334259, 0.3333333333333335369, 0.3333333333333333703, 0.3333333333333333703, 0.3333333333333333703, 0.3333333333333334259, 0.3333333333333333703, 0.3333333333333333703, 0.3333333333333334259, 0.3333333333333333703, 0.3333333333333334259, 0.3333333333333332593, 0.3333333333333334259, 0.3333333333333334259, 0.3333333333333333148, 0.3333333333333333703, 0.3333333333333333703, 0.3333333333333333703, 0.3333333333333333703, 0.3333333333333334259, 0.3333333333333334259, 0.3333333333333334259, 0.3333333333333333148, 0.3333333333333333703, 0.3333333333333334259, 0.3333333333333332593, 0.3333333333333334814, 0.3333333333333333148, 0.3333333333333332593, 0.3333333333333335369, 0.3333333333333333148, 0.3333333333333333703, 0.3333333333333334259, 0.3333333333333333148, 0.3333333333333333703, 0.3333333333333334259, 0.3333333333333333148, 0.3333333333333335369, 0.3333333333333332593, 0.3333333333333333703, 0.3333333333333334259, 0.3333333333333333148, 0.3333333333333334259, 0.3333333333333333148, 0.3333333333333333703, 0.3333333333333333703, 0.3333333333333333703, 0.3333333333333333703, 0.3333333333333334259, 0.3333333333333332593, 0.3333333333333334259, 0.3333333333333334259, 0.3333333333333333703, 0.3333333333333333703, 0.3333333333333333148, 0.3333333333333334814, 0.3333333333333333703, 0.3333333333333332593, 0.3333333333333334259, 0.3333333333333334259, 0.3333333333333334259, 0.3333333333333333703, 0.3333333333333332038, 0.3333333333333335369, 0.3333333333333333148, 0.3333333333333333148, 0.3333333333333333703, 0.3333333333333333703, 0.3333333333333333703, 0.3333333333333334259, 0.3333333333333333148, 0.3333333333333334814, 0.3333333333333333148, 0.3333333333333333703, 0.3333333333333334259, 0.3333333333333333148, 0.3333333333333334259, 0.3333333333333333148, 0.3333333333333334259, 0.3333333333333333148, 0.3333333333333333703, 0.3333333333333333703, 0.3333333333333334259, 0.3333333333333333703, 0.3333333333333333148, 0.3333333333333334814, 0.3333333333333334259, 0.3333333333333333703, 0.3333333333333333148, 0.3333333333333334259, 0.3333333333333333703, 0.3333333333333333703, 0.3333333333333334259, 0.3333333333333333703, 0.3333333333333334814, 0.3333333333333333148, 0.3333333333333334259, 0.3333333333333333703, 0.3333333333333334259, 0.3333333333333333148, 0.3333333333333333703, 0.3333333333333334259, 0.3333333333333333703, 0.3333333333333334259, 0.3333333333333332593, 0.3333333333333333703, 0.3333333333333332593, 0.3333333333333334259, 0.3333333333333333703, 0.3333333333333334259, 0.3333333333333334259, 0.3333333333333333148, 0.3333333333333333148, 0.3333333333333334259, 0.3333333333333333148, 0.3333333333333333148, 0.3333333333333333703, 0.3333333333333333703, 0.3333333333333334259, 0.3333333333333333703, 0.3333333333333334814, 0.3333333333333332593, 0.3333333333333334259, 0.3333333333333333703, 0.3333333333333333703, 0.3333333333333334259, 0.3333333333333333703, 0.3333333333333333703, 0.3333333333333334259, 0.3333333333333334259, 0.3333333333333334814, 0.3333333333333333148, 0.3333333333333333148, 0.3333333333333333703, 0.3333333333333333148, 0.3333333333333334259, 0.3333333333333333703, 0.3333333333333333148, 0.3333333333333332593, 0.3333333333333334259, 0.3333333333333334259, 0.3333333333333333148, 0.3333333333333333703, 0.3333333333333334259, 0.3333333333333333148, 0.3333333333333334259, 0.3333333333333334259, 0.3333333333333334814, 0.3333333333333333148, 0.3333333333333333703, 0.3333333333333332593, 0.3333333333333334814, 0.3333333333333333703, 0.3333333333333332593, 0.3333333333333334814, 0.3333333333333332593, 0.3333333333333334259, 0.3333333333333333703, 0.3333333333333333148, 0.3333333333333333148, 0.3333333333333334259, 0.3333333333333333703, 0.3333333333333333703, 0.3333333333333333703, 0.3333333333333333703, 0.3333333333333334259, 0.3333333333333333148, 0.3333333333333334259, 0.3333333333333332038, 0.3333333333333334259, 0.3333333333333333148, 0.3333333333333334814, 0.3333333333333333703, 0.3333333333333333703, 0.3333333333333334259, 0.3333333333333333148, 0.3333333333333333703, 0.3333333333333333703, 0.3333333333333333703, 0.3333333333333333703, 0.3333333333333333703, 0.3333333333333334259, 0.3333333333333333148, 0.3333333333333334814, 0.3333333333333334259, 0.3333333333333332593, 0.3333333333333333703, 0.3333333333333333703, 0.3333333333333333703, 0.3333333333333333703, 0.3333333333333333703, 0.3333333333333334259, 0.3333333333333333148, 0.3333333333333333703, 0.3333333333333334259, 0.3333333333333335369, 0.3333333333333333148, 0.3333333333333333703, 0.3333333333333334259, 0.3333333333333333703, 0.3333333333333333703, 0.3333333333333333703, 0.3333333333333333703, 0.3333333333333333703, 0.3333333333333333703, 0.3333333333333333703, 0.3333333333333333703, 0.3333333333333334259, 0.3333333333333332593, 0.3333333333333334814, 0.3333333333333332593, 0.3333333333333334259, 0.3333333333333333703, 0.3333333333333333703, 0.3333333333333334814, 0.3333333333333333148, 0.3333333333333333703, 0.3333333333333333703),
 ( 0.3333333333333334259, 0.3333333333333334259, 0.3333333333333333703, 0.3333333333333333703, 0.3333333333333334259, 0.3333333333333333703, 0.3333333333333333703, 0.3333333333333334259, 0.3333333333333333148, 0.3333333333333334814, 0.3333333333333332593, 0.3333333333333335369, 0.3333333333333333148, 0.3333333333333333703, 0.3333333333333334259, 0.3333333333333332593, 0.3333333333333333703, 0.3333333333333333703, 0.3333333333333334259, 0.3333333333333334814, 0.3333333333333333148, 0.3333333333333334259, 0.3333333333333333703, 0.3333333333333333703, 0.3333333333333333148, 0.3333333333333333703, 0.3333333333333334259, 0.3333333333333332038, 0.3333333333333334259, 0.3333333333333333703, 0.3333333333333334259, 0.3333333333333333703, 0.3333333333333333148, 0.3333333333333334259, 0.3333333333333334259, 0.3333333333333333703, 0.3333333333333334814, 0.3333333333333332593, 0.3333333333333334259, 0.3333333333333334259, 0.3333333333333333148, 0.3333333333333333703, 0.3333333333333333148, 0.3333333333333333703, 0.3333333333333333148, 0.3333333333333333703, 0.3333333333333333703, 0.3333333333333333703, 0.3333333333333333148, 0.3333333333333333148, 0.3333333333333334259, 0.3333333333333332593, 0.3333333333333333703, 0.3333333333333333703, 0.3333333333333333703, 0.3333333333333332593, 0.3333333333333334259, 0.3333333333333333148, 0.3333333333333333148, 0.3333333333333333703, 0.3333333333333333703, 0.3333333333333333703, 0.3333333333333334259, 0.3333333333333333148, 0.3333333333333334259, 0.3333333333333334259, 0.3333333333333333703, 0.3333333333333333703, 0.3333333333333333148, 0.3333333333333333703, 0.3333333333333333703, 0.3333333333333333148, 0.3333333333333333703, 0.3333333333333332593, 0.3333333333333334814, 0.3333333333333333148, 0.3333333333333333703, 0.3333333333333332593, 0.3333333333333335369, 0.3333333333333333703, 0.3333333333333333703, 0.3333333333333333703, 0.3333333333333334259, 0.3333333333333334259, 0.3333333333333333148, 0.3333333333333334259, 0.3333333333333333148, 0.3333333333333333703, 0.3333333333333335369, 0.3333333333333333148, 0.3333333333333334259, 0.3333333333333334814, 0.3333333333333333148, 0.3333333333333335369, 0.3333333333333332593, 0.3333333333333333703, 0.3333333333333333148, 0.3333333333333334259, 0.3333333333333333148, 0.3333333333333334814, 0.3333333333333333703, 0.3333333333333333148, 0.3333333333333333703, 0.3333333333333334259, 0.3333333333333333703, 0.3333333333333334259, 0.3333333333333332593, 0.3333333333333335924, 0.3333333333333333148, 0.3333333333333333148, 0.3333333333333334259, 0.3333333333333332593, 0.3333333333333333703, 0.3333333333333333148, 0.3333333333333335369, 0.3333333333333333703, 0.3333333333333333703, 0.3333333333333334259, 0.3333333333333334259, 0.3333333333333333703, 0.3333333333333333703, 0.3333333333333333703, 0.3333333333333333703, 0.3333333333333334259, 0.3333333333333333703, 0.3333333333333333703, 0.3333333333333333703, 0.3333333333333334259, 0.3333333333333333148, 0.3333333333333333703, 0.3333333333333333703, 0.3333333333333334259, 0.3333333333333333148, 0.3333333333333333703, 0.3333333333333333703, 0.3333333333333333703, 0.3333333333333333148, 0.3333333333333334259, 0.3333333333333333148, 0.3333333333333333703, 0.3333333333333334259, 0.3333333333333333703, 0.3333333333333333703, 0.3333333333333333703, 0.3333333333333333703, 0.3333333333333334259, 0.3333333333333334259, 0.3333333333333334259, 0.3333333333333333148, 0.3333333333333334259, 0.3333333333333333148, 0.3333333333333334259, 0.3333333333333334259, 0.3333333333333333703, 0.3333333333333333148, 0.3333333333333333703, 0.3333333333333333703, 0.3333333333333333148, 0.3333333333333334259, 0.3333333333333335369, 0.3333333333333333148, 0.3333333333333332593, 0.3333333333333334814, 0.3333333333333332593, 0.3333333333333333703, 0.3333333333333333703, 0.3333333333333333703, 0.3333333333333334259, 0.3333333333333334259, 0.3333333333333334259, 0.3333333333333335369, 0.3333333333333333703, 0.3333333333333333703, 0.3333333333333333703, 0.3333333333333334259, 0.3333333333333333703, 0.3333333333333333703, 0.3333333333333334259, 0.3333333333333333703, 0.3333333333333334259, 0.3333333333333332593, 0.3333333333333334259, 0.3333333333333334259, 0.3333333333333333148, 0.3333333333333333703, 0.3333333333333333703, 0.3333333333333333703, 0.3333333333333333703, 0.3333333333333334259, 0.3333333333333334259, 0.3333333333333334259, 0.3333333333333333148, 0.3333333333333333703, 0.3333333333333334259, 0.3333333333333332593, 0.3333333333333334814, 0.3333333333333333148, 0.3333333333333332593, 0.3333333333333335369, 0.3333333333333333148, 0.3333333333333333703, 0.3333333333333334259, 0.3333333333333333148, 0.3333333333333333703, 0.3333333333333334259, 0.3333333333333333148, 0.3333333333333335369, 0.3333333333333332593, 0.3333333333333333703, 0.3333333333333334259, 0.3333333333333333148, 0.3333333333333334259, 0.3333333333333333148, 0.3333333333333333703, 0.3333333333333333703, 0.3333333333333333703, 0.3333333333333333703, 0.3333333333333334259, 0.3333333333333332593, 0.3333333333333334259, 0.3333333333333334259, 0.3333333333333333703, 0.3333333333333333703, 0.3333333333333333148, 0.3333333333333334814, 0.3333333333333333703, 0.3333333333333332593, 0.3333333333333334259, 0.3333333333333334259, 0.3333333333333334259, 0.3333333333333333703, 0.3333333333333332038, 0.3333333333333335369, 0.3333333333333333148, 0.3333333333333333148, 0.3333333333333333703, 0.3333333333333333703, 0.3333333333333333703, 0.3333333333333334259, 0.3333333333333333148, 0.3333333333333334814, 0.3333333333333333148, 0.3333333333333333703, 0.3333333333333334259, 0.3333333333333333148, 0.3333333333333334259, 0.3333333333333333148, 0.3333333333333334259, 0.3333333333333333148, 0.3333333333333333703, 0.3333333333333333703, 0.3333333333333334259, 0.3333333333333333703, 0.3333333333333333148, 0.3333333333333334814, 0.3333333333333334259, 0.3333333333333333703, 0.3333333333333333148, 0.3333333333333334259, 0.3333333333333333703, 0.3333333333333333703, 0.3333333333333334259, 0.3333333333333333703, 0.3333333333333334814, 0.3333333333333333148, 0.3333333333333334259, 0.3333333333333333703, 0.3333333333333334259, 0.3333333333333333148, 0.3333333333333333703, 0.3333333333333334259, 0.3333333333333333703, 0.3333333333333334259, 0.3333333333333332593, 0.3333333333333333703, 0.3333333333333332593, 0.3333333333333334259, 0.3333333333333333703, 0.3333333333333334259, 0.3333333333333334259, 0.3333333333333333148, 0.3333333333333333148, 0.3333333333333334259, 0.3333333333333333148, 0.3333333333333333148, 0.3333333333333333703, 0.3333333333333333703, 0.3333333333333334259, 0.3333333333333333703, 0.3333333333333334814, 0.3333333333333332593, 0.3333333333333334259, 0.3333333333333333703, 0.3333333333333333703, 0.3333333333333334259, 0.3333333333333333703, 0.3333333333333333703, 0.3333333333333334259, 0.3333333333333334259, 0.3333333333333334814, 0.3333333333333333148, 0.3333333333333333148, 0.3333333333333333703, 0.3333333333333333148, 0.3333333333333334259, 0.3333333333333333703, 0.3333333333333333148, 0.3333333333333332593, 0.3333333333333334259, 0.3333333333333334259, 0.3333333333333333148, 0.3333333333333333703, 0.3333333333333334259, 0.3333333333333333148, 0.3333333333333334259, 0.3333333333333334259, 0.3333333333333334814, 0.3333333333333333148, 0.3333333333333333703, 0.3333333333333332593, 0.3333333333333334814, 0.3333333333333333703, 0.3333333333333332593, 0.3333333333333334814, 0.3333333333333332593, 0.3333333333333334259, 0.3333333333333333703, 0.3333333333333333148, 0.3333333333333333148, 0.3333333333333334259, 0.3333333333333333703, 0.3333333333333333703, 0.3333333333333333703, 0.3333333333333333703, 0.3333333333333334259, 0.3333333333333333148, 0.3333333333333334259, 0.3333333333333332038, 0.3333333333333334259, 0.3333333333333333148, 0.3333333333333334814, 0.3333333333333333703, 0.3333333333333333703, 0.3333333333333334259, 0.3333333333333333148, 0.3333333333333333703, 0.3333333333333333703, 0.3333333333333333703, 0.3333333333333333703, 0.3333333333333333703, 0.3333333333333334259, 0.3333333333333333148, 0.3333333333333334814, 0.3333333333333334259, 0.3333333333333332593, 0.3333333333333333703, 0.3333333333333333703, 0.3333333333333333703, 0.3333333333333333703, 0.3333333333333333703, 0.3333333333333334259, 0.3333333333333333148, 0.3333333333333333703, 0.3333333333333334259, 0.3333333333333335369, 0.3333333333333333148, 0.3333333333333333703, 0.3333333333333334259, 0.3333333333333333703, 0.3333333333333333703, 0.3333333333333333703, 0.3333333333333333703, 0.3333333333333333703, 0.3333333333333333703, 0.3333333333333333703, 0.3333333333333333703, 0.3333333333333334259, 0.3333333333333332593, 0.3333333333333334814, 0.3333333333333332593, 0.3333333333333334259, 0.3333333333333333703, 0.3333333333333333703, 0.3333333333333334814, 0.3333333333333333148, 0.3333333333333333703, 0.3333333333333333703),
 ( 1.000000000000000222, 1.000000000000000222, 0.9999999999999997780, 1.000000000000000222, 1.000000000000000000, 1.000000000000000000, 0.9999999999999997780, 1.000000000000000000, 1.000000000000000000, 1.000000000000000000, 1.000000000000000000, 1.000000000000000222, 1.000000000000000000, 1.000000000000000000, 1.000000000000000222, 0.9999999999999994449, 1.000000000000000222, 1.000000000000000000, 0.9999999999999997780, 1.000000000000000444, 1.000000000000000000, 1.000000000000000222, 1.000000000000000000, 1.000000000000000000, 0.9999999999999996669, 1.000000000000000000, 1.000000000000000222, 0.9999999999999996669, 1.000000000000000222, 1.000000000000000000, 1.000000000000000222, 1.000000000000000000, 1.000000000000000222, 0.9999999999999997780, 1.000000000000000444, 1.000000000000000000, 1.000000000000000222, 0.9999999999999997780, 1.000000000000000222, 1.000000000000000000, 1.000000000000000000, 0.9999999999999997780, 1.000000000000000000, 0.9999999999999997780, 1.000000000000000000, 0.9999999999999997780, 1.000000000000000000, 1.000000000000000000, 0.9999999999999997780, 1.000000000000000000, 1.000000000000000222, 0.9999999999999996669, 1.000000000000000000, 1.000000000000000000, 1.000000000000000222, 0.9999999999999997780, 1.000000000000000444, 1.000000000000000000, 0.9999999999999997780, 1.000000000000000000, 1.000000000000000000, 1.000000000000000000, 1.000000000000000222, 1.000000000000000000, 1.000000000000000000, 1.000000000000000222, 1.000000000000000000, 1.000000000000000000, 0.9999999999999997780, 1.000000000000000222, 1.000000000000000000, 0.9999999999999997780, 1.000000000000000000, 1.000000000000000000, 1.000000000000000000, 1.000000000000000000, 1.000000000000000222, 0.9999999999999996669, 1.000000000000000444, 0.9999999999999996669, 1.000000000000000000, 0.9999999999999996669, 1.000000000000000444, 1.000000000000000000, 1.000000000000000000, 1.000000000000000222, 1.000000000000000000, 1.000000000000000000, 1.000000000000000222, 0.9999999999999997780, 1.000000000000000000, 1.000000000000000444, 0.9999999999999997780, 1.000000000000000444, 0.9999999999999997780, 1.000000000000000000, 1.000000000000000222, 1.000000000000000000, 0.9999999999999997780, 1.000000000000000222, 1.000000000000000222, 0.9999999999999997780, 1.000000000000000000, 1.000000000000000222, 0.9999999999999997780, 1.000000000000000444, 0.9999999999999997780, 1.000000000000000444, 0.9999999999999997780, 1.000000000000000000, 1.000000000000000222, 0.9999999999999996669, 1.000000000000000000, 1.000000000000000000, 1.000000000000000444, 1.000000000000000222, 0.9999999999999997780, 1.000000000000000222, 1.000000000000000222, 1.000000000000000000, 1.000000000000000222, 0.9999999999999997780, 1.000000000000000000, 1.000000000000000222, 0.9999999999999996669, 1.000000000000000000, 1.000000000000000000, 1.000000000000000000, 1.000000000000000000, 1.000000000000000000, 1.000000000000000000, 1.000000000000000000, 0.9999999999999997780, 1.000000000000000222, 0.9999999999999997780, 1.000000000000000000, 0.9999999999999997780, 1.000000000000000222, 1.000000000000000000, 1.000000000000000000, 1.000000000000000000, 1.000000000000000222, 0.9999999999999997780, 0.9999999999999997780, 1.000000000000000222, 1.000000000000000222, 1.000000000000000000, 1.000000000000000444, 0.9999999999999996669, 1.000000000000000444, 0.9999999999999997780, 1.000000000000000222, 1.000000000000000000, 1.000000000000000000, 1.000000000000000000, 1.000000000000000222, 0.9999999999999997780, 0.9999999999999997780, 1.000000000000000444, 1.000000000000000444, 0.9999999999999997780, 1.000000000000000000, 1.000000000000000000, 1.000000000000000000, 1.000000000000000222, 1.000000000000000000, 1.000000000000000000, 1.000000000000000222, 1.000000000000000222, 1.000000000000000000, 1.000000000000000444, 1.000000000000000000, 1.000000000000000222, 1.000000000000000000, 1.000000000000000000, 1.000000000000000444, 1.000000000000000000, 1.000000000000000222, 1.000000000000000000, 1.000000000000000222, 0.9999999999999997780, 1.000000000000000222, 1.000000000000000222, 1.000000000000000000, 0.9999999999999996669, 1.000000000000000222, 1.000000000000000000, 1.000000000000000000, 1.000000000000000222, 1.000000000000000222, 1.000000000000000222, 0.9999999999999997780, 1.000000000000000000, 1.000000000000000222, 1.000000000000000000, 1.000000000000000000, 1.000000000000000000, 0.9999999999999996669, 1.000000000000000444, 1.000000000000000222, 0.9999999999999996669, 1.000000000000000444, 1.000000000000000000, 1.000000000000000000, 1.000000000000000222, 0.9999999999999997780, 1.000000000000000444, 0.9999999999999997780, 0.9999999999999997780, 1.000000000000000444, 0.9999999999999997780, 1.000000000000000222, 1.000000000000000000, 1.000000000000000000, 1.000000000000000000, 0.9999999999999997780, 1.000000000000000000, 1.000000000000000222, 0.9999999999999996669, 1.000000000000000222, 1.000000000000000000, 1.000000000000000222, 0.9999999999999996669, 0.9999999999999997780, 1.000000000000000444, 0.9999999999999997780, 0.9999999999999997780, 1.000000000000000000, 1.000000000000000222, 1.000000000000000000, 1.000000000000000000, 0.9999999999999996669, 1.000000000000000222, 1.000000000000000000, 0.9999999999999997780, 1.000000000000000000, 1.000000000000000000, 0.9999999999999997780, 1.000000000000000444, 0.9999999999999996669, 1.000000000000000444, 0.9999999999999997780, 1.000000000000000000, 1.000000000000000222, 0.9999999999999997780, 1.000000000000000222, 1.000000000000000222, 0.9999999999999997780, 1.000000000000000000, 1.000000000000000000, 1.000000000000000000, 1.000000000000000222, 1.000000000000000000, 1.000000000000000000, 1.000000000000000222, 1.000000000000000222, 1.000000000000000000, 1.000000000000000000, 1.000000000000000222, 0.9999999999999997780, 1.000000000000000000, 1.000000000000000222, 1.000000000000000000, 1.000000000000000222, 0.9999999999999997780, 1.000000000000000222, 0.9999999999999997780, 1.000000000000000222, 0.9999999999999997780, 1.000000000000000222, 1.000000000000000000, 1.000000000000000000, 1.000000000000000444, 0.9999999999999996669, 1.000000000000000222, 0.9999999999999997780, 1.000000000000000000, 1.000000000000000222, 1.000000000000000000, 1.000000000000000222, 0.9999999999999997780, 0.9999999999999997780, 1.000000000000000000, 0.9999999999999997780, 1.000000000000000000, 1.000000000000000000, 1.000000000000000222, 1.000000000000000000, 1.000000000000000000, 1.000000000000000222, 1.000000000000000000, 1.000000000000000000, 1.000000000000000000, 1.000000000000000000, 0.9999999999999997780, 1.000000000000000222, 1.000000000000000222, 0.9999999999999997780, 1.000000000000000444, 1.000000000000000444, 0.9999999999999997780, 1.000000000000000000, 0.9999999999999997780, 1.000000000000000000, 1.000000000000000000, 1.000000000000000000, 1.000000000000000000, 0.9999999999999997780, 1.000000000000000222, 1.000000000000000000, 0.9999999999999997780, 1.000000000000000222, 1.000000000000000000, 1.000000000000000000, 1.000000000000000000, 1.000000000000000444, 1.000000000000000000, 0.9999999999999997780, 0.9999999999999997780, 0.9999999999999997780, 1.000000000000000222, 1.000000000000000222, 0.9999999999999996669, 1.000000000000000222, 0.9999999999999997780, 1.000000000000000222, 1.000000000000000000, 1.000000000000000000, 0.9999999999999996669, 1.000000000000000222, 1.000000000000000222, 1.000000000000000000, 1.000000000000000000, 1.000000000000000222, 0.9999999999999997780, 1.000000000000000000, 1.000000000000000222, 0.9999999999999994449, 1.000000000000000222, 1.000000000000000000, 1.000000000000000222, 0.9999999999999997780, 1.000000000000000000, 1.000000000000000000, 0.9999999999999997780, 1.000000000000000000, 1.000000000000000222, 0.9999999999999997780, 1.000000000000000000, 1.000000000000000000, 1.000000000000000000, 1.000000000000000000, 1.000000000000000222, 1.000000000000000000, 0.9999999999999996669, 0.9999999999999996669, 1.000000000000000222, 0.9999999999999997780, 1.000000000000000222, 1.000000000000000000, 0.9999999999999997780, 1.000000000000000222, 0.9999999999999997780, 1.000000000000000444, 1.000000000000000222, 1.000000000000000000, 1.000000000000000222, 1.000000000000000222, 1.000000000000000000, 1.000000000000000000, 1.000000000000000000, 1.000000000000000000, 1.000000000000000000, 1.000000000000000000, 1.000000000000000000, 0.9999999999999997780, 1.000000000000000000, 0.9999999999999996669, 1.000000000000000444, 0.9999999999999996669, 1.000000000000000000, 1.000000000000000000, 0.9999999999999997780, 1.000000000000000444, 1.000000000000000000, 1.000000000000000000, 1.000000000000000000),
 ( 0.3333333333333334259, 0.3333333333333334259, 0.3333333333333333703, 0.3333333333333333703, 0.3333333333333334259, 0.3333333333333333703, 0.3333333333333333703, 0.3333333333333334259, 0.3333333333333333148, 0.3333333333333334814, 0.3333333333333332593, 0.3333333333333335369, 0.3333333333333333148, 0.3333333333333333703, 0.3333333333333334259, 0.3333333333333332593, 0.3333333333333333703, 0.3333333333333333703, 0.3333333333333334259, 0.3333333333333334814, 0.3333333333333333148, 0.3333333333333334259, 0.3333333333333333703, 0.3333333333333333703, 0.3333333333333333148, 0.3333333333333333703, 0.3333333333333334259, 0.3333333333333332038, 0.3333333333333334259, 0.3333333333333333703, 0.3333333333333334259, 0.3333333333333333703, 0.3333333333333333148, 0.3333333333333334259, 0.3333333333333334259, 0.3333333333333333703, 0.3333333333333334814, 0.3333333333333332593, 0.3333333333333334259, 0.3333333333333334259, 0.3333333333333333148, 0.3333333333333333703, 0.3333333333333333148, 0.3333333333333333703, 0.3333333333333333148, 0.3333333333333333703, 0.3333333333333333703, 0.3333333333333333703, 0.3333333333333333148, 0.3333333333333333148, 0.3333333333333334259, 0.3333333333333332593, 0.3333333333333333703, 0.3333333333333333703, 0.3333333333333333703, 0.3333333333333332593, 0.3333333333333334259, 0.3333333333333333148, 0.3333333333333333148, 0.3333333333333333703, 0.3333333333333333703, 0.3333333333333333703, 0.3333333333333334259, 0.3333333333333333148, 0.3333333333333334259, 0.3333333333333334259, 0.3333333333333333703, 0.3333333333333333703, 0.3333333333333333148, 0.3333333333333333703, 0.3333333333333333703, 0.3333333333333333148, 0.3333333333333333703, 0.3333333333333332593, 0.3333333333333334814, 0.3333333333333333148, 0.3333333333333333703, 0.3333333333333332593, 0.3333333333333335369, 0.3333333333333333703, 0.3333333333333333703, 0.3333333333333333703, 0.3333333333333334259, 0.3333333333333334259, 0.3333333333333333148, 0.3333333333333334259, 0.3333333333333333148, 0.3333333333333333703, 0.3333333333333335369, 0.3333333333333333148, 0.3333333333333334259, 0.3333333333333334814, 0.3333333333333333148, 0.3333333333333335369, 0.3333333333333332593, 0.3333333333333333703, 0.3333333333333333148, 0.3333333333333334259, 0.3333333333333333148, 0.3333333333333334814, 0.3333333333333333703, 0.3333333333333333148, 0.3333333333333333703, 0.3333333333333334259, 0.3333333333333333703, 0.3333333333333334259, 0.3333333333333332593, 0.3333333333333335924, 0.3333333333333333148, 0.3333333333333333148, 0.3333333333333334259, 0.3333333333333332593, 0.3333333333333333703, 0.3333333333333333148, 0.3333333333333335369, 0.3333333333333333703, 0.3333333333333333703, 0.3333333333333334259, 0.3333333333333334259, 0.3333333333333333703, 0.3333333333333333703, 0.3333333333333333703, 0.3333333333333333703, 0.3333333333333334259, 0.3333333333333333703, 0.3333333333333333703, 0.3333333333333333703, 0.3333333333333334259, 0.3333333333333333148, 0.3333333333333333703, 0.3333333333333333703, 0.3333333333333334259, 0.3333333333333333148, 0.3333333333333333703, 0.3333333333333333703, 0.3333333333333333703, 0.3333333333333333148, 0.3333333333333334259, 0.3333333333333333148, 0.3333333333333333703, 0.3333333333333334259, 0.3333333333333333703, 0.3333333333333333703, 0.3333333333333333703, 0.3333333333333333703, 0.3333333333333334259, 0.3333333333333334259, 0.3333333333333334259, 0.3333333333333333148, 0.3333333333333334259, 0.3333333333333333148, 0.3333333333333334259, 0.3333333333333334259, 0.3333333333333333703, 0.3333333333333333148, 0.3333333333333333703, 0.3333333333333333703, 0.3333333333333333148, 0.3333333333333334259, 0.3333333333333335369, 0.3333333333333333148, 0.3333333333333332593, 0.3333333333333334814, 0.3333333333333332593, 0.3333333333333333703, 0.3333333333333333703, 0.3333333333333333703, 0.3333333333333334259, 0.3333333333333334259, 0.3333333333333334259, 0.3333333333333335369, 0.3333333333333333703, 0.3333333333333333703, 0.3333333333333333703, 0.3333333333333334259, 0.3333333333333333703, 0.3333333333333333703, 0.3333333333333334259, 0.3333333333333333703, 0.3333333333333334259, 0.3333333333333332593, 0.3333333333333334259, 0.3333333333333334259, 0.3333333333333333148, 0.3333333333333333703, 0.3333333333333333703, 0.3333333333333333703, 0.3333333333333333703, 0.3333333333333334259, 0.3333333333333334259, 0.3333333333333334259, 0.3333333333333333148, 0.3333333333333333703, 0.3333333333333334259, 0.3333333333333332593, 0.3333333333333334814, 0.3333333333333333148, 0.3333333333333332593, 0.3333333333333335369, 0.3333333333333333148, 0.3333333333333333703, 0.3333333333333334259, 0.3333333333333333148, 0.3333333333333333703, 0.3333333333333334259, 0.3333333333333333148, 0.3333333333333335369, 0.3333333333333332593, 0.3333333333333333703, 0.3333333333333334259, 0.3333333333333333148, 0.3333333333333334259, 0.3333333333333333148, 0.3333333333333333703, 0.3333333333333333703, 0.3333333333333333703, 0.3333333333333333703, 0.3333333333333334259, 0.3333333333333332593, 0.3333333333333334259, 0.3333333333333334259, 0.3333333333333333703, 0.3333333333333333703, 0.3333333333333333148, 0.3333333333333334814, 0.3333333333333333703, 0.3333333333333332593, 0.3333333333333334259, 0.3333333333333334259, 0.3333333333333334259, 0.3333333333333333703, 0.3333333333333332038, 0.3333333333333335369, 0.3333333333333333148, 0.3333333333333333148, 0.3333333333333333703, 0.3333333333333333703, 0.3333333333333333703, 0.3333333333333334259, 0.3333333333333333148, 0.3333333333333334814, 0.3333333333333333148, 0.3333333333333333703, 0.3333333333333334259, 0.3333333333333333148, 0.3333333333333334259, 0.3333333333333333148, 0.3333333333333334259, 0.3333333333333333148, 0.3333333333333333703, 0.3333333333333333703, 0.3333333333333334259, 0.3333333333333333703, 0.3333333333333333148, 0.3333333333333334814, 0.3333333333333334259, 0.3333333333333333703, 0.3333333333333333148, 0.3333333333333334259, 0.3333333333333333703, 0.3333333333333333703, 0.3333333333333334259, 0.3333333333333333703, 0.3333333333333334814, 0.3333333333333333148, 0.3333333333333334259, 0.3333333333333333703, 0.3333333333333334259, 0.3333333333333333148, 0.3333333333333333703, 0.3333333333333334259, 0.3333333333333333703, 0.3333333333333334259, 0.3333333333333332593, 0.3333333333333333703, 0.3333333333333332593, 0.3333333333333334259, 0.3333333333333333703, 0.3333333333333334259, 0.3333333333333334259, 0.3333333333333333148, 0.3333333333333333148, 0.3333333333333334259, 0.3333333333333333148, 0.3333333333333333148, 0.3333333333333333703, 0.3333333333333333703, 0.3333333333333334259, 0.3333333333333333703, 0.3333333333333334814, 0.3333333333333332593, 0.3333333333333334259, 0.3333333333333333703, 0.3333333333333333703, 0.3333333333333334259, 0.3333333333333333703, 0.3333333333333333703, 0.3333333333333334259, 0.3333333333333334259, 0.3333333333333334814, 0.3333333333333333148, 0.3333333333333333148, 0.3333333333333333703, 0.3333333333333333148, 0.3333333333333334259, 0.3333333333333333703, 0.3333333333333333148, 0.3333333333333332593, 0.3333333333333334259, 0.3333333333333334259, 0.3333333333333333148, 0.3333333333333333703, 0.3333333333333334259, 0.3333333333333333148, 0.3333333333333334259, 0.3333333333333334259, 0.3333333333333334814, 0.3333333333333333148, 0.3333333333333333703, 0.3333333333333332593, 0.3333333333333334814, 0.3333333333333333703, 0.3333333333333332593, 0.3333333333333334814, 0.3333333333333332593, 0.3333333333333334259, 0.3333333333333333703, 0.3333333333333333148, 0.3333333333333333148, 0.3333333333333334259, 0.3333333333333333703, 0.3333333333333333703, 0.3333333333333333703, 0.3333333333333333703, 0.3333333333333334259, 0.3333333333333333148, 0.3333333333333334259, 0.3333333333333332038, 0.3333333333333334259, 0.3333333333333333148, 0.3333333333333334814, 0.3333333333333333703, 0.3333333333333333703, 0.3333333333333334259, 0.3333333333333333148, 0.3333333333333333703, 0.3333333333333333703, 0.3333333333333333703, 0.3333333333333333703, 0.3333333333333333703, 0.3333333333333334259, 0.3333333333333333148, 0.3333333333333334814, 0.3333333333333334259, 0.3333333333333332593, 0.3333333333333333703, 0.3333333333333333703, 0.3333333333333333703, 0.3333333333333333703, 0.3333333333333333703, 0.3333333333333334259, 0.3333333333333333148, 0.3333333333333333703, 0.3333333333333334259, 0.3333333333333335369, 0.3333333333333333148, 0.3333333333333333703, 0.3333333333333334259, 0.3333333333333333703, 0.3333333333333333703, 0.3333333333333333703, 0.3333333333333333703, 0.3333333333333333703, 0.3333333333333333703, 0.3333333333333333703, 0.3333333333333333703, 0.3333333333333334259, 0.3333333333333332593, 0.3333333333333334814, 0.3333333333333332593, 0.3333333333333334259, 0.3333333333333333703, 0.3333333333333333703, 0.3333333333333334814, 0.3333333333333333148, 0.3333333333333333703, 0.3333333333333333703),
 ( 0.3333333333333334259, 0.3333333333333334259, 0.3333333333333333703, 0.3333333333333333703, 0.3333333333333334259, 0.3333333333333333703, 0.3333333333333333703, 0.3333333333333334259, 0.3333333333333333148, 0.3333333333333334814, 0.3333333333333332593, 0.3333333333333335369, 0.3333333333333333148, 0.3333333333333333703, 0.3333333333333334259, 0.3333333333333332593, 0.3333333333333333703, 0.3333333333333333703, 0.3333333333333334259, 0.3333333333333334814, 0.3333333333333333148, 0.3333333333333334259, 0.3333333333333333703, 0.3333333333333333703, 0.3333333333333333148, 0.3333333333333333703, 0.3333333333333334259, 0.3333333333333332038, 0.3333333333333334259, 0.3333333333333333703, 0.3333333333333334259, 0.3333333333333333703, 0.3333333333333333148, 0.3333333333333334259, 0.3333333333333334259, 0.3333333333333333703, 0.3333333333333334814, 0.3333333333333332593, 0.3333333333333334259, 0.3333333333333334259, 0.3333333333333333148, 0.3333333333333333703, 0.3333333333333333148, 0.3333333333333333703, 0.3333333333333333148, 0.3333333333333333703, 0.3333333333333333703, 0.3333333333333333703, 0.3333333333333333148, 0.3333333333333333148, 0.3333333333333334259, 0.3333333333333332593, 0.3333333333333333703, 0.3333333333333333703, 0.3333333333333333703, 0.3333333333333332593, 0.3333333333333334259, 0.3333333333333333148, 0.3333333333333333148, 0.3333333333333333703, 0.3333333333333333703, 0.3333333333333333703, 0.3333333333333334259, 0.3333333333333333148, 0.3333333333333334259, 0.3333333333333334259, 0.3333333333333333703, 0.3333333333333333703, 0.3333333333333333148, 0.3333333333333333703, 0.3333333333333333703, 0.3333333333333333148, 0.3333333333333333703, 0.3333333333333332593, 0.3333333333333334814, 0.3333333333333333148, 0.3333333333333333703, 0.3333333333333332593, 0.3333333333333335369, 0.3333333333333333703, 0.3333333333333333703, 0.3333333333333333703, 0.3333333333333334259, 0.3333333333333334259, 0.3333333333333333148, 0.3333333333333334259, 0.3333333333333333148, 0.3333333333333333703, 0.3333333333333335369, 0.3333333333333333148, 0.3333333333333334259, 0.3333333333333334814, 0.3333333333333333148, 0.3333333333333335369, 0.3333333333333332593, 0.3333333333333333703, 0.3333333333333333148, 0.3333333333333334259, 0.3333333333333333148, 0.3333333333333334814, 0.3333333333333333703, 0.3333333333333333148, 0.3333333333333333703, 0.3333333333333334259, 0.3333333333333333703, 0.3333333333333334259, 0.3333333333333332593, 0.3333333333333335924, 0.3333333333333333148, 0.3333333333333333148, 0.3333333333333334259, 0.3333333333333332593, 0.3333333333333333703, 0.3333333333333333148, 0.3333333333333335369, 0.3333333333333333703, 0.3333333333333333703, 0.3333333333333334259, 0.3333333333333334259, 0.3333333333333333703, 0.3333333333333333703, 0.3333333333333333703, 0.3333333333333333703, 0.3333333333333334259, 0.3333333333333333703, 0.3333333333333333703, 0.3333333333333333703, 0.3333333333333334259, 0.3333333333333333148, 0.3333333333333333703, 0.3333333333333333703, 0.3333333333333334259, 0.3333333333333333148, 0.3333333333333333703, 0.3333333333333333703, 0.3333333333333333703, 0.3333333333333333148, 0.3333333333333334259, 0.3333333333333333148, 0.3333333333333333703, 0.3333333333333334259, 0.3333333333333333703, 0.3333333333333333703, 0.3333333333333333703, 0.3333333333333333703, 0.3333333333333334259, 0.3333333333333334259, 0.3333333333333334259, 0.3333333333333333148, 0.3333333333333334259, 0.3333333333333333148, 0.3333333333333334259, 0.3333333333333334259, 0.3333333333333333703, 0.3333333333333333148, 0.3333333333333333703, 0.3333333333333333703, 0.3333333333333333148, 0.3333333333333334259, 0.3333333333333335369, 0.3333333333333333148, 0.3333333333333332593, 0.3333333333333334814, 0.3333333333333332593, 0.3333333333333333703, 0.3333333333333333703, 0.3333333333333333703, 0.3333333333333334259, 0.3333333333333334259, 0.3333333333333334259, 0.3333333333333335369, 0.3333333333333333703, 0.3333333333333333703, 0.3333333333333333703, 0.3333333333333334259, 0.3333333333333333703, 0.3333333333333333703, 0.3333333333333334259, 0.3333333333333333703, 0.3333333333333334259, 0.3333333333333332593, 0.3333333333333334259, 0.3333333333333334259, 0.3333333333333333148, 0.3333333333333333703, 0.3333333333333333703, 0.3333333333333333703, 0.3333333333333333703, 0.3333333333333334259, 0.3333333333333334259, 0.3333333333333334259, 0.3333333333333333148, 0.3333333333333333703, 0.3333333333333334259, 0.3333333333333332593, 0.3333333333333334814, 0.3333333333333333148, 0.3333333333333332593, 0.3333333333333335369, 0.3333333333333333148, 0.3333333333333333703, 0.3333333333333334259, 0.3333333333333333148, 0.3333333333333333703, 0.3333333333333334259, 0.3333333333333333148, 0.3333333333333335369, 0.3333333333333332593, 0.3333333333333333703, 0.3333333333333334259, 0.3333333333333333148, 0.3333333333333334259, 0.3333333333333333148, 0.3333333333333333703, 0.3333333333333333703, 0.3333333333333333703, 0.3333333333333333703, 0.3333333333333334259, 0.3333333333333332593, 0.3333333333333334259, 0.3333333333333334259, 0.3333333333333333703, 0.3333333333333333703, 0.3333333333333333148, 0.3333333333333334814, 0.3333333333333333703, 0.3333333333333332593, 0.3333333333333334259, 0.3333333333333334259, 0.3333333333333334259, 0.3333333333333333703, 0.3333333333333332038, 0.3333333333333335369, 0.3333333333333333148, 0.3333333333333333148, 0.3333333333333333703, 0.3333333333333333703, 0.3333333333333333703, 0.3333333333333334259, 0.3333333333333333148, 0.3333333333333334814, 0.3333333333333333148, 0.3333333333333333703, 0.3333333333333334259, 0.3333333333333333148, 0.3333333333333334259, 0.3333333333333333148, 0.3333333333333334259, 0.3333333333333333148, 0.3333333333333333703, 0.3333333333333333703, 0.3333333333333334259, 0.3333333333333333703, 0.3333333333333333148, 0.3333333333333334814, 0.3333333333333334259, 0.3333333333333333703, 0.3333333333333333148, 0.3333333333333334259, 0.3333333333333333703, 0.3333333333333333703, 0.3333333333333334259, 0.3333333333333333703, 0.3333333333333334814, 0.3333333333333333148, 0.3333333333333334259, 0.3333333333333333703, 0.3333333333333334259, 0.3333333333333333148, 0.3333333333333333703, 0.3333333333333334259, 0.3333333333333333703, 0.3333333333333334259, 0.3333333333333332593, 0.3333333333333333703, 0.3333333333333332593, 0.3333333333333334259, 0.3333333333333333703, 0.3333333333333334259, 0.3333333333333334259, 0.3333333333333333148, 0.3333333333333333148, 0.3333333333333334259, 0.3333333333333333148, 0.3333333333333333148, 0.3333333333333333703, 0.3333333333333333703, 0.3333333333333334259, 0.3333333333333333703, 0.3333333333333334814, 0.3333333333333332593, 0.3333333333333334259, 0.3333333333333333703, 0.3333333333333333703, 0.3333333333333334259, 0.3333333333333333703, 0.3333333333333333703, 0.3333333333333334259, 0.3333333333333334259, 0.3333333333333334814, 0.3333333333333333148, 0.3333333333333333148, 0.3333333333333333703, 0.3333333333333333148, 0.3333333333333334259, 0.3333333333333333703, 0.3333333333333333148, 0.3333333333333332593, 0.3333333333333334259, 0.3333333333333334259, 0.3333333333333333148, 0.3333333333333333703, 0.3333333333333334259, 0.3333333333333333148, 0.3333333333333334259, 0.3333333333333334259, 0.3333333333333334814, 0.3333333333333333148, 0.3333333333333333703, 0.3333333333333332593, 0.3333333333333334814, 0.3333333333333333703, 0.3333333333333332593, 0.3333333333333334814, 0.3333333333333332593, 0.3333333333333334259, 0.3333333333333333703, 0.3333333333333333148, 0.3333333333333333148, 0.3333333333333334259, 0.3333333333333333703, 0.3333333333333333703, 0.3333333333333333703, 0.3333333333333333703, 0.3333333333333334259, 0.3333333333333333148, 0.3333333333333334259, 0.3333333333333332038, 0.3333333333333334259, 0.3333333333333333148, 0.3333333333333334814, 0.3333333333333333703, 0.3333333333333333703, 0.3333333333333334259, 0.3333333333333333148, 0.3333333333333333703, 0.3333333333333333703, 0.3333333333333333703, 0.3333333333333333703, 0.3333333333333333703, 0.3333333333333334259, 0.3333333333333333148, 0.3333333333333334814, 0.3333333333333334259, 0.3333333333333332593, 0.3333333333333333703, 0.3333333333333333703, 0.3333333333333333703, 0.3333333333333333703, 0.3333333333333333703, 0.3333333333333334259, 0.3333333333333333148, 0.3333333333333333703, 0.3333333333333334259, 0.3333333333333335369, 0.3333333333333333148, 0.3333333333333333703, 0.3333333333333334259, 0.3333333333333333703, 0.3333333333333333703, 0.3333333333333333703, 0.3333333333333333703, 0.3333333333333333703, 0.3333333333333333703, 0.3333333333333333703, 0.3333333333333333703, 0.3333333333333334259, 0.3333333333333332593, 0.3333333333333334814, 0.3333333333333332593, 0.3333333333333334259, 0.3333333333333333703, 0.3333333333333333703, 0.3333333333333334814, 0.3333333333333333148, 0.3333333333333333703, 0.3333333333333333703),
 ( 1.000000000000000222, 1.000000000000000222, 0.9999999999999997780, 1.000000000000000222, 1.000000000000000000, 1.000000000000000000, 0.9999999999999997780, 1.000000000000000000, 1.000000000000000000, 1.000000000000000000, 1.000000000000000000, 1.000000000000000222, 1.000000000000000000, 1.000000000000000000, 1.000000000000000222, 0.9999999999999994449, 1.000000000000000222, 1.000000000000000000, 0.9999999999999997780, 1.000000000000000444, 1.000000000000000000, 1.000000000000000222, 1.000000000000000000, 1.000000000000000000, 0.9999999999999996669, 1.000000000000000000, 1.000000000000000222, 0.9999999999999996669, 1.000000000000000222, 1.000000000000000000, 1.000000000000000222, 1.000000000000000000, 1.000000000000000222, 0.9999999999999997780, 1.000000000000000444, 1.000000000000000000, 1.000000000000000222, 0.9999999999999997780, 1.000000000000000222, 1.000000000000000000, 1.000000000000000000, 0.9999999999999997780, 1.000000000000000000, 0.9999999999999997780, 1.000000000000000000, 0.9999999999999997780, 1.000000000000000000, 1.000000000000000000, 0.9999999999999997780, 1.000000000000000000, 1.000000000000000222, 0.9999999999999996669, 1.000000000000000000, 1.000000000000000000, 1.000000000000000222, 0.9999999999999997780, 1.000000000000000444, 1.000000000000000000, 0.9999999999999997780, 1.000000000000000000, 1.000000000000000000, 1.000000000000000000, 1.000000000000000222, 1.000000000000000000, 1.000000000000000000, 1.000000000000000222, 1.000000000000000000, 1.000000000000000000, 0.9999999999999997780, 1.000000000000000222, 1.000000000000000000, 0.9999999999999997780, 1.000000000000000000, 1.000000000000000000, 1.000000000000000000, 1.000000000000000000, 1.000000000000000222, 0.9999999999999996669, 1.000000000000000444, 0.9999999999999996669, 1.000000000000000000, 0.9999999999999996669, 1.000000000000000444, 1.000000000000000000, 1.000000000000000000, 1.000000000000000222, 1.000000000000000000, 1.000000000000000000, 1.000000000000000222, 0.9999999999999997780, 1.000000000000000000, 1.000000000000000444, 0.9999999999999997780, 1.000000000000000444, 0.9999999999999997780, 1.000000000000000000, 1.000000000000000222, 1.000000000000000000, 0.9999999999999997780, 1.000000000000000222, 1.000000000000000222, 0.9999999999999997780, 1.000000000000000000, 1.000000000000000222, 0.9999999999999997780, 1.000000000000000444, 0.9999999999999997780, 1.000000000000000444, 0.9999999999999997780, 1.000000000000000000, 1.000000000000000222, 0.9999999999999996669, 1.000000000000000000, 1.000000000000000000, 1.000000000000000444, 1.000000000000000222, 0.9999999999999997780, 1.000000000000000222, 1.000000000000000222, 1.000000000000000000, 1.000000000000000222, 0.9999999999999997780, 1.000000000000000000, 1.000000000000000222, 0.9999999999999996669, 1.000000000000000000, 1.000000000000000000, 1.000000000000000000, 1.000000000000000000, 1.000000000000000000, 1.000000000000000000, 1.000000000000000000, 0.9999999999999997780, 1.000000000000000222, 0.9999999999999997780, 1.000000000000000000, 0.9999999999999997780, 1.000000000000000222, 1.000000000000000000, 1.000000000000000000, 1.000000000000000000, 1.000000000000000222, 0.9999999999999997780, 0.9999999999999997780, 1.000000000000000222, 1.000000000000000222, 1.000000000000000000, 1.000000000000000444, 0.9999999999999996669, 1.000000000000000444, 0.9999999999999997780, 1.000000000000000222, 1.000000000000000000, 1.000000000000000000, 1.000000000000000000, 1.000000000000000222, 0.9999999999999997780, 0.9999999999999997780, 1.000000000000000444, 1.000000000000000444, 0.9999999999999997780, 1.000000000000000000, 1.000000000000000000, 1.000000000000000000, 1.000000000000000222, 1.000000000000000000, 1.000000000000000000, 1.000000000000000222, 1.000000000000000222, 1.000000000000000000, 1.000000000000000444, 1.000000000000000000, 1.000000000000000222, 1.000000000000000000, 1.000000000000000000, 1.000000000000000444, 1.000000000000000000, 1.000000000000000222, 1.000000000000000000, 1.000000000000000222, 0.9999999999999997780, 1.000000000000000222, 1.000000000000000222, 1.000000000000000000, 0.9999999999999996669, 1.000000000000000222, 1.000000000000000000, 1.000000000000000000, 1.000000000000000222, 1.000000000000000222, 1.000000000000000222, 0.9999999999999997780, 1.000000000000000000, 1.000000000000000222, 1.000000000000000000, 1.000000000000000000, 1.000000000000000000, 0.9999999999999996669, 1.000000000000000444, 1.000000000000000222, 0.9999999999999996669, 1.000000000000000444, 1.000000000000000000, 1.000000000000000000, 1.000000000000000222, 0.9999999999999997780, 1.000000000000000444, 0.9999999999999997780, 0.9999999999999997780, 1.000000000000000444, 0.9999999999999997780, 1.000000000000000222, 1.000000000000000000, 1.000000000000000000, 1.000000000000000000, 0.9999999999999997780, 1.000000000000000000, 1.000000000000000222, 0.9999999999999996669, 1.000000000000000222, 1.000000000000000000, 1.000000000000000222, 0.9999999999999996669, 0.9999999999999997780, 1.000000000000000444, 0.9999999999999997780, 0.9999999999999997780, 1.000000000000000000, 1.000000000000000222, 1.000000000000000000, 1.000000000000000000, 0.9999999999999996669, 1.000000000000000222, 1.000000000000000000, 0.9999999999999997780, 1.000000000000000000, 1.000000000000000000, 0.9999999999999997780, 1.000000000000000444, 0.9999999999999996669, 1.000000000000000444, 0.9999999999999997780, 1.000000000000000000, 1.000000000000000222, 0.9999999999999997780, 1.000000000000000222, 1.000000000000000222, 0.9999999999999997780, 1.000000000000000000, 1.000000000000000000, 1.000000000000000000, 1.000000000000000222, 1.000000000000000000, 1.000000000000000000, 1.000000000000000222, 1.000000000000000222, 1.000000000000000000, 1.000000000000000000, 1.000000000000000222, 0.9999999999999997780, 1.000000000000000000, 1.000000000000000222, 1.000000000000000000, 1.000000000000000222, 0.9999999999999997780, 1.000000000000000222, 0.9999999999999997780, 1.000000000000000222, 0.9999999999999997780, 1.000000000000000222, 1.000000000000000000, 1.000000000000000000, 1.000000000000000444, 0.9999999999999996669, 1.000000000000000222, 0.9999999999999997780, 1.000000000000000000, 1.000000000000000222, 1.000000000000000000, 1.000000000000000222, 0.9999999999999997780, 0.9999999999999997780, 1.000000000000000000, 0.9999999999999997780, 1.000000000000000000, 1.000000000000000000, 1.000000000000000222, 1.000000000000000000, 1.000000000000000000, 1.000000000000000222, 1.000000000000000000, 1.000000000000000000, 1.000000000000000000, 1.000000000000000000, 0.9999999999999997780, 1.000000000000000222, 1.000000000000000222, 0.9999999999999997780, 1.000000000000000444, 1.000000000000000444, 0.9999999999999997780, 1.000000000000000000, 0.9999999999999997780, 1.000000000000000000, 1.000000000000000000, 1.000000000000000000, 1.000000000000000000, 0.9999999999999997780, 1.000000000000000222, 1.000000000000000000, 0.9999999999999997780, 1.000000000000000222, 1.000000000000000000, 1.000000000000000000, 1.000000000000000000, 1.000000000000000444, 1.000000000000000000, 0.9999999999999997780, 0.9999999999999997780, 0.9999999999999997780, 1.000000000000000222, 1.000000000000000222, 0.9999999999999996669, 1.000000000000000222, 0.9999999999999997780, 1.000000000000000222, 1.000000000000000000, 1.000000000000000000, 0.9999999999999996669, 1.000000000000000222, 1.000000000000000222, 1.000000000000000000, 1.000000000000000000, 1.000000000000000222, 0.9999999999999997780, 1.000000000000000000, 1.000000000000000222, 0.9999999999999994449, 1.000000000000000222, 1.000000000000000000, 1.000000000000000222, 0.9999999999999997780, 1.000000000000000000, 1.000000000000000000, 0.9999999999999997780, 1.000000000000000000, 1.000000000000000222, 0.9999999999999997780, 1.000000000000000000, 1.000000000000000000, 1.000000000000000000, 1.000000000000000000, 1.000000000000000222, 1.000000000000000000, 0.9999999999999996669, 0.9999999999999996669, 1.000000000000000222, 0.9999999999999997780, 1.000000000000000222, 1.000000000000000000, 0.9999999999999997780, 1.000000000000000222, 0.9999999999999997780, 1.000000000000000444, 1.000000000000000222, 1.000000000000000000, 1.000000000000000222, 1.000000000000000222, 1.000000000000000000, 1.000000000000000000, 1.000000000000000000, 1.000000000000000000, 1.000000000000000000, 1.000000000000000000, 1.000000000000000000, 0.9999999999999997780, 1.000000000000000000, 0.9999999999999996669, 1.000000000000000444, 0.9999999999999996669, 1.000000000000000000, 1.000000000000000000, 0.9999999999999997780, 1.000000000000000444, 1.000000000000000000, 1.000000000000000000, 1.000000000000000000) ) ) 
 REPRESENTATION_ITEM ( '' )  SURFACE ( )  );
#180106=CARTESIAN_POINT ( 'NONE',  ( 6.670655732516626912, 7.629137130509076492, 2.426260288887295502 ) ) ;
#180110=CARTESIAN_POINT ( 'NONE',  ( 0.2862814217290919894, -1.017545141758866789, 1.907252267444502269 ) ) ;
#180113=CARTESIAN_POINT ( 'NONE',  ( 2.168725436055967570, -1.667931858681595880, -0.7425449061374129744 ) ) ;
#180115=CARTESIAN_POINT ( 'NONE',  ( 3.768406797884563453, -1.226484811506942219, 1.352366043108323979 ) ) ;
#180118=CARTESIAN_POINT ( 'NONE',  ( 3.279706249791583872, -1.898816934168370496, 0.5228806403664593150 ) ) ;
#180120=CARTESIAN_POINT ( 'NONE',  ( 4.493657767381210810, -1.941711754461509232, -0.04422589797668275563 ) ) ;
#180124=CARTESIAN_POINT ( 'NONE',  ( 5.414351406770180120, -2.120778210838507150, 0.002142078463891750485 ) ) ;
#180126=CARTESIAN_POINT ( 'NONE',  ( 2.578645926699867363, -1.317302948579327504, 1.386430337501590282 ) ) ;
#180131=CARTESIAN_POINT ( 'NONE',  ( 4.494793336055456834, -1.953237823851183164, -0.4868166104980836684 ) ) ;
#180133=CARTESIAN_POINT ( 'NONE',  ( 5.566980414702134894, -1.652319403193935887, -0.7768266693391965294 ) ) ;
#180134=CARTESIAN_POINT ( 'NONE',  ( 0.4849360239999983002, 1.980737741294085419, 0.6024896509310637693 ) ) ;
#180138=CARTESIAN_POINT ( 'NONE',  ( 5.313307075269409374, -0.2735208697075517947, 1.850433306854900817 ) ) ;
#180149=CARTESIAN_POINT ( 'NONE',  ( 0.8661811918178536907, -2.060611401584189650, 0.1992402130865863485 ) ) ;
#180150=CARTESIAN_POINT ( 'NONE',  ( 2.812237032231167611, 1.173781612916646289, -1.761886306039317285 ) ) ;
#180153=CARTESIAN_POINT ( 'NONE',  ( 6.983263157960365675, -0.006178392973848687020, 2.053544886540019210 ) ) ;
#180158=CARTESIAN_POINT ( 'NONE',  ( 2.291363848578463980, 1.773334254936178356, 1.452501744581054632 ) ) ;
#180159=CARTESIAN_POINT ( 'NONE',  ( 0.02954982209854747910, -1.120125052174587577, -1.442194003765177035 ) ) ;
#180160=CARTESIAN_POINT ( 'NONE',  ( 1.916128293556786044, -1.911906470838855343, 0.05044092668918254141 ) ) ;
#180164=CARTESIAN_POINT ( 'NONE',  ( 1.213140692357208117, 1.643459361250454442, -1.162501220127802437 ) ) ;
#180165=CARTESIAN_POINT ( 'NONE',  ( 1.024179675629211861, 0.9620134025654383247, 1.709582039726687652 ) ) ;
#180169=CARTESIAN_POINT ( 'NONE',  ( 4.171883282844288665, -1.203828960760118694, 1.709054251895093746 ) ) ;
#180170=CARTESIAN_POINT ( 'NONE',  ( 1.973191454406374890, 1.694654629526294087, -0.5103889506637182549 ) ) ;
#180173=CARTESIAN_POINT ( 'NONE',  ( 5.085981902069889315, -2.274473487728204013, -0.2844877896996683142 ) ) ;
#180174=CARTESIAN_POINT ( 'NONE',  ( 4.909954989264024405, 1.196826376938535219, -1.263709391550037031 ) ) ;
#180177=CARTESIAN_POINT ( 'NONE',  ( 4.094866968876837987, 0.9280426781237434142, -1.464329598137555477 ) ) ;
#180181=CARTESIAN_POINT ( 'NONE',  ( 4.932167329841075976, 1.246153044254302289, 1.777787927081382779 ) ) ;
#180183=CARTESIAN_POINT ( 'NONE',  ( 5.981657729715996297, -0.6748525008196132324, 1.900413905137773529 ) ) ;
#180184=CARTESIAN_POINT ( 'NONE',  ( 0.4062500000042400528, 1.895863743059760909, -0.7852924748300097457 ) ) ;
#180187=CARTESIAN_POINT ( 'NONE',  ( 3.434515876041916105, 1.879162883219337665, 0.4232601004234298747 ) ) ;
#180189=CARTESIAN_POINT ( 'NONE',  ( 5.836230100724939085, -1.233609159639902142, -1.847210489216906781 ) ) ;
#180191=CARTESIAN_POINT ( 'NONE',  ( 6.983263157960335477, 6.035714437257905018, 2.641087593604172667 ) ) ;
#180195=CARTESIAN_POINT ( 'NONE',  ( 1.260717678522350838, 2.218966152042425755, 0.1042569218142989779 ) ) ;
#180196=CARTESIAN_POINT ( 'NONE',  ( 6.830524215763060347, -1.208013408316032322, 1.546442907991877558 ) ) ;
#180202=CARTESIAN_POINT ( 'NONE',  ( 4.105966297347532823, 0.6976637339557908435, -1.941222516249243579 ) ) ;
#180206=CARTESIAN_POINT ( 'NONE',  ( 6.468025801952650866, 0.9617254617904011926, 1.604207369834034669 ) ) ;
#180207=CARTESIAN_POINT ( 'NONE',  ( 6.205661552121055635, 1.621658882679182456, 0.6149916719311411262 ) ) ;
#180208=CARTESIAN_POINT ( 'NONE',  ( 4.511116409865087995, -1.705632679577104849, 0.3454082310308664305 ) ) ;
#180210=CARTESIAN_POINT ( 'NONE',  ( 2.736170862265740578, 2.275407485025813692, 0.2777600125268233633 ) ) ;
#180212=CARTESIAN_POINT ( 'NONE',  ( 0.9898993202219902310, -0.4452471680344311511, -1.786356756097874587 ) ) ;
#180214=CARTESIAN_POINT ( 'NONE',  ( 2.437500000000002220, 1.451031289061020857, -1.451031289061217366 ) ) ;
#180215=CARTESIAN_POINT ( 'NONE',  ( 1.518276268637512194, 1.228937244518006011, -1.350148523839814096 ) ) ;
#180216=CARTESIAN_POINT ( 'NONE',  ( 2.531875153343257523, -1.674887184936912909, 1.122499117612890673 ) ) ;
#180217=CARTESIAN_POINT ( 'NONE',  ( 1.763894328224338448, 1.128481436294457740, 1.878420861880884862 ) ) ;
#180219=CARTESIAN_POINT ( 'NONE',  ( 4.612399560509667928, -0.8980232107528103302, -1.905027153144087437 ) ) ;
#180221=CARTESIAN_POINT ( 'NONE',  ( 1.627480586986803868, 0.1543294891723171747, -2.064685722993148342 ) ) ;
#180224=CARTESIAN_POINT ( 'NONE',  ( 3.422626747576805961, -0.8610355553571764631, -1.937992358232228041 ) ) ;
#180226=CARTESIAN_POINT ( 'NONE',  ( -0.01707793031917748464, -0.1336475082493841504, -1.895772241332476682 ) ) ;
#180233=CARTESIAN_POINT ( 'NONE',  ( 3.709244008563481465, 1.704072514596865817, -1.083995235011512515 ) ) ;
#180234=CARTESIAN_POINT ( 'NONE',  ( 0.6925746140923200178, -2.090094003047581861, -0.2575201054717362048 ) ) ;
#180237=CARTESIAN_POINT ( 'NONE',  ( 5.629708122894265365, 1.793948666107824774, -0.4946651665681394139 ) ) ;
#180242=CARTESIAN_POINT ( 'NONE',  ( 6.297740734744428970, -0.6968897171561654336, 1.939616516419547132 ) ) ;
#180246=CARTESIAN_POINT ( 'NONE',  ( 2.372030889105484430, -0.3844106184479143540, 1.690481094739235912 ) ) ;
#180247=CARTESIAN_POINT ( 'NONE',  ( 0.8139225777531241546, 1.606474054549825503, 0.6698172574813018310 ) ) ;
#180248=CARTESIAN_POINT ( 'NONE',  ( 0.2183775786483640735, -2.262126603235939282, 0.4550015798871313577 ) ) ;
#180251=CARTESIAN_POINT ( 'NONE',  ( 2.934896792925650644, 0.2487164785463981398, 2.045624280402899231 ) ) ;
#180253=CARTESIAN_POINT ( 'NONE',  ( 1.616564310028177243, 0.5879328921069119085, -1.928455639302439462 ) ) ;
#180257=CARTESIAN_POINT ( 'NONE',  ( 0.9011734813738042638, 1.610450750236171125, 1.136898926478569383 ) ) ;
#180258=CARTESIAN_POINT ( 'NONE',  ( 4.851772015791367743, -1.356534033432246211, -1.348250844427544282 ) ) ;
#180260=CARTESIAN_POINT ( 'NONE',  ( 6.199877634063251541, -0.7475181258948644381, 2.076568058718592624 ) ) ;
#180264=CARTESIAN_POINT ( 'NONE',  ( -0.04036499569192492781, -1.562578347245877630, -1.279382211958324689 ) ) ;
#180266=CARTESIAN_POINT ( 'NONE',  ( 4.173124822893734986, -2.151704308474690741, -0.8341741560445140591 ) ) ;
#180267=CARTESIAN_POINT ( 'NONE',  ( 4.844172697165038066, -0.9265620464425131653, 1.729294158640543699 ) ) ;
#180268=CARTESIAN_POINT ( 'NONE',  ( 1.446067858876250112, -0.8869304882095051523, 1.749921244195346004 ) ) ;
#180272=CARTESIAN_POINT ( 'NONE',  ( 0.6029268795967283046, 1.958829854606686904, 0.8042956034161384826 ) ) ;
#180275=CARTESIAN_POINT ( 'NONE',  ( 0.6031360380127914755, -1.832534659106283659, 0.1778487281504093076 ) ) ;
#180277=CARTESIAN_POINT ( 'NONE',  ( 3.766621525425926098, -0.8750874339106663458, -1.987059052243181689 ) ) ;
#180279=CARTESIAN_POINT ( 'NONE',  ( 1.775790443353560732, 0.3575140072833470906, -2.090081039791711337 ) ) ;
#180284=CARTESIAN_POINT ( 'NONE',  ( 2.811851269462920744, -2.038842655386669644, 0.2989082417928933810 ) ) ;
#180287=CARTESIAN_POINT ( 'NONE',  ( -0.05938221139379848412, -1.422385081007140117, -1.168950373246782526 ) ) ;
#180289=CARTESIAN_POINT ( 'NONE',  ( -0.02264175331115856477, 0.2280268304470518537, -2.122276614016995744 ) ) ;
#180292=CARTESIAN_POINT ( 'NONE',  ( 0.9665587677401198397, 1.115807381107810192, 1.968008997871427468 ) ) ;
#180294=CARTESIAN_POINT ( 'NONE',  ( 1.019438801881300316, -0.4388897500222695425, 1.757493349343726585 ) ) ;
#180295=CARTESIAN_POINT ( 'NONE',  ( 2.483477273924311834, -0.5967159848992757976, 1.820515277383168540 ) ) ;
#180296=CARTESIAN_POINT ( 'NONE',  ( 3.174344110969638866, -1.018096006688212096, -1.802650257252853772 ) ) ;
#180299=CARTESIAN_POINT ( 'NONE',  ( 1.463681139585114588, 1.942636298559533792, -0.3350429378523085977 ) ) ;
#180300=CARTESIAN_POINT ( 'NONE',  ( 5.391212663409540973, 1.697947877755761947, -0.9101574019480199729 ) ) ;
#180301=CARTESIAN_POINT ( 'NONE',  ( 0.7510979139944070626, 0.6750874020578813139, 2.206752807669599470 ) ) ;
#180304=CARTESIAN_POINT ( 'NONE',  ( 5.687952575977194947, -1.305682642493616541, -1.596842856974973301 ) ) ;
#180309=CARTESIAN_POINT ( 'NONE',  ( 6.821333371289608927, -0.1635999628400324479, 2.070553102365073173 ) ) ;
#180311=CARTESIAN_POINT ( 'NONE',  ( 4.534552404040613105, 2.118918870418550870, 0.4265773709258223190 ) ) ;
#180312=CARTESIAN_POINT ( 'NONE',  ( 4.951822102061871789, -1.429791030739693047, -1.426725901824247078 ) ) ;
#180319=CARTESIAN_POINT ( 'NONE',  ( 3.591030000661588062, 1.731995077137841843, 1.032480907900306111 ) ) ;
#180322=CARTESIAN_POINT ( 'NONE',  ( 5.207972885698374022, -2.151664816535401314, 0.2080130470862306957 ) ) ;
#180324=FILL_AREA_STYLE ('',( #196574 ) ) ;
#180327=CARTESIAN_POINT ( 'NONE',  ( 5.062125140741547291, -1.117816439015427044, 1.678017345901124058 ) ) ;
#180329=CARTESIAN_POINT ( 'NONE',  ( 1.312684994149786455, 1.519677550804766852, 0.8159285863849721210 ) ) ;
#180334=CARTESIAN_POINT ( 'NONE',  ( 6.432864026670258362, 0.1834693771665257822, 1.861492386831371748 ) ) ;
#180335=PRODUCT_DEFINITION_FORMATION_WITH_SPECIFIED_SOURCE ( 'ANY', '', #67584, .NOT_KNOWN. ) ;
#180336=CARTESIAN_POINT ( 'NONE',  ( 0.6627443117090633384, 0.5862905632768620201, 1.925809981296212170 ) ) ;
#180338=CARTESIAN_POINT ( 'NONE',  ( 2.731697238759897672, -2.059418846490802313, 0.7933392487004319316 ) ) ;
#180343=CARTESIAN_POINT ( 'NONE',  ( 1.910938629679886480, -0.5684797485801665884, -2.042784538176869003 ) ) ;
#180344=CARTESIAN_POINT ( 'NONE',  ( 1.370720498019749378, -0.2986500928384462350, -1.994069080148860973 ) ) ;
#180345=CARTESIAN_POINT ( 'NONE',  ( 2.320317256442219644, -0.6965147209693119956, -1.672536871252501500 ) ) ;
#180350=CARTESIAN_POINT ( 'NONE',  ( 0.7256311455483875905, 0.7733690622436960593, -1.752846625659326696 ) ) ;
#180357=CARTESIAN_POINT ( 'NONE',  ( 5.243122039519461097, -1.856066598825537373, 1.107904190987746063 ) ) ;
#180360=CARTESIAN_POINT ( 'NONE',  ( 1.652743449602233294, 2.098267697663996234, 0.3060111223712051465 ) ) ;
#180363=CARTESIAN_POINT ( 'NONE',  ( 3.426987366535645396, 0.04501397872612270673, 1.970993176858675699 ) ) ;
#180364=CARTESIAN_POINT ( 'NONE',  ( 5.836178160628028522, -1.067892152678026951, -1.586260290404594597 ) ) ;
#180366=CARTESIAN_POINT ( 'NONE',  ( 6.725064210944283971, -1.800211566667491825, -0.7994317546313032263 ) ) ;
#180367=CARTESIAN_POINT ( 'NONE',  ( 1.376788300709189450, 1.794419955772775355, -0.7429034522522351969 ) ) ;
#180372=CARTESIAN_POINT ( 'NONE',  ( 2.238330470135694750, 0.4590858415520538416, 2.039436070248427324 ) ) ;
#180376=CARTESIAN_POINT ( 'NONE',  ( 5.848291733227988232, 0.9385554955868085081, -1.666026892748099009 ) ) ;
#180378=CARTESIAN_POINT ( 'NONE',  ( 4.020313978404310262, -1.133593497508533110, -1.893353337301090233 ) ) ;
#180379=CARTESIAN_POINT ( 'NONE',  ( 1.624349867039249329, -1.226448341774049267, -1.834376716147153363 ) ) ;
#180381=CARTESIAN_POINT ( 'NONE',  ( 0.3461628310420067911, 0.9829124436787042285, -1.640176041098049264 ) ) ;
#180384=CARTESIAN_POINT ( 'NONE',  ( 4.070807014193541740, 1.466255041752505539, -1.461937513464212079 ) ) ;
#180386=CARTESIAN_POINT ( 'NONE',  ( 1.569428280142046717, 0.1587979871724466974, -2.155937297210829495 ) ) ;
#180387=CARTESIAN_POINT ( 'NONE',  ( 3.790727848299980440, 1.850687065220711469, -1.173560875862532660 ) ) ;
#180395=CARTESIAN_POINT ( 'NONE',  ( 0.7037502660087076034, 1.864169469917423161, 0.7691187473759173443 ) ) ;
#180398=CARTESIAN_POINT ( 'NONE',  ( 4.364170320198999420, -2.065056620294950740, 0.1471644388686063065 ) ) ;
#180399=CARTESIAN_POINT ( 'NONE',  ( 3.633351821168579132, -1.779675539450284560, 0.7381315413402672609 ) ) ;
#180400=CARTESIAN_POINT ( 'NONE',  ( 5.589508065689547500, -0.5136281568550029597, 2.053882654316901313 ) ) ;
#180404=CARTESIAN_POINT ( 'NONE',  ( 4.346514977827297344, -1.947402357529237626, -0.2931004117151541633 ) ) ;
#180405=CARTESIAN_POINT ( 'NONE',  ( 6.509759575370489770, -1.074588918421373940, -2.024802758542126213 ) ) ;
#180406=CARTESIAN_POINT ( 'NONE',  ( 4.459475772512963232, 0.3974328844052883447, -1.781742007231662983 ) ) ;
#180413=CARTESIAN_POINT ( 'NONE',  ( 4.746344407351839045, 1.031357595523854309, -1.728805965807812095 ) ) ;
#180414=CARTESIAN_POINT ( 'NONE',  ( 6.276074014454348315, 2.002121775873589637, -1.129333029253890341 ) ) ;
#180415=CARTESIAN_POINT ( 'NONE',  ( 4.170719094083116474, 1.390339895272204362, -1.384257141873693087 ) ) ;
#180420=CARTESIAN_POINT ( 'NONE',  ( 0.2575178465553956686, 2.067414111102347185, -0.3107122069949171395 ) ) ;
#180421=CARTESIAN_POINT ( 'NONE',  ( 5.998865924308096176, 1.444533723251522073, -1.022291996631684574 ) ) ;
#180422=DIRECTION ( 'NONE',  ( -1.000000000000000000, 1.014813233446432150E-15, 1.972152263052529514E-31 ) ) ;
#180423=CARTESIAN_POINT ( 'NONE',  ( 6.175724022258248347, -1.036883830621424307, 1.641789595683869729 ) ) ;
#180424=CARTESIAN_POINT ( 'NONE',  ( 2.379091696419192381, 2.003018898301941686, -0.8894332929959417600 ) ) ;
#180425=CARTESIAN_POINT ( 'NONE',  ( 1.083124124047912362, -0.7835505874942759741, 1.554128773191378432 ) ) ;
#180428=CARTESIAN_POINT ( 'NONE',  ( 2.226796682701466246, -0.001291377463900899485, 1.725068445404242201 ) ) ;
#180429=CARTESIAN_POINT ( 'NONE',  ( 1.329895901633147748, 1.076045675571284166, -1.909117696414885934 ) ) ;
#180430=CARTESIAN_POINT ( 'NONE',  ( 4.266400587755204477, 1.039063272370500668, 1.946970035688735390 ) ) ;
#180431=CARTESIAN_POINT ( 'NONE',  ( 1.868283874303029446, -2.155004017527381244, 0.2628641719419066991 ) ) ;
#180432=CARTESIAN_POINT ( 'NONE',  ( 0.1350027811974127134, -1.670744041527939094, 0.7364786222084362954 ) ) ;
#180433=CARTESIAN_POINT ( 'NONE',  ( 2.641944905847165792, 2.106676525318150972, -0.2125944600365035908 ) ) ;
#180434=CARTESIAN_POINT ( 'NONE',  ( 6.639320575229253230, 6.038193673056963640, 2.491643636677738360 ) ) ;
#180437=CARTESIAN_POINT ( 'NONE',  ( 2.999882145774832143, -2.289621049425132338, 0.1149546659729560466 ) ) ;
#180442=CARTESIAN_POINT ( 'NONE',  ( 4.653117599668723514, 0.3792583102804178985, 2.188544891856615049 ) ) ;
#180449=CARTESIAN_POINT ( 'NONE',  ( 3.358046224211252095, 0.04667712216412447934, -2.016033814150198999 ) ) ;
#180451=CARTESIAN_POINT ( 'NONE',  ( 2.729405006034294257, 0.1058063225414084541, -2.059999219628326994 ) ) ;
#180452=DIRECTION ( 'NONE',  ( 1.040834085586084257E-15, 1.000000000000000000, -4.622230424712076367E-32 ) ) ;
#180457=CARTESIAN_POINT ( 'NONE',  ( 4.523480939507462217, -1.347072049868164978, -1.728447516733351952 ) ) ;
#180458=CARTESIAN_POINT ( 'NONE',  ( 2.039685609654022347, -1.556907966322677472, 1.281362143053674130 ) ) ;
#180459=CARTESIAN_POINT ( 'NONE',  ( 1.610644152589552958, -0.2245515952020246675, 1.827417025815617935 ) ) ;
#180462=CARTESIAN_POINT ( 'NONE',  ( 5.034128509002383289, 0.9373949799435166153, -1.566401400633938179 ) ) ;
#180463=CARTESIAN_POINT ( 'NONE',  ( 6.434220164165640021, -1.621181005584397372, -1.198863592720422977 ) ) ;
#180465=CARTESIAN_POINT ( 'NONE',  ( 4.522535110384587220, 1.395170471642327437, -1.781064426588598426 ) ) ;
#180467=CARTESIAN_POINT ( 'NONE',  ( 0.9792911203426227784, -0.05348914117170092131, -2.105562491362684252 ) ) ;
#180470=CARTESIAN_POINT ( 'NONE',  ( 5.107906530550561541, 0.6527686194882609261, -1.964817160181751010 ) ) ;
#180478=CARTESIAN_POINT ( 'NONE',  ( 2.162617739553638785, 2.221014589654236371, 0.04931172913892957477 ) ) ;
#180482=CARTESIAN_POINT ( 'NONE',  ( 3.103904542773823660, 0.7086415210641981988, -1.829580771271981154 ) ) ;
#180488=CARTESIAN_POINT ( 'NONE',  ( 2.250376613284802207, 0.9954810856505689198, -1.872389709364124188 ) ) ;
#180490=CARTESIAN_POINT ( 'NONE',  ( 5.248475795274027078, -1.946838731704622072, -0.2419367024937419397 ) ) ;
#180492=CARTESIAN_POINT ( 'NONE',  ( 3.292016909520224743, -0.8776455207864016783, 1.975710135277891633 ) ) ;
#180493=CARTESIAN_POINT ( 'NONE',  ( 2.929072846782492245, -1.238530643895646488, -1.362589426554157157 ) ) ;
#180497=CARTESIAN_POINT ( 'NONE',  ( 4.488070181461626618, -0.3849740463353290010, -1.697036094149968255 ) ) ;
#180501=CARTESIAN_POINT ( 'NONE',  ( 2.061604318190731533, 0.3698614785779800185, -2.129673623264888960 ) ) ;
#180502=CARTESIAN_POINT ( 'NONE',  ( 4.393907559866160994, 0.09612058942952760032, 2.013924333851605297 ) ) ;
#180504=CARTESIAN_POINT ( 'NONE',  ( 0.9015118058452382677, 1.767791302423503685, 1.243857928393626633 ) ) ;
#180505=CARTESIAN_POINT ( 'NONE',  ( 2.389859445797080095, -0.8464594663768022498, 1.780534303499915927 ) ) ;
#180507=CARTESIAN_POINT ( 'NONE',  ( 3.860829347334773232, 0.2347576860389360420, -1.927744540433872888 ) ) ;
#180516=CARTESIAN_POINT ( 'NONE',  ( 1.360703683432495259, 0.8952624662355921359, 2.017188127302282030 ) ) ;
#180518=CARTESIAN_POINT ( 'NONE',  ( 5.207842308544940124, 0.6190457291245822224, -1.861560318597937913 ) ) ;
#180519=CARTESIAN_POINT ( 'NONE',  ( 3.063770578283632862, 1.346675374253442969, 1.633852266970806211 ) ) ;
#180521=CARTESIAN_POINT ( 'NONE',  ( 4.646344025792163990, -1.477054284018078256, 1.098930429567553047 ) ) ;
#180524=CARTESIAN_POINT ( 'NONE',  ( 4.676102344489991403, 2.097148071331572439, -0.3138259731317455392 ) ) ;
#180529=CARTESIAN_POINT ( 'NONE',  ( 6.292271403379039896, -2.050439857688883372, -0.2063938634464974886 ) ) ;
#180531=CARTESIAN_POINT ( 'NONE',  ( 0.2560159283585193846, -1.860519322180047785, -0.05176575080893807551 ) ) ;
#180532=CARTESIAN_POINT ( 'NONE',  ( 3.544333174469185721, -1.503253232081468216, 1.062929765333266108 ) ) ;
#180537=CARTESIAN_POINT ( 'NONE',  ( 3.035963658818414235, -1.482449291622448095, -1.634993338104336891 ) ) ;
#180538=CARTESIAN_POINT ( 'NONE',  ( 4.850980959722003938, -1.821092479232713446, 1.342276170020906711 ) ) ;
#180540=CARTESIAN_POINT ( 'NONE',  ( 5.730666697864316816, 1.210223194361861543, -1.348246716841319692 ) ) ;
#180541=CARTESIAN_POINT ( 'NONE',  ( 5.647645028696767433, 1.886156043628923529, -0.3343808708002778407 ) ) ;
#180543=CARTESIAN_POINT ( 'NONE',  ( 5.770339134078734666, -1.185559297855027561, 1.446973003893243348 ) ) ;
#180545=CARTESIAN_POINT ( 'NONE',  ( 6.109776933011930922, 0.5395433811187456685, -1.781096067677762962 ) ) ;
#180548=CARTESIAN_POINT ( 'NONE',  ( 6.174623306383559829, -1.681873830149778648, -0.5512017132776861894 ) ) ;
#180549=CARTESIAN_POINT ( 'NONE',  ( 1.094935803221647186, 1.780670018850015079, 0.9462964651613046119 ) ) ;
#180551=CARTESIAN_POINT ( 'NONE',  ( 3.422586708326117666, 1.336063110485498973, -1.628023012543792447 ) ) ;
#180555=CARTESIAN_POINT ( 'NONE',  ( 2.285421205933793942, 0.09476354472776055138, -2.017669629103500117 ) ) ;
#180558=CARTESIAN_POINT ( 'NONE',  ( 3.690839692606663558, -0.4176960054509891163, -2.120685484085436112 ) ) ;
#180559=CARTESIAN_POINT ( 'NONE',  ( 6.890000000000050306, -0.002781820520068867264, 1.999840353888074240 ) ) ;
#180567=CARTESIAN_POINT ( 'NONE',  ( 1.365048776756357940, 0.1565470504056795942, -2.186014887712848243 ) ) ;
#180569=CARTESIAN_POINT ( 'NONE',  ( 3.151526295007577527, -1.848778841746369972, -1.303968314058404854 ) ) ;
#180576=CARTESIAN_POINT ( 'NONE',  ( 3.268565602506213974, -1.633896335792903054, -0.6804537918285047393 ) ) ;
#180578=CARTESIAN_POINT ( 'NONE',  ( 3.141273780804701765, 0.05169848057553745602, 2.012594475454997145 ) ) ;
#180579=CARTESIAN_POINT ( 'NONE',  ( 6.528370574810466564, 1.275976099532463381, -1.800301716031265764 ) ) ;
#180583=CARTESIAN_POINT ( 'NONE',  ( 5.132435489663482286, 0.5880379476735001498, 1.928747580961232444 ) ) ;
#180585=CARTESIAN_POINT ( 'NONE',  ( 2.096370420935515178, -0.4963513585865795275, -1.803540123670114736 ) ) ;
#180586=CARTESIAN_POINT ( 'NONE',  ( 3.502843950909264592, 0.4983820457637299639, 2.009271733256080772 ) ) ;
#180588=CARTESIAN_POINT ( 'NONE',  ( 2.039183100597967258, 0.003605121848727563250, 1.912571728241836633 ) ) ;
#180593=CARTESIAN_POINT ( 'NONE',  ( 1.002048865836258518, -0.8573748960705519506, 1.709468765625526521 ) ) ;
#180594=CARTESIAN_POINT ( 'NONE',  ( 3.139059813392345077, -0.1416510307416830594, -1.956792864499560691 ) ) ;
#180595=CARTESIAN_POINT ( 'NONE',  ( 0.7903884775103053872, -1.915307795730587959, 0.6297756287277082032 ) ) ;
#180599=CARTESIAN_POINT ( 'NONE',  ( 6.802032592820894230, -1.970958832386409565, 0.04617810802716794394 ) ) ;
#180601=CARTESIAN_POINT ( 'NONE',  ( 2.144791297303435762, 1.953827510466410455, 0.4849535144586021307 ) ) ;
#180603=CARTESIAN_POINT ( 'NONE',  ( 1.845463042662376818, 0.3584012047737962781, -2.086523245552903472 ) ) ;
#180605=CARTESIAN_POINT ( 'NONE',  ( 3.684089399883890614, -1.230936008959164996, -1.664559344884769088 ) ) ;
#180607=CARTESIAN_POINT ( 'NONE',  ( 5.982390446235332782, -0.3055207467456683701, -2.068066053634140200 ) ) ;
#180609=CARTESIAN_POINT ( 'NONE',  ( 4.577060434696750946, -0.0006114206978560799951, -1.825762228460731551 ) ) ;
#180614=CARTESIAN_POINT ( 'NONE',  ( 6.335036379411270957, 0.2100110484798515254, 2.196758413611602290 ) ) ;
#180616=VERTEX_POINT ( 'NONE', #120272 ) ;
#180617=CARTESIAN_POINT ( 'NONE',  ( 4.723256143441832755, 1.665581346147155806, 0.9393396248940300008 ) ) ;
#180627=CARTESIAN_POINT ( 'NONE',  ( 0.2746299231596514012, 1.718356743839201561, -0.6618312839273902126 ) ) ;
#180631=CARTESIAN_POINT ( 'NONE',  ( 4.762891570102392613, -1.670096840553733752, -0.8426394062573672183 ) ) ;
#180632=CARTESIAN_POINT ( 'NONE',  ( 0.07661050522434449672, 6.948789054712463553, -2.305832378935098514 ) ) ;
#180637=CARTESIAN_POINT ( 'NONE',  ( 0.7077770966438132749, 0.6232387800201264483, -1.868272854783992187 ) ) ;
#180638=CARTESIAN_POINT ( 'NONE',  ( 2.109000121467627498, 0.002830143620808495131, 2.016598147190066914 ) ) ;
#180642=CARTESIAN_POINT ( 'NONE',  ( 2.115410589380119610, -2.125216164159982046, 0.5342070311455533460 ) ) ;
#180653=CARTESIAN_POINT ( 'NONE',  ( 4.370544011308346910, -0.004580445953385886559, -1.841430844414258861 ) ) ;
#180654=CARTESIAN_POINT ( 'NONE',  ( 2.033841672972019676, -1.952135521142538854, 0.4911360252713212193 ) ) ;
#180655=CARTESIAN_POINT ( 'NONE',  ( 3.339543098909302898, -1.371423271284638590, 1.844254897846734131 ) ) ;
#180657=CARTESIAN_POINT ( 'NONE',  ( 0.8130640335680532349, -1.568041438259277554, -1.001899246494031948 ) ) ;
#180660=CARTESIAN_POINT ( 'NONE',  ( 5.502191098127390489, -0.8541586074963626318, 1.711093258865265643 ) ) ;
#180663=CARTESIAN_POINT ( 'NONE',  ( 3.544548742447044987, -1.707904676211311479, 1.205638247120393247 ) ) ;
#180664=CARTESIAN_POINT ( 'NONE',  ( 3.801501934187266230, -0.5436965770258190833, 1.789884385262895616 ) ) ;
#180666=CARTESIAN_POINT ( 'NONE',  ( 5.618664544990171095, -0.03892770779775727580, 1.841008343696965310 ) ) ;
#180669=CARTESIAN_POINT ( 'NONE',  ( 5.426277463695272196, 1.022757762066462961, -1.388784613272223689 ) ) ;
#180671=CARTESIAN_POINT ( 'NONE',  ( 0.6153164582703105623, 0.1250789957258427176, 1.729716150945133535 ) ) ;
#180675=CARTESIAN_POINT ( 'NONE',  ( 5.084931552659712750, 2.075598280349931546, 0.6366630897998347693 ) ) ;
#180676=CARTESIAN_POINT ( 'NONE',  ( 3.158640206316553289, -1.382037546686708973, 1.193037399656725395 ) ) ;
#180677=CARTESIAN_POINT ( 'NONE',  ( 1.639427129605858902, 1.814645582613241714, -0.7458448512465406521 ) ) ;
#180678=CARTESIAN_POINT ( 'NONE',  ( 5.893796404173470727, -2.101076160772547219, 0.2616963346634570975 ) ) ;
#180679=CARTESIAN_POINT ( 'NONE',  ( 5.689115845898126800, 1.733752489355618875, 1.499825188574270607 ) ) ;
#180682=CARTESIAN_POINT ( 'NONE',  ( 1.594549238318817785, -1.131586138893545979, 1.793127659086241499 ) ) ;
#180687=CARTESIAN_POINT ( 'NONE',  ( 6.403213944470495633, -1.838587781526521248, 1.154350301468348272 ) ) ;
#180688=CARTESIAN_POINT ( 'NONE',  ( 6.883263157960330503, 2.417872181280413812, 2.534681901920758929 ) ) ;
#180690=CARTESIAN_POINT ( 'NONE',  ( 2.209928731909744481, 1.719286606775907611, 1.406518386542881638 ) ) ;
#180692=CARTESIAN_POINT ( 'NONE',  ( 6.029922689959810178, -1.701949372586025744, 1.081063231324945528 ) ) ;
#180694=CARTESIAN_POINT ( 'NONE',  ( 5.049704294756152123, 1.524832160660544611, 1.389060530156678297 ) ) ;
#180696=CARTESIAN_POINT ( 'NONE',  ( -0.2409995289980037536, -0.004801160710915518791, -2.000252362011435192 ) ) ;
#180701=CARTESIAN_POINT ( 'NONE',  ( 4.634224865634020141, 0.3196297827482602050, 1.813140464320086132 ) ) ;
#180704=CARTESIAN_POINT ( 'NONE',  ( -0.2104748580754183807, 2.005809028216706924, -2.517884123765606663 ) ) ;
#180705=CARTESIAN_POINT ( 'NONE',  ( 1.359898630301906053, 0.6939498547450100308, 1.579201994853156821 ) ) ;
#180706=CARTESIAN_POINT ( 'NONE',  ( -0.1706859984542466180, -1.561801110730935971, -1.275320528755889526 ) ) ;
#180707=CARTESIAN_POINT ( 'NONE',  ( 2.145563594533715257, 0.9871410470321148045, 2.076082784368099787 ) ) ;
#180709=CARTESIAN_POINT ( 'NONE',  ( 1.177466099744011174, -0.05591215127281846942, -2.261859306125458158 ) ) ;
#180710=CARTESIAN_POINT ( 'NONE',  ( 4.705754021700633949, -0.5625300431781330435, 2.029483779808038957 ) ) ;
#180712=CARTESIAN_POINT ( 'NONE',  ( 2.038023431533928509, 1.749628755847471018, 0.2652362932685590757 ) ) ;
#180718=CARTESIAN_POINT ( 'NONE',  ( 2.549219474610735947, 0.2639673528169217964, 2.104066465523121376 ) ) ;
#180719=CARTESIAN_POINT ( 'NONE',  ( 5.572587854402127228, 0.9002147710611071441, 2.031021293335387501 ) ) ;
#180720=CARTESIAN_POINT ( 'NONE',  ( 3.222796723461582413, 0.05406831605479084368, 2.190948157972896659 ) ) ;
#180723=CARTESIAN_POINT ( 'NONE',  ( 6.375647721065083928, 0.3630326626483972308, -2.089014862189771726 ) ) ;
#180725=CARTESIAN_POINT ( 'NONE',  ( 6.610000000000030518, 1.266345627986571021, 2.115470293623383569 ) ) ;
#180727=CARTESIAN_POINT ( 'NONE',  ( 5.625269520628737752, 1.871107552910089122, 0.9978724776121964402 ) ) ;
#180733=CARTESIAN_POINT ( 'NONE',  ( 6.093280168761200599, -0.6138376400152152357, 1.736067454429328416 ) ) ;
#180736=CARTESIAN_POINT ( 'NONE',  ( 1.856607919947508956, 0.2971036446917668106, -1.714703581143263156 ) ) ;
#180741=CARTESIAN_POINT ( 'NONE',  ( 6.034075718726629844, 1.069613854859407631, -1.878468107683453514 ) ) ;
#180745=CARTESIAN_POINT ( 'NONE',  ( 5.541917325712655717, 0.8799508658935292216, -1.974686638939105343 ) ) ;
#180749=CARTESIAN_POINT ( 'NONE',  ( 5.940691962724923059, 0.3820465716247494758, 1.933821394355714096 ) ) ;
#180750=CARTESIAN_POINT ( 'NONE',  ( 5.061730935934568798, 1.440722419422343803, -0.9642406207952100017 ) ) ;
#180752=CARTESIAN_POINT ( 'NONE',  ( 2.454835928891830221, -1.908367152989149718, -1.077367144120815023 ) ) ;
#180753=CARTESIAN_POINT ( 'NONE',  ( 3.786388324757625323, -1.140120265720317327, 2.006200910446949592 ) ) ;
#180754=CARTESIAN_POINT ( 'NONE',  ( 4.622373940358720290, 1.271062617260295458, -1.621988140548079826 ) ) ;
#180755=CARTESIAN_POINT ( 'NONE',  ( 0.7263842893957738189, 0.1423072432159468159, 1.936797167885440096 ) ) ;
#180759=CARTESIAN_POINT ( 'NONE',  ( 4.306960158517386894, -0.4675538901007176285, -2.068242682749166672 ) ) ;
#180761=CARTESIAN_POINT ( 'NONE',  ( 1.758435621656749603, 1.928751379572872571, -0.5880216644931559600 ) ) ;
#180763=CARTESIAN_POINT ( 'NONE',  ( 4.208205882762393379, -2.201082536721191474, 0.1591639695062776749 ) ) ;
#180767=CARTESIAN_POINT ( 'NONE',  ( 6.825078400183551608, 4.689370880799383912, 2.706890346843467299 ) ) ;
#180770=CARTESIAN_POINT ( 'NONE',  ( 4.399328490915206835, 1.653984737846543540, 1.229246434344443806 ) ) ;
#180772=UNCERTAINTY_MEASURE_WITH_UNIT (LENGTH_MEASURE( 1.000000000000000082E-05 ), #67595, 'distance_accuracy_value', 'NONE');
#180773=CARTESIAN_POINT ( 'NONE',  ( -0.2106854629475400364, 0.7093903261615883693, -2.078205123749873984 ) ) ;
#180775=CARTESIAN_POINT ( 'NONE',  ( 3.211586479193883292, 1.593432852337670624, 1.240894322269629813 ) ) ;
#180779=CARTESIAN_POINT ( 'NONE',  ( 2.905207415116388248, 1.740275362031361794, 1.103647167516639938 ) ) ;
#180783=CARTESIAN_POINT ( 'NONE',  ( -0.1411974294642046046, 7.629137130509075604, -2.500278959528269063 ) ) ;
#180785=CARTESIAN_POINT ( 'NONE',  ( 0.8844010234979463592, 1.624802019249080853, -0.8659260420235401767 ) ) ;
#180787=CARTESIAN_POINT ( 'NONE',  ( 6.586557750117827403, -2.163372447211810989, -0.4352210726449382006 ) ) ;
#180789=CARTESIAN_POINT ( 'NONE',  ( 0.9663661119345479111, 1.064502738163356721, 1.881203019380036867 ) ) ;
#180791=CARTESIAN_POINT ( 'NONE',  ( 2.395720570290179374, -1.993893129684479293, 0.3006499569925198956 ) ) ;
#180792=CARTESIAN_POINT ( 'NONE',  ( 1.827921470121370850, -1.625240468190300103, 1.625389258475460563 ) ) ;
#180794=CARTESIAN_POINT ( 'NONE',  ( 0.1275333129481092398, -1.147091320445620566, -1.478225367208672703 ) ) ;
#180795=CARTESIAN_POINT ( 'NONE',  ( 4.592626242060598329, -0.4308863251132522554, -1.923655822462609466 ) ) ;
#180796=CARTESIAN_POINT ( 'NONE',  ( 5.032435514249763209, 0.5899841883351600869, 1.928258608204669766 ) ) ;
#180800=CARTESIAN_POINT ( 'NONE',  ( 6.059223728125719965, -1.805531155315470926, -1.083989359861557533 ) ) ;
#180801=CARTESIAN_POINT ( 'NONE',  ( 6.689897370947560873, -1.349224794794257720, -1.570457413003906177 ) ) ;
#180804=CARTESIAN_POINT ( 'NONE',  ( 6.539320575229292665, 4.694805244051019066, 2.565894911293948422 ) ) ;
#180805=CARTESIAN_POINT ( 'NONE',  ( 5.361584196017279424, -1.594725845915157647, -1.239436484511841519 ) ) ;
#180807=CARTESIAN_POINT ( 'NONE',  ( 3.387651152892924955, 2.086375235072422285, -0.9864360317304238235 ) ) ;
#180808=CARTESIAN_POINT ( 'NONE',  ( 1.903259321421392425, -1.744647275545135212, 1.099889041785537813 ) ) ;
#180814=CARTESIAN_POINT ( 'NONE',  ( 3.859984642892180684, -0.6334943099049659132, 2.076686793900458294 ) ) ;
#180817=CARTESIAN_POINT ( 'NONE',  ( 2.384105128782065819, -0.3166398734758494315, -1.813660976904336808 ) ) ;
#180819=CARTESIAN_POINT ( 'NONE',  ( 4.089532599075940134, -0.8378280566024614018, 2.025282237563410526 ) ) ;
#180821=CARTESIAN_POINT ( 'NONE',  ( 5.489262863951156923, 1.998152018339900415, -1.061309651537506227 ) ) ;
#180827=CARTESIAN_POINT ( 'NONE',  ( 6.854783864179318620, -1.365764260946045860, 1.125274747944494891 ) ) ;
#180829=CARTESIAN_POINT ( 'NONE',  ( 4.213543065054736303, 1.618255708775760970, 1.197237177376732964 ) ) ;
#180831=CARTESIAN_POINT ( 'NONE',  ( 3.364387735031381332, 0.9452183826245286191, 1.881983119561444040 ) ) ;
#180832=CARTESIAN_POINT ( 'NONE',  ( 2.108866759644252298, 0.002224897612410503371, 1.915793139840407333 ) ) ;
#180834=CARTESIAN_POINT ( 'NONE',  ( 3.701571259021796845, -1.489687541828330852, -1.288469680017936048 ) ) ;
#180835=CARTESIAN_POINT ( 'NONE',  ( 0.6900581440293825919, -1.856003987442723657, -0.2331820809091043056 ) ) ;
#180836=CARTESIAN_POINT ( 'NONE',  ( 0.8187140321147531319, -1.423520202335259999, 1.350257566363553208 ) ) ;
#180837=CARTESIAN_POINT ( 'NONE',  ( 0.5274218815167727170, -0.2782315536139517431, 1.891897276498944347 ) ) ;
#180842=CARTESIAN_POINT ( 'NONE',  ( 6.491075539335432687, 1.626419376453295706, -0.9240138038444990487 ) ) ;
#180845=CARTESIAN_POINT ( 'NONE',  ( 6.508651864089095795, 0.6437109847576475419, 1.967739590238902991 ) ) ;
#180848=CARTESIAN_POINT ( 'NONE',  ( 0.5903903138861701372, 1.065687334306382184, -1.774900233272216798 ) ) ;
#180853=CARTESIAN_POINT ( 'NONE',  ( 5.180389117862056914, 1.045492054797515946, 1.844774357600783121 ) ) ;
#180858=CARTESIAN_POINT ( 'NONE',  ( 6.355910407107248083, -0.6622273607519140182, 1.846833223631501264 ) ) ;
#180860=CARTESIAN_POINT ( 'NONE',  ( 4.552111140598270822, 1.802141083034415781, -0.9039717811075360654 ) ) ;
#180861=CARTESIAN_POINT ( 'NONE',  ( 3.274530738273524033, -0.3788105498489474088, -1.877706502262687760 ) ) ;
#180864=CARTESIAN_POINT ( 'NONE',  ( 1.277182604683280598, 2.023070758711601691, -0.8431670391453591762 ) ) ;
#180865=CARTESIAN_POINT ( 'NONE',  ( 0.2331713839410394229, 1.378908429916062994, -2.211717543205340863 ) ) ;
#180866=CARTESIAN_POINT ( 'NONE',  ( 3.690566713891149320, -0.3619836066245524786, -1.835009008997898761 ) ) ;
#180870=CARTESIAN_POINT ( 'NONE',  ( 5.132460035084068117, 0.6155034331737432307, 2.025765117643091529 ) ) ;
#180872=CARTESIAN_POINT ( 'NONE',  ( 2.173483749353939842, 1.288726691912587041, 1.646222326975780526 ) ) ;
#180874=CARTESIAN_POINT ( 'NONE',  ( 0.2875850076352819973, -0.8198804995633873771, 1.517450437728053325 ) ) ;
#180884=CARTESIAN_POINT ( 'NONE',  ( 1.189788175852508845, 1.078664940389061577, 1.455116354534333079 ) ) ;
#180889=CARTESIAN_POINT ( 'NONE',  ( 6.539320575229268684, 7.629137130509104026, 2.396737603865983779 ) ) ;
#180894=CARTESIAN_POINT ( 'NONE',  ( 2.945584473374110779, 1.314022426170344815, 1.318171089286435560 ) ) ;
#180895=CARTESIAN_POINT ( 'NONE',  ( 0.1576404624921414199, 1.103540182269863612, 1.565583644703759436 ) ) ;
#180896=CARTESIAN_POINT ( 'NONE',  ( 6.370143239528382573, 0.9910226482379416169, 1.651782778771145432 ) ) ;
#180897=CARTESIAN_POINT ( 'NONE',  ( 6.162566008723842081, -0.7415158119226210598, -1.933206815039355320 ) ) ;
#180902=CARTESIAN_POINT ( 'NONE',  ( 4.399236341264299632, -1.715665262265529734, 0.9668539646570695201 ) ) ;
#180903=CARTESIAN_POINT ( 'NONE',  ( 1.823052125313681993, 1.569171740784220281, -1.426411057285102979 ) ) ;
#180908=CARTESIAN_POINT ( 'NONE',  ( 5.630878078874809844, -1.982435003639994031, 0.9343296635366815650 ) ) ;
#180910=CARTESIAN_POINT ( 'NONE',  ( 4.067344539004444037, 0.2368424065766552566, -1.911724265930745847 ) ) ;
#180912=CARTESIAN_POINT ( 'NONE',  ( 0.6744773098602949712, -1.717252091951677384, -0.6198786263262797691 ) ) ;
#180913=CARTESIAN_POINT ( 'NONE',  ( 1.014635385311330795, -0.9952708415592588231, -1.969785480804244537 ) ) ;
#180919=CARTESIAN_POINT ( 'NONE',  ( 6.192246204073627247, 0.9737480728593052026, -1.711826031884769339 ) ) ;
#180920=CARTESIAN_POINT ( 'NONE',  ( 1.645936167706591569, 0.6108386606893880799, 1.843543891229272313 ) ) ;
#180921=CARTESIAN_POINT ( 'NONE',  ( 6.327535152267887320, -1.632159162827769405, 1.618470562452605455 ) ) ;
#180923=CARTESIAN_POINT ( 'NONE',  ( 5.471493298581291853, -0.2749614684036653656, 1.840407035693031546 ) ) ;
#180928=CARTESIAN_POINT ( 'NONE',  ( 1.365048776756357940, 0.1565470504056795942, -2.186014887712848243 ) ) ;
#180931=CARTESIAN_POINT ( 'NONE',  ( 1.330379832379691818, 1.758967509726565792, 0.4888242021733391618 ) ) ;
#180936=CARTESIAN_POINT ( 'NONE',  ( 6.509000000000010999, 0.004788705324892603143, 2.000274819378269786 ) ) ;
#180937=CARTESIAN_POINT ( 'NONE',  ( 0.1331565106231328566, 1.371277436080810208, -2.201942895618694607 ) ) ;
#180939=CARTESIAN_POINT ( 'NONE',  ( 0.1879448220486016896, -0.9096115147686645308, 1.698232400582524670 ) ) ;
#180940=CARTESIAN_POINT ( 'NONE',  ( 4.117980938109369937, 1.947433809354440326, -0.2358448244534834815 ) ) ;
#180943=CARTESIAN_POINT ( 'NONE',  ( 4.934296419935967570, -1.134874685878878520, -1.791058398909770588 ) ) ;
#180944=CARTESIAN_POINT ( 'NONE',  ( 3.861010967126535576, 0.2669419790740577558, -2.175157288012785184 ) ) ;
#180946=CARTESIAN_POINT ( 'NONE',  ( 2.623957243734816647, 2.031168598393529034, -0.3995267358143372860 ) ) ;
#180950=CARTESIAN_POINT ( 'NONE',  ( 2.567332952821321790, -1.178922594190381146, 1.973231532614614148 ) ) ;
#180954=CARTESIAN_POINT ( 'NONE',  ( 6.620655732516623537, 7.629137130509068498, 2.426260288887295058 ) ) ;
#180957=CARTESIAN_POINT ( 'NONE',  ( 3.240110121693033474, 0.4724093276110411521, 1.883494029347228871 ) ) ;
#180961=CARTESIAN_POINT ( 'NONE',  ( 3.498220628606643956, -0.9384276995785534314, 1.666209768436441419 ) ) ;
#180962=CARTESIAN_POINT ( 'NONE',  ( 5.209832820053398983, -1.716139821054706749, 0.1720855783484842860 ) ) ;
#180963=CARTESIAN_POINT ( 'NONE',  ( 3.186732694495420848, 1.586669336078951664, -1.244385354607212335 ) ) ;
#180964=CARTESIAN_POINT ( 'NONE',  ( 5.643294731490863470, 0.9288382957042642385, 2.102849567203187053 ) ) ;
#180966=CARTESIAN_POINT ( 'NONE',  ( 0.7334016978863610037, 0.1661181961954381059, 2.200687262777756725 ) ) ;
#180968=CARTESIAN_POINT ( 'NONE',  ( 5.676936032674533728, -0.04454931526533602304, -1.769330457910125443 ) ) ;
#180970=CARTESIAN_POINT ( 'NONE',  ( 2.291363848578463980, 1.773334254936178356, 1.452501744581054632 ) ) ;
#180971=CARTESIAN_POINT ( 'NONE',  ( 0.9721243863554385189, -0.03892262269361351779, -1.740072766964487316 ) ) ;
#180974=CARTESIAN_POINT ( 'NONE',  ( 6.703104427915338448, -0.4847493572297522091, 2.145077170986497528 ) ) ;
#180978=CARTESIAN_POINT ( 'NONE',  ( 1.680376142759659075, -1.205403815041187210, -1.805639882349929781 ) ) ;
#180979=CARTESIAN_POINT ( 'NONE',  ( 2.870327622459168726, -1.987497926849005836, -0.3399570244180456502 ) ) ;
#180982=CARTESIAN_POINT ( 'NONE',  ( 5.356054764349521768, 1.924192155146129624, -0.09673933992536233595 ) ) ;
#180984=CARTESIAN_POINT ( 'NONE',  ( 2.250487404410873804, 1.042729518208513007, -1.961448655418545739 ) ) ;
#180990=CARTESIAN_POINT ( 'NONE',  ( 5.091228679354776965, -0.6197342532976670704, 1.626566373401008070 ) ) ;
#180991=CARTESIAN_POINT ( 'NONE',  ( 3.209375601822930690, -1.602329130913646926, -1.131729396966949963 ) ) ;
#180994=CARTESIAN_POINT ( 'NONE',  ( 4.886124051547468206, -1.072500323723464932, 1.992072436074944219 ) ) ;
#180997=CARTESIAN_POINT ( 'NONE',  ( 0.7837256325555241876, -1.959260395640700203, 0.6451903852672227213 ) ) ;
#181000=CARTESIAN_POINT ( 'NONE',  ( 1.921153072736818013, 2.111338651666348376, 0.8135812809707074766 ) ) ;
#181003=CARTESIAN_POINT ( 'NONE',  ( 2.249088872875557144, -1.499603784168266563, -1.117866018216478574 ) ) ;
#181004=CARTESIAN_POINT ( 'NONE',  ( 1.617354066682510805, 0.1696363612940926524, 1.725835137016252796 ) ) ;
#181005=CARTESIAN_POINT ( 'NONE',  ( 4.775033345069852331, 2.044829088842615494, -0.7888500489584143738 ) ) ;
#181006=CARTESIAN_POINT ( 'NONE',  ( 6.335062919620514599, 0.2175189359726207861, 2.297324976709664845 ) ) ;
#181007=CARTESIAN_POINT ( 'NONE',  ( 1.375931059888847896, 1.226954981729235561, 1.655701539656707411 ) ) ;
#181008=CARTESIAN_POINT ( 'NONE',  ( 4.083879184154452169, -1.920976184332440662, -0.2838548334032560683 ) ) ;
#181010=CARTESIAN_POINT ( 'NONE',  ( 6.591075523649926993, 1.627300515804396941, -0.9222108319836411772 ) ) ;
#181011=CARTESIAN_POINT ( 'NONE',  ( 1.406250000000001332, 1.895863743164055926, -0.7852924748300647018 ) ) ;
#181013=CARTESIAN_POINT ( 'NONE',  ( 6.362657644764971643, -0.6818896071447739793, 1.897407954007489295 ) ) ;
#181017=CARTESIAN_POINT ( 'NONE',  ( 5.871720251644387822, -0.2986239867289949834, -1.994071864161291119 ) ) ;
#181021=CARTESIAN_POINT ( 'NONE',  ( 1.998415063578623085, -0.4859047700337820741, -1.759764234465097221 ) ) ;
#181026=ORIENTED_EDGE ( 'NONE', *, *, #99713, .T. ) ;
#181031=CARTESIAN_POINT ( 'NONE',  ( 6.533853655515883041, -1.958494339806987394, 0.4928751659435038901 ) ) ;
#181032=CARTESIAN_POINT ( 'NONE',  ( 0.01256502854718108061, -2.120115106878577294, -0.04748564598491820943 ) ) ;
#181033=CIRCLE ( 'NONE', #87651, 0.04999999999999972522 ) ;
#181037=CARTESIAN_POINT ( 'NONE',  ( 6.139539385720709674, -1.490912338237950108, -1.423074965643542411 ) ) ;
#181038=CARTESIAN_POINT ( 'NONE',  ( 5.361953999179126740, -0.05229508359532940298, -2.015913028294749942 ) ) ;
#181046=CARTESIAN_POINT ( 'NONE',  ( 4.675157572021750418, -0.8594996001172333644, -1.823839583407538267 ) ) ;
#181047=CARTESIAN_POINT ( 'NONE',  ( 5.085823778388903982, -1.827637283562512538, -0.2220107604927607503 ) ) ;
#181049=CARTESIAN_POINT ( 'NONE',  ( 3.106426088690077858, -2.305020500623474522, 0.1135576804369240328 ) ) ;
#181051=CARTESIAN_POINT ( 'NONE',  ( 5.905597126736788383, -0.5315564325061740147, 2.095088507090197893 ) ) ;
#181053=CARTESIAN_POINT ( 'NONE',  ( 1.188897196845212445, 1.471763766255501427, 1.267211023470141695 ) ) ;
#181055=ORIENTED_EDGE ( 'NONE', *, *, #78162, .F. ) ;
#181056=CARTESIAN_POINT ( 'NONE',  ( 4.710533686004090725, -1.772996550310073971, -1.462542180504990075 ) ) ;
#181059=CARTESIAN_POINT ( 'NONE',  ( 3.028041890241763401, 1.040506211802554981, -1.554362669439563360 ) ) ;
#181060=CARTESIAN_POINT ( 'NONE',  ( 1.564566645345835116, 0.6029492335615972420, 1.814891859350221459 ) ) ;
#181063=CARTESIAN_POINT ( 'NONE',  ( 2.965657822035951963, 0.3232568108629539361, -2.182957019552448141 ) ) ;
#181069=CARTESIAN_POINT ( 'NONE',  ( 0.5968690581132638506, 1.641441770537595435, -1.091469919712923176 ) ) ;
#181070=CARTESIAN_POINT ( 'NONE',  ( 0.7808295286375503963, -1.278884537891399553, 1.920602667021213961 ) ) ;
#181071=CARTESIAN_POINT ( 'NONE',  ( 1.205434515183744226, -1.544416933936803904, -1.209700862059132964 ) ) ;
#181072=CARTESIAN_POINT ( 'NONE',  ( 5.664908073332702187, 1.565568307794177327, -1.342975779555633187 ) ) ;
#181079=CARTESIAN_POINT ( 'NONE',  ( 0.7257146478014552260, 0.2145687282662836204, -2.160472036209131197 ) ) ;
#181081=CARTESIAN_POINT ( 'NONE',  ( 5.882333747326812023, -0.2767177626767613474, -1.820229446528654371 ) ) ;
#181084=CARTESIAN_POINT ( 'NONE',  ( 1.440467042440606749, 0.3595057747620767907, 1.835501880432292010 ) ) ;
#181085=CARTESIAN_POINT ( 'NONE',  ( 5.641917277892137150, 0.8817427965214555963, -1.973778517010720490 ) ) ;
#181088=CARTESIAN_POINT ( 'NONE',  ( -0.02264175331117417728, 6.946776101658422853, -2.684156320254589279 ) ) ;
#181090=CARTESIAN_POINT ( 'NONE',  ( 1.295406243800485635, 1.766531960031037407, -0.7327172462580702206 ) ) ;
#181092=CARTESIAN_POINT ( 'NONE',  ( 3.449836819150660538, 1.770032027316788437, 0.0008499603425977939660 ) ) ;
#181093=CARTESIAN_POINT ( 'NONE',  ( 1.049298088506251947, -1.728493729547801117, 0.8183166869351958805 ) ) ;
#181095=CARTESIAN_POINT ( 'NONE',  ( 5.202711523826980766, 1.771732004023411911, 0.7288693050919017313 ) ) ;
#181097=CARTESIAN_POINT ( 'NONE',  ( 6.127403468923573904, 0.1463605449630276667, -1.964188589371117954 ) ) ;
#181099=CARTESIAN_POINT ( 'NONE',  ( 1.336355901170083849, -1.182550835430173919, -1.760063440837428272 ) ) ;
#181101=CARTESIAN_POINT ( 'NONE',  ( 6.610000000000008313, 7.629137130509070275, 2.600000000000001421 ) ) ;
#181102=CARTESIAN_POINT ( 'NONE',  ( 3.942156681999692491, 1.861596489644477437, 0.1839347620080991341 ) ) ;
#181103=CARTESIAN_POINT ( 'NONE',  ( 0.9612317138737861422, 0.3586375672061762887, -1.789940867121169843 ) ) ;
#181105=CARTESIAN_POINT ( 'NONE',  ( 4.442132104469964204, 0.9450947508268662256, -1.994404356956205326 ) ) ;
#181107=CARTESIAN_POINT ( 'NONE',  ( 2.102078608570765450, 0.7915390796853873923, -1.904948021121543711 ) ) ;
#181112=CARTESIAN_POINT ( 'NONE',  ( 0.1753634416057739953, 5.721028741045294908, -2.738064866945366660 ) ) ;
#181114=CARTESIAN_POINT ( 'NONE',  ( 4.000488093070094564, 2.060113009926473726, 0.2059288336104248551 ) ) ;
#181116=CARTESIAN_POINT ( 'NONE',  ( 1.704591423195594535, -0.7763021076895927353, -2.017573427605146907 ) ) ;
#181118=CARTESIAN_POINT ( 'NONE',  ( 2.526040989133854886, -1.997384215488164694, 0.2984307725432763236 ) ) ;
#181124=CARTESIAN_POINT ( 'NONE',  ( 0.05782782957228919940, 1.164991625563294386, 1.645756161228327130 ) ) ;
#181125=CARTESIAN_POINT ( 'NONE',  ( 4.423480980095358284, -1.348712413769267426, -1.727291790683552541 ) ) ;
#181127=CARTESIAN_POINT ( 'NONE',  ( 4.078302138561982204, 0.9061299177482335931, 1.684124486321957104 ) ) ;
#181131=CARTESIAN_POINT ( 'NONE',  ( 2.337517745082304810, 0.5350678814987767096, -1.944078148028173914 ) ) ;
#181134=CARTESIAN_POINT ( 'NONE',  ( 0.8730959291491724450, -0.06322356207747076295, -2.291674109354911781 ) ) ;
#181136=CARTESIAN_POINT ( 'NONE',  ( 3.856244308521704411, 0.6209911617112495730, 1.609288963722750765 ) ) ;
#181139=CARTESIAN_POINT ( 'NONE',  ( 0.07755575628183573877, -0.002876890934064984216, -2.188974970840869005 ) ) ;
#181140=CARTESIAN_POINT ( 'NONE',  ( 0.09234973940512071489, -0.4041859633337717694, -1.833079292876439670 ) ) ;
#181142=CARTESIAN_POINT ( 'NONE',  ( 0.1753634416057739953, 5.721028741045294908, -2.738064866945366660 ) ) ;
#181146=CARTESIAN_POINT ( 'NONE',  ( 4.846265894328573687, 0.9266178045349574566, -1.556377301703376625 ) ) ;
#181150=CARTESIAN_POINT ( 'NONE',  ( 5.584552742667589165, -1.144318741887658586, 1.404276898221923364 ) ) ;
#181153=CARTESIAN_POINT ( 'NONE',  ( 2.502122453320880346, -0.8398649383675671487, -2.024319193490734303 ) ) ;
#181154=CARTESIAN_POINT ( 'NONE',  ( 6.584420904419787668, 1.070383488754884649, -1.522209605261907406 ) ) ;
#181156=CARTESIAN_POINT ( 'NONE',  ( 4.007376490896687571, -1.831982314510060883, 0.5597367571646000295 ) ) ;
#181163=CARTESIAN_POINT ( 'NONE',  ( 5.384029865600029829, -2.117513407852515073, 0.002815966404249789501 ) ) ;
#181164=CARTESIAN_POINT ( 'NONE',  ( 0.8839147992780392871, 1.452536163361785260, 1.601146772000871188 ) ) ;
#181167=CARTESIAN_POINT ( 'NONE',  ( 0.9205982885796895054, 1.684962172289593996, 0.7030880920091547859 ) ) ;
#181169=CARTESIAN_POINT ( 'NONE',  ( 3.346530664597209714, 0.4423686283943834563, 1.771051422834311051 ) ) ;
#181173=CARTESIAN_POINT ( 'NONE',  ( 2.629305401816001808, 0.09940027615944720119, -1.967183499748959452 ) ) ;
#181175=CARTESIAN_POINT ( 'NONE',  ( 5.003436869212060323, -1.932333990966347503, 0.1943045992871711702 ) ) ;
#181178=CARTESIAN_POINT ( 'NONE',  ( 5.818629517237746462, -0.7649446623404360102, -1.977987144599784086 ) ) ;
#181180=CARTESIAN_POINT ( 'NONE',  ( 3.070860992347378637, -1.446505282863861375, 1.250851760459831041 ) ) ;
#181184=CARTESIAN_POINT ( 'NONE',  ( 3.949861574111676266, -1.389792608731334811, -1.456582260380126392 ) ) ;
#181186=CARTESIAN_POINT ( 'NONE',  ( 5.127504350819418910, -1.732488751877172772, 0.5760870007271366999 ) ) ;
#181187=CARTESIAN_POINT ( 'NONE',  ( 0.9419464005683106933, 1.389173191389100115, 1.535309223701806225 ) ) ;
#181191=CARTESIAN_POINT ( 'NONE',  ( 5.453920962983416665, 1.868457504587007545, -0.09292587778651077712 ) ) ;
#181198=CARTESIAN_POINT ( 'NONE',  ( 0.7431355771655088205, -0.2497938498803170537, -2.055034051290441255 ) ) ;
#181199=CARTESIAN_POINT ( 'NONE',  ( 2.636446987817195886, 0.7160595562910974099, 1.992577970932450704 ) ) ;
#181202=CARTESIAN_POINT ( 'NONE',  ( 5.963751281166302043, -0.5086355806236466659, 2.006660534352236347 ) ) ;
#181207=CARTESIAN_POINT ( 'NONE',  ( 3.064699953192471682, -2.118106589925540906, -0.8768602481810504612 ) ) ;
#181209=CARTESIAN_POINT ( 'NONE',  ( 0.2333690889706925009, 5.722554199285137422, -2.647406232470352894 ) ) ;
#181211=CARTESIAN_POINT ( 'NONE',  ( 2.795058504854182946, -0.1448928079688660830, -1.906987441340234568 ) ) ;
#181215=CARTESIAN_POINT ( 'NONE',  ( 0.8615886222705991804, -1.589730513765170938, -1.235154978249096036 ) ) ;
#181216=CARTESIAN_POINT ( 'NONE',  ( 1.147228161472005681, 1.732707765124143817, -0.9198407203683529598 ) ) ;
#181220=CARTESIAN_POINT ( 'NONE',  ( 4.031257853796605062, -1.441737515256842572, -1.514218249133948868 ) ) ;
#181221=CARTESIAN_POINT ( 'NONE',  ( 2.271989177565427287, -1.091335633969382490, 1.393213513506918133 ) ) ;
#181224=CARTESIAN_POINT ( 'NONE',  ( 5.507889418014947580, -1.026508118683837401, -2.049657838918368391 ) ) ;
#181225=CARTESIAN_POINT ( 'NONE',  ( 4.066134141799277124, -1.624876214689898957, -0.6237973674530649104 ) ) ;
#181228=CARTESIAN_POINT ( 'NONE',  ( 4.006995869149078793, 1.725434352394356052, 0.1705419362300845121 ) ) ;
#181229=CARTESIAN_POINT ( 'NONE',  ( 4.475155579853315579, 1.983319414854123552, 0.8838481202026007288 ) ) ;
#181231=CARTESIAN_POINT ( 'NONE',  ( 5.208220363674559650, 1.197307938467083055, -1.622483861274232719 ) ) ;
#181232=CARTESIAN_POINT ( 'NONE',  ( 0.8750000000000005551, 2.052068128417951609, -5.168192407616667353E-14 ) ) ;
#181234=CARTESIAN_POINT ( 'NONE',  ( 2.678635733147361808, -1.842946530311468045, -0.5607992601908852182 ) ) ;
#181236=CARTESIAN_POINT ( 'NONE',  ( 6.187741696929490054, 2.126074299989196614, -0.6436727651782292448 ) ) ;
#181237=ORIENTED_EDGE ( 'NONE', *, *, #126637, .T. ) ;
#181238=CARTESIAN_POINT ( 'NONE',  ( 6.983263157960404754, -0.005959781318053481922, 2.045923054782183392 ) ) ;
#181241=CARTESIAN_POINT ( 'NONE',  ( 1.788022372910631486, 2.124507586210178989, -0.6485351029156469771 ) ) ;
#181242=CARTESIAN_POINT ( 'NONE',  ( 6.531700620877029628, 1.877769495358465157, -0.5682946464737672621 ) ) ;
#181250=CARTESIAN_POINT ( 'NONE',  ( 4.439923992641017669, 1.344862922493793578, 1.564070066283109295 ) ) ;
#181254=CARTESIAN_POINT ( 'NONE',  ( 5.641831084104285132, 0.7588036158820666843, -1.709917670604633066 ) ) ;
#181255=CARTESIAN_POINT ( 'NONE',  ( 4.799290796133064418, 1.190976682166387413, -1.260762715536057899 ) ) ;
#181256=CARTESIAN_POINT ( 'NONE',  ( 4.089206054525551970, -0.6613740077951230090, 1.610090703890323605 ) ) ;
#181258=CARTESIAN_POINT ( 'NONE',  ( 2.103457651957148844, -0.4980181218575702173, 2.237485198869753944 ) ) ;
#181260=CARTESIAN_POINT ( 'NONE',  ( 6.005435553056907239, -2.074886976054179488, 0.2565860541952763585 ) ) ;
#181261=CARTESIAN_POINT ( 'NONE',  ( 0.7086343398283838635, -0.2726298849291541870, 1.820711063333625646 ) ) ;
#181264=CARTESIAN_POINT ( 'NONE',  ( 2.479138880926802901, -2.011204309026824344, -0.1455328587063598189 ) ) ;
#181265=CARTESIAN_POINT ( 'NONE',  ( 1.236564921189796440, 0.4304113295856800692, 2.148598399174222351 ) ) ;
#181268=CARTESIAN_POINT ( 'NONE',  ( 1.451716722110554025, 1.566445173006292935, 1.353826630019476562 ) ) ;
#181271=CARTESIAN_POINT ( 'NONE',  ( 3.088655771522513582, -1.261447869382603004, 1.704333039148818507 ) ) ;
#181273=CARTESIAN_POINT ( 'NONE',  ( 0.3637320452541660254, 1.905723972499345997, -0.2814332051396683521 ) ) ;
#181280=CARTESIAN_POINT ( 'NONE',  ( 3.638929714444568919, 1.919204589499112323, 0.6297368113697666692 ) ) ;
#181281=CARTESIAN_POINT ( 'NONE',  ( 6.563508857876433567, 0.3837567690821128696, -2.173003994120882076 ) ) ;
#181284=CARTESIAN_POINT ( 'NONE',  ( 5.137489257405690957, 1.737274493258118113, -0.6675986409061424043 ) ) ;
#181289=CARTESIAN_POINT ( 'NONE',  ( 6.702032673877901914, -2.060500267551836018, 0.04777910199381221051 ) ) ;
#181294=CARTESIAN_POINT ( 'NONE',  ( 1.299655142190193402, -1.570548766235444038, 0.7348691985549455907 ) ) ;
#181295=CARTESIAN_POINT ( 'NONE',  ( 0.8842106040080777163, 1.536738824236941747, -0.8168212061390681678 ) ) ;
#181296=CARTESIAN_POINT ( 'NONE',  ( 6.217413992247779575, -0.2892589651934658890, 2.289433544902704565 ) ) ;
#181299=CARTESIAN_POINT ( 'NONE',  ( 2.899741356312244722, -0.6498117751948685461, 1.955694574617524495 ) ) ;
#181301=CARTESIAN_POINT ( 'NONE',  ( 1.071638489536786309, 1.528508772698907059, -1.314793605459969372 ) ) ;
#181305=CARTESIAN_POINT ( 'NONE',  ( 6.772336237553374438, -1.148929780121176414, 1.476827877338216854 ) ) ;
#181307=CARTESIAN_POINT ( 'NONE',  ( 5.133030909251353968, 1.769313487831367659, 0.7262901588861517821 ) ) ;
#181309=CARTESIAN_POINT ( 'NONE',  ( 5.672569038193632451, -1.402732290180560337, 1.703733612381942653 ) ) ;
#181313=CARTESIAN_POINT ( 'NONE',  ( 6.586587867412674768, -1.305319418013479948, 1.671791285998667442 ) ) ;
#181315=CARTESIAN_POINT ( 'NONE',  ( 4.436755630409714435, 2.262211819008316027, 0.4546042144240244887 ) ) ;
#181316=CARTESIAN_POINT ( 'NONE',  ( 4.527759979645433752, 1.903474890065796732, -0.4746247275292309609 ) ) ;
#181318=CARTESIAN_POINT ( 'NONE',  ( 2.184356868638567928, 1.133688150830698627, -1.600809071968431807 ) ) ;
#181322=CARTESIAN_POINT ( 'NONE',  ( 6.503150282362620160, -0.1410805869419759218, 1.984311032119711715 ) ) ;
#181325=CARTESIAN_POINT ( 'NONE',  ( 0.7437973067255730930, 0.5320827018340993364, 1.762565881533173950 ) ) ;
#181327=CARTESIAN_POINT ( 'NONE',  ( 4.803694799390169301, -1.674174935400191799, -1.382237342716886586 ) ) ;
#181329=CARTESIAN_POINT ( 'NONE',  ( 1.740644586495963431, 1.216819214799185866, -1.736574482785017359 ) ) ;
#181334=CARTESIAN_POINT ( 'NONE',  ( 1.563821040897996895, 2.030780823367520416, -0.3493207144565529942 ) ) ;
#181336=CARTESIAN_POINT ( 'NONE',  ( 6.609000000000009756, 0.005669918681722525139, 1.900160851458797318 ) ) ;
#181338=CARTESIAN_POINT ( 'NONE',  ( 0.07735805125223899070, 0.2300150639059690694, -2.122327182112139443 ) ) ;
#181340=CARTESIAN_POINT ( 'NONE',  ( 6.182274467271689389, 0.9872068455926674702, 1.637624497839342830 ) ) ;
#181342=CARTESIAN_POINT ( 'NONE',  ( 1.792605694782311243, -2.251445656634944559, -0.2226877779667023882 ) ) ;
#181344=CARTESIAN_POINT ( 'NONE',  ( 1.089788312850032526, 1.080336570596603929, 1.454002670061284919 ) ) ;
#181345=CARTESIAN_POINT ( 'NONE',  ( 1.903404652330241476, -1.857121539659777998, 0.4695605108672970540 ) ) ;
#181346=CARTESIAN_POINT ( 'NONE',  ( 3.385274849524767316, 0.04804411014160993310, 2.069964801482151895 ) ) ;
#181349=CARTESIAN_POINT ( 'NONE',  ( 1.076956826339631856, -0.04624765943369788662, -1.971079714834519159 ) ) ;
#181350=CARTESIAN_POINT ( 'NONE',  ( 5.092375307706883625, -1.912163826771107855, -0.2340926620403842862 ) ) ;
#181351=CARTESIAN_POINT ( 'NONE',  ( 1.032322977361863847, -1.467698275133515695, -1.780829215104979157 ) ) ;
#181354=CARTESIAN_POINT ( 'NONE',  ( 5.547355216851989290, 1.820699215414087302, -0.9693467284541881224 ) ) ;
#181360=CARTESIAN_POINT ( 'NONE',  ( 6.440466061264603859, 2.082495663875443714, 0.3126870252899079938 ) ) ;
#181363=CARTESIAN_POINT ( 'NONE',  ( 4.464260128311710041, 1.014592192358022338, 1.908665273222116321 ) ) ;
#181364=CARTESIAN_POINT ( 'NONE',  ( 5.285809349500922849, 1.945818207184028426, -0.5408622128197750900 ) ) ;
#181373=CARTESIAN_POINT ( 'NONE',  ( 3.608611488583326032, 1.916353073142588403, 0.6279913346786819561 ) ) ;
#181378=CARTESIAN_POINT ( 'NONE',  ( 4.575171270262055501, 0.003154952768896768234, -2.161883445794945846 ) ) ;
#181383=CARTESIAN_POINT ( 'NONE',  ( 5.993767587909683670, -2.000856116866961187, 0.2496242821527286382 ) ) ;
#181385=CARTESIAN_POINT ( 'NONE',  ( 0.3281590906380106865, 1.648959081962350304, 0.5061492587876709193 ) ) ;
#181390=CARTESIAN_POINT ( 'NONE',  ( 6.397708313642382905, -0.6301307688901837123, 1.761319926792910495 ) ) ;
#181391=CARTESIAN_POINT ( 'NONE',  ( 0.6451818603588607148, 0.1503996631540445994, 2.007543313942860674 ) ) ;
#181392=CARTESIAN_POINT ( 'NONE',  ( 6.539320575229279342, 7.629137130509070275, 2.496737603865983868 ) ) ;
#181393=CARTESIAN_POINT ( 'NONE',  ( 3.153566124713353513, -1.803153744294363481, -1.271922660818012973 ) ) ;
#181397=CARTESIAN_POINT ( 'NONE',  ( 2.192179715818479036, 1.306768369893403170, 1.669877806752372740 ) ) ;
#181398=CARTESIAN_POINT ( 'NONE',  ( 1.493767781312784981, -2.000855510370867840, 0.2496291452861176263 ) ) ;
#181399=CARTESIAN_POINT ( 'NONE',  ( 2.302729407678519191, -0.3129977310964130455, -1.784170229015415332 ) ) ;
#181404=CARTESIAN_POINT ( 'NONE',  ( 0.4267777427376097665, -1.641576225293687630, 0.9873106011929821957 ) ) ;
#181410=CARTESIAN_POINT ( 'NONE',  ( 3.942369626403975147, 2.151062187213080623, 0.2142938780915065733 ) ) ;
#181413=CARTESIAN_POINT ( 'NONE',  ( 2.478903650112133317, -1.459102030866548994, 1.539066919819010781 ) ) ;
#181415=CARTESIAN_POINT ( 'NONE',  ( 3.637922374042131590, 0.8895205046622333134, -1.759358583061757519 ) ) ;
#181417=CARTESIAN_POINT ( 'NONE',  ( 5.635196759804959044, -0.04649108105550652653, -1.969165932527061402 ) ) ;
#181418=CARTESIAN_POINT ( 'NONE',  ( 1.710778446297245958, -0.2380136870633246249, 1.927241887951787858 ) ) ;
#181423=CARTESIAN_POINT ( 'NONE',  ( 2.871125768194443761, 1.984923283205226818, -0.6565763796619171755 ) ) ;
#181427=CARTESIAN_POINT ( 'NONE',  ( 6.164708882046985750, 0.6044385376218417427, 1.814302210532907411 ) ) ;
#181428=ORIENTED_EDGE ( 'NONE', *, *, #182631, .F. ) ;
#181429=CARTESIAN_POINT ( 'NONE',  ( 4.125739685719872263, -2.112183141943014153, 0.6395159525410462065 ) ) ;
#181430=CARTESIAN_POINT ( 'NONE',  ( 1.817678338065799926, -0.2697497798337232244, 2.190168480848574628 ) ) ;
#181432=CARTESIAN_POINT ( 'NONE',  ( 1.172351427048579531, 0.7757545017167380985, 1.748050575570128329 ) ) ;
#181434=DIRECTION ( 'NONE',  ( 2.949029909160572061E-17, 1.000000000000000000, -8.673600428462429131E-15 ) ) ;
#181436=CARTESIAN_POINT ( 'NONE',  ( 3.930184216435282707, 1.147649575447948100, 1.722966636330313328 ) ) ;
#181439=CARTESIAN_POINT ( 'NONE',  ( 2.131903390035182255, -1.411712784473453830, -1.637176306262012826 ) ) ;
#181440=CARTESIAN_POINT ( 'NONE',  ( 3.825867475279482566, 1.171244075711602051, -1.852137614134836907 ) ) ;
#181447=CARTESIAN_POINT ( 'NONE',  ( 5.871638708485903635, -0.2633594344273459398, -1.713904792762838136 ) ) ;
#181449=CARTESIAN_POINT ( 'NONE',  ( 4.856339096887199780, -2.069677458173447171, -0.05615216265978521804 ) ) ;
#181450=CARTESIAN_POINT ( 'NONE',  ( 5.677400705446850715, 1.603760038662904286, 1.382376383168891998 ) ) ;
#181454=CARTESIAN_POINT ( 'NONE',  ( 4.047672669870348905, 1.423397643995693684, 1.361350234347382226 ) ) ;
#181455=CARTESIAN_POINT ( 'NONE',  ( 5.595737365542901465, -2.292435212557204949, -0.004933362929348399616 ) ) ;
#181456=CARTESIAN_POINT ( 'NONE',  ( 3.334410585898534674, 1.781380905032422746, 0.3990451814587444024 ) ) ;
#181463=CARTESIAN_POINT ( 'NONE',  ( 3.691655806294301900, 1.894216563707728396, -0.6821535943304660732 ) ) ;
#181465=CARTESIAN_POINT ( 'NONE',  ( 4.803538753074391821, -1.513872852549098091, -1.247617340562396926 ) ) ;
#181469=CARTESIAN_POINT ( 'NONE',  ( 0.1872078708128835645, 1.551958633911882934, 1.401156373025253421 ) ) ;
#181470=CARTESIAN_POINT ( 'NONE',  ( 5.594547536969180612, -0.4332151766474266474, -1.715878325482506517 ) ) ;
#181472=CARTESIAN_POINT ( 'NONE',  ( 1.465048628566959055, 0.1585425061045864503, -2.185770122351132994 ) ) ;
#181473=CARTESIAN_POINT ( 'NONE',  ( 1.047962540061377679, -1.372746097444921043, 1.069743175550162295 ) ) ;
#181475=CARTESIAN_POINT ( 'NONE',  ( 0.1335669894368292088, 2.005130876877735613, -2.568368839946821414 ) ) ;
#181476=CARTESIAN_POINT ( 'NONE',  ( 1.207153632009206223, -0.4226329412084055548, 1.672169654609439116 ) ) ;
#181477=CARTESIAN_POINT ( 'NONE',  ( 2.085717061910817183, -0.9337068281064246911, 1.982830571388309204 ) ) ;
#181478=CARTESIAN_POINT ( 'NONE',  ( 3.334799921508072806, 2.153101868192684343, 0.4835390122766567433 ) ) ;
#181479=CARTESIAN_POINT ( 'NONE',  ( 1.622189073652591240, 2.139406107190901185, -0.3685050674664645531 ) ) ;
#181480=CARTESIAN_POINT ( 'NONE',  ( 0.1174333910212103232, -1.791171220025630895, 0.3524246893974944395 ) ) ;
#181481=CARTESIAN_POINT ( 'NONE',  ( 1.956417434996825522, -1.298217783395636316, 1.672616391537498526 ) ) ;
#181484=CARTESIAN_POINT ( 'NONE',  ( 6.036148348713140876, 0.9492135318787934262, -1.676240969703364891 ) ) ;
#181485=ORIENTED_EDGE ( 'NONE', *, *, #102016, .T. ) ;
#181486=CARTESIAN_POINT ( 'NONE',  ( 2.841680536636710386, 0.8224841172943345713, -2.139919992735066945 ) ) ;
#181490=CARTESIAN_POINT ( 'NONE',  ( 5.268325480127796112, 2.218825861875061811, -0.1076023827350883894 ) ) ;
#181498=CARTESIAN_POINT ( 'NONE',  ( 2.830704105008190030, 0.7231396562890278767, -1.882474209725725434 ) ) ;
#181500=CARTESIAN_POINT ( 'NONE',  ( 0.9540547974491294658, -0.7459001080754708024, 1.923128640884926410 ) ) ;
#181504=CARTESIAN_POINT ( 'NONE',  ( 3.943468035136340255, 0.7389761752502190806, -2.063229655756371628 ) ) ;
#181505=CARTESIAN_POINT ( 'NONE',  ( 1.143204175302305670, 0.8197749522141674072, 1.842446510343001442 ) ) ;
#181506=CARTESIAN_POINT ( 'NONE',  ( 0.6086344939593493208, -0.2706599535906920040, 1.821105742621460744 ) ) ;
#181510=CARTESIAN_POINT ( 'NONE',  ( 5.157177646623883227, -1.542991646335686973, -0.9753701268572569916 ) ) ;
#181511=CARTESIAN_POINT ( 'NONE',  ( 5.625625018759272677, 0.3960990390993284205, 1.976956468877195894 ) ) ;
#181513=CARTESIAN_POINT ( 'NONE',  ( 4.715850076732730045, -2.219782111298532978, 0.4368881197941154038 ) ) ;
#181515=CARTESIAN_POINT ( 'NONE',  ( 0.6101635361662772761, -2.095732242510168764, 0.2083838208960953620 ) ) ;
#181517=CARTESIAN_POINT ( 'NONE',  ( 4.844224204019831781, -0.9789346907586125024, 1.824324395707350943 ) ) ;
#181527=CARTESIAN_POINT ( 'NONE',  ( 0.2289750728588327566, 1.457791096766167360, -1.540313549178488284 ) ) ;
#181528=CARTESIAN_POINT ( 'NONE',  ( 1.828696429707490578, -1.052382519090878654, -1.956348917980913260 ) ) ;
#181532=CARTESIAN_POINT ( 'NONE',  ( 3.226955236329264398, -1.811681696138227160, -0.7532884077038404236 ) ) ;
#181538=CARTESIAN_POINT ( 'NONE',  ( 2.865608904542978674, -1.736054085904148669, -1.217558864107195715 ) ) ;
#181540=CARTESIAN_POINT ( 'NONE',  ( 3.982823771651412770, 1.862158852298421152, 0.6176278068941787325 ) ) ;
#181541=CARTESIAN_POINT ( 'NONE',  ( 3.432649856329002880, 2.108609624295390006, 0.4754391814798044069 ) ) ;
#181543=CARTESIAN_POINT ( 'NONE',  ( 3.263068207883256466, 1.795673413606920565, -0.4063787724192802209 ) ) ;
#181546=CARTESIAN_POINT ( 'NONE',  ( 5.085792842222247145, -1.727793525551263087, -0.2079256833047369302 ) ) ;
#181550=CARTESIAN_POINT ( 'NONE',  ( 2.096749907087645415, -0.5762017740289016032, -2.083436276955972222 ) ) ;
#181552=CARTESIAN_POINT ( 'NONE',  ( 4.288435361214689046, -1.930121902525683053, 0.5825675424541224556 ) ) ;
#181554=CARTESIAN_POINT ( 'NONE',  ( 1.411231610350563992, 1.906656261001705488, 1.018656936289302539 ) ) ;
#181555=CARTESIAN_POINT ( 'NONE',  ( 2.583225839741074115, 1.803852637447726392, -0.7955871043755156080 ) ) ;
#181556=CARTESIAN_POINT ( 'NONE',  ( 6.509000000000037645, 2.054060622569788386, 2.307050226316338382 ) ) ;
#181557=CARTESIAN_POINT ( 'NONE',  ( 3.597155123818120082, -0.5607282099057244729, 1.859368625674643782 ) ) ;
#181565=CARTESIAN_POINT ( 'NONE',  ( 1.554063478550568256, 0.6399170599369340406, -2.111937735441645980 ) ) ;
#181567=CARTESIAN_POINT ( 'NONE',  ( 5.137533780887935997, 1.831872034461759835, -0.7024582609849658876 ) ) ;
#181569=CARTESIAN_POINT ( 'NONE',  ( 3.432911303685074689, -1.728510519573158266, 1.222591858268074150 ) ) ;
#181571=CARTESIAN_POINT ( 'NONE',  ( 0.1747926744264660381, 7.629137130509078268, -2.455305974604498953 ) ) ;
#181572=CARTESIAN_POINT ( 'NONE',  ( 4.365079047384805122, 1.785254547683400306, -0.4496667978745386152 ) ) ;
#181576=CARTESIAN_POINT ( 'NONE',  ( 5.097945154717048233, 1.425953928781589886, 1.569717048080176314 ) ) ;
#181577=CARTESIAN_POINT ( 'NONE',  ( -0.1106727585415930720, -0.002281114264979212502, -2.003378291782103027 ) ) ;
#181579=CARTESIAN_POINT ( 'NONE',  ( 5.061820804786828276, 2.038956591669589535, -0.2981446164109917696 ) ) ;
#181581=CARTESIAN_POINT ( 'NONE',  ( 0.9239872072115723478, 0.9125040393608827571, 1.621899335316509649 ) ) ;
#181582=CARTESIAN_POINT ( 'NONE',  ( 2.665370095338463585, 0.9869154847663293983, 1.554228294351194473 ) ) ;
#181588=CARTESIAN_POINT ( 'NONE',  ( 2.912931060594741162, 1.598032330669514778, -1.522282275181946032 ) ) ;
#181589=CARTESIAN_POINT ( 'NONE',  ( 5.061948053633171796, 2.238818834584723749, -0.3250485201948364877 ) ) ;
#181591=CARTESIAN_POINT ( 'NONE',  ( 5.256058454422637638, 0.7267480909730811289, -1.659609831382781397 ) ) ;
#181592=CARTESIAN_POINT ( 'NONE',  ( 5.348823992091742419, -1.734843432642660721, -0.8128511771108116735 ) ) ;
#181595=CARTESIAN_POINT ( 'NONE',  ( 5.559403950928493821, 0.3636877230743483236, -1.834782481876767291 ) ) ;
#181596=CARTESIAN_POINT ( 'NONE',  ( 5.969184020103408095, 1.641702931788184383, 0.8765767931452476125 ) ) ;
#181599=CARTESIAN_POINT ( 'NONE',  ( 6.315310819269446263, -0.2119676446582714757, 1.757049200028695690 ) ) ;
#181600=CARTESIAN_POINT ( 'NONE',  ( 0.3215004009857677092, -1.429452135790244549, -1.422604240635255479 ) ) ;
#181602=CARTESIAN_POINT ( 'NONE',  ( 3.317110013156245873, 1.904127318671836600, 0.9001942471269042123 ) ) ;
#181607=CARTESIAN_POINT ( 'NONE',  ( 1.705338084499245843, 1.755316507598453368, -0.9991084507309263563 ) ) ;
#181610=CARTESIAN_POINT ( 'NONE',  ( 3.163507678178357541, 0.3205598832158839673, -2.137589075770351066 ) ) ;
#181611=CARTESIAN_POINT ( 'NONE',  ( 6.620655732516652847, 2.468432086671234149, 2.210906647470804565 ) ) ;
#181618=CARTESIAN_POINT ( 'NONE',  ( 0.8904706703079521279, -0.5376514911656914419, -2.124458794526106864 ) ) ;
#181620=CARTESIAN_POINT ( 'NONE',  ( 1.727766546026089145, -2.130035881452702728, 0.7632205929882311946 ) ) ;
#181627=CARTESIAN_POINT ( 'NONE',  ( 3.127930002535435516, 0.9861435696450934207, -1.469289397387682161 ) ) ;
#181628=CARTESIAN_POINT ( 'NONE',  ( 6.036183878773405453, 1.092744051193066834, -1.917163762461614240 ) ) ;
#181633=CARTESIAN_POINT ( 'NONE',  ( 5.536732523015378327, -1.587826920732600122, 1.242742243127918700 ) ) ;
#181634=CARTESIAN_POINT ( 'NONE',  ( 4.922017755325088118, -1.802143800875387614, 0.1849416998233286979 ) ) ;
#181636=CARTESIAN_POINT ( 'NONE',  ( 2.236979667955760309, -1.672073921526989748, 0.8388852543278202401 ) ) ;
#181637=CARTESIAN_POINT ( 'NONE',  ( 2.747004861044194612, -0.3495022371792326221, -2.040372298647576965 ) ) ;
#181639=CARTESIAN_POINT ( 'NONE',  ( 1.793074957647671663, -0.09724762972821224261, -1.910064080951429100 ) ) ;
#181645=CARTESIAN_POINT ( 'NONE',  ( 1.353610510645312237, -1.387278792934818705, -1.316581319992945920 ) ) ;
#181648=CARTESIAN_POINT ( 'NONE',  ( 3.051168888765115828, 1.684027830550902882, -1.006202029777767848 ) ) ;
#181649=CARTESIAN_POINT ( 'NONE',  ( 0.2982036909132765867, -1.844429998007334648, 0.8144978490535054183 ) ) ;
#181653=CARTESIAN_POINT ( 'NONE',  ( 6.749300054864300513, -1.582014061365591751, -1.175997427595596445 ) ) ;
#181655=CARTESIAN_POINT ( 'NONE',  ( 2.250246052928657203, 0.9454230575737303521, -1.777374461261713279 ) ) ;
#181657=CARTESIAN_POINT ( 'NONE',  ( 1.353279953590967644, 0.1518699462816820722, -2.111824974118434728 ) ) ;
#181659=CARTESIAN_POINT ( 'NONE',  ( 3.209495720308676248, -1.691010085789945716, -1.194244797349801157 ) ) ;
#181661=CARTESIAN_POINT ( 'NONE',  ( 5.894497796308646009, 1.709714471583067885, -1.202884697265863778 ) ) ;
#181663=CARTESIAN_POINT ( 'NONE',  ( 4.102439050647597618, -0.5725816820084869141, -1.733541218493547476 ) ) ;
#181668=CARTESIAN_POINT ( 'NONE',  ( 5.051906976816819217, 0.6964463896041681590, -2.094057263239030853 ) ) ;
#181671=CARTESIAN_POINT ( 'NONE',  ( 4.020093958671668410, -1.906945023982812515, 0.1437811316862200317 ) ) ;
#181676=CARTESIAN_POINT ( 'NONE',  ( 6.589320575229280053, 7.629137130509070275, 2.496737603865983868 ) ) ;
#181678=CARTESIAN_POINT ( 'NONE',  ( 0.04610459085982109018, -1.479553692838073475, 1.095721268101347734 ) ) ;
#181681=CARTESIAN_POINT ( 'NONE',  ( 5.061713478001653499, 1.850364105758989020, -0.2730526881008291662 ) ) ;
#181687=CARTESIAN_POINT ( 'NONE',  ( 1.147236149642312242, 1.739494102415694243, -0.9234435978164361458 ) ) ;
#181688=CARTESIAN_POINT ( 'NONE',  ( 1.950796209937825321, -1.844718841590715863, -0.8146091914792084054 ) ) ;
#181692=CARTESIAN_POINT ( 'NONE',  ( 2.607599380506659514, -2.167453834138896696, 0.3226137089109848421 ) ) ;
#181693=CARTESIAN_POINT ( 'NONE',  ( 6.182242880246401562, -0.9723386526096773341, 1.545037271442825100 ) ) ;
#181701=CARTESIAN_POINT ( 'NONE',  ( 4.845164456061270997, 0.5726227986864868003, -1.750029900461601340 ) ) ;
#181702=CARTESIAN_POINT ( 'NONE',  ( 0.3990879006048999589, -0.2487020831964822098, -1.997621932491387531 ) ) ;
#181703=CARTESIAN_POINT ( 'NONE',  ( 2.988014862494779322, 2.163403104293510459, 0.7763308700806015317 ) ) ;
#181705=CARTESIAN_POINT ( 'NONE',  ( 1.199803204733034923, 0.7606819372595281514, -1.698589668608577963 ) ) ;
#181709=CARTESIAN_POINT ( 'NONE',  ( 4.377155534175989793, -1.710687068321177007, -0.8549628122409487219 ) ) ;
#181713=CARTESIAN_POINT ( 'NONE',  ( 3.316043925569078787, 1.324660045548868181, -1.617576387421674866 ) ) ;
#181714=CARTESIAN_POINT ( 'NONE',  ( 2.658895327995167701, -1.626580691111865207, -0.9237732865615968514 ) ) ;
#181717=CARTESIAN_POINT ( 'NONE',  ( 6.005383971424570255, -1.826508537601937432, 0.2321369796495567073 ) ) ;
#181720=CARTESIAN_POINT ( 'NONE',  ( 4.529763579968347997, -1.064299448457445729, -1.357287084437068803 ) ) ;
#181722=CARTESIAN_POINT ( 'NONE',  ( 0.3165338080420940781, 0.8936020571472038654, -1.485981903106075031 ) ) ;
#181725=CARTESIAN_POINT ( 'NONE',  ( 4.733362013637422372, 0.006437197247223526778, -2.171239809022653677 ) ) ;
#181726=CARTESIAN_POINT ( 'NONE',  ( 3.193790821891542731, -0.7392406677243367197, 1.669511829839696260 ) ) ;
#181727=CARTESIAN_POINT ( 'NONE',  ( 1.428482823135175606, -1.248714028858177061, 1.512975372890807524 ) ) ;
#181728=CARTESIAN_POINT ( 'NONE',  ( 5.876184115051023227, -2.107333617329323783, -0.2052446207758129582 ) ) ;
#181729=CARTESIAN_POINT ( 'NONE',  ( 5.987847201643853978, -2.280908734910926938, -0.2287418647285797413 ) ) ;
#181732=CARTESIAN_POINT ( 'NONE',  ( 1.207859650372544280, 1.608047128250057689, 1.382383069919224106 ) ) ;
#181737=CARTESIAN_POINT ( 'NONE',  ( 6.332918745153389928, -2.058942774313234025, -0.6888473222384088324 ) ) ;
#181738=CARTESIAN_POINT ( 'NONE',  ( 6.883263157960364254, 2.431740398616466070, 2.435552827938294751 ) ) ;
#181741=CARTESIAN_POINT ( 'NONE',  ( 2.491161192834326688, -2.126536535197431022, -0.6419364700022185399 ) ) ;
#181743=CARTESIAN_POINT ( 'NONE',  ( -0.01642261062154842799, -2.298356651571492826, -0.04744217504730821600 ) ) ;
#181745=CARTESIAN_POINT ( 'NONE',  ( 4.733292769410803125, 0.005207392524877744490, -2.062741129207305235 ) ) ;
#181750=CARTESIAN_POINT ( 'NONE',  ( 0.9375778709549039691, 0.8456052968917522339, -1.912177616049218098 ) ) ;
#181751=CARTESIAN_POINT ( 'NONE',  ( 4.247483403459266782, 1.840758003770435414, -0.04960325993209198370 ) ) ;
#181753=CARTESIAN_POINT ( 'NONE',  ( 2.309205411980755240, -0.3811568730716380915, 1.681943839628738058 ) ) ;
#181754=CARTESIAN_POINT ( 'NONE',  ( -0.01248194115436446205, -0.5331630387654020531, 1.944732228473695868 ) ) ;
#181755=CARTESIAN_POINT ( 'NONE',  ( 1.670936656956054644, 1.588967112724626096, 1.661273962566457874 ) ) ;
#181757=CARTESIAN_POINT ( 'NONE',  ( 1.722331603166191050, -1.256259422768091216, -1.881381621351454037 ) ) ;
#181758=CARTESIAN_POINT ( 'NONE',  ( 4.125680639212436773, -2.015421878069530326, 0.6112012065569141228 ) ) ;
#181760=CARTESIAN_POINT ( 'NONE',  ( 2.653260118625869080, 0.4764888685691510140, -1.704286641089979959 ) ) ;
#181768=CARTESIAN_POINT ( 'NONE',  ( 5.115582552657226501, 1.816446842268246931, 1.278514946224351689 ) ) ;
#181769=CARTESIAN_POINT ( 'NONE',  ( 3.152458698460915532, -1.659165413833121550, 1.431739491984926449 ) ) ;
#181772=CARTESIAN_POINT ( 'NONE',  ( 6.164709077089638001, 0.6648188651474650213, 2.013622499735030491 ) ) ;
#181774=CARTESIAN_POINT ( 'NONE',  ( 6.609999999999971010, 7.629137130509032971, 2.319999999999996287 ) ) ;
#181777=CARTESIAN_POINT ( 'NONE',  ( 5.326475955075804514, -0.9554483686352827077, -1.893264085526874974 ) ) ;
#181783=CARTESIAN_POINT ( 'NONE',  ( 5.829618728418341611, 0.9018330327132916269, -1.605192750430362025 ) ) ;
#181786=CARTESIAN_POINT ( 'NONE',  ( 1.188542350144041304, 1.317171145998846216, 1.137751157100845623 ) ) ;
#181788=CARTESIAN_POINT ( 'NONE',  ( 0.2562055958934654210, -1.961350414083770977, -0.05204156388862594962 ) ) ;
#181791=CARTESIAN_POINT ( 'NONE',  ( 5.506754051192107369, 1.639644015412666800, -1.408845030788405506 ) ) ;
#181796=CARTESIAN_POINT ( 'NONE',  ( 4.821240550277555492, -0.1094919189667045711, 2.159058991224649393 ) ) ;
#181800=CARTESIAN_POINT ( 'NONE',  ( 5.501234710350423107, 1.610096860432849830, 1.137200068526170060 ) ) ;
#181801=CARTESIAN_POINT ( 'NONE',  ( 5.553917692138156781, 1.528130387303320514, -0.8190655202615308994 ) ) ;
#181803=CARTESIAN_POINT ( 'NONE',  ( 2.331793494658142230, 1.030094174309360344, -1.934364310732391345 ) ) ;
#181804=CARTESIAN_POINT ( 'NONE',  ( 3.118547318853508887, -1.136067310315771905, -2.008477146686512782 ) ) ;
#181805=CARTESIAN_POINT ( 'NONE',  ( 4.552062217129227761, 2.060418430787996691, -0.04653940209857834048 ) ) ;
#181806=CARTESIAN_POINT ( 'NONE',  ( 0.4275465750286939204, 0.9991681100989335818, -1.665045846455282863 ) ) ;
#181811=CARTESIAN_POINT ( 'NONE',  ( 4.465154236216789307, -1.701427117168831549, 1.265499569954648962 ) ) ;
#181812=CARTESIAN_POINT ( 'NONE',  ( 1.143204175302305670, 0.8197749522141674072, 1.842446510343001442 ) ) ;
#181814=CARTESIAN_POINT ( 'NONE',  ( 4.911249081476436018, 1.917979745144289261, 1.091307337132418454 ) ) ;
#181820=CARTESIAN_POINT ( 'NONE',  ( 6.825078400183550720, 7.629137130509051623, 2.844348168701658075 ) ) ;
#181823=CARTESIAN_POINT ( 'NONE',  ( 3.573166805712838734, 0.05218571934602388163, -2.060405206736420247 ) ) ;
#181826=CARTESIAN_POINT ( 'NONE',  ( 3.070967880043346199, -1.527814596969854000, 1.321012706414641524 ) ) ;
#181829=CARTESIAN_POINT ( 'NONE',  ( 3.221608841920938993, -1.986550002599724252, 0.5482939856576442006 ) ) ;
#181832=CARTESIAN_POINT ( 'NONE',  ( -0.1408020194049912077, 0.6951682901239358836, -2.180991432481160341 ) ) ;
#181833=CARTESIAN_POINT ( 'NONE',  ( 1.200829095903386046, -0.4490931065196464012, 1.785404219219708377 ) ) ;
#181834=CARTESIAN_POINT ( 'NONE',  ( 0.1711457161924005987, -1.502117798334397403, 1.751973695569712497 ) ) ;
#181836=CARTESIAN_POINT ( 'NONE',  ( 2.020999711022552159, 2.016103727727487804, 0.7800470891412072394 ) ) ;
#181838=CARTESIAN_POINT ( 'NONE',  ( 2.149625371984189126, 1.976669504256656218, -0.3981124878784659815 ) ) ;
#181841=CARTESIAN_POINT ( 'NONE',  ( 0.5494049127674709432, 0.5909524230637287490, -1.774924738581270089 ) ) ;
#181843=CARTESIAN_POINT ( 'NONE',  ( 4.293796034307355569, -0.7555264168055545460, 1.821139111365249308 ) ) ;
#181844=CARTESIAN_POINT ( 'NONE',  ( 5.120327457147888950, 1.987497208294352280, 0.3399611521368098854 ) ) ;
#181848=CARTESIAN_POINT ( 'NONE',  ( 6.340466044077378349, 2.082889313809291654, 0.3107213310214774760 ) ) ;
#181849=CARTESIAN_POINT ( 'NONE',  ( 4.826661161267837841, -1.354893614093263254, 1.565527137264411728 ) ) ;
#181853=CARTESIAN_POINT ( 'NONE',  ( 4.974870412032891487, -1.460018184141493647, 1.395898791055903976 ) ) ;
#181855=CARTESIAN_POINT ( 'NONE',  ( 3.616130377633751003, -2.273733826016415716, 0.3936331181264277612 ) ) ;
#181857=CARTESIAN_POINT ( 'NONE',  ( 1.323174825800084609, -1.862915942116917689, -0.8856262590048938899 ) ) ;
#181864=CARTESIAN_POINT ( 'NONE',  ( 3.719319017856066445, -1.913190415241170728, -1.026542932298198485 ) ) ;
#181868=CARTESIAN_POINT ( 'NONE',  ( 2.612652284633736777, -0.1782932461553646819, 1.832575692395449485 ) ) ;
#181870=CARTESIAN_POINT ( 'NONE',  ( 4.757479570170550787, 2.167726397749652367, -0.3216086267831194112 ) ) ;
#181872=CARTESIAN_POINT ( 'NONE',  ( 5.366221907327076046, 1.110187712879026956, 1.971344288924305799 ) ) ;
#181877=CARTESIAN_POINT ( 'NONE',  ( 6.696582006438861256, -0.4751199114862921791, -1.704715723353955381 ) ) ;
#181878=CARTESIAN_POINT ( 'NONE',  ( 3.703774327200870076, 1.459685083667804362, 1.386552827976398339 ) ) ;
#181880=CARTESIAN_POINT ( 'NONE',  ( 3.171027762369707848, -1.945216043820027663, -0.8074606443248407706 ) ) ;
#181881=CARTESIAN_POINT ( 'NONE',  ( 0.5443723441289443077, -1.386745921179835417, 1.321778134454040687 ) ) ;
#181884=CARTESIAN_POINT ( 'NONE',  ( 1.680066331807037905, -1.091455746017004014, -1.639250758224161775 ) ) ;
#181885=CARTESIAN_POINT ( 'NONE',  ( 0.8482696660519238874, 0.5391449902514727777, 1.791282564952957124 ) ) ;
#181886=CARTESIAN_POINT ( 'NONE',  ( 1.082386330805637398, 1.171445227557347923, -1.573568114121715933 ) ) ;
#181887=CARTESIAN_POINT ( 'NONE',  ( 0.4746845637013075159, -1.383529810647101455, 1.320479256824915071 ) ) ;
#181892=CARTESIAN_POINT ( 'NONE',  ( 6.262560305340551636, -1.321439916381482060, 1.324322166508178356 ) ) ;
#181896=CARTESIAN_POINT ( 'NONE',  ( 1.293514844328220281, -1.872496763586928514, 0.8835221827151735763 ) ) ;
#181902=CARTESIAN_POINT ( 'NONE',  ( 5.145234815219777325, 0.1564148900096741512, 2.114790009947895122 ) ) ;
#181909=CARTESIAN_POINT ( 'NONE',  ( 6.531700620877029628, 1.877769495358465157, -0.5682946464737671510 ) ) ;
#181911=CARTESIAN_POINT ( 'NONE',  ( 3.339220083777879378, -1.203169880011810022, 1.617570133648409847 ) ) ;
#181912=CARTESIAN_POINT ( 'NONE',  ( 3.819475811356612738, -1.325201190313522792, -1.383632964731799531 ) ) ;
#181914=CARTESIAN_POINT ( 'NONE',  ( 1.540847765565691807, -1.849059859674206496, 1.176127931831471907 ) ) ;
#181916=CARTESIAN_POINT ( 'NONE',  ( 3.409304255485625657, -0.3681080166235695117, 1.833790788056933962 ) ) ;
#181918=CARTESIAN_POINT ( 'NONE',  ( 4.658451966079163675, 2.008086622728368464, 0.1439865329972197516 ) ) ;
#181922=CARTESIAN_POINT ( 'NONE',  ( 6.151990787553828888, 1.088749021807510431, 1.815729776765177661 ) ) ;
#181925=CARTESIAN_POINT ( 'NONE',  ( 2.648082478619179003, 0.7070732986501033768, 1.967675578925948354 ) ) ;
#181927=CARTESIAN_POINT ( 'NONE',  ( 0.2524154375680361939, -1.389930774942317759, 1.021034751394875428 ) ) ;
#181936=CARTESIAN_POINT ( 'NONE',  ( 0.6447925058646056806, 0.1317677938489550116, 1.806752140514777283 ) ) ;
#181942=CARTESIAN_POINT ( 'NONE',  ( 6.639320575229231025, 3.706874577532508486, 2.311316081152973823 ) ) ;
#181947=CARTESIAN_POINT ( 'NONE',  ( 2.857670863715315424, -0.5868061553097079219, 1.766171933019081042 ) ) ;
#181948=CARTESIAN_POINT ( 'NONE',  ( -0.1236200418614826352, -0.4170706148690634385, -1.876090511053402965 ) ) ;
#181949=CARTESIAN_POINT ( 'NONE',  ( 6.176777841581622575, -1.829441475422811436, -0.6035904912435466896 ) ) ;
#181956=CARTESIAN_POINT ( 'NONE',  ( 4.451979310445155491, -0.7576744193203123201, 1.818072383216073007 ) ) ;
#181957=CARTESIAN_POINT ( 'NONE',  ( 1.278162280329109279, 2.088516533416693743, -0.3659721813360562459 ) ) ;
#181962=CARTESIAN_POINT ( 'NONE',  ( 6.193348084369689310, -0.7418380161853586063, 2.062208804312585020 ) ) ;
#181964=CARTESIAN_POINT ( 'NONE',  ( 3.873980538081963854, 1.069312750484844088, 1.602167800089354222 ) ) ;
#181966=CARTESIAN_POINT ( 'NONE',  ( 1.541937560865791479, -1.600244427420342896, -1.519961040588948986 ) ) ;
#181971=CARTESIAN_POINT ( 'NONE',  ( 5.946149452469858154, -0.8887192358506822432, 1.757629817417952767 ) ) ;
#181972=CARTESIAN_POINT ( 'NONE',  ( 1.874458991091961568, -0.09742729390963811298, -1.939748921942837878 ) ) ;
#181973=CARTESIAN_POINT ( 'NONE',  ( 0.1751529202326657098, -0.8592662624449104447, -1.822031250676876768 ) ) ;
#181975=CARTESIAN_POINT ( 'NONE',  ( 3.889374201350876525, -1.720966249256241865, 0.7085912657165122086 ) ) ;
#181981=CARTESIAN_POINT ( 'NONE',  ( 0.4686481397476391364, -2.065551408369214137, -0.7328327568804984260 ) ) ;
#181985=CARTESIAN_POINT ( 'NONE',  ( 1.664397423953474009, -1.292156093668932693, 1.290017532847971271 ) ) ;
#181987=CARTESIAN_POINT ( 'NONE',  ( 3.322662972295143291, 0.7760272377477626105, -1.550874960589002871 ) ) ;
#181989=CARTESIAN_POINT ( 'NONE',  ( 6.609000000000042618, 6.036791015687303918, 2.594900324319386886 ) ) ;
#181990=CARTESIAN_POINT ( 'NONE',  ( 6.164658409365947556, -1.287482145768016339, 1.294691480910937775 ) ) ;
#181991=CARTESIAN_POINT ( 'NONE',  ( 4.979329090789969214, -0.1002203015587413149, 1.959344625532564610 ) ) ;
#181994=CARTESIAN_POINT ( 'NONE',  ( 4.793665170694914046, 1.978287127071875151, -0.7638792978137475265 ) ) ;
#181998=CARTESIAN_POINT ( 'NONE',  ( 2.377862429009020229, -2.009158356589606953, 0.4988364127441884399 ) ) ;
#182002=CARTESIAN_POINT ( 'NONE',  ( 3.270466940867942984, 2.077131924838520050, -0.9849289250120364381 ) ) ;
#182009=CARTESIAN_POINT ( 'NONE',  ( 4.359561026920276916, -1.481784043772149229, -1.208992945495937610 ) ) ;
#182011=CARTESIAN_POINT ( 'NONE',  ( 5.772382705887088683, -1.090832958316660273, 1.335977363661453809 ) ) ;
#182012=CARTESIAN_POINT ( 'NONE',  ( 3.801970467005914678, -1.040791964576088358, -1.727064642965264740 ) ) ;
#182013=CARTESIAN_POINT ( 'NONE',  ( 4.887441975664971849, -0.7727101442582262614, -2.165022144963870243 ) ) ;
#182015=CARTESIAN_POINT ( 'NONE',  ( 1.278255639411193245, 1.316999024263129092, 1.770685722221450709 ) ) ;
#182017=CARTESIAN_POINT ( 'NONE',  ( 5.430809967973590169, 0.1307738731834498513, 1.764929826691101100 ) ) ;
#182020=CARTESIAN_POINT ( 'NONE',  ( 2.326505592738498329, 2.223965110380062615, 0.5549310701656160472 ) ) ;
#182021=CARTESIAN_POINT ( 'NONE',  ( -0.02397475188680147154, -0.1303385410800334265, -1.711279094490937069 ) ) ;
#182028=CARTESIAN_POINT ( 'NONE',  ( 0.7487581336349375949, -2.154818914559033072, -0.2656684361399003214 ) ) ;
#182029=CARTESIAN_POINT ( 'NONE',  ( 1.780482797753998092, -0.5424726148271253878, -1.942096288550937411 ) ) ;
#182031=CARTESIAN_POINT ( 'NONE',  ( 5.233004834321499210, 0.1438781470856145273, 1.921186297865638215 ) ) ;
#182033=CARTESIAN_POINT ( 'NONE',  ( 2.479030958227887549, -1.528377378988081015, 1.612298682912993275 ) ) ;
#182039=CARTESIAN_POINT ( 'NONE',  ( 4.265022598847971302, 1.686782405526715545, -0.4282675217706712889 ) ) ;
#182040=CARTESIAN_POINT ( 'NONE',  ( 4.053139552913617827, 1.658577106941661272, -1.047563642765911185 ) ) ;
#182047=CARTESIAN_POINT ( 'NONE',  ( 1.064971659385913316, 1.563282549206745475, -1.345778378556292676 ) ) ;
#182050=CARTESIAN_POINT ( 'NONE',  ( 0.6907310396802420760, -2.245820052064306349, -0.2739839911451089627 ) ) ;
#182053=CARTESIAN_POINT ( 'NONE',  ( 2.987410616422137899, 1.320145714686842497, 1.325460448179466066 ) ) ;
#182054=CARTESIAN_POINT ( 'NONE',  ( 1.072469862579095379, -0.7803941858975007584, 1.548669665330544953 ) ) ;
#182055=CARTESIAN_POINT ( 'NONE',  ( 5.390230798962840630, -0.5317533105795355652, -2.125930911514521959 ) ) ;
#182056=CARTESIAN_POINT ( 'NONE',  ( 0.2181801407958559869, -2.163675782650812618, 0.4331315337846516900 ) ) ;
#182057=CARTESIAN_POINT ( 'NONE',  ( 1.235309500465184396, -1.863545150897191416, 0.8803144705526543268 ) ) ;
#182058=CARTESIAN_POINT ( 'NONE',  ( 2.994010707676255212, -0.5641155714235489560, -1.858205125314008832 ) ) ;
#182060=CARTESIAN_POINT ( 'NONE',  ( 5.659403934932580427, 0.3656299861228041737, -1.834283699791404043 ) ) ;
#182061=CARTESIAN_POINT ( 'NONE',  ( 1.093750000000000666, -1.895863743164112547, -0.7852924748299294766 ) ) ;
#182063=CARTESIAN_POINT ( 'NONE',  ( 6.345077344222471716, -1.080897578067066878, 1.701688803805063266 ) ) ;
#182065=CARTESIAN_POINT ( 'NONE',  ( 4.149064681782777875, 0.9530105817698063531, 1.777011888912001014 ) ) ;
#182069=CARTESIAN_POINT ( 'NONE',  ( 2.420285107995377327, 1.192830232448302441, -1.382225081888274643 ) ) ;
#182077=CARTESIAN_POINT ( 'NONE',  ( -0.2048590494372501680, -0.1558505989666530422, -1.986559690435693026 ) ) ;
#182078=CARTESIAN_POINT ( 'NONE',  ( 6.287741706623968696, 2.126563164181693555, -0.6417273904879957636 ) ) ;
#182083=CARTESIAN_POINT ( 'NONE',  ( 6.455941844152293996, 2.055567607077302128, -0.1488206295068068841 ) ) ;
#182084=CARTESIAN_POINT ( 'NONE',  ( 5.625625018759272677, 0.3960990390993284205, 1.976956468877195894 ) ) ;
#182089=( BOUNDED_CURVE ( )  B_SPLINE_CURVE ( 3, ( #41829, #101730, #59111, #25541 ),
 .UNSPECIFIED., .F., .T. ) 
 B_SPLINE_CURVE_WITH_KNOTS ( ( 4, 4 ),
 ( 0.4999999999999967248, 1.000000000000000000 ),
 .UNSPECIFIED. ) 
 CURVE ( )  GEOMETRIC_REPRESENTATION_ITEM ( )  RATIONAL_B_SPLINE_CURVE ( ( 1.000000000000004663, 0.3333333333333334814, 0.3333333333333290960, 1.000000000000000222 ) ) 
 REPRESENTATION_ITEM ( '' )  );
#182093=CARTESIAN_POINT ( 'NONE',  ( 5.149767453795408123, -0.2439937967673235231, -2.001204641050558397 ) ) ;
#182094=CARTESIAN_POINT ( 'NONE',  ( 4.734224819668921391, 0.3176365174208677367, 1.813369535050498360 ) ) ;
#182095=CARTESIAN_POINT ( 'NONE',  ( 0.07661050522430287724, 1.422454998960010153, -1.972067596371825715 ) ) ;
#182096=CARTESIAN_POINT ( 'NONE',  ( 2.825201024400230132, 2.173230126089547909, 0.7765846127750095640 ) ) ;
#182099=CARTESIAN_POINT ( 'NONE',  ( 5.114612887932482366, 1.494710344919391476, -1.561737693111686642 ) ) ;
#182101=CARTESIAN_POINT ( 'NONE',  ( 1.663517674946796143, 1.000093669912437644, 1.664638661912527962 ) ) ;
#182104=CARTESIAN_POINT ( 'NONE',  ( 4.042538402956846966, 2.165829419810465950, -0.7696314825454602104 ) ) ;
#182107=CARTESIAN_POINT ( 'NONE',  ( 2.922558825391399662, 1.760836971185793187, 0.6318509464167121337 ) ) ;
#182108=CARTESIAN_POINT ( 'NONE',  ( 1.054777118923880597, 0.3758132965740559883, 1.874924941132802836 ) ) ;
#182111=CARTESIAN_POINT ( 'NONE',  ( 3.246891520140795517, 0.5363302883765566076, 2.140594385818309409 ) ) ;
#182118=CARTESIAN_POINT ( 'NONE',  ( 0.7023363917650466970, -0.6599406036866415359, -1.857761218813491988 ) ) ;
#182119=CARTESIAN_POINT ( 'NONE',  ( 0.5347316126107805045, 1.182704979252725108, -1.981343935211031138 ) ) ;
#182120=CARTESIAN_POINT ( 'NONE',  ( 1.732786548908150870, -1.861864252656076912, -0.6185235971247133868 ) ) ;
#182122=CARTESIAN_POINT ( 'NONE',  ( 4.856332268735650715, -2.061987677746464076, -0.05593471103338721467 ) ) ;
#182130=CARTESIAN_POINT ( 'NONE',  ( 0.4796376738960402841, -0.1079922143863345368, 2.168524981076371372 ) ) ;
#182134=CARTESIAN_POINT ( 'NONE',  ( 1.053721402318724021, 1.868689351376726204, -0.08586956420430363890 ) ) ;
#182135=CARTESIAN_POINT ( 'NONE',  ( 5.307972821619873827, -2.151738229465068653, 0.2060058040841972193 ) ) ;
#182140=CARTESIAN_POINT ( 'NONE',  ( 1.471198412684338486, -1.640640410176617658, -0.9821394255850326438 ) ) ;
#182141=CARTESIAN_POINT ( 'NONE',  ( 2.606023559441010828, -0.6750964425338638053, -1.636234759011189421 ) ) ;
#182142=CARTESIAN_POINT ( 'NONE',  ( 0.8735180803765253410, 0.3724630581584260081, -1.875478908130092215 ) ) ;
#182144=CARTESIAN_POINT ( 'NONE',  ( 6.011341193797766103, -1.801927099207595084, 0.6504362055675115828 ) ) ;
#182146=CARTESIAN_POINT ( 'NONE',  ( 0.1392002015415672034, -0.1474423581745692435, -2.037351525059682977 ) ) ;
#182147=CARTESIAN_POINT ( 'NONE',  ( 1.389100911873580646, -2.015333191458138273, -0.6601287711371638389 ) ) ;
#182149=CARTESIAN_POINT ( 'NONE',  ( 3.994877460428855276, 1.580554378303768992, -1.000287695324620252 ) ) ;
#182150=CARTESIAN_POINT ( 'NONE',  ( 0.7502976729042536430, 0.5272139720400963459, 1.747899773703022408 ) ) ;
#182152=CARTESIAN_POINT ( 'NONE',  ( 2.948105999307056635, 0.7938017206191756436, -2.059354589195587337 ) ) ;
#182155=CARTESIAN_POINT ( 'NONE',  ( 1.768110600389400933, -2.047337470793224146, 0.2504565381693297788 ) ) ;
#182162=CARTESIAN_POINT ( 'NONE',  ( 4.158688916442685013, -0.6465363538536235133, -1.966910096795893681 ) ) ;
#182164=CARTESIAN_POINT ( 'NONE',  ( 1.546389740860309781, 2.159050155192781872, 0.1077149563947499555 ) ) ;
#182166=CARTESIAN_POINT ( 'NONE',  ( 2.262373273732374290, 2.019286824851754591, 0.04726863806006965929 ) ) ;
#182173=CARTESIAN_POINT ( 'NONE',  ( 6.802112138117927920, -1.802125342305498146, 0.9040232568291312054 ) ) ;
#182174=CARTESIAN_POINT ( 'NONE',  ( 0.1632964843477149597, 1.879801964727344732, -0.7303121171872913875 ) ) ;
#182175=FACE_OUTER_BOUND ( 'NONE', #19057, .T. ) ;
#182176=CARTESIAN_POINT ( 'NONE',  ( 4.862908538974716421, 0.2148362657848034984, -2.180980218048253150 ) ) ;
#182179=CARTESIAN_POINT ( 'NONE',  ( 3.550944491985886575, 0.2853618425060593378, 1.890879049853078087 ) ) ;
#182184=CARTESIAN_POINT ( 'NONE',  ( 1.704704067347760699, 1.882482151684254923, 0.7231221989368596947 ) ) ;
#182186=CARTESIAN_POINT ( 'NONE',  ( 0.6445460132639491135, 0.6724220840489106843, 2.191533042908066165 ) ) ;
#182188=CARTESIAN_POINT ( 'NONE',  ( 3.944159270863063060, 1.716513557549454339, 0.1685945156147239388 ) ) ;
#182192=CARTESIAN_POINT ( 'NONE',  ( 1.592165322863370980, 0.9698756732311950568, -1.705302290208744687 ) ) ;
#182195=CARTESIAN_POINT ( 'NONE',  ( 0.07556134207192893859, 1.990881419511018935, -2.657973000608151448 ) ) ;
#182200=CARTESIAN_POINT ( 'NONE',  ( 4.740750167454264918, 1.734909645891765662, 0.5210944610908369024 ) ) ;
#182204=CARTESIAN_POINT ( 'NONE',  ( 6.516260798181108704, -1.810903427820510503, 0.05229752674829404868 ) ) ;
#182211=CARTESIAN_POINT ( 'NONE',  ( 5.863677653134839574, -0.4517109595482105555, 1.805248464757176041 ) ) ;
#182213=CARTESIAN_POINT ( 'NONE',  ( 3.989770193594462722, -1.910233455636681787, 0.1444642847954723808 ) ) ;
#182219=CARTESIAN_POINT ( 'NONE',  ( 5.647700563513772920, 2.085583167219496215, -0.3645771090082204902 ) ) ;
#182220=CARTESIAN_POINT ( 'NONE',  ( 0.7081719773709762578, -2.151164098719647200, 0.2130325561137471624 ) ) ;
#182223=CARTESIAN_POINT ( 'NONE',  ( 1.184280053745472738, -1.780106929851841491, -0.4042017716930704219 ) ) ;
#182225=CARTESIAN_POINT ( 'NONE',  ( 3.487140482124751362, 1.650829432287181264, -0.7796944959364560113 ) ) ;
#182228=CARTESIAN_POINT ( 'NONE',  ( 2.699605434738296506, -1.457443026130700758, -1.324932107022150918 ) ) ;
#182229=CARTESIAN_POINT ( 'NONE',  ( 4.810071659083087425, 1.336522264689719686, -1.409242981738271894 ) ) ;
#182232=CARTESIAN_POINT ( 'NONE',  ( 5.273731010124149243, 0.4114677744767555878, -2.080124947408354963 ) ) ;
#182234=CARTESIAN_POINT ( 'NONE',  ( 3.281800106729782840, 1.865104756965057620, -0.4213900744019505318 ) ) ;
#182241=CARTESIAN_POINT ( 'NONE',  ( 4.564971734551386717, -1.632036996880025903, -0.8184370388232551363 ) ) ;
#182247=CARTESIAN_POINT ( 'NONE',  ( 5.137510444216992767, -1.323429205136433140, -1.322332877454430955 ) ) ;
#182257=CARTESIAN_POINT ( 'NONE',  ( 6.491115304390381979, 0.2044268322529273207, 2.161409909153473752 ) ) ;
#182258=CARTESIAN_POINT ( 'NONE',  ( 2.583745723679788497, -0.6611301898758483730, 2.011445711247431323 ) ) ;
#182261=CARTESIAN_POINT ( 'NONE',  ( 6.368043163206878354, -2.055323469740528264, 0.2474699835256082281 ) ) ;
#182266=CARTESIAN_POINT ( 'NONE',  ( 2.449550052152906332, 0.6095859302821411418, -2.209661595554306412 ) ) ;
#182269=CARTESIAN_POINT ( 'NONE',  ( 2.091926199050548441, 1.179367891222588005, 1.505316542580182659 ) ) ;
#182273=CARTESIAN_POINT ( 'NONE',  ( 0.7209482731112315523, 1.521806550355369492, -1.318046908132961104 ) ) ;
#182274=CARTESIAN_POINT ( 'NONE',  ( 0.7077677203753615087, 0.6208407433182620005, -1.860969989990405749 ) ) ;
#182277=CARTESIAN_POINT ( 'NONE',  ( 3.820331522234471144, 1.985175722263971654, 0.6558375257153716831 ) ) ;
#182278=CARTESIAN_POINT ( 'NONE',  ( 2.025891818203702233, 1.021928659931588435, -1.444778566663025954 ) ) ;
#182281=CARTESIAN_POINT ( 'NONE',  ( 5.525394443818422374, -1.450416979558573072, -1.775029086184358507 ) ) ;
#182282=CARTESIAN_POINT ( 'NONE',  ( 3.486021976759791308, -0.3410757193606011040, -1.706382030880509104 ) ) ;
#182286=CARTESIAN_POINT ( 'NONE',  ( 3.004952549044386245, 1.720378813442688282, 0.2150250689552536121 ) ) ;
#182287=CARTESIAN_POINT ( 'NONE',  ( 3.701788104937975721, -1.641978770885927252, -1.420606208986204155 ) ) ;
#182289=CARTESIAN_POINT ( 'NONE',  ( 5.559779856078610472, 1.205038519190555268, 1.616695979245158066 ) ) ;
#182290=CARTESIAN_POINT ( 'NONE',  ( 0.7187500000000003331, -0.7852924748299483504, 1.895863743164105220 ) ) ;
#182292=CARTESIAN_POINT ( 'NONE',  ( 2.555585810550043302, 0.5154765373659023764, -1.856070933656640332 ) ) ;
#182294=CARTESIAN_POINT ( 'NONE',  ( 5.888988880356018640, -2.109219445749145994, -0.6973366327849057633 ) ) ;
#182296=CARTESIAN_POINT ( 'NONE',  ( 6.983263157960340806, 6.037546352565132501, 2.441087094350186337 ) ) ;
#182307=CARTESIAN_POINT ( 'NONE',  ( 4.721170020219593866, -1.840989660556498597, -0.9304453918272929114 ) ) ;
#182311=CARTESIAN_POINT ( 'NONE',  ( 5.483624757375023862, 1.255567903217995829, 1.386730702750748945 ) ) ;
#182312=CARTESIAN_POINT ( 'NONE',  ( 4.359819935191601381, -0.006009022472676025205, -1.734343005118470726 ) ) ;
#182313=CARTESIAN_POINT ( 'NONE',  ( 3.931004251652202353, -1.203735069864294571, -1.257276804044287655 ) ) ;
#182315=CARTESIAN_POINT ( 'NONE',  ( 1.435548669473255323, -1.664339209632224481, -1.576619915386682447 ) ) ;
#182317=CARTESIAN_POINT ( 'NONE',  ( 6.163634092203726489, 1.075319730316869560, 1.792882302630414593 ) ) ;
#182318=CARTESIAN_POINT ( 'NONE',  ( 0.5855841007226803008, -1.826885663252286740, -0.2280376995877145263 ) ) ;
#182321=CARTESIAN_POINT ( 'NONE',  ( 2.127577483945505055, 0.4445034925110411539, 1.966644524931899563 ) ) ;
#182327=CARTESIAN_POINT ( 'NONE',  ( 3.862070080935349203, 0.7130468835700142227, -1.997148454185311506 ) ) ;
#182330=CARTESIAN_POINT ( 'NONE',  ( 5.813091150998386247, 1.612263477354998864, 0.8566026058636074803 ) ) ;
#182336=CARTESIAN_POINT ( 'NONE',  ( 3.023699206349286239, -0.3898671064326043045, 1.981619672226095918 ) ) ;
#182337=CARTESIAN_POINT ( 'NONE',  ( 6.370183515248876382, 1.128980158350336049, 1.895982279999992359 ) ) ;
#182339=CARTESIAN_POINT ( 'NONE',  ( 3.871788065385643574, -1.834046284760854961, 0.3141801383321814467 ) ) ;
#182345=CARTESIAN_POINT ( 'NONE',  ( 0.1105426557568081891, -0.9253945370547181914, -1.951590883024490353 ) ) ;
#182349=CARTESIAN_POINT ( 'NONE',  ( 1.176590053548575598, -0.7728590343649595074, -1.552129106697144989 ) ) ;
#182350=CARTESIAN_POINT ( 'NONE',  ( 1.763200577577472172, 0.8928190760214287369, 1.493706742695336764 ) ) ;
#182351=CARTESIAN_POINT ( 'NONE',  ( 6.199901738523720951, -0.7837251098280417771, 2.170682987836409783 ) ) ;
#182354=CARTESIAN_POINT ( 'NONE',  ( 1.493510409444120057, 1.558468831475682492, 1.348393839584006493 ) ) ;
#182356=CARTESIAN_POINT ( 'NONE',  ( 0.4739822347885510601, 1.752760637641921360, 0.9961516927870717186 ) ) ;
#182359=CARTESIAN_POINT ( 'NONE',  ( 6.614126560844452385, -0.8839695271746010885, -1.648598838400926692 ) ) ;
#182360=CARTESIAN_POINT ( 'NONE',  ( 5.045129621168108258, 0.1466893748028277877, 1.906852434080000824 ) ) ;
#182362=CARTESIAN_POINT ( 'NONE',  ( 6.393228082638676923, 1.922373441260841087, -1.083778638264052852 ) ) ;
#182366=CARTESIAN_POINT ( 'NONE',  ( 0.1529977018510132181, 0.3474608822290006782, 1.989397386523162226 ) ) ;
#182368=CARTESIAN_POINT ( 'NONE',  ( 2.995503060082918889, 1.979820613015465858, -1.185208598768563881 ) ) ;
#182369=CARTESIAN_POINT ( 'NONE',  ( 4.685966490639408732, -1.205361723144786845, -1.547842780461285761 ) ) ;
#182371=CARTESIAN_POINT ( 'NONE',  ( 1.850371385673426294, -1.951817131159512719, -0.1975377159662907445 ) ) ;
#182374=CARTESIAN_POINT ( 'NONE',  ( 0.6204977360529799757, 2.087120111646578291, 0.3555802741468729877 ) ) ;
#182377=CARTESIAN_POINT ( 'NONE',  ( 0.3570341529223716726, 1.821527202347131169, -0.2672101559373847857 ) ) ;
#182378=CARTESIAN_POINT ( 'NONE',  ( 4.750930541093643100, -0.4693155065514472701, -2.119606683777853995 ) ) ;
#182380=CARTESIAN_POINT ( 'NONE',  ( 1.705496241919310707, 1.842552997918958768, -1.049655202612943095 ) ) ;
#182386=CARTESIAN_POINT ( 'NONE',  ( 2.143891142268034677, 0.7916089892260335104, -1.902880034897576733 ) ) ;
#182394=CARTESIAN_POINT ( 'NONE',  ( 4.828717125059535320, 1.315996081294769304, -1.387672938220223307 ) ) ;
#182397=CARTESIAN_POINT ( 'NONE',  ( 1.195004664211458456, -0.5499296976853912389, -2.194457269061194982 ) ) ;
#182399=CARTESIAN_POINT ( 'NONE',  ( 1.810541516808946039, -0.4857983738905074511, -1.745121406981971157 ) ) ;
#182400=CARTESIAN_POINT ( 'NONE',  ( 1.446349702961244876, -1.352062789758176731, 1.357433777346368498 ) ) ;
#182401=CARTESIAN_POINT ( 'NONE',  ( 3.068866956829822801, 1.501395149897828851, -1.425812640530661479 ) ) ;
#182404=CARTESIAN_POINT ( 'NONE',  ( 0.6902270635062581761, -1.956280663680696197, -0.2437950987402882630 ) ) ;
#182405=CARTESIAN_POINT ( 'NONE',  ( 5.637312448503878137, -1.740617781635974248, 0.8259078106758013238 ) ) ;
#182406=CARTESIAN_POINT ( 'NONE',  ( 1.647554839532150872, -1.947651944554330772, 1.237524531948221096 ) ) ;
#182409=CARTESIAN_POINT ( 'NONE',  ( 5.178211798877670802, -1.100624681205965461, -1.744318484351764509 ) ) ;
#182413=CARTESIAN_POINT ( 'NONE',  ( 4.928798221971478988, 2.014404525830254311, 0.6141583887315901213 ) ) ;
#182416=CARTESIAN_POINT ( 'NONE',  ( 5.202478051755599964, -0.7228594145181690411, -2.037298988101433839 ) ) ;
#182417=CARTESIAN_POINT ( 'NONE',  ( 5.461584154626091703, -1.593396655685812124, -1.240940796477793873 ) ) ;
#182426=CARTESIAN_POINT ( 'NONE',  ( 4.083220446344194343, 1.622485107653489633, 1.197306254465977826 ) ) ;
#182431=CARTESIAN_POINT ( 'NONE',  ( 4.891577088959510711, 1.599438101461609918, 1.454397306527709155 ) ) ;
#182434=CARTESIAN_POINT ( 'NONE',  ( 6.720655732516672920, 1.239197277384354035, 2.287559680360019332 ) ) ;
#182436=CARTESIAN_POINT ( 'NONE',  ( 5.273064617572334356, 1.777004185780726386, -0.9530273427700783895 ) ) ;
#182438=CARTESIAN_POINT ( 'NONE',  ( 0.3106396986791125081, 1.498014557929911117, 0.8549171915634717900 ) ) ;
#182443=CARTESIAN_POINT ( 'NONE',  ( 6.221928862670094595, -1.039020359566013907, -1.555222851818117924 ) ) ;
#182444=CARTESIAN_POINT ( 'NONE',  ( 0.9439945835589347300, -1.278642754803262171, -1.554848376591860815 ) ) ;
#182450=CARTESIAN_POINT ( 'NONE',  ( 1.823052125313682215, 1.569171740784220281, -1.426411057285102979 ) ) ;
#182451=CARTESIAN_POINT ( 'NONE',  ( 2.249625261780491492, 1.976952429928409805, -0.3961248688731587309 ) ) ;
#182452=CARTESIAN_POINT ( 'NONE',  ( 1.986290607305480460, -1.112306265806988437, 1.429831149274364721 ) ) ;
#182454=CARTESIAN_POINT ( 'NONE',  ( 6.737200384369169903, -1.933438233944266837, 0.9670071574134843084 ) ) ;
#182458=CARTESIAN_POINT ( 'NONE',  ( 0.3916159773660661259, -1.906239802237769787, 0.1905982916604181676 ) ) ;
#182465=CARTESIAN_POINT ( 'NONE',  ( 4.434552454296070145, 2.119417814153037316, 0.4246342833542292028 ) ) ;
#182468=CARTESIAN_POINT ( 'NONE',  ( 1.846092968827160119, -1.388944967848893430, -1.602481653760478020 ) ) ;
#182470=CARTESIAN_POINT ( 'NONE',  ( 3.532457849674102590, 1.922574350601889082, 0.4351428330651128662 ) ) ;
#182471=CARTESIAN_POINT ( 'NONE',  ( 5.484596585704371918, -1.208295678440996390, 1.482354609825987435 ) ) ;
#182474=CARTESIAN_POINT ( 'NONE',  ( 5.564895475732142494, 1.492515675241333772, -1.285245034736775649 ) ) ;
#182475=CARTESIAN_POINT ( 'NONE',  ( 1.095531938664672911, -1.942124713061957220, -0.0005026242578913541230 ) ) ;
#182483=CARTESIAN_POINT ( 'NONE',  ( 5.795548653916324788, 1.765151677092157811, -0.7360495477024899813 ) ) ;
#182485=CARTESIAN_POINT ( 'NONE',  ( 3.018423772948013006, -1.088090592406821155, -1.919924466345590108 ) ) ;
#182486=CARTESIAN_POINT ( 'NONE',  ( 1.940722911589174204, 2.182806717142399489, 0.3235914145361811767 ) ) ;
#182488=CARTESIAN_POINT ( 'NONE',  ( 0.8910925258837493201, -0.04752833427993513604, -1.911862225341356858 ) ) ;
#182491=CARTESIAN_POINT ( 'NONE',  ( 4.492674960910642667, 2.029786422369950216, 0.4070406814440513665 ) ) ;
#182495=CARTESIAN_POINT ( 'NONE',  ( 1.938557520917514987, 2.138169252768943984, 0.3173444169591658204 ) ) ;
#182496=CARTESIAN_POINT ( 'NONE',  ( 3.527062600443749307, -2.024233912922444478, 0.8403589366152917073 ) ) ;
#182501=CARTESIAN_POINT ( 'NONE',  ( 6.152912852923398290, 0.8997199139058277284, 1.482343192998013537 ) ) ;
#182504=CARTESIAN_POINT ( 'NONE',  ( 3.063400401570901543, 1.746483293306470674, 1.111379191485066364 ) ) ;
#182505=CARTESIAN_POINT ( 'NONE',  ( 5.712555019607242990, 2.040694153135207412, 0.5639581637400041814 ) ) ;
#182508=CARTESIAN_POINT ( 'NONE',  ( 3.098452163322249042, 1.954020348291004794, 0.2456459092235723785 ) ) ;
#182509=CARTESIAN_POINT ( 'NONE',  ( 0.6504702201592416078, 1.884490048413577368, 0.3244712162126031085 ) ) ;
#182510=CARTESIAN_POINT ( 'NONE',  ( 5.771479170232404421, 1.361120583587755783, 1.844262159060359174 ) ) ;
#182511=CARTESIAN_POINT ( 'NONE',  ( 2.631258204695927194, -1.703542010001803275, 0.6570300758180421807 ) ) ;
#182517=CARTESIAN_POINT ( 'NONE',  ( 4.342045473679829293, -1.241779438462310203, -1.584497923379190931 ) ) ;
#182518=CARTESIAN_POINT ( 'NONE',  ( 3.871884822249270108, -1.933460040528666379, 0.3310023857948928838 ) ) ;
#182521=CARTESIAN_POINT ( 'NONE',  ( 0.07536363704230969462, 1.333366039338843789, -2.397125032416930424 ) ) ;
#182522=CARTESIAN_POINT ( 'NONE',  ( 0.06416430596320726876, -1.362578676618180884, 1.585857439420575776 ) ) ;
#182523=CARTESIAN_POINT ( 'NONE',  ( 5.330810035471644781, 0.1327828994084866154, 1.764904742964703122 ) ) ;
#182526=CARTESIAN_POINT ( 'NONE',  ( 1.816621679704206516, 2.045545470589833492, 0.7867152234099920038 ) ) ;
#182527=CARTESIAN_POINT ( 'NONE',  ( 0.5205769134342881355, -1.653362465512813184, 0.5437448749807861637 ) ) ;
#182529=CARTESIAN_POINT ( 'NONE',  ( 0.2333690889706925009, 5.722554199285137422, -2.647406232470352894 ) ) ;
#182530=CARTESIAN_POINT ( 'NONE',  ( 0.5919146312290176626, -1.711225830157696137, -0.2159481953097255325 ) ) ;
#182531=CARTESIAN_POINT ( 'NONE',  ( 0.4393512522801552023, 1.325809523182071237, 1.877307722886724317 ) ) ;
#182532=CARTESIAN_POINT ( 'NONE',  ( 1.031118135130421498, -1.979082047791239418, 0.9416876394413642437 ) ) ;
#182533=CARTESIAN_POINT ( 'NONE',  ( 6.204387268089465834, -1.258339971413184433, -1.193046581750532464 ) ) ;
#182534=CARTESIAN_POINT ( 'NONE',  ( 3.123846942790895476, -2.126788776302591888, 0.5888931905130634359 ) ) ;
#182536=CARTESIAN_POINT ( 'NONE',  ( 1.727621483090465926, 0.1626789094613217412, -2.165059144495153021 ) ) ;
#182538=CARTESIAN_POINT ( 'NONE',  ( 2.729822841111886333, 0.7574698553451510996, -1.977403127767562552 ) ) ;
#182539=CARTESIAN_POINT ( 'NONE',  ( 6.727182134110239353, -0.007837387828812587484, 2.289081727344749684 ) ) ;
#182540=CARTESIAN_POINT ( 'NONE',  ( 5.543948526327937998, 0.7806568236609288114, -1.761304856208524283 ) ) ;
#182542=CARTESIAN_POINT ( 'NONE',  ( 3.052548088455210973, -1.734419513972422555, 1.498989523525402934 ) ) ;
#182548=CARTESIAN_POINT ( 'NONE',  ( 4.705860574468672120, 1.645629519818484932, 1.492201155203516150 ) ) ;
#182555=CARTESIAN_POINT ( 'NONE',  ( 2.848279904836711118, 0.2930702634792031747, -1.994869876753922799 ) ) ;
#182557=CARTESIAN_POINT ( 'NONE',  ( 0.7958482667242804398, -1.455889974409400045, -1.461266501696573794 ) ) ;
#182562=CARTESIAN_POINT ( 'NONE',  ( 3.679775893577118318, -1.080384588543949809, 1.906543112819548913 ) ) ;
#182563=CARTESIAN_POINT ( 'NONE',  ( 1.758435621656749603, 1.928751379572872571, -0.5880216644931559600 ) ) ;
#182564=CARTESIAN_POINT ( 'NONE',  ( 0.5031362391596030381, -1.832460416942282011, 0.1798594046882526221 ) ) ;
#182565=CARTESIAN_POINT ( 'NONE',  ( 5.741781754149911876, 2.289535525127144311, 0.1160191304092756254 ) ) ;
#182566=CARTESIAN_POINT ( 'NONE',  ( 4.769393013670423009, 1.062472638025207416, 1.503447196605799174 ) ) ;
#182570=CARTESIAN_POINT ( 'NONE',  ( 4.084828617465196210, -0.1788469021064206521, -1.816781805555576668 ) ) ;
#182571=CARTESIAN_POINT ( 'NONE',  ( 4.483046177357690176, -2.016033783801042034, -0.04667830911464498911 ) ) ;
#182573=CARTESIAN_POINT ( 'NONE',  ( 4.733442339874294191, -2.070396585149585356, 0.9127746130930917134 ) ) ;
#182575=CARTESIAN_POINT ( 'NONE',  ( 6.352575683687115671, 0.6571560004794211318, 2.000881423421707161 ) ) ;
#182577=CARTESIAN_POINT ( 'NONE',  ( 4.914543119725925280, 0.7892175071393169317, 1.914236960262293508 ) ) ;
#182582=CARTESIAN_POINT ( 'NONE',  ( 2.402848698864976207, 1.547341197487204001, -1.147474368762817498 ) ) ;
#182584=CARTESIAN_POINT ( 'NONE',  ( 6.702011354250313246, 0.7569246535186587854, -1.818382958529676019 ) ) ;
#182588=CARTESIAN_POINT ( 'NONE',  ( 1.195735321641926197, 1.957225868588155837, -0.8166992996602240318 ) ) ;
#182589=CARTESIAN_POINT ( 'NONE',  ( 1.846216761830053787, -1.455271069044868693, -1.678405531801461903 ) ) ;
#182590=CARTESIAN_POINT ( 'NONE',  ( 3.838982076996471982, 0.3068427722541127722, 2.083350420514245016 ) ) ;
#182593=CARTESIAN_POINT ( 'NONE',  ( 2.717183929654675811, -1.705535211757349456, -0.9694657131227711888 ) ) ;
#182599=CARTESIAN_POINT ( 'NONE',  ( 2.742561299210785286, 1.174483946500170184, -1.765453564165630596 ) ) ;
#182602=CARTESIAN_POINT ( 'NONE',  ( 4.809014631063706524, -1.576880339463518022, 1.167019128429528374 ) ) ;
#182603=CARTESIAN_POINT ( 'NONE',  ( 3.081113354808207916, -0.1575343947536785305, -2.156009052512488200 ) ) ;
#182604=CARTESIAN_POINT ( 'NONE',  ( 2.542321706073047416, -1.529623444112483632, 1.024600984555257277 ) ) ;
#182608=CARTESIAN_POINT ( 'NONE',  ( 4.822041096100106117, 1.666637052750892911, 0.5010418475075908429 ) ) ;
#182613=CARTESIAN_POINT ( 'NONE',  ( 1.973706723050288936, 2.068691090354588091, -0.6273066937243013674 ) ) ;
#182614=CARTESIAN_POINT ( 'NONE',  ( 4.763045971468515383, -2.015604388477490350, -0.05228862439247972116 ) ) ;
#182616=CARTESIAN_POINT ( 'NONE',  ( 1.481558191429487970, 1.997200094811113491, -0.8276061316847342919 ) ) ;
#182618=CARTESIAN_POINT ( 'NONE',  ( 2.869950281991093810, 1.053363813896515788, 1.666286737264175866 ) ) ;
#182619=CARTESIAN_POINT ( 'NONE',  ( 6.509000000000012776, 6.036089120385641493, 2.694901645009006863 ) ) ;
#182620=CARTESIAN_POINT ( 'NONE',  ( 3.175267148988625721, 1.234016112977231794, 1.499580727898646604 ) ) ;
#182629=CARTESIAN_POINT ( 'NONE',  ( 0.8685540286928781217, 1.089157903960279672, 1.919174906450902274 ) ) ;
#182631=EDGE_CURVE ( 'NONE', #57833, #126082, #123683, .T. ) ;
#182632=CARTESIAN_POINT ( 'NONE',  ( 4.891432378139471737, -1.795214109662087942, 0.7913882323652280393 ) ) ;
#182633=CARTESIAN_POINT ( 'NONE',  ( 1.512342498431101134, -1.897697209584522815, 0.6819976561535445736 ) ) ;
#182635=CARTESIAN_POINT ( 'NONE',  ( 3.520818605202329810, 0.3149718393082919232, 2.093694903831443188 ) ) ;
#182639=CARTESIAN_POINT ( 'NONE',  ( 4.505690185649424251, -0.7896136771840707169, -1.663358820747300237 ) ) ;
#182644=CARTESIAN_POINT ( 'NONE',  ( 4.763993809689464065, 0.6627061821620899851, -2.014485251161435286 ) ) ;
#182645=CARTESIAN_POINT ( 'NONE',  ( -0.2106725631050176684, -0.004273297132624804921, -2.003483006309700887 ) ) ;
#182647=CARTESIAN_POINT ( 'NONE',  ( 6.028604891774052454, 1.984808026635048961, 0.5540661066990509864 ) ) ;
#182649=CARTESIAN_POINT ( 'NONE',  ( 0.6778921365368529850, -0.9907528278601520633, -1.575212976145045518 ) ) ;
#182650=CARTESIAN_POINT ( 'NONE',  ( 2.981803241483144351, -1.814435276338403735, -0.3121031562058202424 ) ) ;
#182656=CARTESIAN_POINT ( 'NONE',  ( 2.069229996397306426, -2.018448871333050842, -0.8927042923378907258 ) ) ;
#182657=CARTESIAN_POINT ( 'NONE',  ( 4.358826825731692445, -1.680320932299755210, 1.515136896344573270 ) ) ;
#182659=CARTESIAN_POINT ( 'NONE',  ( 5.238451434589118882, 1.072694688086765158, -1.459716015685054602 ) ) ;
#182660=CARTESIAN_POINT ( 'NONE',  ( 5.770691199759951040, -0.2880491948782157308, -1.893834403066462446 ) ) ;
#182662=CARTESIAN_POINT ( 'NONE',  ( 4.592568387165754551, -0.4099775813008778025, -1.825014511474598589 ) ) ;
#182663=CARTESIAN_POINT ( 'NONE',  ( 5.371493315669001234, -0.2729949515532895110, 1.840801060123838706 ) ) ;
#182665=CARTESIAN_POINT ( 'NONE',  ( 5.910986595158141732, 1.562736066445655769, 0.8308124446602130897 ) ) ;
#182666=CARTESIAN_POINT ( 'NONE',  ( 0.2511858651975951151, 0.1928294586405615574, -2.007256720055437871 ) ) ;
#182668=CARTESIAN_POINT ( 'NONE',  ( 1.383574010005955701, 1.945322680536746063, -0.8074913105669545565 ) ) ;
#182673=CARTESIAN_POINT ( 'NONE',  ( 2.127218876063118103, 1.806125448131710387, 0.9042179360667053079 ) ) ;
#182676=CARTESIAN_POINT ( 'NONE',  ( 6.620655732516648406, 2.482285041548700111, 2.111775279032622521 ) ) ;
#182679=CARTESIAN_POINT ( 'NONE',  ( 2.144033130777025065, 0.8294244109963678779, -1.996327601563187670 ) ) ;
#182688=CARTESIAN_POINT ( 'NONE',  ( 0.5740950506661415265, -1.212703583203307511, 1.825263377225619266 ) ) ;
#182690=CARTESIAN_POINT ( 'NONE',  ( 1.464152659907109966, 2.228779883755461100, -0.3883945716754066968 ) ) ;
#182697=CARTESIAN_POINT ( 'NONE',  ( 3.250976011129117715, -1.444759545231928843, -1.021753751062564497 ) ) ;
#182700=CARTESIAN_POINT ( 'NONE',  ( 0.1125219251090440048, -0.9011682483198739657, -1.901734387108368063 ) ) ;
#182704=CARTESIAN_POINT ( 'NONE',  ( 5.483999976877721672, -2.016598147233912730, 0.002826481282774962345 ) ) ;
#182705=CARTESIAN_POINT ( 'NONE',  ( 4.798965708296219823, -0.2289270959113845205, -1.797013726050479709 ) ) ;
#182707=CARTESIAN_POINT ( 'NONE',  ( 2.606148294764852213, -0.7140300644919925777, -1.729217693616967644 ) ) ;
#182708=CARTESIAN_POINT ( 'NONE',  ( 2.272408084759574454, -0.9721198248324285363, -1.827787434591138238 ) ) ;
#182711=CARTESIAN_POINT ( 'NONE',  ( 2.197387184563174944, 1.746976956643018442, -0.7784620831182070821 ) ) ;
#182716=CARTESIAN_POINT ( 'NONE',  ( 0.5274218815167727170, -0.2782315536139517431, 1.891897276498944347 ) ) ;
#182718=CARTESIAN_POINT ( 'NONE',  ( 1.750371521623844462, -1.952110535733902585, -0.1955497077021361163 ) ) ;
#182721=CARTESIAN_POINT ( 'NONE',  ( 5.168275554957600271, 2.118074532352266282, -0.1063875075708180934 ) ) ;
#182724=CARTESIAN_POINT ( 'NONE',  ( 0.3154175708385241750, -1.835744252435017598, 0.3582649291258357960 ) ) ;
#182726=CARTESIAN_POINT ( 'NONE',  ( 1.564699064445768784, 0.6353654490140858702, 1.910354371721780797 ) ) ;
#182728=CARTESIAN_POINT ( 'NONE',  ( 0.8084048693777341477, 1.257526981011043654, -1.703196666993979536 ) ) ;
#182730=CARTESIAN_POINT ( 'NONE',  ( 2.523957353938070192, 2.030885678308389952, -0.4015143504868187718 ) ) ;
#182734=CARTESIAN_POINT ( 'NONE',  ( 6.193323979940683621, -0.7056316722037699884, 1.968093674265839477 ) ) ;
#182736=CARTESIAN_POINT ( 'NONE',  ( 4.770415466175468744, -1.191763575130764696, 1.382976834283907053 ) ) ;
#182737=CARTESIAN_POINT ( 'NONE',  ( 2.930093016812723050, -0.8946826049299866357, -1.575034454935933859 ) ) ;
#182741=CARTESIAN_POINT ( 'NONE',  ( 6.890000000000050306, -0.002781820520068867264, 1.999840353888074240 ) ) ;
#182743=CARTESIAN_POINT ( 'NONE',  ( 5.719807747550186505, -2.154180246964752410, 0.4782370604126117142 ) ) ;
#182746=CARTESIAN_POINT ( 'NONE',  ( 4.037688526304391345, -1.829018870347882242, 0.5580751363460645376 ) ) ;
#182753=CARTESIAN_POINT ( 'NONE',  ( -0.02423404108400224397, -1.785672699080865566, -0.4486397487279416563 ) ) ;
#182756=CARTESIAN_POINT ( 'NONE',  ( 3.690566713891149320, -0.3619836066245524786, -1.835009008997898539 ) ) ;
#182761=CARTESIAN_POINT ( 'NONE',  ( 6.860220180191213935, -2.069926439015772335, 0.04462916171246725239 ) ) ;
#182763=CARTESIAN_POINT ( 'NONE',  ( 2.214470461757975794, 1.956567829827577931, 0.4871813834786202224 ) ) ;
#182767=CARTESIAN_POINT ( 'NONE',  ( 2.396645607016957502, 1.759237466006560391, -1.306522788049699679 ) ) ;
#182768=CARTESIAN_POINT ( 'NONE',  ( 6.621730190220365131, -1.769489810573118049, 0.4491385735008179836 ) ) ;
#182776=CARTESIAN_POINT ( 'NONE',  ( 4.159580895514263688, 0.8717668643758098579, 1.621812032879976329 ) ) ;
#182777=CARTESIAN_POINT ( 'NONE',  ( 0.6451818603588607148, 0.1503996631540445994, 2.007543313942860674 ) ) ;
#182778=CARTESIAN_POINT ( 'NONE',  ( 2.689158180196444814, -1.321807234245642615, -1.880123443969876629 ) ) ;
#182780=CARTESIAN_POINT ( 'NONE',  ( 1.428301029171385794, -1.185968821734217027, 1.434052760600286858 ) ) ;
#182784=CARTESIAN_POINT ( 'NONE',  ( 4.869353489999923568, -1.618680692612521455, -1.018082601613921723 ) ) ;
#182788=CARTESIAN_POINT ( 'NONE',  ( 3.685174051874222201, 1.515783366363635531, 1.440268600269165589 ) ) ;
#182789=CARTESIAN_POINT ( 'NONE',  ( 2.061206331123175861, 0.3224310286589862629, -1.842498087946140561 ) ) ;
#182792=CARTESIAN_POINT ( 'NONE',  ( 5.530750200611445067, -1.661959182355336795, 0.7928504710919548337 ) ) ;
#182796=CARTESIAN_POINT ( 'NONE',  ( 4.283650633623343751, 1.129305773815322711, 1.303882612223838500 ) ) ;
#182798=CARTESIAN_POINT ( 'NONE',  ( 0.2286474287733000488, 1.729290747967014097, 0.1301698663358965002 ) ) ;
#182800=CARTESIAN_POINT ( 'NONE',  ( 6.983263157960365675, 2.037486384657179350, 2.358487060789053569 ) ) ;
#182803=CARTESIAN_POINT ( 'NONE',  ( 4.627881963378519536, 2.107464937132212501, -0.5213077441503320975 ) ) ;
#182804=CARTESIAN_POINT ( 'NONE',  ( 3.633261591126951018, -1.686358373764598406, 0.7000054678709469735 ) ) ;
#182805=CARTESIAN_POINT ( 'NONE',  ( 1.481223165768187133, -0.05357505548480785695, 1.961209554040027170 ) ) ;
#182806=CARTESIAN_POINT ( 'NONE',  ( 6.087133394233009476, 1.761630753581880704, 1.174362570269470218 ) ) ;
#182808=CARTESIAN_POINT ( 'NONE',  ( 5.548434679399758984, -1.809038938731177160, 1.407827746306972827 ) ) ;
#182812=CARTESIAN_POINT ( 'NONE',  ( 1.436355765274465623, -1.180822252328097344, -1.761085815303937929 ) ) ;
#182817=CARTESIAN_POINT ( 'NONE',  ( 6.455955546751245500, -0.7393474466994474081, 2.041418194955111787 ) ) ;
#182818=CARTESIAN_POINT ( 'NONE',  ( 6.983263157960331036, 2.967600560354208383, 2.406739638166929041 ) ) ;
#182820=CARTESIAN_POINT ( 'NONE',  ( 1.629831963231648029, -0.2677717415913836718, 2.205032603725831652 ) ) ;
#182822=CARTESIAN_POINT ( 'NONE',  ( 6.012342310302175363, -1.897698807000438359, 0.6819931642896917001 ) ) ;
#182824=CARTESIAN_POINT ( 'NONE',  ( 4.258677893805890236, -0.6421077783588696741, -1.960174235369451123 ) ) ;
#182830=CARTESIAN_POINT ( 'NONE',  ( 0.005962723626575306898, -0.8962717426808585186, -1.887145544106306083 ) ) ;
#182831=CARTESIAN_POINT ( 'NONE',  ( 4.184220324914634581, 1.621181886760931778, 1.198861198883696799 ) ) ;
#182832=CARTESIAN_POINT ( 'NONE',  ( 3.948646536499214932, -1.533023199436277961, -1.019512891124202403 ) ) ;
#182835=CARTESIAN_POINT ( 'NONE',  ( 1.975234724782324980, 1.651647476387863467, -0.4968862749653804589 ) ) ;
#182836=CARTESIAN_POINT ( 'NONE',  ( -0.2058462039469660110, -0.8663896114125648751, -1.819200108291472606 ) ) ;
#182837=CARTESIAN_POINT ( 'NONE',  ( 1.653414166010831243, 1.186659091926351106, 1.968620417403597944 ) ) ;
#182839=CARTESIAN_POINT ( 'NONE',  ( 0.9665587677401198397, 1.115807381107810192, 1.968008997871427468 ) ) ;
#182840=CARTESIAN_POINT ( 'NONE',  ( 3.018300108557407935, -1.038308444602775271, -1.832253800920932596 ) ) ;
#182844=CARTESIAN_POINT ( 'NONE',  ( 6.437500000220395258, 1.451031294483499545, -1.451031289061371021 ) ) ;
#182848=CARTESIAN_POINT ( 'NONE',  ( 4.605860659110106781, 1.647066397540638993, 1.490795591097130002 ) ) ;
#182849=CARTESIAN_POINT ( 'NONE',  ( 3.099763004921416876, -2.188912590334081809, 0.1079765428157742069 ) ) ;
#182856=CARTESIAN_POINT ( 'NONE',  ( 5.344028447597857223, -1.346983732444573256, -1.637812552581649594 ) ) ;
#182866=CARTESIAN_POINT ( 'NONE',  ( 1.663200723894017852, 0.8946008992836312901, 1.492777717291964512 ) ) ;
#182871=CARTESIAN_POINT ( 'NONE',  ( 5.454052192070485638, 2.159419290912270029, -0.1019294599445344784 ) ) ;
#182874=CARTESIAN_POINT ( 'NONE',  ( 4.698204674003193304, -2.161138953124014161, -0.05634304724232848394 ) ) ;
#182877=CARTESIAN_POINT ( 'NONE',  ( 6.186792457355818620, -0.2869052490914354991, -1.950236548312431317 ) ) ;
#182878=CARTESIAN_POINT ( 'NONE',  ( 4.762897148713774342, -1.733524727309469382, -0.04171941676067019572 ) ) ;
#182880=CARTESIAN_POINT ( 'NONE',  ( 1.804482060849887270, 1.621174160030929068, -1.474864209862189579 ) ) ;
#182881=CARTESIAN_POINT ( 'NONE',  ( 2.063905019644726835, 0.3937302209732340685, -2.273608288252434662 ) ) ;
#182882=CARTESIAN_POINT ( 'NONE',  ( 4.833308404897187494, -1.885807738700072678, 0.8313965460460555068 ) ) ;
#182883=CARTESIAN_POINT ( 'NONE',  ( 0.4451279286748652808, 0.6098585162058448583, -1.843775557458992687 ) ) ;
#182887=CARTESIAN_POINT ( 'NONE',  ( 3.375340920106313813, -1.871962376360849056, -0.9962781187466958066 ) ) ;
#182889=CARTESIAN_POINT ( 'NONE',  ( 1.195935645703485539, 1.779627574718087635, 0.9480385367472210500 ) ) ;
#182891=CARTESIAN_POINT ( 'NONE',  ( 4.331241739176756589, 0.1049304944579672605, 2.204394592675275710 ) ) ;
#182893=CARTESIAN_POINT ( 'NONE',  ( 1.621681814730125515, 1.834508062647151272, -0.3115270159769789604 ) ) ;
#182895=CARTESIAN_POINT ( 'NONE',  ( -0.1288028175206907822, 6.946859453142047336, -2.869069570226709498 ) ) ;
#182899=CARTESIAN_POINT ( 'NONE',  ( 6.925078400183545035, 2.404074903924419804, 2.624186486869657831 ) ) ;
#182901=CARTESIAN_POINT ( 'NONE',  ( 3.766525121192493941, -1.385455288492474235, 1.525868174829993373 ) ) ;
#182904=CARTESIAN_POINT ( 'NONE',  ( 2.438154291397228501, -1.164718066671111885, -1.649793688766809430 ) ) ;
#182908=CARTESIAN_POINT ( 'NONE',  ( 1.709912189389639403, -2.045452440186873666, 0.2511061956092154324 ) ) ;
#182912=CARTESIAN_POINT ( 'NONE',  ( -0.1409997244346088141, 4.088373444016307978, -2.555100908668860082 ) ) ;
#182914=CARTESIAN_POINT ( 'NONE',  ( 1.060217833243476182, -1.663605802054025418, -0.7890760572396152694 ) ) ;
#182915=CARTESIAN_POINT ( 'NONE',  ( 5.285833163787800437, 1.479997892162682849, 1.637210856327932618 ) ) ;
#182917=CARTESIAN_POINT ( 'NONE',  ( 1.388190569347878212, -0.9732202972718406730, 1.930209198840258100 ) ) ;
#182920=CARTESIAN_POINT ( 'NONE',  ( 2.132046339962359038, 2.016188815772378629, 0.04465230659478347519 ) ) ;
#182924=CARTESIAN_POINT ( 'NONE',  ( 4.452002833372045387, 1.971050344634683427, -0.04741254548742446229 ) ) ;
#182925=CARTESIAN_POINT ( 'NONE',  ( 3.872279980006509970, -1.995268062538615883, -0.2910826752766728642 ) ) ;
#182929=CARTESIAN_POINT ( 'NONE',  ( 5.777981411418616098, 1.253425007971820326, 1.692306578934036798 ) ) ;
#182930=CARTESIAN_POINT ( 'NONE',  ( 5.881320641815353412, -0.05461762546566179682, 2.069818975884097689 ) ) ;
#182933=CARTESIAN_POINT ( 'NONE',  ( 6.539320575229278454, 2.035006821797652687, 2.408631514295301645 ) ) ;
#182934=CARTESIAN_POINT ( 'NONE',  ( 5.062762828692743966, 0.5904309321736100902, 1.931528952932992427 ) ) ;
#182936=CARTESIAN_POINT ( 'NONE',  ( 1.340767248851399307, -2.011434839998844204, -0.4557168523060088905 ) ) ;
#182944=CARTESIAN_POINT ( 'NONE',  ( 2.858077868800662724, -0.6831540018236246237, 2.060947818793914532 ) ) ;
#182947=CARTESIAN_POINT ( 'NONE',  ( 3.052128622409277181, -1.392423357299840792, 1.204796875372941667 ) ) ;
#182948=EDGE_CURVE ( 'NONE', #40760, #43199, #136177, .T. ) ;
#182950=CARTESIAN_POINT ( 'NONE',  ( 4.282901435897610298, 1.957309562236182021, -0.9860176978964061423 ) ) ;
#182952=CARTESIAN_POINT ( 'NONE',  ( 4.381858629716777642, 1.474804143916402355, 1.715883708886431158 ) ) ;
#182958=CARTESIAN_POINT ( 'NONE',  ( 0.2152203129428611750, -1.737008003653650157, 0.3383841826808623443 ) ) ;
#182959=CARTESIAN_POINT ( 'NONE',  ( 3.985024600404694972, -1.879186454625543901, -0.7224040237710227519 ) ) ;
#182961=CARTESIAN_POINT ( 'NONE',  ( 3.241344266390119078, -1.858123463236575290, 0.9911517508872002002 ) ) ;
#182962=CARTESIAN_POINT ( 'NONE',  ( 0.9486861286592045417, -1.732399544687371229, -0.8177760133930843667 ) ) ;
#182965=CARTESIAN_POINT ( 'NONE',  ( 1.890998328602263800, 0.1897877418215961898, 1.960365536012158127 ) ) ;
#182966=CARTESIAN_POINT ( 'NONE',  ( 0.8131078318618142342, -0.2785150557334699073, 1.849687307983488571 ) ) ;
#182967=CARTESIAN_POINT ( 'NONE',  ( 0.5023040531197673353, 1.956348610274569744, 0.1481081594910879096 ) ) ;
#182968=CARTESIAN_POINT ( 'NONE',  ( 6.533470331352867255, -0.1283082721124771952, 1.781802213622991404 ) ) ;
#182972=CARTESIAN_POINT ( 'NONE',  ( 6.139502064137229986, -1.356240498024411600, -1.288626068300227523 ) ) ;
#182975=CARTESIAN_POINT ( 'NONE',  ( 6.807487347360918761, -1.659057770219806160, -1.238116672595261480 ) ) ;
#182986=CARTESIAN_POINT ( 'NONE',  ( 5.723093114104088386, -1.772945450647535948, -0.8403097561825512152 ) ) ;
#182988=CARTESIAN_POINT ( 'NONE',  ( 3.005232341680406094, 2.000550758621592706, 0.2495690156183311137 ) ) ;
#182989=CARTESIAN_POINT ( 'NONE',  ( 3.889770295363860431, -1.910208526776317806, 0.1464741861031873538 ) ) ;
#182991=CARTESIAN_POINT ( 'NONE',  ( 1.013517375116283592, -2.137022957946862700, 0.4851717564131745597 ) ) ;
#182992=CARTESIAN_POINT ( 'NONE',  ( 0.1331715793776574175, 0.2412765091673596263, -1.987739918565622821 ) ) ;
#182993=CARTESIAN_POINT ( 'NONE',  ( 2.829206387438303327, -1.746784236434804072, 0.6695917499066756928 ) ) ;
#182997=CARTESIAN_POINT ( 'NONE',  ( 5.027025340701954725, -1.815278874653761809, 1.089499710131608401 ) ) ;
#182999=CARTESIAN_POINT ( 'NONE',  ( 5.705552448923417508, -1.629793913574303588, -1.276656259598766940 ) ) ;
#183000=CARTESIAN_POINT ( 'NONE',  ( 2.542619699696859303, -1.736688010486141520, 1.163783427146478200 ) ) ;
#183002=CARTESIAN_POINT ( 'NONE',  ( 1.236830563851202491, -1.561790747969876714, 0.7321873917187391445 ) ) ;
#183012=CARTESIAN_POINT ( 'NONE',  ( 0.4865836442241474602, -1.705128007267729506, -0.6119416708995157883 ) ) ;
#183017=CARTESIAN_POINT ( 'NONE',  ( 6.639320575229254118, 2.070803455257670844, 2.204946390281757207 ) ) ;
#183022=CARTESIAN_POINT ( 'NONE',  ( 2.892830138475974255, 0.2247066616481566970, 1.847348555264594960 ) ) ;
#183023=AXIS2_PLACEMENT_3D ( 'NONE', #4705, #187752, #39381 ) ;
#183024=CARTESIAN_POINT ( 'NONE',  ( 0.5443723441289443077, -1.386745921179835417, 1.321778134454040687 ) ) ;
#183025=CARTESIAN_POINT ( 'NONE',  ( 0.5750489506927083383, -1.533040007955801753, 1.465245631482834821 ) ) ;
#183026=CARTESIAN_POINT ( 'NONE',  ( 0.07680821025393774759, 7.629137130509076492, -2.410791881123967251 ) ) ;
#183027=CARTESIAN_POINT ( 'NONE',  ( -0.1399997263889663501, 0.2375346743129815030, -2.034463206964792548 ) ) ;
#183031=CARTESIAN_POINT ( 'NONE',  ( 5.067230186376567858, 1.711625542863755012, 0.9741009975822639833 ) ) ;
#183032=CARTESIAN_POINT ( 'NONE',  ( 1.049659257133638945, -1.915429643647760249, 0.9100379840868354497 ) ) ;
#183036=CARTESIAN_POINT ( 'NONE',  ( 5.437503290160631941, 0.8905978969957989433, -2.002497223260243153 ) ) ;
#183038=CARTESIAN_POINT ( 'NONE',  ( 4.190394698586521471, -1.905300493120251515, -0.2835615876582204820 ) ) ;
#183040=CARTESIAN_POINT ( 'NONE',  ( 0.4283665542385572955, 1.745377284433462295, 0.5351633580037706839 ) ) ;
#183041=CARTESIAN_POINT ( 'NONE',  ( 1.084930333755677045, -2.153824616689365978, -0.4803136671489223741 ) ) ;
#183046=CARTESIAN_POINT ( 'NONE',  ( 6.385607329849364078, -1.855618941174362879, 0.6602924305801564087 ) ) ;
#183047=CARTESIAN_POINT ( 'NONE',  ( 0.8197486350577835035, 1.155594189952107609, -1.560708653158059622 ) ) ;
#183048=CARTESIAN_POINT ( 'NONE',  ( 0.2630457479233569984, -2.015603748724136945, -0.05229424383911692592 ) ) ;
#183050=CARTESIAN_POINT ( 'NONE',  ( 4.662867571641106323, 1.440366211568647303, -1.178370841985799888 ) ) ;
#183055=CARTESIAN_POINT ( 'NONE',  ( 6.720655732516647163, 0.005566325962592238996, 1.826293863978686982 ) ) ;
#183056=CARTESIAN_POINT ( 'NONE',  ( 0.2752733618501881363, 2.042644424557562122, -0.7945232813236638991 ) ) ;
#183061=CARTESIAN_POINT ( 'NONE',  ( 1.752308680507021155, 0.5713779359179693706, 1.734036872924920702 ) ) ;
#183063=CARTESIAN_POINT ( 'NONE',  ( 4.008270194328780178, -1.657810326508919685, 0.5087727743269004899 ) ) ;
#183065=CARTESIAN_POINT ( 'NONE',  ( 6.509000000000010999, 0.007656933339201045172, 1.900274884395843245 ) ) ;
#183067=CARTESIAN_POINT ( 'NONE',  ( 6.721331454403435934, -0.1262074967819451221, 1.796610827203233063 ) ) ;
#183068=CARTESIAN_POINT ( 'NONE',  ( 4.698074428120575519, 0.8425069249109422564, -1.771795133841249203 ) ) ;
#183073=CARTESIAN_POINT ( 'NONE',  ( 4.301511568767760529, 1.893648340000140040, -0.9544086401246790752 ) ) ;
#183077=CARTESIAN_POINT ( 'NONE',  ( 3.045825399726838079, 1.460771095745692527, 1.467265538693182991 ) ) ;
#183081=CARTESIAN_POINT ( 'NONE',  ( 2.971610153692927803, -2.265147269936502727, -0.3905154627303064618 ) ) ;
#183089=CARTESIAN_POINT ( 'NONE',  ( 3.515784362865181478, -0.5505564139345071606, 1.831456330389509501 ) ) ;
#183091=CARTESIAN_POINT ( 'NONE',  ( 4.787984082328099689, -0.8109719804370466578, 1.522229471167990233 ) ) ;
#183092=CARTESIAN_POINT ( 'NONE',  ( 3.046111529846948329, 0.9110102549910354952, 1.799122713138465279 ) ) ;
#183093=CARTESIAN_POINT ( 'NONE',  ( 4.729243902325204196, 2.292384926013335988, 0.1706581203582517303 ) ) ;
#183095=CARTESIAN_POINT ( 'NONE',  ( 0.9442952520863318044, 0.8911936224933308948, -2.019119535841918278 ) ) ;
#183098=CARTESIAN_POINT ( 'NONE',  ( 5.395664931544272847, -0.6364340197690997458, 1.651504472441939875 ) ) ;
#183100=CARTESIAN_POINT ( 'NONE',  ( 2.431904175345489083, 1.079062523900159221, -2.022394142706671616 ) ) ;
#183102=CARTESIAN_POINT ( 'NONE',  ( 0.4975142532120572225, -0.5819891871022980778, -1.640261313346396133 ) ) ;
#183108=CARTESIAN_POINT ( 'NONE',  ( 6.584440175795505112, 1.195396180001909059, -1.690200020538407566 ) ) ;
#183109=CARTESIAN_POINT ( 'NONE',  ( 0.6554828803995507158, 1.942095732595986890, -0.5424746339172461518 ) ) ;
#183112=CARTESIAN_POINT ( 'NONE',  ( 5.215425455482871619, -0.2808245750387359796, 1.905809792320038998 ) ) ;
#183114=CARTESIAN_POINT ( 'NONE',  ( 1.916566064170255324, -2.220770990188126959, 0.06023022952456217466 ) ) ;
#183123=CARTESIAN_POINT ( 'NONE',  ( 4.405614404729386813, -0.7493292006620960732, -1.571029527175720863 ) ) ;
#183124=CARTESIAN_POINT ( 'NONE',  ( 2.629291921057617554, 0.09916324773191761976, -1.959495597191794225 ) ) ;
#183129=CARTESIAN_POINT ( 'NONE',  ( 1.240767406152184282, -2.011986688465472906, -0.4537849334574247107 ) ) ;
#183132=CARTESIAN_POINT ( 'NONE',  ( 0.9544393508495727652, 2.259765469927646375, -0.1136819296270324686 ) ) ;
#183136=CARTESIAN_POINT ( 'NONE',  ( 2.073319367481298858, 1.791407343212477077, -0.5384048943791116537 ) ) ;
#183137=CARTESIAN_POINT ( 'NONE',  ( 1.002125825150332883, -1.692058386710117990, 0.3787823561424672469 ) ) ;
#183138=CARTESIAN_POINT ( 'NONE',  ( 4.950807510372833065, -1.851323926424643274, -1.172527737679923465 ) ) ;
#183139=CARTESIAN_POINT ( 'NONE',  ( 5.227664224568670193, -2.193190438267843323, 0.7177837189984050958 ) ) ;
#183140=CARTESIAN_POINT ( 'NONE',  ( 1.129840139894950246, -1.306895429219852467, -1.593522927358894004 ) ) ;
#183141=CARTESIAN_POINT ( 'NONE',  ( 3.345582828684705134, 1.942124712213384452, -0.0007862604347076693808 ) ) ;
#183144=CARTESIAN_POINT ( 'NONE',  ( 5.887941446147332947, -0.8415115861447747259, 1.670666529855535654 ) ) ;
#183145=CARTESIAN_POINT ( 'NONE',  ( 1.375000000000000888, 2.052068128417951609, -7.865587939079325464E-14 ) ) ;
#183147=CARTESIAN_POINT ( 'NONE',  ( 0.3679294144470013905, -0.4713284034136792644, 1.668465712161566916 ) ) ;
#183150=CARTESIAN_POINT ( 'NONE',  ( 4.676407821165474488, 1.496050514612049742, 1.352155788975975437 ) ) ;
#183154=CARTESIAN_POINT ( 'NONE',  ( 2.279681363911123970, 1.122676072794186908, 1.439608767588994365 ) ) ;
#183163=CARTESIAN_POINT ( 'NONE',  ( 6.358070640981934751, 0.7709996861101749976, -1.866924874111668853 ) ) ;
#183164=CARTESIAN_POINT ( 'NONE',  ( 6.533822986070857652, -2.155494434802426973, 0.5362405526610786177 ) ) ;
#183169=CARTESIAN_POINT ( 'NONE',  ( 5.418845456765190249, 1.903306360667684993, 0.7908678518537788360 ) ) ;
#183170=CARTESIAN_POINT ( 'NONE',  ( 4.887342357109404567, -0.6819942819097267739, -1.897698409216505011 ) ) ;
#183177=CARTESIAN_POINT ( 'NONE',  ( 5.378279760196133630, -0.2985789616767355326, 1.993766414912321316 ) ) ;
#183178=CARTESIAN_POINT ( 'NONE',  ( 4.628748294741646951, -1.682209325509572473, 0.7487199040775437409 ) ) ;
#183179=CARTESIAN_POINT ( 'NONE',  ( -0.02338929933906607611, 7.629137130509112907, -2.310989781590186976 ) ) ;
#183180=CARTESIAN_POINT ( 'NONE',  ( 2.807580367715529324, 1.950013211217585196, 1.233794411958085036 ) ) ;
#183182=CARTESIAN_POINT ( 'NONE',  ( 5.061884429210019576, 2.138887713127162638, -0.3115965683029159883 ) ) ;
#183184=CARTESIAN_POINT ( 'NONE',  ( -0.006442494416806704600, -1.941642170872309281, -0.04679624317607820189 ) ) ;
#183188=CARTESIAN_POINT ( 'NONE',  ( 3.291731440620565330, -0.7593194595177065187, 1.709801165022284408 ) ) ;
#183189=CARTESIAN_POINT ( 'NONE',  ( 1.318461241437279607, -0.6911404020932455650, -1.783297644634279200 ) ) ;
#183192=CARTESIAN_POINT ( 'NONE',  ( 2.420803835572300500, 1.440536793087299205, -1.671967039616916617 ) ) ;
#183197=CARTESIAN_POINT ( 'NONE',  ( 0.2101411907093185261, -0.8379918008738492796, -1.782380744178988285 ) ) ;
#183198=CARTESIAN_POINT ( 'NONE',  ( 6.463506322211490129, 0.4017315814064837953, -2.272322137143814480 ) ) ;
#183199=CARTESIAN_POINT ( 'NONE',  ( 1.258172656280614365, -1.962046632281065461, -0.003472340283867945618 ) ) ;
#183200=CARTESIAN_POINT ( 'NONE',  ( 4.504768599022889397, 0.5450402360923761735, 1.989220403428487938 ) ) ;
#183208=CARTESIAN_POINT ( 'NONE',  ( 6.338351057450786641, -1.166998422550720393, 1.830725944502207048 ) ) ;
#183210=CARTESIAN_POINT ( 'NONE',  ( 6.427308110136687347, -1.208249125052461181, -1.389453836245766016 ) ) ;
#183214=CARTESIAN_POINT ( 'NONE',  ( 1.739302498465819191, -1.351291084634953066, -1.293660915597586003 ) ) ;
#183218=CARTESIAN_POINT ( 'NONE',  ( 1.365713085969634477, 0.5541664655046051324, -1.830235057661818487 ) ) ;
#183219=CARTESIAN_POINT ( 'NONE',  ( 3.502600007508451352, 1.395586194379776712, -1.088321832170894288 ) ) ;
#183220=CARTESIAN_POINT ( 'NONE',  ( 0.6977377480232997975, 1.284608138224270002, 1.416691289136004395 ) ) ;
#183222=CARTESIAN_POINT ( 'NONE',  ( 3.831564657165886789, 0.6421465917123435618, -1.804920456748728474 ) ) ;
#183224=CARTESIAN_POINT ( 'NONE',  ( 5.916450756658795385, 0.7966118609284984498, 1.801439653064011548 ) ) ;
#183225=CARTESIAN_POINT ( 'NONE',  ( 1.459403507577087700, -1.788631592985808538, 1.138920039206146928 ) ) ;
#183227=CARTESIAN_POINT ( 'NONE',  ( 3.836663719693265584, 0.2738035037005565053, 1.850374562403465983 ) ) ;
#183228=CARTESIAN_POINT ( 'NONE',  ( 0.09986456629675066754, -1.825204794925545881, -0.04862044751281074939 ) ) ;
#183229=ORIENTED_EDGE ( 'NONE', *, *, #14569, .T. ) ;
#183230=CARTESIAN_POINT ( 'NONE',  ( 3.791807063958370971, 1.597966631936774684, 1.522356218736670153 ) ) ;
#183235=CARTESIAN_POINT ( 'NONE',  ( 0.8364713509731898089, -1.147405136530167624, 1.713900253247694350 ) ) ;
#183242=CARTESIAN_POINT ( 'NONE',  ( 3.965334771736851671, 1.774175476309115984, 1.066894043611272824 ) ) ;
#183244=CARTESIAN_POINT ( 'NONE',  ( 1.669428131952359839, 0.1607934374257547205, -2.155692497560882437 ) ) ;
#183246=CARTESIAN_POINT ( 'NONE',  ( 1.506516584307997730, -2.010164795747824140, -0.1955670033209846170 ) ) ;
#183251=CARTESIAN_POINT ( 'NONE',  ( 6.819686488043297246, -1.560180513003786462, 1.276622200526676743 ) ) ;
#183252=CARTESIAN_POINT ( 'NONE',  ( 6.473869786608328347, -0.8128310455158479497, 1.733272608194774689 ) ) ;
#183254=CARTESIAN_POINT ( 'NONE',  ( 4.370767597569780172, -0.0006098066561242150270, -2.191739723162715592 ) ) ;
#183256=CARTESIAN_POINT ( 'NONE',  ( 3.216961742616857745, 1.504763323797538410, -1.180078671740567131 ) ) ;
#183260=CARTESIAN_POINT ( 'NONE',  ( 0.8433753223025289847, 0.3905737783656983431, -1.978056610397058712 ) ) ;
#183262=CARTESIAN_POINT ( 'NONE',  ( 0.1172542576415449567, -0.1040641125494116137, 2.290134469065004730 ) ) ;
#183264=CARTESIAN_POINT ( 'NONE',  ( 3.750762392430748271, -1.410035727865316613, 0.9929894849482110430 ) ) ;
#183265=CARTESIAN_POINT ( 'NONE',  ( -0.1399997263889836974, 2.022132088033218533, -2.415689637818136948 ) ) ;
#183268=CARTESIAN_POINT ( 'NONE',  ( 1.732786548908150870, -1.861864252656076912, -0.6185235971247133868 ) ) ;
#183271=CARTESIAN_POINT ( 'NONE',  ( 0.1753634416057741896, 2.865130778691078905, -2.632309609290182095 ) ) ;
#183274=ORIENTED_EDGE ( 'NONE', *, *, #152161, .T. ) ;
#183275=CARTESIAN_POINT ( 'NONE',  ( 3.686021078551263930, 1.009145865423091815, 1.504116352017518476 ) ) ;
#183279=CARTESIAN_POINT ( 'NONE',  ( 5.022017691244989201, -1.802217576119311770, 0.1829344734397136685 ) ) ;
#183284=CARTESIAN_POINT ( 'NONE',  ( 6.004338076955692216, 1.858996105215251493, 0.09048898905416635774 ) ) ;
#183286=CARTESIAN_POINT ( 'NONE',  ( 3.603066768525709396, -0.1374138116273740384, 1.910719597520103896 ) ) ;
#183293=CARTESIAN_POINT ( 'NONE',  ( 0.7960496800812134621, -0.7770375076890515542, 2.017388685454111652 ) ) ;
#183296=CARTESIAN_POINT ( 'NONE',  ( 1.043660158496478196, 0.7440559408637310579, -1.667260813828251642 ) ) ;
#183298=CARTESIAN_POINT ( 'NONE',  ( 3.065264358586119009, 0.2694654384877669395, -1.805464241506696155 ) ) ;
#183299=CARTESIAN_POINT ( 'NONE',  ( 1.634869402278725348, 1.785593253932623803, 0.6852637533772619749 ) ) ;
#183301=CARTESIAN_POINT ( 'NONE',  ( 2.998452255303164726, 1.954363348466476857, 0.2436675063324095225 ) ) ;
#183302=CARTESIAN_POINT ( 'NONE',  ( 5.249535210367334948, 1.939651965044559390, -0.09935550175556999430 ) ) ;
#183305=CARTESIAN_POINT ( 'NONE',  ( 4.306960158517386894, -0.4675538901007176285, -2.068242682749166672 ) ) ;
#183318=CARTESIAN_POINT ( 'NONE',  ( 4.459475772512963232, 0.3974328844052883447, -1.781742007231662983 ) ) ;
#183323=CARTESIAN_POINT ( 'NONE',  ( 5.506679003988666388, 1.415762158562785533, -1.222804595763474333 ) ) ;
#183334=CARTESIAN_POINT ( 'NONE',  ( 1.476322311366547124, -2.107388574805735271, -0.2037450385454323831 ) ) ;
#183337=CARTESIAN_POINT ( 'NONE',  ( 6.491088764554701740, 0.1969099459505334604, 2.060843999385448821 ) ) ;
#183338=CARTESIAN_POINT ( 'NONE',  ( 1.962219809069129184, -1.683971100191889336, -0.7449956418128443891 ) ) ;
#183343=CARTESIAN_POINT ( 'NONE',  ( 1.746416057278064482, 0.7220573502318957670, 2.175635376676859689 ) ) ;
#183349=CARTESIAN_POINT ( 'NONE',  ( 0.1232915322694717181, 1.753566389086946398, 0.9887636377800024245 ) ) ;
#183350=CARTESIAN_POINT ( 'NONE',  ( 0.6198768371072012062, 1.941228818809427104, -0.2821078022595123747 ) ) ;
#183351=CARTESIAN_POINT ( 'NONE',  ( 6.473846665049121540, -0.8576149079453172508, 1.823233050095712349 ) ) ;
#183355=CARTESIAN_POINT ( 'NONE',  ( 4.207035958355084482, -0.3574298538902004885, 2.059684413417623094 ) ) ;
#183356=CARTESIAN_POINT ( 'NONE',  ( 1.850134630017237880, 0.5516246727584225296, 1.681758779177483287 ) ) ;
#183359=CARTESIAN_POINT ( 'NONE',  ( 5.630919443038269634, -2.074398886797897301, 0.9756724061340553700 ) ) ;
#183360=CARTESIAN_POINT ( 'NONE',  ( 3.837644434229481316, 1.732183052659850286, 0.1680905250187741673 ) ) ;
#183364=CARTESIAN_POINT ( 'NONE',  ( 2.793977985172685141, -1.619072854944574313, 0.6208489642184951141 ) ) ;
#183365=CARTESIAN_POINT ( 'NONE',  ( 3.051421578680337809, 1.863438581370242986, -1.114033871086346217 ) ) ;
#183367=CARTESIAN_POINT ( 'NONE',  ( 4.276577519141481432, -0.4465006364167342645, -1.966305148836451577 ) ) ;
#183368=CARTESIAN_POINT ( 'NONE',  ( 1.093750000000000666, -1.895863743164112547, -0.7852924748299294766 ) ) ;
#183370=CARTESIAN_POINT ( 'NONE',  ( 2.274328125206574569, -1.186679513062695257, 1.517402005686524280 ) ) ;
#183372=CARTESIAN_POINT ( 'NONE',  ( 5.150715375432683985, 2.188637957643671417, 0.3792565894785212000 ) ) ;
#183374=CARTESIAN_POINT ( 'NONE',  ( -0.1110810684432622653, 5.724789179085956192, -2.391029204513066553 ) ) ;
#183380=CARTESIAN_POINT ( 'NONE',  ( 6.144970055084349347, -0.2864424343173576082, -1.940704187532462432 ) ) ;
#183383=CARTESIAN_POINT ( 'NONE',  ( 6.925078400183534377, -0.01048729610059369148, 2.244148362790527429 ) ) ;
#183386=CARTESIAN_POINT ( 'NONE',  ( 4.158677964895734824, -0.6440432224011168882, -1.959637643944433849 ) ) ;
#183391=CARTESIAN_POINT ( 'NONE',  ( 6.344977084850584426, -1.580176071495458023, 1.000667393836668362 ) ) ;
#183392=CARTESIAN_POINT ( 'NONE',  ( 4.482897354602959794, -1.733954122632981099, -0.03610910148283198728 ) ) ;
#183393=CARTESIAN_POINT ( 'NONE',  ( 4.722041168748464912, 1.667336974042502584, 0.4991589302964939412 ) ) ;
#183395=CARTESIAN_POINT ( 'NONE',  ( 1.998001414424467104, -2.291734237260790952, 0.06083037064899367297 ) ) ;
#183397=CARTESIAN_POINT ( 'NONE',  ( 5.935123052105460317, -1.514893180500265002, -1.441204661170019108 ) ) ;
#183398=CARTESIAN_POINT ( 'NONE',  ( 6.527294062531273866, -1.270327234845580078, -1.468905576289506909 ) ) ;
#183399=EDGE_CURVE ( 'NONE', #5628, #26543, #119391, .T. ) ;
#183401=CARTESIAN_POINT ( 'NONE',  ( 1.160779977835691312, 1.203355533934968635, 1.617816888933524710 ) ) ;
#183406=CARTESIAN_POINT ( 'NONE',  ( 3.475340844119987782, -1.870931441966826148, -0.9980012987173058070 ) ) ;
#183408=CARTESIAN_POINT ( 'NONE',  ( 6.024025069106937913, -1.018266858664597763, -1.515143308444939274 ) ) ;
#183416=CARTESIAN_POINT ( 'NONE',  ( 3.252217677095782911, 0.9042450522839510230, -1.806111763424333105 ) ) ;
#183417=CARTESIAN_POINT ( 'NONE',  ( 6.756857042228312515, -1.710155547305733492, 1.394389531264042414 ) ) ;
#183419=CARTESIAN_POINT ( 'NONE',  ( 4.293699386915854177, -1.280875055806574236, -1.350249269484518955 ) ) ;
#183429=CARTESIAN_POINT ( 'NONE',  ( 2.055574482508758738, 1.511248224151232167, -0.8496982089122394610 ) ) ;
#183430=CARTESIAN_POINT ( 'NONE',  ( 1.024908375165583863, -1.101351337790077212, -1.347483777630980040 ) ) ;
#183431=CARTESIAN_POINT ( 'NONE',  ( 6.604155123031994812, -2.307348207032692944, 0.04906353339812623282 ) ) ;
#183434=CARTESIAN_POINT ( 'NONE',  ( 0.8958617733694884677, -0.7443198534227279950, 1.921839338364476513 ) ) ;
#183435=CARTESIAN_POINT ( 'NONE',  ( 0.4564073884281876214, 1.492024165150519055, 1.356095248386236074 ) ) ;
#183438=CARTESIAN_POINT ( 'NONE',  ( 6.649288223980674317, -1.503899034092892162, -1.112267350887645945 ) ) ;
#183439=CARTESIAN_POINT ( 'NONE',  ( 4.482611839828003930, -1.244964735940889522, 1.451779576051547282 ) ) ;
#183441=CARTESIAN_POINT ( 'NONE',  ( 6.639307388351803674, -1.973492857608965423, 0.9879489342229507143 ) ) ;
#183446=CARTESIAN_POINT ( 'NONE',  ( 6.445950376775947177, -1.384621037358444662, -1.606076714075025613 ) ) ;
#183447=ORIENTED_EDGE ( 'NONE', *, *, #47479, .F. ) ;
#183448=CARTESIAN_POINT ( 'NONE',  ( 3.171242727813221585, -2.131442559959194849, -0.8847066026466602340 ) ) ;
#183449=CARTESIAN_POINT ( 'NONE',  ( 5.283633159863808437, -1.863482887291990409, 0.6137318589548645953 ) ) ;
#183450=CARTESIAN_POINT ( 'NONE',  ( 0.4792544977638459880, -0.1021076105021078151, 1.959249876678282209 ) ) ;
#183453=CARTESIAN_POINT ( 'NONE',  ( -0.04742653102243841318, -1.377616979729365809, 1.608019283586498371 ) ) ;
#183456=CARTESIAN_POINT ( 'NONE',  ( 3.696278757040452057, 0.9809249153905131857, -1.936940462344426628 ) ) ;
#183458=CARTESIAN_POINT ( 'NONE',  ( 1.283610819548046011, 0.1505422781087061845, -2.115291873224629082 ) ) ;
#183463=CARTESIAN_POINT ( 'NONE',  ( 2.372404410299948196, -1.270453386316850342, 1.622462496149602140 ) ) ;
#183467=CARTESIAN_POINT ( 'NONE',  ( 0.07755575628183573877, 5.720052600789671260, -2.782970829007725744 ) ) ;
#183470=CARTESIAN_POINT ( 'NONE',  ( 4.775979982822478931, 1.890921987351320777, -0.2842533987747336566 ) ) ;
#183472=CARTESIAN_POINT ( 'NONE',  ( 1.933286576697599513, 0.2207578219815004572, 2.251582216785783075 ) ) ;
#183474=CARTESIAN_POINT ( 'NONE',  ( 1.494102799026775008, -0.9672467274632718937, 1.531528279607297094 ) ) ;
#183475=CARTESIAN_POINT ( 'NONE',  ( 1.006889752881213296, -0.04349654304135543159, 1.915380135637449799 ) ) ;
#183476=CARTESIAN_POINT ( 'NONE',  ( 2.348173244826061268, -0.8873571809006628452, 1.870714752860686447 ) ) ;
#183478=CARTESIAN_POINT ( 'NONE',  ( 0.1101414390347132816, -0.8398613168552993002, -1.781629259513841657 ) ) ;
#183479=CARTESIAN_POINT ( 'NONE',  ( 5.654890666209754002, -1.517393486936137403, 1.186882646050735346 ) ) ;
#183480=CARTESIAN_POINT ( 'NONE',  ( 0.4171991508139940574, 1.586773611656131289, -1.675818712001175381 ) ) ;
#183483=CARTESIAN_POINT ( 'NONE',  ( 4.721170020219593866, -1.840989660556498597, -0.9304453918272929114 ) ) ;
#183488=CARTESIAN_POINT ( 'NONE',  ( 5.385806172021708527, 1.412131043145675280, 1.562536384088798691 ) ) ;
#183490=CARTESIAN_POINT ( 'NONE',  ( 0.5905675304203241716, 1.115885162268255293, -1.862360684160404123 ) ) ;
#183492=CARTESIAN_POINT ( 'NONE',  ( 5.413408226029433834, -0.3230527293765028118, 2.137217106551466905 ) ) ;
#183493=CARTESIAN_POINT ( 'NONE',  ( 4.863928438619278261, 0.6316314618598058983, -1.918449035972718431 ) ) ;
#183501=CARTESIAN_POINT ( 'NONE',  ( 3.907435596788138010, -1.928258004016227378, 0.5899861904685861358 ) ) ;
#183505=CARTESIAN_POINT ( 'NONE',  ( 4.592742373648754040, -0.4705147408641910944, -2.109722102427157964 ) ) ;
#183509=CARTESIAN_POINT ( 'NONE',  ( 6.046499952770106212, -1.423952032562772807, 1.427948417171531759 ) ) ;
#183511=CARTESIAN_POINT ( 'NONE',  ( 0.4336905314940731060, 0.8911838752851186651, -1.476660275499335873 ) ) ;
#183517=CARTESIAN_POINT ( 'NONE',  ( 5.466025653875023593, 0.9211120992074215419, 1.627924866423650530 ) ) ;
#183518=CARTESIAN_POINT ( 'NONE',  ( 6.451439527836500432, -1.796305863176387518, 0.9092463195026576628 ) ) ;
#183523=CARTESIAN_POINT ( 'NONE',  ( 2.596466591541984226, -1.087938976695131066, 1.819974527870950265 ) ) ;
#183524=CARTESIAN_POINT ( 'NONE',  ( 1.335564786618839817, 0.5826355126458090394, -1.930425043884367087 ) ) ;
#183525=CARTESIAN_POINT ( 'NONE',  ( 1.283166710957379220, 0.1313358247177751625, -1.806845861898898953 ) ) ;
#183527=CARTESIAN_POINT ( 'NONE',  ( 6.684453901184132185, -2.118919246787358102, -0.4271090584619871566 ) ) ;
#183532=CARTESIAN_POINT ( 'NONE',  ( 0.7432033230480495911, 0.3705163548812146490, -1.879356322977752347 ) ) ;
#183539=CARTESIAN_POINT ( 'NONE',  ( 4.241217004700631676, -1.882188537963986219, 1.063020064016991117 ) ) ;
#183542=CARTESIAN_POINT ( 'NONE',  ( 1.494549364340029163, -1.129948290531690658, 1.794289463044356436 ) ) ;
#183544=CARTESIAN_POINT ( 'NONE',  ( 1.651575284419577461, 0.5759676520707255332, -1.885319811257283096 ) ) ;
#183545=CARTESIAN_POINT ( 'NONE',  ( 5.115449499555525747, 1.566912803841558732, 1.096118974231160781 ) ) ;
#183548=CARTESIAN_POINT ( 'NONE',  ( 6.426221551499647688, 1.011104814135417751, 1.690039303870519705 ) ) ;
#183549=CARTESIAN_POINT ( 'NONE',  ( 1.429522090333503304, 0.9575595492820774268, -1.689375863068052430 ) ) ;
#183557=CARTESIAN_POINT ( 'NONE',  ( 6.076807558263135789, -1.348954070496380941, 1.355674883165632227 ) ) ;
#183559=CARTESIAN_POINT ( 'NONE',  ( 3.721466898765386500, -0.1629207441977159609, 2.200919931280575170 ) ) ;
#183560=CARTESIAN_POINT ( 'NONE',  ( 1.694636308673210801, -2.196210861363355082, -0.2157497520150277182 ) ) ;
#183563=CARTESIAN_POINT ( 'NONE',  ( 0.2934254677693093338, 1.784247535656303230, -0.6883866973072181317 ) ) ;
#183566=CARTESIAN_POINT ( 'NONE',  ( 3.279797552538410876, -1.996039814156633785, 0.5495672325947635883 ) ) ;
#183570=CARTESIAN_POINT ( 'NONE',  ( 1.622176833581047806, -1.201014165160016356, -1.797165035535647659 ) ) ;
#183571=CARTESIAN_POINT ( 'NONE',  ( 3.896163805485418852, -0.6886730243073329039, -2.080591098665984795 ) ) ;
#183577=CARTESIAN_POINT ( 'NONE',  ( 6.240799290569317925, 1.728800370330787928, -0.1372766232172056844 ) ) ;
#183579=CARTESIAN_POINT ( 'NONE',  ( 3.836834752522141567, -1.993853832596056197, -0.5568897355931883286 ) ) ;
#183580=CARTESIAN_POINT ( 'NONE',  ( 4.657876698301413043, 1.220176935102987636, 1.730081886799080593 ) ) ;
#183583=CARTESIAN_POINT ( 'NONE',  ( 3.291813281336749331, -1.319317765291039946, -1.462433841519056532 ) ) ;
#183584=CARTESIAN_POINT ( 'NONE',  ( 0.3867804997886997720, -1.801505969789623629, -0.6421655129100201087 ) ) ;
#183585=CARTESIAN_POINT ( 'NONE',  ( 5.314510991623739855, 2.116275055252315074, 0.8812819573641057502 ) ) ;
#183586=CARTESIAN_POINT ( 'NONE',  ( 2.789462663364688844, 1.291185895303394116, 1.290987730777813702 ) ) ;
#183593=CARTESIAN_POINT ( 'NONE',  ( 3.779544948098710666, 0.2423517821111692006, -1.998478243804775900 ) ) ;
#183594=CARTESIAN_POINT ( 'NONE',  ( 4.575024454672827368, 1.791946274209740952, 0.7988320279663924106 ) ) ;
#183598=CARTESIAN_POINT ( 'NONE',  ( 0.6793770918060678676, 1.407085465964125204, 1.546551842177671166 ) ) ;
#183599=CARTESIAN_POINT ( 'NONE',  ( 5.172599881030584434, -1.667270648082047835, -0.5941068299562983768 ) ) ;
#183601=CARTESIAN_POINT ( 'NONE',  ( 1.904481915951491189, 1.622449043516610123, -1.473309109067892697 ) ) ;
#183602=CARTESIAN_POINT ( 'NONE',  ( 6.685563754570789996, -0.7372397036040450047, 1.575249959525576005 ) ) ;
#183604=CARTESIAN_POINT ( 'NONE',  ( 0.2335667940002320309, 7.629137130509054288, -2.753349444758381281 ) ) ;
#183605=CARTESIAN_POINT ( 'NONE',  ( 0.9962403866136140262, -0.4152203131645367806, -1.674012925115143213 ) ) ;
#183606=CARTESIAN_POINT ( 'NONE',  ( 0.9666848095895408388, 1.880238891319021111, 1.321614243928259880 ) ) ;
#183607=CARTESIAN_POINT ( 'NONE',  ( 0.5565083568685527116, -1.583368386835169783, 1.515454571103365344 ) ) ;
#183609=CARTESIAN_POINT ( 'NONE',  ( 6.626334403847231158, 0.2915952204957816263, -1.708955668912811587 ) ) ;
#183610=CARTESIAN_POINT ( 'NONE',  ( 2.543839704335303153, -1.636039663378138886, -1.481301067789652537 ) ) ;
#183611=CARTESIAN_POINT ( 'NONE',  ( 6.473846665049121540, -0.8576149079453172508, 1.823233050095712349 ) ) ;
#183612=CARTESIAN_POINT ( 'NONE',  ( 0.2862954470153349362, -1.335216113735339105, -1.712835229902017531 ) ) ;
#183614=CARTESIAN_POINT ( 'NONE',  ( 2.360703550434081421, -2.027734997378250359, -0.6095688489828243739 ) ) ;
#183616=CARTESIAN_POINT ( 'NONE',  ( 5.596683124612600757, -0.4680951147424931569, -1.868546797846575513 ) ) ;
#183618=CARTESIAN_POINT ( 'NONE',  ( 1.980407754855911140, -2.249062817636026779, -0.4427264618648701910 ) ) ;
#183622=CARTESIAN_POINT ( 'NONE',  ( 4.723389051577030706, 1.932298245749045629, 1.095468883668549553 ) ) ;
#183630=CARTESIAN_POINT ( 'NONE',  ( 3.270157880292836605, 1.821742160604752137, -0.8647241845514613834 ) ) ;
#183632=CARTESIAN_POINT ( 'NONE',  ( 1.498963261266316183, 0.3983865470186908064, 2.023570823014529729 ) ) ;
#183638=CARTESIAN_POINT ( 'NONE',  ( 4.330150130892728377, 2.148942519667027984, 0.4286813238914553570 ) ) ;
#183639=CARTESIAN_POINT ( 'NONE',  ( 0.8443752267504719411, 0.3905955241953715795, -1.978051186352240309 ) ) ;
#183640=CARTESIAN_POINT ( 'NONE',  ( 1.241482983173985533, 1.839155304979672501, 0.08999620058360720265 ) ) ;
#183641=CARTESIAN_POINT ( 'NONE',  ( 4.757543194620796889, 2.267657608012829673, -0.3350592807548398722 ) ) ;
#183642=CARTESIAN_POINT ( 'NONE',  ( 3.029072736150268952, -1.236975958831527445, -1.363863411116640334 ) ) ;
#183646=CARTESIAN_POINT ( 'NONE',  ( 4.664971680594516279, -1.631047870213175432, -0.8201845326444437978 ) ) ;
#183647=CARTESIAN_POINT ( 'NONE',  ( 5.397111353752316987, -0.9091427841607623295, -1.799923777076550824 ) ) ;
#183649=CARTESIAN_POINT ( 'NONE',  ( 4.961948105735218384, 2.238643107264228327, -0.3270478844536877649 ) ) ;
#183651=CARTESIAN_POINT ( 'NONE',  ( 6.598663424749101836, -0.5579900645847408747, -2.030628608299019700 ) ) ;
#183652=CARTESIAN_POINT ( 'NONE',  ( 3.701679681979888503, -1.565833156357125278, -1.354537944502069102 ) ) ;
#183657=CARTESIAN_POINT ( 'NONE',  ( 1.840333348128117885, 1.905464876828693921, 0.2831333259317326823 ) ) ;
#183660=CARTESIAN_POINT ( 'NONE',  ( 6.754754220498722539, -0.5220956727660872598, -1.898933868174660589 ) ) ;
#183664=CARTESIAN_POINT ( 'NONE',  ( 1.213308285724056690, 1.730450836393576886, -1.225479750871574458 ) ) ;
#183665=CARTESIAN_POINT ( 'NONE',  ( 1.688022500292500228, 2.124017718264622268, -0.6504838024826449239 ) ) ;
#183666=CARTESIAN_POINT ( 'NONE',  ( 3.047987177024631844, 0.7594498649067694673, -1.964434322149722245 ) ) ;
#183670=CARTESIAN_POINT ( 'NONE',  ( 0.3439184179485414439, -0.8825062887024995861, 1.638522830676287789 ) ) ;
#183676=CARTESIAN_POINT ( 'NONE',  ( 1.547299434221154124, 0.2130619955753136618, 2.109896976817266179 ) ) ;
#183679=CARTESIAN_POINT ( 'NONE',  ( 4.299235682465595509, -1.708000122724560477, 0.9650500775852040025 ) ) ;
#183680=CARTESIAN_POINT ( 'NONE',  ( 3.098656953246520906, -0.6260995091542166380, -2.069055637940686143 ) ) ;
#183681=CARTESIAN_POINT ( 'NONE',  ( 1.698526806778306586, 1.531337151408303621, 1.022036240780115346 ) ) ;
#183683=CARTESIAN_POINT ( 'NONE',  ( 0.07755575628181146652, 7.629137130509076492, -2.788902932953696290 ) ) ;
#183684=CARTESIAN_POINT ( 'NONE',  ( 4.118918040174416539, -1.664481161445837687, 0.5081549729096886958 ) ) ;
#183688=CARTESIAN_POINT ( 'NONE',  ( 2.114359756454447847, -1.018641858927371135, -1.906637348776268004 ) ) ;
#183689=CARTESIAN_POINT ( 'NONE',  ( 3.022814370378481552, 2.006652721595225675, -0.1948103792988181704 ) ) ;
#183691=CARTESIAN_POINT ( 'NONE',  ( 0.8487565004985967443, 0.6285140637429244004, 2.068326486519965979 ) ) ;
#183692=CARTESIAN_POINT ( 'NONE',  ( 3.871915168923282913, 1.094167467933440108, 1.639771958457488132 ) ) ;
#183693=CARTESIAN_POINT ( 'NONE',  ( 6.508999999999981689, 4.698440520552249922, 2.462686878797680556 ) ) ;
#183694=CARTESIAN_POINT ( 'NONE',  ( 2.981904208038600679, -1.913756795454506721, -0.3294587723015156011 ) ) ;
#183703=CARTESIAN_POINT ( 'NONE',  ( 0.1302870565101400258, -1.360178740744298675, -1.738515015553928622 ) ) ;
#183705=CARTESIAN_POINT ( 'NONE',  ( 4.610177715184628155, 1.961415711727178213, -0.04403062578262756377 ) ) ;
#183706=CARTESIAN_POINT ( 'NONE',  ( 1.318982659667154334, 0.9913977828604101372, -1.755770081111128977 ) ) ;
#183708=CARTESIAN_POINT ( 'NONE',  ( 3.942653875399897423, -1.566338124119817987, 1.424821879184964946 ) ) ;
#183710=CARTESIAN_POINT ( 'NONE',  ( 0.1745949693968693039, 6.948552162806741705, -2.350360486623141121 ) ) ;
#183712=CARTESIAN_POINT ( 'NONE',  ( 3.275182144284937369, 1.168729223632531733, 1.422615900182722770 ) ) ;
#183716=CARTESIAN_POINT ( 'NONE',  ( 5.748313822965784858, 1.043546352714582071, -1.845953426139717246 ) ) ;
#183719=CARTESIAN_POINT ( 'NONE',  ( 4.938775350723108026, 0.3481798140595788738, 2.030979325763365928 ) ) ;
#183721=CARTESIAN_POINT ( 'NONE',  ( 0.4669691663035968054, 1.616376026143636624, 0.9223025969757200349 ) ) ;
#183722=CARTESIAN_POINT ( 'NONE',  ( 3.052128622409277181, -1.392423357299840792, 1.204796875372941667 ) ) ;
#183728=CARTESIAN_POINT ( 'NONE',  ( 1.823171247573553311, 2.059948494222668014, 0.7922594597074559264 ) ) ;
#183729=CARTESIAN_POINT ( 'NONE',  ( 5.431070396044226811, 0.1588226897794122738, 2.256881284257936215 ) ) ;
#183730=CARTESIAN_POINT ( 'NONE',  ( 3.555875268649951959, 1.124244472066991518, 1.673854899288424347 ) ) ;
#183733=CARTESIAN_POINT ( 'NONE',  ( 4.605596613081209156, 1.347055988495224232, 1.211539923951672648 ) ) ;
#183734=CARTESIAN_POINT ( 'NONE',  ( 4.856599191889834799, -1.806003080954875495, -0.6394761690226327122 ) ) ;
#183736=CARTESIAN_POINT ( 'NONE',  ( 4.047701786889636111, 0.6652045265579300537, -1.855968581334372702 ) ) ;
#183737=CARTESIAN_POINT ( 'NONE',  ( 5.014452206985246185, 1.289541220462528504, -1.355370375751355105 ) ) ;
#183738=CARTESIAN_POINT ( 'NONE',  ( 4.387043322907993925, 0.09000376980121749249, 1.858987348747977331 ) ) ;
#183740=CARTESIAN_POINT ( 'NONE',  ( 0.3566581422463632189, -1.900417414521380133, -0.6748426577906708745 ) ) ;
#183742=CARTESIAN_POINT ( 'NONE',  ( 1.278104297367024467, 1.255928009607910623, 1.690453460462447044 ) ) ;
#183746=CARTESIAN_POINT ( 'NONE',  ( 2.848016566918720294, -1.427295477286108394, -1.568503593382633454 ) ) ;
#183748=CARTESIAN_POINT ( 'NONE',  ( 1.881123716185427286, -1.848401041775033171, -0.8146170886813360879 ) ) ;
#183750=CARTESIAN_POINT ( 'NONE',  ( 6.720655732516647163, 0.005566325962592238996, 1.826293863978686982 ) ) ;
#183753=CARTESIAN_POINT ( 'NONE',  ( 1.722176697685766200, -1.199285583244277253, -1.798187405066300038 ) ) ;
#183754=CARTESIAN_POINT ( 'NONE',  ( 6.890000000000005898, 7.052460701731090076, 2.598152593539102551 ) ) ;
#183762=CARTESIAN_POINT ( 'NONE',  ( 1.488088480104592826, -2.181432686776756391, -0.2102995727721947705 ) ) ;
#183764=CARTESIAN_POINT ( 'NONE',  ( 1.218052960884225433, -2.206959832567402469, 0.4976822367108637013 ) ) ;
#183772=CARTESIAN_POINT ( 'NONE',  ( 4.441862337843591746, 0.7341043403586414717, -1.561010781705338912 ) ) ;
#183774=CARTESIAN_POINT ( 'NONE',  ( 1.809446860903692444, -1.757098282301880365, 0.2103932681993408993 ) ) ;
#183775=CARTESIAN_POINT ( 'NONE',  ( 5.350674426004140116, 0.6359874849255696683, 2.113150234885258438 ) ) ;
#183778=CARTESIAN_POINT ( 'NONE',  ( 5.097279880301520905, -0.2930512725940071506, 1.994873791649566463 ) ) ;
#183781=CARTESIAN_POINT ( 'NONE',  ( 3.115926070338378207, -0.9207206926411042325, -1.628290677324291780 ) ) ;
#183785=CARTESIAN_POINT ( 'NONE',  ( 2.214975196874233720, 1.533708969217022933, -1.142120075431733994 ) ) ;
#183790=CARTESIAN_POINT ( 'NONE',  ( 0.3340484552533556917, -1.024938778295768849, -1.614363347046356978 ) ) ;
#183792=CARTESIAN_POINT ( 'NONE',  ( 1.539427311113782837, 1.813978416018032558, -0.7477436361984082236 ) ) ;
#183793=CARTESIAN_POINT ( 'NONE',  ( 0.1927366488196740335, -1.238295061544148812, -1.591656064170659191 ) ) ;
#183795=CARTESIAN_POINT ( 'NONE',  ( 5.308877466510794285, -0.5174029350529658622, -2.056363676157816123 ) ) ;
#183797=CARTESIAN_POINT ( 'NONE',  ( 0.2978465640060874997, -1.869987984933557890, -0.05268733258671080832 ) ) ;
#183799=CARTESIAN_POINT ( 'NONE',  ( 2.056891478215248981, 0.4451058530966587323, 1.963224067645082949 ) ) ;
#183802=CARTESIAN_POINT ( 'NONE',  ( 0.6677574575255783573, 1.425215384571768551, 1.565850431965072787 ) ) ;
#183804=CARTESIAN_POINT ( 'NONE',  ( 2.980987059868035693, 1.948563265827065960, 0.6999735360200682877 ) ) ;
#183808=CARTESIAN_POINT ( 'NONE',  ( 4.716787809154822320, -0.1028738300157816532, 2.088225860312553195 ) ) ;
#183810=CARTESIAN_POINT ( 'NONE',  ( 3.557459645987316232, 0.4443818804308434789, -1.770531947851671006 ) ) ;
#183811=CARTESIAN_POINT ( 'NONE',  ( 2.226969132303910470, 1.618658205268191930, 0.8133494039403755815 ) ) ;
#183813=CARTESIAN_POINT ( 'NONE',  ( 6.358075476802443227, 2.201304964888863402, -0.1578768562689457922 ) ) ;
#183814=CARTESIAN_POINT ( 'NONE',  ( 6.890000000000008562, 1.260399741928097672, 2.114076522472335462 ) ) ;
#183816=CARTESIAN_POINT ( 'NONE',  ( 5.456176519787153012, 2.204477245749701719, -0.1032804940204190558 ) ) ;
#183819=CARTESIAN_POINT ( 'NONE',  ( 3.545477442914763078, -1.765841875850767906, 0.7343832577718923948 ) ) ;
#183830=CARTESIAN_POINT ( 'NONE',  ( 3.813614929637609841, -1.843318686535613926, 0.3169883347873063695 ) ) ;
#183832=CARTESIAN_POINT ( 'NONE',  ( -0.2409995289980003397, 4.087843961663322645, -2.555282842491034323 ) ) ;
#183836=CARTESIAN_POINT ( 'NONE',  ( 0.3210686601547476093, -1.756690599571947065, -0.8905566435374636658 ) ) ;
#183837=CARTESIAN_POINT ( 'NONE',  ( 2.636342400811112707, 0.6820146075395253638, 1.897692325672148073 ) ) ;
#183840=CARTESIAN_POINT ( 'NONE',  ( 2.484552680892829546, -0.3758780662847274190, -2.158817762932266682 ) ) ;
#183841=CARTESIAN_POINT ( 'NONE',  ( 6.322862864304120478, 1.705426906915354035, 0.6521430802832667295 ) ) ;
#183849=CARTESIAN_POINT ( 'NONE',  ( 3.509164994824386596, -1.813400730843343966, 0.3181347684400454012 ) ) ;
#183850=CARTESIAN_POINT ( 'NONE',  ( 0.7506400166778016692, 1.983664654656223991, 0.3420602577784581655 ) ) ;
#183851=CARTESIAN_POINT ( 'NONE',  ( 3.585630231873372598, 1.460649136416993121, -1.774545834528557409 ) ) ;
#183853=CARTESIAN_POINT ( 'NONE',  ( 0.5318007479364270651, 1.064995724915913433, 1.525891442952797439 ) ) ;
#183856=CARTESIAN_POINT ( 'NONE',  ( 4.588094604188536429, 1.105678411722615051, 1.560157546714964871 ) ) ;
#183860=CARTESIAN_POINT ( 'NONE',  ( 3.896100387133538234, -0.6578992572023834029, -1.984587938432079257 ) ) ;
#183861=CARTESIAN_POINT ( 'NONE',  ( 1.973319494866377699, 1.790917844098998124, -0.5403536831049270406 ) ) ;
#183863=CARTESIAN_POINT ( 'NONE',  ( 3.491524089112467699, -1.738650433694358233, -0.08144215361822156052 ) ) ;
#183867=CARTESIAN_POINT ( 'NONE',  ( 4.178129962880992920, -0.9906059873891288614, 1.411843326160647782 ) ) ;
#183869=CARTESIAN_POINT ( 'NONE',  ( 0.2109833617158912156, 1.658496975328831891, 0.5066527762955413960 ) ) ;
#183870=CARTESIAN_POINT ( 'NONE',  ( 6.235036409211808461, 0.2120174297785166195, 2.196685143856290878 ) ) ;
#183874=CARTESIAN_POINT ( 'NONE',  ( 3.678747780723041760, 1.381198535464265520, -1.675025177318607783 ) ) ;
#183875=CARTESIAN_POINT ( 'NONE',  ( 2.543341688579534576, -1.352695106659363766, -1.226303905950577366 ) ) ;
#183876=CARTESIAN_POINT ( 'NONE',  ( 5.120359440597627376, 2.086519121862129289, 0.3590335527714014763 ) ) ;
#183879=CARTESIAN_POINT ( 'NONE',  ( 5.513300880735551246, -2.237181406077014323, 0.4993042908148867531 ) ) ;
#183882=CARTESIAN_POINT ( 'NONE',  ( 1.840644454891388282, 1.218392294859267144, -1.735325642819862013 ) ) ;
#183889=CARTESIAN_POINT ( 'NONE',  ( 1.102519259163890153, -0.9942956747860592914, 1.986404433118430291 ) ) ;
#183891=CARTESIAN_POINT ( 'NONE',  ( 6.205703963786828758, 1.882472927010571118, 0.7231429968634556227 ) ) ;
#183893=CARTESIAN_POINT ( 'NONE',  ( 3.977431857364383205, -0.1567958407116451236, 2.056696387209145716 ) ) ;
#183895=FACE_OUTER_BOUND ( 'NONE', #214395, .T. ) ;
#183898=ADVANCED_FACE ( 'NONE', ( #37777 ), #43731, .F. ) ;
#183899=CARTESIAN_POINT ( 'NONE',  ( 0.8848510708264365476, 1.842997052242268508, -0.9869714196348714497 ) ) ;
#183900=CARTESIAN_POINT ( 'NONE',  ( 4.992814645674492624, -2.006446365708704160, 0.2004330516618065550 ) ) ;
#183901=CARTESIAN_POINT ( 'NONE',  ( 4.651808992177354440, 0.7092673950449077669, 1.699362209096597187 ) ) ;
#183904=CARTESIAN_POINT ( 'NONE',  ( 1.184105695005283287, -1.681391461502951046, -0.3836232258775870152 ) ) ;
#183905=CARTESIAN_POINT ( 'NONE',  ( -0.2234322562767385167, -0.4468160588090731022, -1.973564571300358228 ) ) ;
#183906=CARTESIAN_POINT ( 'NONE',  ( 0.7745980011552360267, 2.023606461939434720, -1.090472508649400263 ) ) ;
#183908=CARTESIAN_POINT ( 'NONE',  ( 1.704739465036476442, -0.8136145326368517949, -2.111227425349770481 ) ) ;
#183909=CARTESIAN_POINT ( 'NONE',  ( 2.930406704442231725, 1.169546373139153328, -1.751267329298618280 ) ) ;
#183914=CARTESIAN_POINT ( 'NONE',  ( 5.906250000000004441, 1.895863743163945125, -0.7852924748303062863 ) ) ;
#183919=CARTESIAN_POINT ( 'NONE',  ( 5.537407084817251857, -0.05464564937080264306, 2.220880467482534204 ) ) ;
#183920=CARTESIAN_POINT ( 'NONE',  ( 3.855584222106961612, 2.174980185927982923, -0.2676557845137442215 ) ) ;
#183923=CARTESIAN_POINT ( 'NONE',  ( 5.687936657224680559, -1.243353266631580523, -1.517579924814119074 ) ) ;
#183925=CARTESIAN_POINT ( 'NONE',  ( 6.610000000000028741, 4.695285100415147461, 2.562642482393460597 ) ) ;
#183927=CARTESIAN_POINT ( 'NONE',  ( 4.974906307097914926, -1.534222593358970821, 1.464151343314526121 ) ) ;
#183931=CARTESIAN_POINT ( 'NONE',  ( 6.192270064542984898, -2.150811787302907785, -0.2168040374768212541 ) ) ;
#183933=CARTESIAN_POINT ( 'NONE',  ( 5.390138975101268493, -0.4531076923771395482, -1.784498753146485539 ) ) ;
#183935=CARTESIAN_POINT ( 'NONE',  ( 0.6259951400321401849, 0.1256764613348868298, 1.735981902797034238 ) ) ;
#183939=CARTESIAN_POINT ( 'NONE',  ( 5.559502693676295237, 0.4258712887980077300, -2.119171757835013548 ) ) ;
#183944=CARTESIAN_POINT ( 'NONE',  ( 4.469695567000064429, 2.097540297429688838, -0.5223010940857697459 ) ) ;
#183946=CARTESIAN_POINT ( 'NONE',  ( 4.885985806860754010, -0.9320292603649924512, 1.737142539612034353 ) ) ;
#183947=CARTESIAN_POINT ( 'NONE',  ( 4.534371549175888028, 1.681635666518576988, -0.4216726850935527127 ) ) ;
#183948=CARTESIAN_POINT ( 'NONE',  ( 1.505704256594592838, -2.174480876681058827, 0.2726767719730335826 ) ) ;
#183949=CARTESIAN_POINT ( 'NONE',  ( 2.310004868091195540, -0.5052997711322243513, 2.251431844744283151 ) ) ;
#183950=CARTESIAN_POINT ( 'NONE',  ( 5.132131416026131987, 1.062877790662479116, -1.765404227961290484 ) ) ;
#183951=CARTESIAN_POINT ( 'NONE',  ( 6.550339418841141459, -1.498220820903242601, 1.235316290203094081 ) ) ;
#183956=CARTESIAN_POINT ( 'NONE',  ( 1.688125190044654556, 1.678006053171029688, 1.117831401076685660 ) ) ;
#183958=CARTESIAN_POINT ( 'NONE',  ( 2.889901548669851383, 1.559680528474843841, 1.561422205034967314 ) ) ;
#183960=CARTESIAN_POINT ( 'NONE',  ( 1.358004595412452664, -1.861131634099476573, -0.006961619045023344915 ) ) ;
#183961=CARTESIAN_POINT ( 'NONE',  ( -0.1290005225502398323, 0.2247172878383028038, -2.207197350255707402 ) ) ;
#183965=CARTESIAN_POINT ( 'NONE',  ( 6.825078400183579141, 1.241995729952071637, 2.258014901253778461 ) ) ;
#183968=CARTESIAN_POINT ( 'NONE',  ( 3.467699783257427004, 2.010999201309400686, -0.4499753609362132090 ) ) ;
#183971=CARTESIAN_POINT ( 'NONE',  ( 1.875654870896212190, 0.3429857902390308078, -1.990162865174507800 ) ) ;
#183974=AXIS2_PLACEMENT_3D ( 'NONE', #212415, #159421, #194045 ) ;
#183975=CARTESIAN_POINT ( 'NONE',  ( 2.325137485922982084, -0.001238304602014379070, 2.061077815622249343 ) ) ;
#183980=CARTESIAN_POINT ( 'NONE',  ( -0.1408020194050172424, 4.085453189724971956, -2.655103234342595986 ) ) ;
#183981=CARTESIAN_POINT ( 'NONE',  ( 5.127635347277352373, -2.096377701570474539, 0.6897739467496829535 ) ) ;
#183983=CARTESIAN_POINT ( 'NONE',  ( 1.458524589769864210, 0.8745999688587955401, 1.976921506453344080 ) ) ;
#183985=CARTESIAN_POINT ( 'NONE',  ( 1.587125413319636635, 1.679225032509903404, 1.116207499648947943 ) ) ;
#183988=CARTESIAN_POINT ( 'NONE',  ( 2.272138710904994863, -1.152746988206950096, 1.473173409640892162 ) ) ;
#183989=CARTESIAN_POINT ( 'NONE',  ( 4.083220446344194343, 1.622485107653489633, 1.197306254465977826 ) ) ;
#183993=CARTESIAN_POINT ( 'NONE',  ( 5.373694187740483130, 2.029982003570539817, -0.5606972681787207868 ) ) ;
#183997=CARTESIAN_POINT ( 'NONE',  ( 5.133071871609922177, 1.867805937340912159, 0.7691607467245373808 ) ) ;
#183999=CARTESIAN_POINT ( 'NONE',  ( 0.6024794235527919373, 2.056786662827071233, 0.1555941968269194953 ) ) ;
#184007=CARTESIAN_POINT ( 'NONE',  ( 3.490846471615864921, 2.117612208401131735, 0.4786232489656114253 ) ) ;
#184010=CARTESIAN_POINT ( 'NONE',  ( 3.210337823311388394, 1.665856106666419034, 0.7845605768846477535 ) ) ;
#184012=CARTESIAN_POINT ( 'NONE',  ( 4.124703146219878214, 0.1084699374758208573, 2.189010777610411740 ) ) ;
#184013=CARTESIAN_POINT ( 'NONE',  ( 4.663087558633967511, -2.018941045467276929, -1.021363250454855764 ) ) ;
#184018=CARTESIAN_POINT ( 'NONE',  ( 6.081276588353502710, 1.634447734625959825, -0.6791225938206167934 ) ) ;
#184021=CARTESIAN_POINT ( 'NONE',  ( 1.835132634908468452, 0.2055991040930336133, 2.095883127255711464 ) ) ;
#184022=CARTESIAN_POINT ( 'NONE',  ( 1.212342387966048651, 1.846533033048233463, 0.5095510818057205071 ) ) ;
#184026=CARTESIAN_POINT ( 'NONE',  ( 1.996483073472170133, 1.947676829468534265, 0.2919340086137369727 ) ) ;
#184027=CARTESIAN_POINT ( 'NONE',  ( 1.111929834214450796, -0.8377583890188080584, -1.672643128629976772 ) ) ;
#184028=CARTESIAN_POINT ( 'NONE',  ( 0.4847190467827041105, 1.876267867961832980, 0.5731238010058882226 ) ) ;
#184029=CARTESIAN_POINT ( 'NONE',  ( 0.1406777020166137260, 1.830675540527426648, 0.5531436448603862521 ) ) ;
#184034=CARTESIAN_POINT ( 'NONE',  ( 6.385618529757402406, 1.291587659170100766, 1.353439767483602285 ) ) ;
#184036=CARTESIAN_POINT ( 'NONE',  ( 5.963751281166302043, -0.5086355806236466659, 2.006660534352236347 ) ) ;
#184046=CARTESIAN_POINT ( 'NONE',  ( 5.142999638377217408, -0.2383176028181442918, -1.947251298587366231 ) ) ;
#184048=CARTESIAN_POINT ( 'NONE',  ( 3.075545897833771747, 1.462222457232667416, -1.388272539953112839 ) ) ;
#184049=CARTESIAN_POINT ( 'NONE',  ( 2.290125521308879808, -0.7372973962519657753, -1.768360312244516841 ) ) ;
#184052=CARTESIAN_POINT ( 'NONE',  ( 0.3983070667218471805, -0.7439898890007863308, -2.061537379893277677 ) ) ;
#184053=CARTESIAN_POINT ( 'NONE',  ( 0.1333692844072767447, 1.351132181276387678, -2.308013766563504987 ) ) ;
#184054=CARTESIAN_POINT ( 'NONE',  ( 3.075316773429651818, 1.777364689479765003, -0.5833007003755164011 ) ) ;
#184059=CARTESIAN_POINT ( 'NONE',  ( 3.919616530476960126, -1.461442364795034976, -1.532149496301576486 ) ) ;
#184061=CARTESIAN_POINT ( 'NONE',  ( 6.391088794356012848, 0.1989163192229244648, 2.060770550043041993 ) ) ;
#184062=CARTESIAN_POINT ( 'NONE',  ( 1.241864343681793548, 2.088520813897582151, 0.09894013698169208670 ) ) ;
#184063=CARTESIAN_POINT ( 'NONE',  ( 6.620655732516650183, -0.005281389526671976913, 2.273887028200880511 ) ) ;
#184064=CARTESIAN_POINT ( 'NONE',  ( 0.5160737793865723955, 1.194803229551535173, -1.244154219207161960 ) ) ;
#184073=CARTESIAN_POINT ( 'NONE',  ( 0.3986853379376364415, -0.2198743563824180347, -1.798016573952045283 ) ) ;
#184082=ORIENTED_EDGE ( 'NONE', *, *, #85262, .T. ) ;
#184083=CARTESIAN_POINT ( 'NONE',  ( 6.275017575846199236, 1.753023089329442064, -0.9963169848806670004 ) ) ;
#184084=CARTESIAN_POINT ( 'NONE',  ( 0.8738735914427526730, 0.4098651554323496926, -2.080331290949386513 ) ) ;
#184090=CARTESIAN_POINT ( 'NONE',  ( 3.520317136570957128, 0.8812775084000439296, 1.761307543597267822 ) ) ;
#184091=CARTESIAN_POINT ( 'NONE',  ( 1.647299267346370444, 0.2110521635003380359, 2.109970702148834754 ) ) ;
#184095=CARTESIAN_POINT ( 'NONE',  ( 5.666036703420031628, -1.392593631063457682, 1.692088878451535106 ) ) ;
#184097=CARTESIAN_POINT ( 'NONE',  ( 4.313445203237777470, -0.3300861979738233254, 1.897755268844825816 ) ) ;
#184099=CARTESIAN_POINT ( 'NONE',  ( -0.1294898018152304819, 0.2484418290887774605, -1.961697698124951650 ) ) ;
#184100=CARTESIAN_POINT ( 'NONE',  ( 1.225528936851564499, -0.05108506852482053856, 2.206457870188943016 ) ) ;
#184104=CARTESIAN_POINT ( 'NONE',  ( 6.719592862238788378, 0.3399973502477529608, -1.939713583613829728 ) ) ;
#184105=CARTESIAN_POINT ( 'NONE',  ( 0.4681772292557941917, -1.829107974901639899, -0.6530565061142034056 ) ) ;
#184106=CARTESIAN_POINT ( 'NONE',  ( 6.116662973727256869, 0.6756443950356945116, -2.196842021360578823 ) ) ;
#184108=CARTESIAN_POINT ( 'NONE',  ( 4.170637490619288457, 1.318561355513592215, -1.313476238859044409 ) ) ;
#184113=CARTESIAN_POINT ( 'NONE',  ( 6.720655732516650716, 2.984497329163855905, 2.280179935440066252 ) ) ;
#184114=CARTESIAN_POINT ( 'NONE',  ( 6.585487052573138378, -0.8941505307449393314, 1.888277625537030380 ) ) ;
#184120=CARTESIAN_POINT ( 'NONE',  ( 0.6096330727367264002, -1.817201089070449971, 0.1759225495863714350 ) ) ;
#184122=CARTESIAN_POINT ( 'NONE',  ( 2.074501327421875096, -0.7402772072304538709, 1.568325542203717227 ) ) ;
#184125=CARTESIAN_POINT ( 'NONE',  ( 6.322862864304120478, 1.705426906915354035, 0.6521430802832667295 ) ) ;
#184126=CARTESIAN_POINT ( 'NONE',  ( 3.397265449134680981, -1.732261247800225279, 0.9206733083975682241 ) ) ;
#184130=CARTESIAN_POINT ( 'NONE',  ( 4.811248821985151913, 1.762591750878339081, -1.178568461981117643 ) ) ;
#184133=CARTESIAN_POINT ( 'NONE',  ( 2.764580022184208730, -0.7881864689132519475, -1.914544693583389634 ) ) ;
#184134=CARTESIAN_POINT ( 'NONE',  ( 6.827182134110196365, 4.700652535171166768, 2.373648650996477372 ) ) ;
#184136=CARTESIAN_POINT ( 'NONE',  ( 4.881579437514656838, 0.2187098293420664807, -2.210487333941961285 ) ) ;
#184138=CARTESIAN_POINT ( 'NONE',  ( 2.725512391864647999, 2.281683302435618010, 0.2785734649361614745 ) ) ;
#184146=CARTESIAN_POINT ( 'NONE',  ( 4.183787391381143195, 1.853651273288700718, -0.4697857328580385960 ) ) ;
#184148=CARTESIAN_POINT ( 'NONE',  ( 4.418794198169028853, 1.577559062085803765, 0.6976772398503274797 ) ) ;
#184149=CARTESIAN_POINT ( 'NONE',  ( 3.450407915430803385, -1.350735839785843773, 1.497501794165828626 ) ) ;
#184151=CARTESIAN_POINT ( 'NONE',  ( 4.184446765594143081, 1.846410498051667348, 1.369081834291352218 ) ) ;
#184153=CARTESIAN_POINT ( 'NONE',  ( 0.08304785351339466493, -2.141800023564765620, -0.5316218738360134477 ) ) ;
#184156=CARTESIAN_POINT ( 'NONE',  ( 5.167173303313960631, 0.1731176489731758861, -1.761265287352784314 ) ) ;
#184159=CARTESIAN_POINT ( 'NONE',  ( 0.8324521645294904459, 2.259258938120102922, 0.3867697638584958186 ) ) ;
#184160=CARTESIAN_POINT ( 'NONE',  ( 6.456982894382444549, 0.3095715517048603371, -1.814770079682447967 ) ) ;
#184162=CARTESIAN_POINT ( 'NONE',  ( 6.720655732516647163, -0.004400176169771369272, 2.173773060281408931 ) ) ;
#184166=CARTESIAN_POINT ( 'NONE',  ( 0.4499840099862363330, 1.609255455985519445, 1.457649523623653298 ) ) ;
#184167=CARTESIAN_POINT ( 'NONE',  ( 1.446500318503377125, -1.422605717829699801, 1.429450658469958668 ) ) ;
#184170=CARTESIAN_POINT ( 'NONE',  ( 5.795520199677122619, 1.460474902364042649, 1.256451531516086684 ) ) ;
#184172=CARTESIAN_POINT ( 'NONE',  ( 1.020144049103311801, -0.5328101295089396894, 2.156480530197317780 ) ) ;
#184180=CARTESIAN_POINT ( 'NONE',  ( 4.458407330353141518, -1.557363759602323761, -0.7771466779550126880 ) ) ;
#184181=CARTESIAN_POINT ( 'NONE',  ( 2.787496613063783713, -1.831585881375777713, 0.7034878451678548972 ) ) ;
#184185=CARTESIAN_POINT ( 'NONE',  ( 0.9419289695592079070, 1.383825781391546883, 1.529776408950918265 ) ) ;
#184189=CARTESIAN_POINT ( 'NONE',  ( 1.358695222972395422, 0.9186288065576648787, 2.067797507578944760 ) ) ;
#184192=CARTESIAN_POINT ( 'NONE',  ( 2.055717040066493695, 1.865871300129381183, -0.1328275987748789300 ) ) ;
#184193=CARTESIAN_POINT ( 'NONE',  ( 0.9845302160453218709, -1.734343004718540637, -0.001328871039332768294 ) ) ;
#184194=CARTESIAN_POINT ( 'NONE',  ( 5.618738332679400038, -0.05485954975367920983, 2.191026952110195491 ) ) ;
#184195=CARTESIAN_POINT ( 'NONE',  ( 5.315557996638371918, -0.3450676865139382099, 2.281540517825955128 ) ) ;
#184196=CARTESIAN_POINT ( 'NONE',  ( 1.006794875882726314, 1.561001636543899673, -1.345678083183374341 ) ) ;
#184197=CARTESIAN_POINT ( 'NONE',  ( 3.433474178283620670, 0.8725410082476585671, -1.734956227438133158 ) ) ;
#184199=CARTESIAN_POINT ( 'NONE',  ( 5.835183367072669824, -1.691281831231405963, 0.7993005984755219284 ) ) ;
#184201=CARTESIAN_POINT ( 'NONE',  ( 6.661482485103542572, -0.5350097378542042481, -1.943772860543022230 ) ) ;
#184203=CARTESIAN_POINT ( 'NONE',  ( 4.992814645674492624, -2.006446365708704160, 0.2004330516618065550 ) ) ;
#184207=CARTESIAN_POINT ( 'NONE',  ( 1.963248404482214049, 0.3131683437365209710, -1.798463397695612809 ) ) ;
#184216=CARTESIAN_POINT ( 'NONE',  ( 5.180334445267184229, 0.9972254788270168424, 1.756242667785257172 ) ) ;
#184217=CARTESIAN_POINT ( 'NONE',  ( 0.4871770963560326240, -1.998059126451703138, -0.7104936405118513765 ) ) ;
#184221=CARTESIAN_POINT ( 'NONE',  ( 4.768464766973178115, -1.347833537202504317, 1.559116658007191347 ) ) ;
#184222=CARTESIAN_POINT ( 'NONE',  ( 5.080704010962952211, -0.7231418808758652839, 1.882473355234378865 ) ) ;
#184229=CARTESIAN_POINT ( 'NONE',  ( 5.571638683613604037, 1.528505562557905595, -1.314797328242120367 ) ) ;
#184230=CARTESIAN_POINT ( 'NONE',  ( 4.013478867934616723, -0.9481684062532383939, -1.578073411074693899 ) ) ;
#184232=CARTESIAN_POINT ( 'NONE',  ( 1.788135723919834774, 1.593634496655076171, 1.669289477041531633 ) ) ;
#184234=CARTESIAN_POINT ( 'NONE',  ( 4.833375328034618335, -1.978455579520097762, 0.8711445904842631816 ) ) ;
#184236=CARTESIAN_POINT ( 'NONE',  ( 0.5033352851749985923, -1.932590057610440226, 0.1917435184634954937 ) ) ;
#184238=CARTESIAN_POINT ( 'NONE',  ( 3.831692444270826226, -1.546495240224911250, 1.700404426133800939 ) ) ;
#184242=CARTESIAN_POINT ( 'NONE',  ( 3.643291952642300213, -1.415932857957047375, -1.222571138756740838 ) ) ;
#184246=CARTESIAN_POINT ( 'NONE',  ( 1.383733252933561086, 2.037972573443189717, -0.8472329510355591786 ) ) ;
#184251=CARTESIAN_POINT ( 'NONE',  ( 6.819227947992137828, -0.1355634432321853045, 1.940828160714276995 ) ) ;
#184252=CARTESIAN_POINT ( 'NONE',  ( 0.3062966595402705217, -0.6107984557060777142, 2.225206381879496487 ) ) ;
#184253=CARTESIAN_POINT ( 'NONE',  ( 0.9944974185457016169, 1.932217576897478528, 0.3389098420027157332 ) ) ;
#184254=CARTESIAN_POINT ( 'NONE',  ( 4.030177592043080459, 1.141696479982070578, 1.717582018908659025 ) ) ;
#184263=CARTESIAN_POINT ( 'NONE',  ( 6.689883316565048865, -1.412897867115006978, -1.648663827357793155 ) ) ;
#184265=CARTESIAN_POINT ( 'NONE',  ( 5.970224376651540155, -1.750504005202535796, -0.5711807346103907612 ) ) ;
#184268=CARTESIAN_POINT ( 'NONE',  ( 0.8955150854165813135, -0.6789544621725839280, 1.743152336062703256 ) ) ;
#184274=CARTESIAN_POINT ( 'NONE',  ( 1.225099565173026761, 1.686864977381890451, 0.9006792851762451813 ) ) ;
#184275=CARTESIAN_POINT ( 'NONE',  ( 3.484973364136711549, 1.600408865665205571, -0.7559459569618111052 ) ) ;
#184276=CARTESIAN_POINT ( 'NONE',  ( 0.9614044138335111622, -1.507904615609249488, -1.175938229252027956 ) ) ;
#184278=CARTESIAN_POINT ( 'NONE',  ( 4.605048111083247520, -0.08973289204975383460, 1.913620015931324581 ) ) ;
#184280=CARTESIAN_POINT ( 'NONE',  ( 5.037540015474098354, 1.838441386810828693, -0.7070908002782918533 ) ) ;
#184281=CARTESIAN_POINT ( 'NONE',  ( 0.7387272492362946252, 1.258454933865692293, -1.706699550108881080 ) ) ;
#184283=CARTESIAN_POINT ( 'NONE',  ( 3.643291952642300213, -1.415932857957047375, -1.222571138756740838 ) ) ;
#184284=CARTESIAN_POINT ( 'NONE',  ( 5.795441377679017236, 1.310440327830458385, 1.121692192092491380 ) ) ;
#184286=CARTESIAN_POINT ( 'NONE',  ( 3.598431038176507002, -2.204323482753521635, -0.1086902067785888437 ) ) ;
#184290=CARTESIAN_POINT ( 'NONE',  ( 0.3794369086736723018, -0.1030016517138358095, 2.060237976199934984 ) ) ;
#184297=CARTESIAN_POINT ( 'NONE',  ( 3.596198176508007105, 0.9334358170956689182, -1.848091447891623051 ) ) ;
#184299=CARTESIAN_POINT ( 'NONE',  ( 1.985828983967323325, 1.489073237690191398, 1.567133960648489976 ) ) ;
#184301=CARTESIAN_POINT ( 'NONE',  ( 1.137374441040917672, -0.04723908312853628000, 2.019287564836816262 ) ) ;
#184304=CARTESIAN_POINT ( 'NONE',  ( 0.1747926744264452492, 5.725295659261265158, -2.449351454080525681 ) ) ;
#184306=CARTESIAN_POINT ( 'NONE',  ( 6.591172692507557329, 1.163088239368128995, -1.646588791553056152 ) ) ;
#184307=CARTESIAN_POINT ( 'NONE',  ( 6.139839150192680783, 1.910077931696544384, -0.1482136438759658337 ) ) ;
#184308=CARTESIAN_POINT ( 'NONE',  ( 6.639320575229256782, 3.683803431435454190, 2.717262547424610375 ) ) ;
#184309=CARTESIAN_POINT ( 'NONE',  ( 3.597391730528697540, -0.6346259394694170330, 2.097678010650514402 ) ) ;
#184311=CARTESIAN_POINT ( 'NONE',  ( 3.006014587165442453, -0.7710369221427433306, 1.750240277048662030 ) ) ;
#184315=CARTESIAN_POINT ( 'NONE',  ( 1.282827611874960416, 1.646826022920354848, -1.163289555428485667 ) ) ;
#184317=CARTESIAN_POINT ( 'NONE',  ( 0.4688447829373428855, -2.161134926827886549, -0.7649225765839831048 ) ) ;
#184319=CARTESIAN_POINT ( 'NONE',  ( 3.803458131734431813, -0.5007765277059565978, 1.650448229862747196 ) ) ;
#184321=CARTESIAN_POINT ( 'NONE',  ( 0.1394461523057474728, 0.7845381482947767493, -1.808261586923729736 ) ) ;
#184325=CARTESIAN_POINT ( 'NONE',  ( 1.398799877119625501, 0.3793605821263335565, 1.924665094374561791 ) ) ;
#184328=CARTESIAN_POINT ( 'NONE',  ( 0.07536363704235481131, 0.6997989235110781969, -2.226667633679416447 ) ) ;
#184333=CARTESIAN_POINT ( 'NONE',  ( 4.002463340116116264, -1.792309675113772371, -0.2618007260343068743 ) ) ;
#184339=CARTESIAN_POINT ( 'NONE',  ( 5.268131585227527225, 1.809134041791292002, -0.09470131462574123138 ) ) ;
#184343=CARTESIAN_POINT ( 'NONE',  ( 6.285601362909060796, -1.752004058920811902, 0.6281230767469258014 ) ) ;
#184345=CARTESIAN_POINT ( 'NONE',  ( 4.358935675595962955, -0.003970376728411328937, -1.915793142021319007 ) ) ;
#184353=CARTESIAN_POINT ( 'NONE',  ( 1.129994055010040022, -1.371941552271437770, -1.670562328977095445 ) ) ;
#184356=CARTESIAN_POINT ( 'NONE',  ( 0.6393319655835437709, -1.287349573739982933, -1.294668131371433661 ) ) ;
#184358=CARTESIAN_POINT ( 'NONE',  ( 3.715676801689533626, -1.798647723735953496, 0.3114480851732701061 ) ) ;
#184360=CARTESIAN_POINT ( 'NONE',  ( 1.617294888471169312, 1.591762500684265946, 1.059657513450793953 ) ) ;
#184361=CARTESIAN_POINT ( 'NONE',  ( 3.068762047175084717, 1.428394590129605346, -1.356294421569247177 ) ) ;
#184362=CARTESIAN_POINT ( 'NONE',  ( 3.315898775378321339, 1.229719374647167296, -1.503149361444736876 ) ) ;
#184365=CARTESIAN_POINT ( 'NONE',  ( 4.447591161967184625, -1.937652164471121763, 0.8620916771790232414 ) ) ;
#184369=CARTESIAN_POINT ( 'NONE',  ( 0.2331563151865451988, 4.092570554693980789, -2.500672995626152861 ) ) ;
#184374=CARTESIAN_POINT ( 'NONE',  ( 3.686012862905340803, -0.8985999850123352894, 1.589152278004740237 ) ) ;
#184375=CARTESIAN_POINT ( 'NONE',  ( 6.034388706570055660, 0.6371486477873434806, 1.913263546360920220 ) ) ;
#184380=CARTESIAN_POINT ( 'NONE',  ( 4.487079325084206260, 1.670935625628103605, -0.8411387520786617333 ) ) ;
#184382=CARTESIAN_POINT ( 'NONE',  ( 3.352094138168077553, 1.926676517159428670, -0.0006976933946620245131 ) ) ;
#184389=CIRCLE ( 'NONE', #7972, 0.05000000000000057176 ) ;
#184390=CARTESIAN_POINT ( 'NONE',  ( 1.493934562436026292, -2.100767169153750391, 0.2631679424494152153 ) ) ;
#184393=CARTESIAN_POINT ( 'NONE',  ( 6.578973861349465935, 1.929489650308688464, 0.7507879531711419974 ) ) ;
#184394=CARTESIAN_POINT ( 'NONE',  ( 1.382094229771430705, -0.2707140722739818650, -1.821126350552772610 ) ) ;
#184396=CARTESIAN_POINT ( 'NONE',  ( 6.065094409921147900, -1.233312222785312384, 1.939673083280533783 ) ) ;
#184400=CARTESIAN_POINT ( 'NONE',  ( 1.851946410329910808, 2.285883199777267283, -0.1717553002464344836 ) ) ;
#184403=CARTESIAN_POINT ( 'NONE',  ( 5.490160960519338218, -0.4736594950825470107, -1.883182239726274076 ) ) ;
#184407=CARTESIAN_POINT ( 'NONE',  ( 0.3342400628787962624, -1.080556536492575770, -1.698484060877824886 ) ) ;
#184412=CARTESIAN_POINT ( 'NONE',  ( 3.257844248621785788, 0.9402718649541740303, 1.867333078124802315 ) ) ;
#184413=CARTESIAN_POINT ( 'NONE',  ( 2.781836775232096048, -0.9115585761545975663, 1.516887842838773759 ) ) ;
#184417=CARTESIAN_POINT ( 'NONE',  ( 4.962941676929116142, 0.2283445767556212536, -2.280853557871139525 ) ) ;
#184418=CARTESIAN_POINT ( 'NONE',  ( 3.784860527941535491, 1.262060850391345523, 1.198560274591720098 ) ) ;
#184422=CARTESIAN_POINT ( 'NONE',  ( 3.128000772048340927, 0.2569867100842055940, -1.714543959099825710 ) ) ;
#184423=CARTESIAN_POINT ( 'NONE',  ( 3.420551359632235222, 0.9736478647841840806, 1.940675715818460878 ) ) ;
#184425=CARTESIAN_POINT ( 'NONE',  ( 4.223842396274177347, 0.8578445224393380641, -1.825075645057252505 ) ) ;
#184426=CARTESIAN_POINT ( 'NONE',  ( 0.7812500000000006661, 0.7852924748300293967, 1.895863743164072357 ) ) ;
#184428=CARTESIAN_POINT ( 'NONE',  ( 1.922754896507544720, 1.796626380246616028, 0.6955005520668521291 ) ) ;
#184430=CARTESIAN_POINT ( 'NONE',  ( 5.642908736356011978, 2.140874091242400912, 0.5926086046802480078 ) ) ;
#184432=CARTESIAN_POINT ( 'NONE',  ( -0.1108833634136767998, 2.883350581177961391, -2.385667623150728556 ) ) ;
#184437=CARTESIAN_POINT ( 'NONE',  ( 0.2236696677372449760, 1.935810370009845460, 1.089285801332658732 ) ) ;
#184438=CARTESIAN_POINT ( 'NONE',  ( 6.250445965835445428, -1.952298026214387416, -0.1936728439068043650 ) ) ;
#184441=CARTESIAN_POINT ( 'NONE',  ( 6.345044588916532113, -1.916324442970654962, 1.202328811479462578 ) ) ;
#184444=CARTESIAN_POINT ( 'NONE',  ( 4.914538883754228316, 0.7863694667932183968, 1.907089347224044884 ) ) ;
#184448=CARTESIAN_POINT ( 'NONE',  ( 5.729731410239141454, -1.186140735684092284, -1.446405967604667886 ) ) ;
#184449=CARTESIAN_POINT ( 'NONE',  ( 4.588316246536889409, -0.4565669943805070186, 1.672893389497135841 ) ) ;
#184450=CARTESIAN_POINT ( 'NONE',  ( 3.227794649281841011, 1.698692639566254936, 0.3781252810216747529 ) ) ;
#184452=CARTESIAN_POINT ( 'NONE',  ( 1.417954980037740009, -1.278267931767061771, -1.902717450791486353 ) ) ;
#184454=CARTESIAN_POINT ( 'NONE',  ( 5.425362623596053702, -1.327343567673059166, -1.615326566546205767 ) ) ;
#184455=CARTESIAN_POINT ( 'NONE',  ( 0.5504183687293667804, -1.553892155338543191, -0.9872222399871022347 ) ) ;
#184457=CARTESIAN_POINT ( 'NONE',  ( 2.110000207431836472, 0.002812218110825881467, 2.016597019944998959 ) ) ;
#184458=CARTESIAN_POINT ( 'NONE',  ( 0.1116237293282626442, -2.148295633857814746, 0.4319020730012904097 ) ) ;
#184462=CARTESIAN_POINT ( 'NONE',  ( 2.719513590175401063, 1.792643918890064247, 1.132349250948051500 ) ) ;
#184464=CARTESIAN_POINT ( 'NONE',  ( 6.041596546049881944, -1.325759876995153075, -1.255439798616593716 ) ) ;
#184470=CARTESIAN_POINT ( 'NONE',  ( 2.496358458697241378, -1.034576831241553307, 1.734530517449877740 ) ) ;
#184471=CARTESIAN_POINT ( 'NONE',  ( 0.3058767667667975365, -0.5614299121656821656, 2.029657625958045664 ) ) ;
#184473=CARTESIAN_POINT ( 'NONE',  ( 3.942128412476927135, -0.9204884114761485714, 1.617296529409748773 ) ) ;
#184482=CARTESIAN_POINT ( 'NONE',  ( 1.440355836138224932, 1.027696236922505557, 1.396268056379332378 ) ) ;
#184483=CARTESIAN_POINT ( 'NONE',  ( 1.640152974701726496, -1.471428658003028911, 0.9289965205148569272 ) ) ;
#184484=CARTESIAN_POINT ( 'NONE',  ( 5.145303760848274344, -1.981494167013456709, 1.182657305203537401 ) ) ;
#184487=CARTESIAN_POINT ( 'NONE',  ( 1.792332366127664223, -2.050593157767267805, -0.2048568651325937962 ) ) ;
#184489=CARTESIAN_POINT ( 'NONE',  ( 6.890000000000009450, -0.01081285896028030651, 2.279840171838908525 ) ) ;
#184492=CARTESIAN_POINT ( 'NONE',  ( 0.5320225927652595388, 1.015637564890453426, -1.689598002260852772 ) ) ;
#184494=CARTESIAN_POINT ( 'NONE',  ( 4.095896644567202038, 1.253117935160457552, 1.444681106026260320 ) ) ;
#184496=CARTESIAN_POINT ( 'NONE',  ( 6.604147088760183415, -2.206502607372296421, 0.04933187264975073122 ) ) ;
#184501=CARTESIAN_POINT ( 'NONE',  ( 0.4694063198951373694, -1.707435420315214003, -1.078448885650341582 ) ) ;
#184503=CARTESIAN_POINT ( 'NONE',  ( 3.557953228543974777, 0.5631008447647236625, -2.237707790512387440 ) ) ;
#184504=CARTESIAN_POINT ( 'NONE',  ( 4.791432466842788784, -1.794507165602466037, 0.7932701521168731285 ) ) ;
#184505=CARTESIAN_POINT ( 'NONE',  ( 0.5847188370675902025, 1.875566754216885013, 0.5750099747552291918 ) ) ;
#184509=CARTESIAN_POINT ( 'NONE',  ( 0.2513570338038995100, 0.2008850299538050832, -2.107768975555255331 ) ) ;
#184512=CARTESIAN_POINT ( 'NONE',  ( 3.643588050499571018, 1.964860050422628124, -0.9237357390106512023 ) ) ;
#184513=CARTESIAN_POINT ( 'NONE',  ( 0.9496594531581278309, -1.914679731917130479, 0.9119059213342151082 ) ) ;
#184518=CARTESIAN_POINT ( 'NONE',  ( 2.056002787803516973, 2.055476740694470728, -0.1483529063488266686 ) ) ;
#184525=CARTESIAN_POINT ( 'NONE',  ( 4.986922676292999235, -1.801926769106906745, -0.6406197933803285949 ) ) ;
#184527=CARTESIAN_POINT ( 'NONE',  ( 0.7204656808509112276, -1.211343046821738101, -1.910610397963452112 ) ) ;
#184529=CARTESIAN_POINT ( 'NONE',  ( 0.9315677820061087910, -1.767094751418090803, 0.3981412331970111684 ) ) ;
#184530=CARTESIAN_POINT ( 'NONE',  ( 0.6904808011564408377, 1.448434100015457693, -1.253846941973751683 ) ) ;
#184531=CARTESIAN_POINT ( 'NONE',  ( 1.451716722110554025, 1.566445173006292935, 1.353826630019476562 ) ) ;
#184533=CARTESIAN_POINT ( 'NONE',  ( 6.772336237553374438, -1.148929780121176414, 1.476827877338216854 ) ) ;
#184534=CARTESIAN_POINT ( 'NONE',  ( 5.479104952107777926, -0.04952074540257554031, -1.926025958231538882 ) ) ;
#184535=CARTESIAN_POINT ( 'NONE',  ( 0.5402173299829955422, -1.636151841282366126, -1.627667753820499330 ) ) ;
#184539=CARTESIAN_POINT ( 'NONE',  ( 3.701677541426426910, -1.560128098810292130, -1.349382831327667454 ) ) ;
#184546=CARTESIAN_POINT ( 'NONE',  ( 5.315496758875870142, -0.3119175628578441661, 2.082610458907033557 ) ) ;
#184548=CARTESIAN_POINT ( 'NONE',  ( 6.039524589772497620, 1.914416561877980261, -0.7887839105886890190 ) ) ;
#184551=CARTESIAN_POINT ( 'NONE',  ( 4.446650332099550518, 0.5718123500428309303, 2.084546224624775679 ) ) ;
#184552=CARTESIAN_POINT ( 'NONE',  ( 4.529947673531667718, -1.980263497020241292, 0.3961197999026391248 ) ) ;
#184559=CARTESIAN_POINT ( 'NONE',  ( 3.854704076794239764, -1.883312302057647880, -0.7212934815618715634 ) ) ;
#184567=CARTESIAN_POINT ( 'NONE',  ( 4.183220377109976518, 1.621195451842275315, 1.198844725951081047 ) ) ;
#184569=CARTESIAN_POINT ( 'NONE',  ( 0.1875851866701295223, -0.8181552731707610882, 1.518483014795414032 ) ) ;
#184574=CARTESIAN_POINT ( 'NONE',  ( 4.938664768831325880, 0.3182328507864223277, 1.843102042236575588 ) ) ;
#184576=CARTESIAN_POINT ( 'NONE',  ( 6.504166875733549347, -0.8557802559411722410, 1.820156917002911712 ) ) ;
#184581=CARTESIAN_POINT ( 'NONE',  ( 0.4918148228068714989, -2.006445053647107013, 0.2004575690456936732 ) ) ;
#184583=CARTESIAN_POINT ( 'NONE',  ( 1.441375510584298913, -1.705046834049932292, 0.6123784311264174329 ) ) ;
#184585=CARTESIAN_POINT ( 'NONE',  ( 6.649309733611729278, -1.732918351142084035, -1.292073167451508686 ) ) ;
#184588=CARTESIAN_POINT ( 'NONE',  ( -0.1884536309573183466, -1.180508991428173671, -1.509157985239983679 ) ) ;
#184590=CARTESIAN_POINT ( 'NONE',  ( 6.559000000000036579, 7.629137130509070275, 2.600000000000001421 ) ) ;
#184596=CARTESIAN_POINT ( 'NONE',  ( 4.135729569369491543, -1.488772398488471094, -1.567562023322838671 ) ) ;
#184600=CARTESIAN_POINT ( 'NONE',  ( 1.195735321641926197, 1.957225868588155837, -0.8166992996602241428 ) ) ;
#184602=CARTESIAN_POINT ( 'NONE',  ( 2.477749938138404051, 1.209727786519874559, 1.556487202666415604 ) ) ;
#184603=CARTESIAN_POINT ( 'NONE',  ( 4.306835718904429733, -0.4242474483713705169, -1.864571660543254961 ) ) ;
#184606=CARTESIAN_POINT ( 'NONE',  ( 6.338338845641732888, -1.054863691225367939, 1.663055945198953278 ) ) ;
#184607=CARTESIAN_POINT ( 'NONE',  ( 0.8318532965871343610, 1.913089267318631270, 0.3326846900589939815 ) ) ;
#184613=CARTESIAN_POINT ( 'NONE',  ( 4.600206319907148789, -0.8982956317880007591, 1.688143452400918454 ) ) ;
#184615=CARTESIAN_POINT ( 'NONE',  ( 3.703933201646680828, -0.6411959742554216302, 2.111683309420588905 ) ) ;
#184617=CARTESIAN_POINT ( 'NONE',  ( 2.362605853119781774, 0.9431403173822919817, 1.995201469058570432 ) ) ;
#184619=CARTESIAN_POINT ( 'NONE',  ( 0.4340482808194641162, -1.023182136338888659, -1.615339470012015166 ) ) ;
#184623=CARTESIAN_POINT ( 'NONE',  ( 3.437997351728830697, 1.311287738946330439, 1.602184970737066338 ) ) ;
#184627=CARTESIAN_POINT ( 'NONE',  ( 1.165152350680317195, -1.954565670758709128, -0.9236901323337529668 ) ) ;
#184628=CARTESIAN_POINT ( 'NONE',  ( 2.577880719133851084, -1.123996537731044354, 1.881222605751430521 ) ) ;
#184635=CARTESIAN_POINT ( 'NONE',  ( 6.275961099261262000, 1.503942705979001593, -0.8632642021696999013 ) ) ;
#184637=CARTESIAN_POINT ( 'NONE',  ( 3.713788242813487184, 0.5077267127921447631, -2.006887321594638784 ) ) ;
#184638=CARTESIAN_POINT ( 'NONE',  ( 4.429392955138825805, -1.637772332673973485, -1.341807030983455773 ) ) ;
#184641=CARTESIAN_POINT ( 'NONE',  ( 2.395301122324170695, -1.761490415372953589, 0.8809153588016715997 ) ) ;
#184642=CARTESIAN_POINT ( 'NONE',  ( 0.6856317642073318508, 1.842354612247762091, -0.5124485439033445999 ) ) ;
#184643=CARTESIAN_POINT ( 'NONE',  ( 5.244168061255013669, 0.6613091839676830119, 2.194790591360805898 ) ) ;
#184644=CARTESIAN_POINT ( 'NONE',  ( 2.613660848560445782, -1.805822647967848971, 0.2677728182119283318 ) ) ;
#184648=CARTESIAN_POINT ( 'NONE',  ( 4.552993993533384298, 0.3484205210483002357, 1.982688671860346252 ) ) ;
#184649=CARTESIAN_POINT ( 'NONE',  ( 4.891432378139471737, -1.795214109662087942, 0.7913882323652280393 ) ) ;
#184652=CARTESIAN_POINT ( 'NONE',  ( 0.1753634416057739953, 5.721028741045294908, -2.738064866945366660 ) ) ;
#184653=CARTESIAN_POINT ( 'NONE',  ( -0.1291982275798781443, -0.004298614154785855221, -2.073875112923003083 ) ) ;
#184654=CARTESIAN_POINT ( 'NONE',  ( 5.348444421042818142, 0.5165251424982686412, 1.692803071163173634 ) ) ;
#184655=PLANE ( 'NONE',  #43479 ) ;
#184657=CARTESIAN_POINT ( 'NONE',  ( 1.429895766826321690, 1.077743243251317429, -1.908043295719801025 ) ) ;
#184658=CARTESIAN_POINT ( 'NONE',  ( 6.210887288261135453, -0.2055507460125911567, 1.728089712739445671 ) ) ;
#184661=CARTESIAN_POINT ( 'NONE',  ( 0.04690384546136848465, -1.329360633743952746, -1.098954345569080893 ) ) ;
#184662=CARTESIAN_POINT ( 'NONE',  ( 1.283028839759347894, -2.242172747002548316, 0.5046827817699239827 ) ) ;
#184663=CARTESIAN_POINT ( 'NONE',  ( 0.2401087780563165297, 2.186128513634697512, 0.1550312349237955856 ) ) ;
#184664=CARTESIAN_POINT ( 'NONE',  ( 6.608738931450677256, 0.6592670866186548517, -1.603827835538347291 ) ) ;
#184665=CARTESIAN_POINT ( 'NONE',  ( 3.528125218122651230, -1.314342534882004809, -1.772652456903674567 ) ) ;
#184666=CARTESIAN_POINT ( 'NONE',  ( 0.3566018059198462486, -2.170557273582163216, -0.05455199461934338162 ) ) ;
#184668=CARTESIAN_POINT ( 'NONE',  ( 1.692723046232265105, 1.565162839624185898, -1.426121385913220019 ) ) ;
#184669=CARTESIAN_POINT ( 'NONE',  ( 6.727182134110167411, 4.685720203848058318, 2.851561905840187983 ) ) ;
#184670=CARTESIAN_POINT ( 'NONE',  ( 5.877940811483009398, 1.147681995895684315, 1.547064007116766060 ) ) ;
#184672=CARTESIAN_POINT ( 'NONE',  ( 1.716775041481681585, 2.140780187006920077, 0.8202503203454788450 ) ) ;
#184676=CARTESIAN_POINT ( 'NONE',  ( 3.264521566599550173, 2.221473416772083098, -0.001674386450213962828 ) ) ;
#184681=AXIS2_PLACEMENT_3D ( 'NONE', #27005, #93111, #39011 ) ;
#184684=CARTESIAN_POINT ( 'NONE',  ( 2.022111496571117772, -1.799922141918413487, 0.9091460122201827643 ) ) ;
#184686=CARTESIAN_POINT ( 'NONE',  ( 1.393505825229651052, -1.866293207157668776, 0.8783701326641482066 ) ) ;
#184691=CARTESIAN_POINT ( 'NONE',  ( 4.154361996720875361, -1.624486827992781990, 1.471056368041193219 ) ) ;
#184692=CARTESIAN_POINT ( 'NONE',  ( 0.7740648250077889481, 1.777010169924503558, -0.9530137779002674225 ) ) ;
#184693=CARTESIAN_POINT ( 'NONE',  ( 0.7316835000789992938, 1.813914744281470925, 0.3150931809976220133 ) ) ;
#184694=CARTESIAN_POINT ( 'NONE',  ( 5.759400667030329934, 2.259083744078540956, -0.3884743064591251738 ) ) ;
#184695=CARTESIAN_POINT ( 'NONE',  ( 3.398233898566359823, 1.450718870894672330, -1.133551952132209717 ) ) ;
#184697=CARTESIAN_POINT ( 'NONE',  ( 4.401258566127845384, 1.466438172381477445, 1.087111955044787859 ) ) ;
#184698=CARTESIAN_POINT ( 'NONE',  ( 5.168592345394213972, 1.356298078840772803, 1.492257005506092193 ) ) ;
#184700=CARTESIAN_POINT ( 'NONE',  ( 4.346707190358800155, 0.5996197433882300976, 2.181559591530066289 ) ) ;
#184702=CARTESIAN_POINT ( 'NONE',  ( 6.721705546354253435, -2.043712959172855115, 0.5078683761520035311 ) ) ;
#184703=CARTESIAN_POINT ( 'NONE',  ( 3.086448098943677998, 1.152334561581969785, -1.719836228861029603 ) ) ;
#184708=CARTESIAN_POINT ( 'NONE',  ( 1.559075672363739118, -1.651969382833524902, -0.9909376787137593734 ) ) ;
#184709=CARTESIAN_POINT ( 'NONE',  ( 6.860212146170862724, -1.969081375482661267, 0.04489377202578949400 ) ) ;
#184714=CARTESIAN_POINT ( 'NONE',  ( 2.057158355326561772, 0.4919409011131297138, 2.166103627455501890 ) ) ;
#184715=CARTESIAN_POINT ( 'NONE',  ( 3.065558131891146676, 0.3103791954156452371, -2.082839965623133782 ) ) ;
#184718=CARTESIAN_POINT ( 'NONE',  ( 0.6251817401201573698, 0.1879592460329523318, -1.851551742960926727 ) ) ;
#184723=CARTESIAN_POINT ( 'NONE',  ( 1.336355901170083849, -1.182550835430173919, -1.760063440837428272 ) ) ;
#184726=CARTESIAN_POINT ( 'NONE',  ( 4.545333077707183200, 1.753367681936630840, -0.8802267832125689750 ) ) ;
#184727=CARTESIAN_POINT ( 'NONE',  ( 3.028364643526501698, 1.202066397148596977, -1.796461956351296019 ) ) ;
#184728=CARTESIAN_POINT ( 'NONE',  ( 1.751249726499287673, 1.836263021919124050, -0.1365115386888632321 ) ) ;
#184730=CARTESIAN_POINT ( 'NONE',  ( 5.156098626313831090, -1.256936769724174674, 1.203943403725541206 ) ) ;
#184734=CARTESIAN_POINT ( 'NONE',  ( 2.008865009297224447, 1.601992838228694316, -1.451600824242594845 ) ) ;
#184736=CARTESIAN_POINT ( 'NONE',  ( 3.602888598310006074, 0.9090057795711030675, -1.799647124144133858 ) ) ;
#184738=CARTESIAN_POINT ( 'NONE',  ( 1.129994055010040022, -1.371941552271437770, -1.670562328977095445 ) ) ;
#184739=CARTESIAN_POINT ( 'NONE',  ( 2.905103271286565647, 1.664600965932877319, 1.056039161509576108 ) ) ;
#184742=CARTESIAN_POINT ( 'NONE',  ( 3.333474266508968054, 0.8707927262202612706, -1.735945723835415677 ) ) ;
#184747=CARTESIAN_POINT ( 'NONE',  ( -0.1108833634137010304, 7.629137130509073828, -2.496956624467902675 ) ) ;
#184752=CARTESIAN_POINT ( 'NONE',  ( 0.5873203293235219613, -0.2722241568871349160, -2.189838084831654541 ) ) ;
#184754=CARTESIAN_POINT ( 'NONE',  ( 4.135565103414404753, 1.848670044762780407, -0.6568835154602686854 ) ) ;
#184757=CARTESIAN_POINT ( 'NONE',  ( 1.776017750421728270, 1.753029812786778940, -0.9963028777105963352 ) ) ;
#184759=CARTESIAN_POINT ( 'NONE',  ( 3.134099051248913970, 2.117513410275436936, -0.004568276605129357668 ) ) ;
#184763=CARTESIAN_POINT ( 'NONE',  ( 2.607153984523866264, -1.821078476238715327, 0.2702138248509636242 ) ) ;
#184768=CARTESIAN_POINT ( 'NONE',  ( 3.797228045176269440, -0.2112621354826669517, -2.110076569278092062 ) ) ;
#184772=CARTESIAN_POINT ( 'NONE',  ( 5.677046966798700467, -0.04615325445976201785, -2.060428132270344381 ) ) ;
#184773=CARTESIAN_POINT ( 'NONE',  ( 0.8361097980106885208, -1.038377568841988063, 1.544222109484013172 ) ) ;
#184774=CARTESIAN_POINT ( 'NONE',  ( 2.296224312773272658, 1.477747569344042278, -1.098160524033331642 ) ) ;
#184780=CARTESIAN_POINT ( 'NONE',  ( 2.491098823239074278, -0.3784457004711218042, -2.174036671264235387 ) ) ;
#184781=CARTESIAN_POINT ( 'NONE',  ( 5.114671183409561728, 1.565253227384774792, -1.633764300155052807 ) ) ;
#184783=CARTESIAN_POINT ( 'NONE',  ( 4.482537919100934687, -1.178242479775050811, 1.376196796631526720 ) ) ;
#184784=CARTESIAN_POINT ( 'NONE',  ( 4.065584057473277113, 1.255829935711678669, 1.446728075138058678 ) ) ;
#184786=CARTESIAN_POINT ( 'NONE',  ( 3.731288366010646396, -1.822051990069279315, 0.7533225318517923208 ) ) ;
#184787=CARTESIAN_POINT ( 'NONE',  ( 4.873830839387755631, 1.077430855447782942, 1.529020332772989210 ) ) ;
#184788=CARTESIAN_POINT ( 'NONE',  ( 4.738624546071780408, -1.804922690063763824, -0.4530168641722984169 ) ) ;
#184790=CLOSED_SHELL ( 'NONE', ( #207611, #59839, #67480, #24832, #48574, #205842, #152194, #107061 ) ) ;
#184791=CARTESIAN_POINT ( 'NONE',  ( 0.2336117360935245635, 0.6279853779636718203, -1.916355031878452797 ) ) ;
#184793=CARTESIAN_POINT ( 'NONE',  ( 1.928482936185798247, 1.211665229685221057, -1.722411974427066506 ) ) ;
#184796=CARTESIAN_POINT ( 'NONE',  ( 0.07479286986305544449, 2.046156589154801253, -2.272744413733415403 ) ) ;
#184798=CARTESIAN_POINT ( 'NONE',  ( 1.336200995665462354, -1.125576746034629094, -1.676869184967361814 ) ) ;
#184804=CARTESIAN_POINT ( 'NONE',  ( 2.601032539102793084, 1.737798908178284307, -1.285340053188685383 ) ) ;
#184805=CARTESIAN_POINT ( 'NONE',  ( 6.610000000000006537, 0.002781820520842553934, 2.000159646111852929 ) ) ;
#184812=CARTESIAN_POINT ( 'NONE',  ( 0.9607770615731696662, -1.983481723135366304, -0.9323335341336475013 ) ) ;
#184814=CARTESIAN_POINT ( 'NONE',  ( 1.604739632818411144, -0.8155265934593752819, -2.110601385940619412 ) ) ;
#184821=CARTESIAN_POINT ( 'NONE',  ( 3.527714679269139619, -1.028799902082434992, -1.384306889003545926 ) ) ;
#184824=CARTESIAN_POINT ( 'NONE',  ( 2.424752316626857862, -0.004995123648579914352, 1.769921776121333945 ) ) ;
#184825=CARTESIAN_POINT ( 'NONE',  ( 5.737410212107617369, -1.997324651315037780, 0.9386623957203032997 ) ) ;
#184827=CARTESIAN_POINT ( 'NONE',  ( 4.183856667257361828, 1.958065582907195568, -0.4948979464895820191 ) ) ;
#184829=CARTESIAN_POINT ( 'NONE',  ( 3.708611378246814638, 1.915606880664010747, 0.6298579873919087913 ) ) ;
#184830=CARTESIAN_POINT ( 'NONE',  ( 4.130988372668517705, 1.658889437441883441, 0.7283703743019008803 ) ) ;
#184832=CARTESIAN_POINT ( 'NONE',  ( 2.588565208901713266, -0.3177388942022137397, -1.843305967786903032 ) ) ;
#184833=AXIS2_PLACEMENT_3D ( 'NONE', #44569, #176683, #28295 ) ;
#184835=CARTESIAN_POINT ( 'NONE',  ( 2.127084423382288314, 1.709874882824816478, 0.8565708355050825062 ) ) ;
#184842=CARTESIAN_POINT ( 'NONE',  ( 0.4570967503451648373, -1.639016809899789040, 0.9851245988263114262 ) ) ;
#184843=CARTESIAN_POINT ( 'NONE',  ( 4.171111447311355747, 1.799123655847803205, -0.9110083886025857058 ) ) ;
#184845=CARTESIAN_POINT ( 'NONE',  ( 2.049198471137442912, 1.708465938063120637, -0.9642302061752603404 ) ) ;
#184849=CARTESIAN_POINT ( 'NONE',  ( 4.148766697842418694, 2.080301416381886703, 0.4105806053946169376 ) ) ;
#184852=CARTESIAN_POINT ( 'NONE',  ( 5.413337677306027551, -0.2920802625693446619, 1.949502277767001690 ) ) ;
#184854=CARTESIAN_POINT ( 'NONE',  ( 1.019790247428183472, -0.4849793317353002786, 1.953821064534920326 ) ) ;
#184856=CARTESIAN_POINT ( 'NONE',  ( 1.265409400557556907, 1.954659568096604350, -0.8140754496198910894 ) ) ;
#184858=CARTESIAN_POINT ( 'NONE',  ( 2.576698201331685922, 1.354182300986291887, -1.566139152919379107 ) ) ;
#184862=CARTESIAN_POINT ( 'NONE',  ( 4.576172254314175625, -2.027756842407653082, -0.5083681234262329429 ) ) ;
#184864=CARTESIAN_POINT ( 'NONE',  ( 2.696107482849848580, -1.820545782403935720, -0.1364615833806467338 ) ) ;
#184865=CARTESIAN_POINT ( 'NONE',  ( 1.137045503269896285, -0.04498225810314023659, 1.811072777871777006 ) ) ;
#184866=ORIENTED_EDGE ( 'NONE', *, *, #150667, .T. ) ;
#184867=CARTESIAN_POINT ( 'NONE',  ( 6.656857027519620829, -1.708965229049699053, 1.396003577074665714 ) ) ;
#184870=CARTESIAN_POINT ( 'NONE',  ( 5.421004802376033993, 2.037064969303593820, 0.8491359902737596332 ) ) ;
#184873=CARTESIAN_POINT ( 'NONE',  ( 4.283787348595206268, 1.854039900284172315, -0.4678174759695231666 ) ) ;
#184876=CARTESIAN_POINT ( 'NONE',  ( 6.865700769154306826, -0.4580177224273937475, 2.026514595051785772 ) ) ;
#184883=CARTESIAN_POINT ( 'NONE',  ( 3.286256049847174676, -1.842268013383094427, -0.3231441395407097517 ) ) ;
#184890=CARTESIAN_POINT ( 'NONE',  ( 6.631696427350994405, 1.982895789845315671, -0.5951614246157420629 ) ) ;
#184891=CARTESIAN_POINT ( 'NONE',  ( 0.7906389332529573100, 1.525030349845598820, -1.319245847334844735 ) ) ;
#184894=CARTESIAN_POINT ( 'NONE',  ( 0.8850414913617115076, 1.931072968267994794, -1.036053359626129877 ) ) ;
#184895=CARTESIAN_POINT ( 'NONE',  ( 6.656878040733529289, -1.407521694628325770, 1.162499734694094844 ) ) ;
#184903=CARTESIAN_POINT ( 'NONE',  ( 4.018977146631536712, -1.760761141180338774, 0.5383908109771737838 ) ) ;
#184904=CARTESIAN_POINT ( 'NONE',  ( 1.049477475095396573, -1.818952357203638570, 0.8628315626280655959 ) ) ;
#184905=CARTESIAN_POINT ( 'NONE',  ( 1.968534425330380921, 1.910819170882430695, 1.277001204893423170 ) ) ;
#184907=CARTESIAN_POINT ( 'NONE',  ( 0.4263013476871494456, -1.221759592413705908, 1.403788950402263369 ) ) ;
#184911=CARTESIAN_POINT ( 'NONE',  ( 4.183787391381143195, 1.853651273288700718, -0.4697857328580385960 ) ) ;
#184915=CARTESIAN_POINT ( 'NONE',  ( 4.001575260567552306, -2.085028717228009310, 0.1556281442064103848 ) ) ;
#184916=CARTESIAN_POINT ( 'NONE',  ( 2.606148294764852213, -0.7140300644919925777, -1.729217693616967644 ) ) ;
#184919=CARTESIAN_POINT ( 'NONE',  ( 3.087183437724149826, -0.7025620359558025774, 1.592517242405028233 ) ) ;
#184923=CARTESIAN_POINT ( 'NONE',  ( 3.650762458506318087, -1.408968171862119423, 0.9946885059901353632 ) ) ;
#184924=CARTESIAN_POINT ( 'NONE',  ( 3.878626735558046157, -0.2160506499642600997, -2.180900317982924275 ) ) ;
#184925=CARTESIAN_POINT ( 'NONE',  ( 6.199877634063251541, -0.7475181258948644381, 2.076568058718592624 ) ) ;
#184927=CARTESIAN_POINT ( 'NONE',  ( 4.012681996134721096, 0.7761599038508348869, 2.027777647250021076 ) ) ;
#184928=CARTESIAN_POINT ( 'NONE',  ( 1.857752496991037061, 1.820901040755190214, -0.1330985588276211995 ) ) ;
#184929=CARTESIAN_POINT ( 'NONE',  ( 0.3210474040165818277, -1.749687966165301090, -0.8873976775175674847 ) ) ;
#184930=CARTESIAN_POINT ( 'NONE',  ( 4.803976500543080341, -1.135498674831243227, -1.786957999583696610 ) ) ;
#184932=CARTESIAN_POINT ( 'NONE',  ( 4.634495141935854434, 0.3908333592176889137, 2.258673302944668837 ) ) ;
#184934=CARTESIAN_POINT ( 'NONE',  ( 6.720655732516641834, 0.008434553976904584152, 1.726293928996263771 ) ) ;
#184936=CARTESIAN_POINT ( 'NONE',  ( 0.9090200710941964690, -0.5189423241485704441, -2.055877189782874481 ) ) ;
#184942=CARTESIAN_POINT ( 'NONE',  ( 5.660779783930850684, 1.203351582566011047, 1.617819807990819481 ) ) ;
#184944=CARTESIAN_POINT ( 'NONE',  ( 4.645415531332927728, 1.844630620182326153, -0.9228673458712335353 ) ) ;
#184949=CARTESIAN_POINT ( 'NONE',  ( 0.1331565106231571705, 4.092041177288479048, -2.500854978060399691 ) ) ;
#184950=CARTESIAN_POINT ( 'NONE',  ( 0.2872076490801517279, 1.550519377178682268, 1.402564467939530823 ) ) ;
#184951=CARTESIAN_POINT ( 'NONE',  ( 4.658827374183164949, 1.163267680695536876, 1.646840100852072997 ) ) ;
#184952=CARTESIAN_POINT ( 'NONE',  ( 4.511176471348508521, -1.804767551675333204, 0.3638508048048467169 ) ) ;
#184955=CARTESIAN_POINT ( 'NONE',  ( 1.025878534523045449, 1.032422052977323590, -1.381481875464431797 ) ) ;
#184956=CARTESIAN_POINT ( 'NONE',  ( 0.1457207355009884908, 1.993892511249679034, -0.3006540981884687214 ) ) ;
#184957=CARTESIAN_POINT ( 'NONE',  ( 0.8976324851915818970, -1.040256531696292397, -2.049935236865876309 ) ) ;
#184959=CARTESIAN_POINT ( 'NONE',  ( 0.8083708232014105155, -2.251370329867402376, 0.2228818479251652163 ) ) ;
#184960=CARTESIAN_POINT ( 'NONE',  ( 2.789785578339375238, 1.489779160094312660, 1.488918557309417467 ) ) ;
#184964=PRESENTATION_STYLE_ASSIGNMENT (( #186037 ) ) ;
#184970=CARTESIAN_POINT ( 'NONE',  ( 5.273765199871699672, 0.4330091245797212385, -2.178642023334904199 ) ) ;
#184971=CARTESIAN_POINT ( 'NONE',  ( 2.238457302780196390, 0.4817095239468481283, 2.137691825660259948 ) ) ;
#184974=CARTESIAN_POINT ( 'NONE',  ( 5.336364984333265227, -1.091323163865608459, 1.630109012322231266 ) ) ;
#184976=CARTESIAN_POINT ( 'NONE',  ( 6.890000000000039648, 4.701345932300413644, 2.282685536056531461 ) ) ;
#184979=CARTESIAN_POINT ( 'NONE',  ( 4.482752736079084421, -1.382999391253452615, 1.607682512923855445 ) ) ;
#184983=CARTESIAN_POINT ( 'NONE',  ( 6.420800710400103917, 2.015122584031241004, 0.7829223626853940576 ) ) ;
#184985=CARTESIAN_POINT ( 'NONE',  ( 4.845164456061270997, 0.5726227986864868003, -1.750029900461601340 ) ) ;
#184988=CARTESIAN_POINT ( 'NONE',  ( 0.8193799409778947940, 1.038239828973979373, -1.396697621350863505 ) ) ;
#184993=CARTESIAN_POINT ( 'NONE',  ( 5.752838164830007983, -1.706859214253673152, 1.326403591387192771 ) ) ;
#184998=CARTESIAN_POINT ( 'NONE',  ( 5.190363053866647647, -2.144918610114197488, -0.2683968819863768451 ) ) ;
#185000=CARTESIAN_POINT ( 'NONE',  ( 5.096930449404251107, 1.640577245564038389, -1.092763768510503608 ) ) ;
#185001=CARTESIAN_POINT ( 'NONE',  ( 4.059675810253587258, 1.465203325174119664, -0.9266335502581940498 ) ) ;
#185003=CARTESIAN_POINT ( 'NONE',  ( 1.312353134292881141, 1.468346937154514364, -1.627112938194043235 ) ) ;
#185004=CARTESIAN_POINT ( 'NONE',  ( 2.643975807074511408, -1.709602402607094396, -1.550068159870971574 ) ) ;
#185005=CARTESIAN_POINT ( 'NONE',  ( 5.009085904467641015, 1.791045569760267631, 1.019200576588958240 ) ) ;
#185006=CARTESIAN_POINT ( 'NONE',  ( 6.620655732516682157, 0.004685112605702904456, 1.926407831898164114 ) ) ;
#185011=CARTESIAN_POINT ( 'NONE',  ( 3.417197246517459597, 1.994164043739574232, 0.9453733912969732867 ) ) ;
#185013=CARTESIAN_POINT ( 'NONE',  ( 0.5669689972240202769, 1.615300940711749789, 0.9240007631576854230 ) ) ;
#185020=CARTESIAN_POINT ( 'NONE',  ( 6.070224334863941529, -1.749758606415029449, -0.5730458292283467925 ) ) ;
#185022=CARTESIAN_POINT ( 'NONE',  ( 2.922786580453646366, 1.940006684909411971, 0.6957959148722169251 ) ) ;
#185026=CARTESIAN_POINT ( 'NONE',  ( 1.752609234595727816, 1.998021763388730720, 0.2939949305936078172 ) ) ;
#185029=CARTESIAN_POINT ( 'NONE',  ( 1.762645127485995555, -1.458140857472267626, 1.456663342728149901 ) ) ;
#185035=CARTESIAN_POINT ( 'NONE',  ( 5.057340365224886725, -1.863002784048470639, -1.182737378625432489 ) ) ;
#185036=CARTESIAN_POINT ( 'NONE',  ( 1.599129061979026822, 1.768144091905754500, -1.243190488262067683 ) ) ;
#185038=CARTESIAN_POINT ( 'NONE',  ( 0.3918150239524306189, -2.006371095615328226, 0.2024682584410575914 ) ) ;
#185039=CARTESIAN_POINT ( 'NONE',  ( 2.003655084434956102, 2.273349380270474729, 0.3377564834418695927 ) ) ;
#185043=CARTESIAN_POINT ( 'NONE',  ( 1.762360912074714125, -1.325010844092512796, 1.320751239342173200 ) ) ;
#185044=CARTESIAN_POINT ( 'NONE',  ( 3.573454097414618946, 1.463926983822515293, 1.387100322000796027 ) ) ;
#185048=CARTESIAN_POINT ( 'NONE',  ( 4.776057437618447921, 1.212020014983648863, 1.722159047642721541 ) ) ;
#185053=CARTESIAN_POINT ( 'NONE',  ( 4.816668504955663899, -0.6845142050268312461, -1.900371106210005712 ) ) ;
#185055=CARTESIAN_POINT ( 'NONE',  ( 1.252863987647494515, -0.4972004349026898362, -2.001653351804733028 ) ) ;
#185063=CARTESIAN_POINT ( 'NONE',  ( 2.998652106967353514, 2.154486853421373027, 0.2683346083656880099 ) ) ;
#185066=CARTESIAN_POINT ( 'NONE',  ( 2.331387312403776946, 0.8663521307504215008, -1.624669977836174839 ) ) ;
#185068=CARTESIAN_POINT ( 'NONE',  ( 4.318054327947466575, 1.347776305887092185, -1.728067674571641898 ) ) ;
#185070=CARTESIAN_POINT ( 'NONE',  ( 4.557670991828286056, 0.4998169670675355336, -2.206472437794388952 ) ) ;
#185078=CARTESIAN_POINT ( 'NONE',  ( 5.237463280334829996, -1.251769750873907849, -1.251277626909578222 ) ) ;
#185079=CARTESIAN_POINT ( 'NONE',  ( 3.193996758133522018, 1.278685386795814560, 1.554813472153792286 ) ) ;
#185081=CARTESIAN_POINT ( 'NONE',  ( 2.028482804581877019, 1.213238276247522895, -1.721163102310949045 ) ) ;
#185084=CARTESIAN_POINT ( 'NONE',  ( 1.627339542692422869, 0.1479755015179542166, -1.964067387968527312 ) ) ;
#185085=CARTESIAN_POINT ( 'NONE',  ( 0.7779422811538607707, -1.042605501850740080, 1.552959968518424771 ) ) ;
#185086=CARTESIAN_POINT ( 'NONE',  ( 1.187862215860764126, -1.241893603568875903, -1.518774446641702580 ) ) ;
#185087=CARTESIAN_POINT ( 'NONE',  ( 6.381129877538572970, -1.660329982341423705, -0.7251259014357125388 ) ) ;
#185091=CARTESIAN_POINT ( 'NONE',  ( 5.823093596695693819, -0.04436734784114480107, 1.870300906237104988 ) ) ;
#185092=CARTESIAN_POINT ( 'NONE',  ( 5.664915734613278353, 1.571387620024040199, -1.347999112033698044 ) ) ;
#185094=CARTESIAN_POINT ( 'NONE',  ( 0.07680821025393690105, 0.005952109439256307241, -1.810863387344714193 ) ) ;
#185102=CARTESIAN_POINT ( 'NONE',  ( 4.896903505236655185, 0.3334610245491422265, 1.933150054703360432 ) ) ;
#185105=CARTESIAN_POINT ( 'NONE',  ( 3.655624903986275154, -0.3905385215352343287, -1.977747697055858955 ) ) ;
#185106=CARTESIAN_POINT ( 'NONE',  ( 2.307709453281155731, -1.106667911223922829, -1.563510803672981231 ) ) ;
#185108=CARTESIAN_POINT ( 'NONE',  ( 0.2928600448571065940, 1.818678932476354149, -1.222557900829209121 ) ) ;
#185109=CARTESIAN_POINT ( 'NONE',  ( 0.2331713839410628208, 0.2432647426263275514, -1.987790486660771627 ) ) ;
#185110=CARTESIAN_POINT ( 'NONE',  ( 2.213927045526514537, -0.8776910013945339317, -1.651823421649289081 ) ) ;
#185112=CARTESIAN_POINT ( 'NONE',  ( 3.744393049878576463, 1.073438034848249290, -1.702967747733853843 ) ) ;
#185115=CARTESIAN_POINT ( 'NONE',  ( 4.587589571003643840, -0.5631140419127963481, 2.040926637660822163 ) ) ;
#185118=CARTESIAN_POINT ( 'NONE',  ( 5.740704066448026666, -2.019076491677873619, -0.4572469816465085657 ) ) ;
#185119=CARTESIAN_POINT ( 'NONE',  ( 1.558266987246118562, -1.476132899515494534, 1.480894285863892934 ) ) ;
#185120=CARTESIAN_POINT ( 'NONE',  ( 6.620655732516649294, 2.950034989283246478, 2.626075342966327497 ) ) ;
#185121=CARTESIAN_POINT ( 'NONE',  ( 6.440460073785046369, 1.806197173870389694, 0.2645596887278709453 ) ) ;
#185124=CARTESIAN_POINT ( 'NONE',  ( 6.825078400183575589, -0.005632053428735600553, 2.144262460745151255 ) ) ;
#185130=CARTESIAN_POINT ( 'NONE',  ( 0.9085206565882588681, -0.4392767353821840914, -1.757246876086359988 ) ) ;
#185137=CARTESIAN_POINT ( 'NONE',  ( 5.976185453469534892, -2.006962702346287930, -0.1948244327795861652 ) ) ;
#185138=CARTESIAN_POINT ( 'NONE',  ( 0.8211285067932658777, 1.603129840700336928, -1.388046135824993366 ) ) ;
#185141=CARTESIAN_POINT ( 'NONE',  ( 0.1405533004714097089, -0.003749010675423158478, -2.279853246149381452 ) ) ;
#185147=CARTESIAN_POINT ( 'NONE',  ( 3.432427499664345127, -1.176894005904068896, 1.578936197102176031 ) ) ;
#185148=CARTESIAN_POINT ( 'NONE',  ( 4.218375177057286152, 1.978055892313890229, 0.3905773888849966013 ) ) ;
#185150=( LENGTH_UNIT ( ) NAMED_UNIT ( * ) SI_UNIT ( .MILLI., .METRE. ) );
#185152=CARTESIAN_POINT ( 'NONE',  ( 4.295009486468337023, 1.759388067201245187, 1.306329983072423984 ) ) ;
#185154=CARTESIAN_POINT ( 'NONE',  ( 3.416937173653651794, 1.740928992956072952, 0.8250102540389223638 ) ) ;
#185156=CARTESIAN_POINT ( 'NONE',  ( -0.1296875068448159751, 0.001480089298542403009, -1.826395826379861864 ) ) ;
#185157=CARTESIAN_POINT ( 'NONE',  ( 0.2939702064862387831, 1.638257335637434364, 1.478849500172851217 ) ) ;
#185162=CARTESIAN_POINT ( 'NONE',  ( 4.627768981117735159, 1.911305289405954344, -0.4745475857620209958 ) ) ;
#185163=CARTESIAN_POINT ( 'NONE',  ( 0.2044968316872765035, 1.690132753820037692, 0.9564217018903762302 ) ) ;
#185164=CARTESIAN_POINT ( 'NONE',  ( 4.547525146836687959, -1.839596654198237369, 0.8179813495266550216 ) ) ;
#185165=CARTESIAN_POINT ( 'NONE',  ( 5.501416862357105586, 2.263058191380825424, 0.4008149593560642598 ) ) ;
#185167=CARTESIAN_POINT ( 'NONE',  ( 3.977287768980780402, -0.1405865315737795385, 1.855722876009910038 ) ) ;
#185173=CARTESIAN_POINT ( 'NONE',  ( 0.4510473619779230003, -1.854578567552306767, -1.167393260480112493 ) ) ;
#185179=CARTESIAN_POINT ( 'NONE',  ( 0.3811277156573149583, 1.704729334087114578, -0.6539457117896373406 ) ) ;
#185181=CARTESIAN_POINT ( 'NONE',  ( 2.390900936787855091, -0.6653014413638760338, -1.601662460290956380 ) ) ;
#185184=MECHANICAL_DESIGN_GEOMETRIC_PRESENTATION_REPRESENTATION('',(#64155),#91857);
#185185=CARTESIAN_POINT ( 'NONE',  ( 5.197797600609998625, -0.6536857159176562293, 1.704833070275885598 ) ) ;
#185186=CARTESIAN_POINT ( 'NONE',  ( 2.922649740298603138, -1.356309479035762378, 1.417576456850026867 ) ) ;
#185190=CARTESIAN_POINT ( 'NONE',  ( 4.442108405842562391, -1.305342523080333272, -1.670987904322115636 ) ) ;
#185193=CARTESIAN_POINT ( 'NONE',  ( 2.887621454190898884, -1.933326653459125355, 0.7409182656877840722 ) ) ;
#185196=CARTESIAN_POINT ( 'NONE',  ( 4.248835331960220785, 2.178490119157860061, 0.4332075398792554766 ) ) ;
#185198=CARTESIAN_POINT ( 'NONE',  ( 3.235276958591898566, 2.298851035330526038, -0.002058992973525546142 ) ) ;
#185206=CARTESIAN_POINT ( 'NONE',  ( 2.742330423940505302, 1.058908597569432120, -1.592262909973440888 ) ) ;
#185208=CARTESIAN_POINT ( 'NONE',  ( 4.207791664195513093, -1.720086916870446236, 0.1276756817342617201 ) ) ;
#185209=CARTESIAN_POINT ( 'NONE',  ( 3.995327539805045181, -0.3399590882401174463, 1.987497567597557468 ) ) ;
#185210=CARTESIAN_POINT ( 'NONE',  ( 3.903220922379626145, -1.182460753651290775, -1.971142157236325243 ) ) ;
#185212=CARTESIAN_POINT ( 'NONE',  ( 5.936178820057578243, 1.039279821879979693, -1.831694563109196316 ) ) ;
#185215=CARTESIAN_POINT ( 'NONE',  ( 5.061649853805494814, 1.750434175623495348, -0.2595850195740417310 ) ) ;
#185217=CARTESIAN_POINT ( 'NONE',  ( 1.306998621393583138, 2.023524796797530723, 1.076953482639223747 ) ) ;
#185218=CARTESIAN_POINT ( 'NONE',  ( 0.2865101139537007402, 1.286042648715233216, 1.172746904078510122 ) ) ;
#185220=CARTESIAN_POINT ( 'NONE',  ( 6.333935822332934507, 2.167035306593240840, 0.3253760364356065860 ) ) ;
#185224=CARTESIAN_POINT ( 'NONE',  ( 0.4675213905811578807, 1.889292113317426969, 1.069767032291484288 ) ) ;
#185225=CARTESIAN_POINT ( 'NONE',  ( 0.8488426437929346147, -1.825078332268307513, -0.8578388575243289793 ) ) ;
#185228=CARTESIAN_POINT ( 'NONE',  ( 4.406810040222974401, 1.488408744443140863, -1.223127719473691588 ) ) ;
#185230=CARTESIAN_POINT ( 'NONE',  ( 0.8091801829576624749, -0.5468400522714472745, -2.152931845550176249 ) ) ;
#185231=CARTESIAN_POINT ( 'NONE',  ( 0.1247927721447598948, 7.629137130509083597, -2.455404827119290978 ) ) ;
#185239=CARTESIAN_POINT ( 'NONE',  ( 4.001278354253400948, -1.735443821832120870, 0.1328310682092836426 ) ) ;
#185240=CARTESIAN_POINT ( 'NONE',  ( 2.928120951529111338, 1.047165451586975049, 1.658829547137883775 ) ) ;
#185246=CARTESIAN_POINT ( 'NONE',  ( 0.3442780524403609155, -0.9739420414685855398, 1.818282578471181132 ) ) ;
#185249=CARTESIAN_POINT ( 'NONE',  ( 4.997279897388729353, -0.2910847460899004258, 1.995267753224789997 ) ) ;
#185250=CARTESIAN_POINT ( 'NONE',  ( 1.639924147338491123, -1.639646335682118927, -1.559238602228057990 ) ) ;
#185254=CARTESIAN_POINT ( 'NONE',  ( 1.458040028222376439, 0.7530789129696242590, 1.712431740859089668 ) ) ;
#185255=CARTESIAN_POINT ( 'NONE',  ( 0.08792998612136559977, -0.4660014661636499578, 1.670295066556278352 ) ) ;
#185256=CARTESIAN_POINT ( 'NONE',  ( 4.212563348414651188, 2.004022095860341413, 0.8874167208733558798 ) ) ;
#185257=CARTESIAN_POINT ( 'NONE',  ( 5.895647473559280982, 1.742329625737188525, 1.513132890121783536 ) ) ;
#185258=CARTESIAN_POINT ( 'NONE',  ( 1.709912189389639403, -2.045452440186873666, 0.2511061956092154324 ) ) ;
#185259=CARTESIAN_POINT ( 'NONE',  ( 3.995986895217980894, -0.6101256969637807170, -1.843678354830182053 ) ) ;
#185261=CARTESIAN_POINT ( 'NONE',  ( 5.870339087135666212, -1.187030499695044039, 1.445606174157453738 ) ) ;
#185263=CARTESIAN_POINT ( 'NONE',  ( 6.432970213454214381, 1.034009579150240610, 1.730599625746793935 ) ) ;
#185267=CARTESIAN_POINT ( 'NONE',  ( 4.377577386359387646, -0.4445010797573499817, -1.966645064109616481 ) ) ;
#185271=CARTESIAN_POINT ( 'NONE',  ( 1.875362892791394787, 1.747422460009705913, -0.5287960245906262458 ) ) ;
#185281=CARTESIAN_POINT ( 'NONE',  ( 5.690105174167163327, 1.204846223408085670, 1.620761788888310351 ) ) ;
#185282=CARTESIAN_POINT ( 'NONE',  ( 0.1356056236470788157, -0.09959319089659908475, 2.118264760961988458 ) ) ;
#185285=CARTESIAN_POINT ( 'NONE',  ( 4.821196345351608237, -0.1031141679418267343, 2.058443437638860285 ) ) ;
#185286=CARTESIAN_POINT ( 'NONE',  ( 4.588517629802620235, -0.5350896943857390564, 1.944070981013110933 ) ) ;
#185294=CARTESIAN_POINT ( 'NONE',  ( 4.850935385407137979, -0.9528642855485233154, 1.776740034556321568 ) ) ;
#185295=CARTESIAN_POINT ( 'NONE',  ( 3.609164914601064922, -1.813629950718143702, 0.3161406477080672128 ) ) ;
#185297=CARTESIAN_POINT ( 'NONE',  ( 2.631810907782325071, -2.152760894471450914, 0.8317484501371147365 ) ) ;
#185299=CARTESIAN_POINT ( 'NONE',  ( 4.763041337456088264, -1.928505312680216743, -0.9765951867335492809 ) ) ;
#185300=CARTESIAN_POINT ( 'NONE',  ( 3.503138892209650024, -0.1435209762444041581, 2.011451614702438828 ) ) ;
#185302=CARTESIAN_POINT ( 'NONE',  ( 0.4154419552040686248, -1.039972057064937783, -1.639973222157356636 ) ) ;
#185304=CARTESIAN_POINT ( 'NONE',  ( 3.954713598875368774, 1.661701185475419118, 1.588069724787332992 ) ) ;
#185307=CARTESIAN_POINT ( 'NONE',  ( 4.030043484472041193, 1.001115284758803625, -1.580040089582811280 ) ) ;
#185309=CARTESIAN_POINT ( 'NONE',  ( 6.403199630258991526, 1.638877779571865423, 1.095505698648422177 ) ) ;
#185313=CARTESIAN_POINT ( 'NONE',  ( 1.225528936851564721, -0.05108506852482053856, 2.206457870188942572 ) ) ;
#185320=CARTESIAN_POINT ( 'NONE',  ( 0.4562421353364953802, 0.7503462943320489131, 1.823165437449389081 ) ) ;
#185321=CARTESIAN_POINT ( 'NONE',  ( 6.639320299308884010, -2.064767919570985821, 1.030881497364994681 ) ) ;
#185322=CARTESIAN_POINT ( 'NONE',  ( 0.5550359226569913096, 1.633180182981083028, -1.086726831054436682 ) ) ;
#185323=CARTESIAN_POINT ( 'NONE',  ( 4.399324768961708543, -1.796976987717312291, 1.012281656189101264 ) ) ;
#185332=CARTESIAN_POINT ( 'NONE',  ( 6.039545795398320926, 2.008403840061912859, -0.8252953610491889913 ) ) ;
#185334=CARTESIAN_POINT ( 'NONE',  ( 5.601068772352080671, -0.4412860211496574814, 1.787476196608045464 ) ) ;
#185342=CARTESIAN_POINT ( 'NONE',  ( 1.348149404638066651, 0.9416913409402675184, -1.664245089135652611 ) ) ;
#185343=CARTESIAN_POINT ( 'NONE',  ( 1.691920373447815207, -1.760920987957525385, -0.1775098275408875104 ) ) ;
#185345=CARTESIAN_POINT ( 'NONE',  ( 6.094395157121155648, -1.075028013068216604, 1.701836141867618446 ) ) ;
#185347=CARTESIAN_POINT ( 'NONE',  ( 4.745656728581866268, 1.894139079640380086, -0.2851870984255585051 ) ) ;
#185349=CARTESIAN_POINT ( 'NONE',  ( 5.810992205472774508, -1.553620646631387991, 1.210443464816546744 ) ) ;
#185350=CARTESIAN_POINT ( 'NONE',  ( 0.3520121086563637314, -1.504009422257305495, -1.495223887398588358 ) ) ;
#185352=CARTESIAN_POINT ( 'NONE',  ( 4.381629165553334815, 1.221847395770376377, 1.416585496670008659 ) ) ;
#185353=CARTESIAN_POINT ( 'NONE',  ( 6.147054438156498435, -1.453121625630097613, 0.9290195162147057983 ) ) ;
#185355=CARTESIAN_POINT ( 'NONE',  ( 3.123846942790895476, -2.126788776302591888, 0.5888931905130634359 ) ) ;
#185358=CARTESIAN_POINT ( 'NONE',  ( 0.6782753517312088976, -1.101985112813896883, -1.743456004656674718 ) ) ;
#185365=CARTESIAN_POINT ( 'NONE',  ( 3.701679681979888503, -1.565833156357125278, -1.354537944502069102 ) ) ;
#185369=CARTESIAN_POINT ( 'NONE',  ( 0.6627674568651781284, 0.5885975752501994007, 1.931983969097182063 ) ) ;
#185373=CARTESIAN_POINT ( 'NONE',  ( 0.1749903794560566384, 0.2522965209616668814, -1.990827758811020809 ) ) ;
#185375=CARTESIAN_POINT ( 'NONE',  ( 6.837263156049210089, -1.242709075549037312, 1.588189626643407681 ) ) ;
#185376=CARTESIAN_POINT ( 'NONE',  ( 5.805858164762184082, -1.070174230454253639, -1.588719782701804695 ) ) ;
#185377=CARTESIAN_POINT ( 'NONE',  ( 6.539320575229297106, 0.5644099559201658511, 2.255290358406045303 ) ) ;
#185378=CARTESIAN_POINT ( 'NONE',  ( 3.509492838045696672, -2.158849082856160173, 0.3763758916049686487 ) ) ;
#185381=CARTESIAN_POINT ( 'NONE',  ( 3.972844611716894736, -1.413603510852480927, 1.288168406687495215 ) ) ;
#185386=CARTESIAN_POINT ( 'NONE',  ( 0.6324356828835416833, 0.5880426346329314935, 1.928746166857209676 ) ) ;
#185388=CARTESIAN_POINT ( 'NONE',  ( 5.583573808894983337, -0.9862700065477579825, 1.957137920222583372 ) ) ;
#185390=CARTESIAN_POINT ( 'NONE',  ( 2.959633327367673150, 1.716642837065301519, -0.1670560860976433859 ) ) ;
#185396=CARTESIAN_POINT ( 'NONE',  ( 1.117545225965112188, 0.3861695934333775337, -1.923310697798483293 ) ) ;
#185399=CARTESIAN_POINT ( 'NONE',  ( 0.1751657365761547513, 0.002452341591364578209, -2.044164811867712483 ) ) ;
#185402=CARTESIAN_POINT ( 'NONE',  ( 4.283730857329768327, 1.755957581118623434, -0.4444456398857503099 ) ) ;
#185406=CARTESIAN_POINT ( 'NONE',  ( 4.740750167454264918, 1.734909645891765662, 0.5210944610908369024 ) ) ;
#185410=CARTESIAN_POINT ( 'NONE',  ( 5.125394178454842020, 0.1826033194989445385, -1.852086804783218188 ) ) ;
#185412=CARTESIAN_POINT ( 'NONE',  ( 2.688967962845473458, 1.619712848077807577, 1.022445119732362961 ) ) ;
#185415=EDGE_CURVE ( 'NONE', #64278, #100328, #149110, .T. ) ;
#185422=CARTESIAN_POINT ( 'NONE',  ( 0.9024203131168639924, 1.581833000263275224, -1.367050110207337799 ) ) ;
#185424=CARTESIAN_POINT ( 'NONE',  ( 0.5690311950540331010, 0.1842100624489529104, -1.816270042949569730 ) ) ;
#185426=CARTESIAN_POINT ( 'NONE',  ( 2.590611583786633254, -0.3098195481324728107, -1.798931244660670448 ) ) ;
#185429=CARTESIAN_POINT ( 'NONE',  ( 1.732793293511214472, -1.869146454778564559, -0.6209850235064825474 ) ) ;
#185430=CARTESIAN_POINT ( 'NONE',  ( 3.772937862106290563, 1.827633595424851043, -0.6570963203050876889 ) ) ;
#185434=CARTESIAN_POINT ( 'NONE',  ( 4.553055379497691568, 0.3652949536288411791, 2.088752307168060707 ) ) ;
#185442=CARTESIAN_POINT ( 'NONE',  ( 3.510199737632841543, -0.7410081052188906003, -1.668730646197075673 ) ) ;
#185448=CARTESIAN_POINT ( 'NONE',  ( 4.856247981345184428, 0.7163626499266174674, 1.728251504774950709 ) ) ;
#185450=CARTESIAN_POINT ( 'NONE',  ( 1.787598692544673851, 1.328180555690385845, 1.395690353023341101 ) ) ;
#185458=CARTESIAN_POINT ( 'NONE',  ( 0.9841680404778062607, -2.117403155482136423, 0.004310642112759220310 ) ) ;
#185462=CARTESIAN_POINT ( 'NONE',  ( 6.385608392048681026, -1.951384585020640383, 0.6918703269920488674 ) ) ;
#185463=CARTESIAN_POINT ( 'NONE',  ( 0.6437974683802077935, 0.5340323341261629109, 1.762076181610471526 ) ) ;
#185465=CARTESIAN_POINT ( 'NONE',  ( 6.434253291069976122, -1.843495385113643525, -1.373021106398547131 ) ) ;
#185468=CARTESIAN_POINT ( 'NONE',  ( 1.219134843238580235, -0.05193690637114551506, 2.291835786607650416 ) ) ;
#185471=CARTESIAN_POINT ( 'NONE',  ( 6.492136518976993287, -0.5202676277693082385, -1.870896455867506747 ) ) ;
#185474=CARTESIAN_POINT ( 'NONE',  ( 6.504189997394580480, -0.8109953713257547214, 1.730197269205424160 ) ) ;
#185475=CARTESIAN_POINT ( 'NONE',  ( 6.333220217719927270, -1.622483202430196725, -1.197309987464048486 ) ) ;
#185478=CARTESIAN_POINT ( 'NONE',  ( 2.941443032221033427, 0.7519493320215028254, -1.950910760374990671 ) ) ;
#185479=CARTESIAN_POINT ( 'NONE',  ( 1.639140867700689785, -1.278921918198316465, -1.223650632631252622 ) ) ;
#185482=CARTESIAN_POINT ( 'NONE',  ( 4.558679923290005043, -2.046282147472633373, -1.033175111039591698 ) ) ;
#185483=CARTESIAN_POINT ( 'NONE',  ( 3.310250384734690243, 1.573932026098995518, 0.7429073729697617257 ) ) ;
#185486=CARTESIAN_POINT ( 'NONE',  ( 3.866272716362227690, -0.5049011280162157833, 1.658656615756588959 ) ) ;
#185487=CARTESIAN_POINT ( 'NONE',  ( 3.719319017856066445, -1.913190415241170728, -1.026542932298198485 ) ) ;
#185489=CARTESIAN_POINT ( 'NONE',  ( 4.329314735043091389, -1.561880650076686861, -1.275557594027726394 ) ) ;
#185490=CARTESIAN_POINT ( 'NONE',  ( 3.468750000000001776, 0.7852924748298147906, -1.895863743164155180 ) ) ;
#185493=CARTESIAN_POINT ( 'NONE',  ( 2.397378046164869936, 1.487928659643242169, 1.223526803071661950 ) ) ;
#185495=CARTESIAN_POINT ( 'NONE',  ( 4.570683916498400556, 0.8515115505445168820, 2.051917206062872978 ) ) ;
#185502=CARTESIAN_POINT ( 'NONE',  ( 0.3643397115577310941, 0.6907578271265965020, -2.111251545739430302 ) ) ;
#185504=CARTESIAN_POINT ( 'NONE',  ( 5.635196431686764207, -0.04651148872366302894, -1.961470878453225763 ) ) ;
#185507=CARTESIAN_POINT ( 'NONE',  ( 0.2808502495336914206, -2.096634173354972486, -0.5254431554712820640 ) ) ;
#185510=CARTESIAN_POINT ( 'NONE',  ( 3.156738326643961923, -0.5960753502360670586, -1.974691822637637761 ) ) ;
#185514=CARTESIAN_POINT ( 'NONE',  ( 5.202362286721474050, -0.6290170809866748591, -1.761763226176292996 ) ) ;
#185515=CARTESIAN_POINT ( 'NONE',  ( 5.256420022722958052, 1.669015333217665820, -0.4704954288548191532 ) ) ;
#185516=CARTESIAN_POINT ( 'NONE',  ( 3.052039328023182119, -1.315916573227500219, 1.139148930295554862 ) ) ;
#185517=CARTESIAN_POINT ( 'NONE',  ( 0.4688447829373428855, -2.161134926827886549, -0.7649225765839831048 ) ) ;
#185519=CARTESIAN_POINT ( 'NONE',  ( 5.759345132242938092, 2.059656548118168562, -0.3582877099650525476 ) ) ;
#185520=CARTESIAN_POINT ( 'NONE',  ( 6.439402819763696328, 0.7408549094962694204, -1.795268486070795477 ) ) ;
#185523=CARTESIAN_POINT ( 'NONE',  ( 1.336564801266389990, 0.5826540126645517459, -1.930418273149013153 ) ) ;
#185524=CARTESIAN_POINT ( 'NONE',  ( 0.1467655724766807612, -1.757430454515636509, 1.308964887167404889 ) ) ;
#185528=CARTESIAN_POINT ( 'NONE',  ( 2.455864667332839257, -1.573010975769023601, -1.422207447652395373 ) ) ;
#185530=CARTESIAN_POINT ( 'NONE',  ( 4.986841741376339066, -0.2268417095559888130, -1.811474396668552700 ) ) ;
#185537=CARTESIAN_POINT ( 'NONE',  ( 2.478776341996299593, -1.389826682745049835, 1.465835156725032506 ) ) ;
#185538=CARTESIAN_POINT ( 'NONE',  ( 0.3761801408644695477, 1.212865950663596371, 1.721436218156185305 ) ) ;
#185540=CARTESIAN_POINT ( 'NONE',  ( 4.065176880270331417, 1.594224420893322725, 0.9597675150698461444 ) ) ;
#185547=CARTESIAN_POINT ( 'NONE',  ( 5.303274670167754223, 1.494737065598227943, 1.048009559513597866 ) ) ;
#185551=CARTESIAN_POINT ( 'NONE',  ( 1.545803854144804479, 1.604466568860075437, -0.6577250193331334316 ) ) ;
#185552=CARTESIAN_POINT ( 'NONE',  ( 0.5502397958263847144, -1.467719461762364341, -0.9348402994967041080 ) ) ;
#185553=CARTESIAN_POINT ( 'NONE',  ( 5.092513741553108986, -2.289745732339975692, -0.2867506301261530388 ) ) ;
#185556=CARTESIAN_POINT ( 'NONE',  ( 1.739600335799436737, -1.490509515545968666, -1.423327880080206720 ) ) ;
#185558=CARTESIAN_POINT ( 'NONE',  ( 6.485746271079104730, 2.140961846981633609, 0.8364165754714718570 ) ) ;
#185561=CARTESIAN_POINT ( 'NONE',  ( 6.666881909320486521, -1.711340306973156977, -0.7558587634414122292 ) ) ;
#185562=CARTESIAN_POINT ( 'NONE',  ( 3.955252344019274169, -1.661368509396843995, 0.9470704235666274062 ) ) ;
#185564=CARTESIAN_POINT ( 'NONE',  ( 5.180388087185870738, -1.228261608319089149, 1.833297759731546073 ) ) ;
#185569=CARTESIAN_POINT ( 'NONE',  ( 6.287751673603878544, 2.029294879081492198, -0.6150919484220889188 ) ) ;
#185571=CARTESIAN_POINT ( 'NONE',  ( 4.014917937017292715, 1.634369553669342778, -1.629294119824703069 ) ) ;
#185572=CARTESIAN_POINT ( 'NONE',  ( 3.842202535371820993, -0.9690557767615382012, 1.705768119890891610 ) ) ;
#185574=CARTESIAN_POINT ( 'NONE',  ( 0.8132426064601482318, -1.654215606812576400, -1.054277637385622857 ) ) ;
#185578=CARTESIAN_POINT ( 'NONE',  ( 5.805875103277515770, -1.124240986939632592, -1.673857227857282082 ) ) ;
#185581=CARTESIAN_POINT ( 'NONE',  ( 2.659224658930594121, 1.746150167319389990, -1.290005652201154263 ) ) ;
#185584=CARTESIAN_POINT ( 'NONE',  ( 0.4574861729177078229, -1.815669959853306370, 1.095388807130371900 ) ) ;
#185590=CARTESIAN_POINT ( 'NONE',  ( 1.598976361298432014, 1.686402000465867301, -1.184152512226148923 ) ) ;
#185596=CARTESIAN_POINT ( 'NONE',  ( 4.600206319907148789, -0.8982956317880007591, 1.688143452400918454 ) ) ;
#185600=CARTESIAN_POINT ( 'NONE',  ( 0.4393641590584134171, -1.719983824569010444, 0.5688467837753272693 ) ) ;
#185602=CARTESIAN_POINT ( 'NONE',  ( 0.4443725376216747236, -1.385435448976629180, 1.323305594895395343 ) ) ;
#185603=CARTESIAN_POINT ( 'NONE',  ( 2.365759603224312446, -0.4558734232973959966, 2.019384234097781228 ) ) ;
#185605=CARTESIAN_POINT ( 'NONE',  ( 0.2331951027847931901, -1.803461566636242797, 0.7967608462288151561 ) ) ;
#185606=CARTESIAN_POINT ( 'NONE',  ( 3.035583632137848653, -1.226507576337819483, -1.352503160878690380 ) ) ;
#185607=CARTESIAN_POINT ( 'NONE',  ( 6.322910218073367616, 2.057572540570989261, 0.7984293639632376038 ) ) ;
#185611=CARTESIAN_POINT ( 'NONE',  ( 4.264169596968480747, -2.057349986699669397, 0.1488187104187361498 ) ) ;
#185615=CARTESIAN_POINT ( 'NONE',  ( 5.456126526903398499, 2.103703387787753343, -0.1000602029373430374 ) ) ;
#185618=CARTESIAN_POINT ( 'NONE',  ( 6.232888004217203459, -1.964670499678453197, -0.6532144590316590893 ) ) ;
#185620=CARTESIAN_POINT ( 'NONE',  ( 3.638091081701349871, 0.9754702174074175725, -1.929073278114090684 ) ) ;
#185621=CARTESIAN_POINT ( 'NONE',  ( 3.879560801468981523, 0.2449043481074340001, -2.004685163654993385 ) ) ;
#185626=CARTESIAN_POINT ( 'NONE',  ( 2.747280062631300535, 0.2910806042949847239, -1.995268371848608835 ) ) ;
#185634=CARTESIAN_POINT ( 'NONE',  ( 4.868767636308747093, -0.2496254991312534810, -2.000855965115163837 ) ) ;
#185637=CARTESIAN_POINT ( 'NONE',  ( 0.1347971297303695026, -1.579520332396977089, 0.6935263066737175075 ) ) ;
#185642=CARTESIAN_POINT ( 'NONE',  ( 5.764887228985436707, -1.690807747980655584, -0.8004016547063924625 ) ) ;
#185643=CARTESIAN_POINT ( 'NONE',  ( 0.08268127059449237315, -1.313209137626596634, 1.525886470183013044 ) ) ;
#185649=CARTESIAN_POINT ( 'NONE',  ( 1.142204091441896718, 0.8197918422115093584, 1.842440257734210052 ) ) ;
#185656=CARTESIAN_POINT ( 'NONE',  ( 6.239839116978105338, 1.910102730490463641, -0.1462054744419109820 ) ) ;
#185665=CARTESIAN_POINT ( 'NONE',  ( 3.749029689823797806, -1.768526636652943296, 1.242828150824742961 ) ) ;
#185668=CARTESIAN_POINT ( 'NONE',  ( 0.9672155168029163974, -1.668165459610539081, 1.309123814877902969 ) ) ;
#185669=CARTESIAN_POINT ( 'NONE',  ( 5.385714059857480862, 1.227405483141888354, 1.351559456777707835 ) ) ;
#185670=CARTESIAN_POINT ( 'NONE',  ( 2.635955087654485940, 0.9327151613215716175, -1.736774642614127284 ) ) ;
#185671=CARTESIAN_POINT ( 'NONE',  ( 4.359561026920276916, -1.481784043772149229, -1.208992945495937610 ) ) ;
#185672=VERTEX_POINT ( 'NONE', #58881 ) ;
#185674=CARTESIAN_POINT ( 'NONE',  ( 5.758249387092365446, -1.969739562807392819, -0.001740234774137705337 ) ) ;
#185675=CARTESIAN_POINT ( 'NONE',  ( 0.2869206542332564114, 1.438414604794725049, 1.304842588618974952 ) ) ;
#185681=CARTESIAN_POINT ( 'NONE',  ( 4.617770051018644573, -0.5065499601877522240, 1.843912185298258066 ) ) ;
#185683=CARTESIAN_POINT ( 'NONE',  ( 0.9212656856641410208, 2.039593612490635532, 0.8430313063367624871 ) ) ;
#185685=CARTESIAN_POINT ( 'NONE',  ( 6.076820132975093713, -1.421968828841757126, 1.425219213311772926 ) ) ;
#185686=CARTESIAN_POINT ( 'NONE',  ( -0.02319159430949970999, 4.096340798889516854, -2.366022381217198767 ) ) ;
#185689=CARTESIAN_POINT ( 'NONE',  ( 2.699741690289765295, -1.532448122638006671, -1.392287113214360605 ) ) ;
#185693=CARTESIAN_POINT ( 'NONE',  ( 0.8136072859011161951, -0.3160970183575459447, 2.138355382504661506 ) ) ;
#185699=CARTESIAN_POINT ( 'NONE',  ( 5.414640894582111841, -1.106827951885097638, -1.334981224695269475 ) ) ;
#185701=CARTESIAN_POINT ( 'NONE',  ( 3.309495622959734096, -1.689761761210720525, -1.195817184978978043 ) ) ;
#185702=CARTESIAN_POINT ( 'NONE',  ( 4.622735098982394319, 0.3634473554468270473, 2.085661844363582595 ) ) ;
#185705=CARTESIAN_POINT ( 'NONE',  ( 2.500782807205007341, 0.4266943614082556180, 1.922505800989605218 ) ) ;
#185706=CARTESIAN_POINT ( 'NONE',  ( 1.371198541116287917, -1.641758494746584418, -0.9804709962101465504 ) ) ;
#185707=CARTESIAN_POINT ( 'NONE',  ( 4.962941676929116142, 0.2283445767556212536, -2.280853557871139525 ) ) ;
#185708=CARTESIAN_POINT ( 'NONE',  ( 2.947667120405720986, 0.6567698719579934119, -1.703645827024417914 ) ) ;
#185712=CARTESIAN_POINT ( 'NONE',  ( 4.535406599088565471, -0.09463749723611977749, 2.011077795214308406 ) ) ;
#185713=CARTESIAN_POINT ( 'NONE',  ( 2.746866186719683967, -0.3305370478365337039, -1.933541032166598672 ) ) ;
#185717=CARTESIAN_POINT ( 'NONE',  ( 0.07536363704233400851, 2.864322694550157866, -2.632457840217194089 ) ) ;
#185718=CARTESIAN_POINT ( 'NONE',  ( 6.228480176075449570, 0.2035102421588113053, 2.080708833908810451 ) ) ;
#185719=CARTESIAN_POINT ( 'NONE',  ( 4.363939919551316216, 0.8349522575829392279, 1.560488599360178474 ) ) ;
#185721=CARTESIAN_POINT ( 'NONE',  ( 0.6038064816080711550, -2.180521553291506986, 0.2185767975278959385 ) ) ;
#185722=CARTESIAN_POINT ( 'NONE',  ( 0.1689663589281220069, 0.9994598401263864451, 1.424626921871420926 ) ) ;
#185725=CARTESIAN_POINT ( 'NONE',  ( 0.3691051123158794467, -0.6094954538576388137, 2.216020297015007134 ) ) ;
#185726=CARTESIAN_POINT ( 'NONE',  ( 0.3456114054924685486, 0.6817542107791437767, -2.082909237240769151 ) ) ;
#185727=CARTESIAN_POINT ( 'NONE',  ( 6.819718782980952909, -1.336886906709513712, 1.104006757392479887 ) ) ;
#185728=CARTESIAN_POINT ( 'NONE',  ( 3.000804911251079510, -0.6410980074830170405, -2.111705341948390657 ) ) ;
#185729=CARTESIAN_POINT ( 'NONE',  ( 6.549308719555964053, 1.892307808498715049, -1.064380946037797093 ) ) ;
#185731=CARTESIAN_POINT ( 'NONE',  ( 1.235738130824210357, 0.6087300624019938988, -2.027988197625143929 ) ) ;
#185732=CARTESIAN_POINT ( 'NONE',  ( 3.968750000000002665, 0.7852924748297764879, -1.895863743164168724 ) ) ;
#185733=CARTESIAN_POINT ( 'NONE',  ( 6.727182134110176293, 6.032839922080010631, 2.883943260000087605 ) ) ;
#185734=CARTESIAN_POINT ( 'NONE',  ( 5.016589502704805525, 1.328544886203905318, -1.395186341261208884 ) ) ;
#185736=CARTESIAN_POINT ( 'NONE',  ( 1.453083402393087642, -1.969018001514400540, -1.173635730923931808 ) ) ;
#185740=CARTESIAN_POINT ( 'NONE',  ( 3.299698294838341539, 2.007417196159299255, -0.9513305067451423014 ) ) ;
#185747=CARTESIAN_POINT ( 'NONE',  ( 2.180314765559120183, 1.560501322096979449, 1.277041908422072991 ) ) ;
#185749=CARTESIAN_POINT ( 'NONE',  ( 6.478975546884585768, 1.923237475310497047, 0.7459448616168369295 ) ) ;
#185752=CARTESIAN_POINT ( 'NONE',  ( 6.321804186586025942, 0.9940233051523542640, -1.428469917405380318 ) ) ;
#185755=CARTESIAN_POINT ( 'NONE',  ( 2.582953972192280734, 1.619985402465830671, -0.7128798769604760555 ) ) ;
#185756=CARTESIAN_POINT ( 'NONE',  ( 1.231092510272915552, 2.014232830173094513, 0.09613330637052441840 ) ) ;
#185757=CARTESIAN_POINT ( 'NONE',  ( 0.4679805871025365382, -1.733519288248483559, -0.6209854868195128219 ) ) ;
#185758=CARTESIAN_POINT ( 'NONE',  ( 5.724266765471021756, 2.208406811287708660, 0.6146092054917261516 ) ) ;
#185759=CARTESIAN_POINT ( 'NONE',  ( 2.923586578878138109, 1.022379729796508041, -1.530975008504284141 ) ) ;
#185762=CARTESIAN_POINT ( 'NONE',  ( 3.821172736587064023, -0.1348131347885111742, 1.820669774636254346 ) ) ;
#185763=CARTESIAN_POINT ( 'NONE',  ( 5.309220276109914316, 1.198862193007979471, -1.621181151826488254 ) ) ;
#185765=CARTESIAN_POINT ( 'NONE',  ( 3.081239027650189310, -0.1650901621712965450, -2.256537306257479614 ) ) ;
#185767=CARTESIAN_POINT ( 'NONE',  ( 6.159223736743516753, -1.804415119744419149, -1.085654967431331164 ) ) ;
#185769=CARTESIAN_POINT ( 'NONE',  ( 3.244645865714153032, -2.039272935636734285, -0.3565889006169955522 ) ) ;
#185772=CARTESIAN_POINT ( 'NONE',  ( 5.690118541956746157, 1.263103799472656164, 1.703077153987264669 ) ) ;
#185775=CARTESIAN_POINT ( 'NONE',  ( 2.209485269003717445, -0.4220890577730853632, 1.879544223609790565 ) ) ;
#185777=CARTESIAN_POINT ( 'NONE',  ( 6.420757345757475143, -1.395243968761919362, 1.390232514205336001 ) ) ;
#185781=CARTESIAN_POINT ( 'NONE',  ( 0.2643399247034176613, 0.6888887472211238094, -2.111998681152967183 ) ) ;
#185782=CARTESIAN_POINT ( 'NONE',  ( 3.803828919190560764, -0.6134138247068477989, 2.014629399117270125 ) ) ;
#185785=CARTESIAN_POINT ( 'NONE',  ( 0.5021285002191768765, 1.855665429770089636, 0.1426183976328247727 ) ) ;
#185791=CARTESIAN_POINT ( 'NONE',  ( 1.125412309253082332, 1.872817075645373697, 0.9946839901537674056 ) ) ;
#185794=CARTESIAN_POINT ( 'NONE',  ( 4.351973852746993110, -0.7528527933186466292, 1.811862133468461922 ) ) ;
#185795=CARTESIAN_POINT ( 'NONE',  ( 1.622176833581047806, -1.201014165160016356, -1.797165035535647659 ) ) ;
#185796=CARTESIAN_POINT ( 'NONE',  ( 2.138008341990283778, 0.4048980806483238326, 1.796005048712509655 ) ) ;
#185800=CARTESIAN_POINT ( 'NONE',  ( 4.031004160980892870, -1.202209430963938619, -1.258585379614601596 ) ) ;
#185804=CARTESIAN_POINT ( 'NONE',  ( 0.5499753625364013354, 0.6768306982547143136, -2.053065283773393368 ) ) ;
#185805=CARTESIAN_POINT ( 'NONE',  ( 3.620470095612156047, 0.4925664443866035191, -1.954873191151075940 ) ) ;
#185808=CARTESIAN_POINT ( 'NONE',  ( 3.344560887785383851, 0.4775036937760200884, 1.912655531573831835 ) ) ;
#185810=CARTESIAN_POINT ( 'NONE',  ( 6.609000000000018638, 2.976782768882420438, 2.353557172130323227 ) ) ;
#185811=CARTESIAN_POINT ( 'NONE',  ( 2.612754452619329371, -0.1881026344860724786, 1.932912858947251511 ) ) ;
#185812=CARTESIAN_POINT ( 'NONE',  ( 6.469012471580376733, -1.473683540339595810, 1.218514635347216046 ) ) ;
#185821=CARTESIAN_POINT ( 'NONE',  ( 0.5170026063063514199, 1.520138765826519300, -1.599913083071627273 ) ) ;
#185823=CARTESIAN_POINT ( 'NONE',  ( 4.680490258543752446, 1.210089798712219222, -1.543956201849092658 ) ) ;
#185825=CARTESIAN_POINT ( 'NONE',  ( 1.881482635453747720, -0.5404922439061732309, -1.942541187959702764 ) ) ;
#185827=CARTESIAN_POINT ( 'NONE',  ( 2.202504513770195516, 1.378945901905674232, -1.606877091071600816 ) ) ;
#185831=CARTESIAN_POINT ( 'NONE',  ( 3.450948914068392881, 0.4461466885457600062, -1.786139022923169506 ) ) ;
#185835=CARTESIAN_POINT ( 'NONE',  ( 4.324552338190708056, -0.9094542848507057853, -1.915842285305848769 ) ) ;
#185838=CARTESIAN_POINT ( 'NONE',  ( 5.360643824631334375, -1.495535663558609674, 1.418079957933044755 ) ) ;
#185840=CARTESIAN_POINT ( 'NONE',  ( 2.753256032281672372, 1.832158412346639453, -0.1828795585285883096 ) ) ;
#185847=CARTESIAN_POINT ( 'NONE',  ( 1.911028901235469313, 1.633884665098099598, -1.483674895440662667 ) ) ;
#185848=CARTESIAN_POINT ( 'NONE',  ( 4.200629628819559258, -0.7044727654359562719, -2.150022973637927048 ) ) ;
#185850=CARTESIAN_POINT ( 'NONE',  ( 3.199259029290311140, 1.635763741490828593, -0.7788767334107206119 ) ) ;
#185851=CARTESIAN_POINT ( 'NONE',  ( 4.346842662630929333, -1.713972709756344859, -0.8558225519783541069 ) ) ;
#185853=CARTESIAN_POINT ( 'NONE',  ( 4.241065053910620719, -1.715758787085974957, 0.9708604712577516560 ) ) ;
#185854=CARTESIAN_POINT ( 'NONE',  ( 0.5164664324388609229, 1.330803901959699997, -1.393038531337851493 ) ) ;
#185855=CARTESIAN_POINT ( 'NONE',  ( 4.996879044411707937, 1.554903924810165705, -1.039696167511289238 ) ) ;
#185856=CARTESIAN_POINT ( 'NONE',  ( 3.668876216774307863, -1.550535085938867352, 1.709345553852769095 ) ) ;
#185857=CARTESIAN_POINT ( 'NONE',  ( 5.389040371011321717, 0.1367655989435011543, 1.856064314752596145 ) ) ;
#185861=CARTESIAN_POINT ( 'NONE',  ( 1.647240615436126543, -1.778467030350115774, 1.127781350514756475 ) ) ;
#185865=CARTESIAN_POINT ( 'NONE',  ( 2.795306286867365486, -0.1602278063087131110, -2.114629986603839829 ) ) ;
#185867=CARTESIAN_POINT ( 'NONE',  ( 1.054951293920348698, 0.3981946776167448188, 1.979963216457211850 ) ) ;
#185871=CARTESIAN_POINT ( 'NONE',  ( 1.739762150092131643, -1.564342989677082629, -1.491970722459233345 ) ) ;
#185872=CARTESIAN_POINT ( 'NONE',  ( 6.610000000000006537, 7.629137130509094256, 2.600000000000001421 ) ) ;
#185874=DIRECTION ( 'NONE',  ( 1.039099362110107450E-15, 1.000000000000000000, -4.583713267641621330E-32 ) ) ;
#185877=CARTESIAN_POINT ( 'NONE',  ( 5.665250009225348826, 1.861346387706263261, -0.7762253298396750711 ) ) ;
#185880=CARTESIAN_POINT ( 'NONE',  ( 0.01162390915069450026, -2.148011843722149372, 0.4338911918742721641 ) ) ;
#185882=CARTESIAN_POINT ( 'NONE',  ( 0.9544393508495727652, 2.259765469927646375, -0.1136819296270324686 ) ) ;
#185885=EDGE_CURVE ( 'NONE', #89432, #40908, #74022, .T. ) ;
#185890=CARTESIAN_POINT ( 'NONE',  ( 4.195721234439112379, -0.6572638427989171417, 1.594953032058670894 ) ) ;
#185892=CARTESIAN_POINT ( 'NONE',  ( 1.844620604044054035, -1.498293487275937697, 0.9415191625909284934 ) ) ;
#185893=CARTESIAN_POINT ( 'NONE',  ( 4.981566806912656631, 2.060606067865732527, -0.7902562557115796471 ) ) ;
#185895=CARTESIAN_POINT ( 'NONE',  ( 3.849871613625083899, -1.395920841890609498, -1.459997210279185831 ) ) ;
#185897=CARTESIAN_POINT ( 'NONE',  ( 4.863993733624056404, 0.6645719631460760279, -2.013739200842738608 ) ) ;
#185898=CARTESIAN_POINT ( 'NONE',  ( 3.585564690064909854, -0.5826378547920657569, 1.930424337232887977 ) ) ;
#185899=CARTESIAN_POINT ( 'NONE',  ( 4.183730900115702589, 1.755568954123175596, -0.4464138967742969366 ) ) ;
#185902=CARTESIAN_POINT ( 'NONE',  ( 1.182252951876180180, -1.824241171369020531, -0.4133900166373091767 ) ) ;
#185904=CARTESIAN_POINT ( 'NONE',  ( 6.533875575962896143, -1.755123972569608615, 0.4478894030855648523 ) ) ;
#185910=CARTESIAN_POINT ( 'NONE',  ( 0.1231139863388103495, 1.664874722635242277, 0.9407772870168448209 ) ) ;
#185913=CARTESIAN_POINT ( 'NONE',  ( 2.014041202081144011, 1.956828179156915315, -0.1411808619533050091 ) ) ;
#185916=CARTESIAN_POINT ( 'NONE',  ( 3.726904977748810577, 1.497142547446396410, -1.502090761940577002 ) ) ;
#185918=CARTESIAN_POINT ( 'NONE',  ( 5.044191579798307679, 1.965876612296811654, 0.1480472272742116568 ) ) ;
#185920=CARTESIAN_POINT ( 'NONE',  ( 0.8264323289940983530, -0.9090603351678091526, -1.796376205119714298 ) ) ;
#185921=ORIENTED_EDGE ( 'NONE', *, *, #85262, .F. ) ;
#185922=CARTESIAN_POINT ( 'NONE',  ( 1.388444276177196235, -0.7657061372807508759, -1.974083799386998406 ) ) ;
#185924=CARTESIAN_POINT ( 'NONE',  ( 2.277862540309500083, -2.008769142935047380, 0.5008063122204224893 ) ) ;
#185927=VERTEX_POINT ( 'NONE', #196355 ) ;
#185928=CARTESIAN_POINT ( 'NONE',  ( 5.173812367756161379, -1.161941297927127525, 1.737786252440294055 ) ) ;
#185930=CARTESIAN_POINT ( 'NONE',  ( 3.328933297416610593, 0.04358344136132231289, 1.825221112333124340 ) ) ;
#185931=CARTESIAN_POINT ( 'NONE',  ( 1.752323211514599688, 1.791785093909546323, 0.2653131528348381396 ) ) ;
#185933=CARTESIAN_POINT ( 'NONE',  ( 6.305322857734435793, 1.832379230283949667, 1.229636283518860118 ) ) ;
#185936=CARTESIAN_POINT ( 'NONE',  ( 5.596761079150560647, -0.5311557606857522096, -2.141783596114990917 ) ) ;
#185940=CARTESIAN_POINT ( 'NONE',  ( 3.984940423737866055, -1.785409543757199291, -0.6854135386504257577 ) ) ;
#185945=CARTESIAN_POINT ( 'NONE',  ( 6.268043187460373922, -2.055199631210804068, 0.2494731385529954104 ) ) ;
#185947=CARTESIAN_POINT ( 'NONE',  ( 6.075747529084263299, -1.173811750163206158, 1.850510016281024850 ) ) ;
#185954=EDGE_CURVE ( 'NONE', #103946, #57811, #84514, .T. ) ;
#185955=CARTESIAN_POINT ( 'NONE',  ( 3.444469828353762697, 0.4513171681363346011, 1.815172769691273613 ) ) ;
#185956=CARTESIAN_POINT ( 'NONE',  ( -0.02319159430949970652, 2.891346550825596218, -2.299931007135449512 ) ) ;
#185960=CARTESIAN_POINT ( 'NONE',  ( 6.543811353064236336, 1.423268159695538326, 1.503672778047180358 ) ) ;
#185961=CARTESIAN_POINT ( 'NONE',  ( 0.7027501817156033281, 1.864177386631181044, 0.7691025790682111118 ) ) ;
#185965=CARTESIAN_POINT ( 'NONE',  ( 1.078377591563362436, -2.138745004354754897, -0.4770250503970187572 ) ) ;
#185966=CARTESIAN_POINT ( 'NONE',  ( 5.988856447087388624, -0.2726756491404982441, -1.805090154579996442 ) ) ;
#185973=CARTESIAN_POINT ( 'NONE',  ( 4.212339636135824961, 1.685202893791247769, 0.7422218904534692019 ) ) ;
#185974=CARTESIAN_POINT ( 'NONE',  ( 1.190090860395363492, 1.200783890555771283, 1.615600688039710020 ) ) ;
#185975=CARTESIAN_POINT ( 'NONE',  ( 2.056460162951703197, 1.999754300726686029, -1.132793482217157033 ) ) ;
#185977=CARTESIAN_POINT ( 'NONE',  ( 6.139501739389007007, 1.813922436357641388, -0.7475906808915923074 ) ) ;
#185980=CARTESIAN_POINT ( 'NONE',  ( 4.201352949932454450, 1.705870964349815333, -0.8646410313453978258 ) ) ;
#185984=CARTESIAN_POINT ( 'NONE',  ( 3.175413592762990067, 1.328342846777453845, 1.614508523670985740 ) ) ;
#185985=CARTESIAN_POINT ( 'NONE',  ( 2.588565208901713266, -0.3177388942022137397, -1.843305967786903032 ) ) ;
#185988=CARTESIAN_POINT ( 'NONE',  ( 2.999246388560794951, -1.738348057599903074, 0.08809733484680536131 ) ) ;
#185992=CARTESIAN_POINT ( 'NONE',  ( 4.266008093515370803, 0.8158808812368329999, 1.519711535667643609 ) ) ;
#185993=CARTESIAN_POINT ( 'NONE',  ( 4.089532599075940134, -0.8378280566024614018, 2.025282237563410526 ) ) ;
#185994=CARTESIAN_POINT ( 'NONE',  ( 6.533804136697315634, -1.437950210024591780, -1.674183229976949905 ) ) ;
#185996=CARTESIAN_POINT ( 'NONE',  ( 3.854478708947015164, -2.168323188329326801, -0.1120144502513506779 ) ) ;
#185997=CARTESIAN_POINT ( 'NONE',  ( 1.717148762710469789, -0.2249250470785572054, 1.811706739299999924 ) ) ;
#185999=CARTESIAN_POINT ( 'NONE',  ( 4.469977352714805008, -0.9950975051371075963, 1.868896417504315677 ) ) ;
#186002=CARTESIAN_POINT ( 'NONE',  ( 4.511445251964079084, -2.248337965441957742, 0.4463705457610280258 ) ) ;
#186004=CARTESIAN_POINT ( 'NONE',  ( 6.620655732516647518, 7.053381450551401421, 2.424417106520880161 ) ) ;
#186006=CARTESIAN_POINT ( 'NONE',  ( 0.7332529803791461021, 1.960763319057107879, 0.8078710241638600298 ) ) ;
#186013=CARTESIAN_POINT ( 'NONE',  ( 5.643203987388664800, 0.8197706014990979728, 1.842448445624145226 ) ) ;
#186015=CARTESIAN_POINT ( 'NONE',  ( 4.944214452789121417, -0.9770834884576683477, 1.816490783314741231 ) ) ;
#186017=CARTESIAN_POINT ( 'NONE',  ( -0.2409995289980003397, 0.7158067089181943121, -2.082568332340509087 ) ) ;
#186021=CARTESIAN_POINT ( 'NONE',  ( 0.1993191639408486426, -0.5556045495253292277, 2.015383906575985318 ) ) ;
#186022=CARTESIAN_POINT ( 'NONE',  ( 4.834611377684539413, 0.6298767044488963185, -1.915599524792414465 ) ) ;
#186023=CARTESIAN_POINT ( 'NONE',  ( 3.808014051635350672, 1.299385917162833692, -1.304790556973287163 ) ) ;
#186027=CARTESIAN_POINT ( 'NONE',  ( 0.2347969022384633897, -1.580228140511737100, 0.6916409326972148275 ) ) ;
#186030=CARTESIAN_POINT ( 'NONE',  ( 0.6515572338587878320, 1.139979866233470807, 1.996073129511093169 ) ) ;
#186032=CARTESIAN_POINT ( 'NONE',  ( 6.332949636392265269, 0.2142684956521986317, 2.252356394309730003 ) ) ;
#186033=CARTESIAN_POINT ( 'NONE',  ( 3.440152538952054861, 0.9466726917620759130, -1.881381795136138679 ) ) ;
#186037=SURFACE_STYLE_USAGE ( .BOTH. , #201212 ) ;
#186043=CARTESIAN_POINT ( 'NONE',  ( 2.461320219219771843, -1.760565900816572826, 1.181798851529712646 ) ) ;
#186044=CARTESIAN_POINT ( 'NONE',  ( 3.551236150222897958, 0.3290391446359001715, 2.196816492004387111 ) ) ;
#186045=CARTESIAN_POINT ( 'NONE',  ( 1.869323357045350686, 2.096458975851514861, -0.6381942758529115522 ) ) ;
#186048=CARTESIAN_POINT ( 'NONE',  ( 5.793401095800717826, -1.774274828963496198, 0.8374297333502839225 ) ) ;
#186053=CARTESIAN_POINT ( 'NONE',  ( 4.816704082729271086, -0.7169179515637627009, -1.995842421597990413 ) ) ;
#186059=CARTESIAN_POINT ( 'NONE',  ( 5.618664544990171095, -0.03892770779775727580, 1.841008343696965310 ) ) ;
#186062=CARTESIAN_POINT ( 'NONE',  ( 0.9600616587607477825, -1.572830678042375974, -0.7454570610717390355 ) ) ;
#186066=CARTESIAN_POINT ( 'NONE',  ( 4.909125497034264818, 1.879091090907711425, 1.068517025386829467 ) ) ;
#186071=CARTESIAN_POINT ( 'NONE',  ( 5.049776242366147194, 0.6816224847111511664, -2.051488706027407183 ) ) ;
#186072=CARTESIAN_POINT ( 'NONE',  ( 5.307875201598577064, -1.962095876955988638, 0.1906144227653387424 ) ) ;
#186073=CARTESIAN_POINT ( 'NONE',  ( 4.094866968876837987, 0.9280426781237434142, -1.464329598137555477 ) ) ;
#186075=CARTESIAN_POINT ( 'NONE',  ( 0.7147126110796617748, 2.027027023440019171, 0.8336157706642086662 ) ) ;
#186076=CARTESIAN_POINT ( 'NONE',  ( 1.817812757297363691, -0.2812075768990837665, 2.290339019377229945 ) ) ;
#186077=CARTESIAN_POINT ( 'NONE',  ( 3.655589845848466801, 0.5043569952981543647, -1.997962123967106374 ) ) ;
#186078=CARTESIAN_POINT ( 'NONE',  ( 6.216353431943378638, 1.813724785205795609, 0.6947406154040984827 ) ) ;
#186086=CARTESIAN_POINT ( 'NONE',  ( 3.610573252990852744, -0.8922430012947217826, -2.018528625508857921 ) ) ;
#186089=CARTESIAN_POINT ( 'NONE',  ( 0.7954780101973528694, -1.310620071111982421, -1.321417528198569613 ) ) ;
#186090=CARTESIAN_POINT ( 'NONE',  ( -0.1288028175206544224, 1.298820314038674928, -2.522219681210400744 ) ) ;
#186094=CARTESIAN_POINT ( 'NONE',  ( 6.825078400183568483, -0.002763825414428457399, 2.044262525762724270 ) ) ;
#186097=CARTESIAN_POINT ( 'NONE',  ( 2.799741500914772807, -0.6479443615096942555, 1.956441213939211554 ) ) ;
#186103=CARTESIAN_POINT ( 'NONE',  ( 1.481398948507294477, 1.904550386266171902, -0.7878645111692607061 ) ) ;
#186108=CARTESIAN_POINT ( 'NONE',  ( 5.813141826352885566, 1.944573597739504889, 1.043518232037063287 ) ) ;
#186109=CARTESIAN_POINT ( 'NONE',  ( 0.3687372981288695728, -1.412185959430117821, 1.636573055046482983 ) ) ;
#186111=CARTESIAN_POINT ( 'NONE',  ( 0.3390778084843976137, -1.706115258973059490, -1.074657883261991076 ) ) ;
#186113=CARTESIAN_POINT ( 'NONE',  ( 1.599382804601066743, 1.132622197759477478, -1.999898178936350357 ) ) ;
#186117=CARTESIAN_POINT ( 'NONE',  ( 2.324885834233282544, -0.002380789299309681549, 1.870836310375329381 ) ) ;
#186118=CARTESIAN_POINT ( 'NONE',  ( 3.503138892209650024, -0.1435209762444041581, 2.011451614702438828 ) ) ;
#186122=CARTESIAN_POINT ( 'NONE',  ( 4.565121803138184831, -1.881030885445551304, -0.9473677958443439406 ) ) ;
#186127=CARTESIAN_POINT ( 'NONE',  ( 4.060810560252373413, 0.5428485958907465214, 1.945370397410832730 ) ) ;
#186129=CARTESIAN_POINT ( 'NONE',  ( 1.024372331059967056, 1.013329571420513053, 1.796381585629814426 ) ) ;
#186131=CARTESIAN_POINT ( 'NONE',  ( 5.817692603468245238, -2.110333850551704415, 0.4673072906974176655 ) ) ;
#186136=CARTESIAN_POINT ( 'NONE',  ( 2.699877945841188343, -1.607453219145397849, -1.459642119406568739 ) ) ;
#186139=CARTESIAN_POINT ( 'NONE',  ( 1.962219809069129184, -1.683971100191889336, -0.7449956418128443891 ) ) ;
#186141=CARTESIAN_POINT ( 'NONE',  ( 3.650093349144762023, 0.7902683543556283663, 2.044282924279612779 ) ) ;
#186142=CARTESIAN_POINT ( 'NONE',  ( 6.883263157960421097, 0.5621630953002605402, 2.205140871664055702 ) ) ;
#186143=CARTESIAN_POINT ( 'NONE',  ( 4.715850076732730045, -2.219782111298532978, 0.4368881197941154038 ) ) ;
#186152=CARTESIAN_POINT ( 'NONE',  ( 4.885902211565920972, -0.8344178305333300738, 1.560695085661115922 ) ) ;
#186154=CARTESIAN_POINT ( 'NONE',  ( 1.465998146299499094, 2.074868464730471374, -0.3595401751291906756 ) ) ;
#186157=CARTESIAN_POINT ( 'NONE',  ( 2.031642458604762780, 1.885605923395494044, -0.5689241207685117319 ) ) ;
#186161=CARTESIAN_POINT ( 'NONE',  ( 6.240474538790502734, 1.035194401182498281, -1.486496517754380742 ) ) ;
#186165=CARTESIAN_POINT ( 'NONE',  ( 5.330866702616011921, 0.1386157390740362649, 1.865562100978317206 ) ) ;
#186166=CARTESIAN_POINT ( 'NONE',  ( 5.541872263726007830, 1.386227983376321582, 1.537841262885197846 ) ) ;
#186176=CARTESIAN_POINT ( 'NONE',  ( 5.230891786122516152, -1.846674803186045821, -0.6626716404555529349 ) ) ;
#186178=CARTESIAN_POINT ( 'NONE',  ( 3.022814370378481552, 2.006652721595225675, -0.1948103792988181704 ) ) ;
#186179=CARTESIAN_POINT ( 'NONE',  ( 2.782342135839787289, -0.5608490805640730104, -1.831745072482870107 ) ) ;
#186181=CARTESIAN_POINT ( 'NONE',  ( 0.06437606466144081552, -1.426665095847098330, 1.663708609037084951 ) ) ;
#186183=CARTESIAN_POINT ( 'NONE',  ( 2.389737607000471442, -0.8038258883538218491, 1.689183408448757362 ) ) ;
#186185=CARTESIAN_POINT ( 'NONE',  ( 4.447525235540350508, -1.838889683631849348, 0.8198632543043646859 ) ) ;
#186188=CARTESIAN_POINT ( 'NONE',  ( 4.148151592129151410, 0.9998098737230370903, 1.866312969332243998 ) ) ;
#186189=CARTESIAN_POINT ( 'NONE',  ( 0.1747926744264668986, 7.629137130509083597, -2.455305974604498953 ) ) ;
#186190=CARTESIAN_POINT ( 'NONE',  ( 6.268043187460373922, -2.055199631210803624, 0.2494731385529954104 ) ) ;
#186191=CARTESIAN_POINT ( 'NONE',  ( 1.734041596967655252, 2.068474147835582144, 0.3034153833333247396 ) ) ;
#186192=CARTESIAN_POINT ( 'NONE',  ( 6.620655732516651071, -0.002413161512292844035, 2.173887093218453082 ) ) ;
#186193=CARTESIAN_POINT ( 'NONE',  ( 0.1293586867831516274, -1.054425554818343880, -1.365251215659948558 ) ) ;
#186202=CARTESIAN_POINT ( 'NONE',  ( 0.3459856143687444208, 0.9327069207067508749, -1.552719410179828952 ) ) ;
#186212=CARTESIAN_POINT ( 'NONE',  ( 5.941029844038744123, -1.730876725876070221, -1.034150010194856417 ) ) ;
#186213=CARTESIAN_POINT ( 'NONE',  ( -0.05774110376318035420, -1.308430771297011130, -1.669371405835825550 ) ) ;
#186220=CARTESIAN_POINT ( 'NONE',  ( 3.221498965751792731, 0.2935017643310656177, -1.947342446911073610 ) ) ;
#186221=CARTESIAN_POINT ( 'NONE',  ( 5.044546077387519922, -1.458546410489666600, 1.392558106302365095 ) ) ;
#186224=CARTESIAN_POINT ( 'NONE',  ( 4.593798273609356997, -2.190911875110569174, -0.05534364095756416635 ) ) ;
#186226=CARTESIAN_POINT ( 'NONE',  ( 3.030207491816420795, 1.071487476811390449, -1.600714694641630853 ) ) ;
#186229=CARTESIAN_POINT ( 'NONE',  ( 0.1331565106231571705, 6.948071080078889850, -2.540993614958915181 ) ) ;
#186233=CARTESIAN_POINT ( 'NONE',  ( 4.592606226310515183, 1.930599660924517957, 0.3882996684868595394 ) ) ;
#186235=CARTESIAN_POINT ( 'NONE',  ( 0.8549040543346017040, 0.3774493213832031402, -1.904865965088814228 ) ) ;
#186236=CARTESIAN_POINT ( 'NONE',  ( 3.651042523073198431, 0.2976914719170896118, 1.990856138409332843 ) ) ;
#186237=CARTESIAN_POINT ( 'NONE',  ( 5.448667688119189556, 1.537605954158068666, 1.708491323253034100 ) ) ;
#186238=CARTESIAN_POINT ( 'NONE',  ( 3.783913598179854176, -1.105313619694109795, -1.496993097346049462 ) ) ;
#186244=CARTESIAN_POINT ( 'NONE',  ( 0.08191350661116909848, -1.027414926483052326, 1.935800647029708443 ) ) ;
#186248=CARTESIAN_POINT ( 'NONE',  ( 0.08226035653636187828, -1.769965142718381124, -0.4472663993063328847 ) ) ;
#186250=CARTESIAN_POINT ( 'NONE',  ( 2.426026400502009128, -1.286032909179233297, -1.163566193670103832 ) ) ;
#186252=CARTESIAN_POINT ( 'NONE',  ( 6.509000000000047415, 2.458121647476101401, 2.283885694139938138 ) ) ;
#186255=CARTESIAN_POINT ( 'NONE',  ( 0.4091448426733998445, -1.664836780672280803, 1.230395522420650201 ) ) ;
#186256=CARTESIAN_POINT ( 'NONE',  ( 5.566980414702134894, -1.652319403193935887, -0.7768266693391965294 ) ) ;
#186257=CARTESIAN_POINT ( 'NONE',  ( 3.379693149055284174, -1.891888713350448947, 0.5187481205842572329 ) ) ;
#186262=CARTESIAN_POINT ( 'NONE',  ( 3.967525559752110631, -1.763746451813380967, -1.176840329774282212 ) ) ;
#186265=CARTESIAN_POINT ( 'NONE',  ( 1.375928118113247667, -2.020660359122231409, 0.4497719141252010111 ) ) ;
#186268=CARTESIAN_POINT ( 'NONE',  ( 4.389451384964074165, 0.0001031656717501855256, -2.221473415372441806 ) ) ;
#186270=CARTESIAN_POINT ( 'NONE',  ( 1.635759689059889554, 0.7259864748365916221, 2.181091778573934103 ) ) ;
#186278=CARTESIAN_POINT ( 'NONE',  ( 2.777492966359981441, 0.2764497561681695803, -1.892163382976944419 ) ) ;
#186280=CARTESIAN_POINT ( 'NONE',  ( 3.944159270863063060, 1.716513557549454339, 0.1685945156147239388 ) ) ;
#186281=CARTESIAN_POINT ( 'NONE',  ( 2.729704159269104924, 0.7212915320151757070, -1.883313052590728454 ) ) ;
#186282=CARTESIAN_POINT ( 'NONE',  ( 3.621995078338976715, 0.3387333280310041994, 2.273515639168000035 ) ) ;
#186284=CARTESIAN_POINT ( 'NONE',  ( 6.094376849853386346, -2.095768364502542003, -0.2079484218287275255 ) ) ;
#186286=CARTESIAN_POINT ( 'NONE',  ( 5.219873587733063758, -0.9469346145933134062, -1.494860035008038324 ) ) ;
#186288=CARTESIAN_POINT ( 'NONE',  ( 1.342159615362942704, 2.289816521768207380, 0.1084569774388414870 ) ) ;
#186289=CARTESIAN_POINT ( 'NONE',  ( 6.439398882927052981, 0.6998097629446423662, -1.703160347957879850 ) ) ;
#186292=CARTESIAN_POINT ( 'NONE',  ( 5.173855182012670362, -1.219361875273092366, 1.820681821249593657 ) ) ;
#186297=CARTESIAN_POINT ( 'NONE',  ( 0.7136160920222310855, -1.834322530278935215, -1.161324927271490060 ) ) ;
#186298=CARTESIAN_POINT ( 'NONE',  ( 1.657435761918718331, 1.928256795251210631, -0.5899901959932273288 ) ) ;
#186300=CARTESIAN_POINT ( 'NONE',  ( 4.143132006054106142, -1.675477906314150056, 0.9507637539484592448 ) ) ;
#186302=CARTESIAN_POINT ( 'NONE',  ( 1.705654399339423311, 1.929789488239462836, -1.100201954495036549 ) ) ;
#186312=CARTESIAN_POINT ( 'NONE',  ( 4.106796630993492236, -0.2923914088966376723, 1.715523938624329281 ) ) ;
#186313=CARTESIAN_POINT ( 'NONE',  ( 2.664445928352857429, -0.7481792696971514278, -1.813797970468238985 ) ) ;
#186318=CARTESIAN_POINT ( 'NONE',  ( 6.725062055625550705, -1.793239977796506457, -0.7961783947641184467 ) ) ;
#186321=CARTESIAN_POINT ( 'NONE',  ( 5.102750050473856547, 1.865045247124358818, 0.7672954931761333253 ) ) ;
#186322=CARTESIAN_POINT ( 'NONE',  ( 1.376233744030544104, 1.349093794351564624, 1.816168808025316661 ) ) ;
#186326=CARTESIAN_POINT ( 'NONE',  ( 1.651402116136031051, 0.5479989942898423338, -1.788454331708405620 ) ) ;
#186327=CARTESIAN_POINT ( 'NONE',  ( 0.7032560681843272876, 1.601581415593232860, 0.6654971025301190668 ) ) ;
#186330=CARTESIAN_POINT ( 'NONE',  ( 4.599289333468261631, -0.5842463895667610041, 2.112197083089427885 ) ) ;
#186331=CARTESIAN_POINT ( 'NONE',  ( 5.526528793889518454, 1.380124021263717804, -1.849252619965065847 ) ) ;
#186332=CARTESIAN_POINT ( 'NONE',  ( 6.626252497008212394, 1.190392663088507552, -1.681986249806742384 ) ) ;
#186333=CARTESIAN_POINT ( 'NONE',  ( 3.257691520677992614, 0.8739490649069777684, 1.734254922796226506 ) ) ;
#186337=CARTESIAN_POINT ( 'NONE',  ( 4.904922738988922504, -1.081064280317966420, -1.701948707654332704 ) ) ;
#186341=CARTESIAN_POINT ( 'NONE',  ( 0.9260630535584664091, 1.089557764695957554, -1.464779044915397455 ) ) ;
#186346=ORIENTED_EDGE ( 'NONE', *, *, #98433, .F. ) ;
#186347=CARTESIAN_POINT ( 'NONE',  ( 6.403207051292992169, 1.711950105385249055, 1.147064539034772679 ) ) ;
#186351=CARTESIAN_POINT ( 'NONE',  ( 5.479167871109219767, -1.826835719847461847, -0.8615247647300682265 ) ) ;
#186352=CARTESIAN_POINT ( 'NONE',  ( 5.936230101866142306, -1.231883464771424075, -1.848230934346828391 ) ) ;
#186356=CARTESIAN_POINT ( 'NONE',  ( 5.787979943833009067, -0.9286772032993969583, 1.839872548930401974 ) ) ;
#186357=CARTESIAN_POINT ( 'NONE',  ( 4.395157833011634096, -0.8647231026696032830, -1.821742675176166060 ) ) ;
#186365=CARTESIAN_POINT ( 'NONE',  ( 3.831407535526813124, -1.356092489331266027, 1.492026659919619247 ) ) ;
#186366=CARTESIAN_POINT ( 'NONE',  ( 3.591602706507342369, -1.839109287420921834, -0.08896477992388628075 ) ) ;
#186368=CARTESIAN_POINT ( 'NONE',  ( 2.702171824926146826, -0.7227257407616082263, 2.191671519121952461 ) ) ;
#186370=CARTESIAN_POINT ( 'NONE',  ( 5.009125465012424172, 1.878017946038791575, 1.070212309444783294 ) ) ;
#186372=CARTESIAN_POINT ( 'NONE',  ( 0.1341856092403709844, 0.3330598185416616119, 1.913145364980510799 ) ) ;
#186376=CARTESIAN_POINT ( 'NONE',  ( 2.817106861211693847, -0.1851908181382568019, 1.861470920997858380 ) ) ;
#186378=CARTESIAN_POINT ( 'NONE',  ( 6.649300054797159909, -1.583302550941813491, -1.174460211130315512 ) ) ;
#186381=CARTESIAN_POINT ( 'NONE',  ( 1.928631425534212074, 1.268998755960360603, -1.805353087401928569 ) ) ;
#186387=CARTESIAN_POINT ( 'NONE',  ( 6.614144449397460157, -0.9292204182751627739, -1.738729380627493049 ) ) ;
#186388=CARTESIAN_POINT ( 'NONE',  ( 0.2711454947614586608, -1.503558885491006247, 1.750568091222578282 ) ) ;
#186389=CARTESIAN_POINT ( 'NONE',  ( 0.3616705494772323726, -0.5269360983083425376, 1.889693748445469224 ) ) ;
#186390=CARTESIAN_POINT ( 'NONE',  ( 4.205966187000295342, 0.6995128471476423915, -1.940432845919232374 ) ) ;
#186398=CARTESIAN_POINT ( 'NONE',  ( 0.2393977111345606534, -0.1477851991248577135, -2.137246755706405210 ) ) ;
#186400=CARTESIAN_POINT ( 'NONE',  ( 5.302248432823610358, 1.390444127666954355, -1.207098008268410183 ) ) ;
#186404=CARTESIAN_POINT ( 'NONE',  ( 0.4736314445139556684, 1.071599637473351629, 1.532994764490814177 ) ) ;
#186410=CARTESIAN_POINT ( 'NONE',  ( 2.184116879877880724, -1.735013770989551896, -0.3484325113714877298 ) ) ;
#186411=CARTESIAN_POINT ( 'NONE',  ( 0.06490398442321809735, -1.535895564731554863, 1.139000086266952483 ) ) ;
#186413=CARTESIAN_POINT ( 'NONE',  ( 4.200734335399162411, 1.752999579934441998, 0.7727710859696481638 ) ) ;
#186415=CARTESIAN_POINT ( 'NONE',  ( 5.723099352235532677, -1.779878778038428200, -0.8436364978330126441 ) ) ;
#186416=CARTESIAN_POINT ( 'NONE',  ( 0.03560581989598374242, -0.09759080014098624190, 2.118463022953632091 ) ) ;
#186418=CARTESIAN_POINT ( 'NONE',  ( 2.799504582125960095, -0.5885537693137884441, 1.775713401224961574 ) ) ;
#186419=CARTESIAN_POINT ( 'NONE',  ( 6.305283062370508063, 1.438394668203015092, 0.9516435707833100777 ) ) ;
#186421=CARTESIAN_POINT ( 'NONE',  ( 3.405080638938757343, 1.739790774466195789, -1.357627211771177178 ) ) ;
#186424=CARTESIAN_POINT ( 'NONE',  ( 1.029816311724339961, 1.988459969548944439, -0.5481627708354539497 ) ) ;
#186432=CARTESIAN_POINT ( 'NONE',  ( 3.121598655985452275, 0.3063859900464052100, -2.047459029603612368 ) ) ;
#186436=CARTESIAN_POINT ( 'NONE',  ( 0.8912779446055114629, -0.05177971647825175411, -2.019189627193836323 ) ) ;
#186440=CARTESIAN_POINT ( 'NONE',  ( 0.1745949693968797123, 1.415412180343596837, -2.016327490378281073 ) ) ;
#186442=CARTESIAN_POINT ( 'NONE',  ( 6.884150277402729223, -0.1485532345978715640, 1.983297619905934006 ) ) ;
#186443=CARTESIAN_POINT ( 'NONE',  ( 5.841025094292755071, -1.646784362596087625, -0.9785371348113005574 ) ) ;
#186445=CARTESIAN_POINT ( 'NONE',  ( 3.368858348882136422, 0.05182064297618373117, -2.191103300807801801 ) ) ;
#186448=CARTESIAN_POINT ( 'NONE',  ( 2.496234081663367022, -0.9796988711565941532, 1.642222327643327873 ) ) ;
#186452=CARTESIAN_POINT ( 'NONE',  ( 1.476185646619165626, -2.006963189339417308, -0.1948195631672477446 ) ) ;
#186454=CARTESIAN_POINT ( 'NONE',  ( 6.614806895146394972, -0.1608752592793839531, 2.155998228907447523 ) ) ;
#186456=CARTESIAN_POINT ( 'NONE',  ( 2.748708976905740897, -1.435238111852419562, 0.9561691852014215787 ) ) ;
#186458=CARTESIAN_POINT ( 'NONE',  ( -0.1405533004718312329, 0.7798934913714054007, -1.807795836271476331 ) ) ;
#186463=CARTESIAN_POINT ( 'NONE',  ( 1.416376618315864144, 0.7919773292732554815, 1.795081228748253377 ) ) ;
#186467=ORIENTED_EDGE ( 'NONE', *, *, #178523, .T. ) ;
#186470=CARTESIAN_POINT ( 'NONE',  ( 3.809066866439265286, 1.528366121442883196, -0.9720638507800370975 ) ) ;
#186471=ORIENTED_EDGE ( 'NONE', *, *, #70737, .F. ) ;
#186474=CARTESIAN_POINT ( 'NONE',  ( 4.512255818007496977, -1.811207030272870000, -0.03965706671436861758 ) ) ;
#186481=CARTESIAN_POINT ( 'NONE',  ( 5.687920738472253213, -1.181023890769626217, -1.438316992653262627 ) ) ;
#186484=CARTESIAN_POINT ( 'NONE',  ( 2.372541684819210683, -0.3298082299327957378, -1.886833909188085912 ) ) ;
#186490=CARTESIAN_POINT ( 'NONE',  ( 2.553923023464285347, 1.082840749376843270, 1.700961377887353798 ) ) ;
#186493=CARTESIAN_POINT ( 'NONE',  ( 1.341864181646670540, 2.088322648670298598, 0.1009416716012418447 ) ) ;
#186495=CARTESIAN_POINT ( 'NONE',  ( 6.774445256934315651, -1.184694399318196201, 1.519801669933226407 ) ) ;
#186497=CARTESIAN_POINT ( 'NONE',  ( 2.502731746374619259, 1.467688513602287470, -1.085450786651315225 ) ) ;
#186500=CARTESIAN_POINT ( 'NONE',  ( 2.074333847954575205, 0.8209984392052707136, 1.727357542596375861 ) ) ;
#186501=CARTESIAN_POINT ( 'NONE',  ( 1.433975083751269697, 1.170624227716898780, 1.583764482814524088 ) ) ;
#186502=CARTESIAN_POINT ( 'NONE',  ( 3.579573000355208645, -0.9547435552521261748, 1.691086383587044883 ) ) ;
#186507=CARTESIAN_POINT ( 'NONE',  ( 4.623349522974431025, 1.846400237221163865, 1.042759738753673338 ) ) ;
#186514=CARTESIAN_POINT ( 'NONE',  ( 3.809063337113669068, 1.566667275063510445, 0.9371452329686791316 ) ) ;
#186515=CARTESIAN_POINT ( 'NONE',  ( 6.139861302770143858, 2.010801613648224961, -0.1531635369260639090 ) ) ;
#186518=( BOUNDED_CURVE ( )  B_SPLINE_CURVE ( 3, ( #17740, #197582, #181336, #133698 ),
 .UNSPECIFIED., .F., .T. ) 
 B_SPLINE_CURVE_WITH_KNOTS ( ( 4, 4 ),
 ( 0.000000000000000000, 0.4999999999999988898 ),
 .UNSPECIFIED. ) 
 CURVE ( )  GEOMETRIC_REPRESENTATION_ITEM ( )  RATIONAL_B_SPLINE_CURVE ( ( 1.000000000000000000, 0.3333333333333348691, 0.3333333333333333703, 0.9999999999999985567 ) ) 
 REPRESENTATION_ITEM ( '' )  );
#186522=CARTESIAN_POINT ( 'NONE',  ( 4.346470048663173102, 0.4987854378066917116, 1.802870001028591407 ) ) ;
#186524=CARTESIAN_POINT ( 'NONE',  ( 2.068856375562718508, -1.761265384887151342, -0.7809992120406393790 ) ) ;
#186525=CARTESIAN_POINT ( 'NONE',  ( 6.737165023268617325, -0.09304339776683605290, -1.959646862056351857 ) ) ;
#186531=CARTESIAN_POINT ( 'NONE',  ( 0.9665973488726641305, -2.066607521123296376, -0.4595904307344770290 ) ) ;
#186534=CARTESIAN_POINT ( 'NONE',  ( 4.821179601816666604, -1.846891146645711412, -0.9356023351853595127 ) ) ;
#186535=CARTESIAN_POINT ( 'NONE',  ( 0.3097736896383457839, 1.270387085892955792, -1.333027339516623888 ) ) ;
#186537=CARTESIAN_POINT ( 'NONE',  ( 5.116020035227313301, 0.1674390183682184785, 2.292669612833755810 ) ) ;
#186541=CARTESIAN_POINT ( 'NONE',  ( 0.9730957290566042417, -0.06121152481648738097, -2.291606990885884265 ) ) ;
#186544=CARTESIAN_POINT ( 'NONE',  ( 5.718683143142158087, -0.04558518807709806275, 1.941574535162658544 ) ) ;
#186549=CARTESIAN_POINT ( 'NONE',  ( -0.08764186210430401081, -2.012836238882615980, -0.04531326932211143105 ) ) ;
#186550=CARTESIAN_POINT ( 'NONE',  ( 5.190638768449240104, 1.523797776992100061, -1.320824044268428032 ) ) ;
#186554=CARTESIAN_POINT ( 'NONE',  ( 2.308638494240814687, 1.867967618895223447, 0.9389952993345984655 ) ) ;
#186555=CARTESIAN_POINT ( 'NONE',  ( 1.410649291501327118, 1.558696297929580199, 0.8383436984091273692 ) ) ;
#186556=CARTESIAN_POINT ( 'NONE',  ( 6.469375277500488686, -1.978045142091336306, -0.3906011616893814709 ) ) ;
#186558=CARTESIAN_POINT ( 'NONE',  ( 3.961076342171603315, 0.2821129637899103537, -2.274769079453589526 ) ) ;
#186559=CARTESIAN_POINT ( 'NONE',  ( 2.941039689149751890, 0.6260299441606477222, -1.624016774299047228 ) ) ;
#186563=CARTESIAN_POINT ( 'NONE',  ( 3.145509197426650694, -0.1243275703598344523, -1.729419848027229367 ) ) ;
#186564=CARTESIAN_POINT ( 'NONE',  ( 3.789651875377809898, -2.007375656734013969, 0.8277776116962390907 ) ) ;
#186566=CARTESIAN_POINT ( 'NONE',  ( 4.135954056172497673, 2.015980767636461835, -0.05432360925018697717 ) ) ;
#186567=CARTESIAN_POINT ( 'NONE',  ( 2.500000000000002220, -1.483785425626877107E-13, -2.052068128417949389 ) ) ;
#186569=CARTESIAN_POINT ( 'NONE',  ( 1.360239512323542010, 0.7782574302275366840, 1.762357998526616232 ) ) ;
#186571=CARTESIAN_POINT ( 'NONE',  ( 4.394933515450586192, -2.155188642370196916, -0.5379869938199193236 ) ) ;
#186572=ORIENTED_EDGE ( 'NONE', *, *, #141701, .F. ) ;
#186573=CARTESIAN_POINT ( 'NONE',  ( -0.2106854629475037044, 2.877407191259284680, -2.485613835449883346 ) ) ;
#186578=CARTESIAN_POINT ( 'NONE',  ( 1.172868535947855673, 0.9048325283492463234, 2.028842389263245227 ) ) ;
#186579=CARTESIAN_POINT ( 'NONE',  ( 5.371523934717264304, -0.2895824386080196322, 1.940264742196501802 ) ) ;
#186583=CARTESIAN_POINT ( 'NONE',  ( 0.5796411875719498230, 2.017120475678677582, -0.7774783797904263327 ) ) ;
#186585=CARTESIAN_POINT ( 'NONE',  ( 3.824720269693319796, -1.387356309220557193, 1.526538889744559313 ) ) ;
#186589=CARTESIAN_POINT ( 'NONE',  ( 5.149604166610965095, 0.5880212298954893280, -1.775756280894603689 ) ) ;
#186590=CARTESIAN_POINT ( 'NONE',  ( 4.148821288392518625, 0.8220224570679548481, 1.526945684688446381 ) ) ;
#186591=CARTESIAN_POINT ( 'NONE',  ( 3.561793593276740388, -1.166016580864630781, 1.292293876973077182 ) ) ;
#186593=CARTESIAN_POINT ( 'NONE',  ( 1.031297522511119613, -2.069548003639944511, 0.9861895074133855132 ) ) ;
#186595=CARTESIAN_POINT ( 'NONE',  ( 4.036730150552261698, -1.818196258471163729, 1.032062162679239892 ) ) ;
#186596=CARTESIAN_POINT ( 'NONE',  ( 0.1636598862229492191, -1.205073137261414962, 1.392071761982638378 ) ) ;
#186598=CARTESIAN_POINT ( 'NONE',  ( 1.969375177810539945, -1.978050944945686673, -0.3905967402937361443 ) ) ;
#186599=CARTESIAN_POINT ( 'NONE',  ( 0.2698121887318750689, 1.265274936352598134, 1.789097752032620114 ) ) ;
#186603=CARTESIAN_POINT ( 'NONE',  ( 2.121885542695590487, -0.4617877489709980576, 2.069441001874790409 ) ) ;
#186605=CARTESIAN_POINT ( 'NONE',  ( 5.953692858212231265, 0.5253669772854427933, -1.748464709795935157 ) ) ;
#186613=CARTESIAN_POINT ( 'NONE',  ( 1.969016121511291795, -1.558499072447929956, 1.284715733913702085 ) ) ;
#186614=CARTESIAN_POINT ( 'NONE',  ( 6.106501571484221458, -0.7887142981495840477, -2.061199855587454444 ) ) ;
#186616=CARTESIAN_POINT ( 'NONE',  ( 4.030005733973434978, 1.030655172484344684, 1.549249419044882226 ) ) ;
#186622=CARTESIAN_POINT ( 'NONE',  ( 5.637271085457097541, -1.648663388651723460, 0.7845467231081537651 ) ) ;
#186626=CARTESIAN_POINT ( 'NONE',  ( 0.6140417155099803237, 0.5521904297083098934, -1.643632271941943612 ) ) ;
#186627=CARTESIAN_POINT ( 'NONE',  ( 0.3216633777232960067, 1.663872621647478622, 0.5102041932069888430 ) ) ;
#186628=CARTESIAN_POINT ( 'NONE',  ( 5.584705890799654071, -2.250326009109602232, -0.5107660753775817852 ) ) ;
#186630=CARTESIAN_POINT ( 'NONE',  ( 1.229839986812499175, -1.305282058118014010, -1.594721697489847045 ) ) ;
#186632=CARTESIAN_POINT ( 'NONE',  ( 6.696599425470320277, -1.493074370650529392, -1.747488531831635550 ) ) ;
#186636=CARTESIAN_POINT ( 'NONE',  ( 6.209813078548920728, -1.856259414618817383, 0.2309603555875269776 ) ) ;
#186637=CARTESIAN_POINT ( 'NONE',  ( 3.673993457511487204, 1.897360377298975553, -0.2389773157873422427 ) ) ;
#186639=CARTESIAN_POINT ( 'NONE',  ( 4.512475528931441104, -0.9420208833846724916, -1.995868093903986118 ) ) ;
#186644=CARTESIAN_POINT ( 'NONE',  ( 6.111998723603361938, -0.7147493727725148238, 1.996541221815250733 ) ) ;
#186646=CARTESIAN_POINT ( 'NONE',  ( 3.311855287401725523, -0.4521268412439309325, 2.262704599374213643 ) ) ;
#186647=CARTESIAN_POINT ( 'NONE',  ( 3.525789274851616639, 1.914599547803575330, -0.4273510147508317591 ) ) ;
#186649=CARTESIAN_POINT ( 'NONE',  ( 0.3210474040165818277, -1.749687966165301312, -0.8873976775175674847 ) ) ;
#186653=CARTESIAN_POINT ( 'NONE',  ( 5.858611323429600226, -1.916351766245901977, -0.6279953093112633500 ) ) ;
#186655=CARTESIAN_POINT ( 'NONE',  ( 0.2164228883963260908, -0.09351453081237262599, 1.838880455306932227 ) ) ;
#186656=CARTESIAN_POINT ( 'NONE',  ( 2.641674518982541020, 1.986514366401496590, -0.8763142005700165216 ) ) ;
#186658=CARTESIAN_POINT ( 'NONE',  ( 0.9848172835694012361, -1.340914915981223476, 1.642866500755429948 ) ) ;
#186662=CARTESIAN_POINT ( 'NONE',  ( 0.4739915956469250014, 1.184468288027096694, 1.686179815164081219 ) ) ;
#186668=CARTESIAN_POINT ( 'NONE',  ( 3.949791169003769475, -1.320912084567291034, -1.382976300589415342 ) ) ;
#186669=CARTESIAN_POINT ( 'NONE',  ( 5.489024251479373895, 1.559478583775832261, -0.8368352093669585434 ) ) ;
#186672=CARTESIAN_POINT ( 'NONE',  ( 0.5096461351858303512, -0.6515609501748579335, 1.690550641884549954 ) ) ;
#186674=CARTESIAN_POINT ( 'NONE',  ( 1.094790513324794601, 1.691201413147478183, 0.8998118624304138891 ) ) ;
#186675=CARTESIAN_POINT ( 'NONE',  ( 2.436061438456170958, 1.271862942251865691, 1.633573898902056731 ) ) ;
#186677=CARTESIAN_POINT ( 'NONE',  ( 0.4441303031895106890, 1.966005183986684335, 0.1476035654904006011 ) ) ;
#186678=CARTESIAN_POINT ( 'NONE',  ( 2.701551412915685457, -0.5726843992823158480, 1.733614832724015731 ) ) ;
#186679=CARTESIAN_POINT ( 'NONE',  ( 0.3116875490984937214, 2.011018277352360606, 1.131832386414432179 ) ) ;
#186682=CARTESIAN_POINT ( 'NONE',  ( 4.686014676054621297, -1.266354490919174403, -1.628128356427221313 ) ) ;
#186687=CARTESIAN_POINT ( 'NONE',  ( 4.805753954608172229, -0.5644290981201576241, 2.028831172856554677 ) ) ;
#186689=CARTESIAN_POINT ( 'NONE',  ( 6.865700769154306826, -0.4580177224273937475, 2.026514595051785772 ) ) ;
#186691=CARTESIAN_POINT ( 'NONE',  ( 3.515052679271633895, 1.952536648612019921, 0.9277410485990513767 ) ) ;
#186692=CARTESIAN_POINT ( 'NONE',  ( 4.002606914492294443, -1.998013091498285654, -0.2940530905436929410 ) ) ;
#186693=CARTESIAN_POINT ( 'NONE',  ( 6.620655732516659064, 2.000981103421325180, 2.575746817850287140 ) ) ;
#186698=CARTESIAN_POINT ( 'NONE',  ( 2.764861550476094276, -0.1531697945360478985, -2.010801143277194392 ) ) ;
#186703=CARTESIAN_POINT ( 'NONE',  ( 5.748291730981217817, 0.9368611416523885405, -1.667099895225135686 ) ) ;
#186706=CARTESIAN_POINT ( 'NONE',  ( 4.077750037130567939, -0.7691059624741981571, 1.864175985064358665 ) ) ;
#186709=CARTESIAN_POINT ( 'NONE',  ( 6.598688221398479214, -0.4661808427693337475, -1.660524940999157373 ) ) ;
#186713=( GEOMETRIC_REPRESENTATION_CONTEXT ( 3 ) GLOBAL_UNCERTAINTY_ASSIGNED_CONTEXT ( ( #118722 ) ) GLOBAL_UNIT_ASSIGNED_CONTEXT ( ( #2030, #166705, #68099 ) ) REPRESENTATION_CONTEXT ( 'NONE', 'WORKASPACE' ) );
#186715=CARTESIAN_POINT ( 'NONE',  ( 5.483624757375023862, 1.255567903217995829, 1.386730702750748945 ) ) ;
#186716=CARTESIAN_POINT ( 'NONE',  ( 6.486586620031766337, -1.235515937849906321, 1.590312944162165287 ) ) ;
#186718=CARTESIAN_POINT ( 'NONE',  ( 1.868117093089691538, -2.055091939184821026, 0.2493290443424806546 ) ) ;
#186722=CARTESIAN_POINT ( 'NONE',  ( 0.6148615108944045504, 0.1511614643284354409, 2.010825953887733775 ) ) ;
#186723=CARTESIAN_POINT ( 'NONE',  ( 1.195247182365884564, 1.673216051897677747, -0.6948750315247439469 ) ) ;
#186732=CARTESIAN_POINT ( 'NONE',  ( 6.433208386744649232, -1.541796563146474286, -1.136648034191472645 ) ) ;
#186740=CARTESIAN_POINT ( 'NONE',  ( 2.483474991488154870, 1.976725341044349271, -0.8753317036461552014 ) ) ;
#186743=CARTESIAN_POINT ( 'NONE',  ( 0.7562902151678205787, 0.8540304730459827853, -1.941197329821432227 ) ) ;
#186744=CARTESIAN_POINT ( 'NONE',  ( 5.262654937129007671, -1.321179299781930938, 1.260103332352560779 ) ) ;
#186746=CARTESIAN_POINT ( 'NONE',  ( 1.792193567899300177, -1.961476155570774926, -0.1973719964898524026 ) ) ;
#186747=CARTESIAN_POINT ( 'NONE',  ( 4.588094604188536429, 1.105678411722615051, 1.560157546714964871 ) ) ;
#186749=CARTESIAN_POINT ( 'NONE',  ( 6.875078400183573635, 7.629137130509068498, 2.744348168701661095 ) ) ;
#186750=CARTESIAN_POINT ( 'NONE',  ( 4.598083368088573764, 0.8440023354334601491, -1.779705283501178181 ) ) ;
#186751=CARTESIAN_POINT ( 'NONE',  ( 0.4275465750286939204, 0.9991681100989335818, -1.665045846455282863 ) ) ;
#186757=CARTESIAN_POINT ( 'NONE',  ( 5.004515039866801906, -1.898294113557968510, -0.2302225566794338651 ) ) ;
#186758=CARTESIAN_POINT ( 'NONE',  ( 0.8685540286928780107, 1.089157903960279672, 1.919174906450902274 ) ) ;
#186760=CARTESIAN_POINT ( 'NONE',  ( 6.059245300855401695, -1.699386736952392285, 1.078915776541150340 ) ) ;
#186763=DIRECTION ( 'NONE',  ( -0.9999980456341538426, 0.000000000000000000, -0.001977050295949311660 ) ) ;
#186764=CARTESIAN_POINT ( 'NONE',  ( 2.717306809760032138, -1.800131872397674471, -1.022606600864908621 ) ) ;
#186768=CARTESIAN_POINT ( 'NONE',  ( 0.5675189469334164238, 0.2105291993744831114, -2.151437729447757796 ) ) ;
#186774=CARTESIAN_POINT ( 'NONE',  ( 6.925078400183550364, 4.698656493127392864, 2.418320467900983761 ) ) ;
#186776=CARTESIAN_POINT ( 'NONE',  ( 4.342224273253515676, 0.3742292800460333413, -1.693095411864028677 ) ) ;
#186778=CARTESIAN_POINT ( 'NONE',  ( 3.608316154870555792, 2.070434559819031684, 0.004826415812286819970 ) ) ;
#186779=CARTESIAN_POINT ( 'NONE',  ( 5.009417666957850734, -2.010078760914670859, 0.6651486602928055047 ) ) ;
#186783=CARTESIAN_POINT ( 'NONE',  ( 2.307411487444132270, -1.578694758215667404, -1.177220170345204098 ) ) ;
#186784=CARTESIAN_POINT ( 'NONE',  ( 0.8614045922798494459, -1.509235727096858826, -1.174430983434850972 ) ) ;
#186785=CARTESIAN_POINT ( 'NONE',  ( 4.347812307665041232, 2.291787294364412642, -0.05403505903618135986 ) ) ;
#186786=CARTESIAN_POINT ( 'NONE',  ( 2.314841291766779108, 1.630546960418734148, 0.8213866120303781049 ) ) ;
#186790=CARTESIAN_POINT ( 'NONE',  ( 2.918229521859570408, -2.010703624536396728, 0.1031290223681199103 ) ) ;
#186791=CARTESIAN_POINT ( 'NONE',  ( 3.450005804356533812, -0.7992637590314204399, 1.791754569076028147 ) ) ;
#186794=CARTESIAN_POINT ( 'NONE',  ( 0.07556134207191073093, 7.629137130509040077, -2.844199257382596269 ) ) ;
#186795=CARTESIAN_POINT ( 'NONE',  ( 6.035123006257053113, -1.513425687198214353, -1.442577094899047063 ) ) ;
#186796=CARTESIAN_POINT ( 'NONE',  ( 4.821055670345097077, -0.08498437303107277130, 1.767940285534306488 ) ) ;
#186798=CARTESIAN_POINT ( 'NONE',  ( 0.6565081633774123571, -1.584678946828571133, 1.513927167823600595 ) ) ;
#186799=CARTESIAN_POINT ( 'NONE',  ( 6.404260164931634414, 1.284261220195097808, -1.174706115135275342 ) ) ;
#186802=CARTESIAN_POINT ( 'NONE',  ( 0.2811772945982879968, -2.253408246774822210, 0.4517706223704387458 ) ) ;
#186804=CARTESIAN_POINT ( 'NONE',  ( 6.292339289836506033, -1.631180892843343999, 0.5882027141154468897 ) ) ;
#186805=CARTESIAN_POINT ( 'NONE',  ( 1.735297346119796691, 0.2185962045802778420, 2.196029071591873993 ) ) ;
#186807=CARTESIAN_POINT ( 'NONE',  ( 0.6554289830566867314, 1.805916262795668192, -1.204791683884984810 ) ) ;
#186809=CARTESIAN_POINT ( 'NONE',  ( 1.077539098219507663, 1.607448503539260054, 1.378281722515703800 ) ) ;
#186810=CARTESIAN_POINT ( 'NONE',  ( 4.000000000000002665, -2.278188019141646974E-13, -2.052068128417946280 ) ) ;
#186811=CARTESIAN_POINT ( 'NONE',  ( 6.727182134110219813, 2.036943547479725058, 2.394510323907019345 ) ) ;
#186812=CARTESIAN_POINT ( 'NONE',  ( 4.735331810261827812, -1.761409202268785057, 0.7803939243795944281 ) ) ;
#186814=CARTESIAN_POINT ( 'NONE',  ( 1.734309787148346382, 2.268178062924830041, 0.3313793973579847729 ) ) ;
#186818=CARTESIAN_POINT ( 'NONE',  ( 4.283969606688295961, 2.154612580813870082, -0.5396949931109666920 ) ) ;
#186825=CARTESIAN_POINT ( 'NONE',  ( 1.512342498431101134, -1.897697209584522815, 0.6819976561535444626 ) ) ;
#186827=CARTESIAN_POINT ( 'NONE',  ( 0.2685208109398624088, -0.8776176662104094861, -1.864379643416124166 ) ) ;
#186830=CARTESIAN_POINT ( 'NONE',  ( 0.1164230846485321547, -0.09151219166612066525, 1.839079034809627755 ) ) ;
#186832=CARTESIAN_POINT ( 'NONE',  ( 1.475481261428980506, 1.048764899322068622, 1.425360520505250417 ) ) ;
#186833=CARTESIAN_POINT ( 'NONE',  ( 0.08851783505585240908, -0.5350849913869708541, 1.944072358963434555 ) ) ;
#186834=CARTESIAN_POINT ( 'NONE',  ( 0.04610459085982108324, -1.479553692838073475, 1.095721268101347734 ) ) ;
#186835=CARTESIAN_POINT ( 'NONE',  ( 4.036908492867667064, -1.994400080153370558, 1.130107982421886481 ) ) ;
#186836=CARTESIAN_POINT ( 'NONE',  ( 3.802549092506895878, 1.579937072410386278, 0.9450539169142122553 ) ) ;
#186839=CARTESIAN_POINT ( 'NONE',  ( 4.102439050647597618, -0.5725816820084869141, -1.733541218493547476 ) ) ;
#186840=CARTESIAN_POINT ( 'NONE',  ( 4.570935502227962743, -0.9480417383296577682, 1.779625852769652905 ) ) ;
#186842=CARTESIAN_POINT ( 'NONE',  ( 3.555803421180541157, 0.5519491744547943002, -2.194038648399123215 ) ) ;
#186844=CARTESIAN_POINT ( 'NONE',  ( 0.1707221987203759173, -1.373943582462642921, 1.596272430080846405 ) ) ;
#186846=CARTESIAN_POINT ( 'NONE',  ( 4.053231837324381637, 1.750648263899981849, -1.104974720517466480 ) ) ;
#186849=CARTESIAN_POINT ( 'NONE',  ( 5.742871283745087041, 2.043606947765171267, 0.5656136300068030920 ) ) ;
#186852=CARTESIAN_POINT ( 'NONE',  ( 2.314956460678399885, 1.720770591318865339, 0.8663633404912238767 ) ) ;
#186855=CARTESIAN_POINT ( 'NONE',  ( 6.561384255921438147, 1.635440365473137536, 1.096959908523033711 ) ) ;
#186860=CARTESIAN_POINT ( 'NONE',  ( 0.2467152807458715680, 1.134915856054707906, -1.909484979926486137 ) ) ;
#186861=CARTESIAN_POINT ( 'NONE',  ( 3.592891271941214271, -0.4089703316215765883, -2.065685861495478726 ) ) ;
#186864=CARTESIAN_POINT ( 'NONE',  ( 0.6778921365368529850, -0.9907528278601520633, -1.575212976145045518 ) ) ;
#186868=CARTESIAN_POINT ( 'NONE',  ( 1.389100911873580646, -2.015333191458138273, -0.6601287711371638389 ) ) ;
#186871=CARTESIAN_POINT ( 'NONE',  ( 3.121486724888074882, 0.2905151309811822569, -1.940125473959073421 ) ) ;
#186872=CARTESIAN_POINT ( 'NONE',  ( 2.290102563249151402, -0.9248296759884739870, 1.954025333243500917 ) ) ;
#186873=CARTESIAN_POINT ( 'NONE',  ( 2.190726087351921425, 1.424366561657765207, 1.166803476217087576 ) ) ;
#186876=CARTESIAN_POINT ( 'NONE',  ( 4.048569170814999119, -1.448435850583905671, -0.9644227198624519826 ) ) ;
#186879=CARTESIAN_POINT ( 'NONE',  ( 0.8839147992780393981, 1.452536163361785260, 1.601146772000871188 ) ) ;
#186880=CARTESIAN_POINT ( 'NONE',  ( 3.181017370561005198, -0.9912469002804729090, -1.755500664876320727 ) ) ;
#186884=CARTESIAN_POINT ( 'NONE',  ( 3.537922462266992252, 0.8877721971902104992, -1.760348037230663021 ) ) ;
#186885=CARTESIAN_POINT ( 'NONE',  ( 6.609000000000036401, 1.265604115953523845, 2.115306440354140172 ) ) ;
#186886=CARTESIAN_POINT ( 'NONE',  ( 2.735803960117746403, 1.927664933923057600, 0.2353960755621438972 ) ) ;
#186891=CARTESIAN_POINT ( 'NONE',  ( -0.2108831679770924727, 4.091978752061476321, -2.452067053820900622 ) ) ;
#186896=CARTESIAN_POINT ( 'NONE',  ( 6.458097596740710600, 2.302054065074070177, -0.1608065221961554325 ) ) ;
#186898=CARTESIAN_POINT ( 'NONE',  ( 4.434394140398959294, -1.132915509570767476, 1.601352629973289199 ) ) ;
#186900=CARTESIAN_POINT ( 'NONE',  ( 2.268204128460939550, 1.842446992372799963, -0.8197738674571022344 ) ) ;
#186902=CARTESIAN_POINT ( 'NONE',  ( 2.026704517097451586, 0.4691240347775883501, 2.064561701657470660 ) ) ;
#186906=CARTESIAN_POINT ( 'NONE',  ( 3.327899939431624876, 1.796474422365784029, 0.4023406486387756664 ) ) ;
#186907=ORIENTED_EDGE ( 'NONE', *, *, #84677, .T. ) ;
#186910=CARTESIAN_POINT ( 'NONE',  ( 4.183913158364858553, 2.056144659531285779, -0.5182805708664262045 ) ) ;
#186911=CARTESIAN_POINT ( 'NONE',  ( 0.7086343398283838635, -0.2726298849291541870, 1.820711063333625646 ) ) ;
#186915=CARTESIAN_POINT ( 'NONE',  ( 4.481748981177747559, 1.343215529357727478, 1.562995469165892493 ) ) ;
#186918=CARTESIAN_POINT ( 'NONE',  ( 1.100829259350871281, -0.4471758257712907247, 1.786007343351428966 ) ) ;
#186923=CARTESIAN_POINT ( 'NONE',  ( 1.735297346119796691, 0.2185962045802778420, 2.196029071591873993 ) ) ;
#186924=CARTESIAN_POINT ( 'NONE',  ( 3.884249253383244227, -1.119368145229171052, 1.966044450452981929 ) ) ;
#186926=CARTESIAN_POINT ( 'NONE',  ( 4.130988372668517705, 1.658889437441883441, 0.7283703743019008803 ) ) ;
#186927=CARTESIAN_POINT ( 'NONE',  ( 4.118306542938309889, 1.879866726353071060, 0.3679503660072875881 ) ) ;
#186928=CARTESIAN_POINT ( 'NONE',  ( 5.336411075974297979, -1.153114810915600641, 1.719314882265559286 ) ) ;
#186930=CIRCLE ( 'NONE', #200672, 0.04999999999999929501 ) ;
#186931=CARTESIAN_POINT ( 'NONE',  ( 3.344560887785383851, 0.4775036937760200884, 1.912655531573831835 ) ) ;
#186932=CARTESIAN_POINT ( 'NONE',  ( 1.588762598846172436, -0.2802010128373257913, -1.905785462699102206 ) ) ;
#186933=CARTESIAN_POINT ( 'NONE',  ( 4.399188623838041323, 1.502396186649012311, 1.114296746780506497 ) ) ;
#186934=CARTESIAN_POINT ( 'NONE',  ( 3.036059619770274498, -1.550059391276232601, -1.709768245815939780 ) ) ;
#186935=CARTESIAN_POINT ( 'NONE',  ( 4.000341067899515046, 1.851953036565538335, 0.1839423254178795542 ) ) ;
#186938=CARTESIAN_POINT ( 'NONE',  ( 1.963634227113943087, 0.3588053174017143965, -2.075111507017588064 ) ) ;
#186942=CARTESIAN_POINT ( 'NONE',  ( 2.724977724663907530, 1.532976055022855499, -1.465462182430438798 ) ) ;
#186944=CARTESIAN_POINT ( 'NONE',  ( 0.2463608477257169804, 1.034524919618844407, -1.734561685378380957 ) ) ;
#186949=CARTESIAN_POINT ( 'NONE',  ( 1.687033600898584895, -0.3153356727807927196, -2.138329785107299319 ) ) ;
#186950=CARTESIAN_POINT ( 'NONE',  ( 6.889999999999967706, 0.005249217920031550542, 1.719840535937327664 ) ) ;
#186955=CARTESIAN_POINT ( 'NONE',  ( 5.384000029850495750, -2.016708404008683786, 0.004832792792668073358 ) ) ;
#186957=CARTESIAN_POINT ( 'NONE',  ( 6.356985058417449430, 0.3567463788109735967, -2.059909276252298582 ) ) ;
#186959=CARTESIAN_POINT ( 'NONE',  ( 6.649309733611729278, -1.732918351142084035, -1.292073167451508686 ) ) ;
#186966=CARTESIAN_POINT ( 'NONE',  ( 2.877275982374318364, 1.637783285604855088, -0.5413683153251740432 ) ) ;
#186968=CARTESIAN_POINT ( 'NONE',  ( 2.477515592860125349, 1.084993897938502760, 1.398054747847920609 ) ) ;
#186970=CARTESIAN_POINT ( 'NONE',  ( 2.701816853162309684, 1.425160482578791354, 1.422027561765064174 ) ) ;
#186971=CARTESIAN_POINT ( 'NONE',  ( 5.754950181447250124, -1.742976869204535983, 1.353379275444612562 ) ) ;
#186974=CARTESIAN_POINT ( 'NONE',  ( 4.811248821985151913, 1.762591750878339081, -1.178568461981117643 ) ) ;
#186975=CARTESIAN_POINT ( 'NONE',  ( 3.743767684670766371, 2.000855813463810584, -0.2496267151909299931 ) ) ;
#186976=CARTESIAN_POINT ( 'NONE',  ( 4.658376882426285448, 1.807244876408566681, 0.1260263862136162261 ) ) ;
#186981=CARTESIAN_POINT ( 'NONE',  ( 1.973319494866377699, 1.790917844098998124, -0.5403536831049270406 ) ) ;
#186982=CARTESIAN_POINT ( 'NONE',  ( 6.727182134110220701, 0.005875948494733078051, 1.810970247402940103 ) ) ;
#186983=CARTESIAN_POINT ( 'NONE',  ( 6.516260798181108704, -1.810903427820510503, 0.05229752674829404868 ) ) ;
#186989=CARTESIAN_POINT ( 'NONE',  ( 0.4043728756845180183, -1.898191424145349471, -0.2318213773434482650 ) ) ;
#186992=CARTESIAN_POINT ( 'NONE',  ( 2.101936620064443151, 0.7537240185569763495, -1.811501260397870405 ) ) ;
#186995=CARTESIAN_POINT ( 'NONE',  ( 4.447591161967184625, -1.937652164471121763, 0.8620916771790233524 ) ) ;
#186996=CARTESIAN_POINT ( 'NONE',  ( -0.1296875068448159751, 0.001480089298542403009, -1.826395826379861864 ) ) ;
#186998=CARTESIAN_POINT ( 'NONE',  ( 5.852796007109359877, -1.555770171409420977, 1.210649060634989560 ) ) ;
#187000=CARTESIAN_POINT ( 'NONE',  ( 0.6682274066662279299, 2.010706302723582972, -0.1030755154480169355 ) ) ;
#187002=CARTESIAN_POINT ( 'NONE',  ( -0.1349523647116790404, -0.1509472049114955194, -2.083628827036696052 ) ) ;
#187004=CARTESIAN_POINT ( 'NONE',  ( 1.873570696236816158, -0.2555354716398828274, 2.054483085851127377 ) ) ;
#187008=CARTESIAN_POINT ( 'NONE',  ( 5.279275078172800839, 1.403616728028998395, 1.549557787628618399 ) ) ;
#187010=CARTESIAN_POINT ( 'NONE',  ( 3.592628304870106870, -0.3553021837224104584, -1.790491875447843384 ) ) ;
#187011=CARTESIAN_POINT ( 'NONE',  ( 2.015983567491559381, -1.811083833189537806, 0.04518873659950343319 ) ) ;
#187013=CARTESIAN_POINT ( 'NONE',  ( 6.111994396789379280, -2.190734547077430872, 0.2660306753756238041 ) ) ;
#187015=CARTESIAN_POINT ( 'NONE',  ( 3.926972183325681875, 2.094573593246536802, 0.6948772193901550098 ) ) ;
#187017=CARTESIAN_POINT ( 'NONE',  ( 2.490748672031910083, -1.830495558572857728, -0.5533032672612181457 ) ) ;
#187019=CARTESIAN_POINT ( 'NONE',  ( 6.391088794356012848, 0.1989163192229244648, 2.060770550043041993 ) ) ;
#187022=CARTESIAN_POINT ( 'NONE',  ( 5.987848539424092564, -2.180829346447300310, -0.2163489798085171945 ) ) ;
#187027=CARTESIAN_POINT ( 'NONE',  ( 3.936663633328242096, 0.2718032920513112627, 1.850550731861917653 ) ) ;
#187033=CARTESIAN_POINT ( 'NONE',  ( 6.719590346122157776, 0.3599300073104904074, -2.038585587018165945 ) ) ;
#187035=CARTESIAN_POINT ( 'NONE',  ( 1.423454079394898875, -1.462460055423294047, -1.388472309132340321 ) ) ;
#187039=CARTESIAN_POINT ( 'NONE',  ( 1.359612608069911133, 2.158557413232742750, -0.3773744582575569995 ) ) ;
#187040=CARTESIAN_POINT ( 'NONE',  ( 4.758326833623739205, 0.7015320795021735556, 1.685726030614169924 ) ) ;
#187048=CARTESIAN_POINT ( 'NONE',  ( 3.438839575862782549, -1.396446551253815782, -1.200180114512699792 ) ) ;
#187049=CARTESIAN_POINT ( 'NONE',  ( 5.730732165690560542, 1.348809278943388534, -1.494750323444839601 ) ) ;
#187050=CARTESIAN_POINT ( 'NONE',  ( 2.302535375473542700, -2.053259096611260937, 1.032894330136547856 ) ) ;
#187052=CARTESIAN_POINT ( 'NONE',  ( 6.684431423333510480, 1.132142624513672091, -1.601896353945003071 ) ) ;
#187055=CARTESIAN_POINT ( 'NONE',  ( 3.427896188528327226, -1.883279545317056547, 0.3315703044584616399 ) ) ;
#187059=CARTESIAN_POINT ( 'NONE',  ( 3.122686798916929352, 0.05371976762510695391, 2.090236283336026180 ) ) ;
#187060=CARTESIAN_POINT ( 'NONE',  ( 1.463515404423965105, 1.843522461416190250, -0.3164952454337774390 ) ) ;
#187061=CARTESIAN_POINT ( 'NONE',  ( 2.161482305958133399, -0.5350050527693461788, -1.943774068525660148 ) ) ;
#187064=CARTESIAN_POINT ( 'NONE',  ( 3.104748464929545371, -0.3365338927540823533, 1.707397895346264738 ) ) ;
#187068=CARTESIAN_POINT ( 'NONE',  ( 3.404663882806455266, 1.358838683821527393, -1.062305643495575103 ) ) ;
#187069=CARTESIAN_POINT ( 'NONE',  ( 4.423480980095358284, -1.348712413769267426, -1.727291790683552541 ) ) ;
#187070=CARTESIAN_POINT ( 'NONE',  ( 5.795608111622330583, 1.668732747960173235, 1.444295198399044855 ) ) ;
#187072=CARTESIAN_POINT ( 'NONE',  ( 3.573241956510754491, 1.960547127731948613, 0.9329660139856699175 ) ) ;
#187073=CARTESIAN_POINT ( 'NONE',  ( 2.754317325142870754, 0.6151756178996542479, 1.719052816137212503 ) ) ;
#187075=CARTESIAN_POINT ( 'NONE',  ( 4.505136581001433882, -0.1005046246093168893, 2.115047560132724325 ) ) ;
#187076=CARTESIAN_POINT ( 'NONE',  ( 6.539320575229215393, 2.445213257098968640, 2.379920919941742152 ) ) ;
#187078=CARTESIAN_POINT ( 'NONE',  ( 4.616876278103482001, -0.1136277499396514262, 2.289655339347085317 ) ) ;
#187080=CARTESIAN_POINT ( 'NONE',  ( 6.720655732516649827, 7.053635520514346169, 2.324416633011537225 ) ) ;
#187082=CARTESIAN_POINT ( 'NONE',  ( 0.2938078718510480081, 1.976988316466289142, -0.7672523047414223640 ) ) ;
#187088=CARTESIAN_POINT ( 'NONE',  ( 5.590470263882489910, -0.4872053753022275169, 1.956560708789633285 ) ) ;
#187090=CARTESIAN_POINT ( 'NONE',  ( 3.186439481354142789, 1.149679979862153756, -1.712247615763124120 ) ) ;
#187092=CARTESIAN_POINT ( 'NONE',  ( -0.1408020194050328411, 7.629137130509059617, -2.700278568655100742 ) ) ;
#187096=CARTESIAN_POINT ( 'NONE',  ( 5.806613533822880591, 1.931179984464112653, 1.035834350304319695 ) ) ;
#187097=CARTESIAN_POINT ( 'NONE',  ( 4.096327398540238640, -0.3419367296172080017, 1.987046374476949095 ) ) ;
#187098=CARTESIAN_POINT ( 'NONE',  ( 3.702549152423353807, 1.581054339307564449, 0.9433870219286569769 ) ) ;
#187100=CARTESIAN_POINT ( 'NONE',  ( 0.5336903687956630060, 0.8928529924820073349, -1.475541649381803433 ) ) ;
#187102=CARTESIAN_POINT ( 'NONE',  ( 1.020660257703887908, -2.075033540828072454, 0.9893533861183384515 ) ) ;
#187104=CARTESIAN_POINT ( 'NONE',  ( 0.6501784551898766029, 0.7083214130543177278, -2.148700229429708841 ) ) ;
#187105=CARTESIAN_POINT ( 'NONE',  ( 3.510471945985794928, -0.8535800194418289299, -1.925527614133336840 ) ) ;
#187115=CARTESIAN_POINT ( 'NONE',  ( 2.215225606797793567, 1.700350911433265555, -1.266953333846132512 ) ) ;
#187116=CARTESIAN_POINT ( 'NONE',  ( 4.254274768897357006, 0.9481281144863746846, -2.009013624686401212 ) ) ;
#187117=CARTESIAN_POINT ( 'NONE',  ( 2.308753661914957345, 1.958203289975643191, 0.9839491227633669901 ) ) ;
#187120=CARTESIAN_POINT ( 'NONE',  ( 5.512146440779991607, 1.959692598237902761, -0.09458084330612320789 ) ) ;
#187128=CARTESIAN_POINT ( 'NONE',  ( 4.763993809689464065, 0.6627061821620899851, -2.014485251161435286 ) ) ;
#187131=CARTESIAN_POINT ( 'NONE',  ( 5.471600609837615536, 2.084441204114939161, -0.5725544205837928002 ) ) ;
#187133=CARTESIAN_POINT ( 'NONE',  ( 5.249485218566786848, 1.838879873951340782, -0.09611505855997713732 ) ) ;
#187136=CARTESIAN_POINT ( 'NONE',  ( 0.2568327444973814155, 1.721937519821172602, -0.2522849218079876721 ) ) ;
#187137=CARTESIAN_POINT ( 'NONE',  ( 6.827182134110161726, 7.629137130509051623, 2.510944104600740356 ) ) ;
#187140=CARTESIAN_POINT ( 'NONE',  ( 3.907220446582274853, 1.852832235905249370, 1.113321777468062823 ) ) ;
#187144=CARTESIAN_POINT ( 'NONE',  ( 3.344745324850742385, 0.5235245934552492653, 2.097234944377385002 ) ) ;
#187145=CARTESIAN_POINT ( 'NONE',  ( 4.446526809179438544, 0.5226573815438217974, 1.900768696068744434 ) ) ;
#187146=CARTESIAN_POINT ( 'NONE',  ( 3.620171223323872756, 0.4232754169638303643, -1.681204106648684693 ) ) ;
#187147=CARTESIAN_POINT ( 'NONE',  ( 0.9783777488623355278, -2.139296967303818686, -0.4750931833387496694 ) ) ;
#187148=CARTESIAN_POINT ( 'NONE',  ( 1.237850453945861906, -2.084960033126967982, 0.9891342380793988198 ) ) ;
#187149=CARTESIAN_POINT ( 'NONE',  ( 3.602854949731192136, 1.626725521824391230, -1.265059968925500211 ) ) ;
#187150=CARTESIAN_POINT ( 'NONE',  ( 5.741732329385339284, 1.940029712683045915, 0.09120231522616148445 ) ) ;
#187157=CARTESIAN_POINT ( 'NONE',  ( 3.962124768131184638, 2.190450126196175074, -0.2673064950309556043 ) ) ;
#187159=ORIENTED_EDGE ( 'NONE', *, *, #135726, .T. ) ;
#187160=CARTESIAN_POINT ( 'NONE',  ( 0.7427237327431088776, -0.2200284318808701234, -1.847805914472876232 ) ) ;
#187161=CARTESIAN_POINT ( 'NONE',  ( 6.539320575229276677, 6.035451701470580410, 2.698157228745074576 ) ) ;
#187165=CARTESIAN_POINT ( 'NONE',  ( 6.825078400183550720, 4.691998341648846882, 2.606919129228836507 ) ) ;
#187166=CARTESIAN_POINT ( 'NONE',  ( 6.615202361034350886, -1.784545987531281019, 0.4526050685512914007 ) ) ;
#187167=ORIENTED_EDGE ( 'NONE', *, *, #137354, .F. ) ;
#187168=CARTESIAN_POINT ( 'NONE',  ( 2.096624111547572777, -0.5486670241920866831, -1.986447216630163659 ) ) ;
#187175=CARTESIAN_POINT ( 'NONE',  ( 1.340775744366573541, 0.4011420747369342510, 2.021288966927562214 ) ) ;
#187180=CARTESIAN_POINT ( 'NONE',  ( 5.567066847960510323, -1.993696164035433371, -0.9465883713010987410 ) ) ;
#187181=CARTESIAN_POINT ( 'NONE',  ( 6.608658273995139609, 1.683185115790312603, -1.511970481837302760 ) ) ;
#187183=CARTESIAN_POINT ( 'NONE',  ( 0.2637284958507991606, 0.5978344860198721022, -1.816641584731902626 ) ) ;
#187184=CARTESIAN_POINT ( 'NONE',  ( 0.9367328597341374463, -1.586666764284098807, 1.244388658875786424 ) ) ;
#187186=CARTESIAN_POINT ( 'NONE',  ( 1.441203352352852463, 1.369654091668540241, 1.845602877388529572 ) ) ;
#187191=CARTESIAN_POINT ( 'NONE',  ( 1.674454752297813265, -1.775319108138155633, -0.5897529795871117031 ) ) ;
#187192=CARTESIAN_POINT ( 'NONE',  ( 2.044158018538293042, 0.8666093899718421145, 1.820985203412978093 ) ) ;
#187196=CARTESIAN_POINT ( 'NONE',  ( 5.338542076627605937, 2.074711179890481816, 0.3611063368853023592 ) ) ;
#187201=CARTESIAN_POINT ( 'NONE',  ( 4.324476463189423470, -0.8673186339709404447, -1.824254535609586725 ) ) ;
#187203=CARTESIAN_POINT ( 'NONE',  ( 6.795384964414455276, -1.844194740592384196, 0.9240657454356243639 ) ) ;
#187205=CARTESIAN_POINT ( 'NONE',  ( 5.044278900083454253, 2.155409826167026477, 0.1645634770654491874 ) ) ;
#187211=CARTESIAN_POINT ( 'NONE',  ( 2.453800908837290518, 1.677244079947149302, 1.378686777781912065 ) ) ;
#187214=CARTESIAN_POINT ( 'NONE',  ( 1.593040506729075823, -0.6195558395927207584, 1.734028948791266345 ) ) ;
#187216=CARTESIAN_POINT ( 'NONE',  ( 3.579775959861815515, -1.078688530630707243, 1.907616655872627964 ) ) ;
#187217=CARTESIAN_POINT ( 'NONE',  ( 6.883263157960366030, 0.5727201817382967519, 2.105997115537924902 ) ) ;
#187218=CARTESIAN_POINT ( 'NONE',  ( 3.907294183660753539, 1.938944517003845736, 1.165763813888931688 ) ) ;
#187222=AXIS2_PLACEMENT_3D ( 'NONE', #184590, #36208, #86041 ) ;
#187225=CARTESIAN_POINT ( 'NONE',  ( 5.676936032674533728, -0.04454931526533602304, -1.769330457910125443 ) ) ;
#187227=CARTESIAN_POINT ( 'NONE',  ( 2.151528103076968179, -1.690815887601760270, -1.255243123012689921 ) ) ;
#187230=CARTESIAN_POINT ( 'NONE',  ( 0.5902130973520075541, 1.015489506344388282, -1.687439782384107634 ) ) ;
#187234=CARTESIAN_POINT ( 'NONE',  ( 6.398695480837623961, -1.778505541023298386, -0.3437013697835926140 ) ) ;
#187239=CARTESIAN_POINT ( 'NONE',  ( 4.346470048663173102, 0.4987854378066917116, 1.802870001028591629 ) ) ;
#187242=CARTESIAN_POINT ( 'NONE',  ( 5.928598010555854891, -1.317819122799672504, 1.596621505246295314 ) ) ;
#187252=CARTESIAN_POINT ( 'NONE',  ( 4.615648854252428102, 0.4318217149890530848, -1.913582009320368371 ) ) ;
#187254=CARTESIAN_POINT ( 'NONE',  ( 1.669295836627190610, -0.7230268306642473330, -1.882186858670406693 ) ) ;
#187255=CARTESIAN_POINT ( 'NONE',  ( -0.1108833634137010304, 6.948331553507800962, -2.491992042620773340 ) ) ;
#187256=CARTESIAN_POINT ( 'NONE',  ( -0.1114211809780316365, -0.4883405756051837354, -2.144353428667714390 ) ) ;
#187258=CARTESIAN_POINT ( 'NONE',  ( 2.249088872875557144, -1.499603784168266563, -1.117866018216478574 ) ) ;
#187260=CARTESIAN_POINT ( 'NONE',  ( 3.937747632521654495, -1.925297015496162611, 0.5883167919090799280 ) ) ;
#187264=CARTESIAN_POINT ( 'NONE',  ( 4.007494584968971374, -2.025512140874039524, 0.6163414799803969002 ) ) ;
#187266=CARTESIAN_POINT ( 'NONE',  ( 5.793440749948310042, -1.873300974885267589, 0.8818263447485861217 ) ) ;
#187267=CARTESIAN_POINT ( 'NONE',  ( 1.013356050919094198, -2.038958350640528661, 0.4616950316734638737 ) ) ;
#187268=CARTESIAN_POINT ( 'NONE',  ( 6.720655732516639169, 2.430015300743305406, 2.455394564723146100 ) ) ;
#187269=CARTESIAN_POINT ( 'NONE',  ( 6.036143291503483610, 0.8974207610169572247, -1.589712159477923992 ) ) ;
#187276=CARTESIAN_POINT ( 'NONE',  ( 5.953752735127215701, -1.388294428863137586, -1.315342447896154843 ) ) ;
#187285=CARTESIAN_POINT ( 'NONE',  ( 6.398064575937244314, -0.9530261711272209890, -1.777004751544956962 ) ) ;
#187286=CARTESIAN_POINT ( 'NONE',  ( 0.04773460823432121303, -1.936894771697717621, 0.8635138731061947626 ) ) ;
#187289=CARTESIAN_POINT ( 'NONE',  ( -0.1399997263889819488, 4.088450529495776919, -2.555104583160577203 ) ) ;
#187292=CARTESIAN_POINT ( 'NONE',  ( 3.889471302351163562, -1.821405649934451532, 0.7496272025103620784 ) ) ;
#187294=CARTESIAN_POINT ( 'NONE',  ( 5.026970340808907700, -1.727993218758390404, 1.039010492973009514 ) ) ;
#187297=CARTESIAN_POINT ( 'NONE',  ( 4.962908505822443139, 0.2168217322565080263, -2.180687389885840322 ) ) ;
#187298=CARTESIAN_POINT ( 'NONE',  ( 3.258729403965909821, -1.459781800624770032, 1.257100956980856443 ) ) ;
#187301=CARTESIAN_POINT ( 'NONE',  ( -0.02948999725182251813, 4.092753722544117956, -2.481335295887850290 ) ) ;
#187302=CARTESIAN_POINT ( 'NONE',  ( 0.4697016844467936103, 0.2121168557088908557, -2.196667960996725011 ) ) ;
#187308=CARTESIAN_POINT ( 'NONE',  ( 5.260591308972474067, -0.6599101888420509932, -1.855755260766891235 ) ) ;
#187310=CARTESIAN_POINT ( 'NONE',  ( 0.9076408456279178028, -0.8746481411591797706, -1.734042483418346547 ) ) ;
#187311=CARTESIAN_POINT ( 'NONE',  ( 4.090493406365951934, -1.157184705539246794, 1.647087716845529126 ) ) ;
#187312=CARTESIAN_POINT ( 'NONE',  ( 5.659591354751080772, -0.5502123075824224552, -2.231479479524396403 ) ) ;
#187313=CARTESIAN_POINT ( 'NONE',  ( 3.713571355222999415, 0.4562380391235145161, -1.803994140785330602 ) ) ;
#187319=CARTESIAN_POINT ( 'NONE',  ( 6.532766951017621615, -1.867387138063754337, 0.9404246163645290091 ) ) ;
#187324=CARTESIAN_POINT ( 'NONE',  ( 0.1701549220758866166, -1.195335944658926230, 1.380069390326914336 ) ) ;
#187326=CARTESIAN_POINT ( 'NONE',  ( 2.179902339641195397, 1.341075392948913425, 1.099452185880249067 ) ) ;
#187328=CARTESIAN_POINT ( 'NONE',  ( 6.509000000000048303, 2.074227158855263209, 2.209070705210983032 ) ) ;
#187331=CARTESIAN_POINT ( 'NONE',  ( 6.578989008465588206, 2.022637127319019790, 0.7894149679951308896 ) ) ;
#187332=CARTESIAN_POINT ( 'NONE',  ( 6.076747101522134820, -1.735163100867884500, -0.5679748894881069265 ) ) ;
#187333=CARTESIAN_POINT ( 'NONE',  ( 2.992962298452766845, 0.2353761085502041883, 1.947492218917420637 ) ) ;
#187337=CARTESIAN_POINT ( 'NONE',  ( 3.756581929197760683, 2.110411401290826383, 0.2062832702387565331 ) ) ;
#187341=CARTESIAN_POINT ( 'NONE',  ( 1.745070579777140418, -0.2997347613497360896, -2.048299739058518920 ) ) ;
#187343=CARTESIAN_POINT ( 'NONE',  ( 4.160924129468469346, 0.5925846814045959698, 2.140718581676650079 ) ) ;
#187345=CARTESIAN_POINT ( 'NONE',  ( 2.075183622135381434, -0.9789826713841279782, 2.079913408810558195 ) ) ;
#187347=CARTESIAN_POINT ( 'NONE',  ( 6.297729475711208558, -1.489980986158835119, -1.426453875638087343 ) ) ;
#187353=CARTESIAN_POINT ( 'NONE',  ( 2.548957913124219044, 0.2380835140640499836, 1.897471792728817386 ) ) ;
#187355=CARTESIAN_POINT ( 'NONE',  ( 4.172648073627690302, -1.609630772656017950, -0.6200716988599298540 ) ) ;
#187356=CARTESIAN_POINT ( 'NONE',  ( 2.079314900164643820, 1.561883299538203929, 1.275554356156020086 ) ) ;
#187357=CARTESIAN_POINT ( 'NONE',  ( 4.272342533241332063, 2.053246469231550630, -1.033699615426456830 ) ) ;
#187358=CARTESIAN_POINT ( 'NONE',  ( 4.042437229998629533, 2.251021955006918596, 0.2269351218320627694 ) ) ;
#187359=CARTESIAN_POINT ( 'NONE',  ( 6.252575686221216955, 0.6590897193336446858, 2.000345064990595390 ) ) ;
#187362=CARTESIAN_POINT ( 'NONE',  ( 4.217836599137672060, -0.9083132443464863037, -1.518676986326646938 ) ) ;
#187364=CARTESIAN_POINT ( 'NONE',  ( 0.7797068561936998377, 1.543341569868655450, 1.695032692825575005 ) ) ;
#187365=CARTESIAN_POINT ( 'NONE',  ( 6.175717916360309090, -0.9808100270635997653, 1.557957644481674730 ) ) ;
#187367=CARTESIAN_POINT ( 'NONE',  ( 5.261759291836726860, 1.077959533075742993, 1.907929976554381346 ) ) ;
#187371=CARTESIAN_POINT ( 'NONE',  ( 5.969205681473694902, 1.824102622056431811, 0.9793482939001868504 ) ) ;
#187372=CARTESIAN_POINT ( 'NONE',  ( 1.165250339122084533, 1.861343190080061882, -0.7762330495894869120 ) ) ;
#187374=CARTESIAN_POINT ( 'NONE',  ( 4.775960602080351336, 1.110526314841601359, 1.574030653434669746 ) ) ;
#187376=CARTESIAN_POINT ( 'NONE',  ( 0.7740458967449159733, 0.4260312260581029520, -2.180030009307607042 ) ) ;
#187384=AXIS2_PLACEMENT_3D ( 'NONE', #107990, #189166, #206473 ) ;
#187385=CARTESIAN_POINT ( 'NONE',  ( 2.875390130891414042, -0.1950805366632331617, 1.952157403750237163 ) ) ;
#187389=CARTESIAN_POINT ( 'NONE',  ( 6.883263157960391787, -0.001104538646235289417, 1.946037152736757925 ) ) ;
#187392=CARTESIAN_POINT ( 'NONE',  ( 0.2689492781585648418, -1.474829822998312778, 1.715830925988118816 ) ) ;
#187396=CARTESIAN_POINT ( 'NONE',  ( 1.141631569582121974, 0.7634220068381203372, -1.707866752806507460 ) ) ;
#187397=CARTESIAN_POINT ( 'NONE',  ( 6.837244271306878396, -1.062160112102826126, 1.370476690187643731 ) ) ;
#187399=CARTESIAN_POINT ( 'NONE',  ( 3.685266855566126321, 1.588411730319793769, 1.510178839762461811 ) ) ;
#187400=CARTESIAN_POINT ( 'NONE',  ( 5.333197341169245043, 0.1633263742753125747, 2.301865194068336784 ) ) ;
#187401=CARTESIAN_POINT ( 'NONE',  ( 0.5497720567373615141, 0.6472090466588500401, -1.956683156177397853 ) ) ;
#187402=CARTESIAN_POINT ( 'NONE',  ( 2.519391418834667995, -1.118305101016278558, -1.587446049422422956 ) ) ;
#187408=CARTESIAN_POINT ( 'NONE',  ( 3.586564705785996843, -0.5826563296015655480, 1.930417576838711957 ) ) ;
#187412=CARTESIAN_POINT ( 'NONE',  ( 0.7151340513122245168, -0.2707656271505008982, 1.805370379145049275 ) ) ;
#187418=CARTESIAN_POINT ( 'NONE',  ( 6.578986920187222864, -0.09832028258810160404, -2.058664976587327722 ) ) ;
#187424=CARTESIAN_POINT ( 'NONE',  ( 5.250651393837939551, 1.990147761501987800, 0.3430726210427292311 ) ) ;
#187425=CARTESIAN_POINT ( 'NONE',  ( 5.742908703533418091, 2.140221812536883927, 0.5945068574613203705 ) ) ;
#187429=CARTESIAN_POINT ( 'NONE',  ( 4.979397702276197712, 1.923710689106904015, -0.7398180773239333430 ) ) ;
#187430=CARTESIAN_POINT ( 'NONE',  ( 3.516250148862578584, -1.862017090670412767, 0.7743150488077471527 ) ) ;
#187438=CARTESIAN_POINT ( 'NONE',  ( 4.270861128529729989, -2.010896307770511537, 0.1455111863851859810 ) ) ;
#187439=CARTESIAN_POINT ( 'NONE',  ( 3.943160212656390051, 0.6185462545997171269, -1.734258544408360470 ) ) ;
#187442=CARTESIAN_POINT ( 'NONE',  ( 2.473609491499198398, 0.1116694970143172483, -2.305109432965181337 ) ) ;
#187444=CARTESIAN_POINT ( 'NONE',  ( 3.567792053227138105, 2.109782723108716063, -0.4697668898906853796 ) ) ;
#187448=CARTESIAN_POINT ( 'NONE',  ( 3.075839645193487293, 1.666627022722726670, -1.582919517265988674 ) ) ;
#187450=CARTESIAN_POINT ( 'NONE',  ( 2.236979667955760309, -1.672073921526989748, 0.8388852543278202401 ) ) ;
#187451=CARTESIAN_POINT ( 'NONE',  ( 0.6496080044469240145, 0.6224236735355732630, -1.870565628188630702 ) ) ;
#187455=CARTESIAN_POINT ( 'NONE',  ( 1.647397727484143592, -1.863059487452220386, 1.182652941231487453 ) ) ;
#187461=CARTESIAN_POINT ( 'NONE',  ( 5.875845355493965805, 1.173799634058709129, 1.583810875030462695 ) ) ;
#187462=CARTESIAN_POINT ( 'NONE',  ( 5.496783081331708232, -0.5556612750647730303, -2.239684525637525514 ) ) ;
#187463=CARTESIAN_POINT ( 'NONE',  ( 6.742638014206057129, -1.825417518414352180, -0.3614582840437295941 ) ) ;
#187464=CARTESIAN_POINT ( 'NONE',  ( 3.133693747638730098, 1.960048766001153631, -0.6424893143618380931 ) ) ;
#187471=CARTESIAN_POINT ( 'NONE',  ( 6.426262541905297887, 1.110578645885337501, 1.865513821534901417 ) ) ;
#187472=CARTESIAN_POINT ( 'NONE',  ( 6.727182134110222478, 0.005875948494733079785, 1.810970247402940547 ) ) ;
#187473=CARTESIAN_POINT ( 'NONE',  ( 5.337399561049260832, 0.7408347518493042516, -1.685818907712175019 ) ) ;
#187476=CARTESIAN_POINT ( 'NONE',  ( 0.5087955169046609605, 1.624258005607306599, 0.9276666955444977658 ) ) ;
#187482=CARTESIAN_POINT ( 'NONE',  ( 0.1527893875182678718, 0.3269112364552365091, 1.883972597190447518 ) ) ;
#187483=CARTESIAN_POINT ( 'NONE',  ( 2.412676795855304590, 1.579722209848779313, 0.7981720169879211735 ) ) ;
#187484=CARTESIAN_POINT ( 'NONE',  ( 0.08246951281144777879, -1.249137507218839094, 1.448023666807838117 ) ) ;
#187486=CARTESIAN_POINT ( 'NONE',  ( 4.728101222851567975, 1.910784947378706855, 0.1365434035073622987 ) ) ;
#187488=CARTESIAN_POINT ( 'NONE',  ( 5.283641479639247684, -1.870778298764510961, 0.6161543930274359093 ) ) ;
#187489=CARTESIAN_POINT ( 'NONE',  ( -0.2046613956954954905, -0.1581703332043625232, -2.086340352340488646 ) ) ;
#187491=CARTESIAN_POINT ( 'NONE',  ( 3.291731440620565330, -0.7593194595177065187, 1.709801165022284408 ) ) ;
#187492=CARTESIAN_POINT ( 'NONE',  ( 6.393153111415212031, 1.496800677787715639, -0.8570667202875602575 ) ) ;
#187494=CARTESIAN_POINT ( 'NONE',  ( 1.928631425534212074, 1.268998755960360603, -1.805353087401928569 ) ) ;
#187497=CARTESIAN_POINT ( 'NONE',  ( 0.2212323960570794501, -1.841704181501323312, -0.9290775759197547057 ) ) ;
#187505=CARTESIAN_POINT ( 'NONE',  ( 3.033707436314789785, 1.966763487489433970, -0.6469820378900912328 ) ) ;
#187509=CARTESIAN_POINT ( 'NONE',  ( 1.453777360798803819, -1.464386276593489189, -1.391179603160071387 ) ) ;
#187513=CARTESIAN_POINT ( 'NONE',  ( 0.07499057489264349119, 0.002531239327734773146, -1.955573237620360505 ) ) ;
#187515=CARTESIAN_POINT ( 'NONE',  ( 4.973982425466109802, 1.752763018817087293, 0.9961474888594208377 ) ) ;
#187516=CARTESIAN_POINT ( 'NONE',  ( 5.471877088563796399, -0.8550440501978623375, 1.714365851762880144 ) ) ;
#187517=CARTESIAN_POINT ( 'NONE',  ( 6.539320575229256249, 7.052319431262985105, 2.701414634427783845 ) ) ;
#187518=CARTESIAN_POINT ( 'NONE',  ( 3.404031855413204966, -0.8899279105200922357, -2.002928011436304612 ) ) ;
#187520=CARTESIAN_POINT ( 'NONE',  ( 2.285291272251275707, 0.09004542135446562401, -1.910373438827176251 ) ) ;
#187523=CARTESIAN_POINT ( 'NONE',  ( 0.7027501817156033281, 1.864177386631181044, 0.7691025790682111118 ) ) ;
#187525=CARTESIAN_POINT ( 'NONE',  ( 6.075747529084263299, -1.173811750163206158, 1.850510016281024850 ) ) ;
#187527=CARTESIAN_POINT ( 'NONE',  ( 3.082691909922595563, -0.1251556739016151387, -1.720276473149193297 ) ) ;
#187533=CARTESIAN_POINT ( 'NONE',  ( 0.4144086874100678664, 0.7473079093508437909, 1.814158889769983185 ) ) ;
#187538=ORIENTED_EDGE ( 'NONE', *, *, #14569, .F. ) ;
#187540=CARTESIAN_POINT ( 'NONE',  ( 3.756361958294622383, 1.803085962505234008, 0.1738922897399265421 ) ) ;
#187544=CARTESIAN_POINT ( 'NONE',  ( 4.424329001689049079, -0.7786147893445326540, -1.635752125832173220 ) ) ;
#187548=CARTESIAN_POINT ( 'NONE',  ( 4.932013296703669170, 1.071099452130529039, 1.521725064211083112 ) ) ;
#187550=CARTESIAN_POINT ( 'NONE',  ( 2.864735742032016752, -0.1435939464786405995, -1.910298799178041351 ) ) ;
#187559=CARTESIAN_POINT ( 'NONE',  ( 1.798888674052185888, 1.738860765912113138, 1.160333176109765274 ) ) ;
#187561=CARTESIAN_POINT ( 'NONE',  ( 6.475613818078473471, 1.843275991838376981, -0.5597920731088936730 ) ) ;
#187564=CARTESIAN_POINT ( 'NONE',  ( 2.537895388257872753, 0.8626947210231518115, -1.608888323311054691 ) ) ;
#187566=CARTESIAN_POINT ( 'NONE',  ( 1.346085547170269070, -0.8884179423524626307, 1.757888261374307870 ) ) ;
#187567=CARTESIAN_POINT ( 'NONE',  ( 4.106929586529986409, -0.3288250506029398168, 1.913867117139455676 ) ) ;
#187571=CARTESIAN_POINT ( 'NONE',  ( 6.280112003059028503, -1.032894792506684034, -1.547752956576850858 ) ) ;
#187573=CARTESIAN_POINT ( 'NONE',  ( 4.219064148821600746, 1.637239594409030330, -1.347683705884415106 ) ) ;
#187580=CARTESIAN_POINT ( 'NONE',  ( 4.107882937833263526, -1.820653182827164596, 0.1363937739093170898 ) ) ;
#187586=CARTESIAN_POINT ( 'NONE',  ( 4.276139911362797363, -1.077190196239918851, 1.529178877381555335 ) ) ;
#187589=CARTESIAN_POINT ( 'NONE',  ( 1.980962579895541920, -0.09440724433935901438, -1.924309447538669060 ) ) ;
#187590=CARTESIAN_POINT ( 'NONE',  ( 6.895372015613538963, -1.753720159772365284, 0.8792710811909019153 ) ) ;
#187595=CARTESIAN_POINT ( 'NONE',  ( 1.318125747981816698, 1.040119728068724880, -1.844044674895953806 ) ) ;
#187598=CARTESIAN_POINT ( 'NONE',  ( 4.768459183169745152, -0.8803848081004579385, -1.873848736155204087 ) ) ;
#187599=CARTESIAN_POINT ( 'NONE',  ( 0.7668492355173107677, 1.774547462407764842, -0.4907661837717376407 ) ) ;
#187601=CARTESIAN_POINT ( 'NONE',  ( 5.168667805954368255, 1.541955118739355424, 1.704926945024546336 ) ) ;
#187605=CARTESIAN_POINT ( 'NONE',  ( 1.148812421071528256, -1.804313360470580108, 1.413740901141118611 ) ) ;
#187608=CARTESIAN_POINT ( 'NONE',  ( 4.751864635371732426, 0.7446896046985322926, 1.793680106537680174 ) ) ;
#187612=CARTESIAN_POINT ( 'NONE',  ( 0.01783784634934187929, -0.5327901187049766119, 1.941387642157591742 ) ) ;
#187613=CARTESIAN_POINT ( 'NONE',  ( 6.175017591530616023, 1.752142144017948100, -0.9981200475188132248 ) ) ;
#187617=CARTESIAN_POINT ( 'NONE',  ( 2.818400364232038768, 1.968743758771305918, 0.7038092692753412649 ) ) ;
#187618=CARTESIAN_POINT ( 'NONE',  ( 0.8304726968981954727, 0.1242609525908405232, 1.765545458023538572 ) ) ;
#187621=CARTESIAN_POINT ( 'NONE',  ( 4.541174964560028116, -1.770302748489580358, -1.456204954804733998 ) ) ;
#187622=CARTESIAN_POINT ( 'NONE',  ( 2.360927591450364904, 1.706848764895356085, -0.3387292939842252437 ) ) ;
#187626=CARTESIAN_POINT ( 'NONE',  ( 2.125947893326819660, 0.3012468308378027371, -1.707275946889510676 ) ) ;
#187628=CARTESIAN_POINT ( 'NONE',  ( 2.014367633873125563, 2.165423841567072127, -0.1585431616079237827 ) ) ;
#187630=CARTESIAN_POINT ( 'NONE',  ( 4.417204035549080920, -1.841734835922325120, 0.8216704330437707426 ) ) ;
#187631=CARTESIAN_POINT ( 'NONE',  ( 3.250000000000002665, 1.855058607017213327E-13, 2.052068128417948056 ) ) ;
#187633=CARTESIAN_POINT ( 'NONE',  ( 1.272347295514785870, -1.224129819625971782, 1.487435282370595857 ) ) ;
#187635=CARTESIAN_POINT ( 'NONE',  ( 4.078556047614148028, 1.049247773278503049, 1.958029639119197585 ) ) ;
#187637=CARTESIAN_POINT ( 'NONE',  ( -0.1106856583841242386, 6.948332279000682732, -2.591999772403537516 ) ) ;
#187641=CARTESIAN_POINT ( 'NONE',  ( 0.3115808214643934204, 1.843292235811417878, -1.239274738845694390 ) ) ;
#187642=CARTESIAN_POINT ( 'NONE',  ( 5.336364984333265227, -1.091323163865608459, 1.630109012322231266 ) ) ;
#187645=CARTESIAN_POINT ( 'NONE',  ( 0.4390364970160881564, 0.3691015439823107092, 2.129678967336546602 ) ) ;
#187649=CARTESIAN_POINT ( 'NONE',  ( 3.754389245258652252, -2.060177385294372776, -0.1042076536686628307 ) ) ;
#187653=CARTESIAN_POINT ( 'NONE',  ( 5.044154037833219029, 1.865456107639616556, 0.1390639465682907416 ) ) ;
#187654=CARTESIAN_POINT ( 'NONE',  ( 3.885211248783075888, -0.5490618756427265712, -1.644986201639383028 ) ) ;
#187655=CARTESIAN_POINT ( 'NONE',  ( 2.946521060880839205, -1.424341091986385921, -0.9998927444686573907 ) ) ;
#187656=CARTESIAN_POINT ( 'NONE',  ( 0.3458147113889240565, 0.7113776200376471515, -2.179290858394256070 ) ) ;
#187658=CARTESIAN_POINT ( 'NONE',  ( 5.073812392315714348, -1.160337598488449196, 1.738990438290926921 ) ) ;
#187659=CARTESIAN_POINT ( 'NONE',  ( 6.351511478899689145, 1.936555568076937295, -0.1455203235936879114 ) ) ;
#187661=CARTESIAN_POINT ( 'NONE',  ( 1.055314813143366726, -1.277040974352643854, 1.560502084637045650 ) ) ;
#187662=CARTESIAN_POINT ( 'NONE',  ( 0.6684183810189650021, 2.117893379942568988, -0.1100008709709817956 ) ) ;
#187663=CARTESIAN_POINT ( 'NONE',  ( 6.328750030911493241, 0.7691242348151774433, -1.864167186630163009 ) ) ;
#187666=CARTESIAN_POINT ( 'NONE',  ( 2.069135417989849568, -1.637292086295978111, 1.347470637625711731 ) ) ;
#187668=CARTESIAN_POINT ( 'NONE',  ( 4.898959864523320107, 1.516061528642864253, -1.016892643307308441 ) ) ;
#187674=CARTESIAN_POINT ( 'NONE',  ( 2.672133692126318127, 2.009681031688851593, -0.2020390005853574256 ) ) ;
#187675=CARTESIAN_POINT ( 'NONE',  ( 5.825267882404531861, -0.05969703229705652925, 2.206138628428089277 ) ) ;
#187679=CARTESIAN_POINT ( 'NONE',  ( 3.397144026274971029, -1.643366908016094641, 0.8731178804023755902 ) ) ;
#187685=CARTESIAN_POINT ( 'NONE',  ( 5.285714101943871590, 1.228958891529348785, 1.350286652578087665 ) ) ;
#187689=CARTESIAN_POINT ( 'NONE',  ( 6.854846703925610463, -0.8643618726141141240, 1.819651424301058640 ) ) ;
#187690=CARTESIAN_POINT ( 'NONE',  ( -0.02397475188680147154, -0.1303385410800334265, -1.711279094490937069 ) ) ;
#187691=CARTESIAN_POINT ( 'NONE',  ( 5.461655971716653291, 0.4551397948197592469, -2.262217722918384410 ) ) ;
#187693=CARTESIAN_POINT ( 'NONE',  ( 6.591117433763723277, 1.884315261875910474, -1.059023293578951863 ) ) ;
#187697=CARTESIAN_POINT ( 'NONE',  ( 6.151801744867631427, -0.3282927394851458125, -2.274731023314037870 ) ) ;
#187700=CARTESIAN_POINT ( 'NONE',  ( 6.139502064137229986, -1.356240498024411600, -1.288626068300227523 ) ) ;
#187701=CARTESIAN_POINT ( 'NONE',  ( 3.533378866418676711, -0.1359047358975660202, 1.907598245988059826 ) ) ;
#187703=CARTESIAN_POINT ( 'NONE',  ( 5.250674450588199704, 0.6379336648693231249, 2.112661011922472021 ) ) ;
#187704=CARTESIAN_POINT ( 'NONE',  ( 4.803976500543080341, -1.135498674831243227, -1.786957999583696610 ) ) ;
#187706=CARTESIAN_POINT ( 'NONE',  ( 6.983263157960372780, 1.247263239625576059, 2.158450195331083510 ) ) ;
#187709=CARTESIAN_POINT ( 'NONE',  ( 5.619825546450978315, -0.5151785252428126016, 2.056841324599982368 ) ) ;
#187710=CARTESIAN_POINT ( 'NONE',  ( 2.661487998672926292, -2.007448288467659214, -1.137923995292255741 ) ) ;
#187711=CARTESIAN_POINT ( 'NONE',  ( 3.736726379466179804, -1.890069333072645241, -0.5255722985574098338 ) ) ;
#187713=CARTESIAN_POINT ( 'NONE',  ( 0.2390249890181182224, -0.1369461163322066299, -1.930431041017650395 ) ) ;
#187717=CARTESIAN_POINT ( 'NONE',  ( 5.612517632836664383, 1.944729323200470095, 0.5331731267440716904 ) ) ;
#187719=CARTESIAN_POINT ( 'NONE',  ( 0.09336763325077861164, -1.840659761701424646, -0.04852334659839750014 ) ) ;
#187721=CARTESIAN_POINT ( 'NONE',  ( 3.625983508040203862, 2.119313185944927902, -0.4706255054970372997 ) ) ;
#187723=CARTESIAN_POINT ( 'NONE',  ( 0.8441712343106638761, -1.349783269286155774, -1.635521010841307410 ) ) ;
#187727=CARTESIAN_POINT ( 'NONE',  ( 0.8607048193125128588, -1.494471031236654257, 1.419199468611084480 ) ) ;
#187733=CARTESIAN_POINT ( 'NONE',  ( 3.070860992347378637, -1.446505282863861375, 1.250851760459831041 ) ) ;
#187736=CARTESIAN_POINT ( 'NONE',  ( 5.700005536890629720, -1.770032025875327042, 0.003423177859356376761 ) ) ;
#187739=CARTESIAN_POINT ( 'NONE',  ( 0.7557781591117664899, 0.7332364915693561080, -1.656728582389139781 ) ) ;
#187741=CARTESIAN_POINT ( 'NONE',  ( 1.112342557844925750, 1.847186106069747646, 0.5076494344821417259 ) ) ;
#187742=CARTESIAN_POINT ( 'NONE',  ( 1.768117254402020277, -2.054967671486531255, 0.2513356459030794410 ) ) ;
#187744=CARTESIAN_POINT ( 'NONE',  ( 6.332864056472936376, 0.1854757364097951722, 1.861418627818342664 ) ) ;
#187745=CARTESIAN_POINT ( 'NONE',  ( 2.437895498511342574, 0.8609710149188254391, -1.609920059450341778 ) ) ;
#187746=CARTESIAN_POINT ( 'NONE',  ( 6.621690180768193379, -2.141820631849135292, 0.5315211216728524812 ) ) ;
#187749=CARTESIAN_POINT ( 'NONE',  ( 3.684078386338876854, -1.226296459201616340, -1.658441301575198645 ) ) ;
#187752=DIRECTION ( 'NONE',  ( 1.039099362110107450E-15, 1.000000000000000000, -4.583713267641621330E-32 ) ) ;
#187753=CARTESIAN_POINT ( 'NONE',  ( 0.8784639925019832596, -1.201575844224999301, 1.796657101444131932 ) ) ;
#187754=CARTESIAN_POINT ( 'NONE',  ( 6.320769956279724155, -1.466918727022302971, 1.461273828345016845 ) ) ;
#187756=CARTESIAN_POINT ( 'NONE',  ( 3.954491917119377753, 0.7739500986865335275, 2.018479124525011770 ) ) ;
#187757=CARTESIAN_POINT ( 'NONE',  ( 4.406902263202909786, -0.4446603063312704607, -1.969940172527106625 ) ) ;
#187758=CARTESIAN_POINT ( 'NONE',  ( 6.620655732516611103, 6.033324165176342291, 2.868629481857593255 ) ) ;
#187764=CARTESIAN_POINT ( 'NONE',  ( 2.114470590943520634, 1.957170936680457052, 0.4852650170619755565 ) ) ;
#187768=CARTESIAN_POINT ( 'NONE',  ( 5.642805672956042962, 1.844803604357934779, 0.5037821151940986564 ) ) ;
#187772=CARTESIAN_POINT ( 'NONE',  ( 4.886342304379579282, -0.6820123065829878373, -1.897693145932321857 ) ) ;
#187775=CARTESIAN_POINT ( 'NONE',  ( 6.792093547228882144, -0.7321312287554645470, 1.560492760358098918 ) ) ;
#187780=CARTESIAN_POINT ( 'NONE',  ( 5.272658424858247095, -1.760895560629770262, -0.6313210838888929644 ) ) ;
#187782=CARTESIAN_POINT ( 'NONE',  ( 1.938418878558012315, -1.110983660290700170, 1.746734030103759938 ) ) ;
#187787=CARTESIAN_POINT ( 'NONE',  ( 0.6324356828835416833, 0.5880426346329314935, 1.928746166857209676 ) ) ;
#187788=CARTESIAN_POINT ( 'NONE',  ( 1.458926887072587553, -1.529292093677349307, 0.9708203095366783053 ) ) ;
#187795=CARTESIAN_POINT ( 'NONE',  ( 5.624599552000627334, 0.3785363404739845450, 1.877648607602548925 ) ) ;
#187803=CARTESIAN_POINT ( 'NONE',  ( 2.975616057669258741, 2.053088362031017855, -0.6768339029224537118 ) ) ;
#187806=CARTESIAN_POINT ( 'NONE',  ( 1.125412309253082332, 1.872817075645373697, 0.9946839901537675166 ) ) ;
#187807=EDGE_CURVE ( 'NONE', #64278, #76973, #19562, .T. ) ;
#187808=CARTESIAN_POINT ( 'NONE',  ( 5.702125722003772879, -1.825762228975034596, 0.002264948092654816680 ) ) ;
#187810=CARTESIAN_POINT ( 'NONE',  ( 1.862511354659317053, -1.396895987378836690, 1.391268958170795100 ) ) ;
#187811=CARTESIAN_POINT ( 'NONE',  ( 4.078302138561982204, 0.9061299177482335931, 1.684124486321957104 ) ) ;
#187813=CARTESIAN_POINT ( 'NONE',  ( 4.932068866601894364, 1.132370341068598796, 1.611282302955379553 ) ) ;
#187814=CARTESIAN_POINT ( 'NONE',  ( 0.6912261618599843116, -0.6995774015170745930, 1.811736774657431548 ) ) ;
#187820=CARTESIAN_POINT ( 'NONE',  ( 5.303337639526568559, 1.684534858470821961, -0.9050978215178404618 ) ) ;
#187823=CARTESIAN_POINT ( 'NONE',  ( 1.220068447022312652, -2.152735442661047216, 0.4846846590640523367 ) ) ;
#187825=CARTESIAN_POINT ( 'NONE',  ( 5.760407631487725055, 2.010880845746499279, 0.09660876809274536459 ) ) ;
#187826=CARTESIAN_POINT ( 'NONE',  ( 0.07680821025393863577, 5.725641208404781857, -2.404836704152548688 ) ) ;
#187829=CARTESIAN_POINT ( 'NONE',  ( 3.139188941651628539, -0.1496422021231707811, -2.064996656166856237 ) ) ;
#187833=CARTESIAN_POINT ( 'NONE',  ( 0.7081719773709761467, -2.151164098719647200, 0.2130325561137471624 ) ) ;
#187838=CARTESIAN_POINT ( 'NONE',  ( 6.925078400183547700, 0.5992389604297322370, 1.809181922849491198 ) ) ;
#187840=CARTESIAN_POINT ( 'NONE',  ( 5.063005163341266268, -0.9570555141230531193, 1.445894719807367723 ) ) ;
#187843=CARTESIAN_POINT ( 'NONE',  ( 1.973570569994816060, -0.2575147360633044391, 2.054139978358980656 ) ) ;
#187844=CARTESIAN_POINT ( 'NONE',  ( 5.114917985578482096, 0.1569784262732084601, 2.111484538518786813 ) ) ;
#187847=CARTESIAN_POINT ( 'NONE',  ( 1.674589265674136129, 1.326639880153294371, -1.455732889183375178 ) ) ;
#187850=CARTESIAN_POINT ( 'NONE',  ( 5.015721488424509822, -1.223180480392561886, -1.938471153541870384 ) ) ;
#187851=CARTESIAN_POINT ( 'NONE',  ( 1.453431991042982041, 0.5316948868413253759, -1.746555546766684675 ) ) ;
#187855=CARTESIAN_POINT ( 'NONE',  ( 3.076434440837049866, 0.9091080936043660632, 1.796352098325330715 ) ) ;
#187856=CARTESIAN_POINT ( 'NONE',  ( 3.502741298630154709, 0.4721981695934416856, 1.903977903881831191 ) ) ;
#187860=CARTESIAN_POINT ( 'NONE',  ( 6.597611690090901426, -2.090214587215084130, 0.04977907537380765746 ) ) ;
#187861=CARTESIAN_POINT ( 'NONE',  ( 4.557331473417879586, 0.3865553534455662965, -1.726927170965624647 ) ) ;
#187863=CARTESIAN_POINT ( 'NONE',  ( 0.2346725361867564585, 0.3788711812165134196, 2.158297013397599162 ) ) ;
#187864=CARTESIAN_POINT ( 'NONE',  ( 5.349435159262297290, 1.738085940734758639, -0.09086515553361101949 ) ) ;
#187866=CARTESIAN_POINT ( 'NONE',  ( 6.399114681295562157, -1.079681622539971464, -2.029393132690388235 ) ) ;
#187868=CARTESIAN_POINT ( 'NONE',  ( 5.940742354060237318, 1.035569694170878519, 1.390440122839208703 ) ) ;
#187869=CARTESIAN_POINT ( 'NONE',  ( 1.963769682107346037, 0.3752889857368995608, -2.174583152744386627 ) ) ;
#187871=CARTESIAN_POINT ( 'NONE',  ( 6.074718851800529507, 1.462630930118626660, -1.604749943717192373 ) ) ;
#187874=CARTESIAN_POINT ( 'NONE',  ( 1.112693368687894369, 2.042276985739148731, 0.5586806735067056939 ) ) ;
#187875=CARTESIAN_POINT ( 'NONE',  ( 3.437500000000002665, 1.451031289060976448, -1.451031289061255780 ) ) ;
#187876=CARTESIAN_POINT ( 'NONE',  ( 6.727182134110194944, 2.413774403037728167, 2.569658639860139093 ) ) ;
#187877=CARTESIAN_POINT ( 'NONE',  ( 4.823225626762606133, -0.09501261394700975804, 1.924175346943966414 ) ) ;
#187878=CARTESIAN_POINT ( 'NONE',  ( 0.7861345822535183991, 2.139302153856616151, -0.5977261144227277168 ) ) ;
#187880=CARTESIAN_POINT ( 'NONE',  ( 1.593750267980385882, -0.7671775610453807070, 2.160330554385545110 ) ) ;
#187884=CARTESIAN_POINT ( 'NONE',  ( 3.563320577568354075, -1.815308083731239419, 1.279909030408127091 ) ) ;
#187890=CARTESIAN_POINT ( 'NONE',  ( 1.283827520628720187, 1.646837967535810021, -1.163270716046126196 ) ) ;
#187892=CARTESIAN_POINT ( 'NONE',  ( 6.215292634054179643, -1.767141628190834757, -1.063693359622622125 ) ) ;
#187895=CARTESIAN_POINT ( 'NONE',  ( 0.2218712608162629052, 1.761692264604281633, 0.5354471447000588302 ) ) ;
#187897=CARTESIAN_POINT ( 'NONE',  ( 1.211743588231738888, -0.7890745783359112142, -1.584151303567796543 ) ) ;
#187898=CARTESIAN_POINT ( 'NONE',  ( 0.2467204944939948574, 1.994070950632735428, -0.2986300710981006357 ) ) ;
#187899=CARTESIAN_POINT ( 'NONE',  ( 6.603062865972897377, -0.3679811349713958957, 1.707173594542527040 ) ) ;
#187900=CARTESIAN_POINT ( 'NONE',  ( 4.300488954165425426, 1.772315894223834176, -1.453880271152303116 ) ) ;
#187901=CARTESIAN_POINT ( 'NONE',  ( 3.820104440490858622, 1.748809976318686177, 0.5759312369505511509 ) ) ;
#187903=CARTESIAN_POINT ( 'NONE',  ( 3.434410497111122673, 1.780829521046650932, 0.4009754434649847044 ) ) ;
#187904=CARTESIAN_POINT ( 'NONE',  ( 4.236954046275762664, 2.015912997090345549, -0.05229627655192746472 ) ) ;
#187906=CARTESIAN_POINT ( 'NONE',  ( 3.784249319668216760, -1.117672106238891461, 1.967118024168002410 ) ) ;
#187908=CARTESIAN_POINT ( 'NONE',  ( 5.438542061945497608, 2.074265116652589391, 0.3630613376124564584 ) ) ;
#187910=CARTESIAN_POINT ( 'NONE',  ( 3.385274849524767316, 0.04804411014160993310, 2.069964801482151895 ) ) ;
#187913=CARTESIAN_POINT ( 'NONE',  ( 6.287751673603878544, 2.029294879081492198, -0.6150919484220889188 ) ) ;
#187915=CARTESIAN_POINT ( 'NONE',  ( 1.014139625077722595, -0.8655271193952519537, -1.721200913303379654 ) ) ;
#187922=CARTESIAN_POINT ( 'NONE',  ( 0.9146621208586953600, -2.221583675102642097, 0.007239306818007660779 ) ) ;
#187924=CARTESIAN_POINT ( 'NONE',  ( 2.503073473877976518, 1.692030140557040152, -1.253631523096561784 ) ) ;
#187927=CARTESIAN_POINT ( 'NONE',  ( 0.1329588055935396196, 0.006246367379872731426, -1.846049620084761367 ) ) ;
#187935=CARTESIAN_POINT ( 'NONE',  ( 3.666413850373055006, -0.7928392042928497085, -1.794698522912529182 ) ) ;
#187936=CARTESIAN_POINT ( 'NONE',  ( 1.692469166403000491, -2.151312531270420436, -0.2117842694067117448 ) ) ;
#187937=CARTESIAN_POINT ( 'NONE',  ( 1.733694375844633706, 1.821329977863223926, 0.2691589665217360983 ) ) ;
#187940=CARTESIAN_POINT ( 'NONE',  ( 3.696946667989671642, -0.5033324012985186391, 1.665945954428204923 ) ) ;
#187944=CARTESIAN_POINT ( 'NONE',  ( 0.7433210806352362754, -1.853469564684958382, 1.112228649290482263 ) ) ;
#187946=CARTESIAN_POINT ( 'NONE',  ( 3.497422563753574298, 1.966343570655813666, 0.4444343670074250574 ) ) ;
#187948=CARTESIAN_POINT ( 'NONE',  ( 0.1280963075596490419, -1.331634228802502928, -1.703589906866372017 ) ) ;
#187950=CARTESIAN_POINT ( 'NONE',  ( 2.237131214483905950, -1.761753319436863086, 0.8849394531919276830 ) ) ;
#187951=CARTESIAN_POINT ( 'NONE',  ( 6.609000000000036401, 0.5823242425131782696, 2.053003180352876100 ) ) ;
#187952=CARTESIAN_POINT ( 'NONE',  ( 2.278764488077251738, 1.774667200368160280, -0.7891824313753895703 ) ) ;
#187957=CARTESIAN_POINT ( 'NONE',  ( -0.1108833634137009749, 4.092508091048022933, -2.451885048449681914 ) ) ;
#187961=CARTESIAN_POINT ( 'NONE',  ( 5.508889292638126989, 1.751971812537992834, -1.501964572959401778 ) ) ;
#187964=CARTESIAN_POINT ( 'NONE',  ( 4.153139481255548660, 1.659551801668930793, -1.045809187271130591 ) ) ;
#187966=CARTESIAN_POINT ( 'NONE',  ( 0.4928148368598186946, -2.006445878461552645, 0.2004378712678403507 ) ) ;
#187968=CARTESIAN_POINT ( 'NONE',  ( 2.624332661740484962, 2.101919520188862744, 0.2543673568942694252 ) ) ;
#187972=CARTESIAN_POINT ( 'NONE',  ( 2.941158370608713213, 0.6622022323767087215, -1.718108305994885177 ) ) ;
#187976=CARTESIAN_POINT ( 'NONE',  ( 3.674183785563363447, 2.104178206457421485, -0.2630699042918820396 ) ) ;
#187977=CARTESIAN_POINT ( 'NONE',  ( 0.6382991350510487383, -1.580419255802448575, 0.9442637585924051891 ) ) ;
#187982=CARTESIAN_POINT ( 'NONE',  ( 3.848945901207713849, -1.686846252213095365, 1.183521113291643223 ) ) ;
#187984=CARTESIAN_POINT ( 'NONE',  ( 1.628196140939692338, 0.1813696128579282696, 1.832309401408799276 ) ) ;
#187989=CARTESIAN_POINT ( 'NONE',  ( 1.541937560865791479, -1.600244427420342896, -1.519961040588948986 ) ) ;
#187990=CARTESIAN_POINT ( 'NONE',  ( 4.042437229998629533, 2.251021955006918596, 0.2269351218320627694 ) ) ;
#187992=CARTESIAN_POINT ( 'NONE',  ( 3.375094514129430845, -1.600109896321648462, -0.8493348278759412784 ) ) ;
#187993=CARTESIAN_POINT ( 'NONE',  ( 3.766719225569253204, -0.1932013629946625344, -1.905979854919868988 ) ) ;
#187994=CARTESIAN_POINT ( 'NONE',  ( 5.811005889236001032, -1.634438611397070806, 1.270752202701043609 ) ) ;
#187996=CARTESIAN_POINT ( 'NONE',  ( 3.309407512850143451, -0.3859909667141645517, 1.933149248684182808 ) ) ;
#187997=CARTESIAN_POINT ( 'NONE',  ( 1.202032481184050816, -1.926566264184792709, -0.002868833312720530347 ) ) ;
#187998=CARTESIAN_POINT ( 'NONE',  ( 4.082764389539480732, -0.1829629792115642917, -1.861669828791753467 ) ) ;
#187999=CARTESIAN_POINT ( 'NONE',  ( 3.229449743806306561, 0.05664919459314603917, 2.307159798345681523 ) ) ;
#188000=CARTESIAN_POINT ( 'NONE',  ( 3.754231824312683763, -1.858861104869345082, -0.09317703841194531489 ) ) ;
#188003=CARTESIAN_POINT ( 'NONE',  ( 0.8914058518391498875, 1.856551077915175707, -0.9943519572734434986 ) ) ;
#188007=CARTESIAN_POINT ( 'NONE',  ( 6.925078400183550364, -0.007619068086212391067, 2.144148427808051594 ) ) ;
#188009=CARTESIAN_POINT ( 'NONE',  ( 0.5803392809272100994, 0.9991348162329892757, 1.755301537792392175 ) ) ;
#188014=CARTESIAN_POINT ( 'NONE',  ( 0.8257154465432202661, -2.052837714267462754, 0.6772920067378007669 ) ) ;
#188017=CARTESIAN_POINT ( 'NONE',  ( 6.925078400183590333, 2.970608243536181359, 2.408862486266015512 ) ) ;
#188020=CARTESIAN_POINT ( 'NONE',  ( 5.559779856078610472, 1.205038519190555268, 1.616695979245158066 ) ) ;
#188022=CARTESIAN_POINT ( 'NONE',  ( 0.3983070667218471805, -0.7439898890007863308, -2.061537379893277677 ) ) ;
#188024=CARTESIAN_POINT ( 'NONE',  ( 0.9016947886714383742, 1.851236229948808543, 1.300475659685183416 ) ) ;
#188028=CARTESIAN_POINT ( 'NONE',  ( 1.352997864604365885, 0.1391545085356447886, -1.910588907247000368 ) ) ;
#188032=CARTESIAN_POINT ( 'NONE',  ( 2.701417116451056533, -0.5414251306648624196, 1.637772108618321454 ) ) ;
#188034=CARTESIAN_POINT ( 'NONE',  ( 2.459888865612788855, 0.7521488021439284299, 1.602074255657309099 ) ) ;
#188036=CARTESIAN_POINT ( 'NONE',  ( 5.719807747550186505, -2.154180246964752410, 0.4782370604126117142 ) ) ;
#188038=CARTESIAN_POINT ( 'NONE',  ( 4.095966777872499520, 1.322572826423114911, 1.526597406435834081 ) ) ;
#188040=CARTESIAN_POINT ( 'NONE',  ( 4.319064098534145302, 1.638436671179326787, -1.346072318137331969 ) ) ;
#188041=CARTESIAN_POINT ( 'NONE',  ( 4.112907772398490813, 0.1017678201147946826, 2.013986186455194449 ) ) ;
#188045=CARTESIAN_POINT ( 'NONE',  ( 1.498681428038322272, 1.531199225506232553, -1.074333469806128427 ) ) ;
#188048=CARTESIAN_POINT ( 'NONE',  ( 6.006502151196043471, -1.803439199047681907, -0.1703578026433834602 ) ) ;
#188055=ADVANCED_FACE ( 'NONE', ( #122406 ), #146607, .F. ) ;
#188059=CARTESIAN_POINT ( 'NONE',  ( 4.236665939827915395, 1.302216991916404387, -1.673619383358643908 ) ) ;
#188062=CARTESIAN_POINT ( 'NONE',  ( 5.747334165637288272, -1.552519754122901663, -1.214743736649764649 ) ) ;
#188064=CARTESIAN_POINT ( 'NONE',  ( 0.4221356392010866543, -2.003110517487953324, 0.2016333174496009462 ) ) ;
#188066=CARTESIAN_POINT ( 'NONE',  ( 0.5095558700928676243, -2.008984845895735116, 0.6684745883070477568 ) ) ;
#188069=CARTESIAN_POINT ( 'NONE',  ( 1.732962091629593804, -1.965256999408044436, -0.6514315320021792921 ) ) ;
#188073=CARTESIAN_POINT ( 'NONE',  ( 4.224618542793646014, 0.1023655851960032920, 2.088258538514795593 ) ) ;
#188076=CARTESIAN_POINT ( 'NONE',  ( 3.082817581614716307, -0.1327354176642106531, -1.820802398864965088 ) ) ;
#188077=CARTESIAN_POINT ( 'NONE',  ( 1.435880962511564718, -1.006192904286895340, -1.506089461148002018 ) ) ;
#188081=CARTESIAN_POINT ( 'NONE',  ( 4.067547972739316897, 0.2730280005818259137, -2.189760481282684967 ) ) ;
#188084=CARTESIAN_POINT ( 'NONE',  ( 2.314975094136799694, 1.534822137071165660, -1.140449143091977646 ) ) ;
#188086=CARTESIAN_POINT ( 'NONE',  ( 5.969205681473694902, 1.824102622056431811, 0.9793482939001868504 ) ) ;
#188088=CARTESIAN_POINT ( 'NONE',  ( 6.128506746050899068, 0.2130254606748181456, 2.181202035047181020 ) ) ;
#188095=CARTESIAN_POINT ( 'NONE',  ( -0.2409995289980003397, 0.7158067089181943121, -2.082568332340509087 ) ) ;
#188100=CARTESIAN_POINT ( 'NONE',  ( 5.418829850390409320, -1.503349927839289002, 1.423607673449282851 ) ) ;
#188101=CARTESIAN_POINT ( 'NONE',  ( 4.160710321027959679, -1.426769435979913236, 1.294678423299196579 ) ) ;
#188102=CARTESIAN_POINT ( 'NONE',  ( 1.054314798682391530, -1.277026470193865171, 1.560515422851154854 ) ) ;
#188107=CARTESIAN_POINT ( 'NONE',  ( 1.095947417326826212, -2.191629467406099430, 0.003159298377679311057 ) ) ;
#188108=CARTESIAN_POINT ( 'NONE',  ( 5.707590141996651489, -0.4392596013848491521, 1.771934311310577659 ) ) ;
#188116=CARTESIAN_POINT ( 'NONE',  ( 2.577489280727011778, -0.9446877197298314544, 1.580272903027237774 ) ) ;
#188117=CARTESIAN_POINT ( 'NONE',  ( 6.222908185483853494, 1.488938611106488841, -1.355157726057078404 ) ) ;
#188118=CARTESIAN_POINT ( 'NONE',  ( 2.232162068744643069, -2.100961912546659871, -0.9323289839222002051 ) ) ;
#188120=CARTESIAN_POINT ( 'NONE',  ( 6.807479307002794577, -1.573682814073861902, -1.171087784426767753 ) ) ;
#188123=CARTESIAN_POINT ( 'NONE',  ( 3.656429697474584017, 1.903630103707624865, 0.1825790434749063051 ) ) ;
#188125=CARTESIAN_POINT ( 'NONE',  ( 0.2036857628631080219, -1.599406074100502506, -1.314310892166506095 ) ) ;
#188127=CARTESIAN_POINT ( 'NONE',  ( 2.155913254374627552, 0.8966022695893551830, 1.888892756932699646 ) ) ;
#188128=CARTESIAN_POINT ( 'NONE',  ( 0.9537216069140028729, 1.868711056098860235, -0.08788249432020722729 ) ) ;
#188129=CARTESIAN_POINT ( 'NONE',  ( 2.003279617838377824, 1.993765885540278004, 0.2985825316763612847 ) ) ;
#188133=CARTESIAN_POINT ( 'NONE',  ( 3.649730646487856056, 0.6304092353721781894, 1.622436561192377891 ) ) ;
#188137=CARTESIAN_POINT ( 'NONE',  ( 2.613528241349000858, -1.706151288242565567, 0.2525731233022251443 ) ) ;
#188138=CARTESIAN_POINT ( 'NONE',  ( 3.070069520051089906, -1.303570237086741024, 1.761582097007891923 ) ) ;
#188139=CARTESIAN_POINT ( 'NONE',  ( 5.321004863918796346, 2.037934703285459115, 0.8473243778325880715 ) ) ;
#188141=CARTESIAN_POINT ( 'NONE',  ( 3.186559800492471783, 1.209906992153013894, -1.802498320862821579 ) ) ;
#188142=CARTESIAN_POINT ( 'NONE',  ( 2.297230901563730665, 1.410920830412419003, 1.158640757216542028 ) ) ;
#188143=CARTESIAN_POINT ( 'NONE',  ( 0.3737810522974581717, -1.925036204310347943, 0.3769080146646397456 ) ) ;
#188145=CARTESIAN_POINT ( 'NONE',  ( 4.100857973768299303, 1.937344669444723166, 0.8546590867991187279 ) ) ;
#188148=CARTESIAN_POINT ( 'NONE',  ( 5.038769576086907342, -1.967128976631225434, 1.176836258767649745 ) ) ;
#188150=CARTESIAN_POINT ( 'NONE',  ( 0.07755575628183573877, -0.002876890934064984216, -2.188974970840869005 ) ) ;
#188152=CARTESIAN_POINT ( 'NONE',  ( 0.2410938523699951708, 2.030451451530786766, 0.6113826261911479154 ) ) ;
#188157=CARTESIAN_POINT ( 'NONE',  ( 5.678361341766085424, 1.528739221709461082, 1.314999087022615587 ) ) ;
#188159=CARTESIAN_POINT ( 'NONE',  ( 3.080982041725123910, 1.940567726598545040, 0.6991345639211270502 ) ) ;
#188161=CARTESIAN_POINT ( 'NONE',  ( -0.2409995289980003397, 2.873648158547074338, -2.488896373646624749 ) ) ;
#188165=CARTESIAN_POINT ( 'NONE',  ( 6.281208295753298643, 1.508423295503196648, 1.589913042345507455 ) ) ;
#188166=CARTESIAN_POINT ( 'NONE',  ( 3.270157880292836605, 1.821742160604752137, -0.8647241845514613834 ) ) ;
#188167=CARTESIAN_POINT ( 'NONE',  ( 3.737712173649463399, 1.832726675769575486, 0.1767833568970395008 ) ) ;
#188169=CARTESIAN_POINT ( 'NONE',  ( 2.250000000000001776, 1.285947368876626068E-13, 2.052068128417949389 ) ) ;
#188170=CARTESIAN_POINT ( 'NONE',  ( 0.5160737793865723955, 1.194803229551535173, -1.244154219207161960 ) ) ;
#188172=CARTESIAN_POINT ( 'NONE',  ( 1.196342457394595993, 2.030139636617489085, 1.078195451733245047 ) ) ;
#188174=CARTESIAN_POINT ( 'NONE',  ( 0.3689490567273964738, -1.476270946665221517, 1.714425361395756964 ) ) ;
#188175=CARTESIAN_POINT ( 'NONE',  ( 1.787856894401329333, 1.453325235529376869, 1.524497383921459726 ) ) ;
#188183=CARTESIAN_POINT ( 'NONE',  ( 3.797323596237450971, -0.2205154750010793197, -2.210469098741683514 ) ) ;
#188184=CARTESIAN_POINT ( 'NONE',  ( 2.220887445055406584, 0.001640320231081903845, 2.191629467496846839 ) ) ;
#188186=CARTESIAN_POINT ( 'NONE',  ( 0.6278963055918493907, -2.094311335337955882, 0.6960538111202837497 ) ) ;
#188188=CARTESIAN_POINT ( 'NONE',  ( 5.248475795274027078, -1.946838731704622072, -0.2419367024937419397 ) ) ;
#188193=CARTESIAN_POINT ( 'NONE',  ( 4.799148092389167175, -0.2621723519393297508, -2.104289960152181393 ) ) ;
#188196=CARTESIAN_POINT ( 'NONE',  ( 5.893488898593548520, 1.633865717575968324, 1.415524914074948404 ) ) ;
#188198=CARTESIAN_POINT ( 'NONE',  ( 5.231922985772964552, 1.814955821992572993, 0.3091130605668013231 ) ) ;
#188201=CARTESIAN_POINT ( 'NONE',  ( 6.580030513128129144, -1.708294420148011472, -0.3314369902002142765 ) ) ;
#188202=CARTESIAN_POINT ( 'NONE',  ( 6.827182134110196365, 4.700652535171166768, 2.373648650996477372 ) ) ;
#188205=CARTESIAN_POINT ( 'NONE',  ( 3.977527890101069996, 2.036293384626610248, -0.7259696361804208742 ) ) ;
#188208=CARTESIAN_POINT ( 'NONE',  ( 2.975616057669258741, 2.053088362031017855, -0.6768339029224537118 ) ) ;
#188209=CARTESIAN_POINT ( 'NONE',  ( 5.413337677306027551, -0.2920802625693446619, 1.949502277767001690 ) ) ;
#188210=CARTESIAN_POINT ( 'NONE',  ( 4.042145929572971141, 1.632826047920731050, -0.5835893337435077433 ) ) ;
#188211=CARTESIAN_POINT ( 'NONE',  ( 1.294752383181968503, 1.788903229852260246, -1.265732775075766092 ) ) ;
#188212=CARTESIAN_POINT ( 'NONE',  ( 1.431196836673795936, 2.224535207900823153, 0.6132342015414853353 ) ) ;
#188213=CARTESIAN_POINT ( 'NONE',  ( 3.884101140911602634, -1.018864849042991461, 1.791236251998897133 ) ) ;
#188214=CARTESIAN_POINT ( 'NONE',  ( 5.812047917624927784, 1.301047364602755829, -1.442011890679588904 ) ) ;
#188221=CARTESIAN_POINT ( 'NONE',  ( 3.030518406005321186, 1.227118389542980026, -1.833929004854919054 ) ) ;
#188224=CARTESIAN_POINT ( 'NONE',  ( 0.2329586101569866563, 0.008238550247445517935, -1.845944905557160398 ) ) ;
#188225=CARTESIAN_POINT ( 'NONE',  ( -0.1291982275798392032, 1.351143144720265532, -2.329141727150272789 ) ) ;
#188230=CARTESIAN_POINT ( 'NONE',  ( 6.527308116070499544, -1.206667617865687214, -1.390688675169844624 ) ) ;
#188232=CARTESIAN_POINT ( 'NONE',  ( 1.850533416564412725, 0.6455992098736047513, 1.957236905219070566 ) ) ;
#188238=CARTESIAN_POINT ( 'NONE',  ( 1.375931059888847896, 1.226954981729235561, 1.655701539656707411 ) ) ;
#188240=CARTESIAN_POINT ( 'NONE',  ( 5.302248432823610358, 1.390444127666954355, -1.207098008268410183 ) ) ;
#188243=CARTESIAN_POINT ( 'NONE',  ( -0.2409995289980245703, 0.2355275985303668385, -2.034371242098035548 ) ) ;
#188244=CARTESIAN_POINT ( 'NONE',  ( 4.670673364294657404, -1.443042178620690841, 1.669811033208345341 ) ) ;
#188245=CARTESIAN_POINT ( 'NONE',  ( 0.1811626231076196580, -0.1537715369321658587, -2.127283700313627346 ) ) ;
#188247=CARTESIAN_POINT ( 'NONE',  ( 0.4219365929402639215, -1.902980170924161385, 0.1897552588234762416 ) ) ;
#188248=CARTESIAN_POINT ( 'NONE',  ( 1.007046422456716384, -0.04465021774549028655, 2.016188868504041665 ) ) ;
#188250=CARTESIAN_POINT ( 'NONE',  ( 1.406082690172899108, 0.4493768194517386849, 2.253890741632145200 ) ) ;
#188251=CARTESIAN_POINT ( 'NONE',  ( 6.825078400183573812, 0.002648415797040087893, 1.855566311045192540 ) ) ;
#188255=CARTESIAN_POINT ( 'NONE',  ( 1.358040219746913024, 0.7549631825471068147, 1.711723683848711985 ) ) ;
#188256=CARTESIAN_POINT ( 'NONE',  ( 2.413296319342159713, -1.879803466158457059, 0.7303082167480907660 ) ) ;
#188260=CARTESIAN_POINT ( 'NONE',  ( 5.461587592249073531, 0.4120570304669196604, -2.065184316587692415 ) ) ;
#188266=CARTESIAN_POINT ( 'NONE',  ( 4.605726162909654420, 1.499404818428259345, 1.353488595782571524 ) ) ;
#188268=CARTESIAN_POINT ( 'NONE',  ( 6.320769014966518107, -1.461346085113580440, 1.455966316998691168 ) ) ;
#188270=CARTESIAN_POINT ( 'NONE',  ( 4.798204600472657511, -2.160985683756014630, -0.05834674948757002932 ) ) ;
#188276=CARTESIAN_POINT ( 'NONE',  ( 1.662788154211870983, -0.7805772603099859763, -2.026187018951190133 ) ) ;
#188279=CARTESIAN_POINT ( 'NONE',  ( 1.751249726499287673, 1.836263021919124050, -0.1365115386888632321 ) ) ;
#188281=CARTESIAN_POINT ( 'NONE',  ( 3.755584314896889264, 2.174856280799509545, -0.2696606696684644700 ) ) ;
#188283=CARTESIAN_POINT ( 'NONE',  ( 3.573342120354418672, 0.05797898436993471211, -2.261936065680466346 ) ) ;
#188289=CARTESIAN_POINT ( 'NONE',  ( 5.395664931544272847, -0.6364340197690997458, 1.651504472441939875 ) ) ;
#188290=CARTESIAN_POINT ( 'NONE',  ( 3.422524054001755633, -0.8179560535927836717, -1.839607883820688405 ) ) ;
#188292=CARTESIAN_POINT ( 'NONE',  ( 1.694499644457616583, -2.095784359944006248, -0.2068371402374687973 ) ) ;
#188295=CARTESIAN_POINT ( 'NONE',  ( 0.9769314595147912117, 1.818477718279483568, 0.7569839642056105378 ) ) ;
#188298=CARTESIAN_POINT ( 'NONE',  ( 5.414259967653319627, -1.811767230315189048, 0.008324397547932599339 ) ) ;
#188301=CARTESIAN_POINT ( 'NONE',  ( 5.366025703835962446, 0.9229158262306772498, 1.627043297953718382 ) ) ;
#188303=CARTESIAN_POINT ( 'NONE',  ( 4.381733404717279790, -1.982624999272283084, 0.5960583376443122638 ) ) ;
#188315=CARTESIAN_POINT ( 'NONE',  ( 4.703538834289092030, -1.515240342570793430, -1.246145567450624991 ) ) ;
#188317=CARTESIAN_POINT ( 'NONE',  ( 1.651720012567552853, -0.2930234437087535504, -1.994564656426714988 ) ) ;
#188319=CARTESIAN_POINT ( 'NONE',  ( 0.4861908890553789386, -2.175720422541329580, -0.2624175912114696252 ) ) ;
#188321=CARTESIAN_POINT ( 'NONE',  ( 1.756895065592100291, -1.601674646019658255, -0.9660157589584242865 ) ) ;
#188323=CARTESIAN_POINT ( 'NONE',  ( 3.726818050638240898, 1.420666359685630598, -1.426677609031762994 ) ) ;
#188326=CARTESIAN_POINT ( 'NONE',  ( 3.532911237611217281, -1.729578172696862426, 1.220892919093808482 ) ) ;
#188329=CARTESIAN_POINT ( 'NONE',  ( 4.598136200040512378, 0.8882050449813773119, -1.870312673664726644 ) ) ;
#188331=CARTESIAN_POINT ( 'NONE',  ( 1.277023361749257457, 1.930420895987930097, -0.8034254789068133729 ) ) ;
#188332=CARTESIAN_POINT ( 'NONE',  ( 6.720655732516641834, 7.051887106169240305, 2.771889904330120391 ) ) ;
#188333=CARTESIAN_POINT ( 'NONE',  ( 6.071303273277399271, 0.1315155018670917386, -1.820917815106848359 ) ) ;
#188341=CARTESIAN_POINT ( 'NONE',  ( 5.848291733227988232, 0.9385554955868085081, -1.666026892748099009 ) ) ;
#188348=CARTESIAN_POINT ( 'NONE',  ( 6.327749939939702806, 0.7691082200134463642, -1.864175038933603146 ) ) ;
#188351=CARTESIAN_POINT ( 'NONE',  ( 0.1394461523057137220, 5.725876337386284654, -2.313825101289856967 ) ) ;
#188355=CARTESIAN_POINT ( 'NONE',  ( 3.379706166375577414, -1.899257087701329949, 0.5209217831910922802 ) ) ;
#188356=CARTESIAN_POINT ( 'NONE',  ( 4.025017672583341977, -1.753021876717888006, 0.9963191169995513352 ) ) ;
#188359=CARTESIAN_POINT ( 'NONE',  ( 5.156268285673103691, -1.588865937562380148, 1.509524371192130676 ) ) ;
#188361=CARTESIAN_POINT ( 'NONE',  ( 2.678635733147361808, -1.842946530311468045, -0.5607992601908852182 ) ) ;
#188363=CARTESIAN_POINT ( 'NONE',  ( -0.1298852118744101003, 4.098067735550426249, -2.281510303361510061 ) ) ;
#188364=CARTESIAN_POINT ( 'NONE',  ( 0.1331565106231363538, 0.2470099659030860484, -1.980838409567912572 ) ) ;
#188371=CARTESIAN_POINT ( 'NONE',  ( 6.374545129912787544, -0.09763137639631430664, -1.838803627010993313 ) ) ;
#188372=CARTESIAN_POINT ( 'NONE',  ( 3.035794076406534536, -1.939542403429166395, 0.5389024948808174287 ) ) ;
#188373=CARTESIAN_POINT ( 'NONE',  ( 5.817770776407988009, -1.817369610395104695, 1.406990027747441419 ) ) ;
#188375=CARTESIAN_POINT ( 'NONE',  ( 3.063170293922971243, 1.569483505267080359, 0.9996245905467721071 ) ) ;
#188381=CARTESIAN_POINT ( 'NONE',  ( 6.040588761503070003, -1.765850204961866954, 1.119074740713212002 ) ) ;
#188386=CARTESIAN_POINT ( 'NONE',  ( 0.3635304476994546952, 1.806310985241452949, -0.2645042207462811046 ) ) ;
#188389=CARTESIAN_POINT ( 'NONE',  ( 2.109626794357027268, 0.001117226762978317921, 1.734343004219033757 ) ) ;
#188394=CARTESIAN_POINT ( 'NONE',  ( 6.860228214211484321, -2.170771502548960452, 0.04436455139915015944 ) ) ;
#188395=CARTESIAN_POINT ( 'NONE',  ( 5.918537399722813674, 1.222626809077583587, -1.356019982345892050 ) ) ;
#188396=CARTESIAN_POINT ( 'NONE',  ( 3.098438489093110704, 1.946378968836332213, 0.2448508753878294586 ) ) ;
#188400=CARTESIAN_POINT ( 'NONE',  ( 3.264422710156249963, 2.120667954687505574, -0.001943060928578931989 ) ) ;
#188404=CARTESIAN_POINT ( 'NONE',  ( 1.815371668717490339, -1.773540675419151169, -1.067758146248848128 ) ) ;
#188405=CARTESIAN_POINT ( 'NONE',  ( 6.827182134110225675, 7.053278108740402175, 2.409100297097351184 ) ) ;
#188408=CARTESIAN_POINT ( 'NONE',  ( 4.178555957833706813, 1.047420865545487523, 1.958865958838784005 ) ) ;
#188410=CARTESIAN_POINT ( 'NONE',  ( 1.688534781859708067, 1.914194972067848832, 1.272504748915660899 ) ) ;
#188412=CARTESIAN_POINT ( 'NONE',  ( 6.719587945281444874, 0.3584770237896938716, -2.031047634367310284 ) ) ;
#188416=CARTESIAN_POINT ( 'NONE',  ( 6.198766299729112639, 1.534709720371667308, 1.016988835930050739 ) ) ;
#188419=CARTESIAN_POINT ( 'NONE',  ( 3.304848191199673213, -0.3775801424153284458, -1.874573493127674961 ) ) ;
#188420=CARTESIAN_POINT ( 'NONE',  ( -0.1104750535120268828, 7.629137130509074716, -2.703481013110929254 ) ) ;
#188421=CARTESIAN_POINT ( 'NONE',  ( 3.539825753290166688, 0.7759033148657649148, -1.540472896381483769 ) ) ;
#188422=CARTESIAN_POINT ( 'NONE',  ( 1.938685741270998797, -1.555697844595272716, 1.282991390469834458 ) ) ;
#188423=CARTESIAN_POINT ( 'NONE',  ( 4.377739380128500279, -0.5030580445687399260, -2.242836179151234344 ) ) ;
#188425=CARTESIAN_POINT ( 'NONE',  ( 3.286655449121218542, -2.228332854187901280, -0.3904065581350114611 ) ) ;
#188426=CARTESIAN_POINT ( 'NONE',  ( 6.481095854277318935, -0.1012916397761880333, -2.103764601514758414 ) ) ;
#188429=CARTESIAN_POINT ( 'NONE',  ( 4.815556489234497306, -1.735627832820924477, 0.3447801454335273630 ) ) ;
#188431=CARTESIAN_POINT ( 'NONE',  ( 0.6215105264332577706, -2.174887359234744633, 0.7243307227927602288 ) ) ;
#188432=CARTESIAN_POINT ( 'NONE',  ( 5.929618730664214077, 0.9035273275350870215, -1.604119651413847603 ) ) ;
#188435=CARTESIAN_POINT ( 'NONE',  ( 5.595707529797693702, -2.191629465999441084, -0.002916574791289594515 ) ) ;
#188438=CARTESIAN_POINT ( 'NONE',  ( 5.670397268163976712, -0.9275489576153757021, -1.851018422006404096 ) ) ;
#188439=CARTESIAN_POINT ( 'NONE',  ( -0.1531117392989979065, -1.803405091603600185, -0.9023890051431044945 ) ) ;
#188441=CARTESIAN_POINT ( 'NONE',  ( 4.547439623722833169, -1.490282656903282099, -1.220848939070565686 ) ) ;
#188445=CARTESIAN_POINT ( 'NONE',  ( 1.266231527720959926, 0.6383494478915030523, -2.127751457625071563 ) ) ;
#188448=CARTESIAN_POINT ( 'NONE',  ( 6.720655732516622294, 7.629137130509072051, 2.773739711112707340 ) ) ;
#188455=CARTESIAN_POINT ( 'NONE',  ( 1.416376618315864144, 0.7919773292732554815, 1.795081228748253377 ) ) ;
#188459=CARTESIAN_POINT ( 'NONE',  ( 6.250445965835445428, -1.952298026214387194, -0.1936728439068043650 ) ) ;
#188462=CARTESIAN_POINT ( 'NONE',  ( 0.5501786683353731000, 0.7064523498505774768, -2.149447411369388217 ) ) ;
#188466=CARTESIAN_POINT ( 'NONE',  ( 1.950266909631480861, 0.5821006739541793040, 1.777759251391328732 ) ) ;
#188467=CARTESIAN_POINT ( 'NONE',  ( 7.214646527853999024E-05, -1.701284277595259464, 0.3348680416483724720 ) ) ;
#188469=CARTESIAN_POINT ( 'NONE',  ( 4.616832073239669043, -0.1072513232249286408, 2.189039617437993357 ) ) ;
#188470=CARTESIAN_POINT ( 'NONE',  ( 4.050101169753547836, 0.7808133845815302676, -2.171591319759837546 ) ) ;
#188472=CARTESIAN_POINT ( 'NONE',  ( 6.555941810938458403, 2.055592219362284201, -0.1468124517445909549 ) ) ;
#188473=CARTESIAN_POINT ( 'NONE',  ( 2.449080105735270685, 0.5175099976203160201, -1.871664248846743872 ) ) ;
#188478=CARTESIAN_POINT ( 'NONE',  ( 5.185831674374465905, 2.043064739972153543, -0.5678235988075125418 ) ) ;
#188480=CARTESIAN_POINT ( 'NONE',  ( 3.533827422916273164, -1.646839391163470223, 1.163268690995450383 ) ) ;
#188484=CARTESIAN_POINT ( 'NONE',  ( 1.119449510670032177, -1.781678707675336870, 0.3977030049751931196 ) ) ;
#188488=EDGE_LOOP ( 'NONE', ( #189956, #98734 ) ) ;
#188489=CARTESIAN_POINT ( 'NONE',  ( 5.858293207932864455, 0.8329246649354884457, 1.885258002110825615 ) ) ;
#188493=CARTESIAN_POINT ( 'NONE',  ( 5.145178147197468022, 0.1505999202349363186, 2.014131245181075336 ) ) ;
#188494=CARTESIAN_POINT ( 'NONE',  ( 5.865950696152278709, 0.6470421894613547220, -2.124994868043238672 ) ) ;
#188498=CARTESIAN_POINT ( 'NONE',  ( 4.575106920794588916, 0.002012451770977418796, -2.061077815012714254 ) ) ;
#188499=CARTESIAN_POINT ( 'NONE',  ( 4.201796189063250253, 1.844709454618495670, 0.8146275914719460776 ) ) ;
#188506=CARTESIAN_POINT ( 'NONE',  ( 4.552111140598270822, 1.802141083034415781, -0.9039717811075360654 ) ) ;
#188507=CARTESIAN_POINT ( 'NONE',  ( 3.450948914068392881, 0.4461466885457600062, -1.786139022923169506 ) ) ;
#188510=CARTESIAN_POINT ( 'NONE',  ( 1.682680061667326088, -1.231660274741898320, 1.951365989292063174 ) ) ;
#188512=CARTESIAN_POINT ( 'NONE',  ( 4.165412764819938829, 0.2691229397190370576, -2.144731622849817221 ) ) ;
#188515=CARTESIAN_POINT ( 'NONE',  ( 3.216491754421717530, -1.877423419238280822, -1.325616196499669108 ) ) ;
#188517=CARTESIAN_POINT ( 'NONE',  ( 2.026040307571222332, 1.079255042350239391, -1.527726335390042767 ) ) ;
#188518=CARTESIAN_POINT ( 'NONE',  ( 0.1749903794560749015, 0.004523422195312763391, -1.955468523092759536 ) ) ;
#188523=CARTESIAN_POINT ( 'NONE',  ( 1.524350002934187653, -1.228176919886795782, -1.833354347511229498 ) ) ;
#188528=CARTESIAN_POINT ( 'NONE',  ( 5.805538644497215017, -0.4794378417142564075, 1.912156289036368806 ) ) ;
#188530=CARTESIAN_POINT ( 'NONE',  ( 5.795647523915807398, 1.743732541305573758, 1.511695197786174782 ) ) ;
#188531=CARTESIAN_POINT ( 'NONE',  ( 0.6605093422152423788, -0.6574743052488278838, -1.848563176889833626 ) ) ;
#188532=CARTESIAN_POINT ( 'NONE',  ( 3.450102088163331082, -0.8403066601648312428, 1.883826651212586745 ) ) ;
#188539=CARTESIAN_POINT ( 'NONE',  ( 5.846172790272405884, -0.9815748167120906809, 1.936718618010783377 ) ) ;
#188541=CARTESIAN_POINT ( 'NONE',  ( 5.003375819710620398, -1.831856422778654681, 0.1858995714831001289 ) ) ;
#188543=CARTESIAN_POINT ( 'NONE',  ( 6.620655732516647518, 7.053381450551401421, 2.424417106520880161 ) ) ;
#188545=CARTESIAN_POINT ( 'NONE',  ( 0.3505827959322353471, -1.506356567903786470, 1.108807183729618062 ) ) ;
#188546=CARTESIAN_POINT ( 'NONE',  ( 0.7380304622728722785, -1.600708836854593198, -1.599060815671312641 ) ) ;
#188551=CARTESIAN_POINT ( 'NONE',  ( 1.656752475421595872, -1.515787608549432175, -0.9133899773908128461 ) ) ;
#188552=CARTESIAN_POINT ( 'NONE',  ( 6.621754286443582771, -0.4424289334611238300, 1.971349943050800801 ) ) ;
#188555=CARTESIAN_POINT ( 'NONE',  ( 3.620622283765279725, 0.2843237153829519248, 1.894267977526209012 ) ) ;
#188557=CARTESIAN_POINT ( 'NONE',  ( 3.912524032909367566, 0.7067130192578415793, 1.838586846604377323 ) ) ;
#188558=CARTESIAN_POINT ( 'NONE',  ( -0.01710467543277957581, -1.380256469788909035, 1.610041658517608054 ) ) ;
#188560=CARTESIAN_POINT ( 'NONE',  ( 2.606148294764852213, -0.7140300644919925777, -1.729217693616967644 ) ) ;
#188561=CARTESIAN_POINT ( 'NONE',  ( 6.217413168894407427, -0.2034119912461933299, 1.712789424573582409 ) ) ;
#188563=CARTESIAN_POINT ( 'NONE',  ( 2.157103830005083100, -1.704838622333640030, 1.401371054633032909 ) ) ;
#188566=CARTESIAN_POINT ( 'NONE',  ( 6.338335788673861160, -1.050647824335379399, 1.656640365463659670 ) ) ;
#188574=CARTESIAN_POINT ( 'NONE',  ( 2.594261239525695206, 0.9781076984213372683, -1.824767828009652426 ) ) ;
#188578=CARTESIAN_POINT ( 'NONE',  ( 0.3463606850301796380, 1.036194208456611809, -1.733443346147050868 ) ) ;
#188581=CARTESIAN_POINT ( 'NONE',  ( 0.07459516483346650961, 6.948550711820903558, -2.350542341214032493 ) ) ;
#188583=CARTESIAN_POINT ( 'NONE',  ( 5.817732461567613811, -1.591073081590413052, 1.238133459405404757 ) ) ;
#188584=CARTESIAN_POINT ( 'NONE',  ( 5.823430154129352054, -1.392497453891910375, -1.315930268783272794 ) ) ;
#188586=CARTESIAN_POINT ( 'NONE',  ( 4.036819321710017228, -1.906298169312226953, 1.081085072550565407 ) ) ;
#188587=( BOUNDED_CURVE ( )  B_SPLINE_CURVE ( 3, ( #43079, #206603, #108117, #208728 ),
 .UNSPECIFIED., .F., .T. ) 
 B_SPLINE_CURVE_WITH_KNOTS ( ( 4, 4 ),
 ( 0.000000000000000000, 0.5000000000000006661 ),
 .UNSPECIFIED. ) 
 CURVE ( )  GEOMETRIC_REPRESENTATION_ITEM ( )  RATIONAL_B_SPLINE_CURVE ( ( 1.000000000000000000, 0.3333333333333324822, 0.3333333333333333703, 1.000000000000000888 ) ) 
 REPRESENTATION_ITEM ( '' )  );
#188589=CARTESIAN_POINT ( 'NONE',  ( 2.566550162062298579, 0.6480892470011965223, 1.799338185917313870 ) ) ;
#188593=CARTESIAN_POINT ( 'NONE',  ( 0.1402502066264778580, 0.7743353953559418690, 1.862009890338502505 ) ) ;
#188596=CARTESIAN_POINT ( 'NONE',  ( 5.864808805604324604, 0.1626094438406736342, -2.185560445749204828 ) ) ;
#188598=CARTESIAN_POINT ( 'NONE',  ( 3.188212539307228699, -1.698978696193183202, -0.2961410920078124676 ) ) ;
#188600=CARTESIAN_POINT ( 'NONE',  ( 6.293239850429793947, -0.1054838202379469042, -2.118119863012501991 ) ) ;
#188603=CARTESIAN_POINT ( 'NONE',  ( 0.5023040531197673353, 1.956348610274569744, 0.1481081594910879096 ) ) ;
#188609=CARTESIAN_POINT ( 'NONE',  ( 2.894932696777189118, -0.1353093493836102779, -1.806485987321084341 ) ) ;
#188614=CARTESIAN_POINT ( 'NONE',  ( 3.422321195131371674, -0.7368491698513750521, -1.655029553552778809 ) ) ;
#188616=( NAMED_UNIT ( * ) SI_UNIT ( $, .STERADIAN. ) SOLID_ANGLE_UNIT ( ) );
#188618=CARTESIAN_POINT ( 'NONE',  ( 5.178104514100493994, -0.9952990805809349695, -1.572330789729664779 ) ) ;
#188620=CARTESIAN_POINT ( 'NONE',  ( 2.741684679331716890, 1.906140283219289966, -0.1903247725174895544 ) ) ;
#188621=CARTESIAN_POINT ( 'NONE',  ( 1.342497868159111984, 0.3520595052693386018, 1.791136884925909056 ) ) ;
#188622=DIRECTION ( 'NONE',  ( -1.000000000000000000, 1.016547956922408957E-15, 1.479114432388267300E-31 ) ) ;
#188632=CARTESIAN_POINT ( 'NONE',  ( 1.359446872921949101, 2.059443214669457234, -0.3588360909314599612 ) ) ;
#188633=CARTESIAN_POINT ( 'NONE',  ( 0.2701547006425785713, -1.196777392914155635, 1.378664180083796875 ) ) ;
#188636=CARTESIAN_POINT ( 'NONE',  ( 1.922601709848625440, 1.702220721529534853, 0.6601445126475160574 ) ) ;
#188637=CARTESIAN_POINT ( 'NONE',  ( 3.387540773601561916, 1.995160029947869340, -0.9435142334218297178 ) ) ;
#188639=CARTESIAN_POINT ( 'NONE',  ( 1.002048865836258518, -0.8573748960705518396, 1.709468765625526521 ) ) ;
#188640=CARTESIAN_POINT ( 'NONE',  ( 1.170285302187854981, -0.8824026946198880728, -1.760880109839728647 ) ) ;
#188641=CARTESIAN_POINT ( 'NONE',  ( 3.544416897000971289, -1.586007893901800969, 1.120530928797113246 ) ) ;
#188645=CARTESIAN_POINT ( 'NONE',  ( 6.860206125033806224, -1.860540838789390694, 0.04523802485481390190 ) ) ;
#188650=CARTESIAN_POINT ( 'NONE',  ( 2.700927432832851860, 1.852951201923001223, 1.169960570980829839 ) ) ;
#188654=CARTESIAN_POINT ( 'NONE',  ( 3.914527900857078357, 1.289819402409349669, -1.292354223553587644 ) ) ;
#188655=CARTESIAN_POINT ( 'NONE',  ( 5.999232488047272049, -0.2420365156972601739, 2.001857322483958423 ) ) ;
#188661=CARTESIAN_POINT ( 'NONE',  ( 4.311305935566238645, -0.3199438451688824125, 1.842931056080451935 ) ) ;
#188663=CARTESIAN_POINT ( 'NONE',  ( 2.508321089405711746, -0.7374124507862482858, -1.779973396525496909 ) ) ;
#188664=CARTESIAN_POINT ( 'NONE',  ( 6.508651776674191147, 0.6122461511635870490, 1.863871573545019755 ) ) ;
#188670=CARTESIAN_POINT ( 'NONE',  ( -0.1408020194050146334, -0.005144001661238749128, -2.100147592658160089 ) ) ;
#188673=CARTESIAN_POINT ( 'NONE',  ( 5.155165671438199482, 1.724248240607465732, -1.145533019084030268 ) ) ;
#188674=CARTESIAN_POINT ( 'NONE',  ( -0.09456490281532430042, -0.7861721075429689565, -1.663503389917226460 ) ) ;
#188676=CARTESIAN_POINT ( 'NONE',  ( 4.922631952865072158, -1.624392127635465144, -1.626674183726722678 ) ) ;
#188680=CARTESIAN_POINT ( 'NONE',  ( 0.7270408775228944798, 0.1741418271693234987, 2.285704298519490862 ) ) ;
#188683=CARTESIAN_POINT ( 'NONE',  ( 4.769442245286214188, 1.119358777157190010, 1.586704836592154333 ) ) ;
#188687=CARTESIAN_POINT ( 'NONE',  ( 6.539320575229249144, 0.007148032025052972194, 1.896977914940492393 ) ) ;
#188688=CARTESIAN_POINT ( 'NONE',  ( 1.101696929656799995, -1.725068445828933594, -0.003817819714259720019 ) ) ;
#188689=CARTESIAN_POINT ( 'NONE',  ( 5.946499988598237252, -1.422611626450220434, 1.429444749906971790 ) ) ;
#188693=CARTESIAN_POINT ( 'NONE',  ( 2.343796043118621775, 2.090200655756014658, 0.05028463699395351039 ) ) ;
#188694=CARTESIAN_POINT ( 'NONE',  ( 1.779799802231885275, -0.9501279348179264561, 1.492983415055911367 ) ) ;
#188697=CARTESIAN_POINT ( 'NONE',  ( 3.908379099077957886, 1.621946506101832775, -1.620046465671644675 ) ) ;
#188698=CARTESIAN_POINT ( 'NONE',  ( 2.378492463385312394, 1.591508763844831531, -0.7045900751257595518 ) ) ;
#188701=CARTESIAN_POINT ( 'NONE',  ( 2.354500945691032410, -0.7452406562851380256, 1.565668601905329638 ) ) ;
#188703=CARTESIAN_POINT ( 'NONE',  ( 1.363465259770980209, -0.4569337200135030197, 1.803945581614458282 ) ) ;
#188704=CARTESIAN_POINT ( 'NONE',  ( 1.944024895830529731, 1.496304202470769340, 1.573470141065239414 ) ) ;
#188706=CARTESIAN_POINT ( 'NONE',  ( 3.221888912838869690, 0.9023448338944944913, -1.803416113280359445 ) ) ;
#188707=CARTESIAN_POINT ( 'NONE',  ( 2.781250000000002665, 0.7852924748301273183, 1.895863743164028170 ) ) ;
#188709=CARTESIAN_POINT ( 'NONE',  ( 1.026247228566424363, 1.149774913616221417, -1.545494133055951069 ) ) ;
#188711=CARTESIAN_POINT ( 'NONE',  ( 4.271885190509593144, 0.4847678284230126922, -2.167736239397171083 ) ) ;
#188717=CARTESIAN_POINT ( 'NONE',  ( 0.4170203200158085211, -0.7540967040414385814, -2.089506846138278195 ) ) ;
#188718=CARTESIAN_POINT ( 'NONE',  ( 4.844172697165038066, -0.9265620464425131653, 1.729294158640543477 ) ) ;
#188721=CARTESIAN_POINT ( 'NONE',  ( 5.413438844936455219, -0.3396298981525199823, 2.236681904191807568 ) ) ;
#188723=CARTESIAN_POINT ( 'NONE',  ( 2.875492298462109630, -0.2048798925258775439, 2.052495523891383566 ) ) ;
#188728=CARTESIAN_POINT ( 'NONE',  ( 4.464026755505964950, 0.8799173153972823513, 1.650629236088823282 ) ) ;
#188729=CARTESIAN_POINT ( 'NONE',  ( 3.252318870217449920, 1.690988760736945373, -0.3835568649490900817 ) ) ;
#188730=CARTESIAN_POINT ( 'NONE',  ( 3.895860127252141591, -0.5505607855701463160, -1.651121638195630181 ) ) ;
#188731=CARTESIAN_POINT ( 'NONE',  ( 1.083963445724302588, -1.025016635393001252, 2.050507297876194901 ) ) ;
#188732=CARTESIAN_POINT ( 'NONE',  ( 1.413402608508182556, 1.946665536341249503, 1.039416302365432587 ) ) ;
#188733=CARTESIAN_POINT ( 'NONE',  ( 4.528904929885309905, -1.910896387970087096, 0.8487916243252179305 ) ) ;
#188734=CARTESIAN_POINT ( 'NONE',  ( 5.578056150152780113, -1.895089194937165100, -0.4233685073328739557 ) ) ;
#188737=CARTESIAN_POINT ( 'NONE',  ( 0.9146856577476671912, -1.281363086869342194, -1.556907195799726917 ) ) ;
#188738=CARTESIAN_POINT ( 'NONE',  ( 0.7035762090183244055, 1.867434778015097940, -1.004864118554361863 ) ) ;
#188743=CARTESIAN_POINT ( 'NONE',  ( 3.967279163243800255, 0.2216459979678051528, -1.812115712870238537 ) ) ;
#188749=CARTESIAN_POINT ( 'NONE',  ( 2.127218876063118103, 1.806125448131710387, 0.9042179360667053079 ) ) ;
#188750=CARTESIAN_POINT ( 'NONE',  ( 5.385833121705805304, 1.478444731487274399, 1.638484004604986000 ) ) ;
#188752=CARTESIAN_POINT ( 'NONE',  ( 2.711566728334329213, 0.5015729494155155566, -1.791976956261555953 ) ) ;
#188758=CARTESIAN_POINT ( 'NONE',  ( 5.092344371507952161, -1.812320225013038133, -0.2200062734805732223 ) ) ;
#188763=CARTESIAN_POINT ( 'NONE',  ( 0.1570416503036062006, -0.3615154868755916517, -1.700924732364687220 ) ) ;
#188764=CARTESIAN_POINT ( 'NONE',  ( 0.2337849711155593480, 0.2922425735506446465, 1.715447441342861534 ) ) ;
#188765=CARTESIAN_POINT ( 'NONE',  ( 5.936188932989287181, 1.142819166849334378, -2.004778302753240649 ) ) ;
#188767=CARTESIAN_POINT ( 'NONE',  ( 0.3333698182165916735, -1.885181130612986866, 0.8328085122516776240 ) ) ;
#188769=CARTESIAN_POINT ( 'NONE',  ( 5.712396407272276377, -1.806953704233695612, -1.420304717212710122 ) ) ;
#188772=CARTESIAN_POINT ( 'NONE',  ( 5.770339134078734666, -1.185559297855027561, 1.446973003893243348 ) ) ;
#188774=CARTESIAN_POINT ( 'NONE',  ( 3.216961742616857745, 1.504763323797538410, -1.180078671740567131 ) ) ;
#188777=CARTESIAN_POINT ( 'NONE',  ( 5.479209177496175087, -0.05098606815037013545, -2.206463706674952618 ) ) ;
#188778=CARTESIAN_POINT ( 'NONE',  ( 5.155504860159462410, 2.039786097693491396, -0.5674642188294597434 ) ) ;
#188781=CARTESIAN_POINT ( 'NONE',  ( -0.2108831679770961920, 2.882544375557041239, -2.385815782126240236 ) ) ;
#188785=CARTESIAN_POINT ( 'NONE',  ( 5.531924462405465981, -2.068776410037334479, 0.4646945096876684556 ) ) ;
#188787=CARTESIAN_POINT ( 'NONE',  ( 2.028779783278670035, 1.327905328797769569, -1.887045328260747112 ) ) ;
#188788=CARTESIAN_POINT ( 'NONE',  ( 3.226955236329264398, -1.811681696138227160, -0.7532884077038404236 ) ) ;
#188790=CARTESIAN_POINT ( 'NONE',  ( 6.543808478091840186, 1.418056970388498206, 1.498012503012560170 ) ) ;
#188794=CARTESIAN_POINT ( 'NONE',  ( 5.471888747823221877, -0.9023485654677811940, 1.803414228490702209 ) ) ;
#188797=CARTESIAN_POINT ( 'NONE',  ( -0.1408020194049780516, -0.005144001661201014555, -2.100147592658160089 ) ) ;
#188798=CARTESIAN_POINT ( 'NONE',  ( 1.956167536658510953, -0.7342896127641992399, 2.043222018709658805 ) ) ;
#188800=CARTESIAN_POINT ( 'NONE',  ( 0.9320672075895162223, -2.067649466203642206, 0.4702014512557165515 ) ) ;
#188806=CARTESIAN_POINT ( 'NONE',  ( 1.054063116485728813, 2.058546115662110765, -0.09824037785954514712 ) ) ;
#188813=CARTESIAN_POINT ( 'NONE',  ( 3.475170734053119048, -1.687717282722025924, -0.8990902037325496643 ) ) ;
#188814=CARTESIAN_POINT ( 'NONE',  ( 5.014393912088591421, 1.219005865285277546, -1.283338120600298726 ) ) ;
#188817=CARTESIAN_POINT ( 'NONE',  ( 0.5272532902790193488, -0.2650996996472804734, 1.791917353721095285 ) ) ;
#188819=CARTESIAN_POINT ( 'NONE',  ( 6.151949797202925119, 0.9892698599738621867, 1.640257924793379063 ) ) ;
#188820=CARTESIAN_POINT ( 'NONE',  ( 1.363825363374836286, -0.5049007678423790280, 2.007717453658082629 ) ) ;
#188822=CARTESIAN_POINT ( 'NONE',  ( 5.752782329262380756, -1.473788443143897675, 1.151991621687727507 ) ) ;
#188823=CARTESIAN_POINT ( 'NONE',  ( 2.279681363911123970, 1.122676072794186908, 1.439608767588994365 ) ) ;
#188824=CARTESIAN_POINT ( 'NONE',  ( 5.901041445831936016, 1.806360628843254768, -1.267562117129708232 ) ) ;
#188827=CARTESIAN_POINT ( 'NONE',  ( 4.387212324874685265, 0.09821595252585722802, 2.060445151624993976 ) ) ;
#188831=CARTESIAN_POINT ( 'NONE',  ( 0.3159878724818786511, -2.119942686789745068, 0.4214050671751194410 ) ) ;
#188832=CARTESIAN_POINT ( 'NONE',  ( 6.461392557816405535, 1.719054114842766268, 1.153505076091146053 ) ) ;
#188834=CARTESIAN_POINT ( 'NONE',  ( 3.462350783624254191, 0.9684823049558517472, 1.932541222812742987 ) ) ;
#188835=CARTESIAN_POINT ( 'NONE',  ( 4.108072977939541737, -0.7709450260172491243, 1.866947522544240901 ) ) ;
#188836=CARTESIAN_POINT ( 'NONE',  ( 2.611707774152134842, 0.5260268489151798121, -1.889944157703125072 ) ) ;
#188842=CARTESIAN_POINT ( 'NONE',  ( 2.237517880698642880, 0.5331670712399002587, -1.944730990508992008 ) ) ;
#188846=CARTESIAN_POINT ( 'NONE',  ( 6.011958326525193463, -0.6379227081053112647, 1.803018720113582996 ) ) ;
#188850=CARTESIAN_POINT ( 'NONE',  ( 3.884388800492278193, -0.6352171928143932611, -1.913798906059568594 ) ) ;
#188853=CARTESIAN_POINT ( 'NONE',  ( 6.721745554788610022, -1.671375598274482677, 0.4255071719459716517 ) ) ;
#188857=CARTESIAN_POINT ( 'NONE',  ( 4.393722961847310593, -0.7179090532695198146, 1.727491627791829742 ) ) ;
#188858=CARTESIAN_POINT ( 'NONE',  ( -0.1288028175206907822, -0.008968661790493270836, -2.273875003271644157 ) ) ;
#188859=CARTESIAN_POINT ( 'NONE',  ( 1.762639944428091576, -0.7413553172891699239, -1.933158369416078770 ) ) ;
#188862=CARTESIAN_POINT ( 'NONE',  ( 0.9840001696646907270, -2.016598147255070472, 0.002831364411433334727 ) ) ;
#188863=CARTESIAN_POINT ( 'NONE',  ( -0.2110808730067273986, 0.0005491059566040295322, -1.796958327270286704 ) ) ;
#188869=CARTESIAN_POINT ( 'NONE',  ( 6.485945863600712791, -1.915068438110486770, 0.05257573307166327897 ) ) ;
#188876=CARTESIAN_POINT ( 'NONE',  ( 2.905317003618158367, 1.825515667692039878, 1.157497049167732550 ) ) ;
#188879=CARTESIAN_POINT ( 'NONE',  ( 0.7738737444688469358, 0.4079195088417564286, -2.080830740624163955 ) ) ;
#188880=CARTESIAN_POINT ( 'NONE',  ( 6.106453908201667780, -0.6597477751954274883, -1.702385593799011110 ) ) ;
#188881=CARTESIAN_POINT ( 'NONE',  ( 0.8253839628637716919, -1.873344321310044469, 0.6141440057798281948 ) ) ;
#188882=CARTESIAN_POINT ( 'NONE',  ( 3.041163856788456687, 0.05134138945498378792, 1.911883771832747048 ) ) ;
#188885=CARTESIAN_POINT ( 'NONE',  ( 5.494576857243831824, 1.940090112543988665, 0.3384423684570179724 ) ) ;
#188886=CARTESIAN_POINT ( 'NONE',  ( 0.1638716437233995460, -1.269140265717118465, 1.469938112931449270 ) ) ;
#188890=CARTESIAN_POINT ( 'NONE',  ( 6.082307721193076944, 1.091511717630256673, 1.817998432235830908 ) ) ;
#188892=CARTESIAN_POINT ( 'NONE',  ( 5.022078740994724733, -1.902695638548990820, 0.1913334245251183119 ) ) ;
#188894=CARTESIAN_POINT ( 'NONE',  ( 0.5170026063063514199, 1.520138765826519300, -1.599913083071627273 ) ) ;
#188896=CARTESIAN_POINT ( 'NONE',  ( 6.516276865632868898, -2.012592099345715813, 0.05177761937730576691 ) ) ;
#188899=CARTESIAN_POINT ( 'NONE',  ( 1.803268859043684058, -1.750145871244257467, 1.105767233283899920 ) ) ;
#188903=CARTESIAN_POINT ( 'NONE',  ( 1.024558638192473170, 1.287004556549703693, -1.736669753874709343 ) ) ;
#188911=CARTESIAN_POINT ( 'NONE',  ( 0.1331715793776600543, 0.003733371859311258086, -1.953671397793784736 ) ) ;
#188913=CARTESIAN_POINT ( 'NONE',  ( 6.925078400183582339, 2.988348447159621113, 2.209593971251204714 ) ) ;
#188916=CARTESIAN_POINT ( 'NONE',  ( 4.500456895562253479, -1.699381082468238713, 0.3444616058281315119 ) ) ;
#188918=CARTESIAN_POINT ( 'NONE',  ( 1.938418878558012315, -1.110983660290700170, 1.746734030103759938 ) ) ;
#188919=CARTESIAN_POINT ( 'NONE',  ( 3.515340291283968632, -1.955329406025432482, 0.8124583124677657864 ) ) ;
#188922=CARTESIAN_POINT ( 'NONE',  ( 1.727339394501678838, 0.1499709341525606032, -1.963822474445919175 ) ) ;
#188924=CARTESIAN_POINT ( 'NONE',  ( 0.03522015555855115276, -0.09184495783944729430, 1.910282976853895587 ) ) ;
#188925=CARTESIAN_POINT ( 'NONE',  ( 3.943561162899355654, 0.7735357226616009774, -2.157932208606289759 ) ) ;
#188926=CARTESIAN_POINT ( 'NONE',  ( 1.840199252755945425, 1.805614550920462635, 0.2691313018618191055 ) ) ;
#188931=CARTESIAN_POINT ( 'NONE',  ( 2.847905013607958669, -1.355098151751940483, -1.488992504630684000 ) ) ;
#188932=CARTESIAN_POINT ( 'NONE',  ( 3.080854412065773928, 1.845568107317007822, 0.6654098317215583203 ) ) ;
#188936=CARTESIAN_POINT ( 'NONE',  ( 5.929650942584956397, 1.031255971971676955, -1.818501217082470145 ) ) ;
#188937=CARTESIAN_POINT ( 'NONE',  ( 4.451851733873055217, 1.769451340447548038, -0.04442182319205205399 ) ) ;
#188939=CARTESIAN_POINT ( 'NONE',  ( 0.8674257402763450031, 2.111068143204323455, -0.5878430487569612506 ) ) ;
#188940=CARTESIAN_POINT ( 'NONE',  ( 5.103314706128504241, -1.731452751257630096, 0.1754873227253881951 ) ) ;
#188943=CARTESIAN_POINT ( 'NONE',  ( 6.604150285194997139, -0.1511744057106997885, 2.264526297252217990 ) ) ;
#188945=CARTESIAN_POINT ( 'NONE',  ( 5.747320757027973848, -1.692087196126054849, -0.3772414270737846631 ) ) ;
#188946=CARTESIAN_POINT ( 'NONE',  ( 2.069229996397306426, -2.018448871333050842, -0.8927042923378907258 ) ) ;
#188947=CARTESIAN_POINT ( 'NONE',  ( 6.338351057450786641, -1.166998422550720393, 1.830725944502207048 ) ) ;
#188949=CARTESIAN_POINT ( 'NONE',  ( 1.499367237992894841, -0.2534978968403051591, 2.102027841304268119 ) ) ;
#188950=CARTESIAN_POINT ( 'NONE',  ( 3.031250000000001776, -0.7852924748301450819, -1.895863743164018400 ) ) ;
#188952=CARTESIAN_POINT ( 'NONE',  ( 4.682597122082689189, -1.868462817326870473, -0.4683620393717678465 ) ) ;
#188953=CARTESIAN_POINT ( 'NONE',  ( 0.8916360836422586589, -0.05999620363036740206, -2.220659203727569420 ) ) ;
#188958=CARTESIAN_POINT ( 'NONE',  ( 3.352378926113183777, 0.9974692666060747115, -1.984802063203878086 ) ) ;
#188963=CARTESIAN_POINT ( 'NONE',  ( 1.776017750421728270, 1.753029812786778940, -0.9963028777105964462 ) ) ;
#188965=CARTESIAN_POINT ( 'NONE',  ( 0.4091259740910870302, -1.658837074242287102, 1.225595967756993865 ) ) ;
#188968=CARTESIAN_POINT ( 'NONE',  ( 6.462468575563847573, -1.595429648854440385, -0.6960047898553810564 ) ) ;
#188970=CARTESIAN_POINT ( 'NONE',  ( 1.123854678948147834, 1.060202766368176786, -1.416847970540972668 ) ) ;
#188971=CARTESIAN_POINT ( 'NONE',  ( 0.01820432788856435335, -1.842448466851685840, 0.8197770699841927522 ) ) ;
#188972=CARTESIAN_POINT ( 'NONE',  ( 0.2218712608162629052, 1.761692264604281633, 0.5354471447000588302 ) ) ;
#188973=CARTESIAN_POINT ( 'NONE',  ( 4.318134875187846333, 1.410584032999320225, -1.806939822960533348 ) ) ;
#188974=CARTESIAN_POINT ( 'NONE',  ( 2.308333576337255000, 1.644441489820291924, 0.8281405146027611686 ) ) ;
#188978=CARTESIAN_POINT ( 'NONE',  ( 3.328933297416610593, 0.04358344136132231289, 1.825221112333124340 ) ) ;
#188979=CARTESIAN_POINT ( 'NONE',  ( 4.201796189063250253, 1.844709454618495670, 0.8146275914719460776 ) ) ;
#188981=CARTESIAN_POINT ( 'NONE',  ( 3.590934319571597033, -0.4389823211032486960, -2.219365549907009960 ) ) ;
#188983=CARTESIAN_POINT ( 'NONE',  ( 5.069407556592405939, 0.2091588727727889396, -2.095552839448256766 ) ) ;
#188985=CARTESIAN_POINT ( 'NONE',  ( 2.805202726412972858, -1.722705984639979704, 1.148039668612794051 ) ) ;
#188988=CARTESIAN_POINT ( 'NONE',  ( 6.129554906816851556, -0.2598956320666659381, 2.104415924757463419 ) ) ;
#188992=CARTESIAN_POINT ( 'NONE',  ( 0.8910897993890665170, 1.699419447932304594, -0.9074141512597186932 ) ) ;
#188999=CARTESIAN_POINT ( 'NONE',  ( 1.020144049103311801, -0.5328101295089396894, 2.156480530197317780 ) ) ;
#189000=CARTESIAN_POINT ( 'NONE',  ( 2.749164281075014760, -1.751614713500139198, 1.168827980950073009 ) ) ;
#189003=CARTESIAN_POINT ( 'NONE',  ( 5.928513603989616243, -1.181800583780348468, 1.437463819671711995 ) ) ;
#189010=CARTESIAN_POINT ( 'NONE',  ( -0.1049925189658337810, -2.058569791948822392, -0.5088776734372552069 ) ) ;
#189013=CARTESIAN_POINT ( 'NONE',  ( 2.892962425504439050, 0.2373818416543191367, 1.947367909387688112 ) ) ;
#189014=CARTESIAN_POINT ( 'NONE',  ( 2.606508400632711719, -0.8264410288459265175, -1.997682696722333784 ) ) ;
#189015=CARTESIAN_POINT ( 'NONE',  ( 0.9777802892061361328, -1.796362506263926795, -0.4033719513514140709 ) ) ;
#189019=CARTESIAN_POINT ( 'NONE',  ( 3.222313301838835020, 0.04370593061932443596, 1.739952058630070519 ) ) ;
#189022=CARTESIAN_POINT ( 'NONE',  ( 0.8663662989462637132, 1.066309655776727539, 1.880320099339624296 ) ) ;
#189024=CARTESIAN_POINT ( 'NONE',  ( 1.915388525686153143, 0.6297767875703685903, 1.915307412907449436 ) ) ;
#189025=PLANE ( 'NONE',  #89548 ) ;
#189026=CARTESIAN_POINT ( 'NONE',  ( 0.2862814217290919894, -1.017545141758866789, 1.907252267444502269 ) ) ;
#189027=CARTESIAN_POINT ( 'NONE',  ( 2.166812389411576056, -1.801713905456410858, -0.8007201275355458892 ) ) ;
#189029=CARTESIAN_POINT ( 'NONE',  ( -0.02319159430947368913, 6.948789054712430691, -2.406029888528108618 ) ) ;
#189037=CARTESIAN_POINT ( 'NONE',  ( 2.842449411481930532, 1.120122121419616423, -1.680381219987029606 ) ) ;
#189040=CARTESIAN_POINT ( 'NONE',  ( 5.298025090176222029, -0.8365315220497183679, 2.150796518170698057 ) ) ;
#189042=CARTESIAN_POINT ( 'NONE',  ( 2.957805016080543581, -0.6199431972748243869, 1.861265166911831859 ) ) ;
#189044=CARTESIAN_POINT ( 'NONE',  ( 0.05336153386781630759, -1.314994204386025434, 1.528742563917218078 ) ) ;
#189046=CARTESIAN_POINT ( 'NONE',  ( 2.536447107014605962, 0.7179835868570243473, 1.991995636484017673 ) ) ;
#189049=CARTESIAN_POINT ( 'NONE',  ( 2.571990918753517708, -1.761868631437716548, -0.5344257538507577454 ) ) ;
#189053=CARTESIAN_POINT ( 'NONE',  ( 4.535463010148616192, -0.1012041512906610846, 2.118281909017679432 ) ) ;
#189054=CARTESIAN_POINT ( 'NONE',  ( 0.3746297210940018885, 1.718982886236510854, -0.6599183738737608440 ) ) ;
#189058=CARTESIAN_POINT ( 'NONE',  ( 3.884101140911602634, -1.018864849042991461, 1.791236251998897133 ) ) ;
#189060=CARTESIAN_POINT ( 'NONE',  ( 0.9602180038516641147, -1.664555262390180257, -0.7873027242753791732 ) ) ;
#189066=CARTESIAN_POINT ( 'NONE',  ( 1.120068590173186163, -2.152398693614396397, 0.4866647226241942459 ) ) ;
#189067=CARTESIAN_POINT ( 'NONE',  ( 3.972163192483857408, 1.252710246566196783, 1.883753103390993777 ) ) ;
#189069=CARTESIAN_POINT ( 'NONE',  ( 3.568453337068989928, 0.6571482028082703541, 1.688366419454911727 ) ) ;
#189070=CARTESIAN_POINT ( 'NONE',  ( 4.171028900271775974, 1.708651049203385286, -0.8665242481073615055 ) ) ;
#189071=CARTESIAN_POINT ( 'NONE',  ( 4.949704645232674061, 1.531818663031824013, 1.392983054852282132 ) ) ;
#189075=CARTESIAN_POINT ( 'NONE',  ( 3.151204110225252819, -1.610897424746060791, -1.136263970179009819 ) ) ;
#189076=CARTESIAN_POINT ( 'NONE',  ( 0.7977241263109683400, -0.6962278615636787737, 1.796346399320443821 ) ) ;
#189077=CARTESIAN_POINT ( 'NONE',  ( 3.608139902456270143, -0.7572706533398064765, -1.710698989992056607 ) ) ;
#189078=CARTESIAN_POINT ( 'NONE',  ( 2.192384427926857615, -0.9847255960707482769, 2.087179981119008598 ) ) ;
#189079=CARTESIAN_POINT ( 'NONE',  ( 4.035495103658576888, 1.752908062920730092, -0.6255878229263853729 ) ) ;
#189084=CARTESIAN_POINT ( 'NONE',  ( 0.6277293814327978838, -1.999128025905463568, 0.6627883249872651428 ) ) ;
#189089=CARTESIAN_POINT ( 'NONE',  ( 1.652743449602233072, 2.098267697663995790, 0.3060111223712052020 ) ) ;
#189090=CARTESIAN_POINT ( 'NONE',  ( 0.3694064801790334918, -1.708597689296184274, -1.076810303892479226 ) ) ;
#189095=CARTESIAN_POINT ( 'NONE',  ( 1.106953007505812492, 1.637591863572019690, -1.411084338363017832 ) ) ;
#189097=CARTESIAN_POINT ( 'NONE',  ( 6.825078400183556937, 1.282741234726336943, 1.971047034039685952 ) ) ;
#189100=CARTESIAN_POINT ( 'NONE',  ( 5.999232488047272049, -0.2420365156972601739, 2.001857322483958423 ) ) ;
#189102=CARTESIAN_POINT ( 'NONE',  ( -0.09381621004311831158, -0.9424329983100244723, -1.976553698157037076 ) ) ;
#189104=CARTESIAN_POINT ( 'NONE',  ( 6.666866396406604167, -1.974176978123330040, -0.8811043787171415342 ) ) ;
#189108=CARTESIAN_POINT ( 'NONE',  ( 0.7025736824820059123, 1.770395976773591284, 0.7320947492839694482 ) ) ;
#189112=CARTESIAN_POINT ( 'NONE',  ( 3.299128894759464359, 1.360359547890070964, 1.060362228049552158 ) ) ;
#189114=CARTESIAN_POINT ( 'NONE',  ( 0.8777613430710672349, -0.9896981104785051997, 1.466914328529956180 ) ) ;
#189115=CARTESIAN_POINT ( 'NONE',  ( 1.611978021082097978, -0.6760664726842831040, 1.896312242100234524 ) ) ;
#189118=CARTESIAN_POINT ( 'NONE',  ( 4.278500955059440614, -1.273273528111932063, 1.802203266693293671 ) ) ;
#189122=CARTESIAN_POINT ( 'NONE',  ( 4.248766647586673884, 2.079802475202694900, 0.4125236972643344102 ) ) ;
#189123=CARTESIAN_POINT ( 'NONE',  ( 4.148064665909578785, 0.9530284220014314522, 1.777003606838889915 ) ) ;
#189124=CARTESIAN_POINT ( 'NONE',  ( 3.023486134662889402, -0.3489238238089559241, 1.777470660238470224 ) ) ;
#189128=CARTESIAN_POINT ( 'NONE',  ( 1.445950363956361340, 1.868363765441739099, 0.09516058986362013750 ) ) ;
#189129=CARTESIAN_POINT ( 'NONE',  ( 6.182242880246401562, -0.9723386526096773341, 1.545037271442825100 ) ) ;
#189131=CARTESIAN_POINT ( 'NONE',  ( 6.609000000000036401, 7.629137130509070275, 2.600000000000000977 ) ) ;
#189138=CARTESIAN_POINT ( 'NONE',  ( 4.640951271726033056, 2.030106984047326701, 0.6129599860185754867 ) ) ;
#189140=CARTESIAN_POINT ( 'NONE',  ( -0.02948999725177046949, 0.7228889410342426158, -2.008564694272568563 ) ) ;
#189142=CARTESIAN_POINT ( 'NONE',  ( 5.501234710350423107, 1.610096860432849830, 1.137200068526170060 ) ) ;
#189144=CARTESIAN_POINT ( 'NONE',  ( 0.3518148739534024960, -1.426620726115679361, -1.420723246562720421 ) ) ;
#189147=CARTESIAN_POINT ( 'NONE',  ( 0.3338148283143215767, 0.6594671527525318711, -2.011992694175788188 ) ) ;
#189149=CARTESIAN_POINT ( 'NONE',  ( 1.275928261265106833, -2.020323679977220621, 0.4517519998969782291 ) ) ;
#189152=CARTESIAN_POINT ( 'NONE',  ( 4.119144422497845959, -2.000575632760223765, 0.6069725389450402186 ) ) ;
#189155=CARTESIAN_POINT ( 'NONE',  ( 2.344514592193002400, 0.3973361102717865023, 1.781653928021959432 ) ) ;
#189156=CARTESIAN_POINT ( 'NONE',  ( 1.312835156398382885, 1.481033882128342194, -1.042734985588577468 ) ) ;
#189158=CARTESIAN_POINT ( 'NONE',  ( 5.250674450588199704, 0.6379336648693231249, 2.112661011922472021 ) ) ;
#189160=CARTESIAN_POINT ( 'NONE',  ( 4.489439581592091777, 1.972811803287272348, -0.9889974963176446643 ) ) ;
#189163=CARTESIAN_POINT ( 'NONE',  ( 2.930216680654484041, -0.9444820207657660394, -1.662695861641521278 ) ) ;
#189165=CARTESIAN_POINT ( 'NONE',  ( 5.266107318980479235, -2.060723932065291031, 0.1993833602659672022 ) ) ;
#189166=DIRECTION ( 'NONE',  ( 1.908195823574487804E-17, 1.000000000000000000, -3.097714438736600596E-15 ) ) ;
#189167=CARTESIAN_POINT ( 'NONE',  ( 6.286699343557897279, 1.907799665397521105, -1.078441415684105120 ) ) ;
#189172=CARTESIAN_POINT ( 'NONE',  ( -0.02319159430947624612, 7.629137130509076492, -2.410989586153564623 ) ) ;
#189179=CARTESIAN_POINT ( 'NONE',  ( 6.297728486381423352, -1.495382609916453998, -1.431936454106122358 ) ) ;
#189180=CARTESIAN_POINT ( 'NONE',  ( 4.424389683245252947, 1.183944675904605504, -1.519688292035234367 ) ) ;
#189181=CARTESIAN_POINT ( 'NONE',  ( 0.5093889453341126083, -1.913797760093600919, 0.6352206787166372326 ) ) ;
#189185=CARTESIAN_POINT ( 'NONE',  ( 0.6038064816080711550, -2.180521553291506986, 0.2185767975278959385 ) ) ;
#189186=CARTESIAN_POINT ( 'NONE',  ( 5.391160240453525709, 1.608232483172780558, -0.8641324296934371763 ) ) ;
#189194=CARTESIAN_POINT ( 'NONE',  ( 3.122423488780329492, 0.04808623196613136253, 1.840796284283818585 ) ) ;
#189195=CARTESIAN_POINT ( 'NONE',  ( 6.451439527836500432, -1.796305863176387518, 0.9092463195026576628 ) ) ;
#189196=CARTESIAN_POINT ( 'NONE',  ( 2.021309514094786763, 2.292189817666248075, -0.1691314976695507954 ) ) ;
#189197=CARTESIAN_POINT ( 'NONE',  ( 6.948121807170864805, -0.8414398651286276731, 1.770450887113049099 ) ) ;
#189201=CARTESIAN_POINT ( 'NONE',  ( 0.3618904354094238385, -0.5536326762660361833, 1.994880328902041589 ) ) ;
#189203=CARTESIAN_POINT ( 'NONE',  ( 2.630511997247253486, 0.2585083551314356631, 2.074647729848762889 ) ) ;
#189204=CARTESIAN_POINT ( 'NONE',  ( 0.6548940681232479077, -1.578012236938080015, -1.004313744925364071 ) ) ;
#189205=CARTESIAN_POINT ( 'NONE',  ( 1.686874821769188237, -1.117660090026689979, -1.677749154088927552 ) ) ;
#189208=CARTESIAN_POINT ( 'NONE',  ( 1.926944929849357280, -1.137335869680399902, -1.317475996949101669 ) ) ;
#189211=CARTESIAN_POINT ( 'NONE',  ( 2.683889919492283394, -0.8868522494023568514, 1.479262710868123110 ) ) ;
#189212=CARTESIAN_POINT ( 'NONE',  ( 2.560326853991791829, -1.509077608345666066, 1.589458984681046516 ) ) ;
#189213=CARTESIAN_POINT ( 'NONE',  ( 0.01762850287782054270, -1.587011929513387098, 0.6995264333442567928 ) ) ;
#189214=CARTESIAN_POINT ( 'NONE',  ( 5.531908139154323223, -1.397534428995873546, -1.707979418440738195 ) ) ;
#189217=CARTESIAN_POINT ( 'NONE',  ( 2.975608675790370583, -0.2172404834940108442, 2.160205341352925856 ) ) ;
#189218=CARTESIAN_POINT ( 'NONE',  ( 1.119449510670032177, -1.781678707675336870, 0.3977030049751931196 ) ) ;
#189220=CARTESIAN_POINT ( 'NONE',  ( 4.487589638097394307, -0.5612149057237262317, 2.041579019078069379 ) ) ;
#189223=CARTESIAN_POINT ( 'NONE',  ( 4.775077868145559457, 2.139425163340304525, -0.8237163094031977328 ) ) ;
#189228=CARTESIAN_POINT ( 'NONE',  ( 6.586594613159782341, -1.369803613283290700, 1.749543456560544552 ) ) ;
#189234=CARTESIAN_POINT ( 'NONE',  ( 4.834611377684539413, 0.6298767044488963185, -1.915599524792414465 ) ) ;
#189236=CARTESIAN_POINT ( 'NONE',  ( 2.852447711054075796, -2.056726475855717773, -0.1563953359742433491 ) ) ;
#189238=CARTESIAN_POINT ( 'NONE',  ( -0.2408018239684097672, 5.720833683022617855, -2.694520676430669059 ) ) ;
#189241=CARTESIAN_POINT ( 'NONE',  ( 5.683573789218531402, -0.9880169931659465998, 1.956149625775935430 ) ) ;
#189242=CARTESIAN_POINT ( 'NONE',  ( 3.111954093273407107, 0.05229746705895028935, 2.015912966248374349 ) ) ;
#189243=CARTESIAN_POINT ( 'NONE',  ( 2.753256032281672372, 1.832158412346639453, -0.1828795585285883096 ) ) ;
#189247=CARTESIAN_POINT ( 'NONE',  ( 6.370122744524995717, 0.9412729668686821149, 1.564051812004362940 ) ) ;
#189249=CARTESIAN_POINT ( 'NONE',  ( 6.315309700038255869, -0.2845791475536703086, 2.244501093609466924 ) ) ;
#189250=CARTESIAN_POINT ( 'NONE',  ( 2.104260374134783174, -2.105582044810641484, 0.05271062337313356383 ) ) ;
#189259=CARTESIAN_POINT ( 'NONE',  ( 4.113701061080524468, 1.785520537663972451, 1.321432767922005924 ) ) ;
#189260=CARTESIAN_POINT ( 'NONE',  ( 2.009981539508858273, -1.034714594384738229, -1.931790675223004738 ) ) ;
#189261=CARTESIAN_POINT ( 'NONE',  ( 0.6630615684519860498, -1.595754342771567025, 1.524677653706180802 ) ) ;
#189263=CARTESIAN_POINT ( 'NONE',  ( 4.316819842036943911, -1.455217238560998272, 1.315978175897666080 ) ) ;
#189270=CARTESIAN_POINT ( 'NONE',  ( 3.885109016898561585, -1.979880364965879380, -0.7601140796509860964 ) ) ;
#189272=CARTESIAN_POINT ( 'NONE',  ( 5.260679775997886054, -1.568431141927080219, 1.487858469166832176 ) ) ;
#189273=CARTESIAN_POINT ( 'NONE',  ( 4.054132754448328768, -1.361571661076573792, 1.239656203754434971 ) ) ;
#189276=CARTESIAN_POINT ( 'NONE',  ( 6.386628771994263154, 1.510377909004370522, -0.8644441249686038997 ) ) ;
#189277=CARTESIAN_POINT ( 'NONE',  ( 6.827182134110225675, 7.053278108740402175, 2.409100297097351184 ) ) ;
#189280=CARTESIAN_POINT ( 'NONE',  ( 4.135729569369491543, -1.488772398488470872, -1.567562023322838671 ) ) ;
#189282=CARTESIAN_POINT ( 'NONE',  ( 5.501327308730313170, 1.985796898448642933, 0.3474119236192701465 ) ) ;
#189284=CARTESIAN_POINT ( 'NONE',  ( 3.625982885822197410, -1.285997354380935098, -1.737435825693343094 ) ) ;
#189285=CARTESIAN_POINT ( 'NONE',  ( 4.235589135538409877, -1.357111243005538759, -1.430095230664797379 ) ) ;
#189286=CARTESIAN_POINT ( 'NONE',  ( 0.2049558871960316941, 1.909868400323280424, 1.074723926240577221 ) ) ;
#189287=CARTESIAN_POINT ( 'NONE',  ( 1.167484012262551607, -2.087313454887162578, -0.9842159052040798661 ) ) ;
#189288=CARTESIAN_POINT ( 'NONE',  ( 3.268875894143012939, -1.902732241629549348, -0.7919657925325486181 ) ) ;
#189289=CARTESIAN_POINT ( 'NONE',  ( 5.618683182394583753, -0.04358239772479224894, 1.941727988928889204 ) ) ;
#189297=CARTESIAN_POINT ( 'NONE',  ( 2.819571115601596123, -0.2173934082839618642, 2.196046946737562511 ) ) ;
#189300=CARTESIAN_POINT ( 'NONE',  ( 0.3032578436052570936, -1.433215674808469009, -1.186817810889209124 ) ) ;
#189301=CARTESIAN_POINT ( 'NONE',  ( -0.1290005225502675879, 5.719648796287211567, -2.768066027128403217 ) ) ;
#189307=CARTESIAN_POINT ( 'NONE',  ( 6.158133876658566486, -1.298579738958350660, 1.305440813956220136 ) ) ;
#189309=CARTESIAN_POINT ( 'NONE',  ( 2.536071046656536598, 0.9725223524452746293, -1.817000187329747884 ) ) ;
#189316=CARTESIAN_POINT ( 'NONE',  ( 1.252885565054340011, -1.625093837591420787, 1.267311679704327121 ) ) ;
#189318=CARTESIAN_POINT ( 'NONE',  ( 4.616662711240536510, -0.08544939198026380023, 1.839383977539174264 ) ) ;
#189322=CARTESIAN_POINT ( 'NONE',  ( 3.985166894971280183, -0.2153072539897090687, -2.196357064762343825 ) ) ;
#189323=CARTESIAN_POINT ( 'NONE',  ( 0.6851285477917113953, -0.2638797801631336259, -2.145333599305146333 ) ) ;
#189325=CARTESIAN_POINT ( 'NONE',  ( 0.1934256698341470238, 1.783621342183003389, -0.6902995980747894667 ) ) ;
#189326=CARTESIAN_POINT ( 'NONE',  ( 1.182827746461931229, 1.645757370610765102, -1.164989914844760444 ) ) ;
#189328=CARTESIAN_POINT ( 'NONE',  ( 0.07536363704233049743, 0.2309889609098912111, -2.177957698420322163 ) ) ;
#189332=CARTESIAN_POINT ( 'NONE',  ( 0.3209005354254980680, -0.09642172165634513292, 1.868300368337752815 ) ) ;
#189334=CARTESIAN_POINT ( 'NONE',  ( 2.501185699981960830, -0.1928336239410358699, 2.007256303757164240 ) ) ;
#189338=CARTESIAN_POINT ( 'NONE',  ( 3.633512520595981066, -1.945918672469678867, 0.8060524589711003385 ) ) ;
#189342=CARTESIAN_POINT ( 'NONE',  ( 3.744402900219420793, 1.076886947916893211, -1.708549110318995368 ) ) ;
#189345=CARTESIAN_POINT ( 'NONE',  ( 4.376362478467909156, -1.248523626585487989, 1.764366501186130698 ) ) ;
#189351=CARTESIAN_POINT ( 'NONE',  ( 2.524086392267041568, 2.129678358216775536, -0.4216712753718852014 ) ) ;
#189354=CARTESIAN_POINT ( 'NONE',  ( 1.171164436615620863, 1.096940724416964885, 1.478650282607060662 ) ) ;
#189356=CARTESIAN_POINT ( 'NONE',  ( 3.632539538618652752, 0.3231117836275976818, 2.167502126216628522 ) ) ;
#189358=CARTESIAN_POINT ( 'NONE',  ( 3.731548843211284439, -2.091483890824384684, 0.8634027215336376182 ) ) ;
#189364=CARTESIAN_POINT ( 'NONE',  ( 4.991328707773068807, 1.311207439723049317, 1.188721964340031301 ) ) ;
#189366=CARTESIAN_POINT ( 'NONE',  ( 1.184755817749640894, -2.054561091436296838, -0.4616562467647678525 ) ) ;
#189369=CARTESIAN_POINT ( 'NONE',  ( 1.099984078287146394, 0.8012805854674235340, -1.799388124431312797 ) ) ;
#189372=CARTESIAN_POINT ( 'NONE',  ( 6.258062559271784231, 0.6844122130202813237, -1.677549884021255933 ) ) ;
#189377=CARTESIAN_POINT ( 'NONE',  ( 4.996879044411707937, 1.554903924810165705, -1.039696167511289238 ) ) ;
#189379=CARTESIAN_POINT ( 'NONE',  ( 4.153231765667256603, 1.751622898902647663, -1.103220242290925190 ) ) ;
#189389=CARTESIAN_POINT ( 'NONE',  ( 4.404711838702720428, 0.5211615849865286476, 1.891323523724611766 ) ) ;
#189390=CARTESIAN_POINT ( 'NONE',  ( 2.600935288962639369, 0.9528664403582010056, -1.776738882381201812 ) ) ;
#189391=CARTESIAN_POINT ( 'NONE',  ( -0.1108833634136768137, 2.883350581177961391, -2.385667623150728112 ) ) ;
#189394=CARTESIAN_POINT ( 'NONE',  ( 1.704156511045151978, -0.6684128243485131238, -1.747238085743174185 ) ) ;
#189396=CARTESIAN_POINT ( 'NONE',  ( 4.254156334807709605, 0.8570458487419434501, -1.821774543695050319 ) ) ;
#189399=CARTESIAN_POINT ( 'NONE',  ( 3.726253221435165575, 2.107214626963071602, 0.2054869192316331195 ) ) ;
#189400=CARTESIAN_POINT ( 'NONE',  ( 6.825078400183546279, 2.419143596098617621, 2.525240329153962904 ) ) ;
#189401=CARTESIAN_POINT ( 'NONE',  ( 5.213363469605923228, -1.747142239327776903, -1.110534646669825376 ) ) ;
#189403=CARTESIAN_POINT ( 'NONE',  ( 6.714806893291140888, -0.1599574331335733013, 2.055667697375664016 ) ) ;
#189404=CARTESIAN_POINT ( 'NONE',  ( 6.720655732516654268, 4.688933928088002467, 2.736284108207136079 ) ) ;
#189405=CARTESIAN_POINT ( 'NONE',  ( 6.000976577881286467, 1.490888274384492895, -1.053294804101669868 ) ) ;
#189413=CARTESIAN_POINT ( 'NONE',  ( 6.393217174440144035, -0.09883813596619006603, -1.909861267343159863 ) ) ;
#189424=CARTESIAN_POINT ( 'NONE',  ( 5.536732523015378327, -1.587826920732600122, 1.242742243127918700 ) ) ;
#189427=CARTESIAN_POINT ( 'NONE',  ( -0.1405533004718676759, 6.947778977978678050, -2.315285900534403307 ) ) ;
#189430=CARTESIAN_POINT ( 'NONE',  ( 2.694150338025066205, 0.9325801345280826382, -1.734679099899273824 ) ) ;
#189431=CARTESIAN_POINT ( 'NONE',  ( 4.833611329963474645, 0.6298591494234163646, -1.915606498650752831 ) ) ;
#189433=CARTESIAN_POINT ( 'NONE',  ( 6.827182134110230116, 2.398703475977175703, 2.668604416072619223 ) ) ;
#189434=CARTESIAN_POINT ( 'NONE',  ( 4.277398745584213735, 1.430588233724191083, 1.660156109410643177 ) ) ;
#189436=CARTESIAN_POINT ( 'NONE',  ( 3.698194863803183630, -1.924136204678703832, -0.09579085892482024078 ) ) ;
#189439=CARTESIAN_POINT ( 'NONE',  ( 0.3994152196779980346, 1.832435997337564348, -1.229551327501000157 ) ) ;
#189446=CARTESIAN_POINT ( 'NONE',  ( 6.163598723784101452, 0.9525508894225950263, 1.575581956637741587 ) ) ;
#189447=CARTESIAN_POINT ( 'NONE',  ( 2.455728839946738518, -1.493258543598206201, -1.350275873876593868 ) ) ;
#189448=CARTESIAN_POINT ( 'NONE',  ( 5.097139630348237027, 1.187786601409031695, -1.967583100176452549 ) ) ;
#189450=CARTESIAN_POINT ( 'NONE',  ( 2.852234624111050110, -1.855622028292166714, -0.1419291048156411938 ) ) ;
#189456=CARTESIAN_POINT ( 'NONE',  ( 6.427293192253748622, -1.366186911818557226, -1.582700853868714397 ) ) ;
#189462=CARTESIAN_POINT ( 'NONE',  ( 6.059189007909253633, -1.483166448586000774, -0.8803546789384365523 ) ) ;
#189464=CARTESIAN_POINT ( 'NONE',  ( 0.9845302160453218709, -1.734343004718540637, -0.001328871039332768294 ) ) ;
#189469=CARTESIAN_POINT ( 'NONE',  ( 5.401315523140023167, -1.865749354952720207, 1.109950958716971803 ) ) ;
#189470=CARTESIAN_POINT ( 'NONE',  ( 5.232948167349782409, 0.1380416123818763163, 1.820529236867339584 ) ) ;
#189471=CARTESIAN_POINT ( 'NONE',  ( 2.571086506140254357, 1.750134206675527437, 0.8865088104979682582 ) ) ;
#189475=CARTESIAN_POINT ( 'NONE',  ( 4.143311163141574660, 0.1052805922370502884, 2.118007119816091688 ) ) ;
#189479=CARTESIAN_POINT ( 'NONE',  ( 1.797802452481820135, -1.496673605676283714, -1.430578824989765518 ) ) ;
#189481=CARTESIAN_POINT ( 'NONE',  ( 3.703960633009816483, 1.609604546992912999, 1.531039788047829253 ) ) ;
#189483=CARTESIAN_POINT ( 'NONE',  ( 1.407308937662318460, -1.282028150163934122, -1.907831638372993410 ) ) ;
#189485=CARTESIAN_POINT ( 'NONE',  ( 0.4089400952669055567, -1.579117232646386704, 1.163831224039679979 ) ) ;
#189492=CARTESIAN_POINT ( 'NONE',  ( -0.2102771530458276972, -0.008943344768331040057, -2.203482896658352175 ) ) ;
#189493=CARTESIAN_POINT ( 'NONE',  ( 2.713528120726243831, -1.706327644498882634, 0.2505720552260106149 ) ) ;
#189494=CARTESIAN_POINT ( 'NONE',  ( 2.835173002801576914, -1.651343842416474139, -1.157098616274463865 ) ) ;
#189495=CARTESIAN_POINT ( 'NONE',  ( 2.549810578889585067, -1.582449011024213981, 1.667500336659861748 ) ) ;
#189496=CARTESIAN_POINT ( 'NONE',  ( 3.374574379025939486, -1.350666858538966064, 1.814832908163630742 ) ) ;
#189497=CARTESIAN_POINT ( 'NONE',  ( 5.760410450299061402, 0.8521563956989952615, 1.926159629354136316 ) ) ;
#189499=CARTESIAN_POINT ( 'NONE',  ( 3.497073372749549769, 1.393195626148287403, 1.091155617269304878 ) ) ;
#189501=CARTESIAN_POINT ( 'NONE',  ( 5.899983332490822185, -0.8214817842997054198, -2.140285636048167017 ) ) ;
#189502=CARTESIAN_POINT ( 'NONE',  ( 5.314338895140062746, 1.702579029208791450, 0.7012131971957940024 ) ) ;
#189504=CARTESIAN_POINT ( 'NONE',  ( 5.578137875217415775, -2.137416510240647494, -0.4829537091169676666 ) ) ;
#189507=CARTESIAN_POINT ( 'NONE',  ( 5.705552448923417508, -1.629793913574303588, -1.276656259598766940 ) ) ;
#189508=CARTESIAN_POINT ( 'NONE',  ( -0.1355283706049141557, -1.957205112593700003, -0.4852584411360050254 ) ) ;
#189511=CARTESIAN_POINT ( 'NONE',  ( 3.879452639046445661, 1.813680402594812557, -0.6499425845708036720 ) ) ;
#189513=CARTESIAN_POINT ( 'NONE',  ( -0.1399463097118925359, -1.722747986054250058, -1.402038615606171046 ) ) ;
#189523=CARTESIAN_POINT ( 'NONE',  ( 1.240593047436115759, -1.913272810121857237, -0.4332019784048374289 ) ) ;
#189526=CARTESIAN_POINT ( 'NONE',  ( 5.951606347324345236, 1.484592722905058393, 1.282605414028796353 ) ) ;
#189529=CARTESIAN_POINT ( 'NONE',  ( 6.684453901184132185, -2.118919246787358102, -0.4271090584619871566 ) ) ;
#189533=CARTESIAN_POINT ( 'NONE',  ( 1.932664581101939838, 0.1784410483233467293, 1.861995071071875785 ) ) ;
#189534=CARTESIAN_POINT ( 'NONE',  ( 0.1758332513315676859, 1.282751065617006248, 1.167194905859494591 ) ) ;
#189536=CARTESIAN_POINT ( 'NONE',  ( 4.581673536070863584, -1.032772929490553215, 1.932928240684625099 ) ) ;
#189537=CARTESIAN_POINT ( 'NONE',  ( 4.841030633121579996, 0.3891503725830172677, 2.274395804800657839 ) ) ;
#189538=CARTESIAN_POINT ( 'NONE',  ( 0.2157906144764632494, -2.021207876486079691, 0.4015242071495705445 ) ) ;
#189539=CARTESIAN_POINT ( 'NONE',  ( 2.870961461768199108, 1.843879596475753502, -0.6095136124301904212 ) ) ;
#189542=CARTESIAN_POINT ( 'NONE',  ( 5.168275554957600271, 2.118074532352266282, -0.1063875075708180934 ) ) ;
#189544=CARTESIAN_POINT ( 'NONE',  ( 3.182267690267494231, 1.591318367894577701, 1.238320962759748234 ) ) ;
#189548=CARTESIAN_POINT ( 'NONE',  ( 1.558932953716257730, -1.564965500463588732, -0.9399777662534372080 ) ) ;
#189554=CARTESIAN_POINT ( 'NONE',  ( 6.016494556629995216, 1.386029456380773572, -1.525348796181945854 ) ) ;
#189560=CARTESIAN_POINT ( 'NONE',  ( 4.002606914492294443, -1.998013091498285654, -0.2940530905436929410 ) ) ;
#189561=CARTESIAN_POINT ( 'NONE',  ( 5.285853969472154468, 2.141190784740894415, -0.5908706489107099502 ) ) ;
#189566=CARTESIAN_POINT ( 'NONE',  ( 3.748945967280458369, -1.685778541264292274, 1.185220002557571206 ) ) ;
#189567=CARTESIAN_POINT ( 'NONE',  ( 3.709611425391425854, 1.915599900965975433, 0.6298755557959597740 ) ) ;
#189568=EDGE_LOOP ( 'NONE', ( #6531, #71709 ) ) ;
#189573=CARTESIAN_POINT ( 'NONE',  ( 3.673203737196802710, -0.8145011343782401214, -1.844427810980188820 ) ) ;
#189574=CARTESIAN_POINT ( 'NONE',  ( 2.607153984523866264, -1.821078476238715327, 0.2702138248509636242 ) ) ;
#189576=CARTESIAN_POINT ( 'NONE',  ( 0.6105616303546910206, -2.295997848557976617, 0.2320981213338509652 ) ) ;
#189578=CARTESIAN_POINT ( 'NONE',  ( 3.761131992884462871, -1.904433681825665969, -1.022602951024270679 ) ) ;
#189581=CARTESIAN_POINT ( 'NONE',  ( 3.269240723250285363, -2.295843464198448203, 0.1100516299901241751 ) ) ;
#189583=CARTESIAN_POINT ( 'NONE',  ( 2.465516990510143280, 1.834972510290140191, -0.3627323784974947340 ) ) ;
#189586=CARTESIAN_POINT ( 'NONE',  ( 5.682488568729203493, -1.923295458312636264, -0.4324549907560610307 ) ) ;
#189590=CARTESIAN_POINT ( 'NONE',  ( 0.6982365061397632910, -0.7907169553198112322, 2.060542492664858560 ) ) ;
#189595=CARTESIAN_POINT ( 'NONE',  ( 5.735224789204648843, -1.782488891340678894, 0.8425237689327728097 ) ) ;
#189596=CARTESIAN_POINT ( 'NONE',  ( 5.725286558339668375, -0.06233732282829743815, 2.307013574275817547 ) ) ;
#189597=CARTESIAN_POINT ( 'NONE',  ( 0.2737812321212430566, -1.924752420120953822, 0.3788971555385572954 ) ) ;
#189598=CARTESIAN_POINT ( 'NONE',  ( 2.993094585481168579, 0.2480512885563341541, 2.047511573040517341 ) ) ;
#189605=CARTESIAN_POINT ( 'NONE',  ( 5.389208567375425751, 0.1545246996936377182, 2.165725388718000133 ) ) ;
#189607=CARTESIAN_POINT ( 'NONE',  ( 5.636236351835953506, 0.3653394402399374741, 1.804471444190151930 ) ) ;
#189609=CARTESIAN_POINT ( 'NONE',  ( 6.620655732516651071, 7.053049904137934867, 2.524417197114035005 ) ) ;
#189610=CARTESIAN_POINT ( 'NONE',  ( 6.462441986028243157, -2.002789442531027309, -0.8901952361822995652 ) ) ;
#189611=CARTESIAN_POINT ( 'NONE',  ( 0.2099203756031532975, -0.7936979409460078738, -1.692237190125941648 ) ) ;
#189612=CARTESIAN_POINT ( 'NONE',  ( 0.2810632938833834693, -2.195003449849114663, -0.5476492663787374537 ) ) ;
#189617=CARTESIAN_POINT ( 'NONE',  ( 0.2406774923011632261, 1.829974501424940891, 0.5550298453492612527 ) ) ;
#189618=CARTESIAN_POINT ( 'NONE',  ( 2.359889027365429826, 0.7540158325645224258, 1.601324458166239806 ) ) ;
#189620=CARTESIAN_POINT ( 'NONE',  ( -0.1049974700286886165, -0.1398519552151776535, -1.881156918050665094 ) ) ;
#189622=CARTESIAN_POINT ( 'NONE',  ( 3.269047429782430125, 1.730524700466531396, -0.8218109994902050852 ) ) ;
#189624=CARTESIAN_POINT ( 'NONE',  ( 4.527769023902194157, 1.910916496070225179, -0.4765158004534468805 ) ) ;
#189625=CARTESIAN_POINT ( 'NONE',  ( 6.205333298273250975, 1.755376394247827987, -0.9990029765977179732 ) ) ;
#189627=CARTESIAN_POINT ( 'NONE',  ( 2.553401164250346245, 0.5009360343536627402, -1.802255699741683870 ) ) ;
#189628=CARTESIAN_POINT ( 'NONE',  ( 5.602095939246814815, -1.725068444894608310, 0.006287883723511687381 ) ) ;
#189630=CARTESIAN_POINT ( 'NONE',  ( 2.508667999599442755, -0.8457060194008919618, -2.038605049697986615 ) ) ;
#189633=CARTESIAN_POINT ( 'NONE',  ( 6.092239754786219486, 0.9682357284593717806, -1.706234036142616928 ) ) ;
#189639=CARTESIAN_POINT ( 'NONE',  ( 1.645070734656968625, -0.3017366986639741788, -2.048123538821471801 ) ) ;
#189643=CARTESIAN_POINT ( 'NONE',  ( 0.1705770660650838266, 0.7750864355984161680, 1.865232097879976125 ) ) ;
#189649=CARTESIAN_POINT ( 'NONE',  ( 5.167342215279057349, -0.6766115767681827320, -1.899327316215810635 ) ) ;
#189650=CARTESIAN_POINT ( 'NONE',  ( 5.243340954880816973, 0.3670949043641066889, -1.880036887305686966 ) ) ;
#189651=CARTESIAN_POINT ( 'NONE',  ( 6.539320575229258914, 2.958022083381315337, 2.556018433155104574 ) ) ;
#189652=CARTESIAN_POINT ( 'NONE',  ( 2.841561854484982774, 0.7863008361240211297, -2.045831095052422555 ) ) ;
#189654=CARTESIAN_POINT ( 'NONE',  ( 2.320441991784210067, -0.7354482596747035084, -1.765520077574176172 ) ) ;
#189657=CARTESIAN_POINT ( 'NONE',  ( -0.0003749349099593791675, -1.976945657698804704, 0.3961262320883383592 ) ) ;
#189659=CARTESIAN_POINT ( 'NONE',  ( 6.251546423958431298, 2.185849743821382862, -0.1592787069685035195 ) ) ;
#189661=CARTESIAN_POINT ( 'NONE',  ( 2.889346415704593607, 1.218289440699829473, 1.221169829160633435 ) ) ;
#189662=ORIENTED_EDGE ( 'NONE', *, *, #32479, .F. ) ;
#189663=CARTESIAN_POINT ( 'NONE',  ( 5.941668366282723213, -1.996146358238064522, 0.7160658055916299114 ) ) ;
#189666=CARTESIAN_POINT ( 'NONE',  ( 0.4847190467827041105, 1.876267867961832980, 0.5731238010058882226 ) ) ;
#189673=CARTESIAN_POINT ( 'NONE',  ( 3.070771698229213698, -1.370002115350689165, 1.185199408711124835 ) ) ;
#189677=CARTESIAN_POINT ( 'NONE',  ( 3.387185712204858312, 0.04143215291275677975, -1.811162278692766581 ) ) ;
#189682=CARTESIAN_POINT ( 'NONE',  ( 4.773795620589037725, -1.825254877749547866, 0.3623055857514579370 ) ) ;
#189684=CARTESIAN_POINT ( 'NONE',  ( 3.128438982650301625, 0.4684375082077455454, 1.857299403769121060 ) ) ;
#189685=CARTESIAN_POINT ( 'NONE',  ( 1.430379662499326354, 1.758314708518812663, 0.4907259477668829972 ) ) ;
#189691=CARTESIAN_POINT ( 'NONE',  ( 6.925078400183577010, 2.950057911518181974, 2.596529392604688180 ) ) ;
#189693=CARTESIAN_POINT ( 'NONE',  ( 5.946149452469858154, -0.8887192358506822432, 1.757629817417952767 ) ) ;
#189695=CARTESIAN_POINT ( 'NONE',  ( 1.060620546929908148, -1.890798925694850974, -0.8922787324358200101 ) ) ;
#189696=CARTESIAN_POINT ( 'NONE',  ( 6.704134009050578769, -1.925936059460537697, 0.04828832120675958378 ) ) ;
#189698=CARTESIAN_POINT ( 'NONE',  ( 1.957752326685862077, 1.820926393389955988, -0.1310869387763091420 ) ) ;
#189699=CARTESIAN_POINT ( 'NONE',  ( 2.983271218942393332, -0.1628219013674602478, -2.200934326520533446 ) ) ;
#189701=CARTESIAN_POINT ( 'NONE',  ( 0.4922593472763935329, -1.060406550076501642, 1.591262010887870115 ) ) ;
#189702=CARTESIAN_POINT ( 'NONE',  ( 1.381238074367253876, -0.05158952566820934615, 1.969057209924016227 ) ) ;
#189703=CARTESIAN_POINT ( 'NONE',  ( 2.208448867685277150, 1.735655609654564113, 0.8713670519163093653 ) ) ;
#189707=CARTESIAN_POINT ( 'NONE',  ( 6.332830178222744522, -1.766687566082520533, -0.5848361604409312298 ) ) ;
#189712=CARTESIAN_POINT ( 'NONE',  ( 2.331793494658142230, 1.030094174309360344, -1.934364310732391345 ) ) ;
#189717=CARTESIAN_POINT ( 'NONE',  ( 2.490611698265518648, -0.3118145247060916114, -1.798701865878708839 ) ) ;
#189718=CARTESIAN_POINT ( 'NONE',  ( 5.981657729715996297, -0.6748525008196132324, 1.900413905137773529 ) ) ;
#189723=CARTESIAN_POINT ( 'NONE',  ( 2.156748612084181005, -1.489394325481137260, 1.221923121036755600 ) ) ;
#189725=CARTESIAN_POINT ( 'NONE',  ( 6.157081138237819218, 1.605775322519078729, -1.126676614267435150 ) ) ;
#189733=CARTESIAN_POINT ( 'NONE',  ( 5.225469540725330653, 0.2083811790645866135, -2.059773418507819365 ) ) ;
#189735=CARTESIAN_POINT ( 'NONE',  ( 5.221416903470996296, 2.264307454851313572, 0.3953409806420198347 ) ) ;
#189739=CARTESIAN_POINT ( 'NONE',  ( 6.532792773074245218, -2.049936377808206700, 1.026291560346163534 ) ) ;
#189742=CARTESIAN_POINT ( 'NONE',  ( 5.402268692527759875, 1.469326413266746956, -1.269838510729433212 ) ) ;
#189746=CARTESIAN_POINT ( 'NONE',  ( 6.451426615364327155, -1.705040744490589066, 0.8662930942644477827 ) ) ;
#189747=CARTESIAN_POINT ( 'NONE',  ( 0.9083514600924915694, 1.308824770132447135, -1.123559637378883203 ) ) ;
#189748=CARTESIAN_POINT ( 'NONE',  ( 5.893767612163585135, -2.000732204962274441, 0.2516274335107801519 ) ) ;
#189752=CARTESIAN_POINT ( 'NONE',  ( 1.130938551725582109, -1.889365942417848832, 0.8953178049561462126 ) ) ;
#189753=CARTESIAN_POINT ( 'NONE',  ( 1.322737547172361472, -0.04825712817433693014, 1.769365563168373345 ) ) ;
#189756=CARTESIAN_POINT ( 'NONE',  ( 4.365347222306335873, 2.224029864950861857, -0.5546456485611241938 ) ) ;
#189757=CARTESIAN_POINT ( 'NONE',  ( 2.343362483081043557, 1.739954169810492557, 0.04345107811378270263 ) ) ;
#189759=CARTESIAN_POINT ( 'NONE',  ( 3.199588043238619228, 1.915454767000431602, -0.9102714984489732597 ) ) ;
#189762=CARTESIAN_POINT ( 'NONE',  ( 2.706025971585944490, -1.282006620817040643, -1.167505586895122072 ) ) ;
#189764=CARTESIAN_POINT ( 'NONE',  ( 1.381066672459789979, -0.05041352683890670816, 1.860554536023711458 ) ) ;
#189765=CARTESIAN_POINT ( 'NONE',  ( 2.172564162468085147, -1.022266837292043595, -1.915435327925461229 ) ) ;
#189767=CARTESIAN_POINT ( 'NONE',  ( 3.749232653202066778, 0.2420323627391370025, -2.001857840249580800 ) ) ;
#189768=CARTESIAN_POINT ( 'NONE',  ( 3.000000000000002665, -1.776620610948833047E-13, -2.052068128417948945 ) ) ;
#189771=CARTESIAN_POINT ( 'NONE',  ( 1.307504913943892122, -0.4706295199745584301, 1.867897339068110618 ) ) ;
#189773=CARTESIAN_POINT ( 'NONE',  ( 5.097972104635399404, 1.492264293747805226, 1.645667271412653898 ) ) ;
#189779=CARTESIAN_POINT ( 'NONE',  ( 5.730790430626864662, 1.492114905813126446, -1.645873056973495618 ) ) ;
#189780=CARTESIAN_POINT ( 'NONE',  ( 5.160583804383015227, -0.6592509027269661814, -1.847929681152965520 ) ) ;
#189783=CARTESIAN_POINT ( 'NONE',  ( 5.694667785318580755, -0.5416461603767928068, -2.196524604246933521 ) ) ;
#189786=CARTESIAN_POINT ( 'NONE',  ( 2.770046845359328103, -2.040585247751625086, 0.3002346618998888439 ) ) ;
#189791=CARTESIAN_POINT ( 'NONE',  ( 4.288257209584379837, -1.849852534125648207, -0.2767368629695772797 ) ) ;
#189792=CARTESIAN_POINT ( 'NONE',  ( 3.410549273128512304, -1.036309148604511288, -1.390238610006881981 ) ) ;
#189793=CARTESIAN_POINT ( 'NONE',  ( 1.715945410011958217, 1.623988859063689949, 0.6264298892959454523 ) ) ;
#189794=CARTESIAN_POINT ( 'NONE',  ( 1.101600182630409819, -0.5506920761103645257, 2.225148091679912454 ) ) ;
#189795=CARTESIAN_POINT ( 'NONE',  ( 1.343116161061377545, 0.4315099961175078436, 2.164003993775004187 ) ) ;
#189796=CARTESIAN_POINT ( 'NONE',  ( 4.317973780707057507, 1.284968578774790426, -1.649195526182813509 ) ) ;
#189797=CARTESIAN_POINT ( 'NONE',  ( 5.419850138435895914, 1.155063568626579995, -1.560950513000541662 ) ) ;
#189800=CARTESIAN_POINT ( 'NONE',  ( 0.7213275451133926985, 1.987047012402185731, 0.3419330716275259530 ) ) ;
#189805=CARTESIAN_POINT ( 'NONE',  ( 4.301258635363705451, 1.467727663998198429, 1.085573330547324744 ) ) ;
#189806=CARTESIAN_POINT ( 'NONE',  ( 1.870444250305805856, 1.134645063044220858, 1.892580404734986121 ) ) ;
#189814=CARTESIAN_POINT ( 'NONE',  ( 0.7385429019767172365, 1.199765550694283478, -1.624703887242204825 ) ) ;
#189817=CARTESIAN_POINT ( 'NONE',  ( 3.291705155655884951, -1.246473628130102762, -1.382024748694546501 ) ) ;
#189824=CARTESIAN_POINT ( 'NONE',  ( 4.758326833623739205, 0.7015320795021735556, 1.685726030614169924 ) ) ;
#189828=CARTESIAN_POINT ( 'NONE',  ( 0.1922019376490837483, -1.058930769078871403, -1.372993611190379104 ) ) ;
#189829=CARTESIAN_POINT ( 'NONE',  ( 0.5854151811709865649, -1.726609166672494311, -0.2174223460936832719 ) ) ;
#189830=CARTESIAN_POINT ( 'NONE',  ( 3.897355454345535097, 1.950357463199345442, -1.233256315927799607 ) ) ;
#189832=CARTESIAN_POINT ( 'NONE',  ( 6.608665842073913943, 1.606649649811153990, -1.446306907624186344 ) ) ;
#189836=CARTESIAN_POINT ( 'NONE',  ( 6.169324051992485458, -0.8183585724929974825, -2.147936757437307165 ) ) ;
#189839=CARTESIAN_POINT ( 'NONE',  ( 5.541831131927607679, 0.7570117910807551143, -1.710825945835430462 ) ) ;
#189841=CARTESIAN_POINT ( 'NONE',  ( 2.759904966095374501, 0.6844231338998980618, -1.785916880244736715 ) ) ;
#189843=CARTESIAN_POINT ( 'NONE',  ( 5.461621781982892720, 0.4335984126433762853, -2.163701019753036192 ) ) ;
#189844=CARTESIAN_POINT ( 'NONE',  ( 4.856716432673345629, -1.994826133969303195, -0.7102248925668596113 ) ) ;
#189850=CARTESIAN_POINT ( 'NONE',  ( 2.749405113950495583, -1.918974089273906003, 1.281321877411125909 ) ) ;
#189851=CARTESIAN_POINT ( 'NONE',  ( 3.789464544343919883, -1.813617537123424661, 0.7486148740368094856 ) ) ;
#189853=CARTESIAN_POINT ( 'NONE',  ( 6.772339297775464395, -0.9671665324481359960, -1.821725317472399963 ) ) ;
#189857=CARTESIAN_POINT ( 'NONE',  ( 5.243375144629232487, 0.3886363430659239837, -1.978554426619572926 ) ) ;
#189863=CARTESIAN_POINT ( 'NONE',  ( 1.815514387157551646, -1.860550965366158715, -1.118705476460989168 ) ) ;
#189865=PLANE ( 'NONE',  #117365 ) ;
#189870=CARTESIAN_POINT ( 'NONE',  ( 1.440775599906311433, 0.3991536164789717955, 2.021572055866586837 ) ) ;
#189871=CARTESIAN_POINT ( 'NONE',  ( -0.02224634325202321655, 2.854569189074110280, -2.777010687634806629 ) ) ;
#189872=CARTESIAN_POINT ( 'NONE',  ( 6.727182134110170075, 7.629137130509032971, 2.510944104600740356 ) ) ;
#189876=CARTESIAN_POINT ( 'NONE',  ( 3.387273370026026686, 0.04433669930821101945, -1.911926451916061476 ) ) ;
#189877=CARTESIAN_POINT ( 'NONE',  ( 5.682415782506053503, -1.727394229680437876, -0.3844701117694647174 ) ) ;
#189881=CARTESIAN_POINT ( 'NONE',  ( 6.538697978567284963, -1.477089011224671955, 1.219511253712385335 ) ) ;
#189884=CARTESIAN_POINT ( 'NONE',  ( 0.7485892145711986467, -2.054541080789675789, -0.2550698046258002005 ) ) ;
#189886=CARTESIAN_POINT ( 'NONE',  ( 5.629731426258720361, -1.187751674602673058, -1.445209747047627946 ) ) ;
#189887=CARTESIAN_POINT ( 'NONE',  ( 2.490611698265518648, -0.3118145247060916114, -1.798701865878708839 ) ) ;
#189889=CARTESIAN_POINT ( 'NONE',  ( 5.707716145626243964, -0.5396369327701348029, 2.139774205771049154 ) ) ;
#189892=CARTESIAN_POINT ( 'NONE',  ( 3.086439574430835275, 1.148074821921121647, -1.713452782031915200 ) ) ;
#189896=CARTESIAN_POINT ( 'NONE',  ( 0.4038910500440278106, -0.5768866637368921246, 2.083095904058133385 ) ) ;
#189898=CARTESIAN_POINT ( 'NONE',  ( 5.143061708805018561, -0.2499388813127951525, -2.055141626981969338 ) ) ;
#189900=CARTESIAN_POINT ( 'NONE',  ( 3.497504216883956296, 1.701635573755799324, 1.332874705691905248 ) ) ;
#189902=CARTESIAN_POINT ( 'NONE',  ( 2.930336769707508893, -0.9972767022783147750, -1.756213584645490267 ) ) ;
#189903=CARTESIAN_POINT ( 'NONE',  ( 2.488659587246494276, 1.902222718079676689, 0.4795239450603656084 ) ) ;
#189904=CARTESIAN_POINT ( 'NONE',  ( 6.720655732516642722, 6.033109933379183332, 2.868628414513713309 ) ) ;
#189908=CARTESIAN_POINT ( 'NONE',  ( 2.589077643123653072, 1.706113014995232380, 1.074661422923957055 ) ) ;
#189912=CARTESIAN_POINT ( 'NONE',  ( 5.695548698317931091, 1.764485844685494742, -0.7379451211212140205 ) ) ;
#189916=CARTESIAN_POINT ( 'NONE',  ( 2.794546173781168541, 1.458544728081469177, -1.392559875802508396 ) ) ;
#189919=CARTESIAN_POINT ( 'NONE',  ( 0.06452196833307657919, -1.538014849765593439, -0.7809378474108348289 ) ) ;
#189923=CARTESIAN_POINT ( 'NONE',  ( 4.428871017648271291, 0.08965458760558722706, 1.868499062828571367 ) ) ;
#189925=CARTESIAN_POINT ( 'NONE',  ( 1.727480438796034745, 0.1563249218069600044, -2.064440809470533544 ) ) ;
#189929=CARTESIAN_POINT ( 'NONE',  ( 0.6854714705560975840, 1.745592605935637920, -0.4840870370880663853 ) ) ;
#189937=CARTESIAN_POINT ( 'NONE',  ( 5.519116348382159032, -1.729776616345682028, 0.8233883490022309015 ) ) ;
#189938=CARTESIAN_POINT ( 'NONE',  ( 6.827182134110198142, 0.003888933837258023996, 1.810856214465889069 ) ) ;
#189943=CARTESIAN_POINT ( 'NONE',  ( 3.239309987758617115, -1.907233169736745060, 1.017530501952010447 ) ) ;
#189947=CARTESIAN_POINT ( 'NONE',  ( -0.08743476694611679312, -2.120266877281291595, -0.04547849331201780226 ) ) ;
#189948=CARTESIAN_POINT ( 'NONE',  ( 6.282242891264209206, -0.9739734823789309992, 1.543877162560061134 ) ) ;
#189950=CARTESIAN_POINT ( 'NONE',  ( 0.6847650648834556764, -0.2371060910116972453, -1.956967405937762639 ) ) ;
#189953=CARTESIAN_POINT ( 'NONE',  ( 4.861744415569490663, -0.5273948137594737240, 1.897533870164061831 ) ) ;
#189955=CARTESIAN_POINT ( 'NONE',  ( 6.005412763054238212, -1.926851508234005195, 0.2422190414417753623 ) ) ;
#189956=ORIENTED_EDGE ( 'NONE', *, *, #117909, .T. ) ;
#189959=CARTESIAN_POINT ( 'NONE',  ( 6.170199167347634628, 2.114832956739281400, -0.1575216572810705096 ) ) ;
#189961=CARTESIAN_POINT ( 'NONE',  ( 3.861887077619485797, 0.6414691495152945455, -1.801623935260010079 ) ) ;
#189962=ORIENTED_EDGE ( 'NONE', *, *, #190238, .F. ) ;
#189963=CARTESIAN_POINT ( 'NONE',  ( 1.167327668269029228, -1.995579438226593894, -0.9423882379527288577 ) ) ;
#189966=CARTESIAN_POINT ( 'NONE',  ( 6.164703283132928924, 0.6335332109005767931, 1.910856914995302303 ) ) ;
#189968=CARTESIAN_POINT ( 'NONE',  ( 6.586557105272873969, -1.791547847876047594, -0.3505316570680468979 ) ) ;
#189969=CARTESIAN_POINT ( 'NONE',  ( 2.295452831283749440, -1.850383948470477602, 0.9288054807428182125 ) ) ;
#189978=CARTESIAN_POINT ( 'NONE',  ( 6.925078400183531713, 2.446544591822760850, 2.338552149501707422 ) ) ;
#189980=CARTESIAN_POINT ( 'NONE',  ( 5.133366751340045830, 0.5111148723837605212, 1.657103328152222055 ) ) ;
#189982=CARTESIAN_POINT ( 'NONE',  ( 2.606376076552410659, 2.069701014239883730, 0.05521581806712527740 ) ) ;
#189983=CARTESIAN_POINT ( 'NONE',  ( 3.937202496034042376, -1.761399977300786901, -1.174509457245224597 ) ) ;
#189987=CARTESIAN_POINT ( 'NONE',  ( 1.551539110526085619, 1.487754399324931365, 1.290523904849065095 ) ) ;
#189990=CARTESIAN_POINT ( 'NONE',  ( 0.2813230411330031044, 0.1852680230450229892, -1.903361379684164412 ) ) ;
#189991=CARTESIAN_POINT ( 'NONE',  ( 3.293229231460121031, 1.807080150709074129, 1.410200864199236293 ) ) ;
#189992=CARTESIAN_POINT ( 'NONE',  ( 1.523764310407934808, -1.012771255265769943, -1.518815351243132161 ) ) ;
#189997=CARTESIAN_POINT ( 'NONE',  ( 3.427992945418765203, -1.982693224445150060, 0.3483943456095982549 ) ) ;
#189998=CARTESIAN_POINT ( 'NONE',  ( 2.957805016080543581, -0.6199431972748243869, 1.861265166911831859 ) ) ;
#190002=CARTESIAN_POINT ( 'NONE',  ( 5.648407305961395508, -1.648567506571393615, 1.285558710341473621 ) ) ;
#190003=CARTESIAN_POINT ( 'NONE',  ( 4.592510532270950740, -0.3890688374885014067, -1.726373200486588377 ) ) ;
#190005=CARTESIAN_POINT ( 'NONE',  ( 0.7443833103580773658, 0.6396484562771963533, 2.096019810003430184 ) ) ;
#190006=CARTESIAN_POINT ( 'NONE',  ( 5.824081541776103599, 1.678935111502709354, 0.4578980800337121848 ) ) ;
#190009=CARTESIAN_POINT ( 'NONE',  ( 0.1331715793776860612, 5.723291439345874920, -2.547624684121822636 ) ) ;
#190010=CARTESIAN_POINT ( 'NONE',  ( 6.240923344934847350, 2.292853006454723452, -0.1649963611656188323 ) ) ;
#190012=CARTESIAN_POINT ( 'NONE',  ( 5.624279254961046526, 0.3357223255188810374, -1.700804604882939053 ) ) ;
#190013=CARTESIAN_POINT ( 'NONE',  ( 5.547405112160277874, 1.917339678720403118, -1.018715297254897401 ) ) ;
#190015=CARTESIAN_POINT ( 'NONE',  ( -0.1001773172763717329, -2.075113514603315945, 0.4199855073994100407 ) ) ;
#190016=CARTESIAN_POINT ( 'NONE',  ( 3.781250000000002665, 0.7852924748301846058, 1.895863743164001081 ) ) ;
#190017=CARTESIAN_POINT ( 'NONE',  ( 6.827182134110199030, -0.004087946457608306570, 2.088967824442849341 ) ) ;
#190018=CARTESIAN_POINT ( 'NONE',  ( 3.944294614955777600, 1.917013643722576433, 0.1899554498810165082 ) ) ;
#190020=CARTESIAN_POINT ( 'NONE',  ( 1.067367041543025197, -1.747990651676500029, 1.370551686305313321 ) ) ;
#190025=CARTESIAN_POINT ( 'NONE',  ( 2.860263265526213683, 0.7972832613293324711, -2.073463298260522780 ) ) ;
#190031=CARTESIAN_POINT ( 'NONE',  ( 0.7916389524552720491, 1.525042296397002284, -1.319230309296010928 ) ) ;
#190033=CARTESIAN_POINT ( 'NONE',  ( 6.865701141133224716, -0.4594653659172152071, 2.018469443450424894 ) ) ;
#190038=CARTESIAN_POINT ( 'NONE',  ( 1.317257508235271102, -1.728110672573167639, 0.3808341387830004865 ) ) ;
#190039=CARTESIAN_POINT ( 'NONE',  ( 6.469374514269041754, -1.702674068921444572, -0.3278888851577909658 ) ) ;
#190040=CARTESIAN_POINT ( 'NONE',  ( 0.01093749962182561514, -1.805946196879631094, 0.3578947576599255664 ) ) ;
#190041=CARTESIAN_POINT ( 'NONE',  ( 4.423529165095542837, -1.409716928370784661, -1.807567988613969723 ) ) ;
#190043=CARTESIAN_POINT ( 'NONE',  ( 2.484105014303281234, -0.3146448974087300288, -1.813890345909507928 ) ) ;
#190046=CARTESIAN_POINT ( 'NONE',  ( 2.959763373685083909, 1.816946311034864703, -0.1772020141349931188 ) ) ;
#190047=CARTESIAN_POINT ( 'NONE',  ( 3.639296212489909532, 0.7283784247123014088, 1.880435045658496618 ) ) ;
#190049=CARTESIAN_POINT ( 'NONE',  ( 3.977597974223236132, 2.131470459685447238, -0.7591987100158004154 ) ) ;
#190051=CARTESIAN_POINT ( 'NONE',  ( 4.999102919943527290, 1.752478773177888582, -1.167534824283325667 ) ) ;
#190053=CARTESIAN_POINT ( 'NONE',  ( 2.822784111170244525, -1.429543836668966561, 1.497820115680066344 ) ) ;
#190056=CARTESIAN_POINT ( 'NONE',  ( 4.776102292387626846, 2.097323840013893381, -0.3118266106481304423 ) ) ;
#190059=CARTESIAN_POINT ( 'NONE',  ( 0.6098321186917586845, -1.917330571200571265, 0.1878080533235688687 ) ) ;
#190066=CARTESIAN_POINT ( 'NONE',  ( 0.9673671849170182302, -1.746833394359051495, 1.372194155552537431 ) ) ;
#190067=CARTESIAN_POINT ( 'NONE',  ( 1.923017885777689839, 1.964713842245609410, 0.7587240108328905386 ) ) ;
#190070=CARTESIAN_POINT ( 'NONE',  ( 6.825069993440997074, -1.701324435194497831, -0.7545304760708021474 ) ) ;
#190075=CARTESIAN_POINT ( 'NONE',  ( -0.01710467543277957581, -1.380256469788909035, 1.610041658517608054 ) ) ;
#190078=CARTESIAN_POINT ( 'NONE',  ( 3.051168888765115828, 1.684027830550902882, -1.006202029777767848 ) ) ;
#190079=CARTESIAN_POINT ( 'NONE',  ( 2.624079441566569582, -1.243859440641072123, -1.767801033134681843 ) ) ;
#190083=CARTESIAN_POINT ( 'NONE',  ( 3.960698422707895627, 0.2102999545306425688, -1.727497421908174458 ) ) ;
#190087=CARTESIAN_POINT ( 'NONE',  ( 2.056017322730230301, 1.755501262438976751, -0.9912458455646618871 ) ) ;
#190088=CARTESIAN_POINT ( 'NONE',  ( 6.825078400183544503, 6.034152930826206962, 2.739236550662868197 ) ) ;
#190090=CARTESIAN_POINT ( 'NONE',  ( 1.938291742056476030, 1.949724373066508143, 0.2912656003557292927 ) ) ;
#190096=CARTESIAN_POINT ( 'NONE',  ( 2.016276777042900203, -2.019190368190917795, 0.05175015523710930349 ) ) ;
#190099=CARTESIAN_POINT ( 'NONE',  ( 6.036188935239226616, 1.144513723677667461, -2.003705632283636184 ) ) ;
#190101=CARTESIAN_POINT ( 'NONE',  ( 3.239059677355364375, -0.1396402669299641186, -1.956817938210092089 ) ) ;
#190103=CARTESIAN_POINT ( 'NONE',  ( 1.020157974382044364, -1.821741137083273010, 0.8647263380179845971 ) ) ;
#190105=CARTESIAN_POINT ( 'NONE',  ( 1.903655596893740087, -2.052436370740511773, 0.5197080100793128876 ) ) ;
#190108=CARTESIAN_POINT ( 'NONE',  ( 2.448939195788137013, 0.4911642875529352303, -1.774347143093172097 ) ) ;
#190111=CARTESIAN_POINT ( 'NONE',  ( 3.146849984228027974, 2.069795010335002239, 0.4607391970517027979 ) ) ;
#190112=CARTESIAN_POINT ( 'NONE',  ( 0.02305342982030639601, -1.130023889514218505, -1.454075609423427728 ) ) ;
#190116=CARTESIAN_POINT ( 'NONE',  ( 4.675106833541732954, 0.004019643978107888781, -2.060967561157340810 ) ) ;
#190119=CARTESIAN_POINT ( 'NONE',  ( 1.329379181053941483, 0.9071106928158387817, -1.602193565413398968 ) ) ;
#190121=CARTESIAN_POINT ( 'NONE',  ( -0.02244404828157658613, 0.6916080914694566761, -2.270927585766496559 ) ) ;
#190124=CARTESIAN_POINT ( 'NONE',  ( 1.067327838873022516, -1.996528553209110379, -0.9406146916221403975 ) ) ;
#190125=CARTESIAN_POINT ( 'NONE',  ( 3.233911077135812384, -1.516719621523674677, -1.678889276187053081 ) ) ;
#190127=CARTESIAN_POINT ( 'NONE',  ( 3.709066938097814514, 1.527391393591450486, -0.9738182928965555263 ) ) ;
#190128=CARTESIAN_POINT ( 'NONE',  ( 3.256958599878871485, 0.04175330623504669436, -1.915424027289241993 ) ) ;
#190129=CARTESIAN_POINT ( 'NONE',  ( 4.773920332862017446, -2.031068740936771366, 0.4005940302675218834 ) ) ;
#190131=CARTESIAN_POINT ( 'NONE',  ( 3.186357099593698283, -1.942036093696447363, -0.3385421596419062595 ) ) ;
#190132=CARTESIAN_POINT ( 'NONE',  ( 1.377817859240665577, 1.145177193861897758, 1.548917676831958801 ) ) ;
#190133=CARTESIAN_POINT ( 'NONE',  ( 3.502682687546424312, 1.475339254275360279, -1.149998991230333223 ) ) ;
#190136=CARTESIAN_POINT ( 'NONE',  ( 2.473609491499198398, 0.1116694970143172483, -2.305109432965181337 ) ) ;
#190137=CARTESIAN_POINT ( 'NONE',  ( 4.246440214068532448, -1.840602306905499086, -0.2743259802632999622 ) ) ;
#190142=CARTESIAN_POINT ( 'NONE',  ( 0.1179828827667589730, -2.064941173381201978, 0.4132506003948192563 ) ) ;
#190146=CARTESIAN_POINT ( 'NONE',  ( 6.714160596891073141, -1.012370167489636819, -1.909856561116265672 ) ) ;
#190147=CARTESIAN_POINT ( 'NONE',  ( 1.564851893998190135, 0.6701894319398638000, 2.011955567234039677 ) ) ;
#190148=CARTESIAN_POINT ( 'NONE',  ( 0.7912781446984231692, -0.05379174966265751895, -2.019256707098691095 ) ) ;
#190152=CARTESIAN_POINT ( 'NONE',  ( 0.9839146201040609441, 1.450980403326153301, 1.602422216231303320 ) ) ;
#190154=CARTESIAN_POINT ( 'NONE',  ( 6.925078400183531713, 7.629137130509038300, 2.555651831298339616 ) ) ;
#190157=CARTESIAN_POINT ( 'NONE',  ( 5.735564631760892595, 0.5807582108038509272, -1.931123567068816493 ) ) ;
#190162=CARTESIAN_POINT ( 'NONE',  ( 0.1634265777989383772, -2.022787333623011108, -1.013812598571243617 ) ) ;
#190166=CARTESIAN_POINT ( 'NONE',  ( 0.2806859451011362583, 1.592165405827509650, -1.064819009530016958 ) ) ;
#190170=CARTESIAN_POINT ( 'NONE',  ( 3.316762602600237475, 1.559927958434914608, 0.7363868292221543710 ) ) ;
#190173=CARTESIAN_POINT ( 'NONE',  ( 1.159032429170350653, 0.3524738178620877571, -1.734097463706934183 ) ) ;
#190174=CARTESIAN_POINT ( 'NONE',  ( 1.717441043944417878, 1.674910534618522906, 1.116504076032026616 ) ) ;
#190175=CARTESIAN_POINT ( 'NONE',  ( 6.825078400183575589, -0.005632053428735600553, 2.144262460745151255 ) ) ;
#190176=CARTESIAN_POINT ( 'NONE',  ( 4.700333112842928429, -2.206180118464650786, -0.05804534286662357823 ) ) ;
#190179=CARTESIAN_POINT ( 'NONE',  ( 4.530007735025624704, -2.079396993832134388, 0.4145621898983055109 ) ) ;
#190180=CARTESIAN_POINT ( 'NONE',  ( 3.075796161730546707, -0.8146103074460913085, 1.844718345957757188 ) ) ;
#190181=CARTESIAN_POINT ( 'NONE',  ( 3.955163173390123799, -1.573275279051716158, 0.8980309717551668847 ) ) ;
#190184=CARTESIAN_POINT ( 'NONE',  ( 1.674454752297813265, -1.775319108138155633, -0.5897529795871117031 ) ) ;
#190185=CARTESIAN_POINT ( 'NONE',  ( 6.199803715563785289, -0.6102442156579389598, 1.720816905678754782 ) ) ;
#190187=CARTESIAN_POINT ( 'NONE',  ( 2.606530347446478046, 1.805417332896454230, 0.6411187296449465389 ) ) ;
#190195=CARTESIAN_POINT ( 'NONE',  ( 3.445663904809421307, -1.957918079443463855, 0.8150281543025170716 ) ) ;
#190198=CARTESIAN_POINT ( 'NONE',  ( 4.411372364376418886, -0.3401156029278085136, 1.941656249039567905 ) ) ;
#190199=CARTESIAN_POINT ( 'NONE',  ( -0.07006079923273231258, -1.973546630392996493, 0.3967976802892440036 ) ) ;
#190201=CARTESIAN_POINT ( 'NONE',  ( 0.5271635063940235399, -1.813475876746664772, 1.092501443452270404 ) ) ;
#190202=CARTESIAN_POINT ( 'NONE',  ( 1.750525128138082254, -2.060206210462053988, -0.2049951091474821463 ) ) ;
#190206=CARTESIAN_POINT ( 'NONE',  ( 4.048837805470763662, -1.738144455908509078, -1.161405209330027555 ) ) ;
#190209=CARTESIAN_POINT ( 'NONE',  ( 0.3108108888784698598, 1.507076236086818399, -1.004716094995859121 ) ) ;
#190211=CARTESIAN_POINT ( 'NONE',  ( 5.988949835885216011, -0.3198878037087344306, -2.183464699167809275 ) ) ;
#190213=CARTESIAN_POINT ( 'NONE',  ( 4.436686946050734548, 2.163524548302516060, 0.4339203326570104102 ) ) ;
#190217=CARTESIAN_POINT ( 'NONE',  ( 3.070860992347378637, -1.446505282863861375, 1.250851760459831041 ) ) ;
#190219=CARTESIAN_POINT ( 'NONE',  ( 5.055165704564410944, 1.723227314588217318, -1.147259442322377865 ) ) ;
#190221=CARTESIAN_POINT ( 'NONE',  ( 2.465889518630470789, 2.120156730345585938, -0.4209195040108040797 ) ) ;
#190222=CARTESIAN_POINT ( 'NONE',  ( 6.058177568126345669, -1.550975213528119623, 1.548612826651605712 ) ) ;
#190223=VERTEX_POINT ( 'NONE', #83132 ) ;
#190232=CARTESIAN_POINT ( 'NONE',  ( 5.682505902380680318, 1.237739610710282046, -1.659335868388504220 ) ) ;
#190233=CARTESIAN_POINT ( 'NONE',  ( 4.107974109700462506, -1.921244671385572422, 0.1431019773510885384 ) ) ;
#190234=CARTESIAN_POINT ( 'NONE',  ( 0.5797041155359906606, -0.7231210598357665775, 1.882482590253447663 ) ) ;
#190238=EDGE_CURVE ( 'NONE', #111140, #136413, #166476, .T. ) ;
#190239=CARTESIAN_POINT ( 'NONE',  ( 0.8322822162843239724, 2.159637434087835928, 0.3711470721824081109 ) ) ;
#190240=CARTESIAN_POINT ( 'NONE',  ( 4.811078068098579408, 1.589968679568127596, 0.8971634079883784585 ) ) ;
#190247=CARTESIAN_POINT ( 'NONE',  ( 3.210337823311388394, 1.665856106666419034, 0.7845605768846477535 ) ) ;
#190248=CARTESIAN_POINT ( 'NONE',  ( 5.748296788003684377, 0.9886478197097836595, -1.753632158501418514 ) ) ;
#190249=CARTESIAN_POINT ( 'NONE',  ( 1.247910673863032116, -2.242740372501272006, -0.5020730165456227523 ) ) ;
#190250=CARTESIAN_POINT ( 'NONE',  ( 6.508651776674191147, 0.6122461511635870490, 1.863871573545019533 ) ) ;
#190254=CARTESIAN_POINT ( 'NONE',  ( 0.3091450132529197647, -1.663722454078466306, 1.232067777400827069 ) ) ;
#190256=CARTESIAN_POINT ( 'NONE',  ( 2.735971011012145127, 2.075282486531265569, 0.2531079119270570610 ) ) ;
#190257=CARTESIAN_POINT ( 'NONE',  ( 1.041631754505952134, 0.7616270086890539748, -1.708776438048253077 ) ) ;
#190258=CARTESIAN_POINT ( 'NONE',  ( 1.475935241056694602, 1.776738309990203213, 0.9528675108748105860 ) ) ;
#190262=CARTESIAN_POINT ( 'NONE',  ( 2.559766225087984903, -1.198919528351283681, 1.261881593406234403 ) ) ;
#190266=CARTESIAN_POINT ( 'NONE',  ( 2.877275982374318364, 1.637783285604855088, -0.5413683153251740432 ) ) ;
#190267=( BOUNDED_CURVE ( )  B_SPLINE_CURVE ( 3, ( #172092, #71353, #5276, #206705 ),
 .UNSPECIFIED., .F., .T. ) 
 B_SPLINE_CURVE_WITH_KNOTS ( ( 4, 4 ),
 ( 0.000000000000000000, 0.4999999999999992784 ),
 .UNSPECIFIED. ) 
 CURVE ( )  GEOMETRIC_REPRESENTATION_ITEM ( )  RATIONAL_B_SPLINE_CURVE ( ( 1.000000000000000000, 0.3333333333333343140, 0.3333333333333333703, 0.9999999999999990008 ) ) 
 REPRESENTATION_ITEM ( '' )  );
#190268=CARTESIAN_POINT ( 'NONE',  ( 3.157961424266928052, 0.9873743524775533409, 1.956624655947765357 ) ) ;
#190269=CARTESIAN_POINT ( 'NONE',  ( 5.233140740401229785, 0.1595256157847015632, 2.201181388321731269 ) ) ;
#190271=CARTESIAN_POINT ( 'NONE',  ( 2.501036472447940362, 0.4719354416190780777, 2.119019701963683833 ) ) ;
#190272=CARTESIAN_POINT ( 'NONE',  ( 1.471042373949003501, 0.1361147407585860392, -1.820667060309004937 ) ) ;
#190273=CARTESIAN_POINT ( 'NONE',  ( 3.907494643824228397, -2.025022917198250560, 0.6182885518764801303 ) ) ;
#190274=CARTESIAN_POINT ( 'NONE',  ( 6.539320575229236709, 2.970193638644866851, 2.450124720169952752 ) ) ;
#190276=CARTESIAN_POINT ( 'NONE',  ( 3.790815982946276641, 1.936215313137353178, -1.226956277148362862 ) ) ;
#190280=CARTESIAN_POINT ( 'NONE',  ( 0.04773460823432121303, -1.936894771697717621, 0.8635138731061947626 ) ) ;
#190287=CARTESIAN_POINT ( 'NONE',  ( 4.553361389630797618, -1.314998166741452090, 1.528740011303417745 ) ) ;
#190289=CARTESIAN_POINT ( 'NONE',  ( 3.309489505334945569, -1.683523595015530505, -1.191345380358753925 ) ) ;
#190293=CARTESIAN_POINT ( 'NONE',  ( 6.404242042726283834, 1.626525233829802408, -1.468802942141099299 ) ) ;
#190294=CARTESIAN_POINT ( 'NONE',  ( 3.656875104409584853, 1.122498086849915921, 1.674887873639265390 ) ) ;
#190295=CARTESIAN_POINT ( 'NONE',  ( 3.016969003575611818, -1.773741936391802332, 0.4936923545346691977 ) ) ;
#190297=CARTESIAN_POINT ( 'NONE',  ( 6.264658373536385660, -1.288822541704701452, 1.293195164663100583 ) ) ;
#190298=CARTESIAN_POINT ( 'NONE',  ( 0.2472849680876147149, 2.272430822888141133, -0.3459996173978163725 ) ) ;
#190300=CARTESIAN_POINT ( 'NONE',  ( 6.280173827431851485, -1.216757814587710929, 1.907326054681435235 ) ) ;
#190301=CARTESIAN_POINT ( 'NONE',  ( 2.174573150871310201, -1.294977634586411908, 1.660803824364719405 ) ) ;
#190310=CARTESIAN_POINT ( 'NONE',  ( 2.250376613284802207, 0.9954810856505689198, -1.872389709364124188 ) ) ;
#190311=CARTESIAN_POINT ( 'NONE',  ( 3.691809873939347675, 2.090716244852005357, -0.7509968985505171002 ) ) ;
#190312=CARTESIAN_POINT ( 'NONE',  ( 0.7268461993804631316, 0.1648446022758827123, 2.185306563462440899 ) ) ;
#190313=CARTESIAN_POINT ( 'NONE',  ( 0.2939702064862387276, 1.638257335637434364, 1.478849500172851217 ) ) ;
#190315=CARTESIAN_POINT ( 'NONE',  ( 4.685966490639408732, -1.205361723144786845, -1.547842780461285761 ) ) ;
#190324=CARTESIAN_POINT ( 'NONE',  ( 3.709332143218791789, 1.789599998243587731, -1.137392358348317201 ) ) ;
#190326=CARTESIAN_POINT ( 'NONE',  ( 5.981359018292748075, 1.999130597612966742, -0.8229454869796914984 ) ) ;
#190327=CARTESIAN_POINT ( 'NONE',  ( 3.772867777003403589, 1.732451475078290448, -0.6238847238279123797 ) ) ;
#190330=CARTESIAN_POINT ( 'NONE',  ( -0.1123202547218312558, -0.3730905450354308206, -1.705658634530213602 ) ) ;
#190331=CARTESIAN_POINT ( 'NONE',  ( 6.827182134110203471, 2.976138737189625516, 2.364467684523130497 ) ) ;
#190335=CARTESIAN_POINT ( 'NONE',  ( 4.575171270262055501, 0.003154952768896768234, -2.161883445794945846 ) ) ;
#190336=CARTESIAN_POINT ( 'NONE',  ( 5.747422657745248742, -1.966344092054626680, -0.4444320411668146731 ) ) ;
#190338=CARTESIAN_POINT ( 'NONE',  ( 3.959979445722985325, 2.145676688911036578, -0.2621329562078680842 ) ) ;
#190339=CARTESIAN_POINT ( 'NONE',  ( 3.550034410471062163, 1.971530340838826278, 0.003394978380427334484 ) ) ;
#190341=CARTESIAN_POINT ( 'NONE',  ( 1.554236647822554218, 0.6679093176565461532, -2.208796357520240949 ) ) ;
#190342=CARTESIAN_POINT ( 'NONE',  ( 3.356764223755447141, -1.562743594079138321, 1.343508228479517230 ) ) ;
#190343=CARTESIAN_POINT ( 'NONE',  ( 5.196799823744689739, 1.589972550305688070, 1.114921412299192172 ) ) ;
#190351=CARTESIAN_POINT ( 'NONE',  ( 1.940722911589174204, 2.182806717142399489, 0.3235914145361811767 ) ) ;
#190353=CARTESIAN_POINT ( 'NONE',  ( 6.315287901512626867, -1.680818388338392699, -1.011408691396285420 ) ) ;
#190354=CARTESIAN_POINT ( 'NONE',  ( -0.1291982275798807533, 2.865258409039960430, -2.562285117308207294 ) ) ;
#190359=CARTESIAN_POINT ( 'NONE',  ( 4.980324010294663317, -0.2286266671043569454, -1.826820671449409295 ) ) ;
#190361=CARTESIAN_POINT ( 'NONE',  ( 2.483339057139447803, 1.884786786457379737, -0.8339860623947179530 ) ) ;
#190364=CARTESIAN_POINT ( 'NONE',  ( 0.07680821025393774759, 7.629137130509076492, -2.410791881123967251 ) ) ;
#190368=CARTESIAN_POINT ( 'NONE',  ( 1.358354339613274675, 0.8343398477911911915, 1.884629720726511692 ) ) ;
#190370=CARTESIAN_POINT ( 'NONE',  ( 4.827609030688454261, 0.9420861819694618111, -1.581835861328761528 ) ) ;
#190375=CARTESIAN_POINT ( 'NONE',  ( 6.610000000000010090, 0.5825982378308904863, 2.053072689460200273 ) ) ;
#190377=CARTESIAN_POINT ( 'NONE',  ( 4.934293700819583073, 1.136511309699510308, -1.891595316245115788 ) ) ;
#190378=CARTESIAN_POINT ( 'NONE',  ( 0.3159878724818787066, -2.119942686789745068, 0.4214050671751194410 ) ) ;
#190380=CARTESIAN_POINT ( 'NONE',  ( 0.1231139863388103495, 1.664874722635242277, 0.9407772870168448209 ) ) ;
#190381=CARTESIAN_POINT ( 'NONE',  ( -0.06521966986864842497, -1.616690375843790051, 1.205047459138554045 ) ) ;
#190386=CARTESIAN_POINT ( 'NONE',  ( 6.111958284735683478, -0.6397702040911549259, 1.802229686255519603 ) ) ;
#190388=CARTESIAN_POINT ( 'NONE',  ( 0.6900581440293825919, -1.856003987442723657, -0.2331820809091043056 ) ) ;
#190389=CARTESIAN_POINT ( 'NONE',  ( 2.887907956677421506, -2.014008092954455265, 0.1037802451031161477 ) ) ;
#190391=CARTESIAN_POINT ( 'NONE',  ( 4.020224483524700076, -1.082363273655801095, -1.806513482918799429 ) ) ;
#190396=CARTESIAN_POINT ( 'NONE',  ( 3.638929714444568919, 1.919204589499112323, 0.6297368113697666692 ) ) ;
#190399=CARTESIAN_POINT ( 'NONE',  ( 4.499409293453607184, 1.733128992574247684, 1.291583502853070886 ) ) ;
#190406=CARTESIAN_POINT ( 'NONE',  ( 1.451894146256039519, 1.643730891105445346, 1.418569794807096107 ) ) ;
#190409=CARTESIAN_POINT ( 'NONE',  ( 0.3449248370967008537, 0.5783895242766275979, -1.748133987124582012 ) ) ;
#190411=CARTESIAN_POINT ( 'NONE',  ( 3.140350738262797314, 0.5347024899306859202, 2.125194831261326911 ) ) ;
#190412=CARTESIAN_POINT ( 'NONE',  ( 6.883263157960349155, 7.052567563008111051, 2.551962282169925711 ) ) ;
#190413=CARTESIAN_POINT ( 'NONE',  ( 4.065478255348141445, 0.2803405965145295275, -2.245028738816820635 ) ) ;
#190419=CARTESIAN_POINT ( 'NONE',  ( 4.710057611840397840, -0.7560107150014344635, -1.600242281814190148 ) ) ;
#190422=CARTESIAN_POINT ( 'NONE',  ( 0.2531349071235571846, -1.691105571228457505, 1.254881668439677966 ) ) ;
#190425=CARTESIAN_POINT ( 'NONE',  ( 0.9945129418027212065, 1.939812372797902862, 0.3400383455644633290 ) ) ;
#190427=CARTESIAN_POINT ( 'NONE',  ( 6.028922772295511656, -1.701938481575874684, 1.081082441910637071 ) ) ;
#190430=CARTESIAN_POINT ( 'NONE',  ( 4.856247981345184428, 0.7163626499266175784, 1.728251504774950709 ) ) ;
#190431=VERTEX_POINT ( 'NONE', #213684 ) ;
#190432=CARTESIAN_POINT ( 'NONE',  ( 3.995033623311712301, 0.2988084191791628985, 2.048438004591215389 ) ) ;
#190442=CARTESIAN_POINT ( 'NONE',  ( 4.211346380768822506, -1.629847038978438079, -1.091715234301626314 ) ) ;
#190443=CARTESIAN_POINT ( 'NONE',  ( 2.495470048217228065, 1.954872899240958972, 0.4925676099705801891 ) ) ;
#190448=CARTESIAN_POINT ( 'NONE',  ( 1.159204581426832803, 0.3705859133612994794, -1.833297903905316772 ) ) ;
#190450=CARTESIAN_POINT ( 'NONE',  ( 2.496342308839387680, -1.031403195114518390, 1.728778584395810114 ) ) ;
#190452=CARTESIAN_POINT ( 'NONE',  ( 3.515340291283968632, -1.955329406025432482, 0.8124583124677657864 ) ) ;
#190454=CARTESIAN_POINT ( 'NONE',  ( 4.703616579153604427, -1.598285800263723910, -1.315984976451072930 ) ) ;
#190456=CARTESIAN_POINT ( 'NONE',  ( 0.5739142741672832448, -1.158190483201524179, 1.740425096305434183 ) ) ;
#190457=CARTESIAN_POINT ( 'NONE',  ( 6.620655732516615544, 0.0004550665019913135447, 2.073887158236031425 ) ) ;
#190458=CARTESIAN_POINT ( 'NONE',  ( 5.737271026523679041, -1.649412122839075234, 0.7826820710771440481 ) ) ;
#190465=CARTESIAN_POINT ( 'NONE',  ( 6.287759715630294011, 1.828497742151834027, -0.5598019499635784602 ) ) ;
#190474=CARTESIAN_POINT ( 'NONE',  ( 5.202749988929913805, 1.864175517894875789, 0.7691070904374335271 ) ) ;
#190480=CARTESIAN_POINT ( 'NONE',  ( 1.955843269872016066, -0.6684750375501640196, 1.852638994923772930 ) ) ;
#190481=CARTESIAN_POINT ( 'NONE',  ( 2.864861414439429321, -0.1511590275467006306, -2.010826137130202529 ) ) ;
#190483=CARTESIAN_POINT ( 'NONE',  ( 6.827182134110198142, 6.033542260787205791, 2.783941933017803905 ) ) ;
#190485=CARTESIAN_POINT ( 'NONE',  ( 3.328257738700185264, 2.138080787187321086, 0.4799892483983853042 ) ) ;
#190487=CARTESIAN_POINT ( 'NONE',  ( 2.379798427543390105, 1.183398162072072823, 1.519983715915488531 ) ) ;
#190489=CARTESIAN_POINT ( 'NONE',  ( -0.1296875068448125057, 7.629137130509072939, -2.426516348560475933 ) ) ;
#190497=CARTESIAN_POINT ( 'NONE',  ( 5.601068772352080671, -0.4412860211496574814, 1.787476196608045464 ) ) ;
#190498=CARTESIAN_POINT ( 'NONE',  ( 3.193996758133522018, 1.278685386795814560, 1.554813472153792286 ) ) ;
#190499=CARTESIAN_POINT ( 'NONE',  ( 4.271116411733427043, -2.292556078035115075, 0.1642532200917065921 ) ) ;
#190500=CARTESIAN_POINT ( 'NONE',  ( -0.02919842301642854021, 4.085261895051949921, -2.628472738367752637 ) ) ;
#190501=CARTESIAN_POINT ( 'NONE',  ( 3.098338563049109151, 1.846317948315750357, 0.2325098740301386746 ) ) ;
#190505=CARTESIAN_POINT ( 'NONE',  ( 6.504189997394580480, -0.8109953713257547214, 1.730197269205424160 ) ) ;
#190508=CARTESIAN_POINT ( 'NONE',  ( 5.706606250695148042, 1.844387978369428582, 0.9845570724962575682 ) ) ;
#190514=CARTESIAN_POINT ( 'NONE',  ( 6.322847717702526182, 1.612277268089978621, 0.6135241758537502976 ) ) ;
#190516=CARTESIAN_POINT ( 'NONE',  ( 1.125167334363995852, 0.3372632679971860337, 1.700812921812058454 ) ) ;
#190520=CARTESIAN_POINT ( 'NONE',  ( 6.104372708633159839, 2.168188666507598228, 0.1146961476086311021 ) ) ;
#190521=CARTESIAN_POINT ( 'NONE',  ( 4.512205841073367196, -0.7830535718562798841, -1.649371741558727678 ) ) ;
#190522=CARTESIAN_POINT ( 'NONE',  ( 2.553501467334079678, 1.513274546892771966, 1.248348448719404535 ) ) ;
#190527=CARTESIAN_POINT ( 'NONE',  ( 3.141385665567609564, 0.05408136815227351790, 2.119969838212852675 ) ) ;
#190532=CARTESIAN_POINT ( 'NONE',  ( 1.622023338512183832, 2.040292009219225378, -0.3499636251925800079 ) ) ;
#190535=CARTESIAN_POINT ( 'NONE',  ( 3.897323497890590627, -0.2185073706607517652, -2.210542651646169698 ) ) ;
#190537=CARTESIAN_POINT ( 'NONE',  ( 2.321245813631057864, 1.080353426350823209, -2.028982405110477227 ) ) ;
#190539=CARTESIAN_POINT ( 'NONE',  ( 6.139522945012108934, 1.907909241145373525, -0.7841019685283256990 ) ) ;
#190543=CARTESIAN_POINT ( 'NONE',  ( 6.233933901472759942, 1.822226914158030286, 0.2631550708301691466 ) ) ;
#190544=CARTESIAN_POINT ( 'NONE',  ( -0.2106725631050281045, 2.870437361830021405, -2.492085498774513574 ) ) ;
#190545=CARTESIAN_POINT ( 'NONE',  ( 3.135487559415173653, -1.157359333423061409, -1.278988843622446137 ) ) ;
#190546=CARTESIAN_POINT ( 'NONE',  ( 2.413296319342159713, -1.879803466158457059, 0.7303082167480907660 ) ) ;
#190547=CARTESIAN_POINT ( 'NONE',  ( 2.690384307321362467, 1.943607183752774636, 1.227106530010623864 ) ) ;
#190548=CARTESIAN_POINT ( 'NONE',  ( 3.937032273161138463, 0.3271595461276222139, 2.238503835787652996 ) ) ;
#190549=CARTESIAN_POINT ( 'NONE',  ( 5.813134535821789406, 1.856751089961257373, 0.9939634876292826604 ) ) ;
#190551=CARTESIAN_POINT ( 'NONE',  ( 3.760817854529928894, -1.559684770762577388, -0.8363013385033011282 ) ) ;
#190553=CARTESIAN_POINT ( 'NONE',  ( 5.917577160708873407, -1.270305590232129633, -1.908037719346373784 ) ) ;
#190554=CARTESIAN_POINT ( 'NONE',  ( 5.947170714876299336, 0.5300644225827764178, -1.763184533696081857 ) ) ;
#190559=CARTESIAN_POINT ( 'NONE',  ( 5.121103774788174690, -2.081602751171758747, 0.6852947426586111224 ) ) ;
#190562=CARTESIAN_POINT ( 'NONE',  ( 5.811005889236001032, -1.634438611397070806, 1.270752202701043609 ) ) ;
#190563=CARTESIAN_POINT ( 'NONE',  ( 0.3390778084843976137, -1.706115258973059490, -1.074657883261991076 ) ) ;
#190565=CARTESIAN_POINT ( 'NONE',  ( 3.281779325460960628, 1.222525406819600757, 1.488901545882119759 ) ) ;
#190568=CARTESIAN_POINT ( 'NONE',  ( 0.2818602545999105424, 0.2096452599892709712, -2.211486639639495433 ) ) ;
#190577=CARTESIAN_POINT ( 'NONE',  ( 1.838261372102001800, -1.052240823716396267, 1.655630454418555830 ) ) ;
#190580=CARTESIAN_POINT ( 'NONE',  ( 5.810985101215744741, -1.547553103248515027, 1.205733875218002238 ) ) ;
#190582=CIRCLE ( 'NONE', #211305, 0.04999999999999969746 ) ;
#190584=CARTESIAN_POINT ( 'NONE',  ( 6.438358464623771482, 2.137424745569570295, 0.3223339197731683869 ) ) ;
#190588=CARTESIAN_POINT ( 'NONE',  ( 0.7197278698120103124, -0.9953326032119573785, -1.583558375183778288 ) ) ;
#190589=CARTESIAN_POINT ( 'NONE',  ( 5.694640849732851784, -1.102317705797692726, -1.338331167630167684 ) ) ;
#190591=CARTESIAN_POINT ( 'NONE',  ( 3.210657068901449307, 1.982179491636561819, 0.9350799695589939731 ) ) ;
#190592=CARTESIAN_POINT ( 'NONE',  ( 3.909432592967517550, 1.977442543354444249, 1.189201670975383429 ) ) ;
#190593=CARTESIAN_POINT ( 'NONE',  ( 0.1279053400650804195, -1.267571945882491447, -1.625495855733450457 ) ) ;
#190594=CARTESIAN_POINT ( 'NONE',  ( 2.326030237553232016, 1.883725225384206281, 0.4715086074991140519 ) ) ;
#190597=CARTESIAN_POINT ( 'NONE',  ( 5.590118541908202232, 1.264772504208915072, 1.701965355810124203 ) ) ;
#190599=CARTESIAN_POINT ( 'NONE',  ( 3.287732575140737801, 1.587837554856496691, -1.242726844152845178 ) ) ;
#190603=CARTESIAN_POINT ( 'NONE',  ( 1.365546509989667534, 1.798985258052044900, -0.3101867277976525505 ) ) ;
#190608=CARTESIAN_POINT ( 'NONE',  ( 5.436423068491611055, 2.030003055342466389, 0.3545201283375771228 ) ) ;
#190612=CARTESIAN_POINT ( 'NONE',  ( 4.213539248340679499, 1.623360089863118860, 1.201376956910469307 ) ) ;
#190613=CARTESIAN_POINT ( 'NONE',  ( 5.549557930969759134, -2.008940618436024117, 0.9481178722350207533 ) ) ;
#190618=CARTESIAN_POINT ( 'NONE',  ( 3.643480044026959241, -1.559369103033839465, -1.347540176210021423 ) ) ;
#190619=CARTESIAN_POINT ( 'NONE',  ( 3.973279856364997809, -1.994869694282218386, -0.2930714778977619450 ) ) ;
#190626=CARTESIAN_POINT ( 'NONE',  ( 3.444685325028495004, 1.276847194542466646, 1.560261755768836744 ) ) ;
#190627=CARTESIAN_POINT ( 'NONE',  ( 2.835703941817575569, 1.827261480098177682, 0.2250241719141123087 ) ) ;
#190628=CARTESIAN_POINT ( 'NONE',  ( 0.5577797733781300060, -1.952719008213155139, -1.229525757098411942 ) ) ;
#190630=CARTESIAN_POINT ( 'NONE',  ( 3.778741785029844369, -2.082091666206013159, -0.5805316298483630399 ) ) ;
#190636=CARTESIAN_POINT ( 'NONE',  ( 1.832664747978371533, 0.1804508633567840359, 1.861920966532565336 ) ) ;
#190637=CARTESIAN_POINT ( 'NONE',  ( 5.348493512783888626, 0.5714336785274246600, 1.886844506308351210 ) ) ;
#190641=CARTESIAN_POINT ( 'NONE',  ( 0.01274299142895937362, -0.9473294304004549193, -1.991142614049784099 ) ) ;
#190645=CARTESIAN_POINT ( 'NONE',  ( 6.539320575229278454, 3.689604457162498630, 2.617406275049142916 ) ) ;
#190646=CARTESIAN_POINT ( 'NONE',  ( 5.787953125587765868, -0.8870788200928159117, 1.760698262704742723 ) ) ;
#190647=CARTESIAN_POINT ( 'NONE',  ( 5.198025161738785371, -0.8347013672818380803, 2.151627338387426036 ) ) ;
#190648=CARTESIAN_POINT ( 'NONE',  ( 5.986726177563552298, 1.793701560725208699, 0.4957798874403050449 ) ) ;
#190649=CARTESIAN_POINT ( 'NONE',  ( 2.694246160070143503, 0.9763755106866910394, -1.816870488346455037 ) ) ;
#190656=CARTESIAN_POINT ( 'NONE',  ( 4.967309339809048652, 1.886637975807739176, 1.074439269227177363 ) ) ;
#190659=CARTESIAN_POINT ( 'NONE',  ( 4.493604616018744835, -1.840970053361364656, -0.04044509776383875543 ) ) ;
#190662=CARTESIAN_POINT ( 'NONE',  ( 6.374583145400191775, -0.1054333438532777389, -2.189162923280890904 ) ) ;
#190664=CARTESIAN_POINT ( 'NONE',  ( 0.9314073880264511773, 0.1673361042086803641, 2.256242939573564144 ) ) ;
#190670=CARTESIAN_POINT ( 'NONE',  ( 0.3382653665467276749, 0.2958422019357190291, 1.744775138515190616 ) ) ;
#190672=CARTESIAN_POINT ( 'NONE',  ( 5.215494488825547670, 1.647103507230001096, 1.157162265453457239 ) ) ;
#190674=CARTESIAN_POINT ( 'NONE',  ( 4.278421442896533478, -1.214510211351152336, 1.720268157014235078 ) ) ;
#190676=CARTESIAN_POINT ( 'NONE',  ( 2.952642602588346321, -1.771063984568725935, -0.7304820402930515266 ) ) ;
#190678=CARTESIAN_POINT ( 'NONE',  ( -0.02244404828160087226, 1.995160441984781041, -2.602654351998904492 ) ) ;
#190679=CARTESIAN_POINT ( 'NONE',  ( 4.158625497742932886, -0.6157697831138170264, -1.870904811771924470 ) ) ;
#190680=CARTESIAN_POINT ( 'NONE',  ( 5.941667304196568189, -1.900381328601069342, 0.6844855596733252501 ) ) ;
#190681=CARTESIAN_POINT ( 'NONE',  ( 2.272138710904994863, -1.152746988206950096, 1.473173409640892162 ) ) ;
#190682=CARTESIAN_POINT ( 'NONE',  ( 5.021954727502539129, -0.9268850835505036967, -1.454474922752227339 ) ) ;
#190683=CARTESIAN_POINT ( 'NONE',  ( 1.353610510645312237, -1.387278792934818705, -1.316581319992945920 ) ) ;
#190685=CARTESIAN_POINT ( 'NONE',  ( 1.911028901235469313, 1.633884665098099598, -1.483674895440662667 ) ) ;
#190688=CARTESIAN_POINT ( 'NONE',  ( 6.478960399985357554, 1.830089090633261417, 0.7073212282268787066 ) ) ;
#190695=CARTESIAN_POINT ( 'NONE',  ( 1.996617168637443429, 2.047528291220417351, 0.3059219562495316125 ) ) ;
#190699=CARTESIAN_POINT ( 'NONE',  ( 6.393239817247728496, -0.1034752114322245314, -2.118097640427937911 ) ) ;
#190704=CARTESIAN_POINT ( 'NONE',  ( 5.395861176733054876, 0.1455124041884261754, 2.010896217931843921 ) ) ;
#190706=CARTESIAN_POINT ( 'NONE',  ( 5.331221607142452967, -1.514317160175217447, -1.173313937468897672 ) ) ;
#190707=CARTESIAN_POINT ( 'NONE',  ( 6.639320575229283428, 0.5834889568891787892, 2.056715522164854981 ) ) ;
#190708=CARTESIAN_POINT ( 'NONE',  ( 3.175498511859841333, 1.392037702009111033, 1.692654053968026151 ) ) ;
#190711=CARTESIAN_POINT ( 'NONE',  ( 5.783453021694040963, 0.1439598661895292731, -2.008088619348106896 ) ) ;
#190712=CARTESIAN_POINT ( 'NONE',  ( 1.388764059443419407, -1.816923020173771830, -0.5969786173363604842 ) ) ;
#190715=CARTESIAN_POINT ( 'NONE',  ( 6.503513627744350600, -2.053693679520858684, 0.5143327402655095693 ) ) ;
#190717=CARTESIAN_POINT ( 'NONE',  ( 3.403930425450612418, -0.8493818440679711257, -1.910634358282743417 ) ) ;
#190719=CARTESIAN_POINT ( 'NONE',  ( 1.957592155046536941, 1.720466030779904454, -0.1226356519287794405 ) ) ;
#190720=EDGE_LOOP ( 'NONE', ( #46916, #119594, #87515, #89911 ) ) ;
#190729=CARTESIAN_POINT ( 'NONE',  ( 3.316878987808123735, 1.426168316962544091, -1.116757653536442740 ) ) ;
#190733=CARTESIAN_POINT ( 'NONE',  ( 3.475094438140493125, -1.599078698050887981, -0.8510578468755282122 ) ) ;
#190734=CARTESIAN_POINT ( 'NONE',  ( 6.539320575229215393, 2.445213257098968640, 2.379920919941742152 ) ) ;
#190737=CARTESIAN_POINT ( 'NONE',  ( 3.806960202730264253, -1.522499362102507359, 1.069998817686746984 ) ) ;
#190739=CARTESIAN_POINT ( 'NONE',  ( 1.810024464468898309, 1.101340386757416967, -1.567151550741460397 ) ) ;
#190740=CARTESIAN_POINT ( 'NONE',  ( 1.289775909805501719, -0.8246113042270180049, 1.628811597173693393 ) ) ;
#190749=CARTESIAN_POINT ( 'NONE',  ( 5.366046204681790499, -1.960318410495393238, 0.1889891646899461708 ) ) ;
#190753=CARTESIAN_POINT ( 'NONE',  ( 6.597619724345276104, -2.191060131252516641, 0.04951108399064289151 ) ) ;
#190754=CARTESIAN_POINT ( 'NONE',  ( 6.141620278036529434, -1.395723430145169752, -1.327979989909616521 ) ) ;
#190756=CARTESIAN_POINT ( 'NONE',  ( 1.254616015376356586, -1.441780481750528420, 1.119729341354458452 ) ) ;
#190757=CARTESIAN_POINT ( 'NONE',  ( 2.455956380646412196, 0.5873987694336445520, -2.127207350628975924 ) ) ;
#190759=CARTESIAN_POINT ( 'NONE',  ( 1.371198541116287917, -1.641758494746584418, -0.9804709962101465504 ) ) ;
#190760=CARTESIAN_POINT ( 'NONE',  ( 0.2562226757886588713, -1.969045882358761101, -0.05199970915584737480 ) ) ;
#190761=CARTESIAN_POINT ( 'NONE',  ( 2.261185778363482779, 1.904153404235246594, -0.3810316102009890238 ) ) ;
#190765=CARTESIAN_POINT ( 'NONE',  ( 6.789920448004552078, -1.215336557376142101, -1.409407482083424590 ) ) ;
#190771=CARTESIAN_POINT ( 'NONE',  ( 2.841561854484982774, 0.7863008361240211297, -2.045831095052422555 ) ) ;
#190775=CARTESIAN_POINT ( 'NONE',  ( 2.842213963582499670, 1.811911227886909614, 0.2232855069103783507 ) ) ;
#190779=CARTESIAN_POINT ( 'NONE',  ( 6.925078400183548588, 0.0006614011395407459748, 1.855452278108092656 ) ) ;
#190781=CARTESIAN_POINT ( 'NONE',  ( 0.5746741651161955122, -1.813631458699631160, -0.6500969746191431753 ) ) ;
#190782=CARTESIAN_POINT ( 'NONE',  ( 5.383633123045536983, -1.864019207510819953, 0.6117972396969258986 ) ) ;
#190787=CARTESIAN_POINT ( 'NONE',  ( 5.126606437771586755, 0.1607948393855564151, 2.185736094377451089 ) ) ;
#190791=CARTESIAN_POINT ( 'NONE',  ( 5.594608825991118195, 2.038665915018455177, 0.3594684214384344378 ) ) ;
#190795=CARTESIAN_POINT ( 'NONE',  ( 4.729243902325204196, 2.292384926013335988, 0.1706581203582517303 ) ) ;
#190799=CARTESIAN_POINT ( 'NONE',  ( 0.3051332635122120385, 1.997493689478089252, 1.124391992203729540 ) ) ;
#190801=CARTESIAN_POINT ( 'NONE',  ( 4.857337426984369877, 1.920559571908975194, -0.2866867867914507650 ) ) ;
#190805=CARTESIAN_POINT ( 'NONE',  ( 5.097880177178074845, 1.288836597028759634, 1.412999258680311510 ) ) ;
#190806=CARTESIAN_POINT ( 'NONE',  ( 6.440463960111763697, 1.706863596762456581, 0.2470990609701722573 ) ) ;
#190807=CARTESIAN_POINT ( 'NONE',  ( 6.016814611094169152, 0.2024578496369993375, 2.006372135924570088 ) ) ;
#190811=CARTESIAN_POINT ( 'NONE',  ( 1.798888674052185888, 1.738860765912113138, 1.160333176109765274 ) ) ;
#190812=CARTESIAN_POINT ( 'NONE',  ( 0.6371259318241145886, -1.247223858821765230, -1.255979444004810430 ) ) ;
#190813=CARTESIAN_POINT ( 'NONE',  ( 6.311172677262812059, 1.158691452862798954, -1.650079838712660063 ) ) ;
#190815=CARTESIAN_POINT ( 'NONE',  ( 2.765910322896072859, 1.227222833649963540, 1.935908780871216761 ) ) ;
#190816=CARTESIAN_POINT ( 'NONE',  ( 2.396107360292961008, 1.398095582919863133, -1.036136137726038520 ) ) ;
#190817=CARTESIAN_POINT ( 'NONE',  ( 3.146849984228027974, 2.069795010335002239, 0.4607391970517027979 ) ) ;
#190819=CARTESIAN_POINT ( 'NONE',  ( 1.844673738135360175, -0.9321790797625574276, 1.461707330738234667 ) ) ;
#190821=CARTESIAN_POINT ( 'NONE',  ( 1.539268068193447858, 1.721329529071988107, -0.7080023387807417024 ) ) ;
#190822=CARTESIAN_POINT ( 'NONE',  ( 2.524086392267041568, 2.129678358216775536, -0.4216712753718852014 ) ) ;
#190823=CARTESIAN_POINT ( 'NONE',  ( 3.608611488583326032, 1.916353073142588403, 0.6279913346786819561 ) ) ;
#190824=CARTESIAN_POINT ( 'NONE',  ( 4.093750000000002665, -1.895863743164171611, -0.7852924748297696045 ) ) ;
#190828=CARTESIAN_POINT ( 'NONE',  ( 1.412975430660408538, 1.697568229685364249, 0.9106500277177332903 ) ) ;
#190830=CARTESIAN_POINT ( 'NONE',  ( 3.533611464748823927, -0.1604399991079318022, 2.215644447872004985 ) ) ;
#190836=CARTESIAN_POINT ( 'NONE',  ( 5.695613681701293451, 2.052597959444299125, -0.8498680618601384129 ) ) ;
#190837=CARTESIAN_POINT ( 'NONE',  ( 4.527759979645433752, 1.903474890065796732, -0.4746247275292309609 ) ) ;
#190841=CARTESIAN_POINT ( 'NONE',  ( 6.151720675889260193, 0.6653518678880927517, -2.162357237652327679 ) ) ;
#190843=CARTESIAN_POINT ( 'NONE',  ( 1.820832581213110313, -1.460207654653251419, 1.457104742506893036 ) ) ;
#190849=CARTESIAN_POINT ( 'NONE',  ( 3.549935554046261821, 1.870726058081632504, 0.003126486288931861444 ) ) ;
#190850=CARTESIAN_POINT ( 'NONE',  ( 2.865509578329272777, -0.1299577181766899403, -1.729349861900606022 ) ) ;
#190851=CARTESIAN_POINT ( 'NONE',  ( 6.409741707328596938, -1.031184584194230647, -1.933826218581576439 ) ) ;
#190852=CARTESIAN_POINT ( 'NONE',  ( 0.5697015142280477118, 0.2141057807664332180, -2.196374807094509496 ) ) ;
#190853=CARTESIAN_POINT ( 'NONE',  ( 4.704676425016507402, 1.819892833079386651, 1.028999879293402531 ) ) ;
#190854=CARTESIAN_POINT ( 'NONE',  ( 5.630791504788829727, -1.754662785997921359, 0.8323459256341717571 ) ) ;
#190857=CARTESIAN_POINT ( 'NONE',  ( 0.0006249722829775038483, -1.976948959267275541, 0.3961041280396286890 ) ) ;
#190864=CARTESIAN_POINT ( 'NONE',  ( 4.002439121739418404, -0.5745171773131328985, -1.733004836422600725 ) ) ;
#190865=CARTESIAN_POINT ( 'NONE',  ( 2.643839551151895506, -1.634601560588926361, -1.482707865360691990 ) ) ;
#190870=CARTESIAN_POINT ( 'NONE',  ( 1.353777543752776591, -1.465856132443652760, -1.389804628120022478 ) ) ;
#190873=CARTESIAN_POINT ( 'NONE',  ( 2.887382943596613849, -1.738241981009930992, 0.6650857031204291392 ) ) ;
#190880=CARTESIAN_POINT ( 'NONE',  ( 4.336427269025699971, 1.790907886515300085, 0.3537760332646966432 ) ) ;
#190884=CARTESIAN_POINT ( 'NONE',  ( 0.7722569432341424012, -1.726285329646786382, 0.1615719764154876226 ) ) ;
#190885=CARTESIAN_POINT ( 'NONE',  ( 6.158133876658566486, -1.298579738958350660, 1.305440813956220136 ) ) ;
#190886=CARTESIAN_POINT ( 'NONE',  ( 4.934332944283116973, 1.189700906406887082, -1.977258547338469841 ) ) ;
#190888=CARTESIAN_POINT ( 'NONE',  ( 6.555963963954187790, 2.156316573842661732, -0.1517529999496904924 ) ) ;
#190891=CARTESIAN_POINT ( 'NONE',  ( 5.519047587058080850, 2.296088720628499669, -0.1051655125834053545 ) ) ;
#190895=CARTESIAN_POINT ( 'NONE',  ( 5.330866702616011921, 0.1386157390740362649, 1.865562100978317206 ) ) ;
#190897=CARTESIAN_POINT ( 'NONE',  ( 2.390748813209525814, -1.831196095803063528, -0.5514187292172747501 ) ) ;
#190899=CARTESIAN_POINT ( 'NONE',  ( 3.457846583235091753, 0.5364296187198510646, -2.140574738106671759 ) ) ;
#190900=CARTESIAN_POINT ( 'NONE',  ( 4.680926624126137803, 1.758507693093620539, -1.179036559061322542 ) ) ;
#190902=CARTESIAN_POINT ( 'NONE',  ( 6.883263157960393563, 1.268976584491373183, 2.060807272249213451 ) ) ;
#190903=CARTESIAN_POINT ( 'NONE',  ( -0.2110808730067300354, 7.629137130509040077, -2.397154524934116182 ) ) ;
#190906=CARTESIAN_POINT ( 'NONE',  ( 2.556097155687846900, 0.6156694008866661072, -2.223864192518353544 ) ) ;
#190907=CARTESIAN_POINT ( 'NONE',  ( 2.699599903323801620, -1.451799986561516764, -1.319707477925702310 ) ) ;
#190909=CARTESIAN_POINT ( 'NONE',  ( 6.596538677256176264, 2.039275035945103731, 0.3085339683557372092 ) ) ;
#190913=CARTESIAN_POINT ( 'NONE',  ( 4.680875185974167074, 1.673856063443099895, -1.124242729735332347 ) ) ;
#190918=CARTESIAN_POINT ( 'NONE',  ( 2.254941745292405653, -0.5755891407489240885, -2.093346358694737841 ) ) ;
#190922=CARTESIAN_POINT ( 'NONE',  ( 2.090876104454452378, 1.629797177321444579, -0.9178172146045021629 ) ) ;
#190923=CARTESIAN_POINT ( 'NONE',  ( 0.3333698182165916735, -1.885181130612986866, 0.8328085122516776240 ) ) ;
#190928=CARTESIAN_POINT ( 'NONE',  ( 3.879479457080482696, 0.2311173251203814394, -1.898182577502210977 ) ) ;
#190930=CARTESIAN_POINT ( 'NONE',  ( 4.733122822409558950, -1.617543599503493468, 0.7186682867280795861 ) ) ;
#190931=CARTESIAN_POINT ( 'NONE',  ( 1.523922206041250949, -1.897707704667614959, 0.2351830868887184178 ) ) ;
#190933=CARTESIAN_POINT ( 'NONE',  ( 0.04005665835727333091, 0.7356861536649759170, 1.769027722964914728 ) ) ;
#190935=CARTESIAN_POINT ( 'NONE',  ( 1.082579992370054311, 1.234693400583252609, -1.661741702728709802 ) ) ;
#190937=CARTESIAN_POINT ( 'NONE',  ( 5.910993886665249164, 1.650546521282238110, 0.8803886038859505270 ) ) ;
#190938=CARTESIAN_POINT ( 'NONE',  ( 2.033574986395149775, -1.191784744093337123, -1.383114941912518159 ) ) ;
#190939=CARTESIAN_POINT ( 'NONE',  ( 5.742855475442601332, 0.4270144693867898300, 2.165010647329483895 ) ) ;
#190942=CARTESIAN_POINT ( 'NONE',  ( 2.664570663672768180, -0.7871131050594852852, -1.906781320289064885 ) ) ;
#190948=CARTESIAN_POINT ( 'NONE',  ( 5.670397268163976712, -0.9275489576153757021, -1.851018422006404096 ) ) ;
#190950=CARTESIAN_POINT ( 'NONE',  ( 2.302237272444170202, -2.161155982280529297, 0.05054500047013688047 ) ) ;
#190952=CARTESIAN_POINT ( 'NONE',  ( 3.176430186773027575, 0.9099569689122315452, 1.803159259486881938 ) ) ;
#190953=CARTESIAN_POINT ( 'NONE',  ( 2.119516022818414669, 0.3384452847540948550, -1.932298432780136244 ) ) ;
#190958=CARTESIAN_POINT ( 'NONE',  ( 1.727750297885573882, 0.7672897036171549834, -1.865047645237365215 ) ) ;
#190960=CARTESIAN_POINT ( 'NONE',  ( 5.583573808894983337, -0.9862700065477579825, 1.957137920222583372 ) ) ;
#190962=CARTESIAN_POINT ( 'NONE',  ( 5.836178160628028522, -1.067892152678026951, -1.586260290404594597 ) ) ;
#190966=CARTESIAN_POINT ( 'NONE',  ( 3.691029940746898053, 1.730877988113326493, 1.034147909374658392 ) ) ;
#190969=CARTESIAN_POINT ( 'NONE',  ( 4.946200454639571475, 1.720373684868029329, 0.1241775145462056112 ) ) ;
#190973=CARTESIAN_POINT ( 'NONE',  ( 4.639837347815604751, 0.8015432297804045980, -1.690266223530467293 ) ) ;
#190975=CARTESIAN_POINT ( 'NONE',  ( 0.9189038144036645317, -1.502058968113138437, 1.424965263859011122 ) ) ;
#190981=CARTESIAN_POINT ( 'NONE',  ( 0.01720424586787797083, -1.842442205116225695, 0.8197940039925479816 ) ) ;
#190982=CARTESIAN_POINT ( 'NONE',  ( 0.6151243592659773052, 1.481389731780102137, 1.042453732408530342 ) ) ;
#190987=CARTESIAN_POINT ( 'NONE',  ( 6.830517471914854255, -1.143533572366756124, 1.468690548319721900 ) ) ;
#190989=CARTESIAN_POINT ( 'NONE',  ( 5.308173953863717820, 1.137349973717050267, -1.541276042019421810 ) ) ;
#190996=CARTESIAN_POINT ( 'NONE',  ( 3.081113354808207916, -0.1575343947536785305, -2.156009052512488200 ) ) ;
#190999=CARTESIAN_POINT ( 'NONE',  ( 0.07077104593807002908, 0.8175350930016941353, 1.956879683024402183 ) ) ;
#191000=CARTESIAN_POINT ( 'NONE',  ( 4.295794115256676982, -0.6985059363485807138, 1.686860163339451768 ) ) ;
#191002=CARTESIAN_POINT ( 'NONE',  ( 1.194530107633525517, -0.4747795734156860514, -1.913232634659914444 ) ) ;
#191003=CARTESIAN_POINT ( 'NONE',  ( 3.726736447152957599, 1.348887845406310682, -1.355897031963343213 ) ) ;
#191006=CARTESIAN_POINT ( 'NONE',  ( 5.318794011649015552, -1.427836685786993742, 1.356881127696080158 ) ) ;
#191008=CARTESIAN_POINT ( 'NONE',  ( 6.163619218806376310, 1.002299704222510357, 1.663313343435903091 ) ) ;
#191012=CARTESIAN_POINT ( 'NONE',  ( 6.486587849989844834, -1.303813291173651301, 1.673118453357678392 ) ) ;
#191015=CARTESIAN_POINT ( 'NONE',  ( 3.492734469894549942, -1.843672829398453228, -0.5074192597756199685 ) ) ;
#191017=CARTESIAN_POINT ( 'NONE',  ( 0.1830476545506658226, -2.141193618969746471, -0.5335393285625378290 ) ) ;
#191020=CARTESIAN_POINT ( 'NONE',  ( 4.688143804000614701, 1.160868117455503556, 1.644480612105477579 ) ) ;
#191022=CARTESIAN_POINT ( 'NONE',  ( 6.428339884752386268, 1.046657586246093175, -1.495688092090130095 ) ) ;
#191023=CARTESIAN_POINT ( 'NONE',  ( 5.559779856078610472, 1.205038519190555268, 1.616695979245158066 ) ) ;
#191024=CARTESIAN_POINT ( 'NONE',  ( 6.727182134110196721, 2.084960209934753284, 2.120171393779949565 ) ) ;
#191025=CARTESIAN_POINT ( 'NONE',  ( 1.961466609329724164, 1.720096886549182136, 1.151944459977225055 ) ) ;
#191029=CARTESIAN_POINT ( 'NONE',  ( 6.596569749568344854, -0.5012203084251048990, -1.802199723311518786 ) ) ;
#191035=CARTESIAN_POINT ( 'NONE',  ( 6.925078400183553029, 7.053346220238264408, 2.353806654540433030 ) ) ;
#191037=CARTESIAN_POINT ( 'NONE',  ( 4.658689525625823613, 1.003974855541647004, 1.413729434382102079 ) ) ;
#191041=CARTESIAN_POINT ( 'NONE',  ( 2.676698048161993082, 1.355622082481915847, -1.564734663558226879 ) ) ;
#191042=CARTESIAN_POINT ( 'NONE',  ( 3.954788147838703249, -1.976257328041197470, -0.7601183944087180899 ) ) ;
#191045=CARTESIAN_POINT ( 'NONE',  ( 1.903111606826495938, -1.666530434877494304, 1.049136497343281738 ) ) ;
#191049=CARTESIAN_POINT ( 'NONE',  ( 3.978722188455630082, -0.2232912938500397904, -2.281366727860510313 ) ) ;
#191050=CARTESIAN_POINT ( 'NONE',  ( 2.121465551170404140, -1.771062468586531047, 0.4427346646293239818 ) ) ;
#191054=CARTESIAN_POINT ( 'NONE',  ( 3.129155277828885140, 1.821763076032786977, 0.8570700399232934474 ) ) ;
#191055=CARTESIAN_POINT ( 'NONE',  ( 2.465611527742004760, -0.4346729355233553416, 1.912824223707191296 ) ) ;
#191058=CARTESIAN_POINT ( 'NONE',  ( 0.07516593201273635838, 0.7223771927552320449, -2.128525933252373381 ) ) ;
#191059=CARTESIAN_POINT ( 'NONE',  ( 4.488279598995706721, -0.4578276946864130448, -2.039718000080573912 ) ) ;
#191060=CARTESIAN_POINT ( 'NONE',  ( 3.397073482672040345, 1.394525624090914961, 1.089649698571172776 ) ) ;
#191062=CARTESIAN_POINT ( 'NONE',  ( 6.193372188798685229, -0.7780443601670664622, 2.156323934359334338 ) ) ;
#191063=CARTESIAN_POINT ( 'NONE',  ( 5.296709758707953242, 1.425846067417353868, 0.9975513609157842243 ) ) ;
#191066=CARTESIAN_POINT ( 'NONE',  ( 5.889324137892314681, -0.8237033142024595689, -2.146187584169775953 ) ) ;
#191068=CARTESIAN_POINT ( 'NONE',  ( 5.518767629808705166, 1.731759826824400106, -0.08707812323833011292 ) ) ;
#191069=CARTESIAN_POINT ( 'NONE',  ( 5.582552312218076018, 1.297699880476494094, -1.740541793301546347 ) ) ;
#191071=CARTESIAN_POINT ( 'NONE',  ( -0.01227199510028028316, -0.5578357038005901103, 2.042509832261687475 ) ) ;
#191072=CARTESIAN_POINT ( 'NONE',  ( 6.093750000000004441, -1.895863743164213355, -0.7852924748296624680 ) ) ;
#191074=CARTESIAN_POINT ( 'NONE',  ( 3.891558735110557610, 1.394649387769153259, 1.329109640543422399 ) ) ;
#191076=CARTESIAN_POINT ( 'NONE',  ( -0.02240927558793281635, -1.987202795932199839, -0.9927825048469391955 ) ) ;
#191081=CARTESIAN_POINT ( 'NONE',  ( 2.543850053281167423, -2.071606161961367043, 0.8020612402455605805 ) ) ;
#191086=CARTESIAN_POINT ( 'NONE',  ( 0.3170300144729014669, 1.034162889623980286, -1.730867746391979933 ) ) ;
#191088=CARTESIAN_POINT ( 'NONE',  ( 5.564908101581790945, 1.564332607353050131, -1.344557729249852729 ) ) ;
#191093=CARTESIAN_POINT ( 'NONE',  ( 1.106321208856683613, 1.344927736385517658, -1.150416400790694960 ) ) ;
#191094=CARTESIAN_POINT ( 'NONE',  ( -0.05211191391743182078, -1.802403943428915412, -0.9041556775107384425 ) ) ;
#191095=CARTESIAN_POINT ( 'NONE',  ( 5.759256982813394821, 1.713166593665109705, -0.3060214249656545982 ) ) ;
#191097=CARTESIAN_POINT ( 'NONE',  ( 3.667766089696015364, 1.274287168460963127, 1.905377313346041435 ) ) ;
#191099=CARTESIAN_POINT ( 'NONE',  ( 1.798526679444776954, 1.530131497970032450, 1.023642133485637595 ) ) ;
#191102=CARTESIAN_POINT ( 'NONE',  ( 3.522295995157864290, 1.158834602800838498, -1.410599190884161969 ) ) ;
#191103=CARTESIAN_POINT ( 'NONE',  ( 4.184220324914634581, 1.621181886760931778, 1.198861198883696799 ) ) ;
#191105=CARTESIAN_POINT ( 'NONE',  ( 2.606633135955916725, -0.8653751708443763180, -2.090666874703292599 ) ) ;
#191107=CARTESIAN_POINT ( 'NONE',  ( 5.122148429244435697, -1.124054950784241891, -1.780691527792167994 ) ) ;
#191110=CARTESIAN_POINT ( 'NONE',  ( 2.523957353938070192, 2.030885678308389952, -0.4015143504868187718 ) ) ;
#191113=CARTESIAN_POINT ( 'NONE',  ( 5.039744756118590630, -2.013340025477545758, 0.6656774797743277849 ) ) ;
#191115=CARTESIAN_POINT ( 'NONE',  ( 0.4867822013649549251, -0.2347038428511475372, -1.912094274373641323 ) ) ;
#191121=CARTESIAN_POINT ( 'NONE',  ( 6.099870585610251084, 1.463495690422533579, 1.534846084132005961 ) ) ;
#191122=CARTESIAN_POINT ( 'NONE',  ( 1.764816150188710298, -1.489710805432680418, 1.488830988054674620 ) ) ;
#191125=CARTESIAN_POINT ( 'NONE',  ( 6.631710597105570315, 1.780986809720253694, -0.5397248755362458184 ) ) ;
#191131=CARTESIAN_POINT ( 'NONE',  ( 0.1938080739139167730, 1.976361990896974508, -0.7691651810952588875 ) ) ;
#191134=CARTESIAN_POINT ( 'NONE',  ( 3.490630252122446375, 1.913478943654752129, 0.4322817992908413176 ) ) ;
#191135=CARTESIAN_POINT ( 'NONE',  ( 0.9015118058452382677, 1.767791302423503685, 1.243857928393626633 ) ) ;
#191140=CARTESIAN_POINT ( 'NONE',  ( 2.800428594868603405, 1.470281860783069439, 0.9307988129052218174 ) ) ;
#191144=CARTESIAN_POINT ( 'NONE',  ( 2.196638537759632470, -1.314794530490107638, -1.528507974810841219 ) ) ;
#191147=CARTESIAN_POINT ( 'NONE',  ( 2.659003877371171942, -1.714407010456520108, -0.9732827283935908680 ) ) ;
#191148=CARTESIAN_POINT ( 'NONE',  ( 5.853752780977106163, -1.389761788226477002, -1.313969904969368496 ) ) ;
#191155=CARTESIAN_POINT ( 'NONE',  ( 1.664719335976164283, 0.6358223015159381042, 1.917034779120100341 ) ) ;
#191157=CARTESIAN_POINT ( 'NONE',  ( 5.983493387795983054, 2.135156284703492169, -0.8757408730279289122 ) ) ;
#191158=CARTESIAN_POINT ( 'NONE',  ( 6.514115657861259123, 1.956686900881845714, -0.1430618042221123987 ) ) ;
#191159=CARTESIAN_POINT ( 'NONE',  ( 2.887496479553632422, -1.832211488775811414, 0.7015765724691159777 ) ) ;
#191161=CARTESIAN_POINT ( 'NONE',  ( 0.2994542103806375755, 1.388483683912977495, -1.462447666687356485 ) ) ;
#191163=CARTESIAN_POINT ( 'NONE',  ( 0.8138397394129359697, -1.348031465540124207, -1.632742428372506049 ) ) ;
#191166=CARTESIAN_POINT ( 'NONE',  ( 1.710644026344819046, -0.2265308078298749472, 1.827073587482845207 ) ) ;
#191169=CARTESIAN_POINT ( 'NONE',  ( 2.953504815971871977, -1.868289524550557523, 1.003269902519101864 ) ) ;
#191173=CARTESIAN_POINT ( 'NONE',  ( 3.796211532432732572, -2.058264701994051649, -0.1047273801592675524 ) ) ;
#191175=CARTESIAN_POINT ( 'NONE',  ( 0.9426144736941791669, -1.451487892885485742, -1.132780452900377099 ) ) ;
#191179=CARTESIAN_POINT ( 'NONE',  ( 1.243116305521356990, 0.4334984505205765060, 2.163720904216937857 ) ) ;
#191180=CARTESIAN_POINT ( 'NONE',  ( 3.058202344463755828, 2.251794067479270911, -0.2186341555679652271 ) ) ;
#191182=CARTESIAN_POINT ( 'NONE',  ( 2.531291980686082521, -0.1736719688998221156, 1.803202784768900502 ) ) ;
#191184=CARTESIAN_POINT ( 'NONE',  ( 3.467908617337426502, -0.9394263201649171169, 1.669454279737823343 ) ) ;
#191185=CARTESIAN_POINT ( 'NONE',  ( 4.475093801846619535, 1.891600172242546840, 0.8420093967692193759 ) ) ;
#191187=CARTESIAN_POINT ( 'NONE',  ( 2.254701366666445939, -1.525215070022269082, 1.249173565255176976 ) ) ;
#191188=CARTESIAN_POINT ( 'NONE',  ( 0.07700591528353968596, 0.003617085621422307627, -1.910863332519038282 ) ) ;
#191189=CARTESIAN_POINT ( 'NONE',  ( 3.713615009860570915, -1.843089489661839053, 0.3189824552965599969 ) ) ;
#191190=CARTESIAN_POINT ( 'NONE',  ( 1.788135723919834774, 1.593634496655076171, 1.669289477041531633 ) ) ;
#191192=CARTESIAN_POINT ( 'NONE',  ( 3.420197418661593769, 0.8345380353566893561, 1.663503485505882118 ) ) ;
#191198=CARTESIAN_POINT ( 'NONE',  ( 1.155059408868217119, -1.659095468083382041, 1.297160957089478206 ) ) ;
#191202=CARTESIAN_POINT ( 'NONE',  ( 6.643834073375672666, 0.8340821395082242962, -1.994398315854857495 ) ) ;
#191203=CARTESIAN_POINT ( 'NONE',  ( 2.654661980655496301, 2.105093816413053709, 0.2552270188876659129 ) ) ;
#191204=CARTESIAN_POINT ( 'NONE',  ( -0.1755239516839811886, -0.8679694584908944632, -1.822324207963136988 ) ) ;
#191208=CARTESIAN_POINT ( 'NONE',  ( 0.8608787451157871029, -1.566265403972837866, 1.489986575276234460 ) ) ;
#191214=CARTESIAN_POINT ( 'NONE',  ( 4.628138809701114020, 2.011451458044950069, 0.1435230606586651581 ) ) ;
#191217=CARTESIAN_POINT ( 'NONE',  ( 6.368072262247213899, 1.106822706796772193, 1.856716078747308263 ) ) ;
#191221=CARTESIAN_POINT ( 'NONE',  ( 0.2455189486357247652, 1.894654674652377135, -0.2817335493821241932 ) ) ;
#191223=CARTESIAN_POINT ( 'NONE',  ( 6.883263157960364254, 2.038911835798001171, 2.358809022084580764 ) ) ;
#191226=CARTESIAN_POINT ( 'NONE',  ( 3.176078081051143531, -1.026819631599368066, 1.385778701376034316 ) ) ;
#191230=CARTESIAN_POINT ( 'NONE',  ( 1.387592303909779279, -0.8018289002829273038, 1.577768680615166952 ) ) ;
#191231=CARTESIAN_POINT ( 'NONE',  ( 1.928386798537110147, -0.9510432213125822321, -1.774292727131807856 ) ) ;
#191233=CARTESIAN_POINT ( 'NONE',  ( 4.208205882762393379, -2.201082536721191474, 0.1591639695062776749 ) ) ;
#191237=CARTESIAN_POINT ( 'NONE',  ( 3.668700845920089826, 0.7647225481513253431, 1.977962425194310203 ) ) ;
#191238=CARTESIAN_POINT ( 'NONE',  ( 3.444935562074178392, -1.779636981393231565, -0.9480232565319337557 ) ) ;
#191239=CARTESIAN_POINT ( 'NONE',  ( 3.884856352912366972, -1.692463592844297704, -0.6465920371584426007 ) ) ;
#191242=ORIENTED_EDGE ( 'NONE', *, *, #79408, .F. ) ;
#191243=CARTESIAN_POINT ( 'NONE',  ( 0.1099206271272800961, -0.7955684105149689600, -1.691499381818922343 ) ) ;
#191244=CARTESIAN_POINT ( 'NONE',  ( 6.358013415952256331, 1.820405254634300363, -0.1396899356524081148 ) ) ;
#191246=CARTESIAN_POINT ( 'NONE',  ( 2.747180457951060362, 0.2762254639866565942, -1.895546175561702018 ) ) ;
#191253=CARTESIAN_POINT ( 'NONE',  ( 2.654661980655496301, 2.105093816413053709, 0.2552270188876659129 ) ) ;
#191254=CARTESIAN_POINT ( 'NONE',  ( -0.02988540731097348233, 2.061246921799511966, -2.144091820287073791 ) ) ;
#191256=CARTESIAN_POINT ( 'NONE',  ( 4.253168938266341570, -1.637241709590877781, -1.097755751903241483 ) ) ;
#191257=CARTESIAN_POINT ( 'NONE',  ( 6.363533315466952445, -1.540175188624912650, -1.133462061071670579 ) ) ;
#191259=CARTESIAN_POINT ( 'NONE',  ( 6.245324861096241520, 0.3598972253578552327, -2.086368836056912368 ) ) ;
#191261=CARTESIAN_POINT ( 'NONE',  ( 1.592325325408463055, 1.022198633559557646, -1.800363622228560168 ) ) ;
#191262=CARTESIAN_POINT ( 'NONE',  ( 3.029168698193057008, -1.304570280419844686, -1.438651077900707120 ) ) ;
#191265=CARTESIAN_POINT ( 'NONE',  ( 3.644548676374514518, -1.708972400646594503, 1.203939368798632836 ) ) ;
#191268=ADVANCED_FACE ( 'NONE', ( #125906 ), #153538, .F. ) ;
#191269=CARTESIAN_POINT ( 'NONE',  ( 0.8381711186948238579, 1.079942214367535680, -1.454201162973115524 ) ) ;
#191271=CARTESIAN_POINT ( 'NONE',  ( 5.813141826352885566, 1.944573597739504889, 1.043518232037063287 ) ) ;
#191273=CARTESIAN_POINT ( 'NONE',  ( 3.012930935654754450, 1.599341701681813666, -1.520756135150652222 ) ) ;
#191275=CARTESIAN_POINT ( 'NONE',  ( 2.824755571612533434, 1.383597569638248315, -1.320258682893655999 ) ) ;
#191278=CARTESIAN_POINT ( 'NONE',  ( 5.547352688424546763, 1.827615396715172258, -0.9727077141251788683 ) ) ;
#191281=CARTESIAN_POINT ( 'NONE',  ( 2.852577672069932735, 0.7271573612388192442, 2.035869728763760378 ) ) ;
#191282=CARTESIAN_POINT ( 'NONE',  ( 4.282901435897610298, 1.957309562236182021, -0.9860176978964061423 ) ) ;
#191291=CARTESIAN_POINT ( 'NONE',  ( -0.2104748580754166598, -0.006608320950483163522, -2.103482951484026753 ) ) ;
#191294=CARTESIAN_POINT ( 'NONE',  ( 5.875854205266583641, -2.021069926245163906, 0.4479438709683660202 ) ) ;
#191295=CARTESIAN_POINT ( 'NONE',  ( 4.547439623722833169, -1.490282656903282099, -1.220848939070565686 ) ) ;
#191296=CARTESIAN_POINT ( 'NONE',  ( 6.398082464950202386, -0.9982666083749867081, -1.867140504451180183 ) ) ;
#191299=CARTESIAN_POINT ( 'NONE',  ( 5.647300209178060193, 1.738727086691471024, -0.9248740175569410971 ) ) ;
#191300=CARTESIAN_POINT ( 'NONE',  ( 0.1819133275808570704, -1.029140439971199417, 1.934768540691175431 ) ) ;
#191301=CARTESIAN_POINT ( 'NONE',  ( 5.356004772612798170, 1.823420152956479523, -0.09349780940721277855 ) ) ;
#191307=CARTESIAN_POINT ( 'NONE',  ( 2.296224312773272658, 1.477747569344042278, -1.098160524033331642 ) ) ;
#191308=CARTESIAN_POINT ( 'NONE',  ( 6.064703285670603350, 0.6354670234634349768, 1.910320939954947228 ) ) ;
#191309=CARTESIAN_POINT ( 'NONE',  ( 1.318156941596902998, -1.811358654967555104, 1.414711894558273730 ) ) ;
#191310=CARTESIAN_POINT ( 'NONE',  ( 5.840667439708360220, -1.913134005453724251, -0.4332900713753874977 ) ) ;
#191314=CARTESIAN_POINT ( 'NONE',  ( 0.1509401653462701109, -0.4529219869476922011, -2.027634260368789576 ) ) ;
#191316=CARTESIAN_POINT ( 'NONE',  ( 1.030938747749777118, -1.888616091942503461, 0.8971857714693499686 ) ) ;
#191317=CARTESIAN_POINT ( 'NONE',  ( 1.094370286708164386, -0.4508366001288487412, -1.815394955969009239 ) ) ;
#191318=CARTESIAN_POINT ( 'NONE',  ( 1.634138513624566302, 0.1511188354343559470, -2.010518437453466589 ) ) ;
#191321=CARTESIAN_POINT ( 'NONE',  ( 2.190578792945916842, 1.345991196328416573, 1.103389618610579381 ) ) ;
#191324=CARTESIAN_POINT ( 'NONE',  ( 6.925078400183574345, 7.629137130509068498, 2.744348168701661095 ) ) ;
#191325=CARTESIAN_POINT ( 'NONE',  ( 3.176078081051143531, -1.026819631599368066, 1.385778701376034316 ) ) ;
#191326=CARTESIAN_POINT ( 'NONE',  ( 3.263397454411249399, 2.137687552337414587, -0.4822058812353549606 ) ) ;
#191327=CARTESIAN_POINT ( 'NONE',  ( 5.215527394842717435, -0.3265260713646127022, 2.182469266582609091 ) ) ;
#191330=CARTESIAN_POINT ( 'NONE',  ( 2.307711192815030898, -1.741648834054570605, -1.296000553170826741 ) ) ;
#191331=CARTESIAN_POINT ( 'NONE',  ( 1.576486190600217663, -1.733098801405801304, -0.5742540608338757568 ) ) ;
#191332=CARTESIAN_POINT ( 'NONE',  ( 3.731751022097353321, 0.7093996228057770637, -1.995120430414954349 ) ) ;
#191333=CARTESIAN_POINT ( 'NONE',  ( 6.539320575229250920, 2.072231551265828475, 2.205269387046896679 ) ) ;
#191335=CARTESIAN_POINT ( 'NONE',  ( 3.509589594912354116, -2.258262956851801118, 0.3931918642409871212 ) ) ;
#191339=CARTESIAN_POINT ( 'NONE',  ( 5.426523936546859161, -0.9972995744461101708, -1.984925452567573023 ) ) ;
#191348=CARTESIAN_POINT ( 'NONE',  ( 4.026017654026761150, -1.753031021560845559, 0.9963007555989014108 ) ) ;
#191350=CARTESIAN_POINT ( 'NONE',  ( 3.871981579112850458, -2.032873796296597479, 0.3478246332576060973 ) ) ;
#191355=CARTESIAN_POINT ( 'NONE',  ( 5.876942531769460132, 2.026063101133714461, -0.8356547683932225024 ) ) ;
#191356=CARTESIAN_POINT ( 'NONE',  ( 3.235000160576475992, 2.016597019841442240, -0.002811030766311505089 ) ) ;
#191357=CARTESIAN_POINT ( 'NONE',  ( 1.804012939494209267, 1.363607186100148638, -1.237405090928713092 ) ) ;
#191360=CARTESIAN_POINT ( 'NONE',  ( 5.930640623865813588, 1.760069778787749506, 0.4843501209313359479 ) ) ;
#191362=CARTESIAN_POINT ( 'NONE',  ( 5.278307949308306490, -1.261584246701217715, 1.877956315871305071 ) ) ;
#191364=CARTESIAN_POINT ( 'NONE',  ( 2.455815469989936606, 0.5610288669116151317, -2.029897440403311215 ) ) ;
#191375=CARTESIAN_POINT ( 'NONE',  ( 2.514199509032362112, -0.6922678517280489441, 2.110887004458279481 ) ) ;
#191376=CARTESIAN_POINT ( 'NONE',  ( 0.4521680116954321371, 0.6883007682146925488, -2.096869779678663281 ) ) ;
#191379=CARTESIAN_POINT ( 'NONE',  ( 4.439869198996494681, 1.279870211898268550, 1.486999339763886097 ) ) ;
#191387=CARTESIAN_POINT ( 'NONE',  ( 3.340189922722580196, -1.266226476691566738, -1.700888996046201029 ) ) ;
#191389=CARTESIAN_POINT ( 'NONE',  ( 6.086834708314957432, -0.3123483334277510348, -2.138898144987111838 ) ) ;
#191390=CARTESIAN_POINT ( 'NONE',  ( 4.071694929070113211, -1.056692140236010102, 1.507659738195665788 ) ) ;
#191394=CARTESIAN_POINT ( 'NONE',  ( 6.509682854689390119, -0.8273637111445523162, -1.531083434488962780 ) ) ;
#191395=CARTESIAN_POINT ( 'NONE',  ( 6.727182134110203826, 7.053687134213418197, 2.309100590371661710 ) ) ;
#191398=CARTESIAN_POINT ( 'NONE',  ( 3.836934241894359054, 0.3148432204054998351, 2.138525872868973998 ) ) ;
#191399=CARTESIAN_POINT ( 'NONE',  ( 5.518907608433407219, 2.013924273726455549, -0.09612181791086168992 ) ) ;
#191401=CARTESIAN_POINT ( 'NONE',  ( 3.256853613824191029, -1.637998819981079990, 1.410756932016984377 ) ) ;
#191402=CARTESIAN_POINT ( 'NONE',  ( 3.637922374042131590, 0.8895205046622333134, -1.759358583061757519 ) ) ;
#191403=CARTESIAN_POINT ( 'NONE',  ( 0.1346727191937693857, 0.3808678606769915209, 2.158067550307264604 ) ) ;
#191404=CARTESIAN_POINT ( 'NONE',  ( 0.7808295286375503963, -1.278884537891399553, 1.920602667021213961 ) ) ;
#191405=CARTESIAN_POINT ( 'NONE',  ( 2.056002787803516973, 2.055476740694470728, -0.1483529063488266686 ) ) ;
#191406=CARTESIAN_POINT ( 'NONE',  ( 5.671417317124205937, 1.160065345341480647, 1.557364503162941061 ) ) ;
#191416=CARTESIAN_POINT ( 'NONE',  ( 1.993488836774780060, 1.919990754028239488, -1.087721427556323617 ) ) ;
#191418=CARTESIAN_POINT ( 'NONE',  ( 6.192239757033616065, 0.9699301198475211994, -1.705161095427814466 ) ) ;
#191422=CARTESIAN_POINT ( 'NONE',  ( 0.07479286986305544449, 2.888457405263197941, -2.344396930208477947 ) ) ;
#191424=CARTESIAN_POINT ( 'NONE',  ( 5.156134521940135329, -1.331146486249596306, 1.272188372451001026 ) ) ;
#191432=CARTESIAN_POINT ( 'NONE',  ( 1.288041055883992536, -0.9272951443832450069, 1.840570288256936804 ) ) ;
#191434=CARTESIAN_POINT ( 'NONE',  ( 1.838117294476193431, -0.9991240133950601843, 1.569924424075196390 ) ) ;
#191435=CARTESIAN_POINT ( 'NONE',  ( 4.546344060013487898, -1.475942220874026489, 1.100600019281534836 ) ) ;
#191442=AXIS2_PLACEMENT_3D ( 'NONE', #24155, #103297, #105456 ) ;
#191443=CARTESIAN_POINT ( 'NONE',  ( 4.125739685719872263, -2.112183141943014153, 0.6395159525410462065 ) ) ;
#191444=CARTESIAN_POINT ( 'NONE',  ( 6.380173838452511959, -1.218392737502610013, 1.906166127322491910 ) ) ;
#191446=CARTESIAN_POINT ( 'NONE',  ( 0.4746845637013075159, -1.383529810647101455, 1.320479256824915071 ) ) ;
#191447=CARTESIAN_POINT ( 'NONE',  ( 0.07540816263147330500, 1.497505997221737273, 1.350731191893522976 ) ) ;
#191450=CARTESIAN_POINT ( 'NONE',  ( 5.637344576021464881, -0.04253375892994575719, 1.911971901805489038 ) ) ;
#191452=CARTESIAN_POINT ( 'NONE',  ( 0.5670072068131201126, 0.1877032549213939472, -1.861219751863735672 ) ) ;
#191453=CARTESIAN_POINT ( 'NONE',  ( 2.079314900164643820, 1.561883299538204151, 1.275554356156020308 ) ) ;
#191455=CARTESIAN_POINT ( 'NONE',  ( 3.809285178775764447, 1.806332912941556623, 1.082654235687771749 ) ) ;
#191460=CARTESIAN_POINT ( 'NONE',  ( 2.812765223479243737, -0.5904890161391795900, -1.931511402468567340 ) ) ;
#191464=CARTESIAN_POINT ( 'NONE',  ( 4.042369558984196587, 2.150769235480045616, 0.2162802025119994753 ) ) ;
#191470=CARTESIAN_POINT ( 'NONE',  ( 1.856167715545921748, -0.7324389044234179691, 2.044012385327702575 ) ) ;
#191473=CARTESIAN_POINT ( 'NONE',  ( 1.241482983173985533, 1.839155304979672501, 0.08999620058360720265 ) ) ;
#191475=CARTESIAN_POINT ( 'NONE',  ( 1.628746693258641853, 0.2190750365392846177, 2.180598679842937759 ) ) ;
#191476=CARTESIAN_POINT ( 'NONE',  ( 6.883263157960381129, 0.5832772681763243039, 2.006853359411898463 ) ) ;
#191477=CARTESIAN_POINT ( 'NONE',  ( 3.239431411193524735, -1.996134195211620721, 1.065073381557869903 ) ) ;
#191483=CARTESIAN_POINT ( 'NONE',  ( 4.780378767880190338, -1.716399873034094803, -0.4305553870933165883 ) ) ;
#191485=CARTESIAN_POINT ( 'NONE',  ( 0.9914056592630847708, 1.857388527897243291, -0.9925227068504693939 ) ) ;
#191489=CARTESIAN_POINT ( 'NONE',  ( 6.310172759758509109, 1.158674036163497734, -1.650093421473826316 ) ) ;
#191490=CARTESIAN_POINT ( 'NONE',  ( 5.203285271772914555, 1.593979872821064570, -0.8609055379997750945 ) ) ;
#191494=CARTESIAN_POINT ( 'NONE',  ( 3.994877460428855720, 1.580554378303768770, -1.000287695324620252 ) ) ;
#191496=CARTESIAN_POINT ( 'NONE',  ( 3.942288228968212849, -1.024710522258945655, 1.798826465557185506 ) ) ;
#191506=CARTESIAN_POINT ( 'NONE',  ( 3.824618516750320385, -1.319357783791510697, 1.452116237791359010 ) ) ;
#191507=CARTESIAN_POINT ( 'NONE',  ( 1.704453651327157537, -1.458331393932917885, -1.392334588655015803 ) ) ;
#191510=CARTESIAN_POINT ( 'NONE',  ( 0.5791066246769066561, 1.747692025923882841, -0.6672336632058751826 ) ) ;
#191512=CARTESIAN_POINT ( 'NONE',  ( 2.865492421389451039, -1.648320183868864364, -1.155634683092461978 ) ) ;
#191514=CARTESIAN_POINT ( 'NONE',  ( 3.655961130333235776, 1.178038043211126817, 1.759042251235248600 ) ) ;
#191515=CARTESIAN_POINT ( 'NONE',  ( 6.825078400183578253, 1.241995729952071414, 2.258014901253778017 ) ) ;
#191516=CARTESIAN_POINT ( 'NONE',  ( 5.459458695672200435, 1.690470114046587646, 1.195012289465044564 ) ) ;
#191518=CARTESIAN_POINT ( 'NONE',  ( 0.3981334665579424059, -0.7082897861981848342, -1.967241634975321452 ) ) ;
#191520=CARTESIAN_POINT ( 'NONE',  ( 4.840742024777624053, 0.3130767520662172121, 1.798364180563789327 ) ) ;
#191528=CARTESIAN_POINT ( 'NONE',  ( 6.375647946566726176, 0.3219878414668366773, -1.884816399834337908 ) ) ;
#191537=CARTESIAN_POINT ( 'NONE',  ( 0.07700591528351626025, 0.2537022344677486996, -1.946355950789683043 ) ) ;
#191541=CARTESIAN_POINT ( 'NONE',  ( 0.1399997263885795762, 1.361443548867202979, -2.255028951473649901 ) ) ;
#191544=CARTESIAN_POINT ( 'NONE',  ( 1.885543262503614592, -1.856164082770836110, 0.6587638493158411990 ) ) ;
#191545=CARTESIAN_POINT ( 'NONE',  ( 3.691029940746898053, 1.730877988113326493, 1.034147909374658392 ) ) ;
#191547=CARTESIAN_POINT ( 'NONE',  ( 6.827182134110223899, 2.937564492898884438, 2.740749177975018380 ) ) ;
#191548=CARTESIAN_POINT ( 'NONE',  ( 3.345827479060593301, 2.191629467292684819, -0.0001215010576177677764 ) ) ;
#191550=CARTESIAN_POINT ( 'NONE',  ( 1.870020283345479539, 0.9883514471830873171, 1.653387599232780447 ) ) ;
#191553=CARTESIAN_POINT ( 'NONE',  ( 0.2329586101569866563, 0.2513371725885656938, -1.880733749865989068 ) ) ;
#191560=CARTESIAN_POINT ( 'NONE',  ( 6.567912610837368881, -1.126952994821692533, 1.456688911285822119 ) ) ;
#191561=CARTESIAN_POINT ( 'NONE',  ( 3.475247029965710777, -1.776355867393118126, -0.9471225605895690070 ) ) ;
#191562=CARTESIAN_POINT ( 'NONE',  ( 4.183220704542046420, -1.177475575078859027, -1.973740397952013836 ) ) ;
#191563=CARTESIAN_POINT ( 'NONE',  ( -0.1291982275798625457, 7.629137130509075604, -2.673995287120598086 ) ) ;
#191564=CARTESIAN_POINT ( 'NONE',  ( 3.485049009367678252, 0.04119252264746588871, 1.860649646085434039 ) ) ;
#191567=CARTESIAN_POINT ( 'NONE',  ( 6.345967646908174054, -1.254484226688237447, -1.443505786478386899 ) ) ;
#191570=CARTESIAN_POINT ( 'NONE',  ( 5.759345132242938092, 2.059656548118168562, -0.3582877099650525476 ) ) ;
#191575=CARTESIAN_POINT ( 'NONE',  ( 5.742733201377892449, 0.3429454505429993527, 1.690258806964558547 ) ) ;
#191577=CARTESIAN_POINT ( 'NONE',  ( 1.388881788488422586, -0.6239178774879328149, -1.618199924151533686 ) ) ;
#191580=PRESENTATION_STYLE_ASSIGNMENT (( #163374 ) ) ;
#191581=CARTESIAN_POINT ( 'NONE',  ( 5.717690620771469945, 0.4309847871033903877, -2.127713340945025511 ) ) ;
#191582=CARTESIAN_POINT ( 'NONE',  ( 4.459475772512963232, 0.3974328844052883447, -1.781742007231662983 ) ) ;
#191583=CARTESIAN_POINT ( 'NONE',  ( 2.483191118468269565, -0.005009705968514814069, 1.961936380092830001 ) ) ;
#191588=CARTESIAN_POINT ( 'NONE',  ( 3.035902975225315714, -2.043024508941180706, 0.5676086983019896781 ) ) ;
#191590=EDGE_CURVE ( 'NONE', #100328, #64278, #160494, .T. ) ;
#191593=CARTESIAN_POINT ( 'NONE',  ( 0.3564121386029559524, -2.069725681613205470, -0.05427943458365809548 ) ) ;
#191596=CARTESIAN_POINT ( 'NONE',  ( 3.282088111431053612, 2.166828800601192206, -0.4882270792503102808 ) ) ;
#191598=CARTESIAN_POINT ( 'NONE',  ( 0.9854702925387841539, -2.298851036028260353, 0.006955682198207107335 ) ) ;
#191600=CARTESIAN_POINT ( 'NONE',  ( 6.491093265613332441, 0.1965012520625461223, 2.053163312798581774 ) ) ;
#191604=CARTESIAN_POINT ( 'NONE',  ( 5.249485218566787736, 1.838879873951341004, -0.09611505855997715120 ) ) ;
#191606=CARTESIAN_POINT ( 'NONE',  ( -0.2102771530458277249, 5.719403664101017526, -2.797728457938574387 ) ) ;
#191607=CARTESIAN_POINT ( 'NONE',  ( 3.346439682166453711, 0.4181539295537542444, 1.673179028346531538 ) ) ;
#191608=CARTESIAN_POINT ( 'NONE',  ( 0.6554828803995507158, 1.942095732595986890, -0.5424746339172461518 ) ) ;
#191609=CARTESIAN_POINT ( 'NONE',  ( 3.393488084526240733, -0.9333142364225041065, -2.100862151682027612 ) ) ;
#191610=CARTESIAN_POINT ( 'NONE',  ( 2.952682139456219268, 0.7592856210697115360, 2.131335665991466843 ) ) ;
#191611=CARTESIAN_POINT ( 'NONE',  ( 5.057299757384343231, -1.778698004947255162, -1.127411927216742216 ) ) ;
#191613=CARTESIAN_POINT ( 'NONE',  ( 3.936565515923634795, 0.2574710272360211105, 1.750749954138763442 ) ) ;
#191615=CARTESIAN_POINT ( 'NONE',  ( 6.304234482382112148, 1.701787343685069009, -1.536020108501337855 ) ) ;
#191616=CARTESIAN_POINT ( 'NONE',  ( 5.033073903806924321, -1.304366766181121573, -1.299653785596634137 ) ) ;
#191620=CARTESIAN_POINT ( 'NONE',  ( 4.892620165872568094, 1.823077252308364482, -1.215776859382920794 ) ) ;
#191623=CARTESIAN_POINT ( 'NONE',  ( 4.545415791725802457, 1.850806902094417783, -0.9279678557222792445 ) ) ;
#191624=CARTESIAN_POINT ( 'NONE',  ( 0.1632964843477149597, 1.879801964727344732, -0.7303121171872913875 ) ) ;
#191626=CARTESIAN_POINT ( 'NONE',  ( 3.668508669297173341, -1.293070320541231721, 1.428231264829373126 ) ) ;
#191629=CARTESIAN_POINT ( 'NONE',  ( 6.433838290133602200, -2.056603270127650429, 0.5165238393732355382 ) ) ;
#191637=CARTESIAN_POINT ( 'NONE',  ( 1.592165322863370980, 0.9698756732311950568, -1.705302290208744687 ) ) ;
#191640=CARTESIAN_POINT ( 'NONE',  ( 5.090269282739749102, 1.010147525469132557, -1.681691772506640481 ) ) ;
#191643=CARTESIAN_POINT ( 'NONE',  ( 6.772347375734490527, -1.334533509509854943, 1.701269717329929820 ) ) ;
#191644=CARTESIAN_POINT ( 'NONE',  ( -0.2106725631050307412, 6.947230693896488951, -2.598707507344534040 ) ) ;
#191647=CARTESIAN_POINT ( 'NONE',  ( 6.696557531595894730, -0.5234078932761144776, -1.900562160593147754 ) ) ;
#191648=CARTESIAN_POINT ( 'NONE',  ( 6.450542193449531503, 1.198949306261879455, 1.252755643323471668 ) ) ;
#191651=CARTESIAN_POINT ( 'NONE',  ( 3.562233144267571650, -1.470601008620987749, 1.625073949779440419 ) ) ;
#191652=CARTESIAN_POINT ( 'NONE',  ( 4.858593139428769803, 0.8780750695473713563, 2.134189430172124702 ) ) ;
#191653=CARTESIAN_POINT ( 'NONE',  ( 6.397740692956204178, -0.6987371234766488470, 1.938827229339795455 ) ) ;
#191654=CARTESIAN_POINT ( 'NONE',  ( 1.833828351339358287, 1.920785844388651409, 0.2851290042146270576 ) ) ;
#191658=CARTESIAN_POINT ( 'NONE',  ( 5.027636390373714903, -0.3086946445357250379, 2.097867224209007730 ) ) ;
#191660=CARTESIAN_POINT ( 'NONE',  ( 3.709611425391425854, 1.915599900965975433, 0.6298755557959597740 ) ) ;
#191669=CARTESIAN_POINT ( 'NONE',  ( 5.717669251203768788, -2.011168408518650974, 0.4492202366306179417 ) ) ;
#191676=CARTESIAN_POINT ( 'NONE',  ( 4.336585317048437638, 1.240917556630851237, -1.593414756171371183 ) ) ;
#191682=CARTESIAN_POINT ( 'NONE',  ( 4.188392892783887156, -2.038203232304033108, -0.3041262925047826249 ) ) ;
#191683=CARTESIAN_POINT ( 'NONE',  ( 2.584611472894111195, -0.6298744119781033435, 1.915600275669691488 ) ) ;
#191690=CARTESIAN_POINT ( 'NONE',  ( 2.723982329760873178, -1.752761823190003287, -0.9961495992579154635 ) ) ;
#191691=CARTESIAN_POINT ( 'NONE',  ( 2.009460956091331685, -0.8672641894471898594, -1.624084198382821587 ) ) ;
#191692=CARTESIAN_POINT ( 'NONE',  ( 1.049971938256549109, -1.822247386521518298, -1.415841994891045674 ) ) ;
#191694=CARTESIAN_POINT ( 'NONE',  ( 3.743588348364734752, -1.634107004491680115, -1.415051943026650161 ) ) ;
#191697=CARTESIAN_POINT ( 'NONE',  ( 3.058317229773829471, 1.972480788633700577, -1.179572646267361025 ) ) ;
#191700=CARTESIAN_POINT ( 'NONE',  ( 1.006479672118578916, 1.419055151971573059, -1.218976214888117804 ) ) ;
#191701=CARTESIAN_POINT ( 'NONE',  ( 6.051636762666342761, 0.5725952485956290472, -1.886469267683591466 ) ) ;
#191706=CARTESIAN_POINT ( 'NONE',  ( 0.5576012004645107822, -1.866542136390366036, -1.177153700605698461 ) ) ;
#191712=CARTESIAN_POINT ( 'NONE',  ( 5.471542181860619358, 1.900225975651721244, -0.5249898485142224791 ) ) ;
#191713=CARTESIAN_POINT ( 'NONE',  ( 4.073124928733475869, -2.152535440544633971, -0.8323431910086924734 ) ) ;
#191714=CARTESIAN_POINT ( 'NONE',  ( 6.004338076955692216, 1.858996105215251493, 0.09048898905416635774 ) ) ;
#191716=CARTESIAN_POINT ( 'NONE',  ( 3.256738233524118620, -0.5941274279437200878, -1.975181216424357400 ) ) ;
#191724=CARTESIAN_POINT ( 'NONE',  ( 5.687976231080541289, -1.372897218612447290, -1.682037316681925132 ) ) ;
#191726=CARTESIAN_POINT ( 'NONE',  ( 4.071694929070113211, -1.056692140236010102, 1.507659738195665788 ) ) ;
#191728=CARTESIAN_POINT ( 'NONE',  ( 6.620655732516611103, 3.701195159515461075, 2.440764268381501179 ) ) ;
#191729=CARTESIAN_POINT ( 'NONE',  ( 6.128506746050899068, 0.2130254606748181456, 2.181202035047181020 ) ) ;
#191731=CARTESIAN_POINT ( 'NONE',  ( 0.3689490567273964738, -1.476270946665221517, 1.714425361395756964 ) ) ;
#191737=CARTESIAN_POINT ( 'NONE',  ( 0.5668360377511200143, 0.1796360565177144708, -1.760708420565498589 ) ) ;
#191738=CARTESIAN_POINT ( 'NONE',  ( 5.285796247307868789, 1.939527786139252585, -0.5389555323440149426 ) ) ;
#191741=CARTESIAN_POINT ( 'NONE',  ( 3.979594558520031189, 1.983667836772174509, -0.7075980189445835178 ) ) ;
#191742=CARTESIAN_POINT ( 'NONE',  ( 2.759290930233889494, 1.818065234828979637, -0.6036251144310407213 ) ) ;
#191744=CARTESIAN_POINT ( 'NONE',  ( 4.439879492920996817, 1.284938098365424164, 1.492779756951348125 ) ) ;
#191745=CARTESIAN_POINT ( 'NONE',  ( 5.783464979101770709, 0.1443126057797445849, -2.014664192723765623 ) ) ;
#191746=CARTESIAN_POINT ( 'NONE',  ( 1.656895194024514906, -1.602792776363659133, -0.9643473572949823325 ) ) ;
#191747=CARTESIAN_POINT ( 'NONE',  ( 4.670341630432963242, -1.123608009272176078, 1.308792564452855522 ) ) ;
#191748=CARTESIAN_POINT ( 'NONE',  ( 1.265713261412576562, 0.5522810963098608861, -1.830935845731461953 ) ) ;
#191750=CARTESIAN_POINT ( 'NONE',  ( 2.069229996397306426, -2.018448871333050842, -0.8927042923378907258 ) ) ;
#191753=CARTESIAN_POINT ( 'NONE',  ( 6.707479306934847507, -1.574971382793718178, -1.169550641929931079 ) ) ;
#191758=CLOSED_SHELL ( 'NONE', ( #56184, #198258, #178564, #29591, #2951, #103662, #146633, #33046 ) ) ;
#191761=CARTESIAN_POINT ( 'NONE',  ( 2.277862540309500083, -2.008769142935047380, 0.5008063122204224893 ) ) ;
#191767=CARTESIAN_POINT ( 'NONE',  ( 6.445950376775947177, -1.384621037358444662, -1.606076714075025613 ) ) ;
#191772=CARTESIAN_POINT ( 'NONE',  ( 5.466172646012215530, 1.646588110366095314, 1.163089216160061001 ) ) ;
#191773=CARTESIAN_POINT ( 'NONE',  ( 4.346842662630929333, -1.713972709756344859, -0.8558225519783541069 ) ) ;
#191774=CARTESIAN_POINT ( 'NONE',  ( 3.210657068901449307, 1.982179491636561819, 0.9350799695589939731 ) ) ;
#191777=CARTESIAN_POINT ( 'NONE',  ( 5.801044709096109031, -0.2997443204828981189, -1.990672168044338886 ) ) ;
#191778=CARTESIAN_POINT ( 'NONE',  ( 1.160255710619631397, 1.910328232974867868, 0.09094507755665059978 ) ) ;
#191781=CARTESIAN_POINT ( 'NONE',  ( 0.01720424586787797083, -1.842442205116225695, 0.8197940039925479816 ) ) ;
#191783=CARTESIAN_POINT ( 'NONE',  ( 3.720331632570073932, 1.985922124624572627, 0.6539709493295197129 ) ) ;
#191785=CARTESIAN_POINT ( 'NONE',  ( 2.027930484333416050, 0.9963118489298377067, -1.407687550210996230 ) ) ;
#191793=CARTESIAN_POINT ( 'NONE',  ( 2.437905218827548737, -1.044187398466125627, -1.480012136316358085 ) ) ;
#191794=ORIENTED_EDGE ( 'NONE', *, *, #202148, .T. ) ;
#191797=CARTESIAN_POINT ( 'NONE',  ( 3.949720763895887110, -1.252031560403286337, -1.309370340798710730 ) ) ;
#191800=CARTESIAN_POINT ( 'NONE',  ( 4.158551126772993989, -0.5825245785200537929, -1.767622772031415490 ) ) ;
#191801=CARTESIAN_POINT ( 'NONE',  ( 1.282674911181800104, 1.565081248417903081, -1.104254300028691071 ) ) ;
#191802=CARTESIAN_POINT ( 'NONE',  ( 0.4108170757193031486, 1.585627777896590151, 0.9046078287104839522 ) ) ;
#191812=CARTESIAN_POINT ( 'NONE',  ( 5.752784996495730496, -0.4749413952093975433, -1.911207028377271522 ) ) ;
#191815=CARTESIAN_POINT ( 'NONE',  ( 0.5684512833941969268, -1.969177116664261762, -0.7025944222667882544 ) ) ;
#191817=CARTESIAN_POINT ( 'NONE',  ( 5.385741010672205675, 1.293702408046822239, 1.427520146239504184 ) ) ;
#191819=CARTESIAN_POINT ( 'NONE',  ( 1.483130931141176889, 1.688290157389197077, -0.6950536248920418103 ) ) ;
#191820=CARTESIAN_POINT ( 'NONE',  ( 2.719571217284349363, -0.2154062111461417239, 2.196339928330424129 ) ) ;
#191823=CARTESIAN_POINT ( 'NONE',  ( 0.5274218815167727170, -0.2782315536139517431, 1.891897276498944347 ) ) ;
#191825=CARTESIAN_POINT ( 'NONE',  ( 0.1859136753566691391, -1.208741973239912726, -1.555490313720475415 ) ) ;
#191826=CARTESIAN_POINT ( 'NONE',  ( 2.138135174613201350, 0.4275120379338535614, 1.894264587998186089 ) ) ;
#191828=CARTESIAN_POINT ( 'NONE',  ( 1.089219988750099732, 1.203171814842165288, -1.617568698395126292 ) ) ;
#191830=CARTESIAN_POINT ( 'NONE',  ( 6.069184012654499583, 1.640672622335254793, 0.8782983229575453965 ) ) ;
#191836=CARTESIAN_POINT ( 'NONE',  ( 2.068174269828721101, -1.345378145056834063, 1.729934933326432445 ) ) ;
#191840=CARTESIAN_POINT ( 'NONE',  ( 2.930095790256614485, 1.013914413367119627, -1.518051517300327502 ) ) ;
#191844=CARTESIAN_POINT ( 'NONE',  ( -0.02968770228137587730, 2.889947918782026726, -2.315223470976325526 ) ) ;
#191846=CARTESIAN_POINT ( 'NONE',  ( 0.4867822013649549251, -0.2347038428511475372, -1.912094274373641323 ) ) ;
#191847=CARTESIAN_POINT ( 'NONE',  ( 5.278158119090741174, -1.046208158741080529, -1.659298866772864756 ) ) ;
#191848=EDGE_CURVE ( 'NONE', #53173, #193311, #86296, .T. ) ;
#191852=CARTESIAN_POINT ( 'NONE',  ( 5.530878137806295669, -1.981686641427220286, 0.9361944923952856268 ) ) ;
#191855=CARTESIAN_POINT ( 'NONE',  ( 3.608316154870555792, 2.070434559819031684, 0.004826415812286819970 ) ) ;
#191859=CARTESIAN_POINT ( 'NONE',  ( 4.377739380128500279, -0.5030580445687399260, -2.242836179151234344 ) ) ;
#191863=CARTESIAN_POINT ( 'NONE',  ( 6.620655732516620873, 0.004685112605665174221, 1.926407831898164558 ) ) ;
#191865=CARTESIAN_POINT ( 'NONE',  ( 5.156170417566459108, -1.405356202774979524, 1.340433341176451520 ) ) ;
#191866=ORIENTED_EDGE ( 'NONE', *, *, #118204, .T. ) ;
#191871=CARTESIAN_POINT ( 'NONE',  ( 5.554919272666569263, 0.3793472168572444292, 1.874222000232607765 ) ) ;
#191872=CARTESIAN_POINT ( 'NONE',  ( 6.651377187556704484, -1.389000575594327103, -1.022263415358831473 ) ) ;
#191873=CARTESIAN_POINT ( 'NONE',  ( 4.364470425680367249, -1.957169923074707274, -0.4852690807995581057 ) ) ;
#191877=CARTESIAN_POINT ( 'NONE',  ( 1.482492212676550070, -0.3080716119066116421, -2.067685480015791111 ) ) ;
#191878=CARTESIAN_POINT ( 'NONE',  ( 6.573528787226094572, 1.692674132781073260, -0.5166258990680439034 ) ) ;
#191879=CARTESIAN_POINT ( 'NONE',  ( 6.240861317752083970, 2.010826688392798101, -0.1511364921914087889 ) ) ;
#191881=CARTESIAN_POINT ( 'NONE',  ( 3.135043019019596144, -2.021410203770683367, 1.080917199049796107 ) ) ;
#191882=CARTESIAN_POINT ( 'NONE',  ( 1.692878195147719422, -0.5885122380313506651, 1.637943671576999272 ) ) ;
#191884=CARTESIAN_POINT ( 'NONE',  ( 0.8250588069352093878, -1.261192405561472274, 1.190076739608906697 ) ) ;
#191886=CARTESIAN_POINT ( 'NONE',  ( 1.504125588540955683, 1.858726126767410669, 0.09586466133617438379 ) ) ;
#191887=CARTESIAN_POINT ( 'NONE',  ( 2.154941862968827504, -0.5775488349282401623, -2.092905974620140164 ) ) ;
#191888=CARTESIAN_POINT ( 'NONE',  ( 3.063685658700274761, 1.282989771343697294, 1.555699169480361022 ) ) ;
#191889=CARTESIAN_POINT ( 'NONE',  ( 5.218750000000002665, -0.7852924748297095414, 1.895863743164193371 ) ) ;
#191891=CARTESIAN_POINT ( 'NONE',  ( 0.3231025844343059505, -0.09812569541690382979, 1.924018777033975836 ) ) ;
#191893=CARTESIAN_POINT ( 'NONE',  ( 3.357896860617498369, -1.684415915708385114, -1.448384614443619434 ) ) ;
#191899=CARTESIAN_POINT ( 'NONE',  ( 6.310783679736120533, -0.5911123833974815112, -2.141223572898354188 ) ) ;
#191900=CARTESIAN_POINT ( 'NONE',  ( 4.246505328441081417, -1.940195102956907336, -0.2900488188990399396 ) ) ;
#191904=CARTESIAN_POINT ( 'NONE',  ( 5.747450795320371064, -1.778423256021565813, -1.398359773074304480 ) ) ;
#191905=CARTESIAN_POINT ( 'NONE',  ( 2.646997546006967905, -0.3502154465670388461, -2.032575613165943818 ) ) ;
#191909=CARTESIAN_POINT ( 'NONE',  ( 3.708139779478221598, -0.7553879706188313392, -1.711406342686023541 ) ) ;
#191910=CARTESIAN_POINT ( 'NONE',  ( 2.848001011750156408, 0.2514756280368075081, -1.715647774213580501 ) ) ;
#191911=CARTESIAN_POINT ( 'NONE',  ( 6.614806895146394972, -0.1608752592793839531, 2.155998228907447523 ) ) ;
#191912=CARTESIAN_POINT ( 'NONE',  ( 1.132168909276673796, -1.401036632855560349, -1.704990472574128502 ) ) ;
#191913=CARTESIAN_POINT ( 'NONE',  ( 6.228462243142912413, 0.1929387083638624822, 1.932343765256574697 ) ) ;
#191916=CARTESIAN_POINT ( 'NONE',  ( 0.7740648250077889481, 1.777010169924503558, -0.9530137779002674225 ) ) ;
#191919=CARTESIAN_POINT ( 'NONE',  ( 6.363907750917786821, -0.1017471579566435469, -2.013986097687201049 ) ) ;
#191923=CARTESIAN_POINT ( 'NONE',  ( 3.633261591126951018, -1.686358373764598406, 0.7000054678709469735 ) ) ;
#191924=CARTESIAN_POINT ( 'NONE',  ( 2.327434156339613924, -0.0004056629378437063877, 2.206952907597827362 ) ) ;
#191930=CARTESIAN_POINT ( 'NONE',  ( 1.142838682686732277, 1.947676595115959586, 0.5347052314127549444 ) ) ;
#191933=CARTESIAN_POINT ( 'NONE',  ( 2.465471660774602558, -0.4132369024843309258, 1.814301444843221089 ) ) ;
#191935=CARTESIAN_POINT ( 'NONE',  ( 6.504528880466823537, -1.955196382115764964, 0.4926337920100053447 ) ) ;
#191939=CARTESIAN_POINT ( 'NONE',  ( 4.266095019097836172, 0.8626762044917112293, 1.609013669381313294 ) ) ;
#191943=CARTESIAN_POINT ( 'NONE',  ( 6.380232485702068246, -0.2495653932444163448, 2.000551205290925783 ) ) ;
#191944=CARTESIAN_POINT ( 'NONE',  ( 5.419803763747102821, 1.093575605593154920, -1.481025086994464113 ) ) ;
#191945=CARTESIAN_POINT ( 'NONE',  ( 4.037936217472848810, -1.589972691411502659, -1.672771819537349325 ) ) ;
#191947=CARTESIAN_POINT ( 'NONE',  ( 0.7200824656817590430, -1.100121004815158177, -1.742362558145001294 ) ) ;
#191949=CARTESIAN_POINT ( 'NONE',  ( 2.665492718168083641, 1.041058713608807418, 1.639284265488485381 ) ) ;
#191950=CARTESIAN_POINT ( 'NONE',  ( 5.272985406448559509, -2.287992931341980896, 0.2183071761258491283 ) ) ;
#191953=CARTESIAN_POINT ( 'NONE',  ( 4.117926171558832671, -0.9613396577640184182, -1.604580606731422554 ) ) ;
#191956=CARTESIAN_POINT ( 'NONE',  ( 2.601700882821424976, 1.355260107747566334, 1.349524769375435973 ) ) ;
#191959=CARTESIAN_POINT ( 'NONE',  ( 3.739080281021701868, 0.3231575147602770426, 2.182976880621155136 ) ) ;
#191963=CARTESIAN_POINT ( 'NONE',  ( 6.883263157960366918, 3.696842586722656865, 2.460469087180997327 ) ) ;
#191966=CARTESIAN_POINT ( 'NONE',  ( 1.897670943237000918, -0.6677869454260307869, 1.854917580456706183 ) ) ;
#191967=CARTESIAN_POINT ( 'NONE',  ( 2.169360633853111509, -2.109970246048063380, -0.9347365353246681607 ) ) ;
#191968=CARTESIAN_POINT ( 'NONE',  ( 2.892962425504439050, 0.2373818416543191367, 1.947367909387688112 ) ) ;
#191970=CARTESIAN_POINT ( 'NONE',  ( 6.051645708474242547, 1.558200330177769377, 1.351431136778310726 ) ) ;
#191973=ORIENTED_EDGE ( 'NONE', *, *, #110985, .T. ) ;
#191974=CARTESIAN_POINT ( 'NONE',  ( 5.102750050473856547, 1.865045247124358818, 0.7672954931761333253 ) ) ;
#191976=DIRECTION ( 'NONE',  ( 2.949029909160572061E-17, 1.000000000000000000, -8.673600428462616880E-15 ) ) ;
#191979=CARTESIAN_POINT ( 'NONE',  ( 2.307711192815030898, -1.741648834054570605, -1.296000553170826741 ) ) ;
#191983=CARTESIAN_POINT ( 'NONE',  ( 2.073319367481298858, 1.791407343212477077, -0.5384048943791116537 ) ) ;
#191984=CARTESIAN_POINT ( 'NONE',  ( 6.854756222516505737, -1.675677847961650313, 1.365199464886861946 ) ) ;
#191986=CARTESIAN_POINT ( 'NONE',  ( 6.727182134110209155, 1.290711256955964448, 1.927001067762003972 ) ) ;
#191988=DIRECTION ( 'NONE',  ( -3.451266460341926649E-31, -5.200010849845536803E-32, 1.000000000000000000 ) ) ;
#191989=CARTESIAN_POINT ( 'NONE',  ( 3.211475575234080004, 1.509012206799903666, 1.174515185244667581 ) ) ;
#191990=CARTESIAN_POINT ( 'NONE',  ( 3.678344558940789266, -1.705506331563589661, -0.4725282708486245875 ) ) ;
#191992=CARTESIAN_POINT ( 'NONE',  ( 2.139182944796279351, 0.001596215867826628054, 1.912461472203148771 ) ) ;
#191995=CARTESIAN_POINT ( 'NONE',  ( 6.415652790497161639, -1.255571041358375384, -1.446825450776100919 ) ) ;
#191997=CARTESIAN_POINT ( 'NONE',  ( 1.398975865466948632, 0.4019745351953528112, 2.030794141931663521 ) ) ;
#191999=CARTESIAN_POINT ( 'NONE',  ( 5.823093596695693819, -0.04436734784114480107, 1.870300906237104988 ) ) ;
#192000=CARTESIAN_POINT ( 'NONE',  ( 1.312830284664792790, 1.609138963534262778, 0.8624270714618911260 ) ) ;
#192001=CARTESIAN_POINT ( 'NONE',  ( 5.936183876523434932, 1.091049494364674466, -1.918236432931222257 ) ) ;
#192004=CARTESIAN_POINT ( 'NONE',  ( 2.980982186342299833, 1.941357688518682290, 0.6972846330933372139 ) ) ;
#192014=CARTESIAN_POINT ( 'NONE',  ( 5.898901817742318698, 0.4001337562283372451, 2.031160294743330486 ) ) ;
#192016=CARTESIAN_POINT ( 'NONE',  ( 2.267066545249882381, -1.975312647937790933, -0.8782872871702239737 ) ) ;
#192018=CARTESIAN_POINT ( 'NONE',  ( 2.613930769413209898, -0.6315753767559011411, 1.918467498408537919 ) ) ;
#192019=CARTESIAN_POINT ( 'NONE',  ( 6.720655732516659597, 0.5653683226944251627, 2.225905711026022971 ) ) ;
#192025=CARTESIAN_POINT ( 'NONE',  ( 1.024625454658374624, 0.3981145430279106057, 1.976669095394629982 ) ) ;
#192027=CARTESIAN_POINT ( 'NONE',  ( 5.566036750361066154, -1.391122746885119499, 1.693456055751572986 ) ) ;
#192029=CARTESIAN_POINT ( 'NONE',  ( 4.974826827724895928, -1.381046924789817831, 1.323090558688621909 ) ) ;
#192033=CARTESIAN_POINT ( 'NONE',  ( 3.796500049179197589, 1.423950305759081214, -1.427950143821264506 ) ) ;
#192035=CARTESIAN_POINT ( 'NONE',  ( 5.702095886272589453, -1.724958192454665085, 0.004281591079305368218 ) ) ;
#192039=CARTESIAN_POINT ( 'NONE',  ( 4.006994748872731549, 1.602975652146242380, 0.9638501484771769823 ) ) ;
#192041=CARTESIAN_POINT ( 'NONE',  ( 1.112269271232646739, 2.068042923180101411, -0.09779880236997220977 ) ) ;
#192044=CARTESIAN_POINT ( 'NONE',  ( -0.2110808730067273986, 0.0005491059566040295322, -1.796958327270286704 ) ) ;
#192047=CARTESIAN_POINT ( 'NONE',  ( -0.08802119743880723601, -1.811174541614871236, -0.04475806069833241502 ) ) ;
#192052=CARTESIAN_POINT ( 'NONE',  ( 0.6605093422152423788, -0.6574743052488278838, -1.848563176889833626 ) ) ;
#192055=CARTESIAN_POINT ( 'NONE',  ( 4.833546035289306708, 0.5969252065377036454, -1.820314225251006945 ) ) ;
#192060=ORIENTED_EDGE ( 'NONE', *, *, #60919, .F. ) ;
#192062=CARTESIAN_POINT ( 'NONE',  ( 1.481558191429488192, 1.997200094811113491, -0.8276061316847342919 ) ) ;
#192065=CARTESIAN_POINT ( 'NONE',  ( 0.2289750728588327566, 1.457791096766167360, -1.540313549178488284 ) ) ;
#192066=CARTESIAN_POINT ( 'NONE',  ( 4.225493254642153751, -1.746956894163293361, 0.5300125199643388463 ) ) ;
#192068=CARTESIAN_POINT ( 'NONE',  ( 0.8429695343807745989, -1.692941477971823483, 1.009804834249914851 ) ) ;
#192069=CARTESIAN_POINT ( 'NONE',  ( 3.656429697474584017, 1.903630103707624865, 0.1825790434749063051 ) ) ;
#192072=CARTESIAN_POINT ( 'NONE',  ( 3.736728436007582310, -1.897426337869069668, -0.5277852043128227200 ) ) ;
#192074=CARTESIAN_POINT ( 'NONE',  ( 6.339402847020720877, 0.7390441267520877489, -1.796137868246181046 ) ) ;
#192078=CARTESIAN_POINT ( 'NONE',  ( 6.029554895997981667, -0.2579198037528374066, 2.104758538420265168 ) ) ;
#192080=CARTESIAN_POINT ( 'NONE',  ( 3.967365900211225593, -1.591558630706500832, -1.059764132600553355 ) ) ;
#192084=CARTESIAN_POINT ( 'NONE',  ( 5.619794420184654804, -0.4867899507037063422, 1.953244479579784976 ) ) ;
#192086=CARTESIAN_POINT ( 'NONE',  ( 5.672426548614882158, -1.154804106291613675, 1.414059844683832834 ) ) ;
#192087=CARTESIAN_POINT ( 'NONE',  ( 5.682827415814322158, 1.645762192317705486, -1.164983060713747909 ) ) ;
#192088=CARTESIAN_POINT ( 'NONE',  ( 1.434126425884488354, 1.231690216755284562, 1.664001042209894088 ) ) ;
#192092=CARTESIAN_POINT ( 'NONE',  ( 6.297708355432167338, -0.6282832542035889922, 1.762108908958268216 ) ) ;
#192094=SURFACE_SIDE_STYLE ('',( #208349 ) ) ;
#192100=FILL_AREA_STYLE ('',( #128289 ) ) ;
#192102=CARTESIAN_POINT ( 'NONE',  ( 3.357800782942537143, 0.03855433513636970927, -1.733892557700001502 ) ) ;
#192104=CARTESIAN_POINT ( 'NONE',  ( 2.149362472714404504, 1.803301116200561882, -1.016697834320609894 ) ) ;
#192106=CARTESIAN_POINT ( 'NONE',  ( 2.970428505833659472, -2.086373159142587586, -0.3592635996705355050 ) ) ;
#192110=CARTESIAN_POINT ( 'NONE',  ( 0.9714669389824581724, -0.2943045352901324518, 1.947222615934702139 ) ) ;
#192115=CARTESIAN_POINT ( 'NONE',  ( 3.855682016854941274, 2.275109001451373292, -0.2794487578934058969 ) ) ;
#192116=CARTESIAN_POINT ( 'NONE',  ( 1.137010146156680834, -1.651496384925277283, 0.7785749969668461778 ) ) ;
#192117=CARTESIAN_POINT ( 'NONE',  ( 2.882959773793275726, -1.768624019741386277, -0.7279546805132871556 ) ) ;
#192121=CARTESIAN_POINT ( 'NONE',  ( 2.162360077456865870, 2.012843401649004882, 0.04526349954376075735 ) ) ;
#192122=CARTESIAN_POINT ( 'NONE',  ( 2.078885752709497492, 1.828579749420868872, 0.7109141669488158177 ) ) ;
#192126=CARTESIAN_POINT ( 'NONE',  ( 0.1751657365761495888, 6.947016338497860488, -2.639079955608885975 ) ) ;
#192127=CARTESIAN_POINT ( 'NONE',  ( 5.560518711993346130, -1.889693770910952253, -0.8946095687128383656 ) ) ;
#192128=CARTESIAN_POINT ( 'NONE',  ( 3.906921071489596997, 1.517988030950194744, 0.9097272527330434455 ) ) ;
#192130=CARTESIAN_POINT ( 'NONE',  ( 6.105493113454719456, -2.275700256682281264, 0.2746985183333852110 ) ) ;
#192131=CARTESIAN_POINT ( 'NONE',  ( 5.419757389058348807, 1.032087642559690543, -1.401099660988463169 ) ) ;
#192134=CARTESIAN_POINT ( 'NONE',  ( 5.975915019019427454, 1.530855338724030457, 0.8140783706773281336 ) ) ;
#192135=CARTESIAN_POINT ( 'NONE',  ( 5.705598495378635171, -1.708133787927707647, -1.340148157549289953 ) ) ;
#192137=CARTESIAN_POINT ( 'NONE',  ( 6.421112215724263272, -1.799107166270615732, 0.9110519380226205222 ) ) ;
#192138=CARTESIAN_POINT ( 'NONE',  ( 4.687500000000003553, -1.451031289060926488, 1.451031289061301521 ) ) ;
#192141=CARTESIAN_POINT ( 'NONE',  ( 3.768508550381458821, -1.294476758928708060, 1.426794059921440594 ) ) ;
#192143=CARTESIAN_POINT ( 'NONE',  ( -0.03994651564155191764, -1.721383993196375251, -1.403517996469628493 ) ) ;
#192148=CARTESIAN_POINT ( 'NONE',  ( 2.297798353768167434, 2.029563722251678026, -0.9032078376340900716 ) ) ;
#192154=CARTESIAN_POINT ( 'NONE',  ( 1.213517774399593740, 1.944071949784083264, 0.5350861613380719639 ) ) ;
#192156=CARTESIAN_POINT ( 'NONE',  ( 5.090308526370699305, 1.063348096890677441, -1.767349029039886110 ) ) ;
#192162=CARTESIAN_POINT ( 'NONE',  ( 0.7371257246046484246, -1.245724469572104587, -1.257322912719664787 ) ) ;
#192163=CARTESIAN_POINT ( 'NONE',  ( 5.854130254062820171, 0.1179724184225266898, -1.730206517700397795 ) ) ;
#192164=CARTESIAN_POINT ( 'NONE',  ( 5.513164599239865460, -1.696177307367072506, 0.3892859123911066588 ) ) ;
#192165=CARTESIAN_POINT ( 'NONE',  ( 2.683473709500754367, 1.623236604230539282, 1.618912294457574674 ) ) ;
#192167=CARTESIAN_POINT ( 'NONE',  ( 1.763359053103892293, 0.9455654613358072114, 1.579637215005654349 ) ) ;
#192170=CARTESIAN_POINT ( 'NONE',  ( 2.537895388257872753, 0.8626947210231518115, -1.608888323311054691 ) ) ;
#192171=CARTESIAN_POINT ( 'NONE',  ( 3.322888845334175389, 0.9041102021897020613, -1.802417075407992897 ) ) ;
#192174=CARTESIAN_POINT ( 'NONE',  ( 5.965875410913440646, 2.075401660611264631, -0.3564754433343624296 ) ) ;
#192177=CARTESIAN_POINT ( 'NONE',  ( 2.172408243068229439, -0.9739482337229148357, -1.826950231780352762 ) ) ;
#192180=CARTESIAN_POINT ( 'NONE',  ( 5.022192282182047940, -2.110239842997441606, 0.2083548542347323507 ) ) ;
#192181=CARTESIAN_POINT ( 'NONE',  ( 1.418447215319606602, 1.294224929256732493, -1.427187236927564440 ) ) ;
#192188=CARTESIAN_POINT ( 'NONE',  ( 6.293239850429793947, -0.1054838202379469042, -2.118119863012501991 ) ) ;
#192189=CARTESIAN_POINT ( 'NONE',  ( 2.327300794530688055, -0.001011052439145453856, 2.106147100168444197 ) ) ;
#192192=CARTESIAN_POINT ( 'NONE',  ( 6.596546450148484730, 1.840605976333910654, 0.2736291870141689397 ) ) ;
#192198=CARTESIAN_POINT ( 'NONE',  ( -0.08743476694611679312, -2.120266877281291595, -0.04547849331201780226 ) ) ;
#192201=CARTESIAN_POINT ( 'NONE',  ( 2.031626174157370457, 1.878314540015123102, -0.5664888411779643862 ) ) ;
#192202=CARTESIAN_POINT ( 'NONE',  ( 1.129994055010040022, -1.371941552271437770, -1.670562328977095445 ) ) ;
#192206=CARTESIAN_POINT ( 'NONE',  ( 4.411323335215872277, 0.4626541248624673752, 1.670896574705359461 ) ) ;
#192207=CARTESIAN_POINT ( 'NONE',  ( 2.290578643201816256, 1.344622755191619445, 1.104862870798990260 ) ) ;
#192210=CARTESIAN_POINT ( 'NONE',  ( 2.003279617838377824, 1.993765885540278004, 0.2985825316763612847 ) ) ;
#192213=CARTESIAN_POINT ( 'NONE',  ( 1.287891803077842345, -0.8884654817012342942, 1.759997859036799284 ) ) ;
#192215=CARTESIAN_POINT ( 'NONE',  ( 5.537344615273096515, -0.04053095765194079242, 1.912125305397804009 ) ) ;
#192220=CARTESIAN_POINT ( 'NONE',  ( 1.330729578248716960, 1.354828421643257119, -1.498027418808007605 ) ) ;
#192222=CARTESIAN_POINT ( 'NONE',  ( 6.053837855137599533, 0.6775820993057954933, -2.205875079116952797 ) ) ;
#192223=CARTESIAN_POINT ( 'NONE',  ( 5.582460749670235423, 1.169929261559121247, -1.574690175210855747 ) ) ;
#192224=CARTESIAN_POINT ( 'NONE',  ( 2.852341167582587378, -1.956174252073937359, -0.1491622203949396763 ) ) ;
#192226=CARTESIAN_POINT ( 'NONE',  ( 0.6685925339881376717, 1.356301626434471164, 1.492253803477984864 ) ) ;
#192228=CARTESIAN_POINT ( 'NONE',  ( 1.253280101782401124, 0.1498745247594003016, -2.112069961602327517 ) ) ;
#192231=CARTESIAN_POINT ( 'NONE',  ( 2.536835285771391835, -1.364265644482412387, -1.236541980112846328 ) ) ;
#192234=CARTESIAN_POINT ( 'NONE',  ( 3.076547362214879566, 0.9570632234598417387, 1.892448740577145738 ) ) ;
#192239=CARTESIAN_POINT ( 'NONE',  ( 3.286453515990275243, -2.029689310919643219, -0.3557144749045982879 ) ) ;
#192241=CARTESIAN_POINT ( 'NONE',  ( 0.7668492355173107677, 1.774547462407764842, -0.4907661837717376407 ) ) ;
#192245=CARTESIAN_POINT ( 'NONE',  ( 0.7685542157043163680, 1.090964843879228097, 1.918292034055509632 ) ) ;
#192246=CARTESIAN_POINT ( 'NONE',  ( 3.146068640573984165, 0.8174054641026907708, -2.109740015476600838 ) ) ;
#192248=CARTESIAN_POINT ( 'NONE',  ( 2.988311359655666077, -1.075548189349010864, 1.457604102852279926 ) ) ;
#192249=CARTESIAN_POINT ( 'NONE',  ( 3.045994482203842502, 0.8657459236516149570, 1.709044100283881429 ) ) ;
#192250=CARTESIAN_POINT ( 'NONE',  ( 4.211429588753928144, -1.719575573843846072, -1.152724658989822348 ) ) ;
#192252=CARTESIAN_POINT ( 'NONE',  ( 3.168780698033875076, -1.820990468880798296, -0.7558852700480926945 ) ) ;
#192253=CARTESIAN_POINT ( 'NONE',  ( 6.322878010905701451, 1.798576545740763644, 0.6907619847127777213 ) ) ;
#192254=CARTESIAN_POINT ( 'NONE',  ( 2.799504582125960095, -0.5885537693137884441, 1.775713401224961574 ) ) ;
#192255=CARTESIAN_POINT ( 'NONE',  ( 2.526355290359350025, -1.329941221805782892, -1.885751665715528880 ) ) ;
#192257=CARTESIAN_POINT ( 'NONE',  ( 3.103785861066649776, 0.6724651444435655323, -1.735490194124859054 ) ) ;
#192260=CARTESIAN_POINT ( 'NONE',  ( 6.514137810226229064, 2.057410315668557921, -0.1480156956644717581 ) ) ;
#192265=CARTESIAN_POINT ( 'NONE',  ( 1.032015147355441309, -1.337601665653989302, -1.626754097558680057 ) ) ;
#192267=CARTESIAN_POINT ( 'NONE',  ( 6.555963963954187790, 2.156316573842661732, -0.1517529999496904924 ) ) ;
#192268=CARTESIAN_POINT ( 'NONE',  ( -0.2106725631050176961, -0.004273297132588448587, -2.003483006309704439 ) ) ;
#192272=CARTESIAN_POINT ( 'NONE',  ( 6.925078400183548588, 0.0006614011395407459748, 1.855452278108092656 ) ) ;
#192274=CARTESIAN_POINT ( 'NONE',  ( -0.2104748580754166598, -0.006608320950483163522, -2.103482951484026753 ) ) ;
#192275=CARTESIAN_POINT ( 'NONE',  ( 4.382046175016578005, -2.016188710442788246, -0.04465648322755921829 ) ) ;
#192279=CARTESIAN_POINT ( 'NONE',  ( 6.543834100630380846, 0.8322713294773576020, -1.995267709627518427 ) ) ;
#192284=CARTESIAN_POINT ( 'NONE',  ( 6.468375372808552903, -1.978050569928070379, -0.3905794195708453542 ) ) ;
#192286=CARTESIAN_POINT ( 'NONE',  ( 6.883263157960367806, 6.035304072343574688, 2.648703854151325032 ) ) ;
#192288=CARTESIAN_POINT ( 'NONE',  ( 1.242334483997083572, 0.3330332824765611099, 1.692230457194281223 ) ) ;
#192292=CARTESIAN_POINT ( 'NONE',  ( 0.5789240690485557561, 1.654349777479852346, -0.6291145533634836529 ) ) ;
#192293=CARTESIAN_POINT ( 'NONE',  ( 2.350245942676463695, 0.9471468416194218642, -1.776342852653712168 ) ) ;
#192295=CARTESIAN_POINT ( 'NONE',  ( 3.839080194659278966, 0.3211572903306300075, 2.183152695405643051 ) ) ;
#192297=CARTESIAN_POINT ( 'NONE',  ( 4.838842012204412235, -2.104300398676747896, -0.5337788192065362480 ) ) ;
#192301=CARTESIAN_POINT ( 'NONE',  ( 3.158948766716848766, 0.5171890032967979556, 2.056314737185329644 ) ) ;
#192302=CARTESIAN_POINT ( 'NONE',  ( 2.794546173781168541, 1.458544728081469177, -1.392559875802508396 ) ) ;
#192303=CARTESIAN_POINT ( 'NONE',  ( 3.779414081507098011, 0.2159278537227064809, -1.798573134706340504 ) ) ;
#192307=CARTESIAN_POINT ( 'NONE',  ( 0.4087956859853311142, 1.625333209436867321, 0.9259686016569528277 ) ) ;
#192310=CARTESIAN_POINT ( 'NONE',  ( 6.252569598636129378, 0.5776572744066664766, 1.731972519516040032 ) ) ;
#192312=CARTESIAN_POINT ( 'NONE',  ( 1.006889752881213296, -0.04349654304135543159, 1.915380135637449799 ) ) ;
#192317=CARTESIAN_POINT ( 'NONE',  ( 5.506754051192107369, 1.639644015412666800, -1.408845030788405506 ) ) ;
#192320=CARTESIAN_POINT ( 'NONE',  ( 3.480829117359967917, -1.421471314662653196, 1.573842340227212366 ) ) ;
#192321=CARTESIAN_POINT ( 'NONE',  ( -0.1298852118743893114, 2.060165343084968459, -2.144168685196511159 ) ) ;
#192323=CARTESIAN_POINT ( 'NONE',  ( 4.341064969683814390, -1.716640784620737659, 0.9690559893368445588 ) ) ;
#192324=CARTESIAN_POINT ( 'NONE',  ( 6.047114369478562956, 0.1942372860762129894, 1.902532258075719351 ) ) ;
#192326=CARTESIAN_POINT ( 'NONE',  ( 5.717987565503318770, 1.041469840191568963, -1.843387895306993318 ) ) ;
#192328=CARTESIAN_POINT ( 'NONE',  ( 0.3442982867475213871, -0.9772804826688463731, 1.825211318103404867 ) ) ;
#192329=CARTESIAN_POINT ( 'NONE',  ( 2.413922445368326564, 1.268163163618090561, -1.470779158573028322 ) ) ;
#192333=CARTESIAN_POINT ( 'NONE',  ( 3.380887635974954453, 1.889918501611790536, -0.8941524261326051493 ) ) ;
#192336=CARTESIAN_POINT ( 'NONE',  ( 0.9260600326868747567, -0.8135480099433598511, -1.618595788997332363 ) ) ;
#192338=CARTESIAN_POINT ( 'NONE',  ( 5.391335350415090488, 1.947751002805158560, -1.037606470750504606 ) ) ;
#192340=CARTESIAN_POINT ( 'NONE',  ( 3.382038520680182181, 1.398480293485371284, 1.707083182650385389 ) ) ;
#192343=CARTESIAN_POINT ( 'NONE',  ( 1.436035868020806738, -1.063167577064242142, -1.589284522738307448 ) ) ;
#192345=CARTESIAN_POINT ( 'NONE',  ( 4.773920332862017446, -2.031068740936771366, 0.4005940302675218834 ) ) ;
#192347=CARTESIAN_POINT ( 'NONE',  ( 2.782270202741622178, -1.112240752214749273, 1.853481441253836071 ) ) ;
#192348=CARTESIAN_POINT ( 'NONE',  ( 4.616832073239669043, -0.1072513232249286408, 2.189039617437993357 ) ) ;
#192359=CARTESIAN_POINT ( 'NONE',  ( 5.805552407531882508, -1.628464769346991581, -1.278160613847306504 ) ) ;
#192360=CARTESIAN_POINT ( 'NONE',  ( 4.740804336882096237, 0.3310356755545171836, 1.897698676112127725 ) ) ;
#192361=CARTESIAN_POINT ( 'NONE',  ( 6.327753876788817955, 0.8101538176374730726, -1.956283944203747849 ) ) ;
#192364=CARTESIAN_POINT ( 'NONE',  ( 4.821133434317745881, -1.757446901322982979, -0.8890814742016742711 ) ) ;
#192365=CARTESIAN_POINT ( 'NONE',  ( 0.6565081633774123571, -1.584678946828571133, 1.513927167823600595 ) ) ;
#192366=CARTESIAN_POINT ( 'NONE',  ( 3.809063337113669068, 1.566667275063510445, 0.9371452329686792426 ) ) ;
#192374=( BOUNDED_SURFACE ( )  B_SPLINE_SURFACE ( 3, 3, ( 
 ( #148075, #118818, #147022, #33240, #66768, #31132, #97207, #34301, #99323, #67838, #116681 ),
 ( #80931, #165373, #132909, #14841, #85188, #133984, #131856, #117764, #213045, #51640, #167513 ),
 ( #114567, #115616, #16966, #2844, #100374, #163259, #196811, #48454, #84123, #166444, #19110 ),
 ( #198914, #183754, #35364, #135033, #101439, #18036, #151271, #201046, #83047, #52689, #180559 ),
 ( #32181, #149122, #15905, #214081, #704, #197863, #170706, #72121, #36434, #43671, #186950 ),
 ( #87330, #11127, #137162, #73191, #203186, #138229, #55894, #54832, #56963, #23374, #154472 ),
 ( #185872, #153397, #69977, #60964, #77205, #53765, #3907, #155539, #89484, #71046, #184805 ) ),
 .UNSPECIFIED., .T., .F., .T. ) 
 B_SPLINE_SURFACE_WITH_KNOTS ( ( 4, 3, 4 ),
 ( 4, 1, 1, 1, 1, 1, 1, 1, 4 ),
 ( 0.000000000000000000, 0.5000000000000000000, 1.000000000000000000 ),
 ( 0.000000000000000000, 0.2255619619413396781, 0.3975297875667437308, 0.5250373104567740423, 0.6172314665434700531, 0.6832587661106447330, 0.7322037845459880012, 0.7729093456892226488, 1.000000000000000000 ),
 .UNSPECIFIED. ) 
 GEOMETRIC_REPRESENTATION_ITEM ( )  RATIONAL_B_SPLINE_SURFACE ( (
 ( 1.000000000000000000, 1.000000000000000000, 1.000000000000000444, 0.9999999999999996669, 1.000000000000000222, 0.9999999999999996669, 1.000000000000000444, 1.000000000000000000, 1.000000000000000000, 1.000000000000000000, 1.000000000000000000),
 ( 0.3333333333333333703, 0.3333333333333333703, 0.3333333333333334814, 0.3333333333333332038, 0.3333333333333333703, 0.3333333333333332593, 0.3333333333333334814, 0.3333333333333333703, 0.3333333333333334814, 0.3333333333333333703, 0.3333333333333333703),
 ( 0.3333333333333333703, 0.3333333333333333703, 0.3333333333333334814, 0.3333333333333332038, 0.3333333333333333703, 0.3333333333333332593, 0.3333333333333334814, 0.3333333333333333703, 0.3333333333333334814, 0.3333333333333333703, 0.3333333333333333703),
 ( 1.000000000000000000, 1.000000000000000000, 1.000000000000000444, 0.9999999999999996669, 1.000000000000000222, 0.9999999999999996669, 1.000000000000000444, 1.000000000000000000, 1.000000000000000000, 1.000000000000000000, 1.000000000000000000),
 ( 0.3333333333333333703, 0.3333333333333333703, 0.3333333333333334814, 0.3333333333333332038, 0.3333333333333333703, 0.3333333333333332593, 0.3333333333333334814, 0.3333333333333333703, 0.3333333333333334814, 0.3333333333333333703, 0.3333333333333333703),
 ( 0.3333333333333333703, 0.3333333333333333703, 0.3333333333333334814, 0.3333333333333332038, 0.3333333333333333703, 0.3333333333333332593, 0.3333333333333334814, 0.3333333333333333703, 0.3333333333333334814, 0.3333333333333333703, 0.3333333333333333703),
 ( 1.000000000000000000, 1.000000000000000000, 1.000000000000000444, 0.9999999999999996669, 1.000000000000000222, 0.9999999999999996669, 1.000000000000000444, 1.000000000000000000, 1.000000000000000000, 1.000000000000000000, 1.000000000000000000) ) ) 
 REPRESENTATION_ITEM ( '' )  SURFACE ( )  );
#192376=CARTESIAN_POINT ( 'NONE',  ( 3.175182228840720988, 1.170341537027960843, 1.421418621496411516 ) ) ;
#192377=CARTESIAN_POINT ( 'NONE',  ( 5.115494517658178530, 1.648350763777502559, 1.155591226287083328 ) ) ;
#192378=CARTESIAN_POINT ( 'NONE',  ( 0.9490539546192258147, 1.544862702020805223, 1.701928257493188434 ) ) ;
#192379=CARTESIAN_POINT ( 'NONE',  ( 5.647302737930705696, 1.731814717071546772, -0.9215059220915235993 ) ) ;
#192384=CARTESIAN_POINT ( 'NONE',  ( 0.5552397518338060278, 1.722184604005328357, -1.148819969904082861 ) ) ;
#192386=CARTESIAN_POINT ( 'NONE',  ( 1.153981415136243527, 0.8505622500237058903, 1.910110313709513674 ) ) ;
#192387=CARTESIAN_POINT ( 'NONE',  ( 0.2505829665140328899, -1.505242420826727656, 1.110479572284161831 ) ) ;
#192389=CARTESIAN_POINT ( 'NONE',  ( -0.1104750535120268551, 0.2303756098476944791, -2.137063993957021513 ) ) ;
#192390=CARTESIAN_POINT ( 'NONE',  ( 1.962089020239773163, -1.591546648218734816, -0.7047476087739585893 ) ) ;
#192394=CARTESIAN_POINT ( 'NONE',  ( 2.982692045960423588, -0.1271664282922572997, -1.720251185527998272 ) ) ;
#192395=CARTESIAN_POINT ( 'NONE',  ( 2.296645709751913955, 1.758124065145909798, -1.308193547052277861 ) ) ;
#192396=CARTESIAN_POINT ( 'NONE',  ( 5.373716497573798101, 2.127666891504222058, -0.5857064233696291922 ) ) ;
#192398=CARTESIAN_POINT ( 'NONE',  ( 3.045941508711128787, 1.532170317875800603, 1.538426465386952380 ) ) ;
#192399=CARTESIAN_POINT ( 'NONE',  ( 0.6447967512687136082, -1.567379569643694515, 0.9359695128687425258 ) ) ;
#192400=CARTESIAN_POINT ( 'NONE',  ( 3.063770578283632862, 1.346675374253442969, 1.633852266970806211 ) ) ;
#192401=CARTESIAN_POINT ( 'NONE',  ( 6.539320575229250032, 3.707580029678263944, 2.311356139567366963 ) ) ;
#192404=CARTESIAN_POINT ( 'NONE',  ( 3.456809812625420975, -2.022294432149398080, -1.079448172897869540 ) ) ;
#192408=CARTESIAN_POINT ( 'NONE',  ( 6.410783699188008278, -0.5891560598917375824, -2.141663135048486044 ) ) ;
#192415=CARTESIAN_POINT ( 'NONE',  ( 4.166638809851969327, 1.319227567334404494, 1.525044649537968589 ) ) ;
#192417=CARTESIAN_POINT ( 'NONE',  ( 1.674751860914457824, 1.388166878297650397, -1.525640323027994683 ) ) ;
#192423=CARTESIAN_POINT ( 'NONE',  ( 4.804715953495782621, 1.905792977913090214, 1.081705336968781239 ) ) ;
#192424=CARTESIAN_POINT ( 'NONE',  ( 2.637342451166882373, 0.6819965276749391236, 1.897697610567940174 ) ) ;
#192425=CARTESIAN_POINT ( 'NONE',  ( 2.278628554356322500, 1.682734121078124812, -0.7478279864501293783 ) ) ;
#192427=CARTESIAN_POINT ( 'NONE',  ( 5.948246703923279810, 1.823645139926059144, 0.08696428134234018836 ) ) ;
#192429=CARTESIAN_POINT ( 'NONE',  ( 6.262609139476608355, -1.605266756365858027, 1.594658822776671592 ) ) ;
#192431=CARTESIAN_POINT ( 'NONE',  ( 1.858176280533967661, 2.100347624109857758, -0.1560452747076390423 ) ) ;
#192437=UNCERTAINTY_MEASURE_WITH_UNIT (LENGTH_MEASURE( 1.000000000000000082E-05 ), #50885, 'distance_accuracy_value', 'NONE');
#192442=CARTESIAN_POINT ( 'NONE',  ( 1.424255164902767934, -2.103954720533041556, 0.2648648325892372646 ) ) ;
#192443=CARTESIAN_POINT ( 'NONE',  ( 2.900855728284880808, -2.189247779298031826, -0.3757519495388698672 ) ) ;
#192444=CARTESIAN_POINT ( 'NONE',  ( 0.6455096168876961471, -1.890800792967793686, 1.137844069391671820 ) ) ;
#192447=CARTESIAN_POINT ( 'NONE',  ( 4.668382477721988444, -0.8370036265390871089, -1.774476930476886594 ) ) ;
#192455=CARTESIAN_POINT ( 'NONE',  ( 3.586284538990120119, 1.181046903802231984, 1.761068336431830472 ) ) ;
#192457=CARTESIAN_POINT ( 'NONE',  ( 4.540002997438313592, 0.9271085556134452954, -1.952944755896801610 ) ) ;
#192458=CARTESIAN_POINT ( 'NONE',  ( 4.212339636135824961, 1.685202893791247769, 0.7422218904534692019 ) ) ;
#192462=CARTESIAN_POINT ( 'NONE',  ( 5.648340061037051107, -1.368025295233719074, 1.075653158840290891 ) ) ;
#192467=CARTESIAN_POINT ( 'NONE',  ( 2.940462584922590938, 2.145230175562794717, 0.2658940370997217584 ) ) ;
#192468=CARTESIAN_POINT ( 'NONE',  ( 5.993517489292202960, 1.942244631591660164, 0.5404061186519912852 ) ) ;
#192470=CARTESIAN_POINT ( 'NONE',  ( 2.290102563249151402, -0.9248296759884739870, 1.954025333243500917 ) ) ;
#192471=CARTESIAN_POINT ( 'NONE',  ( 4.288322324034578692, -1.949444798393678013, -0.2924651067536877536 ) ) ;
#192472=CARTESIAN_POINT ( 'NONE',  ( 0.02921319935947005314, -2.001080581411585513, 0.8940957790435491992 ) ) ;
#192473=CARTESIAN_POINT ( 'NONE',  ( 0.08353690965077953390, -0.1615750995121113531, -2.271551823106517709 ) ) ;
#192474=CARTESIAN_POINT ( 'NONE',  ( 4.388185931656235717, -0.4287674410733510744, -1.893983405979382306 ) ) ;
#192483=CARTESIAN_POINT ( 'NONE',  ( 2.643839551151895506, -1.634601560588926361, -1.482707865360691990 ) ) ;
#192485=CARTESIAN_POINT ( 'NONE',  ( 6.473494419632052299, -0.2434444386649399217, 1.946554233954982172 ) ) ;
#192491=CARTESIAN_POINT ( 'NONE',  ( 5.701068745948241201, -0.4431999317857804876, 1.786873912291174538 ) ) ;
#192496=CARTESIAN_POINT ( 'NONE',  ( 5.976833544478475702, -1.498421880457675215, 1.500811427713820478 ) ) ;
#192500=CARTESIAN_POINT ( 'NONE',  ( 6.626252497008212394, 1.190392663088507552, -1.681986249806742384 ) ) ;
#192502=CARTESIAN_POINT ( 'NONE',  ( 2.435812105726247623, 1.142245297582837882, 1.469210208790121763 ) ) ;
#192503=CARTESIAN_POINT ( 'NONE',  ( 4.388128076750056117, -0.4078595375654435751, -1.795341762384855544 ) ) ;
#192509=CARTESIAN_POINT ( 'NONE',  ( 4.108205984530819421, -2.201057848371779535, 0.1611738814469021175 ) ) ;
#192510=CARTESIAN_POINT ( 'NONE',  ( 5.641944544108610238, 0.9243782401199867049, -2.065144452299176425 ) ) ;
#192512=CARTESIAN_POINT ( 'NONE',  ( 6.205303291940151844, 1.571521137685438108, -0.9011181087926769528 ) ) ;
#192513=CARTESIAN_POINT ( 'NONE',  ( -0.04763828917917976857, -1.313539345393003321, 1.530161206715647149 ) ) ;
#192516=CARTESIAN_POINT ( 'NONE',  ( 6.024064539286675846, -1.897261554996135802, 0.2387622092476364699 ) ) ;
#192518=CARTESIAN_POINT ( 'NONE',  ( 1.199835987674138460, -1.870836310881810682, -0.003643258294119822160 ) ) ;
#192519=CARTESIAN_POINT ( 'NONE',  ( 0.8664231474371618669, -1.968446048378743152, -0.4370742218882398000 ) ) ;
#192521=CARTESIAN_POINT ( 'NONE',  ( 3.492891347888595455, -0.4109570828031941514, -2.065403110348571492 ) ) ;
#192526=CARTESIAN_POINT ( 'NONE',  ( 2.847920605731304011, -1.359688658692468355, -1.493726022120341224 ) ) ;
#192529=CARTESIAN_POINT ( 'NONE',  ( 4.604844690042746436, 1.674155836469687575, -1.367402732809947397 ) ) ;
#192535=CARTESIAN_POINT ( 'NONE',  ( 1.381551413260760031, -0.05389312200515179035, 2.170675147484208534 ) ) ;
#192538=CARTESIAN_POINT ( 'NONE',  ( 0.4328342922346357646, -1.301571265828086688, -1.302605208699902928 ) ) ;
#192541=CARTESIAN_POINT ( 'NONE',  ( 1.839652601550560096, 0.8350199954420146620, -2.026445374841173930 ) ) ;
#192543=CARTESIAN_POINT ( 'NONE',  ( 2.659333574217698004, -1.968172486592324244, -1.115815620033432154 ) ) ;
#192549=CARTESIAN_POINT ( 'NONE',  ( 4.059615542810626643, 1.756569389245852042, -0.2146349482602862846 ) ) ;
#192551=CARTESIAN_POINT ( 'NONE',  ( 1.272647984039422697, -1.336331724779236119, 1.627640044824183674 ) ) ;
#192555=CARTESIAN_POINT ( 'NONE',  ( 6.134388704033759687, 0.6352148712998658686, 1.913799669303432927 ) ) ;
#192560=CARTESIAN_POINT ( 'NONE',  ( 4.047608660086319254, 0.6306619223146043840, -1.761260876548931709 ) ) ;
#192561=CARTESIAN_POINT ( 'NONE',  ( 4.961816271168415504, -0.5573412460852051886, 1.993729458732765858 ) ) ;
#192569=CARTESIAN_POINT ( 'NONE',  ( 4.457442142980160504, 1.574409630067734156, 1.170308293268598421 ) ) ;
#192570=CARTESIAN_POINT ( 'NONE',  ( 0.7200771085676247463, -1.701685607325746252, -1.080902626906909747 ) ) ;
#192574=CARTESIAN_POINT ( 'NONE',  ( 1.440467042440606749, 0.3595057747620767907, 1.835501880432292010 ) ) ;
#192576=CARTESIAN_POINT ( 'NONE',  ( 3.146742683403806140, 1.965092980649842502, 0.4368759242464967940 ) ) ;
#192578=CARTESIAN_POINT ( 'NONE',  ( 3.585668865097063840, -0.6122912394212923770, 2.026781372153120930 ) ) ;
#192580=CARTESIAN_POINT ( 'NONE',  ( 4.844224204019831781, -0.9789346907586125024, 1.824324395707350943 ) ) ;
#192582=CARTESIAN_POINT ( 'NONE',  ( 6.527293198192279711, -1.364605693714017187, -1.583936087800744907 ) ) ;
#192584=CARTESIAN_POINT ( 'NONE',  ( 5.262654937129007671, -1.321179299781930938, 1.260103332352560779 ) ) ;
#192589=CARTESIAN_POINT ( 'NONE',  ( 6.053802686139254874, 0.6462426183462595120, -2.110027337871730690 ) ) ;
#192591=CARTESIAN_POINT ( 'NONE',  ( 5.619756671179353624, -0.4603523440993940175, 1.855926886426212175 ) ) ;
#192603=CARTESIAN_POINT ( 'NONE',  ( 0.07700591528353968596, 0.003617085621422307627, -1.910863332519038282 ) ) ;
#192606=CARTESIAN_POINT ( 'NONE',  ( -0.1405533004718494683, 0.2440837993472090295, -1.754028569132993542 ) ) ;
#192609=CARTESIAN_POINT ( 'NONE',  ( 2.518351277774394159, 0.8375136450692384216, 1.782609909039992946 ) ) ;
#192610=CARTESIAN_POINT ( 'NONE',  ( 3.198842376697589085, 1.824128004127192337, 0.8596145101084637918 ) ) ;
#192613=CARTESIAN_POINT ( 'NONE',  ( 6.827182134110192813, 3.687242579989722824, 2.603029107617850002 ) ) ;
#192615=CARTESIAN_POINT ( 'NONE',  ( 3.679775893577118318, -1.080384588543949809, 1.906543112819548913 ) ) ;
#192617=CARTESIAN_POINT ( 'NONE',  ( 2.151277967514260592, -1.545957563563664650, -1.149148694925563596 ) ) ;
#192620=CARTESIAN_POINT ( 'NONE',  ( 0.1329588055935760349, 7.629137130509077380, -2.445925914280167923 ) ) ;
#192627=CARTESIAN_POINT ( 'NONE',  ( 6.040549724581927293, -1.551790349881351450, 0.9907606852931831742 ) ) ;
#192628=CARTESIAN_POINT ( 'NONE',  ( 2.947904902976675068, -1.353543519239216897, -1.490266562291961749 ) ) ;
#192629=CARTESIAN_POINT ( 'NONE',  ( 4.095287530520356434, 1.233756528997317137, -1.939045446859017030 ) ) ;
#192630=CARTESIAN_POINT ( 'NONE',  ( -0.1290005225502676156, 1.324981729379502537, -2.425680704180297464 ) ) ;
#192631=CARTESIAN_POINT ( 'NONE',  ( 2.430303444995636664, -1.149418499707482999, 1.463420418157684422 ) ) ;
#192636=CARTESIAN_POINT ( 'NONE',  ( 4.511325128988150190, -2.050071535818901225, 0.4094859698564096706 ) ) ;
#192637=CARTESIAN_POINT ( 'NONE',  ( 3.854256360616271415, 0.6726810918341770140, 1.745705178215435582 ) ) ;
#192642=CARTESIAN_POINT ( 'NONE',  ( 5.690025311828595278, -0.7696446287084879323, 1.543740960907719950 ) ) ;
#192644=CARTESIAN_POINT ( 'NONE',  ( 1.916292283401900720, -1.133531090463487212, -1.312443884513394554 ) ) ;
#192648=CARTESIAN_POINT ( 'NONE',  ( 5.348546061712845301, -2.153812021095147688, -0.2729773376510102323 ) ) ;
#192649=CARTESIAN_POINT ( 'NONE',  ( 4.389149243953620605, 1.629682310347341456, -0.8231139397327084106 ) ) ;
#192650=CARTESIAN_POINT ( 'NONE',  ( 2.043732491806522056, 1.349072470436333715, 1.424505092005624807 ) ) ;
#192651=CARTESIAN_POINT ( 'NONE',  ( 6.333232048763643540, -1.701881231816049000, -1.259509043995930222 ) ) ;
#192655=CARTESIAN_POINT ( 'NONE',  ( 2.455864667332839257, -1.573010975769023601, -1.422207447652395373 ) ) ;
#192658=CARTESIAN_POINT ( 'NONE',  ( 0.8661811918178536907, -2.060611401584189650, 0.1992402130865863485 ) ) ;
#192661=CARTESIAN_POINT ( 'NONE',  ( 3.035994277891720827, -2.140246456218936721, 0.5942984311890684435 ) ) ;
#192663=CARTESIAN_POINT ( 'NONE',  ( 0.6866852740153045476, 1.883736933065732533, 1.317207514508748734 ) ) ;
#192665=CARTESIAN_POINT ( 'NONE',  ( 5.401261053844283566, -1.771754184838408630, 1.055722541708886020 ) ) ;
#192669=CARTESIAN_POINT ( 'NONE',  ( 0.2333540202161610289, 0.003568502611739353923, -2.045944795905803471 ) ) ;
#192670=CARTESIAN_POINT ( 'NONE',  ( 5.513187957602974976, -1.795010045117376496, 0.4093405989887277663 ) ) ;
#192672=CARTESIAN_POINT ( 'NONE',  ( -0.1106727585416227011, 0.2327126083698972114, -2.036986407471320426 ) ) ;
#192673=CARTESIAN_POINT ( 'NONE',  ( 2.590480338954644246, -0.2921314510030656453, -1.699667543312991747 ) ) ;
#192674=CARTESIAN_POINT ( 'NONE',  ( 1.253139057289072822, 0.1435168058863903751, -2.011451928166609893 ) ) ;
#192675=CARTESIAN_POINT ( 'NONE',  ( 3.112262249421397620, 0.05891664663748399922, 2.298092032709637689 ) ) ;
#192676=CARTESIAN_POINT ( 'NONE',  ( 2.108995328314038353, 1.677457623459570168, -1.518302342262042304 ) ) ;
#192677=CARTESIAN_POINT ( 'NONE',  ( 5.654936504234950867, -1.661008888676926309, 1.294703585725354156 ) ) ;
#192679=CARTESIAN_POINT ( 'NONE',  ( 3.919032125857401905, -0.1322120426517567060, 1.764875357724977167 ) ) ;
#192682=CARTESIAN_POINT ( 'NONE',  ( 6.075753635015332499, -1.229876075327457130, 1.934346496684937966 ) ) ;
#192683=CARTESIAN_POINT ( 'NONE',  ( 4.786955173189685553, 1.366302399619228947, 1.234289508136581892 ) ) ;
#192687=CARTESIAN_POINT ( 'NONE',  ( 4.523480939507462217, -1.347072049868164978, -1.728447516733351952 ) ) ;
#192690=CARTESIAN_POINT ( 'NONE',  ( 4.861816338261779613, -0.5554421346023461492, 1.994381909410049669 ) ) ;
#192691=CARTESIAN_POINT ( 'NONE',  ( 0.3039231887648624619, -1.082844287645868375, -1.700959134490941160 ) ) ;
#192693=CARTESIAN_POINT ( 'NONE',  ( 3.721244860960619683, -0.1409348896288381003, 1.921400582950444580 ) ) ;
#192696=CARTESIAN_POINT ( 'NONE',  ( 0.1939906290522614152, 2.069702213058471241, -0.8072921158600793179 ) ) ;
#192704=CARTESIAN_POINT ( 'NONE',  ( 1.662477996687723669, -0.7030478115006146833, -1.831755296705489977 ) ) ;
#192706=CARTESIAN_POINT ( 'NONE',  ( 6.596550757224428629, -0.5713381284546023009, -2.084776384472402100 ) ) ;
#192707=CARTESIAN_POINT ( 'NONE',  ( 5.476992472119650124, 1.812042599547862176, 0.7524171098330989516 ) ) ;
#192711=CARTESIAN_POINT ( 'NONE',  ( 6.016527291255574283, 1.455332790597754000, -1.598591904487467463 ) ) ;
#192712=CARTESIAN_POINT ( 'NONE',  ( -0.2106725631050176961, 2.017899180269961956, -2.418275446281520136 ) ) ;
#192716=CARTESIAN_POINT ( 'NONE',  ( 6.766873944267649321, -1.801439555086775002, -0.8010921537245048185 ) ) ;
#192717=CARTESIAN_POINT ( 'NONE',  ( 6.239525021605913047, -1.647457779603450634, -0.5405594386218066649 ) ) ;
#192719=CARTESIAN_POINT ( 'NONE',  ( 2.577880719133851084, -1.123996537731044354, 1.881222605751430521 ) ) ;
#192720=CARTESIAN_POINT ( 'NONE',  ( 4.717980713983113361, -2.264103904663441913, 0.4450920570577068247 ) ) ;
#192721=CARTESIAN_POINT ( 'NONE',  ( 6.081337768261708909, 1.905808788339557802, -0.7845383490599889820 ) ) ;
#192722=CARTESIAN_POINT ( 'NONE',  ( 0.6384921070224542916, -1.665899481912515245, 0.9977595643581302909 ) ) ;
#192725=CARTESIAN_POINT ( 'NONE',  ( 5.238584497427841491, 1.261362679698872169, -1.704546977916908457 ) ) ;
#192727=CARTESIAN_POINT ( 'NONE',  ( 2.707657903872981553, 1.899618770239443366, 0.6767133375917554483 ) ) ;
#192729=CARTESIAN_POINT ( 'NONE',  ( 6.053802686139254874, 0.6462426183462595120, -2.110027337871730690 ) ) ;
#192732=CARTESIAN_POINT ( 'NONE',  ( 0.2580658466875830337, 0.6954254843183353962, 1.688255465954719536 ) ) ;
#192738=CARTESIAN_POINT ( 'NONE',  ( 5.612203307022772591, -0.9243832361092527705, -1.842014774801424615 ) ) ;
#192740=CARTESIAN_POINT ( 'NONE',  ( -0.2108831679770961920, 2.882544375557041239, -2.385815782126240236 ) ) ;
#192743=CARTESIAN_POINT ( 'NONE',  ( 4.617835026475571425, -0.5366920026289195844, 1.946999912814169287 ) ) ;
#192748=CARTESIAN_POINT ( 'NONE',  ( 3.924726224964281140, 1.956320258297845172, 0.6483119717206936583 ) ) ;
#192749=CARTESIAN_POINT ( 'NONE',  ( 3.199842427594956185, 1.824118962040650604, 0.8596310190432244758 ) ) ;
#192751=CARTESIAN_POINT ( 'NONE',  ( 6.727182134110196721, 7.051813866762763006, 2.787205683092201181 ) ) ;
#192756=CARTESIAN_POINT ( 'NONE',  ( 3.057970071934034362, 1.730601471501746147, -1.034006501934421784 ) ) ;
#192757=CARTESIAN_POINT ( 'NONE',  ( 2.308333576337255000, 1.644441489820291924, 0.8281405146027611686 ) ) ;
#192758=CARTESIAN_POINT ( 'NONE',  ( 1.190513350481865240, -1.033627929232444620, 2.063343651489284003 ) ) ;
#192760=CARTESIAN_POINT ( 'NONE',  ( 3.058072297120766336, 2.151488047868503894, -0.2085137855245971505 ) ) ;
#192764=CARTESIAN_POINT ( 'NONE',  ( 0.7427767429722329506, -1.606530860214189893, 0.9580933318182258684 ) ) ;
#192766=CARTESIAN_POINT ( 'NONE',  ( 5.295764336479223289, -0.7102129355434207980, 1.839261741220117097 ) ) ;
#192770=CARTESIAN_POINT ( 'NONE',  ( 0.1181803206181560040, -2.163391993613572151, 0.4351206515559591370 ) ) ;
#192775=CARTESIAN_POINT ( 'NONE',  ( 6.539320575229239374, 3.684509595994990061, 2.717302710099603225 ) ) ;
#192776=CARTESIAN_POINT ( 'NONE',  ( 4.856303703212550893, 0.7536814072931929953, 1.821903339724652460 ) ) ;
#192777=CARTESIAN_POINT ( 'NONE',  ( 6.170177014438331220, 2.014108787598484440, -0.1525786406279260876 ) ) ;
#192779=CARTESIAN_POINT ( 'NONE',  ( 5.004635055918612352, -0.7736033420917761694, -2.174287598079288841 ) ) ;
#192780=CARTESIAN_POINT ( 'NONE',  ( 1.727463565662648026, 0.1559948080240464718, -2.056756566214789306 ) ) ;
#192787=CARTESIAN_POINT ( 'NONE',  ( 5.020078820186387070, 2.148262114505914866, -0.3138009609788168230 ) ) ;
#192788=CARTESIAN_POINT ( 'NONE',  ( 3.010954138651841916, 0.05432569772663429358, 2.015980714967258614 ) ) ;
#192790=CARTESIAN_POINT ( 'NONE',  ( 4.528748383445759806, -1.681502307688139908, 0.7506017836093890061 ) ) ;
#192793=CARTESIAN_POINT ( 'NONE',  ( 5.056268342064010213, -1.587557771011731678, 1.511049258477934032 ) ) ;
#192795=CARTESIAN_POINT ( 'NONE',  ( 5.629810878523249684, -1.430378642458853378, -1.753011776973804725 ) ) ;
#192801=( BOUNDED_SURFACE ( )  B_SPLINE_SURFACE ( 3, 3, ( 
 ( #188251, #60390, #138462, #204482, #39892, #106002, #78770, #97190, #144893, #79842, #65692, #176297, #209828, #47375, #178430, #13766, #129754, #95056, #160036, #161106, #143832, #30038, #32166, #11639, #179494, #110288, #113487, #14826, #210901, #61464, #48437, #147007, #98244, #77711, #96124, #64659, #12694, #177358, #127630, #162179, #112417, #145951, #130803, #15887, #31117, #211961, #197848, #62528, #28972, #128689, #194658, #46302, #93995, #63600, #193596, #195739, #196795, #163243, #80917, #213025, #114552, #180543, #164298, #81971, #148058, #214064, #131840, #45237, #111353, #27900, #102492, #150192, #49480, #181595, #2825, #36413, #86241, #71026, #84105, #198895, #103564, #19091, #168556, #149105, #21207, #169624, #1761, #51621, #20155, #18016, #152312, #67819, #85171, #4949, #115600, #684, #201029, #117746, #167495, #68895, #34282, #99307, #100356, #83030, #183737, #185855, #165354, #118801, #33223, #153378, #16949, #133966, #184787, #66751, #132892, #199973, #151255, #35344, #3888, #137141, #50542, #101423, #135015, #52671, #69958, #136070, #202084, #116664, #182662, #53743, #119877, #37487, #87309, #166425, #42856, #40710, #108963, #39623, #25501, #186933, #173928, #120961, #171758, #73170, #56945, #174983, #140362, #26567, #9258, #156591, #72100, #154452, #92672, #55875, #207451, #122032, #106814, #187998, #138210, #158716, #141445, #105728, #91609, #23353, #172844, #123117, #157660, #10313, #76388, #89463, #75328, #24416, #155516, #90529, #7098, #59070, #8185, #125231, #191189, #203168, #54813, #38565, #104640, #6031, #189077, #170687, #22274, #74270, #205308, #206381, #190133, #139276, #58007, #204223, #124171, #88383, #41789, #107902, #29788, #177099, #95873, #178172, #209565, #80667, #61211, #162991, #77455, #146758, #145710, #14572, #96940, #127368, #212776, #193339, #78520, #161928, #159776, #11375, #142496, #60138, #126295, #13518, #79590, #30863, #44984, #111093, #208503, #211708, #28714, #63344, #192254, #143573, #94800, #43917, #113235, #110032, #160849, #12441, #144637, #128440, #210652, #62279, #129503, #194406, #195484, #47117, #46048, #176044, #179239, #27636, #93737, #112169, #117998, #102755, #167748, #5210, #136331, #186117, #87571, #52927, #183988, #119061, #101679, #202350, #204487, #35602, #137398, #68080, #172025, #134216, #86497, #203416, #19348, #200225, #152562, #169872, #54001, #104902, #155776, #85427, #70220, #103824, #69151, #51876, #151513, #3081, #121221, #55072, #56137, #185043, #36667, #23619, #71286, #135271, #187191, #201286, #168811, #20415, #72364, #170943, #138465, #4149, #120139, #37750, #21462, #153641, #38819, #22542, #88649, #154708, #6290, #122298, #188255, #39895, #106005, #89728, #125490, #92931, #26827, #9517, #109232, #192518, #140628, #75590, #95061, #73438, #110291, #28975, #8438, #44171, #76646, #160039, #143835, #127633, #176300, #94000, #158975, #74526, #207713, #27903, #206640, #77714, #11643, #7361, #141702, #91868, #58274, #209831, #124430, #59336, #190388, #90789, #61467, #193598, #42046, #45240, #108157, #191452, #43117, #111357, #177362, #139541, #174184, #205568, #175242, #25756, #10572, #157924, #57206, #142761, #123366, #189332, #40972, #107083, #173105, #24685, #156853, #208766, #60394, #126557, #130807, #163247, #80920, #148061, #211964, #63603, #178434 ),
 ( #34287, #129758, #13769, #195742, #47379, #113490, #144895, #179498, #112421, #31120, #33227, #32169, #98246, #147009, #196798, #210903, #688, #213030, #66754, #97194, #197852, #62530, #131842, #78772, #14829, #64662, #48440, #132895, #164302, #198899, #181599, #114555, #30041, #96128, #50545, #79845, #15891, #65695, #180548, #194660, #99310, #49483, #83034, #128692, #81975, #115603, #214069, #145954, #162183, #165358, #16953, #149108, #116667, #182665, #161109, #12696, #46305, #71835, #170420, #154188, #137944, #5756, #84107, #55612, #54547, #187736, #189877, #6836, #203966, #39364, #123910, #121767, #57750, #22008, #105460, #171495, #88118, #186669, #136876, #74000, #156329, #23086, #100359, #18020, #56686, #90261, #140093, #124968, #89201, #38296, #157399, #72914, #7912, #202902, #75067, #8992, #155254, #139019, #206120, #205042, #41520, #122852, #107632, #150195, #188814, #120694, #40448, #106550, #172577, #24158, #173664, #1765, #25238, #104374, #91340, #141180, #67822, #207189, #166429, #58815, #190930, #60948, #177909, #158454, #174728, #127105, #144382, #28449, #79331, #130297, #10053, #44721, #78258, #193070, #210382, #13259, #110830, #76130, #92414, #12186, #77187, #94541, #27374, #211446, #62023, #46856, #195220, #42594, #64154, #63080, #112970, #208245, #176835, #142233, #80399, #128179, #160580, #194140, #29522, #93475, #159513, #59878, #11112, #26300, #109773, #175782, #95615, #45789, #111908, #161665, #143309, #212513, #209300, #146495, #145449, #108699, #129248, #126028, #162732, #178982, #191990, #30596, #96683, #14304, #43656, #197336, #69449, #114045, #180039, #34825, #183219, #184275, #32709, #181092, #85719, #199454, #48977, #51096, #196285, #147544, #81467, #200517, #84657, #52162, #115095, #164845, #98790, #198389, #66239, #213565, #100899, #65187, #166988, #99851, #148603, #47932, #18579, #168044, #118289, #165913, #67307, #1247, #50030, #83585, #150745, #16437, #116154, #31660, #97738, #2307, #3380, #82516, #68383, #117222, #134513, #35900, #101976, #19646, #151807, #133448, #172, #182141, #163796, #132388, #15373, #131341, #33771, #17498, #149667, #136622, #139835, #54298, #187483, #120435, #4437, #189618, #73738, #202648, #106296, #170165, #39113, #55358, #90011, #91081, #24978, #186410, #156066, #152859, #38047, #119356, #104117, #21753, #56430, #5501, #204776, #138758, #87861, #157141, #153933, #173396, #71582, #8734, #172316, #135555, #41265, #137690, #201579, #203711, #105196, #122589, #70507, #121510, #53225, #185343, #36966, #188551, #40182, #123656, #171233, #22828, #103047, #23907, #88943, #7654, #169102, #86791, #20699, #205863, #57496, #107374, #154996, #6582, #72661, #76924, #159250, #92155, #61758, #26042, #127927, #192802, #27110, #140915, #193879, #46588, #79062, #44460, #160325, #94285, #143050, #176579, #45526, #207993, #209045, #162468, #206928, #177654, #96417, #75872, #111642, #144124, #12988, #211186, #194952, #29262, #161404, #11929, #141979, #60681, #95354, #59620, #145181, #62811, #74814, #126843, #10850, #125776, #128973, #191737, #110577, #43393, #158208, #112707, #178717, #109514, #30333, #175522, #28188, #78001, #58558, #124711, #190670, #93219, #42331, #210118, #108446, #174466, #9797, #182958, #49766, #18313, #166721, #14042, #35635, #34573, #84397, #179778, #82254 ),
 ( #100645, #131088, #150484, #81203, #197078, #180827, #213313, #97471, #47665, #199185, #67048, #114828, #80128, #146233, #181877, #983, #50832, #101714, #48715, #163528, #68114, #198135, #133185, #113776, #200257, #134251, #32453, #16169, #116960, #98522, #2044, #132125, #51909, #63884, #164584, #31397, #165650, #148345, #115892, #33513, #64938, #130038, #214346, #15114, #65976, #118032, #196029, #83314, #212250, #184018, #147282, #99586, #149400, #17239, #85461, #37785, #55105, #153676, #204521, #41006, #69185, #169909, #203451, #103859, #121254, #138499, #21496, #135306, #3114, #38853, #104937, #87606, #187225, #151547, #7395, #5244, #73474, #4183, #56169, #201319, #122332, #52959, #136367, #71321, #137434, #139575, #170978, #205602, #188289, #22577, #36703, #119097, #57240, #20449, #88683, #72399, #202387, #185078, #106038, #39929, #89763, #102788, #154742, #172060, #70254, #86532, #168846, #6326, #23654, #155811, #123400, #189364, #167785, #19381, #152597, #54038, #120174, #186152, #141733, #9548, #90822, #59366, #58305, #191483, #193627, #127665, #60428, #190419, #124460, #210932, #174216, #110323, #11672, #207741, #140659, #45269, #143868, #29006, #156885, #92962, #61498, #75624, #25790, #42078, #159008, #109264, #175272, #111390, #12729, #27936, #26857, #194694, #125523, #91900, #157956, #43151, #10602, #8472, #76678, #108190, #142792, #177392, #208799, #126588, #192549, #95093, #44202, #161142, #176329, #94030, #160068, #77747, #209861, #206673, #78802, #144926, #62558, #107115, #24720, #128722, #173139, #74558, #67856, #80947, #195770, #100392, #15922, #99340, #145983, #18055, #166462, #147039, #48470, #165389, #14857, #33256, #164333, #132925, #96163, #213061, #211994, #197882, #114585, #82005, #65726, #31149, #162214, #97223, #79873, #180576, #182697, #13799, #115632, #46335, #150228, #112450, #64691, #181627, #63635, #178463, #130836, #148093, #32198, #83063, #134005, #129789, #98274, #214098, #196829, #131873, #16984, #49512, #47409, #113522, #149141, #721, #66785, #198930, #30073, #84140, #50576, #1799, #163276, #116698, #179531, #34316, #117782, #168590, #69996, #53783, #171798, #137180, #105772, #38600, #186968, #188034, #36453, #184824, #89504, #203204, #201065, #54851, #200010, #151291, #85207, #204262, #88425, #55913, #52707, #20190, #118838, #202124, #136108, #2862, #104678, #68932, #170726, #103602, #152348, #51660, #22312, #23392, #122071, #169659, #71064, #4988, #119916, #87351, #154491, #102528, #185892, #73210, #183774, #6070, #7138, #86278, #72141, #121001, #138248, #39664, #155558, #35384, #101459, #167530, #3926, #37526, #19128, #21244, #135052, #153417, #139317, #207489, #9296, #140402, #143611, #58045, #191230, #124211, #8221, #193378, #77492, #206421, #110068, #173965, #42893, #59108, #93773, #94837, #28753, #190173, #159813, #109002, #25538, #175019, #41827, #11417, #26606, #209604, #61248, #205346, #160888, #127405, #45022, #90571, #125268, #189114, #177136, #92707, #141482, #158754, #126333, #107940, #91646, #156632, #157699, #123157, #75369, #10348, #60176, #76422, #208540, #142533, #192292, #12483, #43952, #56983, #176080, #27678, #111132, #40748, #106854, #172883, #24457, #74306, #163027, #165144, #196584, #179279, #14610, #99092, #195521, #80707, #146797, #16735, #469, #78557, #213862 ),
 ( #48227, #30903, #212813, #82821, #47158, #33013, #145746, #113274, #96979, #63385, #161965, #112205, #49276, #131632, #64450, #144675, #210689, #31957, #65483, #115397, #100141, #130595, #13556, #132680, #114339, #197631, #178212, #50331, #198686, #180334, #98041, #181390, #164094, #148897, #15675, #66539, #128476, #81762, #29828, #147843, #116449, #182443, #34070, #129540, #194444, #166205, #95912, #62317, #46086, #79627, #211747, #17794, #121812, #83882, #36194, #153160, #133750, #149972, #102270, #119657, #3671, #54594, #105505, #199758, #19940, #53523, #168345, #185642, #202950, #86026, #51403, #67604, #103344, #169408, #152100, #37274, #1542, #71881, #69747, #137990, #68681, #120741, #117523, #186715, #183517, #200811, #135853, #201875, #204008, #20994, #55656, #38343, #87090, #101197, #35125, #187780, #84954, #4735, #136923, #52461, #167285, #170467, #104419, #154232, #18870, #70810, #22053, #134805, #151043, #2612, #88163, #118587, #39410, #5804, #184574, #56730, #143354, #11158, #57794, #173710, #10100, #140140, #158501, #75115, #43702, #6881, #206166, #122898, #108748, #25286, #141227, #190973, #156374, #72960, #7958, #205089, #91387, #93519, #139061, #26349, #171537, #60997, #23129, #189923, #92462, #188857, #89247, #41568, #58860, #157447, #208290, #47702, #40493, #9041, #207236, #107682, #125017, #142280, #42640, #106598, #172625, #174773, #76174, #59923, #126078, #155298, #77236, #192039, #209349, #74050, #109819, #24202, #175829, #90305, #123954, #27421, #159562, #127150, #193123, #19418, #134288, #67084, #197113, #64971, #3150, #180866, #116993, #18353, #148383, #147321, #51945, #150520, #35673, #163570, #99621, #68154, #16207, #32487, #131124, #165687, #115928, #181916, #200293, #101751, #113816, #34610, #69220, #82290, #98561, #164622, #214384, #66014, #97513, #132163, #48752, #198169, #118068, #17276, #49802, #33548, #184054, #83352, #167818, #149437, #1019, #133218, #199224, #114865, #213348, #84431, #166757, #50871, #179816, #31435, #182993, #100679, #2081, #135339, #85496, #151583, #15153, #201353, #81239, #21526, #120208, #103893, #87637, #169941, #36736, #5277, #4217, #137470, #139610, #171011, #153708, #203484, #73507, #71354, #7426, #186183, #55137, #121282, #37816, #136402, #86568, #23685, #106069, #187258, #52994, #185110, #6359, #39961, #89795, #74587, #38885, #202418, #107146, #22608, #172093, #152630, #24751, #173172, #104970, #88716, #155841, #154775, #205632, #72428, #57270, #102822, #138530, #70286, #204553, #56202, #122365, #188321, #123432, #168877, #189394, #54073, #41036, #90853, #20481, #156917, #119130, #8506, #140690, #10625, #127690, #108219, #124489, #76700, #94054, #192574, #29034, #79895, #174244, #208824, #27961, #142817, #160095, #177416, #60454, #25816, #42106, #77772, #143892, #126611, #11698, #190448, #46355, #44229, #112475, #43175, #95117, #91926, #161166, #157986, #175298, #110350, #176353, #178484, #209886, #30094, #12752, #61524, #75651, #9574, #96184, #59393, #193650, #111412, #26884, #141758, #144947, #78826, #128742, #207766, #45292, #210953, #109288, #125549, #191510, #62580, #194716, #162235, #13821, #206706, #58333, #92987, #159032, #34343, #15943, #115659, #66810, #64713, #167555, #182724, #183797, #51685, #196852, #35407, #32224, #197904, #132953, #80970, #147062 ),
 ( #198956, #98296, #146004, #63658, #99364, #50599, #100416, #19156, #180599, #213082, #200033, #181653, #116724, #31170, #117807, #101485, #164359, #148120, #166487, #114608, #18078, #49533, #84166, #195793, #82027, #97243, #83088, #214121, #33279, #165416, #130856, #47431, #48490, #179549, #65750, #67880, #113546, #744, #212014, #129812, #163297, #131896, #150254, #14878, #17012, #149167, #1822, #134026, #122098, #172912, #201091, #87379, #121031, #21273, #38629, #55945, #153447, #52732, #135078, #170755, #22343, #5020, #186998, #68957, #139345, #137211, #205375, #136137, #188062, #118866, #39691, #2886, #53813, #169685, #71094, #57011, #88456, #123182, #105802, #104705, #168616, #36480, #189142, #152375, #154516, #204288, #119942, #184852, #23420, #171826, #7168, #102555, #203233, #89531, #202153, #3954, #86305, #155583, #6097, #73238, #40780, #106886, #85229, #151318, #72166, #70021, #54877, #20218, #185918, #37553, #103633, #138274, #92737, #109031, #25566, #28784, #157730, #76455, #9325, #107966, #78586, #177167, #91677, #209638, #59139, #142563, #158782, #193410, #194475, #128507, #75399, #45054, #208569, #125298, #60203, #141512, #111166, #126364, #94867, #160921, #24486, #46118, #12515, #144708, #190198, #10379, #74334, #62347, #192323, #26636, #43981, #11449, #207520, #191256, #41857, #42921, #8250, #175050, #110100, #159846, #176111, #93806, #27711, #127440, #77523, #143644, #61278, #210720, #112235, #90598, #156658, #140436, #206448, #58076, #124238, #173994, #165170, #113304, #179311, #51430, #95940, #161996, #16764, #82848, #166235, #14642, #163061, #67631, #181415, #30932, #33042, #178244, #129567, #63415, #182470, #66565, #34099, #97008, #146824, #80735, #180363, #48253, #195554, #148924, #47191, #497, #81791, #130622, #29859, #132707, #149999, #100170, #147874, #49307, #197661, #31988, #65512, #198713, #212844, #98067, #13586, #79659, #50359, #199784, #114368, #131658, #116480, #164122, #145776, #211777, #115423, #99120, #15705, #213890, #64481, #17825, #83908, #1569, #196614, #133777, #101228, #88191, #35151, #86052, #201900, #185670, #89276, #54619, #23161, #138018, #70836, #200834, #68708, #6908, #184602, #120767, #22079, #152128, #151073, #55682, #154264, #39436, #167310, #103373, #71909, #19968, #36219, #134831, #169435, #119684, #37299, #204033, #105529, #117550, #38368, #72985, #3697, #102298, #168372, #69773, #135881, #18897, #53552, #52485, #21019, #121838, #87116, #153187, #4760, #187810, #136953, #171563, #202978, #186746, #104448, #170496, #118615, #2636, #5838, #155324, #139089, #183544, #84981, #205116, #10127, #59953, #61025, #107710, #74078, #159591, #125047, #76202, #90332, #77270, #11190, #173736, #9071, #142312, #41599, #208322, #58893, #43733, #40522, #25314, #24230, #26379, #75145, #191002, #108777, #57820, #106626, #123982, #156401, #141255, #93547, #172655, #92492, #56759, #209381, #122923, #157476, #126108, #7989, #140170, #207263, #174803, #42669, #192068, #188881, #91415, #158530, #109847, #175861, #143382, #27449, #127186, #189950, #206192, #187451, #170135, #71552, #19615, #89979, #87831, #156029, #86759, #72628, #85687, #6550, #168010, #4406, #120402, #104086, #7619, #39079, #73705, #56396, #203681, #119324, #201547, #139801, #103015, #105164, #154965, #70477, #69416, #188518 ),
 ( #122557, #172285, #35870, #171203, #205830, #136592, #169070, #152828, #202615, #54266, #151775, #186378, #53193, #38014, #40149, #153902, #21720, #5471, #106263, #137660, #204745, #20669, #55329, #121480, #22795, #185309, #135523, #138727, #88911, #23873, #101945, #3347, #57461, #123622, #36931, #211151, #9765, #124679, #29227, #159218, #28154, #74780, #161368, #95320, #75839, #191701, #94250, #158173, #176543, #93185, #61723, #24943, #141946, #140880, #126810, #43361, #10818, #209010, #174433, #91047, #26010, #8697, #109482, #111608, #157107, #44425, #189586, #79029, #41232, #207958, #110542, #206893, #107339, #59584, #76892, #175491, #11891, #62775, #58524, #27078, #143016, #125741, #12951, #60647, #160289, #190637, #145145, #173361, #192766, #77966, #144087, #210084, #127891, #193842, #45491, #42297, #177619, #108411, #92120, #197043, #32420, #148312, #113741, #178681, #179745, #162432, #48680, #50796, #30295, #198101, #128937, #18277, #194915, #147248, #49730, #96380, #46552, #213279, #16135, #114796, #165617, #2012, #14008, #131055, #164550, #64906, #82221, #99552, #180795, #80094, #146198, #214311, #65943, #98486, #132092, #112672, #182924, #115858, #34540, #31363, #17205, #212212, #83281, #63848, #97439, #181843, #33479, #100610, #149366, #166686, #948, #67014, #130005, #195995, #84360, #47630, #133149, #199152, #163495, #15078, #116924, #150450, #81167, #86196, #150145, #82987, #166379, #17971, #20110, #183692, #168510, #102442, #202036, #35299, #68852, #152268, #84059, #120911, #136024, #137093, #4903, #1717, #203120, #199930, #151211, #3840, #34240, #100312, #186884, #16907, #149062, #69913, #53698, #87264, #67773, #133923, #54762, #119829, #51576, #185808, #99264, #50502, #198855, #103519, #37441, #169577, #117701, #101376, #167450, #19045, #36367, #85124, #134972, #639, #153330, #2781, #70981, #200980, #21160, #66703, #165312, #132850, #52627, #118755, #184739, #116624, #182618, #158674, #59028, #206336, #121984, #204171, #142454, #105680, #41743, #157617, #73125, #72052, #191147, #141399, #154402, #39577, #9214, #207409, #155465, #171708, #55828, #24370, #40668, #106771, #125186, #174943, #38516, #173880, #208462, #7049, #23306, #89417, #139226, #205257, #22224, #56898, #187950, #123073, #42814, #156547, #189027, #172799, #108920, #90482, #26524, #8141, #74223, #140319, #57963, #124128, #138163, #75285, #91563, #190090, #104594, #170640, #107854, #25455, #92633, #60096, #10271, #76347, #126254, #88338, #5981, #77414, #164015, #31881, #78478, #194365, #30820, #160808, #179197, #95829, #64370, #27595, #12399, #143529, #129461, #46007, #161886, #211665, #177057, #93694, #28674, #11334, #112127, #114260, #159736, #47074, #192213, #81676, #43876, #210612, #113191, #209525, #109991, #62239, #79550, #178130, #14528, #65402, #61166, #29746, #13473, #128398, #145668, #162950, #63301, #127329, #193298, #195444, #180257, #94760, #144597, #147762, #96899, #44943, #80625, #176003, #111051, #146716, #196505, #212732, #48147, #130516, #97958, #15589, #213779, #1460, #148814, #118509, #82741, #184492, #35042, #83800, #197551, #36111, #103266, #135774, #101113, #2525, #150961, #133669, #18788, #102194, #50249, #199672, #4655, #49194, #19861, #153078, #132599, #168261, #200730, #69667, #53438, #37189, #85947, #3590, #68601 ),
 ( #84872, #152022, #51316, #99007, #181305, #134724, #52381, #117443, #167200, #115315, #185561, #183438, #169327, #182359, #201797, #32932, #119575, #165062, #100063, #67525, #20912, #87007, #131549, #16655, #386, #66458, #198604, #116371, #33988, #166126, #17712, #149893, #105423, #104339, #8955, #173629, #186636, #71798, #41487, #25200, #187700, #137911, #21971, #56652, #72876, #138984, #91305, #207155, #70726, #206081, #174691, #39328, #203931, #121734, #171460, #23049, #54512, #89165, #88080, #155219, #157363, #188772, #6800, #205005, #75031, #122814, #141143, #57715, #5721, #55579, #158417, #202865, #120657, #123873, #189839, #58779, #40412, #106514, #26265, #73965, #172541, #140059, #136839, #154153, #170383, #124932, #190895, #42559, #24126, #90228, #156292, #7877, #107598, #108662, #92383, #38262, #211416, #128145, #176799, #76094, #129213, #196254, #14271, #194106, #95582, #29490, #12154, #111873, #195189, #143277, #78226, #97704, #142197, #112938, #31628, #11078, #46824, #79299, #162699, #146462, #130264, #178951, #96644, #161631, #77155, #210349, #13224, #110796, #145415, #27338, #10019, #144348, #94509, #209267, #80366, #60913, #61989, #127071, #93440, #64122, #212478, #193032, #30564, #44688, #45754, #177878, #47899, #180006, #114011, #28416, #208212, #63046, #160547, #59843, #125995, #191953, #43621, #109737, #175745, #159479, #185307, #118258, #168009, #115062, #17466, #213532, #201544, #133414, #165879, #83550, #52131, #199421, #53192, #150712, #140, #147512, #16404, #82482, #84621, #33736, #18545, #166954, #184242, #99814, #51064, #2273, #148571, #36930, #200485, #119322, #69415, #66205, #163763, #49996, #1213, #35868, #68349, #67276, #15341, #65154, #149631, #117187, #183188, #34793, #134481, #100868, #131312, #197303, #101944, #19614, #85686, #151774, #48943, #3346, #135522, #81431, #132351, #181059, #32677, #98755, #164812, #198356, #116118, #182107, #74779, #40148, #8696, #123621, #56394, #186376, #54265, #206892, #170134, #106261, #7618, #137659, #136591, #41230, #205829, #4404, #104085, #73703, #57460, #5469, #21718, #120401, #88910, #105163, #171202, #189583, #24942, #103013, #23871, #58522, #71551, #87830, #153900, #203679, #55328, #86758, #121479, #38013, #187450, #107338, #6548, #39078, #22793, #173360, #154964, #91046, #72627, #138726, #204743, #122556, #188517, #202614, #139800, #156028, #172284, #169068, #20667, #89978, #157105, #140879, #124678, #190636, #152827, #70475, #11890, #95319, #141944, #14007, #96379, #143014, #44424, #161367, #10816, #29226, #160287, #128935, #92119, #76891, #207957, #193841, #110541, #77965, #61722, #27077, #158172, #93183, #75838, #176541, #178680, #9764, #111606, #42296, #146197, #108409, #60646, #177616, #59583, #174430, #112671, #144086, #26008, #162431, #94247, #80093, #159216, #79028, #125739, #12950, #191700, #209009, #126808, #28153, #212211, #45490, #63847, #62773, #210083, #43360, #109481, #130003, #175490, #145144, #211150, #192764, #127890, #194913, #46550, #30294, #197042, #166684, #150449, #98484, #48678, #147247, #181841, #198099, #49727, #2011, #117994, #195994, #116922, #85425, #164549, #114795, #32418, #16134, #82219, #179744, #148311, #213277, #65940, #68079, #99550, #214310, #132090, #134214, #115856, #200223, #180794, #33477, #165614, #17203, #64905 ) ),
 .UNSPECIFIED., .T., .F., .F. ) 
 B_SPLINE_SURFACE_WITH_KNOTS ( ( 4, 3, 4 ),
 ( 4, 1, 1, 1, 1, 1, 1, 1, 1, 1, 1, 1, 1, 1, 1, 1, 1, 1, 1, 1, 1, 1, 1, 1, 1, 1, 1, 1, 1, 1, 1, 1, 1, 1, 1, 1, 1, 1, 1, 1, 1, 1, 1, 1, 1, 1, 1, 1, 1, 1, 1, 1, 1, 1, 1, 1, 1, 1, 1, 1, 1, 1, 1, 1, 1, 1, 1, 1, 1, 1, 1, 1, 1, 1, 1, 1, 1, 1, 1, 1, 1, 1, 1, 1, 1, 1, 1, 1, 1, 1, 1, 1, 1, 1, 1, 1, 1, 1, 1, 1, 1, 1, 1, 1, 1, 1, 1, 1, 1, 1, 1, 1, 1, 1, 1, 1, 1, 1, 1, 1, 1, 1, 1, 1, 1, 1, 1, 1, 1, 1, 1, 1, 1, 1, 1, 1, 1, 1, 1, 1, 1, 1, 1, 1, 1, 1, 1, 1, 1, 1, 1, 1, 1, 1, 1, 1, 1, 1, 1, 1, 1, 1, 1, 1, 1, 1, 1, 1, 1, 1, 1, 1, 1, 1, 1, 1, 1, 1, 1, 1, 1, 1, 1, 1, 1, 1, 1, 1, 1, 1, 1, 1, 1, 1, 1, 1, 1, 1, 1, 1, 1, 1, 1, 1, 1, 1, 1, 1, 1, 1, 1, 1, 1, 1, 1, 1, 1, 1, 1, 1, 1, 1, 1, 1, 1, 1, 1, 1, 1, 1, 1, 1, 1, 1, 1, 1, 1, 1, 1, 1, 1, 1, 1, 1, 1, 1, 1, 1, 1, 1, 1, 1, 1, 1, 1, 1, 1, 1, 1, 1, 1, 1, 1, 1, 1, 1, 1, 1, 1, 1, 1, 1, 1, 1, 1, 1, 1, 1, 1, 1, 1, 1, 1, 1, 1, 1, 1, 1, 1, 1, 1, 1, 1, 1, 1, 1, 1, 1, 1, 1, 1, 1, 1, 1, 1, 1, 1, 1, 1, 1, 1, 1, 1, 1, 1, 1, 1, 1, 1, 1, 1, 1, 1, 1, 1, 1, 1, 1, 1, 1, 1, 1, 1, 1, 1, 1, 1, 1, 1, 1, 1, 1, 1, 1, 1, 1, 1, 1, 1, 1, 1, 1, 1, 1, 1, 1, 1, 1, 1, 1, 1, 1, 1, 1, 1, 1, 1, 1, 1, 1, 1, 1, 1, 1, 1, 1, 1, 1, 1, 1, 1, 1, 1, 1, 4 ),
 ( 0.000000000000000000, 0.5000000000000000000, 1.000000000000000000 ),
 ( 0.000000000000000000, 0.002600154539856827565, 0.005208839490340733125, 0.007813275572638063438, 0.01041576435696154809, 0.01302135854728175661, 0.01562456786780599440, 0.01822932761385693060, 0.02083324874646079461, 0.02343713590986815087, 0.02604192363554110393, 0.02864519953128016536, 0.03125045858075606309, 0.03385359029894085409, 0.03645870005206112291, 0.03906221013386886737, 0.04166657361863843057, 0.04427092160485841116, 0.04687444683368256759, 0.04947954930481244379, 0.05208268618576387260, 0.05468794662449812799, 0.05729120536831356497, 0.05989601299138836571, 0.06249988999545372931, 0.06510378435733490954, 0.06770858081828938502, 0.07031184975024351580, 0.07291710771924506118, 0.07552024060328325905, 0.07812534933470290099, 0.08072885870519988516, 0.08333322157114708695, 0.08593756915452624434, 0.08854109358761537429, 0.09114619558392741960, 0.09374933183658358538, 0.09635459170495851156, 0.09895784999447977681, 0.1015626569530685003, 0.1041665336043751944, 0.1067704272253022224, 0.1093752232910748662, 0.1119784915631429623, 0.1145837490571069844, 0.1171868814509031548, 0.1197919896162490533, 0.1223954986480551566, 0.1249998608471283579, 0.1276042081199000311, 0.1302077318846941445, 0.1328128334964322199, 0.1354159692195129883, 0.1380212286176593917, 0.1406244865514671982, 0.1432292929439143159, 0.1458331693420142072, 0.1484370623210626572, 0.1510418580899855479, 0.1536451258019158050, 0.1562503829188521542, 0.1588535149221727560, 0.1614586226195926788, 0.1640621314121666618, 0.1666664930431534797, 0.1692708401040713406, 0.1718743633000545112, 0.1744794646253388370, 0.1770825999186152189, 0.1796878589445308205, 0.1822911166222762891, 0.1848959225469683498, 0.1874997987909985397, 0.1901036912273387502, 0.1927084867977703619, 0.1953117540492253223, 0.1979170108871138589, 0.2005201425997050479, 0.2031252499273119572, 0.2057287585800815777, 0.2083331197417381819, 0.2109374666895270922, 0.2135409894161511279, 0.2161460905530729892, 0.2187492255162853672, 0.2213544842679382729, 0.2239577417892439637, 0.2265625473445374016, 0.2291664235336075273, 0.2317703155263790282, 0.2343751109966507595, 0.2369783778872631419, 0.2395836345440564008, 0.2421867660656364940, 0.2447918731215153465, 0.2473953817338825356, 0.2499997425249363969, 0.2526040894582959329, 0.2552076118149841921, 0.2578127128616094499, 0.2604158475944712281, 0.2630211061698037311, 0.2656243636342671688, 0.2682291689184919115, 0.2708330451516883230, 0.2734369368000036937, 0.2760417322684234342, 0.2786449988978000336, 0.2812502554714267355, 0.2838533869016899303, 0.2864584937839013135, 0.2890620024552456591, 0.2916663629743991848, 0.2942707099920074398, 0.2968742320781582733, 0.2994793331325310004, 0.3020824677347322962, 0.3046877262316646240, 0.3072909837388622112, 0.3098957888503254821, 0.3124996652267145181, 0.3151035566296633839, 0.3177083521945192612, 0.3203116186622446127, 0.3229168752506134110, 0.3255200066892336430, 0.3281251134958176330, 0.3307286223255002655, 0.3333329826714347410, 0.3359373298719517953, 0.3385408517869427647, 0.3411459529470890484, 0.3437490875183005223, 0.3463543460347343617, 0.3489576036842249041, 0.3515624087212146920, 0.3541662853398466204, 0.3567701765964986227, 0.3593749723560626386, 0.3619782387617029862, 0.3645834954627060198, 0.3671866270093405715, 0.3697917338383204244, 0.3723952429256875973, 0.3749996031970665444, 0.3776039506791386557, 0.3802074725223298923, 0.3828125738862612759, 0.3854157085261381011, 0.3880209671599602617, 0.3906242250512887426, 0.3932290301120778819, 0.3958329070719905363, 0.3984367982813996067, 0.4010415943339316058, 0.4036448607770379837, 0.4062501176885546794, 0.4088532494428480657, 0.4114583563922335485, 0.4140618658366201910, 0.4166662261320933647, 0.4192705739943561327, 0.4218740958650940009, 0.4244791975308115917, 0.4270823323389966175, 0.4296875911880828069, 0.4322908494207843844, 0.4348956546036337745, 0.4374995320038561619, 0.4401034232650644085, 0.4427082197088152427, 0.4453114862889279713, 0.4479167435088288185, 0.4505198755704162283, 0.4531249827382076711, 0.4557284926389418844, 0.4583328530571487147, 0.4609372013982309668, 0.4635407233958523388, 0.4661458254613498609, 0.4687489605374778323, 0.4713542196996960976, 0.4739574783732994345, 0.4765622837764619812, 0.4791661617160185016, 0.4817700531280592058, 0.4843748500612748420, 0.4869781168779269698, 0.4895833745040767959, 0.4921865069725880892, 0.4947916144567798824, 0.4973951249131855490, 0.4999994855527590265, 0.5026038344712867589, 0.5052073566951218453, 0.5078124592583899144, 0.5104155947020908579, 0.5130208542753056378, 0.5156241134893367883, 0.5182289192110610676, 0.5208327977889742888, 0.5234366894508762913, 0.5260414869718011976, 0.5286447541245218318, 0.5312500122547839654, 0.5338531452298473923, 0.5364582531284315392, 0.5390617642398328746, 0.5416661251994032700, 0.5442704747940029231, 0.5468739973433798252, 0.5494791005024090014, 0.5520822364133124438, 0.5546874964953879550, 0.5572907563493740835, 0.5598955624879079496, 0.5624994418032033261, 0.5651033338139942463, 0.5677081320208752224, 0.5703113996091939697, 0.5729166583414331271, 0.5755197919226788805, 0.5781249003336490500, 0.5807284121993739889, 0.5833327735775721834, 0.5859371239468746939, 0.5885406469211225122, 0.5911457507739076300, 0.5937488872516457628, 0.5963541479404496082, 0.5989574085339228748, 0.6015622151875171797, 0.6041660953392257172, 0.6067699877979360057, 0.6093747867890261238, 0.6119780549124759217, 0.6145833143445629254, 0.6171864486316270826, 0.6197915576529816617, 0.6223950703723655220, 0.6249994322678273928, 0.6276037835104713025, 0.6302073070089242446, 0.6328124116534677990, 0.6354155487976793637, 0.6380208101910863627, 0.6406240716235875876, 0.6432288788904997334, 0.6458327599776627626, 0.6484366529833293091, 0.6510414528568908565, 0.6536447216150126360, 0.6562499818448275235, 0.6588531169373553764, 0.6614582266671018562, 0.6640617403394915019, 0.6666661028508605868, 0.6692704550654967610, 0.6718739791874978051, 0.6744790847218130603, 0.6770822226321474568, 0.6796874848280434200, 0.6822907471991253026, 0.6848955551776233497, 0.6874994372992955238, 0.6901033309509650993, 0.6927081318052739078, 0.6953114012976200353, 0.6979166624230551674, 0.7005197984207056638, 0.7031249089568636368, 0.7057284236816204759, 0.7083327869075525252, 0.7109371401928469281, 0.7135406650377511539, 0.7161457715598668061, 0.7187489103359874232, 0.7213541734322722609, 0.7239574368415039318, 0.7265622456298695964, 0.7291661288851226663, 0.7317700232818561412, 0.7343748252152053624, 0.7369780955413426371, 0.7395833576603073611, 0.7421864946627563242, 0.7447916061033615920, 0.7473951219798656842, 0.7499994860190324353, 0.7526038404736700160, 0.7552073661408488237, 0.7578124737488122209, 0.7604156134903999886, 0.7630208775849919300, 0.7656241421319622820, 0.7682289518284949326, 0.7708328363164217434, 0.7734367315572975299, 0.7760415346680002990, 0.7786448059275148381, 0.7812500691379388185, 0.7838532072448821664, 0.7864583196879902927, 0.7890618368156444573, 0.7916662017667361884, 0.7942705574894247667, 0.7968740840782696511, 0.7994791928701499018, 0.8020823336769073997, 0.8046875988677468783, 0.8072908646520678966, 0.8098956753550886623, 0.8124995611748068169, 0.8151034573589240884, 0.8177082617453185209, 0.8203115340378186460, 0.8229167984376549727, 0.8255199377488137147, 0.8281250512925039109, 0.8307285697707365024, 0.8333329357324672504, 0.8359372928219411802, 0.8385408204318668401, 0.8411459305057594760, 0.8437490724774151518, 0.8463543388624672481, 0.8489576059837783406, 0.8515624177916331083, 0.8541663050422881875, 0.8567702022687715413, 0.8593750080292236193, 0.8619782814543437421, 0.8645835471415733720, 0.8671866877566964948, 0.8697918024990743957, 0.8723953224273439666, 0.8749996894984543028, 0.8776040480534781363, 0.8802075767839265819, 0.8828126882379567775, 0.8854158314742670566, 0.8880210991515266050, 0.8906243677094983768, 0.8932291807205616774, 0.8958330695013316802, 0.8984369678693342465, 0.9010417751022415933, 0.9036450497596462128, 0.9062503168322812996, 0.9088534588511494317, 0.9114585748903522022, 0.9140620963681507227, 0.9166664646474114164, 0.9192708247667824573, 0.9218743547172278952, 0.9244794676495572405, 0.9270826122503010858, 0.9296878813177945622, 0.9322911514121841048, 0.9348959657248061550, 0.9374998561347748227, 0.9401037557438677306, 0.9427085645475906661, 0.9453118405358371668, 0.9479171090940153865, 0.9505202526155902554, 0.9531253700418979014, 0.9557288931959170286, 0.9583332627756006028, 0.9609376244112938226, 0.9635411559431285022, 0.9661462708106475228, 0.9687494151757961580, 0.9713546862302190332, 0.9739579640138142924, 0.9765627705390533819, 0.9791666547386930208, 0.9817705986233274951, 0.9843753609709087193, 0.9869785915570626900, 0.9895841932699848131, 0.9921866851465583892, 0.9947911401134668097, 0.9973998225951543617, 1.000000000000000000 ),
 .UNSPECIFIED. ) 
 GEOMETRIC_REPRESENTATION_ITEM ( )  RATIONAL_B_SPLINE_SURFACE ( (
 ( 1.000000000000000000, 1.000000000000000000, 1.000000000000000222, 1.000000000000000000, 0.9999999999999996669, 1.000000000000000444, 0.9999999999999997780, 1.000000000000000000, 1.000000000000000222, 0.9999999999999996669, 1.000000000000000222, 0.9999999999999996669, 1.000000000000000000, 0.9999999999999997780, 1.000000000000000222, 0.9999999999999997780, 1.000000000000000222, 1.000000000000000222, 0.9999999999999997780, 1.000000000000000222, 1.000000000000000222, 0.9999999999999996669, 1.000000000000000444, 0.9999999999999997780, 1.000000000000000000, 1.000000000000000222, 1.000000000000000000, 1.000000000000000000, 1.000000000000000000, 1.000000000000000000, 1.000000000000000222, 1.000000000000000000, 1.000000000000000000, 0.9999999999999997780, 1.000000000000000000, 1.000000000000000000, 1.000000000000000000, 1.000000000000000000, 0.9999999999999997780, 1.000000000000000222, 1.000000000000000000, 1.000000000000000000, 1.000000000000000444, 0.9999999999999997780, 1.000000000000000222, 0.9999999999999996669, 1.000000000000000444, 0.9999999999999997780, 1.000000000000000000, 0.9999999999999997780, 1.000000000000000000, 1.000000000000000222, 0.9999999999999997780, 1.000000000000000444, 0.9999999999999997780, 1.000000000000000000, 0.9999999999999996669, 1.000000000000000444, 0.9999999999999997780, 1.000000000000000444, 1.000000000000000000, 1.000000000000000444, 0.9999999999999996669, 1.000000000000000000, 0.9999999999999996669, 1.000000000000000444, 0.9999999999999997780, 1.000000000000000000, 1.000000000000000000, 1.000000000000000000, 1.000000000000000000, 0.9999999999999996669, 1.000000000000000000, 1.000000000000000222, 0.9999999999999997780, 1.000000000000000000, 0.9999999999999997780, 0.9999999999999997780, 1.000000000000000000, 1.000000000000000222, 0.9999999999999997780, 1.000000000000000000, 1.000000000000000222, 1.000000000000000222, 1.000000000000000222, 0.9999999999999997780, 1.000000000000000000, 1.000000000000000222, 0.9999999999999997780, 1.000000000000000222, 1.000000000000000222, 0.9999999999999997780, 0.9999999999999997780, 0.9999999999999997780, 1.000000000000000444, 1.000000000000000000, 1.000000000000000000, 1.000000000000000000, 1.000000000000000222, 0.9999999999999997780, 1.000000000000000000, 1.000000000000000444, 0.9999999999999996669, 1.000000000000000444, 1.000000000000000000, 1.000000000000000000, 1.000000000000000222, 0.9999999999999997780, 1.000000000000000444, 0.9999999999999996669, 1.000000000000000444, 1.000000000000000000, 0.9999999999999997780, 1.000000000000000222, 0.9999999999999996669, 1.000000000000000222, 1.000000000000000000, 1.000000000000000222, 0.9999999999999997780, 1.000000000000000222, 0.9999999999999996669, 1.000000000000000222, 1.000000000000000222, 1.000000000000000222, 1.000000000000000000, 0.9999999999999997780, 1.000000000000000000, 0.9999999999999997780, 1.000000000000000000, 0.9999999999999997780, 0.9999999999999997780, 1.000000000000000222, 1.000000000000000222, 1.000000000000000222, 0.9999999999999997780, 0.9999999999999997780, 1.000000000000000444, 0.9999999999999997780, 1.000000000000000000, 0.9999999999999997780, 1.000000000000000000, 0.9999999999999997780, 1.000000000000000222, 1.000000000000000000, 1.000000000000000000, 1.000000000000000222, 1.000000000000000000, 0.9999999999999997780, 1.000000000000000444, 1.000000000000000000, 1.000000000000000000, 1.000000000000000444, 0.9999999999999997780, 1.000000000000000222, 0.9999999999999997780, 1.000000000000000444, 1.000000000000000000, 1.000000000000000222, 0.9999999999999997780, 0.9999999999999997780, 1.000000000000000000, 1.000000000000000444, 0.9999999999999996669, 1.000000000000000000, 1.000000000000000222, 1.000000000000000222, 0.9999999999999997780, 1.000000000000000222, 0.9999999999999997780, 1.000000000000000222, 1.000000000000000000, 1.000000000000000000, 0.9999999999999997780, 1.000000000000000444, 0.9999999999999997780, 1.000000000000000222, 0.9999999999999996669, 1.000000000000000444, 0.9999999999999996669, 1.000000000000000222, 1.000000000000000000, 1.000000000000000000, 1.000000000000000000, 1.000000000000000444, 1.000000000000000222, 0.9999999999999997780, 1.000000000000000444, 0.9999999999999997780, 1.000000000000000000, 0.9999999999999996669, 1.000000000000000000, 0.9999999999999996669, 1.000000000000000000, 1.000000000000000222, 1.000000000000000000, 0.9999999999999997780, 1.000000000000000222, 1.000000000000000000, 1.000000000000000222, 0.9999999999999996669, 1.000000000000000000, 1.000000000000000000, 1.000000000000000000, 0.9999999999999997780, 1.000000000000000000, 1.000000000000000000, 1.000000000000000222, 1.000000000000000000, 1.000000000000000000, 0.9999999999999997780, 1.000000000000000000, 1.000000000000000222, 0.9999999999999997780, 1.000000000000000000, 1.000000000000000222, 1.000000000000000000, 1.000000000000000000, 0.9999999999999997780, 0.9999999999999997780, 1.000000000000000000, 1.000000000000000000, 0.9999999999999997780, 1.000000000000000000, 1.000000000000000000, 1.000000000000000000, 1.000000000000000222, 1.000000000000000000, 1.000000000000000000, 0.9999999999999997780, 1.000000000000000000, 0.9999999999999997780, 1.000000000000000444, 0.9999999999999997780, 1.000000000000000222, 0.9999999999999997780, 1.000000000000000444, 0.9999999999999994449, 1.000000000000000444, 0.9999999999999997780, 1.000000000000000222, 1.000000000000000000, 1.000000000000000000, 0.9999999999999997780, 1.000000000000000000, 1.000000000000000000, 0.9999999999999997780, 1.000000000000000000, 1.000000000000000000, 0.9999999999999997780, 1.000000000000000222, 1.000000000000000000, 1.000000000000000222, 0.9999999999999997780, 1.000000000000000222, 0.9999999999999997780, 1.000000000000000222, 0.9999999999999997780, 1.000000000000000444, 0.9999999999999996669, 1.000000000000000222, 0.9999999999999997780, 1.000000000000000000, 1.000000000000000000, 1.000000000000000000, 1.000000000000000222, 1.000000000000000222, 1.000000000000000000, 1.000000000000000444, 1.000000000000000222, 0.9999999999999997780, 1.000000000000000222, 0.9999999999999996669, 1.000000000000000444, 0.9999999999999997780, 0.9999999999999997780, 1.000000000000000222, 1.000000000000000000, 1.000000000000000222, 1.000000000000000000, 1.000000000000000000, 1.000000000000000222, 1.000000000000000000, 0.9999999999999997780, 1.000000000000000222, 0.9999999999999997780, 1.000000000000000000, 1.000000000000000222, 1.000000000000000000, 0.9999999999999997780, 0.9999999999999997780, 1.000000000000000000, 0.9999999999999997780, 1.000000000000000000, 1.000000000000000000, 1.000000000000000000, 1.000000000000000222, 0.9999999999999997780, 1.000000000000000000, 1.000000000000000222, 1.000000000000000000, 0.9999999999999997780, 1.000000000000000000, 1.000000000000000000, 1.000000000000000222, 0.9999999999999997780, 1.000000000000000222, 1.000000000000000000, 1.000000000000000000, 1.000000000000000222, 1.000000000000000000, 1.000000000000000000, 1.000000000000000222, 1.000000000000000000, 1.000000000000000444, 0.9999999999999996669, 1.000000000000000444, 0.9999999999999997780, 1.000000000000000000, 1.000000000000000222, 0.9999999999999996669, 1.000000000000000444, 1.000000000000000000, 1.000000000000000000, 1.000000000000000222, 1.000000000000000444, 1.000000000000000000, 0.9999999999999996669, 1.000000000000000444, 0.9999999999999997780, 0.9999999999999997780, 0.9999999999999997780, 1.000000000000000222, 1.000000000000000000, 0.9999999999999996669, 1.000000000000000222, 1.000000000000000000, 1.000000000000000444, 0.9999999999999997780, 1.000000000000000000, 1.000000000000000222, 1.000000000000000222, 1.000000000000000222, 1.000000000000000222, 1.000000000000000000, 1.000000000000000000, 1.000000000000000000, 1.000000000000000000, 1.000000000000000000, 1.000000000000000444, 1.000000000000000000, 0.9999999999999997780, 1.000000000000000000, 1.000000000000000222, 1.000000000000000000, 1.000000000000000222, 1.000000000000000222, 1.000000000000000000, 0.9999999999999997780, 0.9999999999999997780, 1.000000000000000222, 0.9999999999999997780, 1.000000000000000000, 1.000000000000000222, 1.000000000000000000, 1.000000000000000222, 1.000000000000000000, 0.9999999999999997780, 1.000000000000000000, 0.9999999999999997780, 1.000000000000000222, 1.000000000000000000, 0.9999999999999997780, 0.9999999999999997780, 1.000000000000000222, 1.000000000000000000, 1.000000000000000222, 0.9999999999999996669, 1.000000000000000000, 1.000000000000000222, 0.9999999999999997780, 1.000000000000000000, 1.000000000000000000, 1.000000000000000222, 1.000000000000000222, 1.000000000000000000, 1.000000000000000222, 1.000000000000000222),
 ( 0.3333333333333333703, 0.3333333333333333703, 0.3333333333333333703, 0.3333333333333333703, 0.3333333333333333148, 0.3333333333333334259, 0.3333333333333333703, 0.3333333333333333148, 0.3333333333333334259, 0.3333333333333333148, 0.3333333333333334259, 0.3333333333333332038, 0.3333333333333333703, 0.3333333333333332593, 0.3333333333333333703, 0.3333333333333332593, 0.3333333333333334814, 0.3333333333333334259, 0.3333333333333333703, 0.3333333333333334259, 0.3333333333333334259, 0.3333333333333332038, 0.3333333333333335369, 0.3333333333333333148, 0.3333333333333333148, 0.3333333333333334259, 0.3333333333333333703, 0.3333333333333333148, 0.3333333333333334259, 0.3333333333333333148, 0.3333333333333335369, 0.3333333333333333148, 0.3333333333333334259, 0.3333333333333333148, 0.3333333333333334259, 0.3333333333333333703, 0.3333333333333333148, 0.3333333333333333703, 0.3333333333333334259, 0.3333333333333333703, 0.3333333333333334259, 0.3333333333333333703, 0.3333333333333334814, 0.3333333333333333148, 0.3333333333333334259, 0.3333333333333332593, 0.3333333333333335369, 0.3333333333333332593, 0.3333333333333334259, 0.3333333333333333148, 0.3333333333333333703, 0.3333333333333334259, 0.3333333333333333148, 0.3333333333333334814, 0.3333333333333332593, 0.3333333333333333703, 0.3333333333333332593, 0.3333333333333335369, 0.3333333333333333148, 0.3333333333333334259, 0.3333333333333334259, 0.3333333333333334259, 0.3333333333333333148, 0.3333333333333333148, 0.3333333333333333703, 0.3333333333333333703, 0.3333333333333333703, 0.3333333333333334259, 0.3333333333333333148, 0.3333333333333333703, 0.3333333333333333703, 0.3333333333333332593, 0.3333333333333334259, 0.3333333333333333703, 0.3333333333333333703, 0.3333333333333333148, 0.3333333333333333148, 0.3333333333333334259, 0.3333333333333333148, 0.3333333333333334259, 0.3333333333333333148, 0.3333333333333334259, 0.3333333333333333703, 0.3333333333333334259, 0.3333333333333333703, 0.3333333333333333703, 0.3333333333333333148, 0.3333333333333335369, 0.3333333333333332593, 0.3333333333333334814, 0.3333333333333333703, 0.3333333333333333703, 0.3333333333333333148, 0.3333333333333333703, 0.3333333333333334259, 0.3333333333333334259, 0.3333333333333333148, 0.3333333333333333703, 0.3333333333333334259, 0.3333333333333333148, 0.3333333333333333703, 0.3333333333333334814, 0.3333333333333332038, 0.3333333333333334814, 0.3333333333333333703, 0.3333333333333333148, 0.3333333333333334259, 0.3333333333333333148, 0.3333333333333334259, 0.3333333333333332593, 0.3333333333333333703, 0.3333333333333334259, 0.3333333333333333148, 0.3333333333333333703, 0.3333333333333333148, 0.3333333333333334259, 0.3333333333333333703, 0.3333333333333333703, 0.3333333333333333703, 0.3333333333333334259, 0.3333333333333332038, 0.3333333333333334259, 0.3333333333333334259, 0.3333333333333333703, 0.3333333333333333703, 0.3333333333333332593, 0.3333333333333333703, 0.3333333333333333148, 0.3333333333333334259, 0.3333333333333332593, 0.3333333333333334259, 0.3333333333333333703, 0.3333333333333334259, 0.3333333333333334259, 0.3333333333333333148, 0.3333333333333334259, 0.3333333333333334259, 0.3333333333333332593, 0.3333333333333334259, 0.3333333333333333703, 0.3333333333333333703, 0.3333333333333333148, 0.3333333333333334259, 0.3333333333333333703, 0.3333333333333334259, 0.3333333333333334259, 0.3333333333333333703, 0.3333333333333333703, 0.3333333333333334814, 0.3333333333333333703, 0.3333333333333333703, 0.3333333333333335369, 0.3333333333333332593, 0.3333333333333334259, 0.3333333333333333148, 0.3333333333333334259, 0.3333333333333334259, 0.3333333333333334259, 0.3333333333333332593, 0.3333333333333333148, 0.3333333333333333703, 0.3333333333333334259, 0.3333333333333333148, 0.3333333333333333703, 0.3333333333333333148, 0.3333333333333334259, 0.3333333333333333148, 0.3333333333333334259, 0.3333333333333333148, 0.3333333333333334259, 0.3333333333333333703, 0.3333333333333334259, 0.3333333333333333703, 0.3333333333333334259, 0.3333333333333333148, 0.3333333333333333703, 0.3333333333333333703, 0.3333333333333334259, 0.3333333333333333703, 0.3333333333333334259, 0.3333333333333333703, 0.3333333333333333703, 0.3333333333333334259, 0.3333333333333334814, 0.3333333333333333703, 0.3333333333333333703, 0.3333333333333334814, 0.3333333333333333148, 0.3333333333333333703, 0.3333333333333333148, 0.3333333333333333703, 0.3333333333333333148, 0.3333333333333334259, 0.3333333333333334259, 0.3333333333333333703, 0.3333333333333333703, 0.3333333333333333703, 0.3333333333333333703, 0.3333333333333334259, 0.3333333333333332593, 0.3333333333333333703, 0.3333333333333333703, 0.3333333333333333703, 0.3333333333333333148, 0.3333333333333333703, 0.3333333333333333148, 0.3333333333333334259, 0.3333333333333333148, 0.3333333333333333703, 0.3333333333333333703, 0.3333333333333334259, 0.3333333333333333703, 0.3333333333333333148, 0.3333333333333333703, 0.3333333333333333703, 0.3333333333333333148, 0.3333333333333333703, 0.3333333333333333148, 0.3333333333333333703, 0.3333333333333333703, 0.3333333333333334814, 0.3333333333333333148, 0.3333333333333334259, 0.3333333333333334259, 0.3333333333333333703, 0.3333333333333334259, 0.3333333333333333703, 0.3333333333333334259, 0.3333333333333332593, 0.3333333333333334259, 0.3333333333333333148, 0.3333333333333334259, 0.3333333333333333148, 0.3333333333333334259, 0.3333333333333332593, 0.3333333333333335369, 0.3333333333333332038, 0.3333333333333334259, 0.3333333333333333703, 0.3333333333333333148, 0.3333333333333334259, 0.3333333333333333148, 0.3333333333333333148, 0.3333333333333333148, 0.3333333333333334814, 0.3333333333333332593, 0.3333333333333334259, 0.3333333333333333148, 0.3333333333333333148, 0.3333333333333334814, 0.3333333333333333703, 0.3333333333333334259, 0.3333333333333333148, 0.3333333333333333703, 0.3333333333333332593, 0.3333333333333334814, 0.3333333333333333148, 0.3333333333333334259, 0.3333333333333333148, 0.3333333333333334259, 0.3333333333333333703, 0.3333333333333333703, 0.3333333333333334259, 0.3333333333333333148, 0.3333333333333334814, 0.3333333333333333703, 0.3333333333333333703, 0.3333333333333334814, 0.3333333333333333703, 0.3333333333333332593, 0.3333333333333334259, 0.3333333333333332593, 0.3333333333333334814, 0.3333333333333333148, 0.3333333333333333703, 0.3333333333333333703, 0.3333333333333334259, 0.3333333333333333703, 0.3333333333333333703, 0.3333333333333333148, 0.3333333333333334259, 0.3333333333333334259, 0.3333333333333333703, 0.3333333333333334259, 0.3333333333333333148, 0.3333333333333333703, 0.3333333333333334259, 0.3333333333333333703, 0.3333333333333333148, 0.3333333333333334259, 0.3333333333333333703, 0.3333333333333333148, 0.3333333333333333148, 0.3333333333333334259, 0.3333333333333333148, 0.3333333333333333703, 0.3333333333333333703, 0.3333333333333333703, 0.3333333333333334259, 0.3333333333333334259, 0.3333333333333333148, 0.3333333333333334259, 0.3333333333333333148, 0.3333333333333334814, 0.3333333333333332593, 0.3333333333333334814, 0.3333333333333333703, 0.3333333333333333703, 0.3333333333333334259, 0.3333333333333333703, 0.3333333333333333703, 0.3333333333333333703, 0.3333333333333333703, 0.3333333333333334814, 0.3333333333333333148, 0.3333333333333334259, 0.3333333333333333148, 0.3333333333333333703, 0.3333333333333333703, 0.3333333333333333703, 0.3333333333333335369, 0.3333333333333333703, 0.3333333333333333148, 0.3333333333333334814, 0.3333333333333334259, 0.3333333333333333148, 0.3333333333333333148, 0.3333333333333335369, 0.3333333333333332593, 0.3333333333333333703, 0.3333333333333333148, 0.3333333333333333703, 0.3333333333333333703, 0.3333333333333332593, 0.3333333333333334259, 0.3333333333333332593, 0.3333333333333335369, 0.3333333333333333148, 0.3333333333333333703, 0.3333333333333334259, 0.3333333333333333703, 0.3333333333333333703, 0.3333333333333334814, 0.3333333333333333148, 0.3333333333333333148, 0.3333333333333334259, 0.3333333333333333148, 0.3333333333333333703, 0.3333333333333334814, 0.3333333333333333703, 0.3333333333333333703, 0.3333333333333333703, 0.3333333333333333703, 0.3333333333333334814, 0.3333333333333333703, 0.3333333333333334814, 0.3333333333333333703, 0.3333333333333333703, 0.3333333333333333148, 0.3333333333333334259, 0.3333333333333333148, 0.3333333333333334259, 0.3333333333333333148, 0.3333333333333333703, 0.3333333333333334814, 0.3333333333333333148, 0.3333333333333333148, 0.3333333333333333703, 0.3333333333333333703, 0.3333333333333333703, 0.3333333333333334259, 0.3333333333333333148, 0.3333333333333333703, 0.3333333333333334259, 0.3333333333333333148, 0.3333333333333333703, 0.3333333333333332593, 0.3333333333333333703, 0.3333333333333334259, 0.3333333333333333703, 0.3333333333333333703, 0.3333333333333333703, 0.3333333333333333703, 0.3333333333333334814, 0.3333333333333333703, 0.3333333333333334259, 0.3333333333333334259),
 ( 0.3333333333333333703, 0.3333333333333333703, 0.3333333333333333703, 0.3333333333333333703, 0.3333333333333333148, 0.3333333333333334259, 0.3333333333333333703, 0.3333333333333333148, 0.3333333333333334259, 0.3333333333333333148, 0.3333333333333334259, 0.3333333333333332038, 0.3333333333333333703, 0.3333333333333332593, 0.3333333333333333703, 0.3333333333333332593, 0.3333333333333334814, 0.3333333333333334259, 0.3333333333333333703, 0.3333333333333334259, 0.3333333333333334259, 0.3333333333333332038, 0.3333333333333335369, 0.3333333333333333148, 0.3333333333333333148, 0.3333333333333334259, 0.3333333333333333703, 0.3333333333333333148, 0.3333333333333334259, 0.3333333333333333148, 0.3333333333333335369, 0.3333333333333333148, 0.3333333333333334259, 0.3333333333333333148, 0.3333333333333334259, 0.3333333333333333703, 0.3333333333333333148, 0.3333333333333333703, 0.3333333333333334259, 0.3333333333333333703, 0.3333333333333334259, 0.3333333333333333703, 0.3333333333333334814, 0.3333333333333333148, 0.3333333333333334259, 0.3333333333333332593, 0.3333333333333335369, 0.3333333333333332593, 0.3333333333333334259, 0.3333333333333333148, 0.3333333333333333703, 0.3333333333333334259, 0.3333333333333333148, 0.3333333333333334814, 0.3333333333333332593, 0.3333333333333333703, 0.3333333333333332593, 0.3333333333333335369, 0.3333333333333333148, 0.3333333333333334259, 0.3333333333333334259, 0.3333333333333334259, 0.3333333333333333148, 0.3333333333333333148, 0.3333333333333333703, 0.3333333333333333703, 0.3333333333333333703, 0.3333333333333334259, 0.3333333333333333148, 0.3333333333333333703, 0.3333333333333333703, 0.3333333333333332593, 0.3333333333333334259, 0.3333333333333333703, 0.3333333333333333703, 0.3333333333333333148, 0.3333333333333333148, 0.3333333333333334259, 0.3333333333333333148, 0.3333333333333334259, 0.3333333333333333148, 0.3333333333333334259, 0.3333333333333333703, 0.3333333333333334259, 0.3333333333333333703, 0.3333333333333333703, 0.3333333333333333148, 0.3333333333333335369, 0.3333333333333332593, 0.3333333333333334814, 0.3333333333333333703, 0.3333333333333333703, 0.3333333333333333148, 0.3333333333333333703, 0.3333333333333334259, 0.3333333333333334259, 0.3333333333333333148, 0.3333333333333333703, 0.3333333333333334259, 0.3333333333333333148, 0.3333333333333333703, 0.3333333333333334814, 0.3333333333333332038, 0.3333333333333334814, 0.3333333333333333703, 0.3333333333333333148, 0.3333333333333334259, 0.3333333333333333148, 0.3333333333333334259, 0.3333333333333332593, 0.3333333333333333703, 0.3333333333333334259, 0.3333333333333333148, 0.3333333333333333703, 0.3333333333333333148, 0.3333333333333334259, 0.3333333333333333703, 0.3333333333333333703, 0.3333333333333333703, 0.3333333333333334259, 0.3333333333333332038, 0.3333333333333334259, 0.3333333333333334259, 0.3333333333333333703, 0.3333333333333333703, 0.3333333333333332593, 0.3333333333333333703, 0.3333333333333333148, 0.3333333333333334259, 0.3333333333333332593, 0.3333333333333334259, 0.3333333333333333703, 0.3333333333333334259, 0.3333333333333334259, 0.3333333333333333148, 0.3333333333333334259, 0.3333333333333334259, 0.3333333333333332593, 0.3333333333333334259, 0.3333333333333333703, 0.3333333333333333703, 0.3333333333333333148, 0.3333333333333334259, 0.3333333333333333703, 0.3333333333333334259, 0.3333333333333334259, 0.3333333333333333703, 0.3333333333333333703, 0.3333333333333334814, 0.3333333333333333703, 0.3333333333333333703, 0.3333333333333335369, 0.3333333333333332593, 0.3333333333333334259, 0.3333333333333333148, 0.3333333333333334259, 0.3333333333333334259, 0.3333333333333334259, 0.3333333333333332593, 0.3333333333333333148, 0.3333333333333333703, 0.3333333333333334259, 0.3333333333333333148, 0.3333333333333333703, 0.3333333333333333148, 0.3333333333333334259, 0.3333333333333333148, 0.3333333333333334259, 0.3333333333333333148, 0.3333333333333334259, 0.3333333333333333703, 0.3333333333333334259, 0.3333333333333333703, 0.3333333333333334259, 0.3333333333333333148, 0.3333333333333333703, 0.3333333333333333703, 0.3333333333333334259, 0.3333333333333333703, 0.3333333333333334259, 0.3333333333333333703, 0.3333333333333333703, 0.3333333333333334259, 0.3333333333333334814, 0.3333333333333333703, 0.3333333333333333703, 0.3333333333333334814, 0.3333333333333333148, 0.3333333333333333703, 0.3333333333333333148, 0.3333333333333333703, 0.3333333333333333148, 0.3333333333333334259, 0.3333333333333334259, 0.3333333333333333703, 0.3333333333333333703, 0.3333333333333333703, 0.3333333333333333703, 0.3333333333333334259, 0.3333333333333332593, 0.3333333333333333703, 0.3333333333333333703, 0.3333333333333333703, 0.3333333333333333148, 0.3333333333333333703, 0.3333333333333333148, 0.3333333333333334259, 0.3333333333333333148, 0.3333333333333333703, 0.3333333333333333703, 0.3333333333333334259, 0.3333333333333333703, 0.3333333333333333148, 0.3333333333333333703, 0.3333333333333333703, 0.3333333333333333148, 0.3333333333333333703, 0.3333333333333333148, 0.3333333333333333703, 0.3333333333333333703, 0.3333333333333334814, 0.3333333333333333148, 0.3333333333333334259, 0.3333333333333334259, 0.3333333333333333703, 0.3333333333333334259, 0.3333333333333333703, 0.3333333333333334259, 0.3333333333333332593, 0.3333333333333334259, 0.3333333333333333148, 0.3333333333333334259, 0.3333333333333333148, 0.3333333333333334259, 0.3333333333333332593, 0.3333333333333335369, 0.3333333333333332038, 0.3333333333333334259, 0.3333333333333333703, 0.3333333333333333148, 0.3333333333333334259, 0.3333333333333333148, 0.3333333333333333148, 0.3333333333333333148, 0.3333333333333334814, 0.3333333333333332593, 0.3333333333333334259, 0.3333333333333333148, 0.3333333333333333148, 0.3333333333333334814, 0.3333333333333333703, 0.3333333333333334259, 0.3333333333333333148, 0.3333333333333333703, 0.3333333333333332593, 0.3333333333333334814, 0.3333333333333333148, 0.3333333333333334259, 0.3333333333333333148, 0.3333333333333334259, 0.3333333333333333703, 0.3333333333333333703, 0.3333333333333334259, 0.3333333333333333148, 0.3333333333333334814, 0.3333333333333333703, 0.3333333333333333703, 0.3333333333333334814, 0.3333333333333333703, 0.3333333333333332593, 0.3333333333333334259, 0.3333333333333332593, 0.3333333333333334814, 0.3333333333333333148, 0.3333333333333333703, 0.3333333333333333703, 0.3333333333333334259, 0.3333333333333333703, 0.3333333333333333703, 0.3333333333333333148, 0.3333333333333334259, 0.3333333333333334259, 0.3333333333333333703, 0.3333333333333334259, 0.3333333333333333148, 0.3333333333333333703, 0.3333333333333334259, 0.3333333333333333703, 0.3333333333333333148, 0.3333333333333334259, 0.3333333333333333703, 0.3333333333333333148, 0.3333333333333333148, 0.3333333333333334259, 0.3333333333333333148, 0.3333333333333333703, 0.3333333333333333703, 0.3333333333333333703, 0.3333333333333334259, 0.3333333333333334259, 0.3333333333333333148, 0.3333333333333334259, 0.3333333333333333148, 0.3333333333333334814, 0.3333333333333332593, 0.3333333333333334814, 0.3333333333333333703, 0.3333333333333333703, 0.3333333333333334259, 0.3333333333333333703, 0.3333333333333333703, 0.3333333333333333703, 0.3333333333333333703, 0.3333333333333334814, 0.3333333333333333148, 0.3333333333333334259, 0.3333333333333333148, 0.3333333333333333703, 0.3333333333333333703, 0.3333333333333333703, 0.3333333333333335369, 0.3333333333333333703, 0.3333333333333333148, 0.3333333333333334814, 0.3333333333333334259, 0.3333333333333333148, 0.3333333333333333148, 0.3333333333333335369, 0.3333333333333332593, 0.3333333333333333703, 0.3333333333333333148, 0.3333333333333333703, 0.3333333333333333703, 0.3333333333333332593, 0.3333333333333334259, 0.3333333333333332593, 0.3333333333333335369, 0.3333333333333333148, 0.3333333333333333703, 0.3333333333333334259, 0.3333333333333333703, 0.3333333333333333703, 0.3333333333333334814, 0.3333333333333333148, 0.3333333333333333148, 0.3333333333333334259, 0.3333333333333333148, 0.3333333333333333703, 0.3333333333333334814, 0.3333333333333333703, 0.3333333333333333703, 0.3333333333333333703, 0.3333333333333333703, 0.3333333333333334814, 0.3333333333333333703, 0.3333333333333334814, 0.3333333333333333703, 0.3333333333333333703, 0.3333333333333333148, 0.3333333333333334259, 0.3333333333333333148, 0.3333333333333334259, 0.3333333333333333148, 0.3333333333333333703, 0.3333333333333334814, 0.3333333333333333148, 0.3333333333333333148, 0.3333333333333333703, 0.3333333333333333703, 0.3333333333333333703, 0.3333333333333334259, 0.3333333333333333148, 0.3333333333333333703, 0.3333333333333334259, 0.3333333333333333148, 0.3333333333333333703, 0.3333333333333332593, 0.3333333333333333703, 0.3333333333333334259, 0.3333333333333333703, 0.3333333333333333703, 0.3333333333333333703, 0.3333333333333333703, 0.3333333333333334814, 0.3333333333333333703, 0.3333333333333334259, 0.3333333333333334259),
 ( 1.000000000000000000, 1.000000000000000000, 1.000000000000000222, 1.000000000000000000, 0.9999999999999996669, 1.000000000000000444, 0.9999999999999997780, 1.000000000000000000, 1.000000000000000222, 0.9999999999999996669, 1.000000000000000222, 0.9999999999999996669, 1.000000000000000000, 0.9999999999999997780, 1.000000000000000222, 0.9999999999999997780, 1.000000000000000222, 1.000000000000000222, 0.9999999999999997780, 1.000000000000000222, 1.000000000000000222, 0.9999999999999996669, 1.000000000000000444, 0.9999999999999997780, 1.000000000000000000, 1.000000000000000222, 1.000000000000000000, 1.000000000000000000, 1.000000000000000000, 1.000000000000000000, 1.000000000000000222, 1.000000000000000000, 1.000000000000000000, 0.9999999999999997780, 1.000000000000000000, 1.000000000000000000, 1.000000000000000000, 1.000000000000000000, 0.9999999999999997780, 1.000000000000000222, 1.000000000000000000, 1.000000000000000000, 1.000000000000000444, 0.9999999999999997780, 1.000000000000000222, 0.9999999999999996669, 1.000000000000000444, 0.9999999999999997780, 1.000000000000000000, 0.9999999999999997780, 1.000000000000000000, 1.000000000000000222, 0.9999999999999997780, 1.000000000000000444, 0.9999999999999997780, 1.000000000000000000, 0.9999999999999996669, 1.000000000000000444, 0.9999999999999997780, 1.000000000000000444, 1.000000000000000000, 1.000000000000000444, 0.9999999999999996669, 1.000000000000000000, 0.9999999999999996669, 1.000000000000000444, 0.9999999999999997780, 1.000000000000000000, 1.000000000000000000, 1.000000000000000000, 1.000000000000000000, 0.9999999999999996669, 1.000000000000000000, 1.000000000000000222, 0.9999999999999997780, 1.000000000000000000, 0.9999999999999997780, 0.9999999999999997780, 1.000000000000000000, 1.000000000000000222, 0.9999999999999997780, 1.000000000000000000, 1.000000000000000222, 1.000000000000000222, 1.000000000000000222, 0.9999999999999997780, 1.000000000000000000, 1.000000000000000222, 0.9999999999999997780, 1.000000000000000222, 1.000000000000000222, 0.9999999999999997780, 0.9999999999999997780, 0.9999999999999997780, 1.000000000000000444, 1.000000000000000000, 1.000000000000000000, 1.000000000000000000, 1.000000000000000222, 0.9999999999999997780, 1.000000000000000000, 1.000000000000000444, 0.9999999999999996669, 1.000000000000000444, 1.000000000000000000, 1.000000000000000000, 1.000000000000000222, 0.9999999999999997780, 1.000000000000000444, 0.9999999999999996669, 1.000000000000000444, 1.000000000000000000, 0.9999999999999997780, 1.000000000000000222, 0.9999999999999996669, 1.000000000000000222, 1.000000000000000000, 1.000000000000000222, 0.9999999999999997780, 1.000000000000000222, 0.9999999999999996669, 1.000000000000000222, 1.000000000000000222, 1.000000000000000222, 1.000000000000000000, 0.9999999999999997780, 1.000000000000000000, 0.9999999999999997780, 1.000000000000000000, 0.9999999999999997780, 0.9999999999999997780, 1.000000000000000222, 1.000000000000000222, 1.000000000000000222, 0.9999999999999997780, 0.9999999999999997780, 1.000000000000000444, 0.9999999999999997780, 1.000000000000000000, 0.9999999999999997780, 1.000000000000000000, 0.9999999999999997780, 1.000000000000000222, 1.000000000000000000, 1.000000000000000000, 1.000000000000000222, 1.000000000000000000, 0.9999999999999997780, 1.000000000000000444, 1.000000000000000000, 1.000000000000000000, 1.000000000000000444, 0.9999999999999997780, 1.000000000000000222, 0.9999999999999997780, 1.000000000000000444, 1.000000000000000000, 1.000000000000000222, 0.9999999999999997780, 0.9999999999999997780, 1.000000000000000000, 1.000000000000000444, 0.9999999999999996669, 1.000000000000000000, 1.000000000000000222, 1.000000000000000222, 0.9999999999999997780, 1.000000000000000222, 0.9999999999999997780, 1.000000000000000222, 1.000000000000000000, 1.000000000000000000, 0.9999999999999997780, 1.000000000000000444, 0.9999999999999997780, 1.000000000000000222, 0.9999999999999996669, 1.000000000000000444, 0.9999999999999996669, 1.000000000000000222, 1.000000000000000000, 1.000000000000000000, 1.000000000000000000, 1.000000000000000444, 1.000000000000000222, 0.9999999999999997780, 1.000000000000000444, 0.9999999999999997780, 1.000000000000000000, 0.9999999999999996669, 1.000000000000000000, 0.9999999999999996669, 1.000000000000000000, 1.000000000000000222, 1.000000000000000000, 0.9999999999999997780, 1.000000000000000222, 1.000000000000000000, 1.000000000000000222, 0.9999999999999996669, 1.000000000000000000, 1.000000000000000000, 1.000000000000000000, 0.9999999999999997780, 1.000000000000000000, 1.000000000000000000, 1.000000000000000222, 1.000000000000000000, 1.000000000000000000, 0.9999999999999997780, 1.000000000000000000, 1.000000000000000222, 0.9999999999999997780, 1.000000000000000000, 1.000000000000000222, 1.000000000000000000, 1.000000000000000000, 0.9999999999999997780, 0.9999999999999997780, 1.000000000000000000, 1.000000000000000000, 0.9999999999999997780, 1.000000000000000000, 1.000000000000000000, 1.000000000000000000, 1.000000000000000222, 1.000000000000000000, 1.000000000000000000, 0.9999999999999997780, 1.000000000000000000, 0.9999999999999997780, 1.000000000000000444, 0.9999999999999997780, 1.000000000000000222, 0.9999999999999997780, 1.000000000000000444, 0.9999999999999994449, 1.000000000000000444, 0.9999999999999997780, 1.000000000000000222, 1.000000000000000000, 1.000000000000000000, 0.9999999999999997780, 1.000000000000000000, 1.000000000000000000, 0.9999999999999997780, 1.000000000000000000, 1.000000000000000000, 0.9999999999999997780, 1.000000000000000222, 1.000000000000000000, 1.000000000000000222, 0.9999999999999997780, 1.000000000000000222, 0.9999999999999997780, 1.000000000000000222, 0.9999999999999997780, 1.000000000000000444, 0.9999999999999996669, 1.000000000000000222, 0.9999999999999997780, 1.000000000000000000, 1.000000000000000000, 1.000000000000000000, 1.000000000000000222, 1.000000000000000222, 1.000000000000000000, 1.000000000000000444, 1.000000000000000222, 0.9999999999999997780, 1.000000000000000222, 0.9999999999999996669, 1.000000000000000444, 0.9999999999999997780, 0.9999999999999997780, 1.000000000000000222, 1.000000000000000000, 1.000000000000000222, 1.000000000000000000, 1.000000000000000000, 1.000000000000000222, 1.000000000000000000, 0.9999999999999997780, 1.000000000000000222, 0.9999999999999997780, 1.000000000000000000, 1.000000000000000222, 1.000000000000000000, 0.9999999999999997780, 0.9999999999999997780, 1.000000000000000000, 0.9999999999999997780, 1.000000000000000000, 1.000000000000000000, 1.000000000000000000, 1.000000000000000222, 0.9999999999999997780, 1.000000000000000000, 1.000000000000000222, 1.000000000000000000, 0.9999999999999997780, 1.000000000000000000, 1.000000000000000000, 1.000000000000000222, 0.9999999999999997780, 1.000000000000000222, 1.000000000000000000, 1.000000000000000000, 1.000000000000000222, 1.000000000000000000, 1.000000000000000000, 1.000000000000000222, 1.000000000000000000, 1.000000000000000444, 0.9999999999999996669, 1.000000000000000444, 0.9999999999999997780, 1.000000000000000000, 1.000000000000000222, 0.9999999999999996669, 1.000000000000000444, 1.000000000000000000, 1.000000000000000000, 1.000000000000000222, 1.000000000000000444, 1.000000000000000000, 0.9999999999999996669, 1.000000000000000444, 0.9999999999999997780, 0.9999999999999997780, 0.9999999999999997780, 1.000000000000000222, 1.000000000000000000, 0.9999999999999996669, 1.000000000000000222, 1.000000000000000000, 1.000000000000000444, 0.9999999999999997780, 1.000000000000000000, 1.000000000000000222, 1.000000000000000222, 1.000000000000000222, 1.000000000000000222, 1.000000000000000000, 1.000000000000000000, 1.000000000000000000, 1.000000000000000000, 1.000000000000000000, 1.000000000000000444, 1.000000000000000000, 0.9999999999999997780, 1.000000000000000000, 1.000000000000000222, 1.000000000000000000, 1.000000000000000222, 1.000000000000000222, 1.000000000000000000, 0.9999999999999997780, 0.9999999999999997780, 1.000000000000000222, 0.9999999999999997780, 1.000000000000000000, 1.000000000000000222, 1.000000000000000000, 1.000000000000000222, 1.000000000000000000, 0.9999999999999997780, 1.000000000000000000, 0.9999999999999997780, 1.000000000000000222, 1.000000000000000000, 0.9999999999999997780, 0.9999999999999997780, 1.000000000000000222, 1.000000000000000000, 1.000000000000000222, 0.9999999999999996669, 1.000000000000000000, 1.000000000000000222, 0.9999999999999997780, 1.000000000000000000, 1.000000000000000000, 1.000000000000000222, 1.000000000000000222, 1.000000000000000000, 1.000000000000000222, 1.000000000000000222),
 ( 0.3333333333333333703, 0.3333333333333333703, 0.3333333333333333703, 0.3333333333333333703, 0.3333333333333333148, 0.3333333333333334259, 0.3333333333333333703, 0.3333333333333333148, 0.3333333333333334259, 0.3333333333333333148, 0.3333333333333334259, 0.3333333333333332038, 0.3333333333333333703, 0.3333333333333332593, 0.3333333333333333703, 0.3333333333333332593, 0.3333333333333334814, 0.3333333333333334259, 0.3333333333333333703, 0.3333333333333334259, 0.3333333333333334259, 0.3333333333333332038, 0.3333333333333335369, 0.3333333333333333148, 0.3333333333333333148, 0.3333333333333334259, 0.3333333333333333703, 0.3333333333333333148, 0.3333333333333334259, 0.3333333333333333148, 0.3333333333333335369, 0.3333333333333333148, 0.3333333333333334259, 0.3333333333333333148, 0.3333333333333334259, 0.3333333333333333703, 0.3333333333333333148, 0.3333333333333333703, 0.3333333333333334259, 0.3333333333333333703, 0.3333333333333334259, 0.3333333333333333703, 0.3333333333333334814, 0.3333333333333333148, 0.3333333333333334259, 0.3333333333333332593, 0.3333333333333335369, 0.3333333333333332593, 0.3333333333333334259, 0.3333333333333333148, 0.3333333333333333703, 0.3333333333333334259, 0.3333333333333333148, 0.3333333333333334814, 0.3333333333333332593, 0.3333333333333333703, 0.3333333333333332593, 0.3333333333333335369, 0.3333333333333333148, 0.3333333333333334259, 0.3333333333333334259, 0.3333333333333334259, 0.3333333333333333148, 0.3333333333333333148, 0.3333333333333333703, 0.3333333333333333703, 0.3333333333333333703, 0.3333333333333334259, 0.3333333333333333148, 0.3333333333333333703, 0.3333333333333333703, 0.3333333333333332593, 0.3333333333333334259, 0.3333333333333333703, 0.3333333333333333703, 0.3333333333333333148, 0.3333333333333333148, 0.3333333333333334259, 0.3333333333333333148, 0.3333333333333334259, 0.3333333333333333148, 0.3333333333333334259, 0.3333333333333333703, 0.3333333333333334259, 0.3333333333333333703, 0.3333333333333333703, 0.3333333333333333148, 0.3333333333333335369, 0.3333333333333332593, 0.3333333333333334814, 0.3333333333333333703, 0.3333333333333333703, 0.3333333333333333148, 0.3333333333333333703, 0.3333333333333334259, 0.3333333333333334259, 0.3333333333333333148, 0.3333333333333333703, 0.3333333333333334259, 0.3333333333333333148, 0.3333333333333333703, 0.3333333333333334814, 0.3333333333333332038, 0.3333333333333334814, 0.3333333333333333703, 0.3333333333333333148, 0.3333333333333334259, 0.3333333333333333148, 0.3333333333333334259, 0.3333333333333332593, 0.3333333333333333703, 0.3333333333333334259, 0.3333333333333333148, 0.3333333333333333703, 0.3333333333333333148, 0.3333333333333334259, 0.3333333333333333703, 0.3333333333333333703, 0.3333333333333333703, 0.3333333333333334259, 0.3333333333333332038, 0.3333333333333334259, 0.3333333333333334259, 0.3333333333333333703, 0.3333333333333333703, 0.3333333333333332593, 0.3333333333333333703, 0.3333333333333333148, 0.3333333333333334259, 0.3333333333333332593, 0.3333333333333334259, 0.3333333333333333703, 0.3333333333333334259, 0.3333333333333334259, 0.3333333333333333148, 0.3333333333333334259, 0.3333333333333334259, 0.3333333333333332593, 0.3333333333333334259, 0.3333333333333333703, 0.3333333333333333703, 0.3333333333333333148, 0.3333333333333334259, 0.3333333333333333703, 0.3333333333333334259, 0.3333333333333334259, 0.3333333333333333703, 0.3333333333333333703, 0.3333333333333334814, 0.3333333333333333703, 0.3333333333333333703, 0.3333333333333335369, 0.3333333333333332593, 0.3333333333333334259, 0.3333333333333333148, 0.3333333333333334259, 0.3333333333333334259, 0.3333333333333334259, 0.3333333333333332593, 0.3333333333333333148, 0.3333333333333333703, 0.3333333333333334259, 0.3333333333333333148, 0.3333333333333333703, 0.3333333333333333148, 0.3333333333333334259, 0.3333333333333333148, 0.3333333333333334259, 0.3333333333333333148, 0.3333333333333334259, 0.3333333333333333703, 0.3333333333333334259, 0.3333333333333333703, 0.3333333333333334259, 0.3333333333333333148, 0.3333333333333333703, 0.3333333333333333703, 0.3333333333333334259, 0.3333333333333333703, 0.3333333333333334259, 0.3333333333333333703, 0.3333333333333333703, 0.3333333333333334259, 0.3333333333333334814, 0.3333333333333333703, 0.3333333333333333703, 0.3333333333333334814, 0.3333333333333333148, 0.3333333333333333703, 0.3333333333333333148, 0.3333333333333333703, 0.3333333333333333148, 0.3333333333333334259, 0.3333333333333334259, 0.3333333333333333703, 0.3333333333333333703, 0.3333333333333333703, 0.3333333333333333703, 0.3333333333333334259, 0.3333333333333332593, 0.3333333333333333703, 0.3333333333333333703, 0.3333333333333333703, 0.3333333333333333148, 0.3333333333333333703, 0.3333333333333333148, 0.3333333333333334259, 0.3333333333333333148, 0.3333333333333333703, 0.3333333333333333703, 0.3333333333333334259, 0.3333333333333333703, 0.3333333333333333148, 0.3333333333333333703, 0.3333333333333333703, 0.3333333333333333148, 0.3333333333333333703, 0.3333333333333333148, 0.3333333333333333703, 0.3333333333333333703, 0.3333333333333334814, 0.3333333333333333148, 0.3333333333333334259, 0.3333333333333334259, 0.3333333333333333703, 0.3333333333333334259, 0.3333333333333333703, 0.3333333333333334259, 0.3333333333333332593, 0.3333333333333334259, 0.3333333333333333148, 0.3333333333333334259, 0.3333333333333333148, 0.3333333333333334259, 0.3333333333333332593, 0.3333333333333335369, 0.3333333333333332038, 0.3333333333333334259, 0.3333333333333333703, 0.3333333333333333148, 0.3333333333333334259, 0.3333333333333333148, 0.3333333333333333148, 0.3333333333333333148, 0.3333333333333334814, 0.3333333333333332593, 0.3333333333333334259, 0.3333333333333333148, 0.3333333333333333148, 0.3333333333333334814, 0.3333333333333333703, 0.3333333333333334259, 0.3333333333333333148, 0.3333333333333333703, 0.3333333333333332593, 0.3333333333333334814, 0.3333333333333333148, 0.3333333333333334259, 0.3333333333333333148, 0.3333333333333334259, 0.3333333333333333703, 0.3333333333333333703, 0.3333333333333334259, 0.3333333333333333148, 0.3333333333333334814, 0.3333333333333333703, 0.3333333333333333703, 0.3333333333333334814, 0.3333333333333333703, 0.3333333333333332593, 0.3333333333333334259, 0.3333333333333332593, 0.3333333333333334814, 0.3333333333333333148, 0.3333333333333333703, 0.3333333333333333703, 0.3333333333333334259, 0.3333333333333333703, 0.3333333333333333703, 0.3333333333333333148, 0.3333333333333334259, 0.3333333333333334259, 0.3333333333333333703, 0.3333333333333334259, 0.3333333333333333148, 0.3333333333333333703, 0.3333333333333334259, 0.3333333333333333703, 0.3333333333333333148, 0.3333333333333334259, 0.3333333333333333703, 0.3333333333333333148, 0.3333333333333333148, 0.3333333333333334259, 0.3333333333333333148, 0.3333333333333333703, 0.3333333333333333703, 0.3333333333333333703, 0.3333333333333334259, 0.3333333333333334259, 0.3333333333333333148, 0.3333333333333334259, 0.3333333333333333148, 0.3333333333333334814, 0.3333333333333332593, 0.3333333333333334814, 0.3333333333333333703, 0.3333333333333333703, 0.3333333333333334259, 0.3333333333333333703, 0.3333333333333333703, 0.3333333333333333703, 0.3333333333333333703, 0.3333333333333334814, 0.3333333333333333148, 0.3333333333333334259, 0.3333333333333333148, 0.3333333333333333703, 0.3333333333333333703, 0.3333333333333333703, 0.3333333333333335369, 0.3333333333333333703, 0.3333333333333333148, 0.3333333333333334814, 0.3333333333333334259, 0.3333333333333333148, 0.3333333333333333148, 0.3333333333333335369, 0.3333333333333332593, 0.3333333333333333703, 0.3333333333333333148, 0.3333333333333333703, 0.3333333333333333703, 0.3333333333333332593, 0.3333333333333334259, 0.3333333333333332593, 0.3333333333333335369, 0.3333333333333333148, 0.3333333333333333703, 0.3333333333333334259, 0.3333333333333333703, 0.3333333333333333703, 0.3333333333333334814, 0.3333333333333333148, 0.3333333333333333148, 0.3333333333333334259, 0.3333333333333333148, 0.3333333333333333703, 0.3333333333333334814, 0.3333333333333333703, 0.3333333333333333703, 0.3333333333333333703, 0.3333333333333333703, 0.3333333333333334814, 0.3333333333333333703, 0.3333333333333334814, 0.3333333333333333703, 0.3333333333333333703, 0.3333333333333333148, 0.3333333333333334259, 0.3333333333333333148, 0.3333333333333334259, 0.3333333333333333148, 0.3333333333333333703, 0.3333333333333334814, 0.3333333333333333148, 0.3333333333333333148, 0.3333333333333333703, 0.3333333333333333703, 0.3333333333333333703, 0.3333333333333334259, 0.3333333333333333148, 0.3333333333333333703, 0.3333333333333334259, 0.3333333333333333148, 0.3333333333333333703, 0.3333333333333332593, 0.3333333333333333703, 0.3333333333333334259, 0.3333333333333333703, 0.3333333333333333703, 0.3333333333333333703, 0.3333333333333333703, 0.3333333333333334814, 0.3333333333333333703, 0.3333333333333334259, 0.3333333333333334259),
 ( 0.3333333333333333703, 0.3333333333333333703, 0.3333333333333333703, 0.3333333333333333703, 0.3333333333333333148, 0.3333333333333334259, 0.3333333333333333703, 0.3333333333333333148, 0.3333333333333334259, 0.3333333333333333148, 0.3333333333333334259, 0.3333333333333332038, 0.3333333333333333703, 0.3333333333333332593, 0.3333333333333333703, 0.3333333333333332593, 0.3333333333333334814, 0.3333333333333334259, 0.3333333333333333703, 0.3333333333333334259, 0.3333333333333334259, 0.3333333333333332038, 0.3333333333333335369, 0.3333333333333333148, 0.3333333333333333148, 0.3333333333333334259, 0.3333333333333333703, 0.3333333333333333148, 0.3333333333333334259, 0.3333333333333333148, 0.3333333333333335369, 0.3333333333333333148, 0.3333333333333334259, 0.3333333333333333148, 0.3333333333333334259, 0.3333333333333333703, 0.3333333333333333148, 0.3333333333333333703, 0.3333333333333334259, 0.3333333333333333703, 0.3333333333333334259, 0.3333333333333333703, 0.3333333333333334814, 0.3333333333333333148, 0.3333333333333334259, 0.3333333333333332593, 0.3333333333333335369, 0.3333333333333332593, 0.3333333333333334259, 0.3333333333333333148, 0.3333333333333333703, 0.3333333333333334259, 0.3333333333333333148, 0.3333333333333334814, 0.3333333333333332593, 0.3333333333333333703, 0.3333333333333332593, 0.3333333333333335369, 0.3333333333333333148, 0.3333333333333334259, 0.3333333333333334259, 0.3333333333333334259, 0.3333333333333333148, 0.3333333333333333148, 0.3333333333333333703, 0.3333333333333333703, 0.3333333333333333703, 0.3333333333333334259, 0.3333333333333333148, 0.3333333333333333703, 0.3333333333333333703, 0.3333333333333332593, 0.3333333333333334259, 0.3333333333333333703, 0.3333333333333333703, 0.3333333333333333148, 0.3333333333333333148, 0.3333333333333334259, 0.3333333333333333148, 0.3333333333333334259, 0.3333333333333333148, 0.3333333333333334259, 0.3333333333333333703, 0.3333333333333334259, 0.3333333333333333703, 0.3333333333333333703, 0.3333333333333333148, 0.3333333333333335369, 0.3333333333333332593, 0.3333333333333334814, 0.3333333333333333703, 0.3333333333333333703, 0.3333333333333333148, 0.3333333333333333703, 0.3333333333333334259, 0.3333333333333334259, 0.3333333333333333148, 0.3333333333333333703, 0.3333333333333334259, 0.3333333333333333148, 0.3333333333333333703, 0.3333333333333334814, 0.3333333333333332038, 0.3333333333333334814, 0.3333333333333333703, 0.3333333333333333148, 0.3333333333333334259, 0.3333333333333333148, 0.3333333333333334259, 0.3333333333333332593, 0.3333333333333333703, 0.3333333333333334259, 0.3333333333333333148, 0.3333333333333333703, 0.3333333333333333148, 0.3333333333333334259, 0.3333333333333333703, 0.3333333333333333703, 0.3333333333333333703, 0.3333333333333334259, 0.3333333333333332038, 0.3333333333333334259, 0.3333333333333334259, 0.3333333333333333703, 0.3333333333333333703, 0.3333333333333332593, 0.3333333333333333703, 0.3333333333333333148, 0.3333333333333334259, 0.3333333333333332593, 0.3333333333333334259, 0.3333333333333333703, 0.3333333333333334259, 0.3333333333333334259, 0.3333333333333333148, 0.3333333333333334259, 0.3333333333333334259, 0.3333333333333332593, 0.3333333333333334259, 0.3333333333333333703, 0.3333333333333333703, 0.3333333333333333148, 0.3333333333333334259, 0.3333333333333333703, 0.3333333333333334259, 0.3333333333333334259, 0.3333333333333333703, 0.3333333333333333703, 0.3333333333333334814, 0.3333333333333333703, 0.3333333333333333703, 0.3333333333333335369, 0.3333333333333332593, 0.3333333333333334259, 0.3333333333333333148, 0.3333333333333334259, 0.3333333333333334259, 0.3333333333333334259, 0.3333333333333332593, 0.3333333333333333148, 0.3333333333333333703, 0.3333333333333334259, 0.3333333333333333148, 0.3333333333333333703, 0.3333333333333333148, 0.3333333333333334259, 0.3333333333333333148, 0.3333333333333334259, 0.3333333333333333148, 0.3333333333333334259, 0.3333333333333333703, 0.3333333333333334259, 0.3333333333333333703, 0.3333333333333334259, 0.3333333333333333148, 0.3333333333333333703, 0.3333333333333333703, 0.3333333333333334259, 0.3333333333333333703, 0.3333333333333334259, 0.3333333333333333703, 0.3333333333333333703, 0.3333333333333334259, 0.3333333333333334814, 0.3333333333333333703, 0.3333333333333333703, 0.3333333333333334814, 0.3333333333333333148, 0.3333333333333333703, 0.3333333333333333148, 0.3333333333333333703, 0.3333333333333333148, 0.3333333333333334259, 0.3333333333333334259, 0.3333333333333333703, 0.3333333333333333703, 0.3333333333333333703, 0.3333333333333333703, 0.3333333333333334259, 0.3333333333333332593, 0.3333333333333333703, 0.3333333333333333703, 0.3333333333333333703, 0.3333333333333333148, 0.3333333333333333703, 0.3333333333333333148, 0.3333333333333334259, 0.3333333333333333148, 0.3333333333333333703, 0.3333333333333333703, 0.3333333333333334259, 0.3333333333333333703, 0.3333333333333333148, 0.3333333333333333703, 0.3333333333333333703, 0.3333333333333333148, 0.3333333333333333703, 0.3333333333333333148, 0.3333333333333333703, 0.3333333333333333703, 0.3333333333333334814, 0.3333333333333333148, 0.3333333333333334259, 0.3333333333333334259, 0.3333333333333333703, 0.3333333333333334259, 0.3333333333333333703, 0.3333333333333334259, 0.3333333333333332593, 0.3333333333333334259, 0.3333333333333333148, 0.3333333333333334259, 0.3333333333333333148, 0.3333333333333334259, 0.3333333333333332593, 0.3333333333333335369, 0.3333333333333332038, 0.3333333333333334259, 0.3333333333333333703, 0.3333333333333333148, 0.3333333333333334259, 0.3333333333333333148, 0.3333333333333333148, 0.3333333333333333148, 0.3333333333333334814, 0.3333333333333332593, 0.3333333333333334259, 0.3333333333333333148, 0.3333333333333333148, 0.3333333333333334814, 0.3333333333333333703, 0.3333333333333334259, 0.3333333333333333148, 0.3333333333333333703, 0.3333333333333332593, 0.3333333333333334814, 0.3333333333333333148, 0.3333333333333334259, 0.3333333333333333148, 0.3333333333333334259, 0.3333333333333333703, 0.3333333333333333703, 0.3333333333333334259, 0.3333333333333333148, 0.3333333333333334814, 0.3333333333333333703, 0.3333333333333333703, 0.3333333333333334814, 0.3333333333333333703, 0.3333333333333332593, 0.3333333333333334259, 0.3333333333333332593, 0.3333333333333334814, 0.3333333333333333148, 0.3333333333333333703, 0.3333333333333333703, 0.3333333333333334259, 0.3333333333333333703, 0.3333333333333333703, 0.3333333333333333148, 0.3333333333333334259, 0.3333333333333334259, 0.3333333333333333703, 0.3333333333333334259, 0.3333333333333333148, 0.3333333333333333703, 0.3333333333333334259, 0.3333333333333333703, 0.3333333333333333148, 0.3333333333333334259, 0.3333333333333333703, 0.3333333333333333148, 0.3333333333333333148, 0.3333333333333334259, 0.3333333333333333148, 0.3333333333333333703, 0.3333333333333333703, 0.3333333333333333703, 0.3333333333333334259, 0.3333333333333334259, 0.3333333333333333148, 0.3333333333333334259, 0.3333333333333333148, 0.3333333333333334814, 0.3333333333333332593, 0.3333333333333334814, 0.3333333333333333703, 0.3333333333333333703, 0.3333333333333334259, 0.3333333333333333703, 0.3333333333333333703, 0.3333333333333333703, 0.3333333333333333703, 0.3333333333333334814, 0.3333333333333333148, 0.3333333333333334259, 0.3333333333333333148, 0.3333333333333333703, 0.3333333333333333703, 0.3333333333333333703, 0.3333333333333335369, 0.3333333333333333703, 0.3333333333333333148, 0.3333333333333334814, 0.3333333333333334259, 0.3333333333333333148, 0.3333333333333333148, 0.3333333333333335369, 0.3333333333333332593, 0.3333333333333333703, 0.3333333333333333148, 0.3333333333333333703, 0.3333333333333333703, 0.3333333333333332593, 0.3333333333333334259, 0.3333333333333332593, 0.3333333333333335369, 0.3333333333333333148, 0.3333333333333333703, 0.3333333333333334259, 0.3333333333333333703, 0.3333333333333333703, 0.3333333333333334814, 0.3333333333333333148, 0.3333333333333333148, 0.3333333333333334259, 0.3333333333333333148, 0.3333333333333333703, 0.3333333333333334814, 0.3333333333333333703, 0.3333333333333333703, 0.3333333333333333703, 0.3333333333333333703, 0.3333333333333334814, 0.3333333333333333703, 0.3333333333333334814, 0.3333333333333333703, 0.3333333333333333703, 0.3333333333333333148, 0.3333333333333334259, 0.3333333333333333148, 0.3333333333333334259, 0.3333333333333333148, 0.3333333333333333703, 0.3333333333333334814, 0.3333333333333333148, 0.3333333333333333148, 0.3333333333333333703, 0.3333333333333333703, 0.3333333333333333703, 0.3333333333333334259, 0.3333333333333333148, 0.3333333333333333703, 0.3333333333333334259, 0.3333333333333333148, 0.3333333333333333703, 0.3333333333333332593, 0.3333333333333333703, 0.3333333333333334259, 0.3333333333333333703, 0.3333333333333333703, 0.3333333333333333703, 0.3333333333333333703, 0.3333333333333334814, 0.3333333333333333703, 0.3333333333333334259, 0.3333333333333334259),
 ( 1.000000000000000000, 1.000000000000000000, 1.000000000000000222, 1.000000000000000000, 0.9999999999999996669, 1.000000000000000444, 0.9999999999999997780, 1.000000000000000000, 1.000000000000000222, 0.9999999999999996669, 1.000000000000000222, 0.9999999999999996669, 1.000000000000000000, 0.9999999999999997780, 1.000000000000000222, 0.9999999999999997780, 1.000000000000000222, 1.000000000000000222, 0.9999999999999997780, 1.000000000000000222, 1.000000000000000222, 0.9999999999999996669, 1.000000000000000444, 0.9999999999999997780, 1.000000000000000000, 1.000000000000000222, 1.000000000000000000, 1.000000000000000000, 1.000000000000000000, 1.000000000000000000, 1.000000000000000222, 1.000000000000000000, 1.000000000000000000, 0.9999999999999997780, 1.000000000000000000, 1.000000000000000000, 1.000000000000000000, 1.000000000000000000, 0.9999999999999997780, 1.000000000000000222, 1.000000000000000000, 1.000000000000000000, 1.000000000000000444, 0.9999999999999997780, 1.000000000000000222, 0.9999999999999996669, 1.000000000000000444, 0.9999999999999997780, 1.000000000000000000, 0.9999999999999997780, 1.000000000000000000, 1.000000000000000222, 0.9999999999999997780, 1.000000000000000444, 0.9999999999999997780, 1.000000000000000000, 0.9999999999999996669, 1.000000000000000444, 0.9999999999999997780, 1.000000000000000444, 1.000000000000000000, 1.000000000000000444, 0.9999999999999996669, 1.000000000000000000, 0.9999999999999996669, 1.000000000000000444, 0.9999999999999997780, 1.000000000000000000, 1.000000000000000000, 1.000000000000000000, 1.000000000000000000, 0.9999999999999996669, 1.000000000000000000, 1.000000000000000222, 0.9999999999999997780, 1.000000000000000000, 0.9999999999999997780, 0.9999999999999997780, 1.000000000000000000, 1.000000000000000222, 0.9999999999999997780, 1.000000000000000000, 1.000000000000000222, 1.000000000000000222, 1.000000000000000222, 0.9999999999999997780, 1.000000000000000000, 1.000000000000000222, 0.9999999999999997780, 1.000000000000000222, 1.000000000000000222, 0.9999999999999997780, 0.9999999999999997780, 0.9999999999999997780, 1.000000000000000444, 1.000000000000000000, 1.000000000000000000, 1.000000000000000000, 1.000000000000000222, 0.9999999999999997780, 1.000000000000000000, 1.000000000000000444, 0.9999999999999996669, 1.000000000000000444, 1.000000000000000000, 1.000000000000000000, 1.000000000000000222, 0.9999999999999997780, 1.000000000000000444, 0.9999999999999996669, 1.000000000000000444, 1.000000000000000000, 0.9999999999999997780, 1.000000000000000222, 0.9999999999999996669, 1.000000000000000222, 1.000000000000000000, 1.000000000000000222, 0.9999999999999997780, 1.000000000000000222, 0.9999999999999996669, 1.000000000000000222, 1.000000000000000222, 1.000000000000000222, 1.000000000000000000, 0.9999999999999997780, 1.000000000000000000, 0.9999999999999997780, 1.000000000000000000, 0.9999999999999997780, 0.9999999999999997780, 1.000000000000000222, 1.000000000000000222, 1.000000000000000222, 0.9999999999999997780, 0.9999999999999997780, 1.000000000000000444, 0.9999999999999997780, 1.000000000000000000, 0.9999999999999997780, 1.000000000000000000, 0.9999999999999997780, 1.000000000000000222, 1.000000000000000000, 1.000000000000000000, 1.000000000000000222, 1.000000000000000000, 0.9999999999999997780, 1.000000000000000444, 1.000000000000000000, 1.000000000000000000, 1.000000000000000444, 0.9999999999999997780, 1.000000000000000222, 0.9999999999999997780, 1.000000000000000444, 1.000000000000000000, 1.000000000000000222, 0.9999999999999997780, 0.9999999999999997780, 1.000000000000000000, 1.000000000000000444, 0.9999999999999996669, 1.000000000000000000, 1.000000000000000222, 1.000000000000000222, 0.9999999999999997780, 1.000000000000000222, 0.9999999999999997780, 1.000000000000000222, 1.000000000000000000, 1.000000000000000000, 0.9999999999999997780, 1.000000000000000444, 0.9999999999999997780, 1.000000000000000222, 0.9999999999999996669, 1.000000000000000444, 0.9999999999999996669, 1.000000000000000222, 1.000000000000000000, 1.000000000000000000, 1.000000000000000000, 1.000000000000000444, 1.000000000000000222, 0.9999999999999997780, 1.000000000000000444, 0.9999999999999997780, 1.000000000000000000, 0.9999999999999996669, 1.000000000000000000, 0.9999999999999996669, 1.000000000000000000, 1.000000000000000222, 1.000000000000000000, 0.9999999999999997780, 1.000000000000000222, 1.000000000000000000, 1.000000000000000222, 0.9999999999999996669, 1.000000000000000000, 1.000000000000000000, 1.000000000000000000, 0.9999999999999997780, 1.000000000000000000, 1.000000000000000000, 1.000000000000000222, 1.000000000000000000, 1.000000000000000000, 0.9999999999999997780, 1.000000000000000000, 1.000000000000000222, 0.9999999999999997780, 1.000000000000000000, 1.000000000000000222, 1.000000000000000000, 1.000000000000000000, 0.9999999999999997780, 0.9999999999999997780, 1.000000000000000000, 1.000000000000000000, 0.9999999999999997780, 1.000000000000000000, 1.000000000000000000, 1.000000000000000000, 1.000000000000000222, 1.000000000000000000, 1.000000000000000000, 0.9999999999999997780, 1.000000000000000000, 0.9999999999999997780, 1.000000000000000444, 0.9999999999999997780, 1.000000000000000222, 0.9999999999999997780, 1.000000000000000444, 0.9999999999999994449, 1.000000000000000444, 0.9999999999999997780, 1.000000000000000222, 1.000000000000000000, 1.000000000000000000, 0.9999999999999997780, 1.000000000000000000, 1.000000000000000000, 0.9999999999999997780, 1.000000000000000000, 1.000000000000000000, 0.9999999999999997780, 1.000000000000000222, 1.000000000000000000, 1.000000000000000222, 0.9999999999999997780, 1.000000000000000222, 0.9999999999999997780, 1.000000000000000222, 0.9999999999999997780, 1.000000000000000444, 0.9999999999999996669, 1.000000000000000222, 0.9999999999999997780, 1.000000000000000000, 1.000000000000000000, 1.000000000000000000, 1.000000000000000222, 1.000000000000000222, 1.000000000000000000, 1.000000000000000444, 1.000000000000000222, 0.9999999999999997780, 1.000000000000000222, 0.9999999999999996669, 1.000000000000000444, 0.9999999999999997780, 0.9999999999999997780, 1.000000000000000222, 1.000000000000000000, 1.000000000000000222, 1.000000000000000000, 1.000000000000000000, 1.000000000000000222, 1.000000000000000000, 0.9999999999999997780, 1.000000000000000222, 0.9999999999999997780, 1.000000000000000000, 1.000000000000000222, 1.000000000000000000, 0.9999999999999997780, 0.9999999999999997780, 1.000000000000000000, 0.9999999999999997780, 1.000000000000000000, 1.000000000000000000, 1.000000000000000000, 1.000000000000000222, 0.9999999999999997780, 1.000000000000000000, 1.000000000000000222, 1.000000000000000000, 0.9999999999999997780, 1.000000000000000000, 1.000000000000000000, 1.000000000000000222, 0.9999999999999997780, 1.000000000000000222, 1.000000000000000000, 1.000000000000000000, 1.000000000000000222, 1.000000000000000000, 1.000000000000000000, 1.000000000000000222, 1.000000000000000000, 1.000000000000000444, 0.9999999999999996669, 1.000000000000000444, 0.9999999999999997780, 1.000000000000000000, 1.000000000000000222, 0.9999999999999996669, 1.000000000000000444, 1.000000000000000000, 1.000000000000000000, 1.000000000000000222, 1.000000000000000444, 1.000000000000000000, 0.9999999999999996669, 1.000000000000000444, 0.9999999999999997780, 0.9999999999999997780, 0.9999999999999997780, 1.000000000000000222, 1.000000000000000000, 0.9999999999999996669, 1.000000000000000222, 1.000000000000000000, 1.000000000000000444, 0.9999999999999997780, 1.000000000000000000, 1.000000000000000222, 1.000000000000000222, 1.000000000000000222, 1.000000000000000222, 1.000000000000000000, 1.000000000000000000, 1.000000000000000000, 1.000000000000000000, 1.000000000000000000, 1.000000000000000444, 1.000000000000000000, 0.9999999999999997780, 1.000000000000000000, 1.000000000000000222, 1.000000000000000000, 1.000000000000000222, 1.000000000000000222, 1.000000000000000000, 0.9999999999999997780, 0.9999999999999997780, 1.000000000000000222, 0.9999999999999997780, 1.000000000000000000, 1.000000000000000222, 1.000000000000000000, 1.000000000000000222, 1.000000000000000000, 0.9999999999999997780, 1.000000000000000000, 0.9999999999999997780, 1.000000000000000222, 1.000000000000000000, 0.9999999999999997780, 0.9999999999999997780, 1.000000000000000222, 1.000000000000000000, 1.000000000000000222, 0.9999999999999996669, 1.000000000000000000, 1.000000000000000222, 0.9999999999999997780, 1.000000000000000000, 1.000000000000000000, 1.000000000000000222, 1.000000000000000222, 1.000000000000000000, 1.000000000000000222, 1.000000000000000222) ) ) 
 REPRESENTATION_ITEM ( '' )  SURFACE ( )  );
#192802=CARTESIAN_POINT ( 'NONE',  ( 1.234804682044550850, -1.602240143502192238, 0.7520855130052228610 ) ) ;
#192803=CARTESIAN_POINT ( 'NONE',  ( 5.004545975878083475, -1.998138528169653316, -0.2443019910301855169 ) ) ;
#192805=CARTESIAN_POINT ( 'NONE',  ( 3.592891271941214271, -0.4089703316215765883, -2.065685861495478726 ) ) ;
#192806=CARTESIAN_POINT ( 'NONE',  ( 2.688967962845473458, 1.619712848077807577, 1.022445119732362961 ) ) ;
#192808=CARTESIAN_POINT ( 'NONE',  ( 4.264079249230395163, -1.964438661470244263, 0.1424843695872201332 ) ) ;
#192809=CARTESIAN_POINT ( 'NONE',  ( 5.607677614632407881, 1.532089292189286356, 1.316289066716142431 ) ) ;
#192811=CARTESIAN_POINT ( 'NONE',  ( 1.287742131874554552, -0.8442722623961744777, 1.669378388412197767 ) ) ;
#192812=CARTESIAN_POINT ( 'NONE',  ( 5.461458274417386072, 0.3306134467882023142, -1.692711794494299538 ) ) ;
#192813=CARTESIAN_POINT ( 'NONE',  ( 1.775505761281343631, 0.3235837346332003372, -1.884644527778083001 ) ) ;
#192815=CARTESIAN_POINT ( 'NONE',  ( 1.612255294781844706, -2.189918024983358080, 0.2725913246661854084 ) ) ;
#192820=CARTESIAN_POINT ( 'NONE',  ( 6.819227946136852125, -0.1326586024288610444, 1.840611662119538749 ) ) ;
#192825=CARTESIAN_POINT ( 'NONE',  ( 2.348173244826061268, -0.8873571809006628452, 1.870714752860686447 ) ) ;
#192830=CARTESIAN_POINT ( 'NONE',  ( 6.533838320793388554, -2.056994387304663885, 0.5145578593022880343 ) ) ;
#192835=CARTESIAN_POINT ( 'NONE',  ( 3.972029700707707445, 1.727737986437705819, 1.038833660170018769 ) ) ;
#192836=CARTESIAN_POINT ( 'NONE',  ( 4.522610612662866458, 0.3335214923718023416, 1.886305606834618231 ) ) ;
#192838=CARTESIAN_POINT ( 'NONE',  ( 2.472451708263478487, -2.098117355222902436, -0.6331711661175795092 ) ) ;
#192839=CARTESIAN_POINT ( 'NONE',  ( 0.1335669894368343991, 7.629137130509040965, -2.753547149787978654 ) ) ;
#192841=CARTESIAN_POINT ( 'NONE',  ( 5.431894621915298593, -1.963206642400895374, 0.4451836139030879713 ) ) ;
#192844=CARTESIAN_POINT ( 'NONE',  ( 0.1929827526203631294, 1.755782054984224683, 0.9913788669043410717 ) ) ;
#192846=CARTESIAN_POINT ( 'NONE',  ( 3.562131390660903563, -1.402593093800925894, 1.550658987340556294 ) ) ;
#192848=CARTESIAN_POINT ( 'NONE',  ( 2.221339967433374252, -1.673790515994465711, 0.4157018595009522310 ) ) ;
#192850=CARTESIAN_POINT ( 'NONE',  ( 6.135037582782754129, 1.979230198018981701, 0.7618025574447004900 ) ) ;
#192859=CARTESIAN_POINT ( 'NONE',  ( 2.332397652471474903, 1.182373381703984094, -1.372477691862858729 ) ) ;
#192866=CARTESIAN_POINT ( 'NONE',  ( 2.859786144356114779, 0.6500800702718724233, -1.690994707955698617 ) ) ;
#192867=CARTESIAN_POINT ( 'NONE',  ( 6.539320575229254473, 0.5926322452488984593, 1.950287522085321301 ) ) ;
#192870=CARTESIAN_POINT ( 'NONE',  ( 3.631172916894987779, 0.04772338994715261129, -1.860622308654858559 ) ) ;
#192871=CARTESIAN_POINT ( 'NONE',  ( 1.194790368808082759, 1.690169533058868190, 0.9015364962996033071 ) ) ;
#192872=CARTESIAN_POINT ( 'NONE',  ( 0.6217474354073999621, -0.9722136304874777757, -1.544982199245432897 ) ) ;
#192880=CARTESIAN_POINT ( 'NONE',  ( 5.963713532047742127, -0.4821895448718095945, 1.909345749545824367 ) ) ;
#192883=CARTESIAN_POINT ( 'NONE',  ( 0.1641640845322315523, -1.364019775510204369, 1.584451847793943324 ) ) ;
#192885=CARTESIAN_POINT ( 'NONE',  ( 4.946275538936047766, 1.921213873770099445, 0.1421515328255736899 ) ) ;
#192887=CARTESIAN_POINT ( 'NONE',  ( 0.9030137451815029026, 1.489685209907613661, 1.054989265776705709 ) ) ;
#192888=CARTESIAN_POINT ( 'NONE',  ( 2.350463684150871035, 2.206416367115513477, 0.05273732197710182673 ) ) ;
#192891=CARTESIAN_POINT ( 'NONE',  ( 1.423922367354793606, -1.897583212610975734, 0.2371896777705190806 ) ) ;
#192893=CARTESIAN_POINT ( 'NONE',  ( 0.7835775553649370062, -1.871284325210004429, 0.6146160330302401498 ) ) ;
#192894=CARTESIAN_POINT ( 'NONE',  ( 2.436971693805603856, -1.440716923005976646, -1.302479457752574232 ) ) ;
#192895=CARTESIAN_POINT ( 'NONE',  ( 1.370470000664014254, -0.4925687793003556969, 1.954872606163795989 ) ) ;
#192897=CARTESIAN_POINT ( 'NONE',  ( 5.453892037968048001, -0.6717839469763884352, 1.735626407379993186 ) ) ;
#192903=CARTESIAN_POINT ( 'NONE',  ( 1.575987392057216940, -1.168677030305173004, 1.853764812240476623 ) ) ;
#192907=CARTESIAN_POINT ( 'NONE',  ( 2.262075381241589245, 0.7800679334904643270, 1.650788133108482825 ) ) ;
#192915=CARTESIAN_POINT ( 'NONE',  ( 1.400868510093127073, 1.575373640256217733, -1.108617158386180357 ) ) ;
#192916=CARTESIAN_POINT ( 'NONE',  ( 5.770351633785986145, -0.8788013674413884813, -1.753946858050984048 ) ) ;
#192921=CARTESIAN_POINT ( 'NONE',  ( 4.898067072109578035, -0.7382639882421681010, -2.063579870930781546 ) ) ;
#192923=CARTESIAN_POINT ( 'NONE',  ( 3.520434184366732389, 0.9265386974339048232, 1.851387837889128640 ) ) ;
#192927=CARTESIAN_POINT ( 'NONE',  ( 3.516502792989243176, -2.123307701433849282, 0.8810689989526691024 ) ) ;
#192935=CARTESIAN_POINT ( 'NONE',  ( 3.767467431601259076, 1.079656630588815780, 1.613968600252370322 ) ) ;
#192940=CARTESIAN_POINT ( 'NONE',  ( 5.642805672956042962, 1.844803604357934779, 0.5037821151940986564 ) ) ;
#192941=CARTESIAN_POINT ( 'NONE',  ( 6.668995740727024391, -1.579612310505887685, -0.6930582901118372829 ) ) ;
#192942=CARTESIAN_POINT ( 'NONE',  ( 5.085172837459294826, 1.651341431264556014, 1.157102043685846793 ) ) ;
#192944=CARTESIAN_POINT ( 'NONE',  ( 1.331021600797330118, 2.127646391749141941, 0.5858054460900484761 ) ) ;
#192947=CARTESIAN_POINT ( 'NONE',  ( 1.429752723428807215, 1.029013270877369379, -1.819774963352964292 ) ) ;
#192948=CARTESIAN_POINT ( 'NONE',  ( 6.643818817254954823, 0.6745290893846628277, -1.636350436104140327 ) ) ;
#192949=CARTESIAN_POINT ( 'NONE',  ( 5.713517581197447015, 1.944070655204039433, 0.5350908816983344085 ) ) ;
#192951=CARTESIAN_POINT ( 'NONE',  ( 3.381108394495379699, 2.072348265612040219, -0.9799971971852624586 ) ) ;
#192952=CARTESIAN_POINT ( 'NONE',  ( 0.6557207866510657013, -1.263530833501663952, 1.197007909421362370 ) ) ;
#192953=CARTESIAN_POINT ( 'NONE',  ( 2.584367824843319283, 1.138156186954141003, 1.789115803205274080 ) ) ;
#192955=CARTESIAN_POINT ( 'NONE',  ( 1.545803854144804479, 1.604466568860075437, -0.6577250193331334316 ) ) ;
#192957=CARTESIAN_POINT ( 'NONE',  ( 1.802945237480069407, -1.574492340324705753, 0.9918895310334940874 ) ) ;
#192958=CARTESIAN_POINT ( 'NONE',  ( 1.135490968158389791, -0.05309211241652118246, -2.170675730929682246 ) ) ;
#192959=CARTESIAN_POINT ( 'NONE',  ( 2.905482715143858030, -1.942096844255640109, 0.5424705965835219246 ) ) ;
#192960=CARTESIAN_POINT ( 'NONE',  ( 5.156250000000004441, -1.895863743163967108, 0.7852924748302536617 ) ) ;
#192962=CARTESIAN_POINT ( 'NONE',  ( 6.410771793481705672, 1.425725087049932505, -1.295833391663123724 ) ) ;
#192964=CARTESIAN_POINT ( 'NONE',  ( 3.410577425615939795, -2.218986280728425076, -0.1058077642441344057 ) ) ;
#192971=CARTESIAN_POINT ( 'NONE',  ( 0.2746299231596514012, 1.718356743839201561, -0.6618312839273902126 ) ) ;
#192972=CARTESIAN_POINT ( 'NONE',  ( 4.176187491914356897, -1.006606191838583131, -1.683785057063936552 ) ) ;
#192976=CARTESIAN_POINT ( 'NONE',  ( 6.169232171785941965, 0.1756554044750150145, -2.255672955852848993 ) ) ;
#192977=CARTESIAN_POINT ( 'NONE',  ( 2.084505489600170680, 1.189443612574309084, -1.685003561244757364 ) ) ;
#192981=CARTESIAN_POINT ( 'NONE',  ( 3.655401173194738007, 0.4573680094964555076, -1.813624142381641491 ) ) ;
#192982=CARTESIAN_POINT ( 'NONE',  ( 2.795252500310735133, 1.254151915811404061, -1.197898925204267995 ) ) ;
#192983=CARTESIAN_POINT ( 'NONE',  ( 0.08209332325101456607, -1.073118421065310413, 2.025687816139466246 ) ) ;
#192984=CARTESIAN_POINT ( 'NONE',  ( 1.237671066534186792, -1.994493743981802680, 0.9446329514863486265 ) ) ;
#192985=CARTESIAN_POINT ( 'NONE',  ( 3.959979445722985325, 2.145676688911036578, -0.2621329562078680842 ) ) ;
#192986=CARTESIAN_POINT ( 'NONE',  ( 5.296799794911354553, 1.588725326081788847, 1.116492485978479499 ) ) ;
#192987=CARTESIAN_POINT ( 'NONE',  ( 6.889956934492897034, -0.7990643998789861424, 1.689675875712663755 ) ) ;
#192989=CARTESIAN_POINT ( 'NONE',  ( 0.4374999999988640753, 1.451031289089056431, -1.451031289061139651 ) ) ;
#192992=CARTESIAN_POINT ( 'NONE',  ( 5.854138739207011888, 0.1455364397412381439, -2.011204036175239018 ) ) ;
#192997=CARTESIAN_POINT ( 'NONE',  ( 3.316849939159485228, 1.650902842016691130, 0.7798126646740562995 ) ) ;
#192998=CARTESIAN_POINT ( 'NONE',  ( 1.624349867039249329, -1.226448341774049267, -1.834376716147153363 ) ) ;
#193003=CARTESIAN_POINT ( 'NONE',  ( 0.7737015921927943296, 0.3898077916253924746, -1.981631471940727973 ) ) ;
#193004=CARTESIAN_POINT ( 'NONE',  ( 1.682450335255514240, 1.092831414372618326, 1.817064408815848964 ) ) ;
#193008=CARTESIAN_POINT ( 'NONE',  ( 1.533807339325540475, 1.103149047995868104, 1.498595216881804859 ) ) ;
#193010=CARTESIAN_POINT ( 'NONE',  ( 0.7960496800812133511, -0.7770375076890515542, 2.017388685454111652 ) ) ;
#193011=CARTESIAN_POINT ( 'NONE',  ( 5.959611329766301147, -1.915599147091971544, -0.6298778581111733610 ) ) ;
#193015=CARTESIAN_POINT ( 'NONE',  ( 4.213378774425760476, -0.3099129147984269195, 1.799030153321119263 ) ) ;
#193022=CARTESIAN_POINT ( 'NONE',  ( 6.362657644764971643, -0.6818896071447739793, 1.897407954007489295 ) ) ;
#193023=CARTESIAN_POINT ( 'NONE',  ( 6.210883717528068892, -0.2205035313364057392, 1.827825250963102111 ) ) ;
#193024=CARTESIAN_POINT ( 'NONE',  ( -0.02299388927988389383, 2.039721852852835582, -2.328191723522631928 ) ) ;
#193025=CARTESIAN_POINT ( 'NONE',  ( 4.916800105644766994, 1.594097815661306816, -1.668853466001555486 ) ) ;
#193027=CARTESIAN_POINT ( 'NONE',  ( 5.694645791630270182, -0.5191100231263061637, -2.098234375727751733 ) ) ;
#193028=CARTESIAN_POINT ( 'NONE',  ( 1.821723684117615427, 1.116499850783551073, -1.588862189236692091 ) ) ;
#193029=CARTESIAN_POINT ( 'NONE',  ( 4.376513399274863936, -0.3984044028133710835, 2.263477716089700387 ) ) ;
#193032=CARTESIAN_POINT ( 'NONE',  ( 4.364026845288040413, 0.8817440624687390427, 1.649792572839225091 ) ) ;
#193036=CARTESIAN_POINT ( 'NONE',  ( 2.478646075381494285, -1.315928518397539548, 1.387899491812602859 ) ) ;
#193039=CARTESIAN_POINT ( 'NONE',  ( 4.494872972331320327, -0.4818267175418550208, -2.153482813429814069 ) ) ;
#193040=CARTESIAN_POINT ( 'NONE',  ( 6.883263157960364254, 2.447565407927353220, 2.329071302269662080 ) ) ;
#193041=CARTESIAN_POINT ( 'NONE',  ( -0.2110808730067144090, 0.7535804146166940054, -1.881771259391984197 ) ) ;
#193044=CARTESIAN_POINT ( 'NONE',  ( 1.370321444179344983, -1.253680685346630019, 1.521333489566406127 ) ) ;
#193045=CARTESIAN_POINT ( 'NONE',  ( 1.255362601414770296, -1.817582055312426004, 1.421667062125511860 ) ) ;
#193046=CARTESIAN_POINT ( 'NONE',  ( 2.980854556682940526, 1.846358069237159949, 0.6635599008937702603 ) ) ;
#193048=CARTESIAN_POINT ( 'NONE',  ( 6.473490848629269045, -0.2583879851764906976, 2.046290913384725130 ) ) ;
#193050=CARTESIAN_POINT ( 'NONE',  ( 3.995327539805045181, -0.3399590882401174463, 1.987497567597557468 ) ) ;
#193056=CARTESIAN_POINT ( 'NONE',  ( 1.727621483090465926, 0.1626789094613217412, -2.165059144495153021 ) ) ;
#193061=CARTESIAN_POINT ( 'NONE',  ( 2.829206387438303327, -1.746784236434803850, 0.6695917499066756928 ) ) ;
#193062=CARTESIAN_POINT ( 'NONE',  ( 6.591117433763723277, 1.884315261875910474, -1.059023293578951863 ) ) ;
#193065=CARTESIAN_POINT ( 'NONE',  ( 6.727182134110237577, 2.483225874290733159, 2.096421262816303255 ) ) ;
#193068=CARTESIAN_POINT ( 'NONE',  ( 2.508343198132975349, -1.907285675847451234, -0.1387974571645037292 ) ) ;
#193070=CARTESIAN_POINT ( 'NONE',  ( 4.504631171302628800, 1.367295333670435653, -1.123774403194759408 ) ) ;
#193071=CARTESIAN_POINT ( 'NONE',  ( 1.471198412684338264, -1.640640410176617658, -0.9821394255850326438 ) ) ;
#193074=CARTESIAN_POINT ( 'NONE',  ( 6.292599812010432281, 1.415705964336026357, -1.290654269910092911 ) ) ;
#193076=CARTESIAN_POINT ( 'NONE',  ( 0.5376586404672692998, 1.932363751568724641, -0.7437053376125392079 ) ) ;
#193081=CARTESIAN_POINT ( 'NONE',  ( 5.032044620589739559, 0.9611010790777809731, -1.604743002217932313 ) ) ;
#193082=CARTESIAN_POINT ( 'NONE',  ( 1.840199252755945425, 1.805614550920462635, 0.2691313018618191055 ) ) ;
#193083=CARTESIAN_POINT ( 'NONE',  ( 5.250674450588199704, 0.6379336648693231249, 2.112661011922472021 ) ) ;
#193086=CARTESIAN_POINT ( 'NONE',  ( 2.787610149020779193, -1.925555389141724527, 0.7399787145165384050 ) ) ;
#193095=CARTESIAN_POINT ( 'NONE',  ( 5.336411075974297979, -1.153114810915600641, 1.719314882265559286 ) ) ;
#193097=CARTESIAN_POINT ( 'NONE',  ( 2.864712396292764751, -1.492883925411474078, 1.563474562115530375 ) ) ;
#193099=CARTESIAN_POINT ( 'NONE',  ( 3.668621814757520916, 0.7290426041848938610, 1.883679974206926122 ) ) ;
#193100=CARTESIAN_POINT ( 'NONE',  ( 6.720655732516667591, 2.416141799769660370, 2.554522868665403568 ) ) ;
#193101=ORIENTED_EDGE ( 'NONE', *, *, #133575, .F. ) ;
#193106=CARTESIAN_POINT ( 'NONE',  ( 0.8488426437929346147, -1.825078332268307513, -0.8578388575243289793 ) ) ;
#193109=CARTESIAN_POINT ( 'NONE',  ( 6.093348126157794198, -0.7399906200981147819, 2.062998119606203939 ) ) ;
#193111=CARTESIAN_POINT ( 'NONE',  ( 4.588094604188536429, 1.105678411722615051, 1.560157546714964871 ) ) ;
#193115=CARTESIAN_POINT ( 'NONE',  ( 3.146111402376899235, 0.9091623069825971459, 1.799915193831227889 ) ) ;
#193119=CARTESIAN_POINT ( 'NONE',  ( 5.526277428723715524, 1.024295688422135031, -1.387495638070087134 ) ) ;
#193122=CARTESIAN_POINT ( 'NONE',  ( 6.925078400183575233, 7.629137130509070275, 2.455651831298297338 ) ) ;
#193123=CARTESIAN_POINT ( 'NONE',  ( 3.813614929637610285, -1.843318686535614148, 0.3169883347873064250 ) ) ;
#193125=CARTESIAN_POINT ( 'NONE',  ( 0.9892257793299992219, 0.1485654903058269416, 2.064951490685583924 ) ) ;
#193128=CARTESIAN_POINT ( 'NONE',  ( 5.953728957075980155, -1.316865622510310141, -1.244172183657651365 ) ) ;
#193131=CARTESIAN_POINT ( 'NONE',  ( 0.7030050633033817498, 1.597335618216610964, -0.8546489784103310505 ) ) ;
#193135=CARTESIAN_POINT ( 'NONE',  ( 3.205210054081304438, -0.4271916898582402422, 2.149238826137919389 ) ) ;
#193137=CARTESIAN_POINT ( 'NONE',  ( 1.082386330805637398, 1.171445227557347923, -1.573568114121715933 ) ) ;
#193139=CARTESIAN_POINT ( 'NONE',  ( 5.255460224911852052, 1.844849436727209469, -0.5155117042133209315 ) ) ;
#193146=CARTESIAN_POINT ( 'NONE',  ( 1.323354039402934390, -0.05256100377049736927, 2.161234000603563299 ) ) ;
#193149=CARTESIAN_POINT ( 'NONE',  ( 1.588595499965880675, -0.2641367610144580991, -1.806243275932853498 ) ) ;
#193150=CARTESIAN_POINT ( 'NONE',  ( 0.08834397731360790762, 1.226219587655341448, 1.729930300845914815 ) ) ;
#193151=CARTESIAN_POINT ( 'NONE',  ( 4.524309061075334704, 1.122661849025725189, -1.439470297551891154 ) ) ;
#193152=ADVANCED_FACE ( 'NONE', ( #59850 ), #13724, .F. ) ;
#193154=CARTESIAN_POINT ( 'NONE',  ( 3.146637304467227558, 1.866760668956708447, 0.4145885930168375921 ) ) ;
#193156=CARTESIAN_POINT ( 'NONE',  ( 3.824621415324851892, -1.324631885467566716, 1.457714561274085163 ) ) ;
#193158=CARTESIAN_POINT ( 'NONE',  ( 5.460475975554013317, -1.757383149004720924, -0.8268225932778446863 ) ) ;
#193162=CARTESIAN_POINT ( 'NONE',  ( 6.135037582782754129, 1.979230198018981701, 0.7618025574447004900 ) ) ;
#193164=CARTESIAN_POINT ( 'NONE',  ( 4.072844535355981677, -1.414876986328793329, 1.286614418101794444 ) ) ;
#193169=CARTESIAN_POINT ( 'NONE',  ( 5.707686766122681554, 1.525977179164988540, 1.313104676043591601 ) ) ;
#193171=CARTESIAN_POINT ( 'NONE',  ( 5.637271085457097541, -1.648663388651723460, 0.7845467231081537651 ) ) ;
#193172=CARTESIAN_POINT ( 'NONE',  ( 2.330607996690749140, -1.275545549462468120, 1.630658604070814199 ) ) ;
#193185=CARTESIAN_POINT ( 'NONE',  ( 3.674194220352343443, 1.259077133501560697, 1.192749331401379731 ) ) ;
#193188=CARTESIAN_POINT ( 'NONE',  ( 1.463825199929311260, -0.5068179562870354093, 2.007114080642191656 ) ) ;
#193189=CARTESIAN_POINT ( 'NONE',  ( 2.917688350237046979, -1.423917071783699972, -1.567024636986138253 ) ) ;
#193193=CARTESIAN_POINT ( 'NONE',  ( 0.6198874644624132735, 1.948816017023939251, -0.2832832528399802374 ) ) ;
#193198=CARTESIAN_POINT ( 'NONE',  ( 3.504133162399528434, -0.9285911969159079682, -2.095928835653658062 ) ) ;
#193199=CARTESIAN_POINT ( 'NONE',  ( 0.1350027811974127134, -1.670744041527939094, 0.7364786222084362954 ) ) ;
#193200=EDGE_CURVE ( 'NONE', #168104, #97632, #118806, .T. ) ;
#193201=CARTESIAN_POINT ( 'NONE',  ( 3.515784362865181478, -0.5505564139345071606, 1.831456330389509501 ) ) ;
#193205=CARTESIAN_POINT ( 'NONE',  ( 1.968995789680173303, -1.553632997376572566, 1.280276984777522165 ) ) ;
#193206=CARTESIAN_POINT ( 'NONE',  ( 2.307404798597446849, -1.572557994556064154, -1.172606125687980061 ) ) ;
#193211=CARTESIAN_POINT ( 'NONE',  ( 4.787105812777236125, 1.548788850919210702, 1.404477511574409920 ) ) ;
#193212=CARTESIAN_POINT ( 'NONE',  ( 3.801397759637317186, -0.5140543387622575899, 1.693523888807080047 ) ) ;
#193215=CARTESIAN_POINT ( 'NONE',  ( 5.929661055573363981, 1.134796830042347660, -1.991584109881129327 ) ) ;
#193216=CARTESIAN_POINT ( 'NONE',  ( 4.962738864268898098, 0.1657098081031352088, -1.732421123976911836 ) ) ;
#193220=CARTESIAN_POINT ( 'NONE',  ( 4.569544190834089470, 1.339882265830975694, -1.100422448201631820 ) ) ;
#193221=CARTESIAN_POINT ( 'NONE',  ( 5.107971825378077924, 0.6857059611327814830, -2.060108355502160649 ) ) ;
#193223=CARTESIAN_POINT ( 'NONE',  ( -0.2232446489705899595, -0.4745787333681207865, -2.071451665377940010 ) ) ;
#193224=CARTESIAN_POINT ( 'NONE',  ( 4.656250000000003553, -1.895863743163975101, 0.7852924748302414493 ) ) ;
#193226=CARTESIAN_POINT ( 'NONE',  ( 2.959893420002459585, 1.917249785004307316, -0.1873479421724104088 ) ) ;
#193228=CARTESIAN_POINT ( 'NONE',  ( 0.5752228765869402682, -1.604835199033414872, 1.536031695938171460 ) ) ;
#193230=CARTESIAN_POINT ( 'NONE',  ( -0.1408020194050172424, 4.085453189724971956, -2.655103234342595986 ) ) ;
#193233=CARTESIAN_POINT ( 'NONE',  ( 2.948112417477159575, -1.493347798232132373, -1.644555409524293577 ) ) ;
#193234=CARTESIAN_POINT ( 'NONE',  ( -0.02900071798685177615, 6.946858727649162901, -2.768864135414349281 ) ) ;
#193239=CARTESIAN_POINT ( 'NONE',  ( 1.002577532868035526, -1.966644254196001196, 0.4445047019146358691 ) ) ;
#193241=CARTESIAN_POINT ( 'NONE',  ( 5.863753151201884783, -0.5045919461894343705, 1.999881752496771359 ) ) ;
#193246=CARTESIAN_POINT ( 'NONE',  ( 0.4734442463095941411, 1.011852719971978232, 1.451749726636430093 ) ) ;
#193247=CARTESIAN_POINT ( 'NONE',  ( 5.607993946907785521, -0.03366334548273764576, 1.734015701317252134 ) ) ;
#193248=CARTESIAN_POINT ( 'NONE',  ( 5.495574104867783305, -1.740626723225440209, 0.008114992421901638317 ) ) ;
#193249=CARTESIAN_POINT ( 'NONE',  ( 2.525266882823226311, -2.137704731703232053, 0.8281840208047249741 ) ) ;
#193251=CARTESIAN_POINT ( 'NONE',  ( 2.079791654855645877, -1.805462111169679584, -0.3597937517794968509 ) ) ;
#193253=CARTESIAN_POINT ( 'NONE',  ( 2.221465439867484903, -1.771451409125622600, 0.4407646962370226351 ) ) ;
#193254=CARTESIAN_POINT ( 'NONE',  ( 2.268204128460939550, 1.842446992372799963, -0.8197738674571022344 ) ) ;
#193257=CARTESIAN_POINT ( 'NONE',  ( 4.524511627872906061, 1.297711147994727865, -1.658517390945497549 ) ) ;
#193260=CARTESIAN_POINT ( 'NONE',  ( 2.137250951388528275, -0.09934309608320915363, -2.068088366144354318 ) ) ;
#193263=CARTESIAN_POINT ( 'NONE',  ( 5.233110275169113201, 1.959380141031796585, 0.8112103084707968925 ) ) ;
#193265=CARTESIAN_POINT ( 'NONE',  ( 0.02974079377688309753, -1.184178705181990532, -1.520296634558585547 ) ) ;
#193273=CARTESIAN_POINT ( 'NONE',  ( 6.117454236943913770, 1.763945953808215394, 1.176740244630887222 ) ) ;
#193274=CARTESIAN_POINT ( 'NONE',  ( 1.571456177274520805, 0.1552745290232947217, -2.100303177343607608 ) ) ;
#193277=CARTESIAN_POINT ( 'NONE',  ( 5.805462856137336480, -1.465901670865896067, -1.146230774367855254 ) ) ;
#193285=CARTESIAN_POINT ( 'NONE',  ( 2.558977423257744022, 1.577441344615847951, -1.166261179026031325 ) ) ;
#193286=CARTESIAN_POINT ( 'NONE',  ( 1.270647086845246188, -1.370953960119488668, 1.671340013135722558 ) ) ;
#193290=CARTESIAN_POINT ( 'NONE',  ( 3.004952549044386245, 1.720378813442688282, 0.2150250689552536121 ) ) ;
#193291=CARTESIAN_POINT ( 'NONE',  ( 2.220290661370280638, -0.001068742171999540608, 1.740516466435287235 ) ) ;
#193295=CARTESIAN_POINT ( 'NONE',  ( 2.108749758911751204, 0.7741990562295970602, -1.861730988020185329 ) ) ;
#193296=CARTESIAN_POINT ( 'NONE',  ( 6.825078400183575589, -0.005632053428735600553, 2.144262460745151255 ) ) ;
#193298=CARTESIAN_POINT ( 'NONE',  ( 0.9363264705049412218, 1.941902958617349961, 0.3393069938249710371 ) ) ;
#193299=CARTESIAN_POINT ( 'NONE',  ( 6.275647926998929371, 0.3200337115364471074, -1.885262484646982095 ) ) ;
#193304=CARTESIAN_POINT ( 'NONE',  ( 1.541671952839033688, -1.900923180158103021, 0.6826752959473363358 ) ) ;
#193306=CARTESIAN_POINT ( 'NONE',  ( 4.735574959254028826, -2.111847384580630038, 0.9304801611131856554 ) ) ;
#193307=CARTESIAN_POINT ( 'NONE',  ( 6.109812101310618360, 0.5708666350849945781, -1.876949146916474298 ) ) ;
#193308=CARTESIAN_POINT ( 'NONE',  ( 2.834756127989654484, -1.875839772035441388, -0.5741054328185363209 ) ) ;
#193311=VERTEX_POINT ( 'NONE', #50001 ) ;
#193312=CARTESIAN_POINT ( 'NONE',  ( 1.077539098219507663, 1.607448503539260054, 1.378281722515703800 ) ) ;
#193315=CARTESIAN_POINT ( 'NONE',  ( 1.798526679444776954, 1.530131497970032450, 1.023642133485637595 ) ) ;
#193318=CARTESIAN_POINT ( 'NONE',  ( 2.461320219219771843, -1.760565900816572826, 1.181798851529712646 ) ) ;
#193322=CARTESIAN_POINT ( 'NONE',  ( 3.110674321496671446, 1.495003355660160516, -1.418639704521322153 ) ) ;
#193324=CARTESIAN_POINT ( 'NONE',  ( 0.7492455685023796663, 1.839184785914184994, -0.09005233288367914257 ) ) ;
#193326=CARTESIAN_POINT ( 'NONE',  ( -0.02224634325196857623, 5.718740092702407907, -2.883150554214870098 ) ) ;
#193330=CARTESIAN_POINT ( 'NONE',  ( 2.952682139456219268, 0.7592856210697115360, 2.131335665991466843 ) ) ;
#193332=CARTESIAN_POINT ( 'NONE',  ( 2.425776345151516633, -1.791340243523626974, 0.2692766639123735373 ) ) ;
#193333=CARTESIAN_POINT ( 'NONE',  ( 2.870226655882984090, -1.888176233477338872, -0.3226071530259622677 ) ) ;
#193334=CARTESIAN_POINT ( 'NONE',  ( 4.615722581382986967, 0.4567890626981512270, -2.019179087418949692 ) ) ;
#193337=CARTESIAN_POINT ( 'NONE',  ( 2.078924955456124657, -0.09500079177627264448, -1.969288250925634642 ) ) ;
#193338=CARTESIAN_POINT ( 'NONE',  ( 6.287721633157377532, 1.330437191854600076, 1.393544807510539218 ) ) ;
#193339=CARTESIAN_POINT ( 'NONE',  ( 3.098369316282158614, -0.5415621961667067552, -1.790553177708480215 ) ) ;
#193340=CARTESIAN_POINT ( 'NONE',  ( 2.385774557197326562, 2.109090111016972191, -0.9369807928535575092 ) ) ;
#193342=CARTESIAN_POINT ( 'NONE',  ( 3.033498015644376267, 1.768043114356824930, -0.5812464218588138110 ) ) ;
#193344=CARTESIAN_POINT ( 'NONE',  ( 6.144999177589818729, -0.2990398410713848154, -2.040763669801145319 ) ) ;
#193349=CARTESIAN_POINT ( 'NONE',  ( 6.053767517140953736, 0.6149031373867475114, -2.014179596626505919 ) ) ;
#193351=CARTESIAN_POINT ( 'NONE',  ( 5.782550318682353030, -2.107506929020441788, -0.4798289361013232668 ) ) ;
#193352=CARTESIAN_POINT ( 'NONE',  ( 6.358070640981934751, 0.7709996861101749976, -1.866924874111668853 ) ) ;
#193357=CARTESIAN_POINT ( 'NONE',  ( 6.825078400183574701, 6.039200712630649726, 2.350557101739355392 ) ) ;
#193360=CARTESIAN_POINT ( 'NONE',  ( 4.259000112335223243, -0.004834882008357410665, -2.016708403958865414 ) ) ;
#193365=CARTESIAN_POINT ( 'NONE',  ( 6.280167721515548251, -1.160692707240444710, 1.823489969145650313 ) ) ;
#193370=CARTESIAN_POINT ( 'NONE',  ( 0.2279634046833027561, 1.910523547013969869, 0.1400250592105151126 ) ) ;
#193373=CARTESIAN_POINT ( 'NONE',  ( 2.121340078736310364, -1.673401575455361723, 0.4176718278932553541 ) ) ;
#193378=CARTESIAN_POINT ( 'NONE',  ( 1.334804486018669856, -1.602990312956679597, 0.7502176981645010123 ) ) ;
#193379=CARTESIAN_POINT ( 'NONE',  ( 2.402991782874515092, -0.3463731968284866625, -1.982927098142922784 ) ) ;
#193381=CARTESIAN_POINT ( 'NONE',  ( 4.032405518703926717, 1.182977813604596973, -1.862726815517960821 ) ) ;
#193382=CARTESIAN_POINT ( 'NONE',  ( 5.541899213757757181, 1.452536422000339611, 1.613792965789240696 ) ) ;
#193386=CARTESIAN_POINT ( 'NONE',  ( 3.000754678503589012, -2.089479603458433754, -0.3603616953608209661 ) ) ;
#193387=CARTESIAN_POINT ( 'NONE',  ( 2.900017720922347220, -0.9963201819552582883, -1.753021271517739343 ) ) ;
#193388=CARTESIAN_POINT ( 'NONE',  ( 2.900440330899815233, -1.785477387793675597, -0.3053432404436141057 ) ) ;
#193395=CARTESIAN_POINT ( 'NONE',  ( 6.463509179248937642, 0.3066564278407272748, -1.799597105106438777 ) ) ;
#193397=CARTESIAN_POINT ( 'NONE',  ( 1.920960065284383678, -1.709437138374754639, 0.8649676252809009869 ) ) ;
#193404=CARTESIAN_POINT ( 'NONE',  ( 5.541917325712655717, 0.8799508658935292216, -1.974686638939105343 ) ) ;
#193407=CARTESIAN_POINT ( 'NONE',  ( 3.076547362214879566, 0.9570632234598417387, 1.892448740577145738 ) ) ;
#193408=CARTESIAN_POINT ( 'NONE',  ( -0.1298852118744256712, 1.416581902219627542, -1.986715197202136185 ) ) ;
#193410=CARTESIAN_POINT ( 'NONE',  ( 4.710209360279286273, -0.8403073340159574744, -1.783404427212876842 ) ) ;
#193412=CARTESIAN_POINT ( 'NONE',  ( 0.1408853756387764278, 1.927792606564913136, 0.5802787064154624197 ) ) ;
#193414=CARTESIAN_POINT ( 'NONE',  ( 5.436746213213202061, -1.667492067756784158, 1.304688015722222039 ) ) ;
#193416=CARTESIAN_POINT ( 'NONE',  ( 0.7661813929631040576, -2.060537521029872643, 0.2012509062776293156 ) ) ;
#193417=CARTESIAN_POINT ( 'NONE',  ( 3.152217820003437421, -1.470166820979129207, 1.268861441860974049 ) ) ;
#193421=CARTESIAN_POINT ( 'NONE',  ( 3.503930302474305591, -0.8474990640115993568, -1.911341529346534118 ) ) ;
#193424=CARTESIAN_POINT ( 'NONE',  ( 0.04710954650594124937, -1.657193159602200927, 0.7319819781744562048 ) ) ;
#193426=CARTESIAN_POINT ( 'NONE',  ( 5.004599478379411437, -0.7411955310945413933, -2.078817424605138964 ) ) ;
#193428=CARTESIAN_POINT ( 'NONE',  ( 2.960231987352707428, 2.196266598062237563, -0.2149427413448631863 ) ) ;
#193432=CARTESIAN_POINT ( 'NONE',  ( 1.752457306817490457, 1.891635876823925200, 0.2793096714826873161 ) ) ;
#193434=CARTESIAN_POINT ( 'NONE',  ( 5.178213324540339002, -1.104578422852561914, -1.750899486206449973 ) ) ;
#193436=CARTESIAN_POINT ( 'NONE',  ( 2.940462584922590938, 2.145230175562794717, 0.2658940370997217584 ) ) ;
#193437=CARTESIAN_POINT ( 'NONE',  ( 4.968408144156593487, -2.063508908063705238, -0.7385586828293493333 ) ) ;
#193442=MECHANICAL_DESIGN_GEOMETRIC_PRESENTATION_REPRESENTATION('',(#68940),#93120);
#193445=CARTESIAN_POINT ( 'NONE',  ( 6.827182134110199918, 7.629137130509069387, 2.789055895399249252 ) ) ;
#193446=CARTESIAN_POINT ( 'NONE',  ( 0.5103889644224939293, -1.913802852362625151, 0.6352017490645140985 ) ) ;
#193449=CARTESIAN_POINT ( 'NONE',  ( 4.961816271168416392, -0.5573412460852051886, 1.993729458732765858 ) ) ;
#193450=CARTESIAN_POINT ( 'NONE',  ( 2.982943389344643759, -0.1423259158175680661, -1.921303036959535415 ) ) ;
#193451=CARTESIAN_POINT ( 'NONE',  ( 0.3336115229473045618, 0.6298545048411038350, -1.915608025624820909 ) ) ;
#193455=CARTESIAN_POINT ( 'NONE',  ( 4.399236341264299632, -1.715665262265529734, 0.9668539646570695201 ) ) ;
#193456=CARTESIAN_POINT ( 'NONE',  ( 0.5510472016944796270, -1.853416330350022179, -1.169031858332982177 ) ) ;
#193457=CARTESIAN_POINT ( 'NONE',  ( 3.703562413045482060, -0.5285312144065814621, 1.747510042522756990 ) ) ;
#193463=CARTESIAN_POINT ( 'NONE',  ( 1.786409390178132162, 1.601450680722369846, -0.9084932335857234253 ) ) ;
#193464=CARTESIAN_POINT ( 'NONE',  ( 4.605731108040309607, 1.494732351555028371, 1.348829144277723824 ) ) ;
#193465=CARTESIAN_POINT ( 'NONE',  ( 0.8612291682562907003, -0.8250023432496387255, 2.145356560901264142 ) ) ;
#193466=CARTESIAN_POINT ( 'NONE',  ( 5.032062496497622384, 1.126290172248314292, 1.606047186625796819 ) ) ;
#193472=CARTESIAN_POINT ( 'NONE',  ( 1.962552558803489555, -1.912825090402545225, -0.8444004386199343015 ) ) ;
#193474=CARTESIAN_POINT ( 'NONE',  ( 0.3560485870845608858, 0.7116971694140910021, 1.730184004908103867 ) ) ;
#193475=CARTESIAN_POINT ( 'NONE',  ( -0.1104750535120234134, 0.7027814200676918421, -2.185477693842474256 ) ) ;
#193476=CARTESIAN_POINT ( 'NONE',  ( 1.821426705348125230, 1.001848811563336605, -1.422965107008233643 ) ) ;
#193480=CARTESIAN_POINT ( 'NONE',  ( 2.138867256381206783, -1.541494696628985528, 0.7741069473117598854 ) ) ;
#193481=CARTESIAN_POINT ( 'NONE',  ( 1.575987392057216940, -1.168677030305173004, 1.853764812240476623 ) ) ;
#193482=CARTESIAN_POINT ( 'NONE',  ( 4.406973378220558679, 1.706932345810768359, -1.398813476408675260 ) ) ;
#193486=CARTESIAN_POINT ( 'NONE',  ( 2.518641040286667465, 0.9249485440519630286, 1.964284900515224530 ) ) ;
#193487=CARTESIAN_POINT ( 'NONE',  ( 1.049113529465800054, -1.437755431736492673, -1.125068434497819680 ) ) ;
#193488=CARTESIAN_POINT ( 'NONE',  ( 3.186815374238487930, 1.666415522689016049, -1.306070977860743110 ) ) ;
#193489=CARTESIAN_POINT ( 'NONE',  ( 6.539320575229287336, 0.6031692783194403384, 1.851139666870088130 ) ) ;
#193491=CARTESIAN_POINT ( 'NONE',  ( 3.667766089696015364, 1.274287168460963127, 1.905377313346041435 ) ) ;
#193495=CARTESIAN_POINT ( 'NONE',  ( 6.182328207180960433, 1.139467527619671294, 1.906663674214443382 ) ) ;
#193502=CARTESIAN_POINT ( 'NONE',  ( 3.709611425391425854, 1.915599900965975433, 0.6298755557959597740 ) ) ;
#193504=CARTESIAN_POINT ( 'NONE',  ( 2.342701370759682433, -2.021932799725610241, -0.4066214432158538616 ) ) ;
#193509=CARTESIAN_POINT ( 'NONE',  ( 5.226606370275341362, 0.1587857941063846590, 2.185760735149797185 ) ) ;
#193510=CARTESIAN_POINT ( 'NONE',  ( 2.320935597664942396, 0.9480396085976348086, -1.779626998253575509 ) ) ;
#193511=CARTESIAN_POINT ( 'NONE',  ( 2.471991059931688106, -1.762569054296094340, -0.5325411743367302053 ) ) ;
#193513=CARTESIAN_POINT ( 'NONE',  ( 6.792070425361753649, -0.7769146798779454910, 1.650438213995283565 ) ) ;
#193514=CARTESIAN_POINT ( 'NONE',  ( -0.1394461523061351904, -0.009327122704730000241, -2.280146446826665230 ) ) ;
#193516=CARTESIAN_POINT ( 'NONE',  ( 5.366221907327076046, 1.110187712879026956, 1.971344288924305799 ) ) ;
#193518=CARTESIAN_POINT ( 'NONE',  ( 0.2761803097106649840, 1.214566955493846967, 1.720366990225271842 ) ) ;
#193528=CARTESIAN_POINT ( 'NONE',  ( 3.340272282456987263, -1.325889367010645969, -1.782164031402436954 ) ) ;
#193533=CARTESIAN_POINT ( 'NONE',  ( 3.930091730393743710, 1.087902980620155891, 1.632394305395828304 ) ) ;
#193540=CARTESIAN_POINT ( 'NONE',  ( 3.094099843433151253, 1.348383549611749332, 1.636666742212993686 ) ) ;
#193542=CARTESIAN_POINT ( 'NONE',  ( 4.206063578812153203, -2.156103337031569200, 0.1562769059922017589 ) ) ;
#193543=CARTESIAN_POINT ( 'NONE',  ( 4.018977146631536712, -1.760761141180338774, 0.5383908109771737838 ) ) ;
#193546=CARTESIAN_POINT ( 'NONE',  ( 6.122986541590657694, -1.636244173936936885, 0.5932577488661006093 ) ) ;
#193547=CARTESIAN_POINT ( 'NONE',  ( 6.727182134110205602, 7.053355583909074689, 2.409100679957976165 ) ) ;
#193550=CARTESIAN_POINT ( 'NONE',  ( 3.397504326804317909, 1.702965868850464082, 1.331369057855802174 ) ) ;
#193551=AXIS2_PLACEMENT_3D ( 'NONE', #209599, #61243, #157695 ) ;
#193552=CARTESIAN_POINT ( 'NONE',  ( 5.290388671387995956, -1.915306256023459053, 0.6297802918850338161 ) ) ;
#193554=CARTESIAN_POINT ( 'NONE',  ( 2.114359756454447847, -1.018641858927371135, -1.906637348776268004 ) ) ;
#193555=CARTESIAN_POINT ( 'NONE',  ( 3.303940151695891281, -1.969246965329603638, 0.09337747576219912471 ) ) ;
#193557=CARTESIAN_POINT ( 'NONE',  ( 3.983879235506204264, -1.921370479222897165, -0.2818874784011967671 ) ) ;
#193565=CARTESIAN_POINT ( 'NONE',  ( 2.432911661931828284, 2.140371652790736601, 0.5367425311649312025 ) ) ;
#193567=CARTESIAN_POINT ( 'NONE',  ( 6.649272889308863732, 1.708415183241231983, -0.9640671636572254455 ) ) ;
#193572=CARTESIAN_POINT ( 'NONE',  ( 4.962772036422566480, 0.1772586797372834311, -1.832584332494808121 ) ) ;
#193577=CARTESIAN_POINT ( 'NONE',  ( 5.906510592826289319, -2.110524776404258507, -0.2060971850248518311 ) ) ;
#193580=CARTESIAN_POINT ( 'NONE',  ( 6.714142707505978080, -0.9671387161254895171, -1.819716304366093551 ) ) ;
#193581=CARTESIAN_POINT ( 'NONE',  ( 2.154548830654204217, -0.4927303200079625745, -1.794580903941452865 ) ) ;
#193582=CARTESIAN_POINT ( 'NONE',  ( 3.456447201099471123, -1.625387274077850996, -0.8650149607793489182 ) ) ;
#193588=CARTESIAN_POINT ( 'NONE',  ( 3.053566222061272040, -1.804402116661915967, -1.270350324234905903 ) ) ;
#193589=CARTESIAN_POINT ( 'NONE',  ( 6.274757189715042927, -2.145364790639526564, -0.7184590933012062752 ) ) ;
#193591=CARTESIAN_POINT ( 'NONE',  ( 6.117428737855862941, 1.511353622793030427, 0.9985130155200862001 ) ) ;
#193592=CARTESIAN_POINT ( 'NONE',  ( 6.438697963858233564, -1.475898738386885123, 1.221124472464208743 ) ) ;
#193596=CARTESIAN_POINT ( 'NONE',  ( 5.893391625361731556, 1.417579469995243091, 1.220656814419220249 ) ) ;
#193597=CARTESIAN_POINT ( 'NONE',  ( 5.795548653916324788, 1.765151677092157811, -0.7360495477024899813 ) ) ;
#193598=CARTESIAN_POINT ( 'NONE',  ( 0.6373110600932235803, -1.319858442276698129, -1.325903642019378381 ) ) ;
#193599=CARTESIAN_POINT ( 'NONE',  ( 1.323454262349360144, -1.463929862531298198, -1.387097294446784090 ) ) ;
#193601=CARTESIAN_POINT ( 'NONE',  ( 3.580784747083717523, -2.029690618531124091, -0.5617794247858574064 ) ) ;
#193606=CARTESIAN_POINT ( 'NONE',  ( 2.742449504557340489, 1.118516972803576870, -1.681586373676981827 ) ) ;
#193609=CARTESIAN_POINT ( 'NONE',  ( 3.831458500214664387, -1.998831773244442056, 0.8233788064144487162 ) ) ;
#193615=CARTESIAN_POINT ( 'NONE',  ( 0.3796378701454300453, -0.1059898317679157376, 2.168723291021804833 ) ) ;
#193619=CARTESIAN_POINT ( 'NONE',  ( 2.507599501126521524, -2.167277876680247850, 0.3246147914140809498 ) ) ;
#193620=CARTESIAN_POINT ( 'NONE',  ( 6.983263157960363010, -0.003310164959547181717, 1.953544951557646403 ) ) ;
#193621=CARTESIAN_POINT ( 'NONE',  ( 2.061739773175938595, 0.3863463398323406794, -2.229145236428681454 ) ) ;
#193627=CARTESIAN_POINT ( 'NONE',  ( 4.762845401903825326, -1.580659612885275012, -0.7961057336023872333 ) ) ;
#193629=CARTESIAN_POINT ( 'NONE',  ( 0.4289210115673793844, 2.015304021226202558, 0.6111801191295732627 ) ) ;
#193632=CARTESIAN_POINT ( 'NONE',  ( 6.538686444676896414, -1.556836737174282836, 1.281159629702780078 ) ) ;
#193635=CARTESIAN_POINT ( 'NONE',  ( 3.467518583331068438, 1.825290416974333807, -0.4087457676540603990 ) ) ;
#193636=CARTESIAN_POINT ( 'NONE',  ( 3.098552089154332112, 2.054082100768514607, 0.2579794602402472603 ) ) ;
#193641=SURFACE_STYLE_USAGE ( .BOTH. , #30086 ) ;
#193642=EDGE_CURVE ( 'NONE', #71735, #53136, #5470, .T. ) ;
#193645=CARTESIAN_POINT ( 'NONE',  ( 3.701569118832209515, -1.483977648892897960, -1.283320388228793130 ) ) ;
#193646=CARTESIAN_POINT ( 'NONE',  ( 0.4915642615439493879, 1.928455281639355867, 0.5879340682083398217 ) ) ;
#193650=CARTESIAN_POINT ( 'NONE',  ( 0.7900579835180140398, -1.855660487967484951, -0.2351621623290362506 ) ) ;
#193652=CARTESIAN_POINT ( 'NONE',  ( 2.847905013607958669, -1.355098151751940483, -1.488992504630684000 ) ) ;
#193654=CARTESIAN_POINT ( 'NONE',  ( 1.933370326505511105, -1.702675829696152388, -1.258230627273223545 ) ) ;
#193656=CARTESIAN_POINT ( 'NONE',  ( 3.648938843998358106, -0.4010542052625790110, -2.030977206718207473 ) ) ;
#193658=CARTESIAN_POINT ( 'NONE',  ( 0.09931936810910445279, -0.5537021472524807919, 2.016037456109684989 ) ) ;
#193660=CARTESIAN_POINT ( 'NONE',  ( 5.192344348049102720, -1.811977082810274808, -0.2219828972063255801 ) ) ;
#193666=CARTESIAN_POINT ( 'NONE',  ( 6.282275147445602670, -1.185768659569720329, 1.860957768143455038 ) ) ;
#193668=CARTESIAN_POINT ( 'NONE',  ( 5.602191078447533279, -0.8559053986842229955, 1.710104642658970997 ) ) ;
#193680=SURFACE_STYLE_FILL_AREA ( #61555 ) ;
#193684=CARTESIAN_POINT ( 'NONE',  ( 2.623828205405827507, 1.932375918485039756, -0.3793698109293401344 ) ) ;
#193685=CARTESIAN_POINT ( 'NONE',  ( 3.286732619643798703, 1.587825416925658262, -1.242744175535138940 ) ) ;
#193688=CARTESIAN_POINT ( 'NONE',  ( 6.827182134110222123, 4.687887262399931920, 2.751577338787388083 ) ) ;
#193689=CARTESIAN_POINT ( 'NONE',  ( 3.504031732436951874, -0.8880451304637152488, -2.003635182500095535 ) ) ;
#193691=CARTESIAN_POINT ( 'NONE',  ( 2.063383741992553144, 0.3316209358346365876, -1.897488084917675843 ) ) ;
#193693=CARTESIAN_POINT ( 'NONE',  ( -0.1296875068448125057, 1.390030859318210688, -2.083197486262199138 ) ) ;
#193694=CARTESIAN_POINT ( 'NONE',  ( 0.2329586101569527945, 7.629137130509077380, -2.445728209250570107 ) ) ;
#193701=CARTESIAN_POINT ( 'NONE',  ( 5.302248432823610358, 1.390444127666954355, -1.207098008268410183 ) ) ;
#193702=CARTESIAN_POINT ( 'NONE',  ( 2.209637070578834628, 1.557646164037255643, 1.275278917823706948 ) ) ;
#193703=CARTESIAN_POINT ( 'NONE',  ( 4.007374829128952598, 2.286843722993581185, 0.2302655642077624243 ) ) ;
#193704=CARTESIAN_POINT ( 'NONE',  ( -0.1291982275798625457, 2.008329037175633491, -2.487957029800022202 ) ) ;
#193705=CARTESIAN_POINT ( 'NONE',  ( 2.465471660774602558, -0.4132369024843309258, 1.814301444843221089 ) ) ;
#193708=CARTESIAN_POINT ( 'NONE',  ( 5.062724140118719518, 0.5608846916410530348, 1.828269531156314853 ) ) ;
#193712=CARTESIAN_POINT ( 'NONE',  ( 4.528904929885309905, -1.910896387970087096, 0.8487916243252179305 ) ) ;
#193713=CARTESIAN_POINT ( 'NONE',  ( 3.151090109352538082, -1.528452604574185525, -1.078222621661927061 ) ) ;
#193718=CARTESIAN_POINT ( 'NONE',  ( 5.004412211769132313, -0.5859011197271257743, -1.622467267129880097 ) ) ;
#193720=CARTESIAN_POINT ( 'NONE',  ( 1.775574910200255818, 1.508776774498999718, -0.8547552410581791271 ) ) ;
#193724=CARTESIAN_POINT ( 'NONE',  ( 5.911019566678890058, -1.716411647115582140, 1.329421173595428884 ) ) ;
#193725=CARTESIAN_POINT ( 'NONE',  ( 4.213378774425760476, -0.3099129147984269195, 1.799030153321119263 ) ) ;
#193726=CARTESIAN_POINT ( 'NONE',  ( 1.815213341579174688, -1.679845371888911698, -1.013028538569618719 ) ) ;
#193727=CARTESIAN_POINT ( 'NONE',  ( 0.1931602983361295767, 1.844477155017531844, 1.039358475685886907 ) ) ;
#193731=CARTESIAN_POINT ( 'NONE',  ( 2.596466591541984226, -1.087938976695131066, 1.819974527870950265 ) ) ;
#193735=CARTESIAN_POINT ( 'NONE',  ( 6.912935025559954205, -1.683935878860399971, 1.369999676949062550 ) ) ;
#193738=CARTESIAN_POINT ( 'NONE',  ( 3.580930751873512285, -1.490882799914891033, 1.646821992171596971 ) ) ;
#193740=CARTESIAN_POINT ( 'NONE',  ( 0.8272591630335036639, 0.9250671760404407529, -2.104501483148725427 ) ) ;
#193742=CARTESIAN_POINT ( 'NONE',  ( 5.506706524517535506, 0.5933582781832097419, 1.975413352875006856 ) ) ;
#193745=CARTESIAN_POINT ( 'NONE',  ( 6.110883706712432861, -0.2185277653131960651, 1.828168259763853776 ) ) ;
#193748=CARTESIAN_POINT ( 'NONE',  ( 3.363966847960923268, 0.7745139696748448710, 1.541148353905038126 ) ) ;
#193749=CARTESIAN_POINT ( 'NONE',  ( 0.8312679839070148402, -1.592664559859976237, -1.236796411087807801 ) ) ;
#193750=CARTESIAN_POINT ( 'NONE',  ( 3.200086968229500783, 2.078864265255635946, 0.9811947989078557697 ) ) ;
#193752=CARTESIAN_POINT ( 'NONE',  ( 2.794484930487377561, -2.256151742081555334, -0.1692699688307132133 ) ) ;
#193753=CARTESIAN_POINT ( 'NONE',  ( 4.723321587070372196, -0.1039652108096918437, 2.103624988570974352 ) ) ;
#193755=CARTESIAN_POINT ( 'NONE',  ( 3.127930002535435516, 0.9861435696450934207, -1.469289397387682161 ) ) ;
#193758=CARTESIAN_POINT ( 'NONE',  ( 6.146038201015474378, 0.7148980135479511278, 2.178090959246486324 ) ) ;
#193759=CARTESIAN_POINT ( 'NONE',  ( 4.294743845541324490, 1.480121740587354573, 1.094796260939827404 ) ) ;
#193764=CARTESIAN_POINT ( 'NONE',  ( 4.330150130892728377, 2.148942519667027984, 0.4286813238914553015 ) ) ;
#193770=CARTESIAN_POINT ( 'NONE',  ( 2.895051130818243834, 1.652057846050537515, -0.9908002393040680200 ) ) ;
#193773=CARTESIAN_POINT ( 'NONE',  ( 0.5630927014088433769, 0.6521865704650819939, 2.123503569120980927 ) ) ;
#193780=CARTESIAN_POINT ( 'NONE',  ( 2.770765728838171960, 1.651868531079144553, -0.5482889651245922424 ) ) ;
#193787=CARTESIAN_POINT ( 'NONE',  ( 6.227428301493934448, -2.037140905555033576, 0.7235935974677574212 ) ) ;
#193791=CARTESIAN_POINT ( 'NONE',  ( 0.1923495491853322581, -0.4021996241703913455, -1.833441224692602844 ) ) ;
#193792=CARTESIAN_POINT ( 'NONE',  ( 5.782511917101329502, -1.690859530023439250, 0.3827970650602616765 ) ) ;
#193794=CARTESIAN_POINT ( 'NONE',  ( 3.193114300108112147, 1.729001323093733111, 1.346577201094656395 ) ) ;
#193795=CARTESIAN_POINT ( 'NONE',  ( 3.540313787445231508, 1.039887675495542618, -2.060077152250729071 ) ) ;
#193796=CARTESIAN_POINT ( 'NONE',  ( 5.360643824631334375, -1.495535663558609674, 1.418079957933044755 ) ) ;
#193797=CARTESIAN_POINT ( 'NONE',  ( 1.201004818612857017, -0.4721336787944198643, 1.883569333377318245 ) ) ;
#193801=CARTESIAN_POINT ( 'NONE',  ( 4.271814301144261528, 0.4616217191124799002, -2.069597271375968273 ) ) ;
#193802=CARTESIAN_POINT ( 'NONE',  ( 1.846327496167538884, 0.3419342931599393398, -1.987046799686801757 ) ) ;
#193804=CARTESIAN_POINT ( 'NONE',  ( 5.807716119225245777, -0.5415507062403871474, 2.139171552897000339 ) ) ;
#193807=CARTESIAN_POINT ( 'NONE',  ( 0.3811277156573149583, 1.704729334087114578, -0.6539457117896373406 ) ) ;
#193813=CARTESIAN_POINT ( 'NONE',  ( 4.469639075930389893, 1.999461767218065678, -0.4989166988303375683 ) ) ;
#193815=CARTESIAN_POINT ( 'NONE',  ( -0.2108831679771203116, 0.7314853703891763814, -1.979988191570913880 ) ) ;
#193818=CARTESIAN_POINT ( 'NONE',  ( 4.828773858256512064, 1.391243881446821762, -1.464325142460545459 ) ) ;
#193823=CARTESIAN_POINT ( 'NONE',  ( 3.414965445803084254, 1.862500966792278057, 0.8825600945957471355 ) ) ;
#193824=CARTESIAN_POINT ( 'NONE',  ( 2.865861461037176205, -0.1511401116795624278, -2.010826411938296143 ) ) ;
#193830=CARTESIAN_POINT ( 'NONE',  ( 2.934922540206805319, 1.076151813804010926, 1.704677747124828446 ) ) ;
#193831=CARTESIAN_POINT ( 'NONE',  ( 1.904012794591736668, 1.364881752761820222, -1.235849761865935870 ) ) ;
#193832=CARTESIAN_POINT ( 'NONE',  ( 0.06561565146986823860, -2.064482179495107150, -1.031447015078267304 ) ) ;
#193835=CARTESIAN_POINT ( 'NONE',  ( 2.179201376995115513, -0.1036959380565916911, -2.159207860300814463 ) ) ;
#193841=CARTESIAN_POINT ( 'NONE',  ( 1.516246529245099284, 1.258767711876613848, -1.383943980506313398 ) ) ;
#193842=CARTESIAN_POINT ( 'NONE',  ( 5.207875265678946874, -1.962022031532301369, 0.1926216461900862598 ) ) ;
#193846=CARTESIAN_POINT ( 'NONE',  ( 0.08304785351339466493, -2.141800023564765620, -0.5316218738360134477 ) ) ;
#193847=CARTESIAN_POINT ( 'NONE',  ( 6.496543107701719499, 2.047251205643263017, 0.3077783505985449142 ) ) ;
#193850=CARTESIAN_POINT ( 'NONE',  ( 6.539320575229258914, 2.958022083381315337, 2.556018433155104574 ) ) ;
#193851=CARTESIAN_POINT ( 'NONE',  ( 5.137557537983609812, -1.393591726081166771, -1.394729141857486532 ) ) ;
#193852=CARTESIAN_POINT ( 'NONE',  ( 6.433853624855537134, -1.958103210868083810, 0.4948410764434567066 ) ) ;
#193854=CARTESIAN_POINT ( 'NONE',  ( 4.951972348128318657, 0.7275260799690360658, -2.190091995644850797 ) ) ;
#193856=CARTESIAN_POINT ( 'NONE',  ( 1.481379835429663228, -0.05473030402166743219, 2.062018025990194126 ) ) ;
#193863=CARTESIAN_POINT ( 'NONE',  ( 3.842362351650536301, -1.073271228610745309, 1.887301499758537116 ) ) ;
#193866=CARTESIAN_POINT ( 'NONE',  ( 4.546344060013487898, -1.475942220874026489, 1.100600019281534836 ) ) ;
#193868=CARTESIAN_POINT ( 'NONE',  ( 6.720655732516652492, 7.053303974100803231, 2.424416723604695179 ) ) ;
#193869=CARTESIAN_POINT ( 'NONE',  ( 4.985950990042907094, -2.174969566330759996, -0.2684501861200879747 ) ) ;
#193871=CARTESIAN_POINT ( 'NONE',  ( 5.577129106639307388, -0.04938619725537891220, -2.262140991306497373 ) ) ;
#193874=CARTESIAN_POINT ( 'NONE',  ( -0.1108833634136781182, 7.629137130509072939, -2.496956624467902675 ) ) ;
#193879=CARTESIAN_POINT ( 'NONE',  ( 1.182078593147641632, -1.725526258793514067, -0.3928099155053321745 ) ) ;
#193880=CARTESIAN_POINT ( 'NONE',  ( 5.514319586171100518, -2.013265972089046230, 0.002284521408187425995 ) ) ;
#193882=CARTESIAN_POINT ( 'NONE',  ( 4.243269300766455920, -1.833519874744583111, 1.035826785333898270 ) ) ;
#193883=CARTESIAN_POINT ( 'NONE',  ( 2.073720586576404568, -0.8169873708120840572, 1.732773573125611088 ) ) ;
#193886=CARTESIAN_POINT ( 'NONE',  ( 2.787508051956408384, -1.838732291863707236, 0.7063352763673010903 ) ) ;
#193887=CARTESIAN_POINT ( 'NONE',  ( 5.133071871609922177, 1.867805937340912159, 0.7691607467245373808 ) ) ;
#193888=CARTESIAN_POINT ( 'NONE',  ( 1.322894217037654085, -0.04941562205608432401, 1.870173573632450958 ) ) ;
#193889=CARTESIAN_POINT ( 'NONE',  ( 4.934089290906335634, 0.8825209879863432638, -1.481864930267517089 ) ) ;
#193890=CARTESIAN_POINT ( 'NONE',  ( 1.511816067030671729, -0.6413169068853613597, 1.801808535584384252 ) ) ;
#193892=CARTESIAN_POINT ( 'NONE',  ( 1.629795212970772456, -2.077151576879713080, 0.7458654493318407352 ) ) ;
#193897=CARTESIAN_POINT ( 'NONE',  ( 6.825078400183573812, 0.002648415797040087893, 1.855566311045192540 ) ) ;
#193901=CARTESIAN_POINT ( 'NONE',  ( 0.9243811426856913815, 1.018911950503737174, 1.802186752163869699 ) ) ;
#193906=CARTESIAN_POINT ( 'NONE',  ( 6.551439628692993900, -1.894445571042557619, 0.9528467149547341641 ) ) ;
#193913=CARTESIAN_POINT ( 'NONE',  ( 4.411482401463855396, 0.5350073857553553358, 1.943773423102819864 ) ) ;
#193914=CARTESIAN_POINT ( 'NONE',  ( 5.208173988833650903, 1.135812200204017630, -1.542565181195413526 ) ) ;
#193915=CARTESIAN_POINT ( 'NONE',  ( 3.228257827484398490, 2.138632370135685523, 0.4780590757816546854 ) ) ;
#193918=CARTESIAN_POINT ( 'NONE',  ( 4.922139854824453487, -2.003099925734778797, 0.2017396019941309904 ) ) ;
#193921=CARTESIAN_POINT ( 'NONE',  ( 5.941034585168498694, -1.816085283887830082, -1.088097372982429034 ) ) ;
#193923=CARTESIAN_POINT ( 'NONE',  ( 3.773056988009905410, 1.967892522216899476, -0.7064651350525589235 ) ) ;
#193925=CARTESIAN_POINT ( 'NONE',  ( 2.432253191915220825, 1.672178088080849223, 0.4220979471536658867 ) ) ;
#193927=CARTESIAN_POINT ( 'NONE',  ( 4.816704082729271086, -0.7169179515637627009, -1.995842421597990413 ) ) ;
#193936=CARTESIAN_POINT ( 'NONE',  ( 1.137045503269896285, -0.04498225810314023659, 1.811072777871777006 ) ) ;
#193942=CARTESIAN_POINT ( 'NONE',  ( 3.228980503213836339, 1.638859372766150679, 0.7719998214037685491 ) ) ;
#193943=CARTESIAN_POINT ( 'NONE',  ( 6.639320575229239019, 3.696696400505532942, 2.511109302898812956 ) ) ;
#193947=CARTESIAN_POINT ( 'NONE',  ( 4.123391753781197266, 0.2291962677869363585, -1.846827494033479455 ) ) ;
#193948=CARTESIAN_POINT ( 'NONE',  ( 1.388148191917773611, -0.6910900405009687830, -1.786773533054702545 ) ) ;
#193949=CARTESIAN_POINT ( 'NONE',  ( 6.387721611049761883, 1.328912806184729734, 1.394852177740999233 ) ) ;
#193954=CARTESIAN_POINT ( 'NONE',  ( 6.034039001082764919, 1.170257472284089717, 1.583912470002272199 ) ) ;
#193958=CARTESIAN_POINT ( 'NONE',  ( 6.714806894218784628, -0.1628439675423892508, 2.155775914164249407 ) ) ;
#193960=CARTESIAN_POINT ( 'NONE',  ( 5.069325366411169931, 0.1891801624123757852, -1.917091172425288370 ) ) ;
#193962=CARTESIAN_POINT ( 'NONE',  ( 1.658932825283397250, -1.563847321437005666, -0.9416461389453802955 ) ) ;
#193963=CARTESIAN_POINT ( 'NONE',  ( 2.631697372267821855, -2.058793095894187353, 0.7952504953367269813 ) ) ;
#193964=CARTESIAN_POINT ( 'NONE',  ( 0.08795244648929222142, 1.102731429460445334, 1.562230693318837238 ) ) ;
#193965=ORIENTED_EDGE ( 'NONE', *, *, #182948, .T. ) ;
#193966=CARTESIAN_POINT ( 'NONE',  ( 0.9417814284814338688, 1.320271805612409421, 1.461702747868667496 ) ) ;
#193967=CARTESIAN_POINT ( 'NONE',  ( 2.577597507962032353, -0.9963960007246205342, 1.666827093504752222 ) ) ;
#193968=EDGE_LOOP ( 'NONE', ( #42426, #21812, #138354, #39159 ) ) ;
#193969=CARTESIAN_POINT ( 'NONE',  ( 1.388045824401448414, -0.05229234656609069859, 2.015604296821980057 ) ) ;
#193971=CARTESIAN_POINT ( 'NONE',  ( 5.190230013454653069, 0.9586131782086585451, -1.594917819662385883 ) ) ;
#193977=CARTESIAN_POINT ( 'NONE',  ( 0.9432342461353732110, -1.730868645791438842, -1.344178957308760802 ) ) ;
#193981=CARTESIAN_POINT ( 'NONE',  ( 3.193790821891542731, -0.7392406677243367197, 1.669511829839696260 ) ) ;
#193985=CARTESIAN_POINT ( 'NONE',  ( 6.609000000000029296, 3.690475914267136837, 2.614198802211770367 ) ) ;
#193987=CARTESIAN_POINT ( 'NONE',  ( 1.436025505276457226, 0.9502256629446425018, -1.675776081635256043 ) ) ;
#193988=CARTESIAN_POINT ( 'NONE',  ( 5.137533780887935997, 1.831872034461759835, -0.7024582609849658876 ) ) ;
#193991=CARTESIAN_POINT ( 'NONE',  ( 4.687173145698103838, 1.624054394666199830, 1.471728111018810070 ) ) ;
#193994=CARTESIAN_POINT ( 'NONE',  ( 4.170806909802426965, 1.467596682293986765, -1.460439952253207663 ) ) ;
#193997=EDGE_LOOP ( 'NONE', ( #34692, #161255, #183447, #75015 ) ) ;
#193998=CARTESIAN_POINT ( 'NONE',  ( 3.973462176510922816, -2.273730406356341049, -0.3370867821424743949 ) ) ;
#194005=CARTESIAN_POINT ( 'NONE',  ( 3.345582828684705134, 1.942124712213384452, -0.0007862604347076693808 ) ) ;
#194009=CARTESIAN_POINT ( 'NONE',  ( 5.045129621168108258, 0.1466893748028277877, 1.906852434080000824 ) ) ;
#194011=CARTESIAN_POINT ( 'NONE',  ( 6.229511965242640059, -1.622199917339474329, 0.5863599495292673991 ) ) ;
#194012=CARTESIAN_POINT ( 'NONE',  ( 4.962125165302472496, -1.116212726388360998, 1.679221540125563905 ) ) ;
#194014=CARTESIAN_POINT ( 'NONE',  ( 2.403190426070573871, 1.771669130372434564, -1.315670724662293178 ) ) ;
#194017=CARTESIAN_POINT ( 'NONE',  ( 1.640690513341718670, -1.765443103004183056, 1.119499978516135252 ) ) ;
#194018=CARTESIAN_POINT ( 'NONE',  ( 0.1800360811037614583, -1.714963048871451790, -0.4369287763777151556 ) ) ;
#194019=CARTESIAN_POINT ( 'NONE',  ( 5.643203987388664800, 0.8197706014990979728, 1.842448445624145226 ) ) ;
#194021=CARTESIAN_POINT ( 'NONE',  ( 3.258078344973667662, 1.030780755083884115, 2.047500790377681845 ) ) ;
#194022=CARTESIAN_POINT ( 'NONE',  ( 1.200653373194009443, -0.4260525342448440722, 1.687239105062097400 ) ) ;
#194025=CARTESIAN_POINT ( 'NONE',  ( 0.7371068013607602332, -1.629765380930665364, -0.5920680523868580014 ) ) ;
#194028=CARTESIAN_POINT ( 'NONE',  ( 1.610090671168771470, 0.6309225058772853778, -2.077463247357013820 ) ) ;
#194029=CARTESIAN_POINT ( 'NONE',  ( 1.991423064788412800, -0.4370762659771566527, 1.968445590580846893 ) ) ;
#194030=CARTESIAN_POINT ( 'NONE',  ( 4.375000000000001776, 2.052068128417944504, -2.491713675105573160E-13 ) ) ;
#194032=CARTESIAN_POINT ( 'NONE',  ( 0.4109946218407485308, 1.674316264148696165, 0.9526004100348076653 ) ) ;
#194034=CARTESIAN_POINT ( 'NONE',  ( 2.865722905416301369, -1.818493784693291815, -1.275605581943892730 ) ) ;
#194039=CARTESIAN_POINT ( 'NONE',  ( 5.987833318177087527, -1.732952516383274855, -0.1613439405771869561 ) ) ;
#194040=COLOUR_RGB ( '', 0.66274510, 0.83137255, 0.94901961) ;
#194041=CARTESIAN_POINT ( 'NONE',  ( 3.912515228517557286, 0.7039278570535618673, 1.831416474553926310 ) ) ;
#194045=DIRECTION ( 'NONE',  ( -1.000000000000000000, 0.000000000000000000, 0.000000000000000000 ) ) ;
#194046=CARTESIAN_POINT ( 'NONE',  ( 4.270984383450874944, -2.108973115933824527, -0.8193970387949424117 ) ) ;
#194047=CARTESIAN_POINT ( 'NONE',  ( 2.260285141513069362, -2.062262451202213853, 0.04833688706953364472 ) ) ;
#194051=CARTESIAN_POINT ( 'NONE',  ( 3.813614929637610285, -1.843318686535614148, 0.3169883347873064250 ) ) ;
#194052=CARTESIAN_POINT ( 'NONE',  ( 2.883173651945786009, -0.5064310303744267161, -1.658517218374066848 ) ) ;
#194053=CARTESIAN_POINT ( 'NONE',  ( 6.128506746050899068, 0.2130254606748181456, 2.181202035047181020 ) ) ;
#194054=CARTESIAN_POINT ( 'NONE',  ( 6.686558038528344738, -2.261219263861591333, -0.4595595737692282912 ) ) ;
#194055=CARTESIAN_POINT ( 'NONE',  ( 4.118171802502921253, -1.108985364570359566, -1.855417305202881506 ) ) ;
#194056=CARTESIAN_POINT ( 'NONE',  ( 4.119036135373352003, -1.858019016064060169, 0.5647323716678387395 ) ) ;
#194058=CARTESIAN_POINT ( 'NONE',  ( 6.538356921592370696, 1.850225872366148883, 0.2742375073267953045 ) ) ;
#194062=CARTESIAN_POINT ( 'NONE',  ( 0.1234922912959918878, 1.848187084301698757, 1.039613981531524400 ) ) ;
#194064=CARTESIAN_POINT ( 'NONE',  ( 5.783827325522512552, 1.646840809264274119, -1.163266671679111353 ) ) ;
#194068=CARTESIAN_POINT ( 'NONE',  ( 3.404746562951189937, 1.438594061741470753, -1.123979961188771304 ) ) ;
#194069=CARTESIAN_POINT ( 'NONE',  ( 2.591098708763440062, -0.3764507303484417311, -2.174265822884546395 ) ) ;
#194074=CARTESIAN_POINT ( 'NONE',  ( 0.7912781446984231692, -0.05379174966265751895, -2.019256707098691095 ) ) ;
#194075=CARTESIAN_POINT ( 'NONE',  ( 1.594549238318817785, -1.131586138893545979, 1.793127659086241499 ) ) ;
#194079=CARTESIAN_POINT ( 'NONE',  ( 1.902945097309636013, -1.575467964945817867, 0.9901336090045903537 ) ) ;
#194081=CARTESIAN_POINT ( 'NONE',  ( 5.928604924596339032, 1.985460353506541376, 0.5521678710885301600 ) ) ;
#194082=CARTESIAN_POINT ( 'NONE',  ( 5.678361341766085424, 1.528739221709461082, 1.314999087022615587 ) ) ;
#194086=( BOUNDED_CURVE ( )  B_SPLINE_CURVE ( 3, ( #90319, #6896, #59940, #189938 ),
 .UNSPECIFIED., .F., .T. ) 
 B_SPLINE_CURVE_WITH_KNOTS ( ( 4, 4 ),
 ( 0.000000000000000000, 0.4999999999999984457 ),
 .UNSPECIFIED. ) 
 CURVE ( )  GEOMETRIC_REPRESENTATION_ITEM ( )  RATIONAL_B_SPLINE_CURVE ( ( 1.000000000000000000, 0.3333333333333354243, 0.3333333333333333703, 0.9999999999999978906 ) ) 
 REPRESENTATION_ITEM ( '' )  );
#194089=CARTESIAN_POINT ( 'NONE',  ( 3.650846181029033133, -1.491723252493650564, 1.052289205326197852 ) ) ;
#194093=CARTESIAN_POINT ( 'NONE',  ( 6.239611212763971793, -1.913511330438378177, -0.6350998681113121380 ) ) ;
#194094=CARTESIAN_POINT ( 'NONE',  ( 5.595603887632320195, -1.841320590885606068, 0.004091980732826016286 ) ) ;
#194096=CARTESIAN_POINT ( 'NONE',  ( 0.07700591528351108384, 2.887024434135841755, -2.399578936219012082 ) ) ;
#194097=CARTESIAN_POINT ( 'NONE',  ( 3.967613463194498813, 0.2842429903056520324, -2.290057832888813483 ) ) ;
#194099=CARTESIAN_POINT ( 'NONE',  ( 6.239563118392394969, -1.560868990211834895, -1.495623836407403262 ) ) ;
#194101=CARTESIAN_POINT ( 'NONE',  ( 0.6439600106935819968, 0.5648315236305987419, 1.858087668232853984 ) ) ;
#194103=CARTESIAN_POINT ( 'NONE',  ( 4.323764262282871584, -1.706850429308865547, 1.539420282360188574 ) ) ;
#194106=CARTESIAN_POINT ( 'NONE',  ( 5.032044620589739559, 0.9611010790777809731, -1.604743002217932313 ) ) ;
#194107=CARTESIAN_POINT ( 'NONE',  ( 1.986440140746603911, -1.173720106059353396, 1.509789020923378189 ) ) ;
#194110=CARTESIAN_POINT ( 'NONE',  ( 3.387540773601561916, 1.995160029947869340, -0.9435142334218297178 ) ) ;
#194111=CARTESIAN_POINT ( 'NONE',  ( 6.983263157960402090, 0.5904152146812295943, 1.899285251901380089 ) ) ;
#194116=CARTESIAN_POINT ( 'NONE',  ( 1.176956626245349247, -0.04423564266526488348, -1.971012800895243888 ) ) ;
#194117=CARTESIAN_POINT ( 'NONE',  ( 1.009288123910282442, 1.745381235414251275, -1.509623180311530977 ) ) ;
#194118=CARTESIAN_POINT ( 'NONE',  ( 2.523818479427087702, 1.924573107942130656, -0.3798230296482503210 ) ) ;
#194121=CARTESIAN_POINT ( 'NONE',  ( 4.803617054199708747, -1.591134784341166508, -1.312391874486463550 ) ) ;
#194129=CARTESIAN_POINT ( 'NONE',  ( 1.129994725911891207, 2.092989821048664822, -0.5768834896340956364 ) ) ;
#194133=CARTESIAN_POINT ( 'NONE',  ( 2.442468673064964957, 0.4055347385497136137, 1.825902681341363021 ) ) ;
#194134=CARTESIAN_POINT ( 'NONE',  ( 0.1751657365761209451, 0.002452341591326848407, -2.044164811867712483 ) ) ;
#194136=SURFACE_STYLE_FILL_AREA ( #142228 ) ;
#194139=CARTESIAN_POINT ( 'NONE',  ( 2.631394046745598736, -0.1854624247320437180, 1.903247139735386284 ) ) ;
#194140=CARTESIAN_POINT ( 'NONE',  ( 4.082668839255446436, -0.1736907016443404450, -1.761279006307460371 ) ) ;
#194141=CARTESIAN_POINT ( 'NONE',  ( 2.279812546382542493, 1.875032136476075584, -0.3747091278499328770 ) ) ;
#194144=CARTESIAN_POINT ( 'NONE',  ( 5.835529424904522422, 0.5513129833306378291, -1.834571867064521022 ) ) ;
#194146=CARTESIAN_POINT ( 'NONE',  ( 6.426221551499647688, 1.011104814135417751, 1.690039303870519705 ) ) ;
#194149=CARTESIAN_POINT ( 'NONE',  ( 5.137510444216992767, -1.323429205136433140, -1.322332877454430955 ) ) ;
#194150=CARTESIAN_POINT ( 'NONE',  ( 1.769861954154128725, 0.9373860217288846330, 1.566528536362868707 ) ) ;
#194151=EDGE_LOOP ( 'NONE', ( #33861, #74672, #73935, #108045 ) ) ;
#194152=CARTESIAN_POINT ( 'NONE',  ( 4.389439674793148782, 1.972019932058775016, -0.9908447712502415072 ) ) ;
#194155=CARTESIAN_POINT ( 'NONE',  ( 2.277848244636628827, -2.001361501815647870, 0.4987805053587587856 ) ) ;
#194164=CARTESIAN_POINT ( 'NONE',  ( 5.811005889236001032, -1.634438611397070806, 1.270752202701043609 ) ) ;
#194166=CARTESIAN_POINT ( 'NONE',  ( 2.583474834239877449, 1.977432880963815309, -0.8734481387390122809 ) ) ;
#194168=CARTESIAN_POINT ( 'NONE',  ( 3.492836188673923647, -1.947007740449010926, -0.5366636104956448161 ) ) ;
#194170=CARTESIAN_POINT ( 'NONE',  ( 6.620655732516668834, 6.034240673559561507, 2.768629221164942145 ) ) ;
#194176=CARTESIAN_POINT ( 'NONE',  ( 1.235564962061060257, 0.5807501988173838781, -1.931125984888550473 ) ) ;
#194177=CARTESIAN_POINT ( 'NONE',  ( 5.601184584505256581, -0.5335315006234629953, 2.125516261704554211 ) ) ;
#194179=CARTESIAN_POINT ( 'NONE',  ( 4.605663860560767375, 1.420894170025093439, 1.280184534114735095 ) ) ;
#194183=CARTESIAN_POINT ( 'NONE',  ( 3.603138812553498216, -0.1455146663824242736, 2.011206757212272933 ) ) ;
#194187=CARTESIAN_POINT ( 'NONE',  ( 5.192313411850084215, -1.712133481052197093, -0.2078965086465163203 ) ) ;
#194193=CARTESIAN_POINT ( 'NONE',  ( 0.7782871991188352601, -1.104406889285912907, -1.750870654829151274 ) ) ;
#194196=CARTESIAN_POINT ( 'NONE',  ( 5.391193890671133637, -0.05051413884850668168, -1.810949582550380521 ) ) ;
#194199=CARTESIAN_POINT ( 'NONE',  ( 5.900986446306966116, -0.2725449506757338658, -1.790729509878173475 ) ) ;
#194202=CARTESIAN_POINT ( 'NONE',  ( 2.537292984272555785, -1.624655320356691801, -1.470880813658273389 ) ) ;
#194205=CARTESIAN_POINT ( 'NONE',  ( 0.2034672893990868703, -1.513989045467616146, -1.247398002513319781 ) ) ;
#194207=CARTESIAN_POINT ( 'NONE',  ( 5.167565342116251514, 1.290006671357433632, 1.416291653197629952 ) ) ;
#194215=CARTESIAN_POINT ( 'NONE',  ( 1.727627455807039469, -2.035446057602477321, 0.7283451284763039490 ) ) ;
#194218=CARTESIAN_POINT ( 'NONE',  ( 1.869861807837460921, 0.9356042063937075604, 1.567457579366556386 ) ) ;
#194220=CARTESIAN_POINT ( 'NONE',  ( 5.104447739783800841, -0.6163660037172628003, -1.718524672285254740 ) ) ;
#194222=CARTESIAN_POINT ( 'NONE',  ( 2.443496805918866865, -1.782974011999260977, 0.6919810379762069141 ) ) ;
#194224=CARTESIAN_POINT ( 'NONE',  ( 3.437912432318380507, 1.247599126489881138, 1.524034350268144156 ) ) ;
#194226=CARTESIAN_POINT ( 'NONE',  ( 5.618683182394583753, -0.04358239772479224894, 1.941727988928889204 ) ) ;
#194230=CARTESIAN_POINT ( 'NONE',  ( 5.203433420164765622, 1.869144303625443371, -1.001675624404389620 ) ) ;
#194232=CARTESIAN_POINT ( 'NONE',  ( 3.949791169003769475, -1.320912084567291034, -1.382976300589415342 ) ) ;
#194237=CARTESIAN_POINT ( 'NONE',  ( 4.811194018343159406, 1.672433887399711994, -1.120210643937557871 ) ) ;
#194239=CARTESIAN_POINT ( 'NONE',  ( 6.533835636172961259, -1.196796279342365210, -1.378804128639096849 ) ) ;
#194240=CARTESIAN_POINT ( 'NONE',  ( 1.275928261265106611, -2.020323679977220621, 0.4517519998969781736 ) ) ;
#194247=( LENGTH_UNIT ( ) NAMED_UNIT ( * ) SI_UNIT ( .MILLI., .METRE. ) );
#194253=CARTESIAN_POINT ( 'NONE',  ( 3.340171489122942816, 0.4179119503955433523, -1.682892220811042616 ) ) ;
#194255=CARTESIAN_POINT ( 'NONE',  ( 1.340777958403309267, -2.018934908790828597, -0.4573474576154838989 ) ) ;
#194256=CARTESIAN_POINT ( 'NONE',  ( 1.950926998395795753, -1.937146449801559367, -0.8548520037577662656 ) ) ;
#194260=CARTESIAN_POINT ( 'NONE',  ( 1.112081256596690437, 1.967444819121874744, -0.09107992038001262725 ) ) ;
#194265=CARTESIAN_POINT ( 'NONE',  ( 2.976851957573245944, -0.1693691376928093406, -2.286062073229557345 ) ) ;
#194266=CARTESIAN_POINT ( 'NONE',  ( 0.8030139110496161692, 1.490934425176414724, 1.053415343471690857 ) ) ;
#194267=CARTESIAN_POINT ( 'NONE',  ( 2.988426722125224977, -1.135634098421594240, 1.538566774472991616 ) ) ;
#194272=CARTESIAN_POINT ( 'NONE',  ( 1.511978199970403836, -0.6742157057700901568, 1.897102442587648374 ) ) ;
#194273=CARTESIAN_POINT ( 'NONE',  ( 1.639427129605858902, 1.814645582613241714, -0.7458448512465406521 ) ) ;
#194277=CARTESIAN_POINT ( 'NONE',  ( 4.804676392994963408, 1.818819718876990565, 1.030695182279812272 ) ) ;
#194278=CARTESIAN_POINT ( 'NONE',  ( 3.889309559433737906, 1.281865973830035754, 1.220554204183731173 ) ) ;
#194281=CARTESIAN_POINT ( 'NONE',  ( 0.1819133275808570704, -1.029140439971199417, 1.934768540691175431 ) ) ;
#194282=CARTESIAN_POINT ( 'NONE',  ( 4.663825473582838832, -1.133750416550326046, 1.320446528551111776 ) ) ;
#194286=CARTESIAN_POINT ( 'NONE',  ( 4.235468066436924417, -1.617573843961607416, -0.6246848730444684028 ) ) ;
#194287=CARTESIAN_POINT ( 'NONE',  ( 4.457605324860562490, 1.741341149747036576, 1.296620029562136400 ) ) ;
#194289=CARTESIAN_POINT ( 'NONE',  ( 0.3041147963815365451, -1.138459102943665036, -1.785081232699109233 ) ) ;
#194290=CARTESIAN_POINT ( 'NONE',  ( 6.468749999177490828, 0.7852924545920478838, -1.895863743164218018 ) ) ;
#194292=CARTESIAN_POINT ( 'NONE',  ( 2.801685564775885595, -0.6058112460363762608, 1.828711369353401617 ) ) ;
#194294=CARTESIAN_POINT ( 'NONE',  ( 6.533471383080789785, -0.1550430487086348341, 2.186663148620856756 ) ) ;
#194296=CARTESIAN_POINT ( 'NONE',  ( 6.883263157960402445, 0.5924656843266817852, 1.899575500811432338 ) ) ;
#194300=CARTESIAN_POINT ( 'NONE',  ( 3.053626115265011709, -1.958026000861570415, 1.048987487942198094 ) ) ;
#194307=CARTESIAN_POINT ( 'NONE',  ( 0.4752326960846975923, -2.001511663014220677, -0.2440270837566413387 ) ) ;
#194309=CARTESIAN_POINT ( 'NONE',  ( 5.828601243409065269, -1.311231720126609490, 1.592247268936395121 ) ) ;
#194314=CARTESIAN_POINT ( 'NONE',  ( 0.4382651835369972826, 0.2938455168926180638, 1.745004787994571593 ) ) ;
#194315=CARTESIAN_POINT ( 'NONE',  ( 6.275961099261262000, 1.503942705979001593, -0.8632642021696999013 ) ) ;
#194316=CARTESIAN_POINT ( 'NONE',  ( 5.706559709869656771, 1.539012945689299139, 0.8127616963746787659 ) ) ;
#194317=CARTESIAN_POINT ( 'NONE',  ( 2.841680536636710386, 0.8224841172943345713, -2.139919992735066945 ) ) ;
#194319=CARTESIAN_POINT ( 'NONE',  ( 1.306327274835542784, 1.622920506532832929, 0.8694138843568788300 ) ) ;
#194322=CARTESIAN_POINT ( 'NONE',  ( 1.658932825283397250, -1.563847321437005666, -0.9416461389453802955 ) ) ;
#194323=CARTESIAN_POINT ( 'NONE',  ( 2.672500184003968382, 1.427937546361924381, 1.423961308954827754 ) ) ;
#194324=CARTESIAN_POINT ( 'NONE',  ( 1.043234067691005684, -1.729537258485488893, -1.345685951901639532 ) ) ;
#194326=CARTESIAN_POINT ( 'NONE',  ( 4.137795317726181032, -1.450671198928995098, -1.526879382678330010 ) ) ;
#194329=CARTESIAN_POINT ( 'NONE',  ( 1.381394743813993964, -0.05274132383669553892, 2.069866178704109938 ) ) ;
#194332=CARTESIAN_POINT ( 'NONE',  ( 4.143311163141575548, 0.1052805922370502884, 2.118007119816091688 ) ) ;
#194333=CARTESIAN_POINT ( 'NONE',  ( 0.3461526914491962481, 1.921225470409862357, 0.1432632881103387268 ) ) ;
#194340=CARTESIAN_POINT ( 'NONE',  ( -0.03451705771533463557, -1.778989527951052141, 1.330178892887582398 ) ) ;
#194341=CARTESIAN_POINT ( 'NONE',  ( 1.061710303787483989, 0.4109483673962707750, -2.065292405001526443 ) ) ;
#194345=CARTESIAN_POINT ( 'NONE',  ( 5.032013264887808646, 1.069401199365666688, 1.522792188549914272 ) ) ;
#194352=CARTESIAN_POINT ( 'NONE',  ( 2.365611650783586040, -0.4327418640146083462, 1.913375882425945917 ) ) ;
#194353=CARTESIAN_POINT ( 'NONE',  ( 0.6202742476981680797, -1.157488721396517040, -1.825510493854154426 ) ) ;
#194357=CARTESIAN_POINT ( 'NONE',  ( 2.741176079829604539, -1.657949034129829302, -0.5072451560675111937 ) ) ;
#194358=CARTESIAN_POINT ( 'NONE',  ( 2.712550014960776856, -0.1704709713557898410, 1.731945008791212270 ) ) ;
#194361=AXIS2_PLACEMENT_3D ( 'NONE', #32529, #98604, #66057 ) ;
#194362=CARTESIAN_POINT ( 'NONE',  ( 0.7903884775103054983, -1.915307795730588181, 0.6297756287277083143 ) ) ;
#194363=CARTESIAN_POINT ( 'NONE',  ( 6.925078400183566352, 7.051505795288234957, 2.842497989238515821 ) ) ;
#194365=CARTESIAN_POINT ( 'NONE',  ( 1.657037912627358001, -1.689797944177928279, -1.015304737199155483 ) ) ;
#194366=CARTESIAN_POINT ( 'NONE',  ( 5.414289803398987466, -1.912571729023364364, 0.006307610287324683096 ) ) ;
#194371=CARTESIAN_POINT ( 'NONE',  ( 1.629563124460619239, -0.2448459300014929063, 2.004692427041386615 ) ) ;
#194373=CARTESIAN_POINT ( 'NONE',  ( 5.139818204295112380, -1.627507941656263002, -1.636155730761083227 ) ) ;
#194374=CARTESIAN_POINT ( 'NONE',  ( 6.285602425426498385, -1.847771260692541162, 0.6596951833430019230 ) ) ;
#194375=EDGE_CURVE ( 'NONE', #68014, #95583, #15845, .T. ) ;
#194376=CARTESIAN_POINT ( 'NONE',  ( 2.114041031776827673, 1.956853317873577414, -0.1391692324632237410 ) ) ;
#194380=CARTESIAN_POINT ( 'NONE',  ( 1.727892286414894674, 0.8051050731917328562, -1.958494560251317740 ) ) ;
#194383=CARTESIAN_POINT ( 'NONE',  ( 1.271164299617353333, 1.095269041189731452, 1.479763895647051131 ) ) ;
#194386=CARTESIAN_POINT ( 'NONE',  ( 3.023802379225454473, -0.4096935937694180518, 2.080477853870852378 ) ) ;
#194390=CARTESIAN_POINT ( 'NONE',  ( 3.233719155016498092, -1.381502681103630392, -1.529336839808728365 ) ) ;
#194392=CARTESIAN_POINT ( 'NONE',  ( 0.4504185290156897947, -1.555054577268409899, -0.9855837367087336709 ) ) ;
#194394=CARTESIAN_POINT ( 'NONE',  ( 0.07775346131144458828, -0.005211914751935413023, -2.288974916015192651 ) ) ;
#194397=CARTESIAN_POINT ( 'NONE',  ( 2.583610768588519235, 2.069371435550710459, -0.9147937799905188072 ) ) ;
#194400=CARTESIAN_POINT ( 'NONE',  ( 2.197251250676080847, 1.655042475022786785, -0.7371099161151051238 ) ) ;
#194401=CARTESIAN_POINT ( 'NONE',  ( 2.184663254350202255, 1.535933850207292783, -1.144682215256398239 ) ) ;
#194402=CARTESIAN_POINT ( 'NONE',  ( 2.682155120989743402, -1.190029146579720587, -1.693995171316540427 ) ) ;
#194404=CARTESIAN_POINT ( 'NONE',  ( 2.166812389411576056, -1.801713905456410858, -0.8007201275355458892 ) ) ;
#194405=CARTESIAN_POINT ( 'NONE',  ( 6.463506663115213158, 0.3265968279197262181, -1.898468693527188389 ) ) ;
#194406=CARTESIAN_POINT ( 'NONE',  ( 2.571000202304725590, 0.09389976206976291540, -1.868427151830873267 ) ) ;
#194407=CARTESIAN_POINT ( 'NONE',  ( 0.9269276575891262082, 1.370462819911044239, -1.856556161720348763 ) ) ;
#194409=CARTESIAN_POINT ( 'NONE',  ( 2.277597300015369086, -1.806044765408962194, 0.4486390909646633118 ) ) ;
#194411=CARTESIAN_POINT ( 'NONE',  ( 5.934046607644717142, 1.225649100846971651, 1.658920436798372311 ) ) ;
#194415=CARTESIAN_POINT ( 'NONE',  ( 6.633818197422741925, -1.372689285068533271, -1.597217228543364564 ) ) ;
#194417=CARTESIAN_POINT ( 'NONE',  ( 5.870447946289020003, -1.376328297836002079, 1.666777564274177559 ) ) ;
#194418=CARTESIAN_POINT ( 'NONE',  ( 6.252604593904901975, 1.998004417694958512, 0.2941112629052196614 ) ) ;
#194422=ADVANCED_FACE ( 'NONE', ( #44430 ), #163050, .T. ) ;
#194424=CARTESIAN_POINT ( 'NONE',  ( 6.825078400183572036, 4.699117039843025090, 2.418333817060664526 ) ) ;
#194427=CARTESIAN_POINT ( 'NONE',  ( 4.188685576152741064, 1.555700494002542067, -1.282988152656767911 ) ) ;
#194432=CARTESIAN_POINT ( 'NONE',  ( 6.192270064542984898, -2.150811787302907785, -0.2168040374768212541 ) ) ;
#194437=CARTESIAN_POINT ( 'NONE',  ( 0.08730790862205867198, -0.5103928513382477439, 1.846301284274171728 ) ) ;
#194439=CARTESIAN_POINT ( 'NONE',  ( 6.639320575229294086, 7.051910277135648997, 2.801414343313723965 ) ) ;
#194440=CARTESIAN_POINT ( 'NONE',  ( 1.752176261082264208, 0.5389683859425442591, 1.638572262730133566 ) ) ;
#194444=CARTESIAN_POINT ( 'NONE',  ( 6.169203917683822702, 0.1378038699498609632, -1.865550841118966297 ) ) ;
#194445=CARTESIAN_POINT ( 'NONE',  ( 0.6100213217023927603, -0.7224815109628316412, 1.879156614266486391 ) ) ;
#194447=CARTESIAN_POINT ( 'NONE',  ( 3.100804818134130780, -0.6391501652806098610, -2.112195066926085829 ) ) ;
#194448=CARTESIAN_POINT ( 'NONE',  ( 5.911019566678890058, -1.716411647115582140, 1.329421173595428884 ) ) ;
#194451=CARTESIAN_POINT ( 'NONE',  ( 2.948016456289838771, -1.425740979638410399, -1.569777838261996017 ) ) ;
#194452=CARTESIAN_POINT ( 'NONE',  ( 2.548454031204652637, -1.388473193742698619, 1.462459214312331168 ) ) ;
#194453=CARTESIAN_POINT ( 'NONE',  ( 2.759786284469767814, 0.6482482438519759915, -1.691825979898635035 ) ) ;
#194457=CARTESIAN_POINT ( 'NONE',  ( 0.8658264364783776479, 0.9185255527898968930, 1.629538061279064642 ) ) ;
#194462=CARTESIAN_POINT ( 'NONE',  ( 1.042033841529757421, 0.7795281806207611242, 1.750150644309953041 ) ) ;
#194463=AXIS2_PLACEMENT_3D ( 'NONE', #16494, #130353, #179035 ) ;
#194469=CARTESIAN_POINT ( 'NONE',  ( 4.891577088959510711, 1.599438101461609918, 1.454397306527709155 ) ) ;
#194472=CARTESIAN_POINT ( 'NONE',  ( 3.164422831683691761, 2.120778211551369807, -0.003951117757632071313 ) ) ;
#194475=CARTESIAN_POINT ( 'NONE',  ( 4.692626201678701925, -0.4289087433139714411, -1.923991814828669433 ) ) ;
#194476=CARTESIAN_POINT ( 'NONE',  ( 5.396708386617175890, -1.867154475869851504, -0.4128305108781898936 ) ) ;
#194479=CARTESIAN_POINT ( 'NONE',  ( 0.5903903138861701372, 1.065687334306382184, -1.774900233272216798 ) ) ;
#194480=CARTESIAN_POINT ( 'NONE',  ( 2.747912338643729413, 0.6545661140590716132, 1.828431812057261352 ) ) ;
#194484=CARTESIAN_POINT ( 'NONE',  ( 2.466838723508807174, 0.1015857406408589014, -2.088290385120465498 ) ) ;
#194487=CARTESIAN_POINT ( 'NONE',  ( 0.4690326002820300877, -1.529415377529659503, -0.9703845247886667691 ) ) ;
#194490=CARTESIAN_POINT ( 'NONE',  ( 4.969440760808212509, 0.2186952961555181096, -2.196011921426939129 ) ) ;
#194491=CARTESIAN_POINT ( 'NONE',  ( 3.540233119088306513, 0.9941544567689840628, -1.970234943098593039 ) ) ;
#194494=CARTESIAN_POINT ( 'NONE',  ( 1.963391044528959295, -1.536740334223782867, -1.137898036029337812 ) ) ;
#194496=CARTESIAN_POINT ( 'NONE',  ( 4.246580143467587831, -2.047389768388275577, -0.3068500204662719666 ) ) ;
#194498=CARTESIAN_POINT ( 'NONE',  ( 2.676834871759771417, -2.068302492614528365, -0.6285112194897370941 ) ) ;
#194499=CARTESIAN_POINT ( 'NONE',  ( 4.318054327947466575, 1.347776305887092185, -1.728067674571641898 ) ) ;
#194505=CARTESIAN_POINT ( 'NONE',  ( 0.4576579978108759050, -1.899619568183811058, -0.6767110947205197125 ) ) ;
#194507=CARTESIAN_POINT ( 'NONE',  ( 5.225469540725330653, 0.2083811790645866135, -2.059773418507819365 ) ) ;
#194508=CARTESIAN_POINT ( 'NONE',  ( 3.439987180796261423, 0.8656686944604700118, -1.721121497068250017 ) ) ;
#194509=CARTESIAN_POINT ( 'NONE',  ( 5.888306048034124274, -0.7624388358357903073, -1.975341773770035614 ) ) ;
#194512=CARTESIAN_POINT ( 'NONE',  ( 3.766418665963155998, -0.7939890815925625400, -1.802475468321093732 ) ) ;
#194513=CARTESIAN_POINT ( 'NONE',  ( 6.193372188798685229, -0.7780443601670664622, 2.156323934359334338 ) ) ;
#194514=CARTESIAN_POINT ( 'NONE',  ( 4.371595934376539816, 1.770262903079304451, -0.4459408992859363319 ) ) ;
#194520=CARTESIAN_POINT ( 'NONE',  ( 1.135996871135702024, 0.3593859243370273182, 1.805655672011026391 ) ) ;
#194521=CARTESIAN_POINT ( 'NONE',  ( 5.185796262198086204, 1.939088309008336397, -0.5409127675100529054 ) ) ;
#194522=CARTESIAN_POINT ( 'NONE',  ( 0.4042330683431404892, 0.3962127685512468744, 2.263842283499896801 ) ) ;
#194523=CARTESIAN_POINT ( 'NONE',  ( 5.664887785843471413, 1.487927489739075959, -1.278645765186999128 ) ) ;
#194529=CARTESIAN_POINT ( 'NONE',  ( 1.329752858235648150, 1.027315703197308361, -1.820849364048042318 ) ) ;
#194530=CARTESIAN_POINT ( 'NONE',  ( 6.385617153790816403, 1.223975321695195184, 1.278628327690333411 ) ) ;
#194533=CARTESIAN_POINT ( 'NONE',  ( 0.7490575545651646516, 1.738588327661923394, -0.08332016361957059192 ) ) ;
#194537=CARTESIAN_POINT ( 'NONE',  ( 2.015808680039221201, -0.8114285025175859145, -1.522100016238505216 ) ) ;
#194538=CARTESIAN_POINT ( 'NONE',  ( 1.277182604683280598, 2.023070758711601691, -0.8431670391453591762 ) ) ;
#194539=CARTESIAN_POINT ( 'NONE',  ( 4.530015419921377351, -1.356323209173672106, -1.740806116466916409 ) ) ;
#194542=CARTESIAN_POINT ( 'NONE',  ( 0.8487579731258857452, -2.154475699732544491, -0.2676485622446558299 ) ) ;
#194543=CARTESIAN_POINT ( 'NONE',  ( 0.1526014871912773629, -1.468541917219987836, 1.084465738218153064 ) ) ;
#194544=CARTESIAN_POINT ( 'NONE',  ( 3.872345094350841510, -2.094861191690357227, -0.3068023397686749920 ) ) ;
#194546=CARTESIAN_POINT ( 'NONE',  ( 6.539320575229254473, 0.5926322452488984593, 1.950287522085321301 ) ) ;
#194548=CARTESIAN_POINT ( 'NONE',  ( 4.001757606804694056, -2.286216240038071668, 0.1689928914557006778 ) ) ;
#194553=CARTESIAN_POINT ( 'NONE',  ( 6.147183147440572704, 0.2149688563512392736, 2.210895739474004529 ) ) ;
#194559=CARTESIAN_POINT ( 'NONE',  ( 3.639296212489909532, 0.7283784247123014088, 1.880435045658496618 ) ) ;
#194561=CARTESIAN_POINT ( 'NONE',  ( 2.395447240195498484, -1.844268472375994339, 0.9235843863054800096 ) ) ;
#194566=CARTESIAN_POINT ( 'NONE',  ( 5.244143516318892750, 0.6338322011035132375, 2.097776330851252258 ) ) ;
#194567=CARTESIAN_POINT ( 'NONE',  ( 2.426407915648312930, -1.496052118593782065, -1.352154011671408362 ) ) ;
#194568=CARTESIAN_POINT ( 'NONE',  ( 2.612652284633736777, -0.1782932461553646819, 1.832575692395449485 ) ) ;
#194572=CARTESIAN_POINT ( 'NONE',  ( 5.192344348049102720, -1.811977082810274808, -0.2219828972063255801 ) ) ;
#194573=CARTESIAN_POINT ( 'NONE',  ( 6.574846728087075931, -0.8593996854794653251, 1.822268861383633531 ) ) ;
#194575=CARTESIAN_POINT ( 'NONE',  ( 5.752851848433533810, -1.787673638215280913, 1.386716842396797489 ) ) ;
#194577=CARTESIAN_POINT ( 'NONE',  ( 0.5222713366250474332, -1.128438999127111098, -1.778050165696586360 ) ) ;
#194587=CARTESIAN_POINT ( 'NONE',  ( 1.371502371489873751, -1.821557607348308405, -1.085495857948336251 ) ) ;
#194588=CARTESIAN_POINT ( 'NONE',  ( 3.164521688127000854, 2.221583673635919354, -0.003682443279265367429 ) ) ;
#194593=CARTESIAN_POINT ( 'NONE',  ( 3.578520225191741844, 1.246510459297203610, -1.514941731618473009 ) ) ;
#194599=CARTESIAN_POINT ( 'NONE',  ( 2.531617689938488791, -0.2033970545941807817, 2.110794199748195599 ) ) ;
#194601=CARTESIAN_POINT ( 'NONE',  ( 4.698204674003193304, -2.161138953124014161, -0.05634304724232848394 ) ) ;
#194602=CARTESIAN_POINT ( 'NONE',  ( 3.140019216317342376, 0.4501627324021879040, 1.785233193441162713 ) ) ;
#194605=CARTESIAN_POINT ( 'NONE',  ( 6.035049474595155949, -1.265358352104806183, -1.195092038424966363 ) ) ;
#194606=CARTESIAN_POINT ( 'NONE',  ( 6.727182134110199385, 3.711531441867378600, 2.225637065106730095 ) ) ;
#194609=CARTESIAN_POINT ( 'NONE',  ( 2.958072429731006370, 2.151414462573512765, -0.2105227563667099733 ) ) ;
#194611=CARTESIAN_POINT ( 'NONE',  ( 4.780624950969222020, -1.977747464269607347, 0.3905396900540994420 ) ) ;
#194613=CARTESIAN_POINT ( 'NONE',  ( 2.694378501574711926, -2.155843008138720762, -0.1600555415394027403 ) ) ;
#194615=CARTESIAN_POINT ( 'NONE',  ( 3.005103179519866607, 1.663439489741199928, 1.057676205593648167 ) ) ;
#194617=CARTESIAN_POINT ( 'NONE',  ( 4.440924170176640651, -1.503556815104054811, -1.229221392163130755 ) ) ;
#194626=CARTESIAN_POINT ( 'NONE',  ( 0.7982362974770088604, -0.7925503509537080715, 2.059710425106767939 ) ) ;
#194630=CARTESIAN_POINT ( 'NONE',  ( 5.875826477234550538, -1.914729252524836056, 0.4262945716600323731 ) ) ;
#194634=CARTESIAN_POINT ( 'NONE',  ( 0.07499057489264349119, 0.002531239327734773146, -1.955573237620360505 ) ) ;
#194635=CARTESIAN_POINT ( 'NONE',  ( 4.540845788227630742, -1.424921066559198257, -1.165926479108070346 ) ) ;
#194636=VERTEX_POINT ( 'NONE', #15759 ) ;
#194644=CARTESIAN_POINT ( 'NONE',  ( 6.591097270071800907, 1.795350502275098403, -1.011519373207786288 ) ) ;
#194646=CARTESIAN_POINT ( 'NONE',  ( 1.521681963465530529, 1.834278628056866367, -0.3135228456460791846 ) ) ;
#194647=CARTESIAN_POINT ( 'NONE',  ( 3.878315922200573862, -0.1843894689829879696, -1.832007427040844183 ) ) ;
#194652=CARTESIAN_POINT ( 'NONE',  ( 3.492985898914053866, -0.4302566696539159574, -2.164365734511737305 ) ) ;
#194653=CARTESIAN_POINT ( 'NONE',  ( 5.729810862507367375, -1.428767958649424408, -1.754208347296302373 ) ) ;
#194655=CARTESIAN_POINT ( 'NONE',  ( 5.449399174529797385, -1.634242350402253852, 0.7820841365046418137 ) ) ;
#194656=CARTESIAN_POINT ( 'NONE',  ( 5.928903634556547786, -1.614502157299831042, 1.030912532684091110 ) ) ;
#194658=CARTESIAN_POINT ( 'NONE',  ( 5.963714631206167738, 1.842656449598079060, -0.3214700631931910468 ) ) ;
#194660=CARTESIAN_POINT ( 'NONE',  ( 6.157089704101026406, -1.520188931036812185, -0.9060637366671944193 ) ) ;
#194661=CARTESIAN_POINT ( 'NONE',  ( 0.9543149826918421175, -1.275552737861269437, 1.561884623745241951 ) ) ;
#194663=CARTESIAN_POINT ( 'NONE',  ( 3.141344390434357869, -1.857286833677756599, 0.9929794709265575836 ) ) ;
#194668=CARTESIAN_POINT ( 'NONE',  ( 2.619404093423041591, 1.708565301817746018, 1.076861402434741821 ) ) ;
#194672=CARTESIAN_POINT ( 'NONE',  ( 3.022914066069124051, 2.034213141994867247, 0.7313807043239917149 ) ) ;
#194677=CARTESIAN_POINT ( 'NONE',  ( 0.9948528382496389932, 2.139055259286365640, 0.3712904390174593949 ) ) ;
#194683=CARTESIAN_POINT ( 'NONE',  ( 1.962683346935737205, -2.005255389829229351, -0.8846387633431598285 ) ) ;
#194685=CARTESIAN_POINT ( 'NONE',  ( 2.975713975707586556, 2.148818855599075928, -0.7084362298409478953 ) ) ;
#194687=CARTESIAN_POINT ( 'NONE',  ( 4.540250091716044878, 0.7762272601403925609, 1.861345588084816871 ) ) ;
#194694=CARTESIAN_POINT ( 'NONE',  ( 4.288192095134175652, -1.750260269857591755, -0.2610086191854649740 ) ) ;
#194696=CARTESIAN_POINT ( 'NONE',  ( 6.335036379411270957, 0.2100110484798515254, 2.196758413611602290 ) ) ;
#194699=CARTESIAN_POINT ( 'NONE',  ( 5.923453886551513392, -1.462456689723025782, -1.388475849216065372 ) ) ;
#194700=ORIENTED_EDGE ( 'NONE', *, *, #118594, .F. ) ;
#194702=CARTESIAN_POINT ( 'NONE',  ( 4.135518821028766112, -1.289757458839156934, -1.355179912160727085 ) ) ;
#194703=CARTESIAN_POINT ( 'NONE',  ( 3.608316154870555792, 2.070434559819031684, 0.004826415812286819103 ) ) ;
#194709=CARTESIAN_POINT ( 'NONE',  ( 5.875883356151953230, 1.283970044810868849, 1.738936680771227206 ) ) ;
#194711=CARTESIAN_POINT ( 'NONE',  ( 2.400770673373255448, 0.4268909467371252431, 1.914702609522442867 ) ) ;
#194712=CARTESIAN_POINT ( 'NONE',  ( 0.4564073884281876770, 1.492024165150519055, 1.356095248386236074 ) ) ;
#194716=CARTESIAN_POINT ( 'NONE',  ( 0.5439545674776785633, 1.865077268347898665, 0.1441030193207945287 ) ) ;
#194718=CARTESIAN_POINT ( 'NONE',  ( 3.480730050573742851, -1.348849006198136635, 1.494714382889005488 ) ) ;
#194720=CARTESIAN_POINT ( 'NONE',  ( 1.740021635027885649, 2.111287947816307575, -0.1595968877764943616 ) ) ;
#194722=CARTESIAN_POINT ( 'NONE',  ( 3.965334771736851671, 1.774175476309115984, 1.066894043611272824 ) ) ;
#194724=CARTESIAN_POINT ( 'NONE',  ( 5.314434061427068201, 1.931386623266003078, 0.8008058956679960927 ) ) ;
#194726=CARTESIAN_POINT ( 'NONE',  ( 3.715676801689533626, -1.798647723735953496, 0.3114480851732701061 ) ) ;
#194732=CARTESIAN_POINT ( 'NONE',  ( 6.827182134110222123, -0.006956174471953178659, 2.188967759425272330 ) ) ;
#194734=CARTESIAN_POINT ( 'NONE',  ( 5.092401474535850348, -1.059014397921493433, 1.592059587274458510 ) ) ;
#194744=CARTESIAN_POINT ( 'NONE',  ( 4.323419078940895943, -1.790677508454678657, 0.5408235849187342792 ) ) ;
#194745=CARTESIAN_POINT ( 'NONE',  ( 0.07700591528354487625, 0.7269319812311864082, -1.993543990282041767 ) ) ;
#194749=AXIS2_PLACEMENT_3D ( 'NONE', #179096, #130419, #81582 ) ;
#194753=CARTESIAN_POINT ( 'NONE',  ( 0.8659821450925162534, -1.960479642884611629, 0.1873741036552133976 ) ) ;
#194754=CARTESIAN_POINT ( 'NONE',  ( 2.900017720922347220, -0.9963201819552582883, -1.753021271517739343 ) ) ;
#194758=CARTESIAN_POINT ( 'NONE',  ( 3.767680093253112705, 1.217039798425190167, 1.822233383357040104 ) ) ;
#194761=CARTESIAN_POINT ( 'NONE',  ( 6.825078400183590688, 2.971555572656236599, 2.408956600524428282 ) ) ;
#194769=CARTESIAN_POINT ( 'NONE',  ( 4.669393045487420402, 1.064170941109745305, 1.502380130741477693 ) ) ;
#194770=CARTESIAN_POINT ( 'NONE',  ( 1.348292448571129842, 0.9904378492491233699, -1.752504823097464692 ) ) ;
#194771=CARTESIAN_POINT ( 'NONE',  ( 3.761312542938214598, -2.295521343867617414, -0.1171695491895396041 ) ) ;
#194772=CARTESIAN_POINT ( 'NONE',  ( -0.02900071798685524560, 0.6937575422599016051, -2.255700163050919471 ) ) ;
#194773=CARTESIAN_POINT ( 'NONE',  ( 1.779899486625190264, -1.028416011161866983, -1.550745576289275895 ) ) ;
#194776=CARTESIAN_POINT ( 'NONE',  ( 5.115449499555525747, 1.566912803841558732, 1.096118974231160781 ) ) ;
#194779=CARTESIAN_POINT ( 'NONE',  ( 5.214434122969894503, 1.932256357821033887, 0.7989942847940935122 ) ) ;
#194780=CARTESIAN_POINT ( 'NONE',  ( 2.975316878787794828, 1.776827963633962559, -0.5852370025475408521 ) ) ;
#194782=CARTESIAN_POINT ( 'NONE',  ( 6.304252605626877504, 1.359535501544101077, -1.241908024382516240 ) ) ;
#194786=CARTESIAN_POINT ( 'NONE',  ( 5.250533987919646428, 0.5060912822462645400, 1.648968847961843620 ) ) ;
#194791=CARTESIAN_POINT ( 'NONE',  ( 5.190355475387732120, 1.122157983508360157, -1.858477351540340328 ) ) ;
#194792=CARTESIAN_POINT ( 'NONE',  ( 2.789462663364688844, 1.291185895303394116, 1.290987730777813702 ) ) ;
#194793=CARTESIAN_POINT ( 'NONE',  ( 1.516376426791886445, 0.7900930292849810410, 1.795789229542772647 ) ) ;
#194794=CARTESIAN_POINT ( 'NONE',  ( 6.262923198102183342, -0.1061305018058098515, -2.114825283700927372 ) ) ;
#194795=CARTESIAN_POINT ( 'NONE',  ( 6.603114554492313104, -0.5110835225830052675, 2.243201349117603716 ) ) ;
#194800=CARTESIAN_POINT ( 'NONE',  ( 2.526173596586390957, -2.097057114080549844, 0.3136139059176298871 ) ) ;
#194804=CARTESIAN_POINT ( 'NONE',  ( 0.7958623839904412911, -1.461433461687311253, -1.466603172318406090 ) ) ;
#194805=CARTESIAN_POINT ( 'NONE',  ( 6.883263157960366918, 2.950764357809147143, 2.606098932787728639 ) ) ;
#194807=CARTESIAN_POINT ( 'NONE',  ( 2.438390712420679396, -1.281362850324974989, -1.814285216940268342 ) ) ;
#194809=CARTESIAN_POINT ( 'NONE',  ( 0.8097366424872083357, 1.363176973609769416, -1.850781266144943205 ) ) ;
#194811=CARTESIAN_POINT ( 'NONE',  ( 5.541865367331380909, 1.381078337155069224, 1.532129260548445782 ) ) ;
#194815=CARTESIAN_POINT ( 'NONE',  ( 0.2333540202161349941, 2.877056899079268870, -2.534299598574590640 ) ) ;
#194816=CARTESIAN_POINT ( 'NONE',  ( 5.161589042655139181, 0.9124512986629171873, 1.599201395118980740 ) ) ;
#194819=CARTESIAN_POINT ( 'NONE',  ( 1.817014216480263622, -0.2154200610367338342, 1.711195096342375210 ) ) ;
#194820=CARTESIAN_POINT ( 'NONE',  ( 1.534389036647098692, 0.6371565916030232923, 1.913260934284975345 ) ) ;
#194822=CARTESIAN_POINT ( 'NONE',  ( 2.196875584952286964, -0.6017768564574823564, -2.180865832541518667 ) ) ;
#194823=CARTESIAN_POINT ( 'NONE',  ( 3.967482597722607363, 0.2578578757282763978, -2.090148584218749939 ) ) ;
#194825=CARTESIAN_POINT ( 'NONE',  ( 2.512676673363742452, 1.578732364194649573, 0.7999210992828114097 ) ) ;
#194829=CARTESIAN_POINT ( 'NONE',  ( 5.179329019713509119, 1.537796090523161796, 1.700180828611449035 ) ) ;
#194831=CARTESIAN_POINT ( 'NONE',  ( 4.118977087773854961, -1.761250088754966692, 0.5364436722887636622 ) ) ;
#194835=CARTESIAN_POINT ( 'NONE',  ( 4.875033280109006384, 2.045454206080063120, -0.7869404205859964474 ) ) ;
#194841=CARTESIAN_POINT ( 'NONE',  ( 2.701685709380332145, -0.6039436678997743835, 1.829457556829715115 ) ) ;
#194844=CARTESIAN_POINT ( 'NONE',  ( 5.818629517237746462, -0.7649446623404360102, -1.977987144599784086 ) ) ;
#194851=CARTESIAN_POINT ( 'NONE',  ( 6.163598723784100564, 0.9525508894225949152, 1.575581956637741365 ) ) ;
#194855=CARTESIAN_POINT ( 'NONE',  ( 1.997219015684068344, -1.740079325084613604, 0.04332556902747128347 ) ) ;
#194856=CARTESIAN_POINT ( 'NONE',  ( 0.3792546940144908008, -0.1001052471676349837, 1.959448305358338693 ) ) ;
#194859=CARTESIAN_POINT ( 'NONE',  ( 5.893488898593548520, 1.633865717575968324, 1.415524914074948404 ) ) ;
#194862=CARTESIAN_POINT ( 'NONE',  ( 5.278265135069068137, -1.204163492603943064, 1.795060720813673738 ) ) ;
#194866=CARTESIAN_POINT ( 'NONE',  ( 0.6142526126209290060, 1.294576594435635108, -1.350420462534522859 ) ) ;
#194867=CARTESIAN_POINT ( 'NONE',  ( 6.046190555029876457, 1.600718489819895174, -0.6667736897630163195 ) ) ;
#194869=CARTESIAN_POINT ( 'NONE',  ( 2.753686713869853531, 2.180749500395392282, -0.2175628297749406803 ) ) ;
#194870=CARTESIAN_POINT ( 'NONE',  ( 3.048224541365350593, 0.8318171267079670361, -2.152611968481593419 ) ) ;
#194871=CARTESIAN_POINT ( 'NONE',  ( 5.554002131806472065, 2.058623415865985518, -0.09669752385456369115 ) ) ;
#194872=CARTESIAN_POINT ( 'NONE',  ( 1.236160255307724665, 0.3784122030587311336, 1.904561997804487428 ) ) ;
#194876=CARTESIAN_POINT ( 'NONE',  ( 3.955424862866574021, -1.843446357660895041, 1.048082435718917571 ) ) ;
#194877=CARTESIAN_POINT ( 'NONE',  ( 2.426407915648312930, -1.496052118593782065, -1.352154011671408362 ) ) ;
#194879=CARTESIAN_POINT ( 'NONE',  ( 4.032405518703926717, 1.182977813604596973, -1.862726815517960821 ) ) ;
#194885=CARTESIAN_POINT ( 'NONE',  ( 6.825078400183545391, 2.405270491081310968, 2.624368679222242484 ) ) ;
#194888=CARTESIAN_POINT ( 'NONE',  ( 4.047771301309529335, 0.6961604498142616171, -1.939876652229477028 ) ) ;
#194893=CARTESIAN_POINT ( 'NONE',  ( 2.895180478094826704, -0.1506588039767979559, -2.014126839200135688 ) ) ;
#194898=CARTESIAN_POINT ( 'NONE',  ( 2.799741500914772807, -0.6479443615096942555, 1.956441213939211554 ) ) ;
#194899=CARTESIAN_POINT ( 'NONE',  ( 2.795546247670523954, 1.458556481301529706, -1.392545902517070111 ) ) ;
#194904=CARTESIAN_POINT ( 'NONE',  ( 2.794295885581669747, -1.882186412485300719, 0.7230279869864174591 ) ) ;
#194905=CARTESIAN_POINT ( 'NONE',  ( 1.710644026344819046, -0.2265308078298749472, 1.827073587482845207 ) ) ;
#194906=CARTESIAN_POINT ( 'NONE',  ( 0.2414294658986924358, 0.4011018576653562207, 2.272434410966933438 ) ) ;
#194908=CARTESIAN_POINT ( 'NONE',  ( 2.126461914815626297, 1.246462439515462650, -1.765816729463750123 ) ) ;
#194910=CARTESIAN_POINT ( 'NONE',  ( 4.927025384238821637, -1.814351377589568548, 1.091279385997992568 ) ) ;
#194913=CARTESIAN_POINT ( 'NONE',  ( 0.7076149179639171782, -1.862046558926268913, 0.1791945732521060819 ) ) ;
#194915=CARTESIAN_POINT ( 'NONE',  ( 4.873880070992254510, 1.134317645522317175, 1.612277344948910285 ) ) ;
#194919=CARTESIAN_POINT ( 'NONE',  ( 6.147117739887063337, -1.780134362386740721, 1.125150951816885403 ) ) ;
#194921=CARTESIAN_POINT ( 'NONE',  ( 6.637176860265922684, -0.09746846054551477900, -2.068182370504913159 ) ) ;
#194924=CARTESIAN_POINT ( 'NONE',  ( 6.875078400183575411, 7.629137130509070275, 2.455651831298297338 ) ) ;
#194925=CARTESIAN_POINT ( 'NONE',  ( 4.750830034454851969, -1.584041870840187327, 1.173487520707878096 ) ) ;
#194926=CARTESIAN_POINT ( 'NONE',  ( 6.099869210120771434, 1.395876734396967356, 1.460039163664628159 ) ) ;
#194928=CARTESIAN_POINT ( 'NONE',  ( 4.196143101376831552, -0.8852276965729001246, 2.131346054819768909 ) ) ;
#194929=CARTESIAN_POINT ( 'NONE',  ( 1.639586372526161684, 1.907294469559306815, -0.7855861486642725655 ) ) ;
#194937=CARTESIAN_POINT ( 'NONE',  ( 4.123599099448671090, 0.2696675481538573504, -2.154320840723603414 ) ) ;
#194940=CARTESIAN_POINT ( 'NONE',  ( 4.142028884782995135, 0.4951553702221401232, 1.773339192993342639 ) ) ;
#194943=CARTESIAN_POINT ( 'NONE',  ( 6.620655732516656400, 2.994310854299454316, 2.180639477081049993 ) ) ;
#194944=CARTESIAN_POINT ( 'NONE',  ( 5.741772062182810998, 2.188963553168365994, 0.1087695542012837302 ) ) ;
#194946=CARTESIAN_POINT ( 'NONE',  ( 6.121994746204825866, -1.250886037347900270, -1.885104629530814702 ) ) ;
#194952=CARTESIAN_POINT ( 'NONE',  ( 0.8304726968981954727, 0.1242609525908405232, 1.765545458023538572 ) ) ;
#194953=CARTESIAN_POINT ( 'NONE',  ( 4.740889518710099004, 1.927123460305087965, 0.5820593317791241672 ) ) ;
#194955=CARTESIAN_POINT ( 'NONE',  ( 4.366313571243555458, 0.9904663015308888818, 1.858490915321360237 ) ) ;
#194956=CARTESIAN_POINT ( 'NONE',  ( 2.302218516519896507, 1.249579790052034456, -1.452036884154449314 ) ) ;
#194958=CARTESIAN_POINT ( 'NONE',  ( 3.385164793666879834, 0.04568167736355076974, 1.969186301724828336 ) ) ;
#194959=CARTESIAN_POINT ( 'NONE',  ( 5.150651408520660723, 1.990593866887302221, 0.3411176234145337216 ) ) ;
#194960=CARTESIAN_POINT ( 'NONE',  ( 2.008475284031425723, 1.387998011844304491, -1.254312187223500796 ) ) ;
#194961=CARTESIAN_POINT ( 'NONE',  ( 1.785527960060459440, -1.848404783191982315, 0.6579185095809261252 ) ) ;
#194962=CARTESIAN_POINT ( 'NONE',  ( 4.424228590228207914, 1.058368455644955963, -1.361911123238012111 ) ) ;
#194963=CARTESIAN_POINT ( 'NONE',  ( 0.8789968191965717992, -1.730013457311157188, -0.8152767527440167861 ) ) ;
#194965=CARTESIAN_POINT ( 'NONE',  ( 1.454063653991678473, 0.6380318336138122159, -2.112638918738508398 ) ) ;
#194973=CARTESIAN_POINT ( 'NONE',  ( 0.3794556558127279988, -0.1030994254981997954, 2.067933115924729837 ) ) ;
#194978=CARTESIAN_POINT ( 'NONE',  ( 5.426475896148662770, -0.9536019125786737716, -1.894055658958586852 ) ) ;
#194983=CARTESIAN_POINT ( 'NONE',  ( 6.092239754786219486, 0.9682357284593717806, -1.706234036142616928 ) ) ;
#194985=CARTESIAN_POINT ( 'NONE',  ( 4.147814418418220406, -0.1948115906579734602, -2.006652602119996853 ) ) ;
#194986=CARTESIAN_POINT ( 'NONE',  ( 3.256958599878871485, 0.04175330623504669436, -1.915424027289241993 ) ) ;
#194988=CARTESIAN_POINT ( 'NONE',  ( 1.962683346935737205, -2.005255389829229351, -0.8846387633431598285 ) ) ;
#194991=CARTESIAN_POINT ( 'NONE',  ( 5.361592829351686795, -1.589796019859390563, -1.235070861824426824 ) ) ;
#194994=CARTESIAN_POINT ( 'NONE',  ( 6.081681791882147969, -0.7128978460711818954, 1.993742607474026984 ) ) ;
#194996=CARTESIAN_POINT ( 'NONE',  ( 2.999644136165266595, -2.088248420355208523, 0.1050208477483879216 ) ) ;
#194998=CARTESIAN_POINT ( 'NONE',  ( 1.482971688208828187, 1.595641881047437538, -0.6553127101004208033 ) ) ;
#195000=CARTESIAN_POINT ( 'NONE',  ( 4.904590598983499028, -2.104870323260544129, -0.2570220051709286579 ) ) ;
#195009=ORIENTED_EDGE ( 'NONE', *, *, #70737, .T. ) ;
#195011=CARTESIAN_POINT ( 'NONE',  ( 2.191808917380858812, 1.115356421127197351, 1.427258924012535735 ) ) ;
#195018=CARTESIAN_POINT ( 'NONE',  ( 2.209342481274043646, 1.400903122447524796, 1.148441741360214152 ) ) ;
#195019=CARTESIAN_POINT ( 'NONE',  ( 6.539320575229256249, 4.699150603835311912, 2.459441311396874941 ) ) ;
#195023=CARTESIAN_POINT ( 'NONE',  ( 4.176097997218494839, -0.9553649929725913648, -1.596950837584124816 ) ) ;
#195024=CARTESIAN_POINT ( 'NONE',  ( 1.493601000189462624, -1.900943851588072997, 0.2360903481228252554 ) ) ;
#195025=CARTESIAN_POINT ( 'NONE',  ( 0.2701547006425785713, -1.196777392914155635, 1.378664180083796875 ) ) ;
#195031=CARTESIAN_POINT ( 'NONE',  ( 4.821133434317745881, -1.757446901322982979, -0.8890814742016742711 ) ) ;
#195034=CARTESIAN_POINT ( 'NONE',  ( 0.05869050280414740001, -1.868530317513932504, -0.9378765995749788198 ) ) ;
#195036=CARTESIAN_POINT ( 'NONE',  ( 5.561526637868618117, 0.3756393653304244129, -1.889249976882242610 ) ) ;
#195038=CARTESIAN_POINT ( 'NONE',  ( 1.711645973048509850, -1.812212506298327197, 0.2199163931802459171 ) ) ;
#195039=CARTESIAN_POINT ( 'NONE',  ( 2.385638622766753425, 2.017150886971270651, -0.8956362484653991318 ) ) ;
#195040=CARTESIAN_POINT ( 'NONE',  ( -0.1405747822309927342, -1.479430311965252542, -1.211566217618691210 ) ) ;
#195043=CARTESIAN_POINT ( 'NONE',  ( 0.9769314595147912117, 1.818477718279483568, 0.7569839642056105378 ) ) ;
#195044=CARTESIAN_POINT ( 'NONE',  ( 1.259210993675137225, 1.913035009642606754, -0.3336937221413670551 ) ) ;
#195045=CARTESIAN_POINT ( 'NONE',  ( 1.071638489536786309, 1.528508772698907059, -1.314793605459969372 ) ) ;
#195047=CARTESIAN_POINT ( 'NONE',  ( 5.752756584690191133, -0.4505887142414471969, -1.805456089952769183 ) ) ;
#195053=CARTESIAN_POINT ( 'NONE',  ( 1.611130907606239004, -0.2639259086049255965, 2.175532687872412829 ) ) ;
#195058=CARTESIAN_POINT ( 'NONE',  ( 1.295219883412350503, 1.381147610352757127, 1.194082977437810333 ) ) ;
#195062=CARTESIAN_POINT ( 'NONE',  ( 6.509000000000053632, 2.033894086284238956, 2.405029747421689290 ) ) ;
#195064=CARTESIAN_POINT ( 'NONE',  ( 0.7856181369204550125, 1.292946451617222436, 1.428335531958953464 ) ) ;
#195065=CARTESIAN_POINT ( 'NONE',  ( 4.170719094083116474, 1.390339895272204362, -1.384257141873693087 ) ) ;
#195069=CARTESIAN_POINT ( 'NONE',  ( 4.616832073239669043, -0.1072513232249286408, 2.189039617437993357 ) ) ;
#195072=CARTESIAN_POINT ( 'NONE',  ( 4.434477146351770926, -1.196200190851111733, 1.689492296227593116 ) ) ;
#195078=CARTESIAN_POINT ( 'NONE',  ( 3.498943719384327355, -2.264459259401516267, 0.3945650996091658591 ) ) ;
#195086=CARTESIAN_POINT ( 'NONE',  ( 3.433474178283620670, 0.8725410082476585671, -1.734956227438133158 ) ) ;
#195089=ADVANCED_FACE ( 'NONE', ( #87167 ), #94088, .F. ) ;
#195090=CARTESIAN_POINT ( 'NONE',  ( 4.834190613173367623, -1.027981871586785889, -1.612434056610718480 ) ) ;
#195092=CARTESIAN_POINT ( 'NONE',  ( -0.01747323780270595983, -0.1290080397739183926, -1.696210917522892325 ) ) ;
#195093=CARTESIAN_POINT ( 'NONE',  ( 4.083220446344194343, 1.622485107653489633, 1.197306254465977826 ) ) ;
#195094=CARTESIAN_POINT ( 'NONE',  ( 5.239047776066017903, 2.296150469294107488, -0.1107920306624484569 ) ) ;
#195096=CARTESIAN_POINT ( 'NONE',  ( 0.7509353727821498348, 0.6442623716619542140, 2.110749664216593047 ) ) ;
#195099=CARTESIAN_POINT ( 'NONE',  ( 0.02354010051478470922, -1.288079656314411459, -1.647238045112088267 ) ) ;
#195100=CARTESIAN_POINT ( 'NONE',  ( 0.2679308956112765872, -1.161373500300251216, 1.335597826242039154 ) ) ;
#195101=CARTESIAN_POINT ( 'NONE',  ( 5.256482491209823138, 1.942542154241846397, -0.5404887192124520068 ) ) ;
#195103=CARTESIAN_POINT ( 'NONE',  ( 3.170184779232795957, -1.365206436085873776, 1.841245074435297502 ) ) ;
#195104=CARTESIAN_POINT ( 'NONE',  ( 1.218268023815568535, -0.04584277261814385940, 1.739893813429808311 ) ) ;
#195106=CARTESIAN_POINT ( 'NONE',  ( 1.387607149621207236, -0.04906231267952190778, 1.733339852973712292 ) ) ;
#195109=CARTESIAN_POINT ( 'NONE',  ( 1.328853926488116510, -1.377647258212051362, 1.678094904287985800 ) ) ;
#195110=CARTESIAN_POINT ( 'NONE',  ( 2.026577684455236561, 0.4465047249504557891, 1.966304233017155845 ) ) ;
#195111=CARTESIAN_POINT ( 'NONE',  ( 5.468750000000003553, 0.7852924748297082091, -1.895863743164194704 ) ) ;
#195113=CARTESIAN_POINT ( 'NONE',  ( 0.3055242992691169501, -0.5169788762636564616, 1.855657374570508278 ) ) ;
#195115=CARTESIAN_POINT ( 'NONE',  ( 3.480930870787651621, -1.489476591903232228, 1.648259452209248854 ) ) ;
#195122=CARTESIAN_POINT ( 'NONE',  ( 5.829613671240826633, 0.8500414093583901209, -1.518663286469445151 ) ) ;
#195123=CARTESIAN_POINT ( 'NONE',  ( 3.578520225191741844, 1.246510459297203610, -1.514941731618473009 ) ) ;
#195127=CARTESIAN_POINT ( 'NONE',  ( 4.850980959722003938, -1.821092479232713446, 1.342276170020906711 ) ) ;
#195128=CARTESIAN_POINT ( 'NONE',  ( 1.627463713854758298, 0.1539993984382737602, -2.057001629134532550 ) ) ;
#195131=CARTESIAN_POINT ( 'NONE',  ( 2.360583983009652442, 0.9673915393220763326, 2.045390427905840358 ) ) ;
#195135=CARTESIAN_POINT ( 'NONE',  ( 3.198369223161025676, -0.5396142385952484855, -1.791042426047453784 ) ) ;
#195136=CARTESIAN_POINT ( 'NONE',  ( 2.039351246016813501, -1.339629256360101106, 1.101148611782216014 ) ) ;
#195137=CARTESIAN_POINT ( 'NONE',  ( 6.233935805145816467, 2.167428969419796125, 0.3234103439683775894 ) ) ;
#195138=CARTESIAN_POINT ( 'NONE',  ( 6.721674876502457430, -2.240710703332372766, 0.5512419492274822641 ) ) ;
#195139=CARTESIAN_POINT ( 'NONE',  ( 3.942369626403975147, 2.151062187213080623, 0.2142938780915065733 ) ) ;
#195140=CARTESIAN_POINT ( 'NONE',  ( 4.699130951095971120, -0.5162677480817599029, 1.872006234571305772 ) ) ;
#195143=CARTESIAN_POINT ( 'NONE',  ( 6.802024559211160337, -1.870114703409443857, 0.04643648283486621897 ) ) ;
#195150=CARTESIAN_POINT ( 'NONE',  ( 5.748672702226536479, 1.986101125435947301, -0.3474646712962395911 ) ) ;
#195154=CARTESIAN_POINT ( 'NONE',  ( 3.773894676421325478, 1.015518775504126614, 1.516979517045339509 ) ) ;
#195161=CARTESIAN_POINT ( 'NONE',  ( 6.551426717330563143, -1.803173079755305608, 0.9099084737219197416 ) ) ;
#195162=CARTESIAN_POINT ( 'NONE',  ( 1.471502243059899850, -1.820439715282649251, -1.087164402369590555 ) ) ;
#195165=CARTESIAN_POINT ( 'NONE',  ( 1.656853885927531689, 1.525116498273047405, -1.066097284832379755 ) ) ;
#195167=CARTESIAN_POINT ( 'NONE',  ( 6.086805585656668960, -0.2997611930264115765, -2.038837977671539736 ) ) ;
#195168=CARTESIAN_POINT ( 'NONE',  ( 6.469375277500488686, -1.978045142091336306, -0.3906011616893814709 ) ) ;
#195172=CARTESIAN_POINT ( 'NONE',  ( 3.949673224339702138, 0.6133576713117370183, -1.719707012317383432 ) ) ;
#195177=CARTESIAN_POINT ( 'NONE',  ( 6.573592277014387086, 1.495820547097842068, -1.351949839681469090 ) ) ;
#195178=CARTESIAN_POINT ( 'NONE',  ( 5.279192629422701621, 1.239228542960477242, 1.361826556748657602 ) ) ;
#195180=CARTESIAN_POINT ( 'NONE',  ( 3.194261032343487461, -0.9352514745577229505, 2.109854200106716426 ) ) ;
#195182=CARTESIAN_POINT ( 'NONE',  ( 5.483715611629243369, 1.447241891022777560, 1.605803905980404123 ) ) ;
#195184=CARTESIAN_POINT ( 'NONE',  ( 0.9955321287432462585, -1.942234967994656669, 0.001507142460104027087 ) ) ;
#195189=CARTESIAN_POINT ( 'NONE',  ( 4.944154083221365070, 1.865701114312174225, 0.1370711555178441010 ) ) ;
#195190=CARTESIAN_POINT ( 'NONE',  ( 0.8789968191965717992, -1.730013457311157188, -0.8152767527440167861 ) ) ;
#195193=CARTESIAN_POINT ( 'NONE',  ( 4.143358556170802842, -1.920740624720223666, 1.086653567583625746 ) ) ;
#195198=CARTESIAN_POINT ( 'NONE',  ( 2.231653169902757750, -1.284661796483690832, -1.495404430405805174 ) ) ;
#195199=CARTESIAN_POINT ( 'NONE',  ( 1.343279689680024536, 0.4525242940816387449, 2.262625540901804122 ) ) ;
#195200=CARTESIAN_POINT ( 'NONE',  ( 2.260140581184489239, -1.961506502764579052, 0.04509734162668613960 ) ) ;
#195201=CARTESIAN_POINT ( 'NONE',  ( 4.979373296276208727, -0.1066085398311214100, 2.059958923327874114 ) ) ;
#195208=CARTESIAN_POINT ( 'NONE',  ( 1.305810364819631753, -1.710103357748852027, -1.337415221091219353 ) ) ;
#195214=CARTESIAN_POINT ( 'NONE',  ( 2.565516880305099612, 1.835255434019352094, -0.3607447438512822457 ) ) ;
#195215=CARTESIAN_POINT ( 'NONE',  ( 6.872347393157318685, -1.336039616365672700, 1.699942530728588919 ) ) ;
#195216=CARTESIAN_POINT ( 'NONE',  ( 0.07735805125224680390, 0.7159309182679198802, -2.172969595131315934 ) ) ;
#195217=CARTESIAN_POINT ( 'NONE',  ( 6.827182134110196365, 2.083530588508203607, 2.119847806254702594 ) ) ;
#195219=CARTESIAN_POINT ( 'NONE',  ( 2.016128127738999076, -1.911839501640894001, 0.04842977492004740814 ) ) ;
#195220=CARTESIAN_POINT ( 'NONE',  ( 4.276060399186999206, -1.018433877553532207, 1.447237009025013732 ) ) ;
#195221=CARTESIAN_POINT ( 'NONE',  ( 1.682132150489405564, 0.9841149911452107268, 1.639481845682550398 ) ) ;
#195224=CARTESIAN_POINT ( 'NONE',  ( 5.624599552000627334, 0.3785363404739845450, 1.877648607602548925 ) ) ;
#195225=CARTESIAN_POINT ( 'NONE',  ( 0.1509401653462701109, -0.4529219869476922011, -2.027634260368789576 ) ) ;
#195227=CARTESIAN_POINT ( 'NONE',  ( 2.074623746436579985, 0.9110886696130392481, 1.915067268644244702 ) ) ;
#195228=CARTESIAN_POINT ( 'NONE',  ( 4.680451076648031616, -1.814532364864028136, -0.4542276060127621862 ) ) ;
#195229=CARTESIAN_POINT ( 'NONE',  ( 1.787459277025660542, 1.258035843444211155, 1.323286951131589895 ) ) ;
#195231=CARTESIAN_POINT ( 'NONE',  ( 4.600333186373093852, -2.206333364838486411, -0.05604163552313382035 ) ) ;
#195234=CARTESIAN_POINT ( 'NONE',  ( 2.031754214314248408, 1.974575511506712289, -0.5964607296059397656 ) ) ;
#195243=CARTESIAN_POINT ( 'NONE',  ( 4.211429588753928144, -1.719575573843846072, -1.152724658989822348 ) ) ;
#195246=CARTESIAN_POINT ( 'NONE',  ( 2.601032539102793084, 1.737798908178284307, -1.285340053188685383 ) ) ;
#195248=CARTESIAN_POINT ( 'NONE',  ( 1.488931934708405569, -1.918476728873222070, -0.6315473366199951810 ) ) ;
#195255=CARTESIAN_POINT ( 'NONE',  ( 0.02267320670834571672, 0.3494893071277604402, 1.985867805234131644 ) ) ;
#195256=CARTESIAN_POINT ( 'NONE',  ( 5.495707582769355781, -2.191739722525353429, -0.0009102486706394352645 ) ) ;
#195259=CARTESIAN_POINT ( 'NONE',  ( 4.254103502353132171, 0.8128351696983120434, -1.731171583500931366 ) ) ;
#195264=CARTESIAN_POINT ( 'NONE',  ( 2.478138860811992306, -2.011206848916185397, -0.1455134472309257965 ) ) ;
#195267=CARTESIAN_POINT ( 'NONE',  ( 5.737229663476812291, -1.557457729854847983, 0.7413209835094927147 ) ) ;
#195273=CARTESIAN_POINT ( 'NONE',  ( 1.182579820358391931, 1.236233925375467058, -1.660450453320160058 ) ) ;
#195275=CARTESIAN_POINT ( 'NONE',  ( 4.564998375345614257, -1.451947166338814377, 1.082946968254307585 ) ) ;
#195280=CARTESIAN_POINT ( 'NONE',  ( 5.953728957075980155, -1.316865622510310141, -1.244172183657651365 ) ) ;
#195283=CARTESIAN_POINT ( 'NONE',  ( 3.240350661220792183, 0.5327334615983710941, 2.125583950146384904 ) ) ;
#195286=CARTESIAN_POINT ( 'NONE',  ( 6.883263157960402445, 0.001763689368145578400, 1.846037217754380011 ) ) ;
#195288=CARTESIAN_POINT ( 'NONE',  ( 5.343340938886254499, 0.3690371538600076273, -1.879538113519742204 ) ) ;
#195295=CARTESIAN_POINT ( 'NONE',  ( 1.780366757100563913, -1.156431984057613827, 1.826190802295484472 ) ) ;
#195299=CARTESIAN_POINT ( 'NONE',  ( 1.447985623159939284, 1.823312892812560593, 0.09356915273009414058 ) ) ;
#195301=CARTESIAN_POINT ( 'NONE',  ( 5.192344348049102720, -1.811977082810274808, -0.2219828972063255801 ) ) ;
#195304=CARTESIAN_POINT ( 'NONE',  ( 4.141030287458704606, -0.1905934838449650226, -1.960285098343496291 ) ) ;
#195306=CARTESIAN_POINT ( 'NONE',  ( 5.021012369077997306, -1.842940949158570207, 0.6126725321249880674 ) ) ;
#195310=CARTESIAN_POINT ( 'NONE',  ( 5.062787373817618786, 0.6179034821891697948, 2.028544477791139222 ) ) ;
#195312=CARTESIAN_POINT ( 'NONE',  ( 3.246637215680724164, 1.866209232881730573, 0.4165188312477489663 ) ) ;
#195318=CARTESIAN_POINT ( 'NONE',  ( 4.740889518710099004, 1.927123460305087965, 0.5820593317791241672 ) ) ;
#195320=CARTESIAN_POINT ( 'NONE',  ( 5.338443970399977978, 1.799313579390570128, 0.3082849261525285600 ) ) ;
#195321=CARTESIAN_POINT ( 'NONE',  ( 1.328672132201724532, -1.314895749051579132, 1.599177317581280455 ) ) ;
#195325=CARTESIAN_POINT ( 'NONE',  ( 5.910993886665249164, 1.650546521282238110, 0.8803886038859505270 ) ) ;
#195334=CARTESIAN_POINT ( 'NONE',  ( 1.604436975501881468, 2.067711310959176707, 0.1055696395834623824 ) ) ;
#195335=CARTESIAN_POINT ( 'NONE',  ( 2.530995666134610911, -1.758555926239983691, 1.178765877976214016 ) ) ;
#195338=CARTESIAN_POINT ( 'NONE',  ( 0.7077770966438132749, 0.6232387800201264483, -1.868272854783992187 ) ) ;
#195343=CARTESIAN_POINT ( 'NONE',  ( 2.431904175345489083, 1.079062523900159221, -2.022394142706671616 ) ) ;
#195344=CARTESIAN_POINT ( 'NONE',  ( 1.084280211047653264, -1.780658692889337091, -0.4022698149812459212 ) ) ;
#195345=CARTESIAN_POINT ( 'NONE',  ( 2.162237915172473546, 1.912057200688283665, 0.04323261116381121871 ) ) ;
#195349=CARTESIAN_POINT ( 'NONE',  ( 1.388932857043408742, -1.913036705441802265, -0.6274143624813811604 ) ) ;
#195350=CARTESIAN_POINT ( 'NONE',  ( 1.955835763735654487, -0.6658547638305843952, 1.845409454533278648 ) ) ;
#195354=CARTESIAN_POINT ( 'NONE',  ( 4.839831225001551829, 2.085006553764104265, 0.1541250707555453237 ) ) ;
#195355=CARTESIAN_POINT ( 'NONE',  ( 3.432247180620687566, 1.726460203109028591, 0.3886401920838201685 ) ) ;
#195358=CARTESIAN_POINT ( 'NONE',  ( -0.01142137120296871262, -0.4863542539808898280, -2.144715426241408984 ) ) ;
#195359=CARTESIAN_POINT ( 'NONE',  ( 4.681465254972009049, -0.8165918992961908041, 1.536851246062352905 ) ) ;
#195362=CARTESIAN_POINT ( 'NONE',  ( 4.710095198716817144, -1.340344737836828282, -1.099787012688882015 ) ) ;
#195363=( BOUNDED_SURFACE ( )  B_SPLINE_SURFACE ( 3, 3, ( 
 ( #20971, #69728, #156354, #5781, #119638, #102251, #121791, #56709, #104397, #55635, #135832 ),
 ( #140118, #103324, #187758, #37254, #120720, #40473, #6859, #186693, #205067, #123936, #105483 ),
 ( #38321, #122877, #189904, #72938, #168325, #172603, #170446, #3650, #22032, #109801, #129276 ),
 ( #95643, #91366, #157426, #77215, #93500, #29551, #193100, #28475, #128208, #192019, #78283 ),
 ( #9017, #27401, #210411, #158481, #108728, #207216, #44749, #11138, #175808, #92441, #211474 ),
 ( #79361, #174754, #63109, #144411, #145479, #161694, #10081, #41546, #142259, #62053, #76155 ),
 ( #173689, #42618, #194170, #13288, #208271, #58840, #124995, #59904, #111936, #143334, #159540 ) ),
 .UNSPECIFIED., .T., .F., .T. ) 
 B_SPLINE_SURFACE_WITH_KNOTS ( ( 4, 3, 4 ),
 ( 4, 1, 1, 1, 1, 1, 1, 1, 4 ),
 ( 0.000000000000000000, 0.5000000000000000000, 1.000000000000000000 ),
 ( 0.000000000000000000, 0.2257091236145174484, 0.3979912149639216468, 0.5260416812932605657, 0.6190739408849097458, 0.6862087210430605211, 0.7361363507675404705, 0.7768852254246026989, 0.9999999999999998890 ),
 .UNSPECIFIED. ) 
 GEOMETRIC_REPRESENTATION_ITEM ( )  RATIONAL_B_SPLINE_SURFACE ( (
 ( 1.000000000000000222, 1.000000000000000222, 1.000000000000000000, 1.000000000000000000, 1.000000000000000222, 1.000000000000000000, 1.000000000000000000, 1.000000000000000000, 1.000000000000000222, 1.000000000000000000, 1.000000000000000000),
 ( 0.3333333333333334259, 0.3333333333333334259, 0.3333333333333333148, 0.3333333333333333703, 0.3333333333333334259, 0.3333333333333333703, 0.3333333333333333703, 0.3333333333333334259, 0.3333333333333333703, 0.3333333333333333703, 0.3333333333333333703),
 ( 0.3333333333333334259, 0.3333333333333334259, 0.3333333333333333148, 0.3333333333333333703, 0.3333333333333334259, 0.3333333333333333703, 0.3333333333333333703, 0.3333333333333334259, 0.3333333333333333703, 0.3333333333333333703, 0.3333333333333333703),
 ( 1.000000000000000222, 1.000000000000000222, 1.000000000000000000, 1.000000000000000000, 1.000000000000000222, 1.000000000000000000, 1.000000000000000000, 1.000000000000000000, 1.000000000000000222, 1.000000000000000000, 1.000000000000000000),
 ( 0.3333333333333334259, 0.3333333333333334259, 0.3333333333333333148, 0.3333333333333333703, 0.3333333333333334259, 0.3333333333333333703, 0.3333333333333333703, 0.3333333333333334259, 0.3333333333333333703, 0.3333333333333333703, 0.3333333333333333703),
 ( 0.3333333333333334259, 0.3333333333333334259, 0.3333333333333333148, 0.3333333333333333703, 0.3333333333333334259, 0.3333333333333333703, 0.3333333333333333703, 0.3333333333333334259, 0.3333333333333333703, 0.3333333333333333703, 0.3333333333333333703),
 ( 1.000000000000000222, 1.000000000000000222, 1.000000000000000000, 1.000000000000000000, 1.000000000000000222, 1.000000000000000000, 1.000000000000000000, 1.000000000000000000, 1.000000000000000222, 1.000000000000000000, 1.000000000000000000) ) ) 
 REPRESENTATION_ITEM ( '' )  SURFACE ( )  );
#195364=CARTESIAN_POINT ( 'NONE',  ( 4.879425774075326849, -0.1113562312203674326, 2.168454086520410495 ) ) ;
#195366=CARTESIAN_POINT ( 'NONE',  ( 6.245327377194020535, 0.3399632236478037917, -1.987496870419297013 ) ) ;
#195367=CARTESIAN_POINT ( 'NONE',  ( 6.375000000015829116, 2.052068128807268188, -3.630807684676397404E-13 ) ) ;
#195369=CARTESIAN_POINT ( 'NONE',  ( 2.924735480247532937, 1.813364411391896969, 0.6504805730627157834 ) ) ;
#195371=CARTESIAN_POINT ( 'NONE',  ( 6.451452576676337536, -1.984925862664425500, 0.9976300440488919952 ) ) ;
#195373=CARTESIAN_POINT ( 'NONE',  ( 6.983263157960407419, 1.286439435963281142, 1.962168536134776931 ) ) ;
#195376=CARTESIAN_POINT ( 'NONE',  ( 1.541950133533489975, -2.090104109921666620, 0.7524221467923494222 ) ) ;
#195377=CARTESIAN_POINT ( 'NONE',  ( 6.865691018405424728, -0.4312029709039078562, 1.920920986087648163 ) ) ;
#195382=CARTESIAN_POINT ( 'NONE',  ( 0.1236729436712938751, 0.3474707636354073537, 1.986100063511665237 ) ) ;
#195384=CARTESIAN_POINT ( 'NONE',  ( 5.916483495826922123, 0.8326555988564422472, 1.887315221659194631 ) ) ;
#195391=CARTESIAN_POINT ( 'NONE',  ( 0.7898890640410756170, -1.755383811729524624, -0.2245491444978504059 ) ) ;
#195392=CARTESIAN_POINT ( 'NONE',  ( 6.065060216814489813, -0.9193275656586662459, 1.470200510888696632 ) ) ;
#195393=CARTESIAN_POINT ( 'NONE',  ( 4.177133728293176418, 1.140962030703307928, 1.314357115670391707 ) ) ;
#195395=CARTESIAN_POINT ( 'NONE',  ( 3.351411269679291038, 0.5553372447333758677, -2.223988721106509470 ) ) ;
#195397=CARTESIAN_POINT ( 'NONE',  ( 1.271164299617353333, 1.095269041189731452, 1.479763895647051353 ) ) ;
#195401=CARTESIAN_POINT ( 'NONE',  ( 1.676486011727536418, -1.732352342712149440, -0.5761224636358779350 ) ) ;
#195402=CARTESIAN_POINT ( 'NONE',  ( 2.777970385693105726, 1.728001979019553325, -1.038993764437286416 ) ) ;
#195403=CARTESIAN_POINT ( 'NONE',  ( 1.552940555598739891, -1.880887156831068552, -1.124362282834884263 ) ) ;
#195405=CARTESIAN_POINT ( 'NONE',  ( 4.366313571243555458, 0.9904663015308888818, 1.858490915321360237 ) ) ;
#195409=CARTESIAN_POINT ( 'NONE',  ( 1.328672132201724532, -1.314895749051579132, 1.599177317581280455 ) ) ;
#195412=CARTESIAN_POINT ( 'NONE',  ( 3.352298257493666167, 0.9517314053594098100, -1.894962337767625904 ) ) ;
#195413=CARTESIAN_POINT ( 'NONE',  ( 0.1000542341482368452, -1.926035175483146400, -0.04890095678477742597 ) ) ;
#195420=CARTESIAN_POINT ( 'NONE',  ( 6.152600690169603759, 2.097733681304454034, 0.3095894981632040244 ) ) ;
#195421=CARTESIAN_POINT ( 'NONE',  ( 0.7453164640696362531, -1.806240154289909139, 1.082582905463305378 ) ) ;
#195424=CARTESIAN_POINT ( 'NONE',  ( 5.664867498354182018, 1.410286671683948168, -1.214315750818369510 ) ) ;
#195430=CARTESIAN_POINT ( 'NONE',  ( 1.908577322519442454, 0.6123880975643315461, 1.863924812142327525 ) ) ;
#195431=CARTESIAN_POINT ( 'NONE',  ( 1.516726440323381331, 1.451591637995581996, -1.601975981646540426 ) ) ;
#195436=CARTESIAN_POINT ( 'NONE',  ( 3.040114402249920911, 1.647253858686392958, -0.5413168154804471888 ) ) ;
#195437=CARTESIAN_POINT ( 'NONE',  ( 2.905909708737213659, 1.260233761464889302, -1.200475698291984861 ) ) ;
#195440=CARTESIAN_POINT ( 'NONE',  ( 2.372404410299948196, -1.270453386316850342, 1.622462496149602140 ) ) ;
#195441=CARTESIAN_POINT ( 'NONE',  ( 0.7552322466577044979, -2.000550463317086525, -0.2495714061315074117 ) ) ;
#195442=CARTESIAN_POINT ( 'NONE',  ( 6.925078400183575233, 4.688909937558557672, 2.706876980850602354 ) ) ;
#195444=CARTESIAN_POINT ( 'NONE',  ( 0.9187500235564357576, 1.820693165844145867, 0.7566030219750378150 ) ) ;
#195446=CARTESIAN_POINT ( 'NONE',  ( 5.326388512780113160, -0.8654452107222168067, -1.705464787417856787 ) ) ;
#195452=CARTESIAN_POINT ( 'NONE',  ( 1.260422244424246108, 2.017472913078500518, 0.09673469748067325957 ) ) ;
#195453=CARTESIAN_POINT ( 'NONE',  ( 4.260959797893453249, -1.712736962785869288, 1.546631824827559454 ) ) ;
#195454=CARTESIAN_POINT ( 'NONE',  ( 6.250445965835445428, -1.952298026214387194, -0.1936728439068043650 ) ) ;
#195455=CARTESIAN_POINT ( 'NONE',  ( 1.709737484509077365, 0.5745576563440238926, -1.875703277996950469 ) ) ;
#195459=CARTESIAN_POINT ( 'NONE',  ( 1.130240340503264829, 2.115179321838219551, 0.09787962981822571906 ) ) ;
#195462=CARTESIAN_POINT ( 'NONE',  ( 1.077780131904103156, -1.795810734350095528, -0.4053039038426771712 ) ) ;
#195464=CARTESIAN_POINT ( 'NONE',  ( 4.522458045437067753, 1.018072405813482018, 1.917541202323807203 ) ) ;
#195466=CARTESIAN_POINT ( 'NONE',  ( 1.564851893998190135, 0.6701894319398638000, 2.011955567234039677 ) ) ;
#195470=CARTESIAN_POINT ( 'NONE',  ( 2.987629706096385895, 1.454891456164056462, 1.459756821352270473 ) ) ;
#195472=CARTESIAN_POINT ( 'NONE',  ( 0.6261898170028465938, 0.1349980957352381883, 1.836376839866371569 ) ) ;
#195474=CARTESIAN_POINT ( 'NONE',  ( -0.02244404828160087226, 1.323617703852699057, -2.440988974267483957 ) ) ;
#195476=CARTESIAN_POINT ( 'NONE',  ( 3.110884140487602867, 1.641001393266024788, -1.557680395459557499 ) ) ;
#195478=CARTESIAN_POINT ( 'NONE',  ( 2.267558116911760902, 0.4800365151868010716, -1.746770699433045415 ) ) ;
#195479=CARTESIAN_POINT ( 'NONE',  ( 1.850665572125685721, -1.753200486404655090, -0.7725721188126480898 ) ) ;
#195480=CARTESIAN_POINT ( 'NONE',  ( 3.578635096964689843, 1.315621898185691974, -1.598582974826658010 ) ) ;
#195482=CARTESIAN_POINT ( 'NONE',  ( 1.410939872204178602, 1.737622768476089430, 0.9313336078424112596 ) ) ;
#195483=CARTESIAN_POINT ( 'NONE',  ( 0.1648913374791864117, -1.719061530832368234, -0.8695707864920312335 ) ) ;
#195484=CARTESIAN_POINT ( 'NONE',  ( 2.553401164250346245, 0.5009360343536627402, -1.802255699741683870 ) ) ;
#195485=CARTESIAN_POINT ( 'NONE',  ( 1.612422076237954860, -2.289831013633353063, 0.2861181584819341706 ) ) ;
#195487=CARTESIAN_POINT ( 'NONE',  ( 2.927998328727512867, 0.9930260268339460294, 1.573771836281928627 ) ) ;
#195489=CARTESIAN_POINT ( 'NONE',  ( 5.512196432965448700, 2.060465348046951917, -0.09781390707789237859 ) ) ;
#195493=CARTESIAN_POINT ( 'NONE',  ( 6.475619172616331909, 2.016361193322095957, -0.6077647485315963438 ) ) ;
#195495=CARTESIAN_POINT ( 'NONE',  ( 5.712251288600168841, -0.9662322189689103169, -1.933677227328117310 ) ) ;
#195496=CARTESIAN_POINT ( 'NONE',  ( -0.1227786480478709891, -1.806133744752127068, -0.9041943026713550324 ) ) ;
#195500=CARTESIAN_POINT ( 'NONE',  ( 6.825078400183575589, 6.038285016609903799, 2.450557349082567171 ) ) ;
#195503=CARTESIAN_POINT ( 'NONE',  ( 4.909388789075159742, -1.913262893431907141, 0.6371506334161003426 ) ) ;
#195508=CARTESIAN_POINT ( 'NONE',  ( 6.297764839082774735, -0.7330946318361495351, 2.033732118066629457 ) ) ;
#195514=CARTESIAN_POINT ( 'NONE',  ( 5.571888728144736902, -0.9040954357531080232, 1.802425742427179012 ) ) ;
#195516=CARTESIAN_POINT ( 'NONE',  ( 1.558790235068749030, -1.477961618093760032, -0.8890178537931183733 ) ) ;
#195521=CARTESIAN_POINT ( 'NONE',  ( 0.2625039974461966241, -1.576774366707566433, -0.8037556782162450508 ) ) ;
#195522=CARTESIAN_POINT ( 'NONE',  ( 1.049477475095396573, -1.818952357203638570, 0.8628315626280655959 ) ) ;
#195524=CARTESIAN_POINT ( 'NONE',  ( 2.942613154609276638, 2.189964478704994555, 0.2713889102748042736 ) ) ;
#195525=CARTESIAN_POINT ( 'NONE',  ( 5.225502712144541206, 0.2199120275673121516, -2.159938666613583802 ) ) ;
#195529=CARTESIAN_POINT ( 'NONE',  ( 2.701940546545733568, 1.501232083741442125, 1.497845299259781049 ) ) ;
#195530=CARTESIAN_POINT ( 'NONE',  ( 2.038685622454153190, -1.556895902704044765, 1.281378572682637218 ) ) ;
#195531=CARTESIAN_POINT ( 'NONE',  ( 2.636723998446516948, 1.707110652976281839, 0.6067464242315090406 ) ) ;
#195539=CARTESIAN_POINT ( 'NONE',  ( 1.393601161502202590, -1.900819510297278025, 0.2380969459827488588 ) ) ;
#195547=CARTESIAN_POINT ( 'NONE',  ( 5.137646372127643524, -1.526005641499485810, -1.531359247741073570 ) ) ;
#195550=CARTESIAN_POINT ( 'NONE',  ( 1.670341986359990205, 2.114562342887704283, -0.1611296783964668855 ) ) ;
#195554=CARTESIAN_POINT ( 'NONE',  ( 3.391827608253958015, -0.8021585586163967330, 1.800962559972321575 ) ) ;
#195555=CARTESIAN_POINT ( 'NONE',  ( 5.343983030329363615, -1.218012673290536974, -1.474316871017400166 ) ) ;
#195558=CARTESIAN_POINT ( 'NONE',  ( 0.1861046438572169504, -1.272802160389638892, -1.633586439835111648 ) ) ;
#195559=CARTESIAN_POINT ( 'NONE',  ( 2.677597413788167735, -0.9980636400313472878, 1.665709379616100883 ) ) ;
#195564=CARTESIAN_POINT ( 'NONE',  ( 2.783241352837596327, 1.478939484563842610, 1.477931775543766202 ) ) ;
#195567=CARTESIAN_POINT ( 'NONE',  ( 6.633470332280523074, -0.1331818211787652029, 1.881796397474523541 ) ) ;
#195569=CARTESIAN_POINT ( 'NONE',  ( 4.160898416275903067, -1.636102012888400292, 1.481223685352812458 ) ) ;
#195570=CARTESIAN_POINT ( 'NONE',  ( 2.854729849855553780, 0.7423848465729750989, 2.078289375090878632 ) ) ;
#195572=CARTESIAN_POINT ( 'NONE',  ( 1.646971982979035909, 0.1886418863925183320, 1.902964618272011021 ) ) ;
#195575=CARTESIAN_POINT ( 'NONE',  ( 4.475093801846619535, 1.891600172242546840, 0.8420093967692193759 ) ) ;
#195578=CARTESIAN_POINT ( 'NONE',  ( 1.833122199354455972, 0.2117775504973731793, 2.151289291301178075 ) ) ;
#195579=CARTESIAN_POINT ( 'NONE',  ( 5.021103811603734535, -2.081066139062941023, 0.6872292908843835590 ) ) ;
#195586=CARTESIAN_POINT ( 'NONE',  ( -0.1048463755018592264, -0.8645036352170620830, -1.819965476435807306 ) ) ;
#195589=CARTESIAN_POINT ( 'NONE',  ( 4.627825472248149552, 2.009385113269086087, -0.4979276649561757417 ) ) ;
#195590=CARTESIAN_POINT ( 'NONE',  ( 3.721244860960619683, -0.1409348896288381003, 1.921400582950444580 ) ) ;
#195591=CARTESIAN_POINT ( 'NONE',  ( 5.923477664823041167, -1.533883339688602465, -1.459648931523350068 ) ) ;
#195594=CARTESIAN_POINT ( 'NONE',  ( 4.328926673881399623, -1.836050571085739769, -0.7129182788949259830 ) ) ;
#195595=CARTESIAN_POINT ( 'NONE',  ( 5.630919443038269634, -2.074398886797897301, 0.9756724061340553700 ) ) ;
#195596=CARTESIAN_POINT ( 'NONE',  ( 3.510199737632841543, -0.7410081052188907114, -1.668730646197075673 ) ) ;
#195604=CARTESIAN_POINT ( 'NONE',  ( 1.118424870118275738, -0.04499623084481922664, 1.840855209834332928 ) ) ;
#195605=CARTESIAN_POINT ( 'NONE',  ( 5.343998949255959197, -1.280338926806196431, -1.553582282148850524 ) ) ;
#195606=CARTESIAN_POINT ( 'NONE',  ( 5.994848186622900421, -2.281820642442307090, 0.2777966721622132096 ) ) ;
#195607=CARTESIAN_POINT ( 'NONE',  ( 5.946142449018281262, -0.8852437533515828960, 1.750773106858094952 ) ) ;
#195611=CARTESIAN_POINT ( 'NONE',  ( 1.663735998746267652, 1.077533827470295913, 1.791552697131219229 ) ) ;
#195612=CARTESIAN_POINT ( 'NONE',  ( 6.684453129459355658, -1.736675761049325972, -0.3400495950729911510 ) ) ;
#195614=CARTESIAN_POINT ( 'NONE',  ( 5.982362851901904754, -0.2873240852911072007, -1.920464370370161600 ) ) ;
#195616=CARTESIAN_POINT ( 'NONE',  ( -0.1106727585416019261, 5.721739388512169455, -2.597565591738408841 ) ) ;
#195617=CARTESIAN_POINT ( 'NONE',  ( 1.012787145881738793, -1.698268246007793802, 0.3799501884491280901 ) ) ;
#195621=CARTESIAN_POINT ( 'NONE',  ( 1.734533752015484875, 0.1665512568347452815, 1.716820151450085596 ) ) ;
#195622=CARTESIAN_POINT ( 'NONE',  ( 1.857222401600963302, 0.3706860215506869172, -2.159823580554325329 ) ) ;
#195624=CARTESIAN_POINT ( 'NONE',  ( 3.791807063958370971, 1.597966631936774684, 1.522356218736670153 ) ) ;
#195626=CARTESIAN_POINT ( 'NONE',  ( 1.815514387157551646, -1.860550965366158715, -1.118705476460989168 ) ) ;
#195628=CARTESIAN_POINT ( 'NONE',  ( 1.903655596893740087, -2.052436370740511773, 0.5197080100793128876 ) ) ;
#195631=CARTESIAN_POINT ( 'NONE',  ( 2.279227788079383643, 2.094250403060330168, -0.9326617097511098464 ) ) ;
#195635=CARTESIAN_POINT ( 'NONE',  ( 6.059279899546098136, -1.878006040282210298, 1.186031488430500769 ) ) ;
#195641=CARTESIAN_POINT ( 'NONE',  ( 2.742814741689561853, 2.006446121045248887, -0.2004354718553730264 ) ) ;
#195643=CARTESIAN_POINT ( 'NONE',  ( 2.149356475496758456, 1.796580072245733462, -1.012980232677022974 ) ) ;
#195650=CARTESIAN_POINT ( 'NONE',  ( 5.349643074071059878, 2.189064600896481139, -0.1049423877047955811 ) ) ;
#195651=CARTESIAN_POINT ( 'NONE',  ( 2.953750172290268150, -1.864168560446223033, -0.7691209412190866956 ) ) ;
#195652=CARTESIAN_POINT ( 'NONE',  ( 1.733694375844633706, 1.821329977863223926, 0.2691589665217360983 ) ) ;
#195655=CARTESIAN_POINT ( 'NONE',  ( 5.227504313999177477, -1.733024862908550290, 0.5741523302658231298 ) ) ;
#195656=CARTESIAN_POINT ( 'NONE',  ( 5.695935454815424848, 1.779625283580280382, 0.9480427965274510482 ) ) ;
#195658=CARTESIAN_POINT ( 'NONE',  ( 5.788003261412111300, -1.023269635773180752, 2.017978558835635372 ) ) ;
#195660=CARTESIAN_POINT ( 'NONE',  ( 0.9617104568129207776, 0.4090027284681818642, -2.065791855309044411 ) ) ;
#195670=CARTESIAN_POINT ( 'NONE',  ( 2.285647630545981190, 0.1040316455800850692, -2.219075330209609120 ) ) ;
#195674=CARTESIAN_POINT ( 'NONE',  ( 3.068751266904270025, 1.422870340827029345, -1.350941015047700366 ) ) ;
#195680=CARTESIAN_POINT ( 'NONE',  ( 2.584367824843319283, 1.138156186954141003, 1.789115803205274080 ) ) ;
#195682=CARTESIAN_POINT ( 'NONE',  ( 3.995124980148881288, 1.827535992889782523, -1.154293374375232828 ) ) ;
#195683=CARTESIAN_POINT ( 'NONE',  ( 3.403688466941825030, -0.7492148395099356151, -1.682118234477212315 ) ) ;
#195686=CARTESIAN_POINT ( 'NONE',  ( 5.419757389058348807, 1.032087642559690543, -1.401099660988463169 ) ) ;
#195690=CARTESIAN_POINT ( 'NONE',  ( 2.659225025413253007, -1.880336703546074073, -1.066323988048665017 ) ) ;
#195692=CARTESIAN_POINT ( 'NONE',  ( 4.973982425466109802, 1.752763018817087293, 0.9961474888594208377 ) ) ;
#195694=CARTESIAN_POINT ( 'NONE',  ( 2.606508400632711719, -0.8264410288459265175, -1.997682696722333784 ) ) ;
#195695=CARTESIAN_POINT ( 'NONE',  ( 3.022686310138736676, 1.855048300136890482, 0.6674203052531629821 ) ) ;
#195697=CARTESIAN_POINT ( 'NONE',  ( 2.870327622459168726, -1.987497926849005836, -0.3399570244180456502 ) ) ;
#195699=CARTESIAN_POINT ( 'NONE',  ( 5.038593826026604994, -1.663644762202406646, 1.001748047271956876 ) ) ;
#195708=CARTESIAN_POINT ( 'NONE',  ( 1.114635189304619356, -0.9934212416997322270, -1.970578525975318573 ) ) ;
#195710=CARTESIAN_POINT ( 'NONE',  ( 5.770351633785986145, -0.8788013674413885923, -1.753946858050984048 ) ) ;
#195715=CARTESIAN_POINT ( 'NONE',  ( 4.769393013670423009, 1.062472638025207416, 1.503447196605799174 ) ) ;
#195723=CARTESIAN_POINT ( 'NONE',  ( 6.819606862646741874, -2.000071036334325036, 0.4962039222910428760 ) ) ;
#195725=CARTESIAN_POINT ( 'NONE',  ( 1.574410529035878969, 1.253355123444719998, -1.375888611855519583 ) ) ;
#195726=CARTESIAN_POINT ( 'NONE',  ( 3.755264181858387840, 1.826884192416846631, -0.2291247506851084581 ) ) ;
#195733=CARTESIAN_POINT ( 'NONE',  ( 3.246891520140795517, 0.5363302883765566076, 2.140594385818309409 ) ) ;
#195734=CARTESIAN_POINT ( 'NONE',  ( 5.501357770389488699, 1.845074063491736860, 1.309031944507930589 ) ) ;
#195736=CARTESIAN_POINT ( 'NONE',  ( 5.783446960131396253, 0.1242560548703756929, -1.807377920737750499 ) ) ;
#195737=CARTESIAN_POINT ( 'NONE',  ( 5.173012249488437853, 1.686445640873093899, -0.9088423865804375890 ) ) ;
#195739=CARTESIAN_POINT ( 'NONE',  ( 5.875831987524620992, 1.115552982110395330, 1.501486808359139946 ) ) ;
#195740=CARTESIAN_POINT ( 'NONE',  ( 6.320743865583476229, -1.315316497155760489, 1.316877014833318649 ) ) ;
#195742=CARTESIAN_POINT ( 'NONE',  ( 6.789980064821725669, -0.7525070324889830964, 1.600651327395278711 ) ) ;
#195743=CARTESIAN_POINT ( 'NONE',  ( 1.780482797753998092, -0.5424726148271253878, -1.942096288550937411 ) ) ;
#195745=CARTESIAN_POINT ( 'NONE',  ( 2.473383067358714715, 0.1024098097114657241, -2.103702895048992882 ) ) ;
#195750=CARTESIAN_POINT ( 'NONE',  ( 2.918227964375613048, -2.017298000423489501, 0.1032239234411459483 ) ) ;
#195753=CARTESIAN_POINT ( 'NONE',  ( 3.462350783624254191, 0.9684823049558517472, 1.932541222812742987 ) ) ;
#195757=CARTESIAN_POINT ( 'NONE',  ( 1.364001086256797945, -0.5279541034660294452, 2.105878793243611824 ) ) ;
#195761=CARTESIAN_POINT ( 'NONE',  ( 2.103317784989285677, -0.4765762082987561321, 2.138964651187735821 ) ) ;
#195763=CARTESIAN_POINT ( 'NONE',  ( 2.466018556964240549, 2.218949015226141963, -0.4410763869808070337 ) ) ;
#195770=CARTESIAN_POINT ( 'NONE',  ( 3.708038350156193541, -0.7148330724025107052, -1.619118029916452262 ) ) ;
#195772=CARTESIAN_POINT ( 'NONE',  ( 5.913141818906856528, 1.943543578741913969, 1.045239939247793792 ) ) ;
#195775=CARTESIAN_POINT ( 'NONE',  ( 5.501577430365036214, -1.966641501487207622, 0.4445218866586594930 ) ) ;
#195778=CARTESIAN_POINT ( 'NONE',  ( 4.170664822833985319, -1.745344833062393075, -0.6735866001992969476 ) ) ;
#195780=CARTESIAN_POINT ( 'NONE',  ( 3.116144222688784549, 2.060704436481402890, -0.1983081510379124945 ) ) ;
#195786=CARTESIAN_POINT ( 'NONE',  ( 1.177825114000274898, 1.883588471398514264, -0.3297955356276888184 ) ) ;
#195787=CARTESIAN_POINT ( 'NONE',  ( 2.594135478747404022, 0.9273930874063830432, -1.728848471177657942 ) ) ;
#195788=CARTESIAN_POINT ( 'NONE',  ( 1.388045824401448414, -0.05229234656609069859, 2.015604296821980057 ) ) ;
#195793=CARTESIAN_POINT ( 'NONE',  ( 6.538353035222548293, 1.949559774641503651, 0.2916953021188176121 ) ) ;
#195795=CARTESIAN_POINT ( 'NONE',  ( 1.388932857043408742, -1.913036705441802265, -0.6274143624813811604 ) ) ;
#195798=CARTESIAN_POINT ( 'NONE',  ( 2.126704408204147967, 0.4671447874508818932, 2.064898165909804906 ) ) ;
#195800=CARTESIAN_POINT ( 'NONE',  ( 3.807136610393092813, -1.694265131726957252, 1.189645435975445809 ) ) ;
#195802=CARTESIAN_POINT ( 'NONE',  ( 5.789036971029382528, 1.582348866732422810, 1.366464223246833809 ) ) ;
#195804=CARTESIAN_POINT ( 'NONE',  ( 3.979382468966369935, 1.719079831940514502, -0.6148086763930470378 ) ) ;
#195809=CARTESIAN_POINT ( 'NONE',  ( 6.229534195615700654, -2.079954537573494466, 0.7377168454194837910 ) ) ;
#195812=CARTESIAN_POINT ( 'NONE',  ( 4.828717125059535320, 1.315996081294769304, -1.387672938220223307 ) ) ;
#195817=CARTESIAN_POINT ( 'NONE',  ( 0.3273695209934923689, 0.9472894719858866441, -1.578709817245539604 ) ) ;
#195820=CARTESIAN_POINT ( 'NONE',  ( 4.288257209584379837, -1.849852534125648207, -0.2767368629695772797 ) ) ;
#195829=CARTESIAN_POINT ( 'NONE',  ( 1.709744157921966101, 0.5768405975999196800, -1.883039948965541610 ) ) ;
#195830=CARTESIAN_POINT ( 'NONE',  ( 2.425407844734633223, -1.496065234337567329, -1.352141214786584777 ) ) ;
#195834=CARTESIAN_POINT ( 'NONE',  ( 2.959115643078192637, 0.3208686883675835877, -2.167707805308824121 ) ) ;
#195837=CARTESIAN_POINT ( 'NONE',  ( 6.825078400183548055, 2.447738240532343124, 2.338733633852312366 ) ) ;
#195845=CARTESIAN_POINT ( 'NONE',  ( 5.390138975101268493, -0.4531076923771395482, -1.784498753146485539 ) ) ;
#195846=CARTESIAN_POINT ( 'NONE',  ( 1.647136526480545982, 0.1996500767776411833, 2.003181903140099696 ) ) ;
#195847=CARTESIAN_POINT ( 'NONE',  ( 2.636409100479879086, 0.1147267580069409321, -2.295643959171574711 ) ) ;
#195849=CARTESIAN_POINT ( 'NONE',  ( 1.850234720775156605, -1.851392121210411634, -0.1886080954226591611 ) ) ;
#195853=CARTESIAN_POINT ( 'NONE',  ( 5.238497809344139000, 1.134185964801931679, -1.539638564045166857 ) ) ;
#195856=CARTESIAN_POINT ( 'NONE',  ( 4.880461040030859010, -0.2572269614671355842, -2.074807210009928848 ) ) ;
#195857=CARTESIAN_POINT ( 'NONE',  ( 3.432352559540859271, 1.824792983844251371, 0.4109263881779609551 ) ) ;
#195859=CARTESIAN_POINT ( 'NONE',  ( 6.286648950733226826, 1.598451336667701339, -0.9137711784916457969 ) ) ;
#195862=CARTESIAN_POINT ( 'NONE',  ( 4.863727610707407223, 1.705404662657764137, -0.2575704655415639310 ) ) ;
#195868=CARTESIAN_POINT ( 'NONE',  ( 4.346645206408905615, -2.146589105242337592, -0.3245344146646060302 ) ) ;
#195869=CARTESIAN_POINT ( 'NONE',  ( 3.668406916800326822, -1.225078373119499187, 1.353803248016255178 ) ) ;
#195870=CARTESIAN_POINT ( 'NONE',  ( 1.235121763443976173, -0.04261391538399812023, -1.961451400788959631 ) ) ;
#195871=CARTESIAN_POINT ( 'NONE',  ( 6.175037754964278314, 1.841102675566621771, -1.045632355512320144 ) ) ;
#195872=CARTESIAN_POINT ( 'NONE',  ( 5.495737418514557326, -2.292545469083116849, -0.002927036808696506075 ) ) ;
#195877=CARTESIAN_POINT ( 'NONE',  ( 2.139458383197485603, 0.002846582261652879763, 2.120667954922689002 ) ) ;
#195881=CARTESIAN_POINT ( 'NONE',  ( 6.737192315218426764, -0.09781360997717462868, -2.168977284074862677 ) ) ;
#195882=CARTESIAN_POINT ( 'NONE',  ( 6.883263157960366030, 0.5727201817382967519, 2.105997115537924902 ) ) ;
#195884=CARTESIAN_POINT ( 'NONE',  ( 1.946216630774719736, -1.453687271215977850, -1.679643103671465632 ) ) ;
#195886=CARTESIAN_POINT ( 'NONE',  ( 0.1417928296247125686, 0.8878553654741733192, 2.120496703859587662 ) ) ;
#195888=CARTESIAN_POINT ( 'NONE',  ( 5.647355161340581020, 1.821535332892617820, -0.9675206831420575249 ) ) ;
#195894=CARTESIAN_POINT ( 'NONE',  ( 0.1331565106231363538, 7.629137130509071163, -2.545925718843544239 ) ) ;
#195895=CARTESIAN_POINT ( 'NONE',  ( 5.776868925826902590, 1.698781319366513998, -0.7106697882480541573 ) ) ;
#195896=CIRCLE ( 'NONE', #9115, 0.04999999999999930889 ) ;
#195900=CARTESIAN_POINT ( 'NONE',  ( 1.764246635482754622, -1.222956780391671439, 1.216502489609740723 ) ) ;
#195901=CARTESIAN_POINT ( 'NONE',  ( 1.587125413319636857, 1.679225032509903626, 1.116207499648947943 ) ) ;
#195902=CARTESIAN_POINT ( 'NONE',  ( 2.092814488687055441, -0.4990534829178472354, 2.243750245495256035 ) ) ;
#195904=CARTESIAN_POINT ( 'NONE',  ( 2.724197551734920175, -1.300482880258296836, -1.851114353284079472 ) ) ;
#195905=CARTESIAN_POINT ( 'NONE',  ( 4.178421505988277218, -1.212938584752444093, 1.721516029631239064 ) ) ;
#195907=CARTESIAN_POINT ( 'NONE',  ( 2.213771126746429729, -0.8293587345859743110, -1.563345763006577238 ) ) ;
#195914=CARTESIAN_POINT ( 'NONE',  ( 6.533471383080789785, -0.1550430487086348341, 2.186663148620856756 ) ) ;
#195915=CARTESIAN_POINT ( 'NONE',  ( 2.976726284633357533, -0.1618151936485581754, -2.185533650236513914 ) ) ;
#195918=CARTESIAN_POINT ( 'NONE',  ( 6.533838320793388554, -2.056994387304663885, 0.5145578593022879232 ) ) ;
#195923=CARTESIAN_POINT ( 'NONE',  ( 5.519825572852568030, -0.5132647233585425628, 2.057443900658859182 ) ) ;
#195928=CARTESIAN_POINT ( 'NONE',  ( 6.374545129912786656, -0.09763137639631429276, -1.838803627010993091 ) ) ;
#195931=CARTESIAN_POINT ( 'NONE',  ( 2.471852389601780331, -1.665955342129191274, -0.5037381675307306406 ) ) ;
#195933=CARTESIAN_POINT ( 'NONE',  ( 0.7308173252688826560, -1.846041318942293286, -0.6644482084196751126 ) ) ;
#195937=CARTESIAN_POINT ( 'NONE',  ( 6.157120911006636277, -1.851533521339579380, -1.115484332758958974 ) ) ;
#195941=CARTESIAN_POINT ( 'NONE',  ( 5.664953204072169513, -1.952404353424816774, -0.9282482345986733385 ) ) ;
#195945=CARTESIAN_POINT ( 'NONE',  ( 5.747334165637288272, -1.552519754122901663, -1.214743736649764649 ) ) ;
#195946=CARTESIAN_POINT ( 'NONE',  ( 5.237493459246572947, -1.633055164623600897, -0.5828427842848020735 ) ) ;
#195948=CARTESIAN_POINT ( 'NONE',  ( 1.452940684028160234, -1.882004992133184285, -1.122693704575933316 ) ) ;
#195949=CARTESIAN_POINT ( 'NONE',  ( 3.206425952641503319, -2.304998342715250281, 0.1115464655990650450 ) ) ;
#195950=CARTESIAN_POINT ( 'NONE',  ( 5.518845395222173877, 1.902436629287082237, 0.7926794616768815249 ) ) ;
#195951=CARTESIAN_POINT ( 'NONE',  ( 1.359210844938564033, 1.913264527786652902, -0.3316978906799557536 ) ) ;
#195956=CARTESIAN_POINT ( 'NONE',  ( 3.726904977748810133, 1.497142547446396410, -1.502090761940577002 ) ) ;
#195958=CARTESIAN_POINT ( 'NONE',  ( 2.725232599228684993, 2.001511357256777313, 0.2440295182731533341 ) ) ;
#195960=CARTESIAN_POINT ( 'NONE',  ( 4.454274341225270994, 2.206355006892012138, -0.05062909709598743119 ) ) ;
#195966=CARTESIAN_POINT ( 'NONE',  ( -0.02900071798685524560, -0.004641455105012376459, -2.173770343569726649 ) ) ;
#195970=CARTESIAN_POINT ( 'NONE',  ( 4.364173291480280881, 0.9696465702416400267, 1.818514982836361593 ) ) ;
#195976=CARTESIAN_POINT ( 'NONE',  ( 3.369790118769320664, 0.4886731666619185677, -1.959541563195909220 ) ) ;
#195980=CARTESIAN_POINT ( 'NONE',  ( 3.309499033229778231, -0.4035708669713148899, 2.020805850887919863 ) ) ;
#195984=CARTESIAN_POINT ( 'NONE',  ( -0.1408020194049965368, 5.721120576699901150, -2.694324532632543345 ) ) ;
#195986=CARTESIAN_POINT ( 'NONE',  ( 1.323879276782027548, 1.773944146221797524, 0.4926282247687193139 ) ) ;
#195987=CARTESIAN_POINT ( 'NONE',  ( -0.02224634325198419221, -0.007204097619508199532, -2.289079630542793620 ) ) ;
#195989=CARTESIAN_POINT ( 'NONE',  ( 2.530746307392011563, 2.096003997654236173, 0.5278882200696957128 ) ) ;
#195991=CARTESIAN_POINT ( 'NONE',  ( 1.604704241733472037, 1.883313803065278513, 0.7212895827233902768 ) ) ;
#195992=CARTESIAN_POINT ( 'NONE',  ( 2.724286267170890952, -1.998689782195923081, -1.134749220811093418 ) ) ;
#195994=CARTESIAN_POINT ( 'NONE',  ( 0.4615142869485132637, 1.850934062480696252, -0.2700578556205368574 ) ) ;
#195995=CARTESIAN_POINT ( 'NONE',  ( 4.153168997088651615, -1.638446398916657776, -1.096151307749502868 ) ) ;
#195997=CARTESIAN_POINT ( 'NONE',  ( 4.469935555517978720, -0.9463019959239076240, 1.780667052345537238 ) ) ;
#196001=CARTESIAN_POINT ( 'NONE',  ( 5.988920713192999123, -0.3073026951427524356, -2.083404400164515113 ) ) ;
#196002=CARTESIAN_POINT ( 'NONE',  ( 6.355931484454268698, -0.7012994977402075003, 1.948090369817329526 ) ) ;
#196006=CARTESIAN_POINT ( 'NONE',  ( 4.416843060293515144, 1.802029179758830812, 0.8000101564944164245 ) ) ;
#196007=CARTESIAN_POINT ( 'NONE',  ( 6.381118777440311085, -1.848351591093103652, -0.8147283084726087976 ) ) ;
#196009=CARTESIAN_POINT ( 'NONE',  ( 4.477368160356545168, 0.002844634383740093052, -2.307868969966973438 ) ) ;
#196010=CARTESIAN_POINT ( 'NONE',  ( 2.079038939659454854, 1.922984332675440777, 0.7462749415493277194 ) ) ;
#196017=CARTESIAN_POINT ( 'NONE',  ( 3.877515590359277287, -0.1633623659567252084, 2.165103034678467431 ) ) ;
#196020=CARTESIAN_POINT ( 'NONE',  ( 3.157574601152390414, 0.8305207305269333151, 1.643389852989694200 ) ) ;
#196022=CARTESIAN_POINT ( 'NONE',  ( 5.284801750429747536, 1.933107837519608685, -1.032524723389722787 ) ) ;
#196024=CARTESIAN_POINT ( 'NONE',  ( 5.770491790047429959, -1.440319307945096217, 1.744843718407377731 ) ) ;
#196029=CARTESIAN_POINT ( 'NONE',  ( 6.134039733390581617, 0.8703851191177320867, -1.540848210998513990 ) ) ;
#196033=CARTESIAN_POINT ( 'NONE',  ( 4.002593568968414672, -1.991494762441379462, -0.2932518702276361022 ) ) ;
#196035=CARTESIAN_POINT ( 'NONE',  ( 2.661270901210018636, -1.831774207203272775, -1.038945448840204122 ) ) ;
#196036=CARTESIAN_POINT ( 'NONE',  ( 2.390125374076298659, -0.7353994070154221685, -1.769027144041198429 ) ) ;
#196038=CARTESIAN_POINT ( 'NONE',  ( 3.209381719453743287, -1.608569549925453313, -1.136198915559688105 ) ) ;
#196039=CARTESIAN_POINT ( 'NONE',  ( 2.043623373375623942, 0.7184291972081280342, -1.727395513401897453 ) ) ;
#196040=CARTESIAN_POINT ( 'NONE',  ( 2.541395235131336694, 1.794889867694851260, -0.7924082849640816661 ) ) ;
#196041=CARTESIAN_POINT ( 'NONE',  ( 4.476996172482918368, -0.003761094005936410634, -1.725068444937064349 ) ) ;
#196042=CARTESIAN_POINT ( 'NONE',  ( 0.08795244648929222142, 1.102731429460445334, 1.562230693318837238 ) ) ;
#196044=CARTESIAN_POINT ( 'NONE',  ( 1.207977004800918852, -0.5332226995428279714, 2.141375170867452660 ) ) ;
#196049=CARTESIAN_POINT ( 'NONE',  ( 6.666881909320486521, -1.711340306973156977, -0.7558587634414122292 ) ) ;
#196053=CARTESIAN_POINT ( 'NONE',  ( 0.8364851226981102617, -1.151554295457988930, 1.720357586142134076 ) ) ;
#196058=CARTESIAN_POINT ( 'NONE',  ( 5.373730994130427874, 0.4134100146411868737, -2.079626175754036410 ) ) ;
#196064=CARTESIAN_POINT ( 'NONE',  ( 6.268018250734934682, -1.947192974725008963, 0.2387856323943157166 ) ) ;
#196066=CARTESIAN_POINT ( 'NONE',  ( 3.778672575519220977, -1.986742196792599335, 0.3418835855632795795 ) ) ;
#196067=CARTESIAN_POINT ( 'NONE',  ( 3.872214865662172656, -1.895674933386840344, -0.2753630107846723463 ) ) ;
#196069=CARTESIAN_POINT ( 'NONE',  ( 1.118978350340808614, -0.04878210919301297771, 2.191179638975069732 ) ) ;
#196074=CARTESIAN_POINT ( 'NONE',  ( 5.712555019607242990, 2.040694153135207412, 0.5639581637400041814 ) ) ;
#196076=CARTESIAN_POINT ( 'NONE',  ( 2.366838851271795718, 0.09958507307840713807, -2.088488507012337347 ) ) ;
#196078=CARTESIAN_POINT ( 'NONE',  ( 1.271983708484729636, -1.098657341177114999, 1.329575768613028286 ) ) ;
#196090=CARTESIAN_POINT ( 'NONE',  ( 1.717148478332259254, 1.506203170942743030, 1.006022724715895045 ) ) ;
#196094=CARTESIAN_POINT ( 'NONE',  ( 6.639320575229278099, 0.5905802482995252678, 1.949996947996739172 ) ) ;
#196098=CARTESIAN_POINT ( 'NONE',  ( 3.209261600960995775, -1.519886386175553605, -1.073685847751577604 ) ) ;
#196099=CARTESIAN_POINT ( 'NONE',  ( -0.05329673158829557195, -1.711387015114009369, -0.8607133870397830622 ) ) ;
#196100=CARTESIAN_POINT ( 'NONE',  ( 0.2350025537052654601, -1.671451849548213797, 0.7345932495873632728 ) ) ;
#196106=CARTESIAN_POINT ( 'NONE',  ( 4.135575292396717728, 1.855891543885644479, -0.6595280497384666818 ) ) ;
#196107=CARTESIAN_POINT ( 'NONE',  ( 2.033984416766075665, -2.056095976692096094, 0.5180656111221926263 ) ) ;
#196110=CARTESIAN_POINT ( 'NONE',  ( 5.560537033210596114, -1.979929515673630513, -0.9395970221138388867 ) ) ;
#196112=CARTESIAN_POINT ( 'NONE',  ( 5.157218254430565807, -1.627291586725558181, -1.030705938667796140 ) ) ;
#196114=CARTESIAN_POINT ( 'NONE',  ( 0.2526013166088726392, -1.469656019175567208, 1.082793315970068004 ) ) ;
#196115=CARTESIAN_POINT ( 'NONE',  ( 0.8564375766340023288, 2.204168734417511821, -0.1118928034387969561 ) ) ;
#196120=CARTESIAN_POINT ( 'NONE',  ( 5.682459527512692787, 1.176241607570350567, -1.579419126353029279 ) ) ;
#196121=CARTESIAN_POINT ( 'NONE',  ( 1.417416744832197484, -1.080314125112752155, -1.613661906057413331 ) ) ;
#196123=CARTESIAN_POINT ( 'NONE',  ( 0.7024996975148189993, -1.423740904080775138, -1.427721366232127753 ) ) ;
#196125=CARTESIAN_POINT ( 'NONE',  ( 5.998848716047340268, 0.3616406339099677014, 1.825274704766747913 ) ) ;
#196130=CARTESIAN_POINT ( 'NONE',  ( 1.171705676731093604, 1.309414992938146893, 1.757219779060022580 ) ) ;
#196135=CARTESIAN_POINT ( 'NONE',  ( 1.154616158753757338, -1.440623569337009968, 1.121372061650728558 ) ) ;
#196140=CARTESIAN_POINT ( 'NONE',  ( 6.270122753791413928, 0.9430518052575274091, 1.563124558401955300 ) ) ;
#196141=CARTESIAN_POINT ( 'NONE',  ( 4.575024454672827368, 1.791946274209740952, 0.7988320279663924106 ) ) ;
#196144=CARTESIAN_POINT ( 'NONE',  ( 4.247736854543925133, 2.191053489037126045, -0.05455935714590579716 ) ) ;
#196146=CARTESIAN_POINT ( 'NONE',  ( 6.609000000000042618, 6.036791015687303918, 2.594900324319386886 ) ) ;
#196147=CARTESIAN_POINT ( 'NONE',  ( 3.661042849074844785, 1.635018244968543977, -1.269851595989857085 ) ) ;
#196151=CARTESIAN_POINT ( 'NONE',  ( 4.237165586469007650, 2.298153656159235503, -0.05646909981197979073 ) ) ;
#196155=CARTESIAN_POINT ( 'NONE',  ( 6.620655732516649294, 4.703748234811334861, 2.289014941052476715 ) ) ;
#196157=CARTESIAN_POINT ( 'NONE',  ( 4.329980137697307718, 1.904743498531726198, 0.3774997404530285317 ) ) ;
#196160=CARTESIAN_POINT ( 'NONE',  ( 4.254103502353132171, 0.8128351696983120434, -1.731171583500931366 ) ) ;
#196162=CARTESIAN_POINT ( 'NONE',  ( 5.526277428723715524, 1.024295688422135031, -1.387495638070087134 ) ) ;
#196163=CARTESIAN_POINT ( 'NONE',  ( 4.153529959351897283, 1.954779968807466295, -0.4946301968136583849 ) ) ;
#196164=CARTESIAN_POINT ( 'NONE',  ( 4.641406123262603600, 0.8788069589312655916, 2.124244668743579201 ) ) ;
#196166=CARTESIAN_POINT ( 'NONE',  ( 0.5752038918783763943, -2.079344756725898691, -0.7397341299467049547 ) ) ;
#196169=CARTESIAN_POINT ( 'NONE',  ( 5.448444396454582339, 0.5145788473605721336, 1.693291817928108234 ) ) ;
#196172=CARTESIAN_POINT ( 'NONE',  ( 1.957357739143847919, 0.3891275796813770116, -2.258848713223185367 ) ) ;
#196173=CARTESIAN_POINT ( 'NONE',  ( 1.552286559517775499, -1.491368903747305019, -0.8966978864634599367 ) ) ;
#196175=CARTESIAN_POINT ( 'NONE',  ( 0.8953158854557360380, 0.1194439997053517860, 1.729786500971510765 ) ) ;
#196178=CARTESIAN_POINT ( 'NONE',  ( 0.9597157272863182653, 1.774996621215488624, 1.250093255441329543 ) ) ;
#196179=CARTESIAN_POINT ( 'NONE',  ( 2.641814858895009444, 2.006371511526034546, -0.2024640970367599380 ) ) ;
#196181=CARTESIAN_POINT ( 'NONE',  ( 6.024042007596412063, -1.072333998858214343, -1.600281699052849893 ) ) ;
#196183=CARTESIAN_POINT ( 'NONE',  ( 1.986886853112525442, -1.362214788617806649, 1.754679387841934002 ) ) ;
#196190=CARTESIAN_POINT ( 'NONE',  ( 5.565861978284946332, -1.097836388496459037, 1.350534753149737366 ) ) ;
#196191=CARTESIAN_POINT ( 'NONE',  ( 3.139059813392345077, -0.1416510307416830594, -1.956792864499560691 ) ) ;
#196195=CARTESIAN_POINT ( 'NONE',  ( 4.745575995134789338, -1.744828745684245508, -1.440138369970354493 ) ) ;
#196196=CARTESIAN_POINT ( 'NONE',  ( 1.346217686498082378, -0.9293675016086970775, 1.841534056632480265 ) ) ;
#196199=CARTESIAN_POINT ( 'NONE',  ( 2.501149491322187224, 1.817439291034177451, -1.347377658580677817 ) ) ;
#196202=CARTESIAN_POINT ( 'NONE',  ( 2.178771278573924608, -0.08713135167291724548, -1.868625915979430951 ) ) ;
#196203=CARTESIAN_POINT ( 'NONE',  ( 1.793227186479518398, 1.284509341651525638, -1.165198513391290103 ) ) ;
#196204=CARTESIAN_POINT ( 'NONE',  ( 5.776942576169182608, 2.025397260235710206, -0.8375503648087383457 ) ) ;
#196205=CARTESIAN_POINT ( 'NONE',  ( 6.739320262688799801, -2.065560010629815313, 1.029036360498974068 ) ) ;
#196206=CARTESIAN_POINT ( 'NONE',  ( 3.924826023212550030, 2.051882857192890430, 0.6804245187241527715 ) ) ;
#196207=CARTESIAN_POINT ( 'NONE',  ( 4.294824717068760123, 1.560567246164183519, 1.155581451937383930 ) ) ;
#196211=CARTESIAN_POINT ( 'NONE',  ( 1.125000000000000888, -2.052068128417952497, 6.471134675641443159E-14 ) ) ;
#196216=CARTESIAN_POINT ( 'NONE',  ( 5.766250055133458119, 1.862018000461727052, -0.7743128548072516493 ) ) ;
#196220=CARTESIAN_POINT ( 'NONE',  ( 2.771877994228102882, 0.9767612972278701955, 1.542236413651025151 ) ) ;
#196227=CARTESIAN_POINT ( 'NONE',  ( 0.1233147457768641181, 1.759488896278412540, 0.9916404401272023161 ) ) ;
#196228=CARTESIAN_POINT ( 'NONE',  ( 1.330900338397854155, 1.421537331630345014, -1.573617108223644312 ) ) ;
#196232=CARTESIAN_POINT ( 'NONE',  ( 0.1632417891470130944, -1.931755829615459996, -0.9703963252955111196 ) ) ;
#196233=CARTESIAN_POINT ( 'NONE',  ( 6.240861317752083970, 2.010826688392798101, -0.1511364921914087889 ) ) ;
#196241=CARTESIAN_POINT ( 'NONE',  ( 5.782577320554741718, -1.967585831723076772, 0.4389650999883643046 ) ) ;
#196242=CARTESIAN_POINT ( 'NONE',  ( 5.050657991863417351, -1.557144343216086968, -0.9820927893566462341 ) ) ;
#196243=CARTESIAN_POINT ( 'NONE',  ( -0.02299388927988389730, 6.948790505698306141, -2.506045543530223352 ) ) ;
#196244=CARTESIAN_POINT ( 'NONE',  ( 3.229449743806306561, 0.05664919459314603917, 2.307159798345681523 ) ) ;
#196246=CARTESIAN_POINT ( 'NONE',  ( 6.221977808853903724, -1.195094089922192016, -1.800988070004491792 ) ) ;
#196248=CARTESIAN_POINT ( 'NONE',  ( 1.575622484978753679, -1.037422314974449478, 1.641571771860099727 ) ) ;
#196251=CARTESIAN_POINT ( 'NONE',  ( 4.587492961451061113, 1.418373992658492400, -1.808456645134959073 ) ) ;
#196254=CARTESIAN_POINT ( 'NONE',  ( 5.067206508511894469, 0.1826785619755930679, -1.861722072867748823 ) ) ;
#196255=CARTESIAN_POINT ( 'NONE',  ( 1.142663480069527671, 1.843847066288730074, 0.5072560978593986247 ) ) ;
#196258=CARTESIAN_POINT ( 'NONE',  ( 3.194164748978207680, -0.8942147705085048415, 2.017778291555922809 ) ) ;
#196264=CARTESIAN_POINT ( 'NONE',  ( 1.669145487688096896, 0.1492116152736686074, -1.965789094590511654 ) ) ;
#196265=CARTESIAN_POINT ( 'NONE',  ( 0.6929124517485165669, -2.290651033777380441, -0.2787006195923043550 ) ) ;
#196266=CARTESIAN_POINT ( 'NONE',  ( 0.8714495147512549833, -0.2914478312704605889, 1.939986204769503786 ) ) ;
#196267=CARTESIAN_POINT ( 'NONE',  ( 5.067260671706765862, 1.791893645760339826, 1.021364248522889762 ) ) ;
#196274=CARTESIAN_POINT ( 'NONE',  ( 0.4093307213487142326, -1.744552795675001100, 1.292164652415381365 ) ) ;
#196279=CARTESIAN_POINT ( 'NONE',  ( 0.8076147168173102298, -1.862120749842037570, 0.1771838942275505424 ) ) ;
#196280=CARTESIAN_POINT ( 'NONE',  ( 5.694645791630270182, -0.5191100231263061637, -2.098234375727751733 ) ) ;
#196282=CARTESIAN_POINT ( 'NONE',  ( -0.02244404828157658613, 7.629137130509074716, -2.789100637983293662 ) ) ;
#196284=CARTESIAN_POINT ( 'NONE',  ( 1.980978873585538480, -1.748965405663160944, -0.7736543689686598002 ) ) ;
#196285=CARTESIAN_POINT ( 'NONE',  ( 3.361912448646987794, 0.7947379027260987883, 1.581431320561203169 ) ) ;
#196286=CARTESIAN_POINT ( 'NONE',  ( 0.3461628310420067911, 0.9829124436787042285, -1.640176041098049264 ) ) ;
#196289=CARTESIAN_POINT ( 'NONE',  ( 5.501554071977204252, -1.867810700675033297, 0.4244617614653464766 ) ) ;
#196290=CARTESIAN_POINT ( 'NONE',  ( 6.373500198570408060, -0.2424619166165129514, 1.954513512140013676 ) ) ;
#196292=CARTESIAN_POINT ( 'NONE',  ( 0.5102161431939798986, -0.7575819503438313562, 1.980855387931411915 ) ) ;
#196293=CARTESIAN_POINT ( 'NONE',  ( 4.592568387165754551, -0.4099775813008778025, -1.825014511474598589 ) ) ;
#196294=CARTESIAN_POINT ( 'NONE',  ( 0.5393321728033516615, -1.288848960320065462, -1.293324666950084190 ) ) ;
#196296=CARTESIAN_POINT ( 'NONE',  ( 4.530015419921377351, -1.356323209173672106, -1.740806116466916409 ) ) ;
#196300=CARTESIAN_POINT ( 'NONE',  ( 2.313000242259897199, -1.596077997345384247, 1.306617308116851062 ) ) ;
#196310=CARTESIAN_POINT ( 'NONE',  ( 4.369627354678314646, -0.3570511267821044332, 2.039192500141631115 ) ) ;
#196312=CARTESIAN_POINT ( 'NONE',  ( 1.159701560084012595, 0.4228694819443152286, -2.119656415666733906 ) ) ;
#196314=CARTESIAN_POINT ( 'NONE',  ( 2.192062543670767027, 1.244387780127395482, 1.590672870423719187 ) ) ;
#196317=CARTESIAN_POINT ( 'NONE',  ( 0.07479286986305545837, 0.7422478802248284602, -1.939684878352589070 ) ) ;
#196321=CARTESIAN_POINT ( 'NONE',  ( 0.6027503803631119039, 1.865048444749048739, 0.7672877736318934883 ) ) ;
#196322=CARTESIAN_POINT ( 'NONE',  ( 5.161759341795384870, 1.079763445194487970, 1.907048802792680631 ) ) ;
#196324=CARTESIAN_POINT ( 'NONE',  ( 5.062724140118718630, 0.5608846916410530348, 1.828269531156314631 ) ) ;
#196328=CARTESIAN_POINT ( 'NONE',  ( 2.179314750421776026, 1.560514648525725967, 1.277027416600539755 ) ) ;
#196330=CARTESIAN_POINT ( 'NONE',  ( 0.4863598079122740114, -2.275998871909711951, -0.2730087134108442615 ) ) ;
#196332=CARTESIAN_POINT ( 'NONE',  ( 4.647282941162062642, -1.334376716645750971, -1.092789356466111972 ) ) ;
#196333=CARTESIAN_POINT ( 'NONE',  ( -0.1399997263889594112, -0.002789056014654289761, -2.000146600338557956 ) ) ;
#196336=FACE_OUTER_BOUND ( 'NONE', #28540, .T. ) ;
#196338=DIRECTION ( 'NONE',  ( 1.214306433183764966E-17, 1.000000000000000000, 5.200009205990155575E-32 ) ) ;
#196340=CARTESIAN_POINT ( 'NONE',  ( 5.531847899045232886, -1.765878665049234186, 0.4030928165594855339 ) ) ;
#196346=CARTESIAN_POINT ( 'NONE',  ( 6.164714480961021259, 0.5753438643430182076, 1.717747506070513852 ) ) ;
#196349=CARTESIAN_POINT ( 'NONE',  ( 2.677880624963273171, -1.125664371729949265, 1.880105217535378959 ) ) ;
#196350=CARTESIAN_POINT ( 'NONE',  ( 6.127394093140170916, 0.1359088500606409067, -1.856169418941427729 ) ) ;
#196352=CARTESIAN_POINT ( 'NONE',  ( 3.655789272196503514, 1.066996606607173659, 1.590710377612122750 ) ) ;
#196355=CARTESIAN_POINT ( 'NONE',  ( 0.2333690889706726279, 7.629137130509075604, -2.653349640194931247 ) ) ;
#196359=CARTESIAN_POINT ( 'NONE',  ( 1.534274790466340299, 1.065227450066742687, -1.880959520452238465 ) ) ;
#196363=CARTESIAN_POINT ( 'NONE',  ( 2.449991753796490368, 1.825138167369045661, 0.04731899098397300552 ) ) ;
#196365=CARTESIAN_POINT ( 'NONE',  ( 3.873894609034499226, 1.013791609252197690, 1.518000939925365778 ) ) ;
#196367=CARTESIAN_POINT ( 'NONE',  ( 2.478646075381494285, -1.315928518397539548, 1.387899491812602859 ) ) ;
#196369=CARTESIAN_POINT ( 'NONE',  ( 4.264079249230395163, -1.964438661470244263, 0.1424843695872201332 ) ) ;
#196371=CARTESIAN_POINT ( 'NONE',  ( 4.511236532831874868, -1.903902423773628838, 0.3822933785788319438 ) ) ;
#196375=CARTESIAN_POINT ( 'NONE',  ( 4.746395313581045272, 1.087821826000658909, -1.820160695957805608 ) ) ;
#196382=CARTESIAN_POINT ( 'NONE',  ( 3.598294619042395226, -0.9903900195140210583, 1.752531985089557098 ) ) ;
#196384=CARTESIAN_POINT ( 'NONE',  ( 4.969292227364340953, 0.1756445257206709631, -1.817221496977147854 ) ) ;
#196385=CARTESIAN_POINT ( 'NONE',  ( 1.152881054890652957, -0.5012615762394446728, -2.008655542368184221 ) ) ;
#196389=CARTESIAN_POINT ( 'NONE',  ( 5.893391625361731556, 1.417579469995243091, 1.220656814419220249 ) ) ;
#196398=CARTESIAN_POINT ( 'NONE',  ( 1.358353136502856939, -2.070434559563800736, -0.003889755252693693176 ) ) ;
#196399=CARTESIAN_POINT ( 'NONE',  ( 2.618900020153229757, 0.2622993368636802325, 2.100875384797147305 ) ) ;
#196402=CARTESIAN_POINT ( 'NONE',  ( 0.6023233765659050665, 1.963792105354182249, 0.1503755929508752975 ) ) ;
#196407=CARTESIAN_POINT ( 'NONE',  ( 2.396762456488350956, 1.839990291603439632, -1.366890742103431755 ) ) ;
#196408=CARTESIAN_POINT ( 'NONE',  ( 0.4865809202317071813, -0.2202831055867389420, -1.812292406919484344 ) ) ;
#196409=CARTESIAN_POINT ( 'NONE',  ( 1.933716311909071006, -1.854087253938462521, 0.4680378644332866545 ) ) ;
#196412=CARTESIAN_POINT ( 'NONE',  ( 1.635022589147613115, 1.879998146294536543, 0.7206230416607807276 ) ) ;
#196413=CARTESIAN_POINT ( 'NONE',  ( 1.235121763443976395, -0.04261391538399812023, -1.961451400788959631 ) ) ;
#196418=CARTESIAN_POINT ( 'NONE',  ( 3.626972257435066460, -1.931581639804475614, 0.8003350836045771688 ) ) ;
#196419=CARTESIAN_POINT ( 'NONE',  ( 2.061070876156974041, 0.3059375065844106012, -1.743026645166842803 ) ) ;
#196422=CARTESIAN_POINT ( 'NONE',  ( 5.455124386806871506, 0.4517125544712205509, -2.247162937307800590 ) ) ;
#196423=CARTESIAN_POINT ( 'NONE',  ( 4.206796582046585797, -0.2943472477981134428, 1.715077512146965688 ) ) ;
#196426=CARTESIAN_POINT ( 'NONE',  ( 4.376141123711778214, -0.2964218048276610618, 1.708115672221988346 ) ) ;
#196427=CARTESIAN_POINT ( 'NONE',  ( 4.387298408599741961, 0.1025060220480543544, 2.168864852262440301 ) ) ;
#196429=CARTESIAN_POINT ( 'NONE',  ( 5.260953973667149342, -0.05432152012316109058, -2.015980820358989511 ) ) ;
#196430=CARTESIAN_POINT ( 'NONE',  ( 0.2187500114561492792, -0.7852927567033060052, 1.895863743164095894 ) ) ;
#196433=CARTESIAN_POINT ( 'NONE',  ( 3.592722855893375478, -0.3746021097269113809, -1.889456300395859989 ) ) ;
#196435=CARTESIAN_POINT ( 'NONE',  ( 5.484718290073375080, -1.409174384840453653, 1.717275654355006509 ) ) ;
#196437=CARTESIAN_POINT ( 'NONE',  ( 6.883263157960373135, 2.058310207169287143, 2.252834201749584153 ) ) ;
#196440=CARTESIAN_POINT ( 'NONE',  ( 1.295894383074674749, 2.050542657126565249, -0.8545418985851579441 ) ) ;
#196449=CARTESIAN_POINT ( 'NONE',  ( 3.842276591979614242, -1.019319043456867524, 1.793165911747495844 ) ) ;
#196453=CARTESIAN_POINT ( 'NONE',  ( 6.766881895623299670, -1.710433013466134744, -0.7576501205904457859 ) ) ;
#196454=CARTESIAN_POINT ( 'NONE',  ( 5.344279299745758216, 0.3302840285365048478, -1.702201177978326818 ) ) ;
#196455=CARTESIAN_POINT ( 'NONE',  ( 4.774825072940077852, 1.621577360410943802, -0.6326411939767513370 ) ) ;
#196457=CARTESIAN_POINT ( 'NONE',  ( 3.404133285375851248, -0.9304739769722850662, -2.095221664589861810 ) ) ;
#196459=CARTESIAN_POINT ( 'NONE',  ( 1.025062291269123405, -1.166378923895025510, -1.424538887614942739 ) ) ;
#196462=CARTESIAN_POINT ( 'NONE',  ( 1.606192798902779328, -0.6535759462080005244, -1.704761432720684144 ) ) ;
#196463=CARTESIAN_POINT ( 'NONE',  ( 2.760388869050140137, 1.913803604375517109, -0.6351994527180188088 ) ) ;
#196464=CARTESIAN_POINT ( 'NONE',  ( 1.447511513890851864, 0.6336015447323711802, -2.097855558553712640 ) ) ;
#196466=CARTESIAN_POINT ( 'NONE',  ( 4.120224405726905736, -1.080582774747363306, -1.807441255628852828 ) ) ;
#196469=CARTESIAN_POINT ( 'NONE',  ( 1.223191768902037957, -1.870915810643185795, -0.8869332102946840823 ) ) ;
#196472=CARTESIAN_POINT ( 'NONE',  ( 3.633539341399088407, -0.1543397204060332761, 2.114911865293423787 ) ) ;
#196474=CARTESIAN_POINT ( 'NONE',  ( 0.3813102713988948955, 1.798072043455358981, -0.6920631024385316410 ) ) ;
#196481=CARTESIAN_POINT ( 'NONE',  ( 3.375264624815476289, -1.783316433176849625, -0.9482593927577113169 ) ) ;
#196482=CARTESIAN_POINT ( 'NONE',  ( 0.9562493570349944738, 2.103547740682055966, -0.1031677049159150372 ) ) ;
#196485=CARTESIAN_POINT ( 'NONE',  ( 5.506657433377460720, 0.5384353192533465338, 1.781376027434707687 ) ) ;
#196490=CARTESIAN_POINT ( 'NONE',  ( 0.08116279290028630133, -0.1557560750096824431, -2.127278773206460638 ) ) ;
#196494=CARTESIAN_POINT ( 'NONE',  ( 2.407222047678575283, 0.3756278383273171095, 1.692465640204628974 ) ) ;
#196495=CARTESIAN_POINT ( 'NONE',  ( 1.060061488152568510, -1.571881217706198042, -0.7472303940359821262 ) ) ;
#196496=CARTESIAN_POINT ( 'NONE',  ( 6.112023189137078205, -2.291079414021851779, 0.2760875835842706016 ) ) ;
#196499=CARTESIAN_POINT ( 'NONE',  ( 2.600915689618611193, 1.657045147975671817, -1.224973224035642794 ) ) ;
#196502=CARTESIAN_POINT ( 'NONE',  ( 1.089219988750099732, 1.203171814842165288, -1.617568698395126292 ) ) ;
#196505=CARTESIAN_POINT ( 'NONE',  ( 0.7253841367629434433, -1.872807053274931244, 0.6160819575430801498 ) ) ;
#196506=CARTESIAN_POINT ( 'NONE',  ( 4.500206361630255003, -0.8965733778899236395, 1.689174240301967389 ) ) ;
#196508=CARTESIAN_POINT ( 'NONE',  ( 5.865903189996044098, 2.174886565178067777, -0.3735607071253948530 ) ) ;
#196512=CARTESIAN_POINT ( 'NONE',  ( 6.639320575229281651, -0.0007625845807879281287, 2.103388539994067497 ) ) ;
#196514=CARTESIAN_POINT ( 'NONE',  ( 4.717980713983113361, -2.264103904663441913, 0.4450920570577068247 ) ) ;
#196515=CARTESIAN_POINT ( 'NONE',  ( 5.723093114104088386, -1.772945450647535948, -0.8403097561825512152 ) ) ;
#196516=CARTESIAN_POINT ( 'NONE',  ( 2.008577182894935476, 0.6104510041588117053, 1.864461945915835583 ) ) ;
#196520=CARTESIAN_POINT ( 'NONE',  ( 0.4095560439901060334, -2.008447366592306604, 0.6704124886842844910 ) ) ;
#196523=CARTESIAN_POINT ( 'NONE',  ( 0.8140990769837241903, 1.700254657383608814, 0.7068247239481674216 ) ) ;
#196524=ORIENTED_EDGE ( 'NONE', *, *, #202148, .F. ) ;
#196525=CARTESIAN_POINT ( 'NONE',  ( 3.819318941869216388, -1.912159422281418220, -1.028266076255865968 ) ) ;
#196527=CARTESIAN_POINT ( 'NONE',  ( 1.846092968827160119, -1.388944967848893430, -1.602481653760478020 ) ) ;
#196532=CARTESIAN_POINT ( 'NONE',  ( 3.743479925124373331, -1.557965094614376378, -1.348979221448711519 ) ) ;
#196534=CARTESIAN_POINT ( 'NONE',  ( 0.8195642880178370948, 1.096917009463085790, -1.478703137254427924 ) ) ;
#196538=CARTESIAN_POINT ( 'NONE',  ( -0.02244404828157658613, -0.004869073801674199918, -2.189079685368473527 ) ) ;
#196539=CARTESIAN_POINT ( 'NONE',  ( 1.230147817042701375, -1.435374304221140651, -1.748800500726248153 ) ) ;
#196541=CARTESIAN_POINT ( 'NONE',  ( 1.248006495514828895, 0.8912474588982389756, -1.577060073313638622 ) ) ;
#196543=CARTESIAN_POINT ( 'NONE',  ( 1.516650397601801759, 0.1914660871255029484, 1.906153142492900132 ) ) ;
#196544=CARTESIAN_POINT ( 'NONE',  ( 2.963400493335893948, 1.747644659881589568, 1.109742091278065113 ) ) ;
#196546=CARTESIAN_POINT ( 'NONE',  ( 1.340630715518615679, 0.3825088487559283323, 1.933841885654476567 ) ) ;
#196547=CARTESIAN_POINT ( 'NONE',  ( 5.162690889178682241, -1.394081347390314640, 1.329872870702011545 ) ) ;
#196548=CARTESIAN_POINT ( 'NONE',  ( 0.8566255916394946990, 2.304767657353411270, -0.1186049529825431298 ) ) ;
#196551=CARTESIAN_POINT ( 'NONE',  ( 5.459457826130150515, 1.684308464339222100, 1.190431669587647567 ) ) ;
#196555=CARTESIAN_POINT ( 'NONE',  ( 6.106491565043327796, -0.7546634490227432934, -1.966289716088761796 ) ) ;
#196557=CARTESIAN_POINT ( 'NONE',  ( 5.132170659515546518, 1.116069247042193124, -1.851066442873222639 ) ) ;
#196558=CARTESIAN_POINT ( 'NONE',  ( 0.9250624443557056154, -1.167992581197497604, -1.423340509374780405 ) ) ;
#196559=CARTESIAN_POINT ( 'NONE',  ( 5.004559639922408820, -2.004681531738555123, -0.2449335584770311880 ) ) ;
#196567=CARTESIAN_POINT ( 'NONE',  ( 3.257046257486408969, 0.04465439498414420366, -2.016188763087948033 ) ) ;
#196572=CARTESIAN_POINT ( 'NONE',  ( 4.944278945467968533, 2.155654431248493985, 0.1625706239713892443 ) ) ;
#196574=FILL_AREA_STYLE_COLOUR ( '', #82736 ) ;
#196577=CARTESIAN_POINT ( 'NONE',  ( 5.501577430365036214, -1.966641501487207622, 0.4445218866586594930 ) ) ;
#196579=CARTESIAN_POINT ( 'NONE',  ( 1.382971869717847690, 1.594974721182834010, -0.6572114825635144708 ) ) ;
#196584=CARTESIAN_POINT ( 'NONE',  ( 0.3327835722091445070, -1.621720136574826610, 0.7089735832957798634 ) ) ;
#196585=CARTESIAN_POINT ( 'NONE',  ( 0.7506400166778016692, 1.983664654656223991, 0.3420602577784581655 ) ) ;
#196587=CARTESIAN_POINT ( 'NONE',  ( 3.276612781706738087, -1.315965827422488132, 1.771305981150771647 ) ) ;
#196588=CARTESIAN_POINT ( 'NONE',  ( 4.891568528303794849, -1.987603774517988642, 0.8738605845971869623 ) ) ;
#196591=CARTESIAN_POINT ( 'NONE',  ( 2.262495435604610527, 2.120074037919957632, 0.04929290001921824566 ) ) ;
#196592=CARTESIAN_POINT ( 'NONE',  ( 1.915638884950950027, -1.319244919589783516, -1.525031147761625405 ) ) ;
#196593=CARTESIAN_POINT ( 'NONE',  ( 1.792921450925293536, -0.09139298786187435852, -1.809423198457478676 ) ) ;
#196598=CARTESIAN_POINT ( 'NONE',  ( 1.745192250125559008, 0.3234662751879986975, -1.888026716711376674 ) ) ;
#196608=CARTESIAN_POINT ( 'NONE',  ( 4.733375416736937069, -1.977748744329570263, 0.8730265686548792647 ) ) ;
#196612=CARTESIAN_POINT ( 'NONE',  ( 1.441811196653530747, -1.994930912159533554, 0.7194735443712959588 ) ) ;
#196613=CARTESIAN_POINT ( 'NONE',  ( -0.1298852118744101003, 4.098067735550426249, -2.281510303361510061 ) ) ;
#196614=CARTESIAN_POINT ( 'NONE',  ( 2.759003776822867238, -1.713332664616385781, -0.9749793123631170788 ) ) ;
#196615=CARTESIAN_POINT ( 'NONE',  ( 5.150612376422202487, 1.885107930906554152, 0.3209214958604587054 ) ) ;
#196618=CARTESIAN_POINT ( 'NONE',  ( 0.2915762745691782287, -1.893489616766583339, 0.8377075429084477332 ) ) ;
#196619=CARTESIAN_POINT ( 'NONE',  ( 2.044773883198697462, -1.559800846558807130, -1.156617037343915966 ) ) ;
#196624=CARTESIAN_POINT ( 'NONE',  ( 2.625039678221803729, -1.950394636745816701, 0.7532777691767779116 ) ) ;
#196627=CARTESIAN_POINT ( 'NONE',  ( 5.865855438783555087, 0.5507134639845879809, -1.831277125143706552 ) ) ;
#196629=CARTESIAN_POINT ( 'NONE',  ( 4.231241840954825584, 0.1069408422738199749, 2.204416794138922331 ) ) ;
#196630=CARTESIAN_POINT ( 'NONE',  ( 2.538337413235943973, 1.040872164564849767, -1.945885072647230318 ) ) ;
#196632=CARTESIAN_POINT ( 'NONE',  ( 1.629408300089076889, -0.2329066467734330903, 1.897959532673603844 ) ) ;
#196636=CARTESIAN_POINT ( 'NONE',  ( 4.545415791725802457, 1.850806902094417783, -0.9279678557222793556 ) ) ;
#196638=CARTESIAN_POINT ( 'NONE',  ( 1.253037233087474611, -1.703760181015579134, 1.330383891403746688 ) ) ;
#196639=CARTESIAN_POINT ( 'NONE',  ( 3.913774547416096095, -1.127657808996849198, -1.879056921112078893 ) ) ;
#196646=CARTESIAN_POINT ( 'NONE',  ( 6.604150274805285825, -0.1349072972122930258, 1.703313905121685456 ) ) ;
#196648=CARTESIAN_POINT ( 'NONE',  ( 4.469627305733424372, -0.3590069766891256231, 2.038746214588673666 ) ) ;
#196649=CARTESIAN_POINT ( 'NONE',  ( 3.598194957300792307, -1.924334687528261201, -0.09379112422614949152 ) ) ;
#196650=CARTESIAN_POINT ( 'NONE',  ( 5.448860601978118723, -1.914358274237770496, -0.9046119500179942152 ) ) ;
#196653=CARTESIAN_POINT ( 'NONE',  ( 3.819166351039466001, -1.734870831597424612, -0.9322225710242746377 ) ) ;
#196654=CARTESIAN_POINT ( 'NONE',  ( 6.298803545911215274, 1.902247386433516541, 1.278772944020603930 ) ) ;
#196655=CARTESIAN_POINT ( 'NONE',  ( 4.283705427790140519, 1.194290084605063251, 1.380960126487425166 ) ) ;
#196661=CARTESIAN_POINT ( 'NONE',  ( 4.939702229944241907, -1.910329301133410151, 0.6354416197995541582 ) ) ;
#196662=CARTESIAN_POINT ( 'NONE',  ( 0.2987795159231512176, -2.099866535080958663, 0.9347484894880775386 ) ) ;
#196663=CARTESIAN_POINT ( 'NONE',  ( 4.469553177461598636, -0.3394721387663233170, 1.932013773527320843 ) ) ;
#196669=CARTESIAN_POINT ( 'NONE',  ( 0.6618065864371965867, 1.033746398093362773, 1.817239694416083795 ) ) ;
#196670=CARTESIAN_POINT ( 'NONE',  ( 6.666889860676148416, -1.620333765578816587, -0.7124167289687727278 ) ) ;
#196672=CARTESIAN_POINT ( 'NONE',  ( 6.228462243142912413, 0.1929387083638624822, 1.932343765256574697 ) ) ;
#196673=CARTESIAN_POINT ( 'NONE',  ( -0.1102773484824119132, 0.6802821481026833927, -2.283667859588431881 ) ) ;
#196674=CARTESIAN_POINT ( 'NONE',  ( 1.258879523317941285, 1.714807473692409268, -0.2965960235774521836 ) ) ;
#196678=CARTESIAN_POINT ( 'NONE',  ( 1.382971869717847690, 1.594974721182834010, -0.6572114825635144708 ) ) ;
#196679=CARTESIAN_POINT ( 'NONE',  ( 1.751786407749492014, 2.185395279939935431, -0.1653414253460702699 ) ) ;
#196680=CARTESIAN_POINT ( 'NONE',  ( 6.889999999999967706, 0.005249217920031550542, 1.719840535937327664 ) ) ;
#196681=CARTESIAN_POINT ( 'NONE',  ( 4.301547675229603129, 1.771612934706376707, 1.315755017190944676 ) ) ;
#196682=CARTESIAN_POINT ( 'NONE',  ( 1.534277631021633059, 1.291084678180357104, 1.745351423456573015 ) ) ;
#196683=CARTESIAN_POINT ( 'NONE',  ( 0.2404813148422607627, 0.3085585699703840556, 1.799268721412583316 ) ) ;
#196684=CARTESIAN_POINT ( 'NONE',  ( 2.518900147204519158, 0.2643050731806431686, 2.100751150841919657 ) ) ;
#196688=CARTESIAN_POINT ( 'NONE',  ( 3.017397247018727580, -2.208655522623126366, 0.6135670354654331193 ) ) ;
#196692=CARTESIAN_POINT ( 'NONE',  ( 4.688250436721117964, 1.278455086129190121, 1.816331037743470933 ) ) ;
#196699=CARTESIAN_POINT ( 'NONE',  ( 2.408827471728996361, -1.163269702728772392, -1.646838680093346996 ) ) ;
#196701=CARTESIAN_POINT ( 'NONE',  ( 1.850508050571671559, -2.052242141108654661, -0.2064673365099172486 ) ) ;
#196706=CARTESIAN_POINT ( 'NONE',  ( 4.558633756138521065, -1.956834287480881063, -0.9866608250781592204 ) ) ;
#196707=CARTESIAN_POINT ( 'NONE',  ( 2.531875153343257523, -1.674887184936912909, 1.122499117612890673 ) ) ;
#196708=CARTESIAN_POINT ( 'NONE',  ( 0.5207438388301621757, -1.748553680932497745, 0.5769860859521497298 ) ) ;
#196710=CARTESIAN_POINT ( 'NONE',  ( 4.911078036072877850, 1.588895129109271220, 0.8988584441092376531 ) ) ;
#196711=CARTESIAN_POINT ( 'NONE',  ( 6.188124994278807023, 1.678003296889327034, 1.117835524071027598 ) ) ;
#196713=CARTESIAN_POINT ( 'NONE',  ( 4.663087558633967511, -2.018941045467276929, -1.021363250454855764 ) ) ;
#196715=CARTESIAN_POINT ( 'NONE',  ( 1.207801281821162975, -0.5101631384078918474, 2.043215687033891559 ) ) ;
#196717=CARTESIAN_POINT ( 'NONE',  ( 4.896967953096117654, 0.3505727482827174502, 2.040303948762006492 ) ) ;
#196727=CARTESIAN_POINT ( 'NONE',  ( 1.547299434221154124, 0.2130619955753136618, 2.109896976817266179 ) ) ;
#196728=CARTESIAN_POINT ( 'NONE',  ( 1.898975720090949837, -2.179683001098455808, -0.4277757613022105110 ) ) ;
#196732=CARTESIAN_POINT ( 'NONE',  ( 3.191801227909254912, -1.315628469008291557, -1.455533501494077342 ) ) ;
#196739=CARTESIAN_POINT ( 'NONE',  ( 2.496466685713152334, -1.086271176545396067, 1.821091972856798913 ) ) ;
#196741=CARTESIAN_POINT ( 'NONE',  ( 5.740667459973674447, -1.913685094937540132, -0.4313615418530327150 ) ) ;
#196742=CARTESIAN_POINT ( 'NONE',  ( 3.555696680978126079, 0.5271953485486252644, -2.096301903996622862 ) ) ;
#196743=CARTESIAN_POINT ( 'NONE',  ( 3.350949008998193257, 0.4442310927498266948, -1.786741727165648497 ) ) ;
#196746=CARTESIAN_POINT ( 'NONE',  ( 6.228409164912255491, 0.1778687648950585953, 1.731214608917114317 ) ) ;
#196750=CARTESIAN_POINT ( 'NONE',  ( 2.887745953747706373, 1.527789104365802286, 1.529575784674996886 ) ) ;
#196752=CARTESIAN_POINT ( 'NONE',  ( 4.833361152654930493, -1.319026006086077230, 1.524810761284051575 ) ) ;
#196755=CARTESIAN_POINT ( 'NONE',  ( 1.885829143180400624, 1.490600019384461072, 1.565824011241300440 ) ) ;
#196756=CARTESIAN_POINT ( 'NONE',  ( 2.618384893494442256, 1.290362544248652599, -1.490430290494165755 ) ) ;
#196758=CARTESIAN_POINT ( 'NONE',  ( 4.071774441262452804, -1.115447612638842401, 1.589602391900000411 ) ) ;
#196766=CARTESIAN_POINT ( 'NONE',  ( 1.378255502416312117, 1.315327575222959622, 1.771799650011764538 ) ) ;
#196768=CARTESIAN_POINT ( 'NONE',  ( 5.436364959771895045, -1.092926877770916017, 1.628904810760459121 ) ) ;
#196771=CARTESIAN_POINT ( 'NONE',  ( 0.1745949693968328054, 4.098633874596197657, -2.310325329485760637 ) ) ;
#196772=CARTESIAN_POINT ( 'NONE',  ( 4.751808913491627706, 0.7073710267669359730, 1.700028372310140368 ) ) ;
#196776=CARTESIAN_POINT ( 'NONE',  ( 4.904590598983499916, -2.104870323260544129, -0.2570220051709286579 ) ) ;
#196780=CARTESIAN_POINT ( 'NONE',  ( 6.784453644556415419, -2.020073987206136401, -0.4066529033334795873 ) ) ;
#196783=CARTESIAN_POINT ( 'NONE',  ( 0.9064450206472760563, 0.5352286137044174330, 1.782442419352270102 ) ) ;
#196784=CARTESIAN_POINT ( 'NONE',  ( 3.561895345837225779, -1.234009368583251387, 1.366721199326895952 ) ) ;
#196789=CARTESIAN_POINT ( 'NONE',  ( 3.475398437264758833, 0.05438942809191970457, -2.206374867412825402 ) ) ;
#196790=CARTESIAN_POINT ( 'NONE',  ( 5.325545376182048152, -2.150690057981026193, 0.7024452394915041697 ) ) ;
#196792=CARTESIAN_POINT ( 'NONE',  ( 6.310821775929002619, -0.4926439853468951857, -1.743236492463080767 ) ) ;
#196793=CARTESIAN_POINT ( 'NONE',  ( 5.313669575012682778, -1.220653882476211427, -1.476441452469556159 ) ) ;
#196795=CARTESIAN_POINT ( 'NONE',  ( 5.858239598252557911, 0.7595784280203803362, 1.709674162104061645 ) ) ;
#196797=CARTESIAN_POINT ( 'NONE',  ( 6.250447302982959030, -1.852220608400175994, -0.1812639614414724432 ) ) ;
#196798=CARTESIAN_POINT ( 'NONE',  ( 6.596581986989779267, -0.4770763175313968429, -1.704276504685025673 ) ) ;
#196799=CARTESIAN_POINT ( 'NONE',  ( 1.147673126774436225, 1.985868168208399842, -0.3494872464938902357 ) ) ;
#196801=CARTESIAN_POINT ( 'NONE',  ( 2.965558217497352267, 0.3084109246280877237, -2.083234000326895430 ) ) ;
#196806=CARTESIAN_POINT ( 'NONE',  ( 1.986587785418312047, -1.239364722674634933, 1.594781737346209871 ) ) ;
#196810=CARTESIAN_POINT ( 'NONE',  ( 2.864712396292764751, -1.492883925411473856, 1.563474562115530375 ) ) ;
#196811=CARTESIAN_POINT ( 'NONE',  ( 6.890000000000037872, 2.400824642991986391, 2.659875214078717853 ) ) ;
#196819=CARTESIAN_POINT ( 'NONE',  ( 1.206853476500208133, 1.935082376036290075, 1.028754739392373496 ) ) ;
#196821=CARTESIAN_POINT ( 'NONE',  ( 2.958202477073975878, 2.251720482184274008, -0.2206431264100849887 ) ) ;
#196829=CARTESIAN_POINT ( 'NONE',  ( 2.934531203469164851, 0.2125141484592401875, 1.756833830538252483 ) ) ;
#196830=CARTESIAN_POINT ( 'NONE',  ( 6.299877592275240801, -0.7493655176046759570, 2.075778730795534877 ) ) ;
#196834=CARTESIAN_POINT ( 'NONE',  ( 5.273064617572334356, 1.777004185780726386, -0.9530273427700783895 ) ) ;
#196835=CARTESIAN_POINT ( 'NONE',  ( 4.974790932252576958, -1.306838681284767212, 1.254843474919357105 ) ) ;
#196837=CARTESIAN_POINT ( 'NONE',  ( 2.377632874612686020, 1.149002834218125102, 1.476114537088555112 ) ) ;
#196838=CARTESIAN_POINT ( 'NONE',  ( 3.590741003927796271, 2.018730135711533258, 0.4582614309688318732 ) ) ;
#196840=CARTESIAN_POINT ( 'NONE',  ( 2.513799616133075343, -0.5961229146635020903, 1.817204401178821760 ) ) ;
#196846=CARTESIAN_POINT ( 'NONE',  ( 1.037202349414727109, -0.04413313863061394532, 1.912034500058952036 ) ) ;
#196847=CARTESIAN_POINT ( 'NONE',  ( 2.295295855072278624, -1.753792786583353580, 0.8793850528211948347 ) ) ;
#196849=CARTESIAN_POINT ( 'NONE',  ( 0.5267199648841465187, 1.994564833640038781, -0.2930222482238133419 ) ) ;
#196852=CARTESIAN_POINT ( 'NONE',  ( 0.2626887844769665303, -1.667795467377327423, -0.8471929967568125885 ) ) ;
#196855=CARTESIAN_POINT ( 'NONE',  ( 2.654045540373184409, 1.135223644230592743, 1.786994778491631797 ) ) ;
#196857=CARTESIAN_POINT ( 'NONE',  ( 3.789561645344252661, -1.914057400617325433, 0.7896510022299551013 ) ) ;
#196859=CARTESIAN_POINT ( 'NONE',  ( 6.052696072153842977, -1.792546385985850810, -1.075631278504029620 ) ) ;
#196861=CARTESIAN_POINT ( 'NONE',  ( 4.559475717982610199, 0.3993622990657343941, -1.781190812766835441 ) ) ;
#196866=CARTESIAN_POINT ( 'NONE',  ( 6.668967514498191029, -2.014860697535350020, -0.9005387006749266954 ) ) ;
#196869=CARTESIAN_POINT ( 'NONE',  ( 5.039673278062164918, -1.814583965733532978, 0.6035816954967700987 ) ) ;
#196877=CARTESIAN_POINT ( 'NONE',  ( 0.5382993156314471728, -1.579489783069366604, 0.9460463261394757017 ) ) ;
#196880=CARTESIAN_POINT ( 'NONE',  ( 5.149604166610964207, 0.5880212298954893280, -1.775756280894603467 ) ) ;
#196886=CARTESIAN_POINT ( 'NONE',  ( 0.7956772557287052905, -1.388798143503049420, -1.396678344884971112 ) ) ;
#196887=CARTESIAN_POINT ( 'NONE',  ( 2.390250109419411295, -0.7743331304885041622, -1.862010821188607945 ) ) ;
#196891=CARTESIAN_POINT ( 'NONE',  ( 2.203317661949526052, -0.4785072280911427667, 2.138412878249687399 ) ) ;
#196901=CARTESIAN_POINT ( 'NONE',  ( 4.651808992177354440, 0.7092673950449077669, 1.699362209096597187 ) ) ;
#196902=CARTESIAN_POINT ( 'NONE',  ( 1.928386798537110147, -0.9510432213125822321, -1.774292727131807856 ) ) ;
#196903=CARTESIAN_POINT ( 'NONE',  ( 2.654040013917441598, -0.3913916837698909745, -2.264681309554557043 ) ) ;
#196904=CARTESIAN_POINT ( 'NONE',  ( -0.1290005225502433017, 7.629137130509076492, -2.773995091683974401 ) ) ;
#196905=CARTESIAN_POINT ( 'NONE',  ( 1.639267886685547460, 1.721996695667164845, -0.7061035538288776836 ) ) ;
#196908=CARTESIAN_POINT ( 'NONE',  ( 5.941656858135131891, -1.798430535887390658, 0.6506349336675710804 ) ) ;
#196911=CARTESIAN_POINT ( 'NONE',  ( 5.021074897447791230, -1.984789774362485604, 0.6572858584967393725 ) ) ;
#196912=CARTESIAN_POINT ( 'NONE',  ( 3.520239479114236403, 1.187513476551487424, -1.445374034619356207 ) ) ;
#196914=CARTESIAN_POINT ( 'NONE',  ( 5.987831981441136264, -1.833028718050220940, -0.1737628300680846560 ) ) ;
#196918=CARTESIAN_POINT ( 'NONE',  ( 4.635198054048816019, -1.575417825122129134, 0.7027606912313691945 ) ) ;
#196920=CARTESIAN_POINT ( 'NONE',  ( 0.7383815455153321938, 1.732312080274291732, -0.08293238807991276662 ) ) ;
#196925=CARTESIAN_POINT ( 'NONE',  ( 4.856392247755495717, -2.170420479375735123, -0.05992511257937349622 ) ) ;
#196926=CARTESIAN_POINT ( 'NONE',  ( 3.615676881913011176, -1.798418494116042821, 0.3134422064149794407 ) ) ;
#196927=CARTESIAN_POINT ( 'NONE',  ( 0.7077677203753615087, 0.6208407433182620005, -1.860969989990405749 ) ) ;
#196928=CARTESIAN_POINT ( 'NONE',  ( 5.542236361656130761, 0.8606211682868989410, 1.934736125387125361 ) ) ;
#196929=CARTESIAN_POINT ( 'NONE',  ( 5.935170609274059039, -1.657740282732190096, -1.583558971889464706 ) ) ;
#196933=CARTESIAN_POINT ( 'NONE',  ( 0.9441710812277158693, -1.348169866081018853, -1.636719737310005973 ) ) ;
#196937=CARTESIAN_POINT ( 'NONE',  ( 6.016515519638066856, 0.8726334679417474538, 1.988148615226674298 ) ) ;
#196938=CARTESIAN_POINT ( 'NONE',  ( 6.883263157960390011, 6.036220326785228352, 2.548703601196927515 ) ) ;
#196940=CARTESIAN_POINT ( 'NONE',  ( 2.104415045828517350, -0.9466870704337572162, 2.009588771043930411 ) ) ;
#196942=CARTESIAN_POINT ( 'NONE',  ( 5.818982467333652764, 0.9914020171761170896, -1.755767668913270407 ) ) ;
#196944=CARTESIAN_POINT ( 'NONE',  ( 5.084863090169797317, 1.972218467801799102, 0.6036872243675943661 ) ) ;
#196949=CARTESIAN_POINT ( 'NONE',  ( 0.2329586101569528500, 5.725166970077667727, -2.439795138137319963 ) ) ;
#196950=CARTESIAN_POINT ( 'NONE',  ( 4.897927690869709139, -0.6253142351902387652, -1.731941863025769246 ) ) ;
#196953=CARTESIAN_POINT ( 'NONE',  ( -0.2104748580754391973, 0.7011259924453935310, -2.185273273056092425 ) ) ;
#196954=CARTESIAN_POINT ( 'NONE',  ( 1.412684849630441386, 1.518645404226389051, 0.8176530575639671117 ) ) ;
#196955=CARTESIAN_POINT ( 'NONE',  ( 0.07540816263147330500, 1.497505997221737495, 1.350731191893522976 ) ) ;
#196956=CARTESIAN_POINT ( 'NONE',  ( 1.969760627029959688, -2.255332599139341809, -0.4437108664413855763 ) ) ;
#196958=CARTESIAN_POINT ( 'NONE',  ( 1.616897013105462522, 1.519709519468028791, -1.676125853178417113 ) ) ;
#196959=CARTESIAN_POINT ( 'NONE',  ( 3.949915024511057471, 0.7098439763573929362, -1.982976504383345162 ) ) ;
#196961=CARTESIAN_POINT ( 'NONE',  ( 2.196244507144041513, -0.4668761045134894871, -1.706985182271273382 ) ) ;
#196967=CARTESIAN_POINT ( 'NONE',  ( 6.451452576676337536, -1.984925862664425500, 0.9976300440488919952 ) ) ;
#196968=CARTESIAN_POINT ( 'NONE',  ( 3.539196308827243787, -1.659330947522210886, -1.431560661003590695 ) ) ;
#196971=CARTESIAN_POINT ( 'NONE',  ( 6.410795937096152919, -0.5649949523399040441, -2.043744576961013859 ) ) ;
#196975=CARTESIAN_POINT ( 'NONE',  ( 5.888958097455845753, -2.014202512972632420, -0.6635655960139997811 ) ) ;
#196980=CARTESIAN_POINT ( 'NONE',  ( 6.620655732516647518, 0.007553340620044743381, 1.826407896915738238 ) ) ;
#196984=CARTESIAN_POINT ( 'NONE',  ( 2.014833872101874146, -1.687939792665555494, 0.4236265878580796618 ) ) ;
#196986=CARTESIAN_POINT ( 'NONE',  ( 0.2737812321212430566, -1.924752420120953822, 0.3788971555385572954 ) ) ;
#196991=CARTESIAN_POINT ( 'NONE',  ( 6.491117449447131982, 1.883434485765375310, -1.060826435891427666 ) ) ;
#196995=CARTESIAN_POINT ( 'NONE',  ( 5.559502693676295237, 0.4258712887980077300, -2.119171757835013548 ) ) ;
#196999=CARTESIAN_POINT ( 'NONE',  ( 6.538353035222548293, 1.949559774641503651, 0.2916953021188176121 ) ) ;
#197000=CARTESIAN_POINT ( 'NONE',  ( 4.938689436542594180, 0.9992198110298566860, 1.416717458774526373 ) ) ;
#197002=CARTESIAN_POINT ( 'NONE',  ( 2.173600921376659834, 1.351110561487681716, 1.725424542402646422 ) ) ;
#197003=CARTESIAN_POINT ( 'NONE',  ( 2.925200879784293218, 2.172439923367448067, 0.7784344579512092466 ) ) ;
#197004=CARTESIAN_POINT ( 'NONE',  ( 5.061820804786828276, 2.038956591669589535, -0.2981446164109917696 ) ) ;
#197005=CARTESIAN_POINT ( 'NONE',  ( 1.007640649619114148, -0.8727987561519714443, -1.734835989144311919 ) ) ;
#197009=CARTESIAN_POINT ( 'NONE',  ( 4.201511661969238531, 1.892856375164463367, -0.9562558712687405649 ) ) ;
#197011=CARTESIAN_POINT ( 'NONE',  ( 2.813125141109920069, 1.117832431973438734, -1.678005364621336426 ) ) ;
#197013=CARTESIAN_POINT ( 'NONE',  ( 4.788207028248289809, -1.043783763870303360, 1.944324211313207318 ) ) ;
#197020=CARTESIAN_POINT ( 'NONE',  ( 4.891509840769978190, 1.525608517091806782, 1.385742337522611223 ) ) ;
#197022=CARTESIAN_POINT ( 'NONE',  ( -0.2108831679770960255, -0.001785917861228669690, -1.896958272444612792 ) ) ;
#197024=CARTESIAN_POINT ( 'NONE',  ( 3.686198542540094714, 1.123799323442754572, 1.677924191584168501 ) ) ;
#197028=CARTESIAN_POINT ( 'NONE',  ( 3.045831416509756195, 0.7432089164593397301, -1.922393172558758634 ) ) ;
#197032=CARTESIAN_POINT ( 'NONE',  ( -0.2408018239684097672, 5.720833683022617855, -2.694520676430669059 ) ) ;
#197034=CARTESIAN_POINT ( 'NONE',  ( 0.9371597039556851527, 0.7481776565299683712, -1.682445429299509909 ) ) ;
#197035=CARTESIAN_POINT ( 'NONE',  ( 0.3644775225865644619, 2.281660525247240834, -0.3449698035877246105 ) ) ;
#197037=CARTESIAN_POINT ( 'NONE',  ( 2.952577552874091626, 0.7252333659365679530, 2.036452211405047397 ) ) ;
#197039=CARTESIAN_POINT ( 'NONE',  ( 2.044158018538293042, 0.8666093899718421145, 1.820985203412978093 ) ) ;
#197040=CARTESIAN_POINT ( 'NONE',  ( 2.759436883174094746, -2.292065780239035178, -0.1713596109048869109 ) ) ;
#197042=CARTESIAN_POINT ( 'NONE',  ( 0.6548940681232479077, -1.578012236938080015, -1.004313744925364071 ) ) ;
#197043=CARTESIAN_POINT ( 'NONE',  ( 5.102397915883716273, -0.6633297369818305089, -1.856656708325474581 ) ) ;
#197044=CARTESIAN_POINT ( 'NONE',  ( 4.434779938697545276, -1.616694733667634942, 1.205040202231235869 ) ) ;
#197048=CARTESIAN_POINT ( 'NONE',  ( 5.760410450299061402, 0.8521563956989952615, 1.926159629354136316 ) ) ;
#197049=CARTESIAN_POINT ( 'NONE',  ( 6.443811375169310907, 1.424792453395683500, 1.502365266013883538 ) ) ;
#197052=CARTESIAN_POINT ( 'NONE',  ( 6.539320575229278454, 0.5749733277502915296, 2.156147827957733742 ) ) ;
#197053=CARTESIAN_POINT ( 'NONE',  ( 5.871354875427445386, -1.734483768580237673, -1.034654692648151464 ) ) ;
#197055=CARTESIAN_POINT ( 'NONE',  ( 2.895503172138352177, 1.978892393434032559, -1.186989842046539234 ) ) ;
#197056=CARTESIAN_POINT ( 'NONE',  ( 1.674751860914457824, 1.388166878297650397, -1.525640323027994683 ) ) ;
#197064=CARTESIAN_POINT ( 'NONE',  ( 4.246645257758387970, -2.146983142244869747, -0.3225670219409969008 ) ) ;
#197067=CARTESIAN_POINT ( 'NONE',  ( 2.401689157922583640, -0.7064633820979376866, -1.700523668893457296 ) ) ;
#197070=CARTESIAN_POINT ( 'NONE',  ( 4.880524338131243312, -0.2681524694418158661, -2.175044001020635331 ) ) ;
#197072=CARTESIAN_POINT ( 'NONE',  ( 5.541944591929171438, 0.9225863094920858654, -2.066052574227566385 ) ) ;
#197078=CARTESIAN_POINT ( 'NONE',  ( 6.872329512321287304, -1.085958120241878877, 1.397742320866280252 ) ) ;
#197079=CARTESIAN_POINT ( 'NONE',  ( 3.861980204584365861, 0.6760143841026149403, -1.896330825423567568 ) ) ;
#197081=CARTESIAN_POINT ( 'NONE',  ( 2.995255089933103854, 1.807040913553149997, -1.081249443666182808 ) ) ;
#197082=CARTESIAN_POINT ( 'NONE',  ( 1.810024464468898309, 1.101340386757416967, -1.567151550741460397 ) ) ;
#197084=CARTESIAN_POINT ( 'NONE',  ( 3.121499051359075239, 0.2915335129191589103, -1.947736612120597455 ) ) ;
#197085=CARTESIAN_POINT ( 'NONE',  ( 0.4791068267422092797, 1.747065859276742072, -0.6691465683838908607 ) ) ;
#197086=CARTESIAN_POINT ( 'NONE',  ( 1.205434515183744226, -1.544416933936803904, -1.209700862059132964 ) ) ;
#197087=CARTESIAN_POINT ( 'NONE',  ( 0.5801457039020865292, 0.9447208859736742070, 1.662703529197881558 ) ) ;
#197093=CARTESIAN_POINT ( 'NONE',  ( 6.719590346122157776, 0.3599300073104904074, -2.038585587018165945 ) ) ;
#197094=CARTESIAN_POINT ( 'NONE',  ( 0.6079806153083644471, 0.6509857562557037625, -1.965403638620793147 ) ) ;
#197099=CARTESIAN_POINT ( 'NONE',  ( 5.901066629635802308, -0.3109326959268610691, -2.097457242586676429 ) ) ;
#197105=CARTESIAN_POINT ( 'NONE',  ( 6.074655751228532630, 1.318658252384183438, -1.452748870126779890 ) ) ;
#197108=CARTESIAN_POINT ( 'NONE',  ( 4.587267430073429963, 1.242536178122002344, -1.587594670648798445 ) ) ;
#197109=CARTESIAN_POINT ( 'NONE',  ( 3.309697661505988986, -1.145383095959727315, -1.535415057543190409 ) ) ;
#197111=CARTESIAN_POINT ( 'NONE',  ( 2.033021410476544943, -1.955939774129427988, 0.9887309579383956049 ) ) ;
#197113=CARTESIAN_POINT ( 'NONE',  ( 3.743291833738107144, -1.414529149469236691, -1.224010458943748603 ) ) ;
#197118=CARTESIAN_POINT ( 'NONE',  ( 5.290659027526918301, 1.602671996148979483, -1.383575156158120878 ) ) ;
#197120=CARTESIAN_POINT ( 'NONE',  ( 1.857086946601906652, 0.3542020299988774545, -2.060351931225719468 ) ) ;
#197122=CARTESIAN_POINT ( 'NONE',  ( 0.9380131109506375520, 1.698111720264935620, 0.3011209518388803241 ) ) ;
#197132=CARTESIAN_POINT ( 'NONE',  ( 1.611653755202663518, -0.6102688749147866520, 1.705724428093706946 ) ) ;
#197136=CARTESIAN_POINT ( 'NONE',  ( 6.539320575229250920, 3.702490941164796379, 2.411252750440337156 ) ) ;
#197142=CARTESIAN_POINT ( 'NONE',  ( 3.402650393365719506, 0.4499446578831092780, 1.805719076957598368 ) ) ;
#197143=CARTESIAN_POINT ( 'NONE',  ( 0.9838322988516207124, -1.915793139027978542, 0.001352086710114385869 ) ) ;
#197144=CARTESIAN_POINT ( 'NONE',  ( 6.686557393816916495, -1.889396554722815758, -0.3748701224956552669 ) ) ;
#197145=CARTESIAN_POINT ( 'NONE',  ( 5.916483165358987328, 0.8355632440216669288, 1.894440869009452300 ) ) ;
#197151=CARTESIAN_POINT ( 'NONE',  ( 4.662928361469391270, 1.524974937183399160, -1.246301010749743199 ) ) ;
#197152=CARTESIAN_POINT ( 'NONE',  ( 1.735180256192244697, 1.979698633766859617, 0.7602586827493148514 ) ) ;
#197156=CARTESIAN_POINT ( 'NONE',  ( 5.736325210887869730, 0.4244523575273988492, 2.149783713274712404 ) ) ;
#197158=CARTESIAN_POINT ( 'NONE',  ( 4.331023931135844940, 0.09395156538319178463, 1.924209479612617235 ) ) ;
#197161=CARTESIAN_POINT ( 'NONE',  ( 0.6455096168876961471, -1.890800792967793686, 1.137844069391671820 ) ) ;
#197167=CARTESIAN_POINT ( 'NONE',  ( 6.280130250669472503, -1.091077088088190372, -1.639371140202023014 ) ) ;
#197168=CARTESIAN_POINT ( 'NONE',  ( 0.9427985035241670531, -1.531986193156938292, -1.193500027965375354 ) ) ;
#197169=CARTESIAN_POINT ( 'NONE',  ( 6.819654193105592732, -1.783474119298094296, 1.449237643660877151 ) ) ;
#197171=CARTESIAN_POINT ( 'NONE',  ( 5.805462856137336480, -1.465901670865896067, -1.146230774367855254 ) ) ;
#197177=CARTESIAN_POINT ( 'NONE',  ( 0.9607770615731696662, -1.983481723135366304, -0.9323335341336475013 ) ) ;
#197181=CARTESIAN_POINT ( 'NONE',  ( 1.471042373949003501, 0.1361147407585860392, -1.820667060309004937 ) ) ;
#197184=CARTESIAN_POINT ( 'NONE',  ( 6.509000000000012776, 6.036089120385641493, 2.694901645009006863 ) ) ;
#197186=CARTESIAN_POINT ( 'NONE',  ( 6.428339884752386268, 1.046657586246093175, -1.495688092090130095 ) ) ;
#197187=CARTESIAN_POINT ( 'NONE',  ( 4.434394140398959294, -1.132915509570767476, 1.601352629973289199 ) ) ;
#197190=CARTESIAN_POINT ( 'NONE',  ( 5.250683377293950294, 2.089169806880130320, 0.3621421040747307973 ) ) ;
#197191=CARTESIAN_POINT ( 'NONE',  ( 4.142245973918059043, 0.5854081421233224836, 2.111838497463234710 ) ) ;
#197193=CARTESIAN_POINT ( 'NONE',  ( 3.133707330959301096, 1.967300496787489639, -0.6450458050009516553 ) ) ;
#197197=CARTESIAN_POINT ( 'NONE',  ( 3.217717873326145117, 2.243214920517083044, 0.5014430322199947554 ) ) ;
#197201=CARTESIAN_POINT ( 'NONE',  ( 6.720655732516647163, 0.002698097948191854455, 1.926293798961113080 ) ) ;
#197203=CARTESIAN_POINT ( 'NONE',  ( 3.292849172082324305, 1.531446531863265736, 1.193990500783614905 ) ) ;
#197206=CARTESIAN_POINT ( 'NONE',  ( 3.586107075002854305, 1.066394011600999780, 1.587261316105821551 ) ) ;
#197208=CARTESIAN_POINT ( 'NONE',  ( 5.034089265250761613, 0.8841871275974706457, -1.480748092288231454 ) ) ;
#197209=CARTESIAN_POINT ( 'NONE',  ( 3.397672961473942266, -1.985868886743065609, 0.3494831190506141883 ) ) ;
#197210=CARTESIAN_POINT ( 'NONE',  ( 4.694093285409329575, 1.999278280869060342, 1.134256664920972213 ) ) ;
#197212=CARTESIAN_POINT ( 'NONE',  ( 1.243116305521356990, 0.4334984505205765060, 2.163720904216937857 ) ) ;
#197214=CARTESIAN_POINT ( 'NONE',  ( 5.887929786387328335, -0.7941975946151798027, 1.581623468068603433 ) ) ;
#197216=CARTESIAN_POINT ( 'NONE',  ( 2.133172796342793998, -2.046422403899459841, 1.032916798664377911 ) ) ;
#197217=CARTESIAN_POINT ( 'NONE',  ( 0.7436347644121766853, 0.5012835123295921180, 1.666554394910790382 ) ) ;
#197223=CARTESIAN_POINT ( 'NONE',  ( 1.627621631281210179, 0.1606834768266463820, -2.165304058017766486 ) ) ;
#197224=CARTESIAN_POINT ( 'NONE',  ( 1.833220611596135363, -1.622487599052296670, -1.197302888167578683 ) ) ;
#197226=CARTESIAN_POINT ( 'NONE',  ( 5.900991307970250510, 1.573582866467116759, -1.111162877451849162 ) ) ;
#197228=CARTESIAN_POINT ( 'NONE',  ( 2.109928881651984778, 1.720655366031418332, 1.405045424887063410 ) ) ;
#197234=CARTESIAN_POINT ( 'NONE',  ( 5.530708837500646347, -1.570004293196942013, 0.7514903552788397834 ) ) ;
#197235=CARTESIAN_POINT ( 'NONE',  ( 3.842202535371820993, -0.9690557767615382012, 1.705768119890891610 ) ) ;
#197236=ADVANCED_FACE ( 'NONE', ( #135368 ), #116267, .F. ) ;
#197240=CARTESIAN_POINT ( 'NONE',  ( 4.499490165225078719, 1.813563011714003803, 1.352382200441957227 ) ) ;
#197241=CARTESIAN_POINT ( 'NONE',  ( 0.8540550061131615411, -0.7440666694851668650, 1.923960566027690833 ) ) ;
#197244=CARTESIAN_POINT ( 'NONE',  ( 2.237552233957947667, -2.020869686619676919, 1.017492276205993695 ) ) ;
#197247=CARTESIAN_POINT ( 'NONE',  ( 2.635844295777586943, 0.8854499327175249235, -1.647724587607077851 ) ) ;
#197248=CARTESIAN_POINT ( 'NONE',  ( 1.670155932360503970, 1.196126419257515838, 1.255837360413303738 ) ) ;
#197249=CARTESIAN_POINT ( 'NONE',  ( 4.968408144156593487, -2.063508908063705238, -0.7385586828293493333 ) ) ;
#197250=CARTESIAN_POINT ( 'NONE',  ( 6.668959562645871308, -2.105872948262592192, -0.9439719561973120010 ) ) ;
#197251=CARTESIAN_POINT ( 'NONE',  ( 3.573254463033649131, 0.05508235185803719847, -2.161170636208443963 ) ) ;
#197252=CARTESIAN_POINT ( 'NONE',  ( 4.927648248775200912, 0.9969592527751047761, -1.666372862991059245 ) ) ;
#197254=CARTESIAN_POINT ( 'NONE',  ( 6.485618507650338316, 1.290063292742931633, 1.354747167150817333 ) ) ;
#197255=CARTESIAN_POINT ( 'NONE',  ( 0.7812500000000006661, 0.7852924748300293967, 1.895863743164072357 ) ) ;
#197260=CARTESIAN_POINT ( 'NONE',  ( 5.168592345394213972, 1.356298078840772803, 1.492257005506092193 ) ) ;
#197264=CARTESIAN_POINT ( 'NONE',  ( 2.543341688579534576, -1.352695106659363766, -1.226303905950577366 ) ) ;
#197266=CARTESIAN_POINT ( 'NONE',  ( -0.1296875068448125057, 1.390030859318210688, -2.083197486262199138 ) ) ;
#197272=CARTESIAN_POINT ( 'NONE',  ( -0.1052055632086721232, -1.960199907271743314, -0.4866737942672630379 ) ) ;
#197273=CARTESIAN_POINT ( 'NONE',  ( 6.322901860479969827, 1.648133277211549563, -1.489392227938668434 ) ) ;
#197277=CARTESIAN_POINT ( 'NONE',  ( 6.526252491562488878, 1.188822440972692185, -1.683233108126303446 ) ) ;
#197278=CARTESIAN_POINT ( 'NONE',  ( 5.238907797441370029, 2.013986022392059816, -0.1017483359899013229 ) ) ;
#197289=CARTESIAN_POINT ( 'NONE',  ( 5.483749906247235906, 1.861732415968733401, 0.7741956105717237024 ) ) ;
#197290=CARTESIAN_POINT ( 'NONE',  ( 4.751808913491627706, 0.7073710267669359730, 1.700028372310140368 ) ) ;
#197292=CARTESIAN_POINT ( 'NONE',  ( 3.756711156304150201, 0.8293906405268698379, 2.153668854807685662 ) ) ;
#197294=CARTESIAN_POINT ( 'NONE',  ( 5.589210384452774960, 1.909260796540311000, -1.013481389624170115 ) ) ;
#197296=CARTESIAN_POINT ( 'NONE',  ( 1.522887052880964598, -1.828065777178315532, 0.6558840488102948285 ) ) ;
#197300=CARTESIAN_POINT ( 'NONE',  ( 4.271116411733427043, -2.292556078035115075, 0.1642532200917065921 ) ) ;
#197303=CARTESIAN_POINT ( 'NONE',  ( 3.203821283898714345, -1.868584281295191607, 0.09040415888627445495 ) ) ;
#197305=CARTESIAN_POINT ( 'NONE',  ( 1.476665317443916603, -1.350161712199383413, 1.354623164920423450 ) ) ;
#197308=CARTESIAN_POINT ( 'NONE',  ( 2.578998426009218470, -2.112161100990978202, -0.6396139477699357423 ) ) ;
#197309=CARTESIAN_POINT ( 'NONE',  ( 6.883263157960391787, -0.001104538646235289417, 1.946037152736757925 ) ) ;
#197314=CARTESIAN_POINT ( 'NONE',  ( 0.7374959811429316892, -1.390993636481972606, -1.397171308748794250 ) ) ;
#197315=CARTESIAN_POINT ( 'NONE',  ( 1.378406844460399405, 1.376398589878137013, 1.852031911770692263 ) ) ;
#197316=CARTESIAN_POINT ( 'NONE',  ( 0.9769180011504545735, 1.811320799089161993, 0.7541596914439269161 ) ) ;
#197317=CARTESIAN_POINT ( 'NONE',  ( 5.823111402427982419, -1.862227451873458728, -0.8870778100700682511 ) ) ;
#197325=CARTESIAN_POINT ( 'NONE',  ( 0.8839112305873472186, -2.062193702853211352, 0.6791930824729536242 ) ) ;
#197329=CARTESIAN_POINT ( 'NONE',  ( 1.563515255687727645, 1.843751956470768283, -0.3144994141817195055 ) ) ;
#197330=CARTESIAN_POINT ( 'NONE',  ( 5.747404748698970778, -1.700087083557629386, -1.334863535946126722 ) ) ;
#197334=CARTESIAN_POINT ( 'NONE',  ( 1.822773347178743508, 1.416086463930026573, -1.285276961632122905 ) ) ;
#197336=CARTESIAN_POINT ( 'NONE',  ( 3.590472238826939666, -0.3446705786002961514, -1.735762067166376710 ) ) ;
#197337=CARTESIAN_POINT ( 'NONE',  ( 0.5746843702075511429, -1.384840223850939855, 1.318951758179337741 ) ) ;
#197339=CARTESIAN_POINT ( 'NONE',  ( 5.396063265741290138, -0.8654563178034151427, -1.709049623916969018 ) ) ;
#197340=CARTESIAN_POINT ( 'NONE',  ( 6.197704753879455630, -1.425424270160932094, -1.359389694413483562 ) ) ;
#197342=CARTESIAN_POINT ( 'NONE',  ( 1.318772358905948794, -0.7683209907942339933, -1.976687055281033611 ) ) ;
#197344=CARTESIAN_POINT ( 'NONE',  ( 5.436355746168001879, 1.843147576875401983, 0.3187000444574567548 ) ) ;
#197345=CARTESIAN_POINT ( 'NONE',  ( 0.4162703231485806454, 1.261427835099769634, -1.320066674804179385 ) ) ;
#197347=CARTESIAN_POINT ( 'NONE',  ( 5.022202109028018668, -1.178465353167540197, -1.865713892744431446 ) ) ;
#197350=CARTESIAN_POINT ( 'NONE',  ( 2.242701489527811454, -2.022432087814116652, -0.4046766347945063846 ) ) ;
#197357=CARTESIAN_POINT ( 'NONE',  ( 4.193848433072798088, -1.425472641756184489, -1.501718461524886195 ) ) ;
#197359=CARTESIAN_POINT ( 'NONE',  ( 1.792469030454997059, -2.151019407201111289, -0.2137723215496489249 ) ) ;
#197361=CARTESIAN_POINT ( 'NONE',  ( 1.717450570094357865, 1.680397536943441406, 1.120097702336475987 ) ) ;
#197362=CARTESIAN_POINT ( 'NONE',  ( 0.07755575628183573877, -0.002876890934064984216, -2.188974970840869005 ) ) ;
#197368=CARTESIAN_POINT ( 'NONE',  ( 0.2336117360935245635, 0.6279853779636718203, -1.916355031878452797 ) ) ;
#197369=CARTESIAN_POINT ( 'NONE',  ( 4.775033345069852331, 2.044829088842615494, -0.7888500489584143738 ) ) ;
#197371=CARTESIAN_POINT ( 'NONE',  ( 3.392734571251673881, -1.844325299564765208, -0.5055192353106837677 ) ) ;
#197376=CARTESIAN_POINT ( 'NONE',  ( 1.898064762488653079, -0.9530305783747442527, -1.777002450075705120 ) ) ;
#197378=CARTESIAN_POINT ( 'NONE',  ( 0.7675861853312654359, 2.207383698986573162, -0.6181827981695892094 ) ) ;
#197380=CARTESIAN_POINT ( 'NONE',  ( 3.961678648311004025, 1.711676862058534088, -0.2113787121680379411 ) ) ;
#197381=CARTESIAN_POINT ( 'NONE',  ( 0.1405533004714175083, 0.2365636613079393491, -2.314604644119310439 ) ) ;
#197385=CARTESIAN_POINT ( 'NONE',  ( 0.1755611466353265426, 6.947017789483680872, -2.839095415174418768 ) ) ;
#197389=CARTESIAN_POINT ( 'NONE',  ( 4.881432045509231266, 0.1721252788823707247, -1.803262557370821417 ) ) ;
#197393=CARTESIAN_POINT ( 'NONE',  ( 5.936161223257452768, -1.012099431654609472, -1.502142840615662944 ) ) ;
#197396=CARTESIAN_POINT ( 'NONE',  ( 3.468858241077877214, 0.05382521638562161315, -2.190950023606648145 ) ) ;
#197397=CARTESIAN_POINT ( 'NONE',  ( 6.672303541529164050, -0.8785034406106060345, -1.640621795851913367 ) ) ;
#197399=CARTESIAN_POINT ( 'NONE',  ( 3.356958492073054412, 0.04375785802200299335, -1.915270648069177462 ) ) ;
#197407=CARTESIAN_POINT ( 'NONE',  ( 5.489508092091861080, -0.5117143178510559220, 2.054485130609058796 ) ) ;
#197408=CARTESIAN_POINT ( 'NONE',  ( 0.8487565004985967443, 0.6285140637429244004, 2.068326486519965979 ) ) ;
#197411=CARTESIAN_POINT ( 'NONE',  ( 0.5865807246496178573, -0.2182756592755269454, -1.812417144444453232 ) ) ;
#197413=CARTESIAN_POINT ( 'NONE',  ( 3.047666980291532823, 0.6586017179070653427, -1.702814618940437619 ) ) ;
#197416=CARTESIAN_POINT ( 'NONE',  ( 3.016014308207531247, 1.960325316701009735, -0.1901906172739661061 ) ) ;
#197418=CARTESIAN_POINT ( 'NONE',  ( 5.091328012616338938, -0.6953414466571452568, 1.813493487445563046 ) ) ;
#197421=CARTESIAN_POINT ( 'NONE',  ( 5.713165544288242970, 1.732532623411761286, -1.222520872474173848 ) ) ;
#197423=CARTESIAN_POINT ( 'NONE',  ( 2.438023429326571456, -1.102505324871098757, -1.562262158393577405 ) ) ;
#197425=CARTESIAN_POINT ( 'NONE',  ( 0.2331563151865694850, 5.724144821786467219, -2.539778028485844885 ) ) ;
#197430=CARTESIAN_POINT ( 'NONE',  ( 4.072905994182826284, -1.490248019560231452, 1.353564014653575009 ) ) ;
#197432=CARTESIAN_POINT ( 'NONE',  ( 5.109893933574640279, -1.816543354971979163, 0.1824992186492402357 ) ) ;
#197433=CARTESIAN_POINT ( 'NONE',  ( 0.8716356842100521085, -0.3054578492302991721, 2.047597563663336118 ) ) ;
#197438=CARTESIAN_POINT ( 'NONE',  ( 6.016445890116215445, 1.255022122864515310, -1.387330985440645037 ) ) ;
#197441=( GEOMETRIC_REPRESENTATION_CONTEXT ( 3 ) GLOBAL_UNCERTAINTY_ASSIGNED_CONTEXT ( ( #35581 ) ) GLOBAL_UNIT_ASSIGNED_CONTEXT ( ( #45925, #23502, #28590 ) ) REPRESENTATION_CONTEXT ( 'NONE', 'WORKASPACE' ) );
#197447=CARTESIAN_POINT ( 'NONE',  ( 1.041946221393402539, 1.387617377995558288, 1.536584593769604323 ) ) ;
#197448=CARTESIAN_POINT ( 'NONE',  ( 2.056417290815291121, -1.299724242359597826, 1.671285701813587821 ) ) ;
#197451=CARTESIAN_POINT ( 'NONE',  ( 6.438344962566215024, -1.112565956905732456, 1.745730973219234539 ) ) ;
#197456=CARTESIAN_POINT ( 'NONE',  ( 2.467065147740226116, 0.1108469335737295169, -2.289696780367215467 ) ) ;
#197458=CARTESIAN_POINT ( 'NONE',  ( 2.373185085050379506, -1.665764800640230803, -0.9392108107411781814 ) ) ;
#197461=CARTESIAN_POINT ( 'NONE',  ( 0.4924401237900773443, -1.114920267122095021, 1.676101429157205613 ) ) ;
#197462=CARTESIAN_POINT ( 'NONE',  ( 1.287862062775881666, -1.240280065097350448, -1.519972987346601023 ) ) ;
#197466=CARTESIAN_POINT ( 'NONE',  ( 3.873056903084231450, 1.968474739099084436, -0.7045419632574521085 ) ) ;
#197467=CARTESIAN_POINT ( 'NONE',  ( 2.377515701973518691, 1.086635889927405341, 1.396898309679272865 ) ) ;
#197471=CARTESIAN_POINT ( 'NONE',  ( 4.804755513996577854, 1.992766236949112812, 1.132715491657744877 ) ) ;
#197472=CARTESIAN_POINT ( 'NONE',  ( 4.294662974013852441, 1.399676235010495873, 1.034011069942197159 ) ) ;
#197475=CARTESIAN_POINT ( 'NONE',  ( 4.463993690379265189, 1.392342236284923152, 1.032948281618131903 ) ) ;
#197477=CARTESIAN_POINT ( 'NONE',  ( 4.967309339809048652, 1.886637975807739176, 1.074439269227177363 ) ) ;
#197479=CARTESIAN_POINT ( 'NONE',  ( 5.243375144629232487, 0.3886363430659239837, -1.978554426619572926 ) ) ;
#197480=CARTESIAN_POINT ( 'NONE',  ( 0.5937500000000017764, -1.895863743164141191, -0.7852924748299565660 ) ) ;
#197483=CARTESIAN_POINT ( 'NONE',  ( 2.467692127658027701, 1.889608252265186694, -0.3738381972786026797 ) ) ;
#197485=CARTESIAN_POINT ( 'NONE',  ( 5.221006152755099272, 1.681885564164938840, -1.451226649161361015 ) ) ;
#197487=CARTESIAN_POINT ( 'NONE',  ( 6.983263157960370116, 7.052597238847845063, 2.544342084569085838 ) ) ;
#197491=CARTESIAN_POINT ( 'NONE',  ( 1.946216630774719736, -1.453687271215977850, -1.679643103671465632 ) ) ;
#197492=CARTESIAN_POINT ( 'NONE',  ( 6.877413162628408294, -0.1429737755889188278, 1.930079329684093237 ) ) ;
#197498=CARTESIAN_POINT ( 'NONE',  ( 4.598127328184369311, 0.8849438138122868169, -1.863347811608778271 ) ) ;
#197502=CARTESIAN_POINT ( 'NONE',  ( 5.940666398231567058, 0.3644617591120716260, 1.834516074763043347 ) ) ;
#197503=CARTESIAN_POINT ( 'NONE',  ( 4.904772540272760217, -0.9336124152922348207, -1.461164293347013921 ) ) ;
#197504=CARTESIAN_POINT ( 'NONE',  ( 4.827569786946327213, 0.8888792617508225469, -1.496182039812316678 ) ) ;
#197506=CARTESIAN_POINT ( 'NONE',  ( 2.402247335887615964, -0.8806970201959153366, -2.116636687559919849 ) ) ;
#197508=CARTESIAN_POINT ( 'NONE',  ( 5.776921370525399446, 1.931409454660049319, -0.8010388902379047549 ) ) ;
#197509=CARTESIAN_POINT ( 'NONE',  ( 1.341482821134845738, 1.838956754096718882, 0.09199767257135617327 ) ) ;
#197511=CARTESIAN_POINT ( 'NONE',  ( 2.584611472894111195, -0.6298744119781033435, 1.915600275669691488 ) ) ;
#197512=CARTESIAN_POINT ( 'NONE',  ( 0.8322822162843239724, 2.159637434087835928, 0.3711470721824081109 ) ) ;
#197515=CARTESIAN_POINT ( 'NONE',  ( 1.592325325408463055, 1.022198633559557646, -1.800363622228560168 ) ) ;
#197518=CARTESIAN_POINT ( 'NONE',  ( 3.668700845920089826, 0.7647225481513253431, 1.977962425194310203 ) ) ;
#197520=CARTESIAN_POINT ( 'NONE',  ( 6.287720257080702702, 1.262826302610157381, 1.318732360701305062 ) ) ;
#197527=CARTESIAN_POINT ( 'NONE',  ( 3.691669705439902138, 1.900360886217996370, -0.6845428438169256502 ) ) ;
#197528=CARTESIAN_POINT ( 'NONE',  ( 1.659346488253128804, -1.806016679666972546, -1.082987972701171309 ) ) ;
#197531=CARTESIAN_POINT ( 'NONE',  ( 5.155058861800134729, 1.548501282276077529, -1.031774840880594901 ) ) ;
#197536=CARTESIAN_POINT ( 'NONE',  ( 0.1984014031938194922, -2.161264429664040421, -0.05129915172277095536 ) ) ;
#197540=CARTESIAN_POINT ( 'NONE',  ( 2.161130077686782336, -0.4579326675830681093, -1.672196941802698733 ) ) ;
#197541=CARTESIAN_POINT ( 'NONE',  ( 1.780815255366276162, 1.198741944763829004, 1.261882163386177869 ) ) ;
#197542=CARTESIAN_POINT ( 'NONE',  ( 0.3062966595402705217, -0.6107984557060777142, 2.225206381879496487 ) ) ;
#197545=CARTESIAN_POINT ( 'NONE',  ( 2.407559617977403477, -0.4546984313768054342, 2.009812782922258734 ) ) ;
#197547=CARTESIAN_POINT ( 'NONE',  ( 1.317732270343049406, -1.591076063098846749, 1.238129638497114771 ) ) ;
#197548=CARTESIAN_POINT ( 'NONE',  ( 6.925078400183545035, 2.404074903924419804, 2.624186486869657831 ) ) ;
#197550=CIRCLE ( 'NONE', #28097, 0.04999999999999969746 ) ;
#197551=CARTESIAN_POINT ( 'NONE',  ( 0.4792893823705188794, 1.840408107720743924, -0.7072656782263522235 ) ) ;
#197552=CARTESIAN_POINT ( 'NONE',  ( 5.080287894202283105, 0.9478536798121822704, 1.660923459347658282 ) ) ;
#197554=CARTESIAN_POINT ( 'NONE',  ( 5.690102719724574598, -0.9953569382129350274, 1.969734210959340093 ) ) ;
#197558=CARTESIAN_POINT ( 'NONE',  ( 0.2936253167127310659, 1.883648094304795961, -0.7291253699766816476 ) ) ;
#197561=CARTESIAN_POINT ( 'NONE',  ( 4.893776379751743733, 1.706213512276737232, 1.553814486356275060 ) ) ;
#197562=CARTESIAN_POINT ( 'NONE',  ( 4.703538834289092030, -1.515240342570793430, -1.246145567450624991 ) ) ;
#197563=CARTESIAN_POINT ( 'NONE',  ( 1.604273143990111672, 1.959273547513197711, 0.1016356785708133759 ) ) ;
#197567=CARTESIAN_POINT ( 'NONE',  ( 0.2689693067343159605, -0.2660441693766130711, -2.100534484541769498 ) ) ;
#197570=CARTESIAN_POINT ( 'NONE',  ( 0.5152501731416662123, -0.9825955030486510644, -1.556829690179861059 ) ) ;
#197572=CARTESIAN_POINT ( 'NONE',  ( 4.100555696908855019, 2.160072011501934064, 0.2185761814032516903 ) ) ;
#197574=CARTESIAN_POINT ( 'NONE',  ( 1.969135536805465492, -1.636093909763213228, 1.349083368969570262 ) ) ;
#197579=CARTESIAN_POINT ( 'NONE',  ( 2.513025655421320170, 1.839406356194466463, 0.9293899518807801075 ) ) ;
#197582=CARTESIAN_POINT ( 'NONE',  ( 6.509000000000010111, 0.007656933339201026957, 1.900274884395844133 ) ) ;
#197584=CARTESIAN_POINT ( 'NONE',  ( -0.02244404828160087226, 4.081832076214893412, -2.743766916979750281 ) ) ;
#197586=CARTESIAN_POINT ( 'NONE',  ( 5.391234928627540057, -0.05113397888981999900, -1.911771334517261556 ) ) ;
#197588=CARTESIAN_POINT ( 'NONE',  ( 1.757462551082995095, -1.940025152074912551, -1.163771565304895450 ) ) ;
#197590=CARTESIAN_POINT ( 'NONE',  ( 1.599580717682536291, 1.250984903983554997, 1.310507481138773800 ) ) ;
#197591=CARTESIAN_POINT ( 'NONE',  ( 2.096773827148257219, 1.713186613203399489, 0.8573791853930428086 ) ) ;
#197592=CARTESIAN_POINT ( 'NONE',  ( 2.770052221688572125, -2.048192801557855436, 0.3012726569043902569 ) ) ;
#197595=CARTESIAN_POINT ( 'NONE',  ( 2.043765361886350274, 0.7562441204337754241, -1.820841827831324533 ) ) ;
#197596=CARTESIAN_POINT ( 'NONE',  ( 5.356054764349521768, 1.924192155146129624, -0.09673933992536233595 ) ) ;
#197597=CARTESIAN_POINT ( 'NONE',  ( 1.173011757359025520, -1.460375281577396489, 1.786833355454720884 ) ) ;
#197600=CARTESIAN_POINT ( 'NONE',  ( 5.564908101581790945, 1.564332607353050131, -1.344557729249852729 ) ) ;
#197603=CARTESIAN_POINT ( 'NONE',  ( -0.01685825368398767912, -0.1589125243241385210, -2.071875930555002743 ) ) ;
#197606=CARTESIAN_POINT ( 'NONE',  ( 4.376362478467909156, -1.248523626585487989, 1.764366501186130698 ) ) ;
#197607=CARTESIAN_POINT ( 'NONE',  ( 5.690105174167163327, 1.204846223408085670, 1.620761788888310351 ) ) ;
#197614=CARTESIAN_POINT ( 'NONE',  ( 3.801970467005914678, -1.040791964576088358, -1.727064642965264740 ) ) ;
#197619=CARTESIAN_POINT ( 'NONE',  ( 4.680646922328831394, -2.095996545452833981, -0.5284188670612932626 ) ) ;
#197624=CARTESIAN_POINT ( 'NONE',  ( 5.800407700000974387, 1.352143934286989868, -1.496062775417882129 ) ) ;
#197626=CARTESIAN_POINT ( 'NONE',  ( 0.6797846375097577054, -0.9621480743811950953, 1.431375779520219549 ) ) ;
#197631=CARTESIAN_POINT ( 'NONE',  ( 6.503191328365395485, 1.555263205862934983, 1.038959965768880389 ) ) ;
#197632=CARTESIAN_POINT ( 'NONE',  ( 0.6275903186243469989, -0.2933333519314991755, 1.991482607974030206 ) ) ;
#197635=CARTESIAN_POINT ( 'NONE',  ( 3.540233119088306513, 0.9941544567689840628, -1.970234943098593039 ) ) ;
#197641=CARTESIAN_POINT ( 'NONE',  ( 1.946092837771850492, -1.387361170020007695, -1.603719225630481970 ) ) ;
#197642=CARTESIAN_POINT ( 'NONE',  ( 1.880482680076976720, -0.5405129038237622696, -1.942536604102131026 ) ) ;
#197643=CARTESIAN_POINT ( 'NONE',  ( 2.707043852439145581, 1.551706383644942289, -0.9346757785875584590 ) ) ;
#197648=CARTESIAN_POINT ( 'NONE',  ( 0.04005665835727333091, 0.7356861536649759170, 1.769027722964914728 ) ) ;
#197656=CARTESIAN_POINT ( 'NONE',  ( 4.381803836707322652, 1.409801062080328959, 1.638821348427916602 ) ) ;
#197659=CARTESIAN_POINT ( 'NONE',  ( 2.215225606797793567, 1.700350911433265555, -1.266953333846132512 ) ) ;
#197661=CARTESIAN_POINT ( 'NONE',  ( 3.180892574772069992, -0.1416633064414400678, -1.966302885814166013 ) ) ;
#197662=CARTESIAN_POINT ( 'NONE',  ( 5.959226163113887864, -1.611951592244726950, 1.028742869173946861 ) ) ;
#197665=CARTESIAN_POINT ( 'NONE',  ( 6.637161372131059167, -0.09511470475139816028, -1.967365288627285214 ) ) ;
#197666=CARTESIAN_POINT ( 'NONE',  ( 1.693202460532976295, -0.6543010362765960819, 1.828533997230662234 ) ) ;
#197671=CARTESIAN_POINT ( 'NONE',  ( 2.835970919032384963, 2.074939634868844252, 0.2550863383830522801 ) ) ;
#197675=CARTESIAN_POINT ( 'NONE',  ( 6.639320575229252341, 0.005161017367553630275, 1.896863882003448021 ) ) ;
#197677=CARTESIAN_POINT ( 'NONE',  ( 4.389439674793148782, 1.972019932058775016, -0.9908447712502415072 ) ) ;
#197678=CARTESIAN_POINT ( 'NONE',  ( 1.518904762042364354, 1.481482853740143435, -1.635709697223409531 ) ) ;
#197680=CARTESIAN_POINT ( 'NONE',  ( 0.7680391878876170475, 1.910087531778673187, -0.09433495293535018589 ) ) ;
#197681=CARTESIAN_POINT ( 'NONE',  ( 0.1833691866889655686, 7.629137130509075604, -2.653448492709729933 ) ) ;
#197683=CARTESIAN_POINT ( 'NONE',  ( 3.965334771736851671, 1.774175476309115984, 1.066894043611272824 ) ) ;
#197685=CARTESIAN_POINT ( 'NONE',  ( 1.868271315571629509, 1.111147431007172726, 1.854118885846419262 ) ) ;
#197686=CARTESIAN_POINT ( 'NONE',  ( 3.491892070630482348, -2.189115664112693871, -0.1057334378413293807 ) ) ;
#197694=CARTESIAN_POINT ( 'NONE',  ( 6.522076087392383315, -1.544353836717025308, 0.7889432867928622972 ) ) ;
#197698=CARTESIAN_POINT ( 'NONE',  ( 4.487213805514509879, 0.09639557921744396074, 2.068113308821089902 ) ) ;
#197699=CARTESIAN_POINT ( 'NONE',  ( 5.255504845270437819, 2.040225721616812482, -0.5655070190290175658 ) ) ;
#197702=CARTESIAN_POINT ( 'NONE',  ( 4.153143631030720151, 1.666095859335927187, -1.049822023992821984 ) ) ;
#197703=CARTESIAN_POINT ( 'NONE',  ( 6.246038198481189241, 0.7129642902690846995, 2.178627299872720524 ) ) ;
#197704=CARTESIAN_POINT ( 'NONE',  ( 2.771877994228102882, 0.9767612972278701955, 1.542236413651025151 ) ) ;
#197710=CARTESIAN_POINT ( 'NONE',  ( 3.990493469460140830, -1.155612956054508977, 1.648335472937176194 ) ) ;
#197711=CARTESIAN_POINT ( 'NONE',  ( 0.1757712021154093640, -0.9832847084251387093, -2.074436467499872094 ) ) ;
#197712=CARTESIAN_POINT ( 'NONE',  ( 4.715648799723409113, 0.4337510919622395988, -1.913030730064477769 ) ) ;
#197716=CARTESIAN_POINT ( 'NONE',  ( 0.9254645587078378366, -1.329342062510083355, -1.613690532076578199 ) ) ;
#197717=CARTESIAN_POINT ( 'NONE',  ( 6.174623306383559829, -1.681873830149778648, -0.5512017132776861894 ) ) ;
#197719=CARTESIAN_POINT ( 'NONE',  ( 1.693587955360946529, -0.7361150630936144079, 2.064250245950305374 ) ) ;
#197720=CARTESIAN_POINT ( 'NONE',  ( 0.9072687458823289752, -0.7809752019604562223, -1.555474206689683836 ) ) ;
#197723=CARTESIAN_POINT ( 'NONE',  ( 0.1333692844072802142, 2.017199222642913625, -2.468757726274827036 ) ) ;
#197724=CARTESIAN_POINT ( 'NONE',  ( 1.857592325351750118, 1.720440678145126467, -0.1246472719800949674 ) ) ;
#197725=CARTESIAN_POINT ( 'NONE',  ( 1.505704256594592838, -2.174480876681058827, 0.2726767719730335826 ) ) ;
#197726=CARTESIAN_POINT ( 'NONE',  ( -0.01748474828899664046, -1.733701077801694579, -0.04590633323625636919 ) ) ;
#197727=CARTESIAN_POINT ( 'NONE',  ( 3.563272299071856164, -1.946135509614330239, -1.040604674307284316 ) ) ;
#197728=CARTESIAN_POINT ( 'NONE',  ( 1.516727516949545107, 0.8775410692131856427, 1.985969635014148915 ) ) ;
#197729=CARTESIAN_POINT ( 'NONE',  ( 0.04711308451243316486, -1.408776630263553375, -1.161003007932148501 ) ) ;
#197730=CARTESIAN_POINT ( 'NONE',  ( 2.114611820864919611, 2.055121497718506163, 0.5091636546959156240 ) ) ;
#197731=CARTESIAN_POINT ( 'NONE',  ( 6.827182134110239886, 1.995248472151121444, 2.590158597942037844 ) ) ;
#197733=CARTESIAN_POINT ( 'NONE',  ( 2.718655769491088225, 2.159526321510790492, 0.7694321526581606729 ) ) ;
#197738=CARTESIAN_POINT ( 'NONE',  ( 4.916739609850255377, -0.7473993280511237458, -2.091895594778249379 ) ) ;
#197746=CARTESIAN_POINT ( 'NONE',  ( 3.481092415823695774, -2.014232707597499505, -0.09613569647320965861 ) ) ;
#197748=CARTESIAN_POINT ( 'NONE',  ( 0.9716179518045722219, -0.3065469058200780972, 2.039571770164672504 ) ) ;
#197753=CARTESIAN_POINT ( 'NONE',  ( 3.732539452256115275, 0.3211115598316104935, 2.167677955659273348 ) ) ;
#197754=CARTESIAN_POINT ( 'NONE',  ( 1.371720446232262081, -0.2986288616722633793, -1.994071132515719658 ) ) ;
#197755=CARTESIAN_POINT ( 'NONE',  ( 1.522747961674526085, -1.733470594775164075, 0.6210259959333885860 ) ) ;
#197758=CARTESIAN_POINT ( 'NONE',  ( 5.262654937129007671, -1.321179299781930938, 1.260103332352560779 ) ) ;
#197759=CARTESIAN_POINT ( 'NONE',  ( 5.748672702226536479, 1.986101125435947301, -0.3474646712962395911 ) ) ;
#197761=CARTESIAN_POINT ( 'NONE',  ( 4.083118212167598848, -0.2185186360062584821, -2.251932414709489905 ) ) ;
#197763=CARTESIAN_POINT ( 'NONE',  ( 1.049603877184020373, -1.661282181752096410, -1.294363288650403732 ) ) ;
#197765=CARTESIAN_POINT ( 'NONE',  ( 4.562978833902987752, 1.602482145440896399, -1.310924660355553106 ) ) ;
#197774=CARTESIAN_POINT ( 'NONE',  ( 0.2816890862925770511, 0.2015970107726860194, -2.110973810222869229 ) ) ;
#197775=CARTESIAN_POINT ( 'NONE',  ( 1.617743263029525869, 1.850308847857740968, 1.228972131997711381 ) ) ;
#197779=CARTESIAN_POINT ( 'NONE',  ( 3.139059813392345077, -0.1416510307416830594, -1.956792864499560691 ) ) ;
#197786=CARTESIAN_POINT ( 'NONE',  ( 1.793382672576701919, -0.1090974814243403090, -2.117938670719583527 ) ) ;
#197788=CARTESIAN_POINT ( 'NONE',  ( 3.965250677406896962, 1.681448970545707855, 1.010551734412237446 ) ) ;
#197789=CARTESIAN_POINT ( 'NONE',  ( 2.817419395390472037, -0.2130390993498078311, 2.151187356804876050 ) ) ;
#197790=CARTESIAN_POINT ( 'NONE',  ( 2.858754248528099229, 0.2676582106064147593, -1.821554178878769470 ) ) ;
#197795=CARTESIAN_POINT ( 'NONE',  ( 4.857210178628561970, 1.720700030253617951, -0.2597475362437673407 ) ) ;
#197800=CARTESIAN_POINT ( 'NONE',  ( 1.991316529349271836, 1.880942973025516940, -1.065213018539921563 ) ) ;
#197801=CARTESIAN_POINT ( 'NONE',  ( 4.868517441940229951, -0.5404072756688071966, 1.942244311778835719 ) ) ;
#197803=CARTESIAN_POINT ( 'NONE',  ( 1.094844843509492183, -0.5259716649698794599, -2.096624219460433647 ) ) ;
#197805=CARTESIAN_POINT ( 'NONE',  ( 2.794160851653566535, -1.965818266918018864, -0.1488234875552247316 ) ) ;
#197806=CARTESIAN_POINT ( 'NONE',  ( 2.817592499383800853, -1.357869084745389809, -1.490969456672403881 ) ) ;
#197809=CARTESIAN_POINT ( 'NONE',  ( 3.298316653532318732, 1.529317551288728483, -1.196868631420761053 ) ) ;
#197812=ORIENTED_EDGE ( 'NONE', *, *, #100013, .T. ) ;
#197819=CARTESIAN_POINT ( 'NONE',  ( 0.8509352111321017986, 0.6423128672003556305, 2.111239891224323983 ) ) ;
#197821=CARTESIAN_POINT ( 'NONE',  ( 5.612146373276853950, 1.959670608579218376, -0.09257137562097839112 ) ) ;
#197823=CARTESIAN_POINT ( 'NONE',  ( 3.274719840360585721, -0.4174103159439371824, -2.075633323822536180 ) ) ;
#197825=CARTESIAN_POINT ( 'NONE',  ( 0.07459516483341446791, 5.726030365519781284, -2.349570391284861781 ) ) ;
#197826=CARTESIAN_POINT ( 'NONE',  ( 4.242028835625204053, 0.4931972713904734795, 1.773778790588397491 ) ) ;
#197830=CARTESIAN_POINT ( 'NONE',  ( 5.414351406770180120, -2.120778210838507150, 0.002142078463891750485 ) ) ;
#197834=CARTESIAN_POINT ( 'NONE',  ( 5.624313186929686736, 1.231095119260311677, -1.652465237140358090 ) ) ;
#197836=CARTESIAN_POINT ( 'NONE',  ( 0.8009387066525032184, -1.599029608822761128, 0.9519043452789009985 ) ) ;
#197837=CARTESIAN_POINT ( 'NONE',  ( 3.087279721815265443, -0.7436087841871074078, 1.684586988852328160 ) ) ;
#197841=CARTESIAN_POINT ( 'NONE',  ( 2.965657822035951963, 0.3232568108629539361, -2.182957019552448141 ) ) ;
#197842=CARTESIAN_POINT ( 'NONE',  ( 4.429186382639688446, 0.1052742795825665628, 2.260063922926962121 ) ) ;
#197844=CARTESIAN_POINT ( 'NONE',  ( 5.009926431283926895, -0.6449355957302944642, 1.693101296380158383 ) ) ;
#197846=CARTESIAN_POINT ( 'NONE',  ( 5.419116407314492179, -1.729028094342921706, 0.8252531017051125684 ) ) ;
#197847=CARTESIAN_POINT ( 'NONE',  ( 6.827182134110198142, 0.003888933837258023996, 1.810856214465889069 ) ) ;
#197848=CARTESIAN_POINT ( 'NONE',  ( 6.034044788248046132, 0.9204803733943857091, -1.628451883209979689 ) ) ;
#197849=CARTESIAN_POINT ( 'NONE',  ( 6.215283151739675382, -1.596727646711604942, -0.9557930639402379969 ) ) ;
#197852=CARTESIAN_POINT ( 'NONE',  ( 6.491055376221456008, 1.537463663300852490, -0.8764918771043300749 ) ) ;
#197853=CARTESIAN_POINT ( 'NONE',  ( 0.4797043241997685503, -0.7212876333932433104, 1.883314553594167107 ) ) ;
#197855=CARTESIAN_POINT ( 'NONE',  ( 2.684315897010148610, -1.081986827455215572, 1.806733699029156259 ) ) ;
#197858=CARTESIAN_POINT ( 'NONE',  ( 6.777182134110200096, 7.629137130509070275, 2.410944104600750038 ) ) ;
#197859=CARTESIAN_POINT ( 'NONE',  ( 2.021745798758204149, -0.4384165714973499162, 1.971471537551409803 ) ) ;
#197862=CARTESIAN_POINT ( 'NONE',  ( 3.075615952314793233, 2.053625483174918553, -0.6748976972978243394 ) ) ;
#197863=CARTESIAN_POINT ( 'NONE',  ( 6.890000000000044977, 2.990039200936049468, 2.173945303097582382 ) ) ;
#197871=CARTESIAN_POINT ( 'NONE',  ( 0.9432342461353732110, -1.730868645791438842, -1.344178957308760802 ) ) ;
#197873=CARTESIAN_POINT ( 'NONE',  ( 1.710245752144876619, -2.245277845785878412, 0.2781651023185549021 ) ) ;
#197882=CARTESIAN_POINT ( 'NONE',  ( 3.409201082634921498, -0.3482811000503453491, 1.734931447941751692 ) ) ;
#197884=CARTESIAN_POINT ( 'NONE',  ( 6.686557766011572923, -2.162873314485185272, -0.4371622687903350957 ) ) ;
#197888=CARTESIAN_POINT ( 'NONE',  ( 5.079703922733037835, -0.7231256174668048153, 1.882480835741196845 ) ) ;
#197890=CARTESIAN_POINT ( 'NONE',  ( 2.764352523130030548, -1.291370965961564421, 1.353630663414123969 ) ) ;
#197891=CARTESIAN_POINT ( 'NONE',  ( 3.819242646454374057, -1.823515126939363462, -0.9802443236400714133 ) ) ;
#197893=CARTESIAN_POINT ( 'NONE',  ( 2.461071540317420592, -1.587761714688111780, 1.065645112462119570 ) ) ;
#197896=FACE_OUTER_BOUND ( 'NONE', #154112, .T. ) ;
#197898=CARTESIAN_POINT ( 'NONE',  ( 0.8965662283535699162, -1.866366896104875162, -0.4163465257057268332 ) ) ;
#197899=CARTESIAN_POINT ( 'NONE',  ( 3.103904542773823660, 0.7086415210641981988, -1.829580771271981154 ) ) ;
#197904=CARTESIAN_POINT ( 'NONE',  ( 0.2099203756031532975, -0.7936979409460078738, -1.692237190125941648 ) ) ;
#197906=CARTESIAN_POINT ( 'NONE',  ( 2.162360077456865870, 2.012843401649004882, 0.04526349954376075735 ) ) ;
#197908=CARTESIAN_POINT ( 'NONE',  ( 2.460703409257146923, -2.027034307268358315, -0.6114533316685047959 ) ) ;
#197911=CARTESIAN_POINT ( 'NONE',  ( 4.105968538015460467, 0.7004154448949986289, -1.948405661837959713 ) ) ;
#197913=CARTESIAN_POINT ( 'NONE',  ( 6.140588758375521650, -1.766823853066697536, 1.117321708369632516 ) ) ;
#197915=CARTESIAN_POINT ( 'NONE',  ( 4.594645031659345236, -0.4005623417570289280, -1.780931357837008733 ) ) ;
#197920=CARTESIAN_POINT ( 'NONE',  ( 5.069440727656137291, 0.2206807655098403653, -2.195719112144229879 ) ) ;
#197923=CARTESIAN_POINT ( 'NONE',  ( 4.477155480220369910, -1.709698060584059043, -0.8567103784868701499 ) ) ;
#197932=CARTESIAN_POINT ( 'NONE',  ( 0.1339853816830008371, 0.3136495386693045062, 1.814181566856580607 ) ) ;
#197937=CARTESIAN_POINT ( 'NONE',  ( 4.428871017648271291, 0.08965458760558722706, 1.868499062828571367 ) ) ;
#197942=CARTESIAN_POINT ( 'NONE',  ( 1.323035253951538426, -1.778235669024318177, -0.8468731209588018505 ) ) ;
#197943=CARTESIAN_POINT ( 'NONE',  ( 2.091422941747251851, -0.4390073250180903663, 1.967893905867940996 ) ) ;
#197948=CARTESIAN_POINT ( 'NONE',  ( 2.554835828347111093, -1.907293181126702653, -1.079063956894068754 ) ) ;
#197958=CARTESIAN_POINT ( 'NONE',  ( 4.616662711240536510, -0.08544939198026380023, 1.839383977539174264 ) ) ;
#197959=CARTESIAN_POINT ( 'NONE',  ( 1.277990700441207661, 1.982931799766519676, -0.3463461644656241623 ) ) ;
#197960=CARTESIAN_POINT ( 'NONE',  ( 3.532835791020246141, 2.243242391287715964, -0.4999081842005962395 ) ) ;
#197962=CARTESIAN_POINT ( 'NONE',  ( 1.270090995528074362, -0.8302864195119415980, -1.665510012463662148 ) ) ;
#197964=CARTESIAN_POINT ( 'NONE',  ( 5.572493885891085519, 0.7809320506734825917, 1.745880147543739325 ) ) ;
#197967=CARTESIAN_POINT ( 'NONE',  ( 3.386350598701783454, -0.4101191253191734387, -2.049945593880502681 ) ) ;
#197968=CARTESIAN_POINT ( 'NONE',  ( 1.850267049257280139, 0.5840378008528935849, 1.777222254475477659 ) ) ;
#197972=CARTESIAN_POINT ( 'NONE',  ( 6.163598723784101452, 0.9525508894225950263, 1.575581956637741587 ) ) ;
#197976=CARTESIAN_POINT ( 'NONE',  ( 5.566962092400322248, -1.562093814453187735, -0.7318214103424671713 ) ) ;
#197978=CARTESIAN_POINT ( 'NONE',  ( 0.4043864329151745651, -0.9253471945274373001, -1.466404024333650247 ) ) ;
#197982=CARTESIAN_POINT ( 'NONE',  ( 4.188457025382522403, 1.166365143183651920, -1.831003835250759604 ) ) ;
#197983=CARTESIAN_POINT ( 'NONE',  ( 3.000428103051573814, -0.5303778429210231904, -1.746945217264872507 ) ) ;
#197984=CARTESIAN_POINT ( 'NONE',  ( 1.287862062775881888, -1.240280065097350226, -1.519972987346601023 ) ) ;
#197985=CARTESIAN_POINT ( 'NONE',  ( 5.489508092091861080, -0.5117143178510559220, 2.054485130609058796 ) ) ;
#197986=CARTESIAN_POINT ( 'NONE',  ( 6.392113680008942644, -0.6066422732131382389, -2.210563551359717938 ) ) ;
#197990=CARTESIAN_POINT ( 'NONE',  ( 1.278162280329109279, 2.088516533416693743, -0.3659721813360562459 ) ) ;
#197996=CARTESIAN_POINT ( 'NONE',  ( 6.631686460494314872, 2.080164978358085559, -0.6217935382996344629 ) ) ;
#197997=CARTESIAN_POINT ( 'NONE',  ( 6.983263157960363010, 6.034173670577698267, 2.748703042679788044 ) ) ;
#197999=CARTESIAN_POINT ( 'NONE',  ( 2.649351634902767483, 0.2746262237617850821, 2.204210978092531192 ) ) ;
#198001=CARTESIAN_POINT ( 'NONE',  ( 6.170546107226446253, 1.392543322632183722, 1.458558933167881211 ) ) ;
#198003=CARTESIAN_POINT ( 'NONE',  ( 4.118078732422246979, 2.047561256575948452, -0.2476526470514497091 ) ) ;
#198005=CARTESIAN_POINT ( 'NONE',  ( -0.2408018239684642792, 0.2331886253038339407, -2.134526469895109635 ) ) ;
#198009=CARTESIAN_POINT ( 'NONE',  ( 4.352959896991869471, 0.3989296284454147412, -1.797357466088687961 ) ) ;
#198013=CARTESIAN_POINT ( 'NONE',  ( 2.344387759578896890, 0.3747227385639141373, 1.683394173241028913 ) ) ;
#198015=CARTESIAN_POINT ( 'NONE',  ( 2.022535828336795127, -2.051039051814534719, 1.038070753253451439 ) ) ;
#198017=CARTESIAN_POINT ( 'NONE',  ( 1.652057636490380732, 0.6571787646297929664, -2.164825341390004709 ) ) ;
#198018=CARTESIAN_POINT ( 'NONE',  ( 4.653012138262506703, -1.691843218806210247, 1.254050867608807129 ) ) ;
#198020=CARTESIAN_POINT ( 'NONE',  ( 1.950134490391452369, 0.5496875458596857111, 1.682295776093334139 ) ) ;
#198027=CARTESIAN_POINT ( 'NONE',  ( 4.535507215201760367, -0.1075840215562298280, 2.218897223943790742 ) ) ;
#198028=CARTESIAN_POINT ( 'NONE',  ( 3.644632398932126094, -1.791719913761843364, 1.261548167004488130 ) ) ;
#198033=CARTESIAN_POINT ( 'NONE',  ( 6.610000000000026077, 2.442988107647511509, 2.382821027452782570 ) ) ;
#198035=CARTESIAN_POINT ( 'NONE',  ( 5.713165544288242970, 1.732532623411761286, -1.222520872474173848 ) ) ;
#198037=ORIENTED_EDGE ( 'NONE', *, *, #118416, .T. ) ;
#198039=CARTESIAN_POINT ( 'NONE',  ( 6.280167721515548251, -1.160692707240444710, 1.823489969145650313 ) ) ;
#198041=CARTESIAN_POINT ( 'NONE',  ( 6.515202330376022921, -1.784155196879381622, 0.4545711315065634195 ) ) ;
#198044=CARTESIAN_POINT ( 'NONE',  ( 0.9776059304600862587, -1.697647217183468449, -0.3827929467696991050 ) ) ;
#198046=CARTESIAN_POINT ( 'NONE',  ( 0.6956633456795427994, -1.384754418207832405, -1.389998539416361645 ) ) ;
#198049=CARTESIAN_POINT ( 'NONE',  ( 4.715790015261832835, -2.120648752638915724, 0.4184459369844309440 ) ) ;
#198052=CARTESIAN_POINT ( 'NONE',  ( 4.311504812833309330, -0.3723461477018601973, 2.129241309423899775 ) ) ;
#198055=CARTESIAN_POINT ( 'NONE',  ( 6.011001170722232168, 1.737326539053269059, 0.9316862151012759163 ) ) ;
#198056=CARTESIAN_POINT ( 'NONE',  ( 5.501237755103592697, 1.708535605516453115, 0.2940088878824585472 ) ) ;
#198059=CARTESIAN_POINT ( 'NONE',  ( 1.769323484426460480, 2.095969018468134770, -0.6401429536977767398 ) ) ;
#198060=CARTESIAN_POINT ( 'NONE',  ( 3.294260915971382264, -0.9370450057796105847, 2.108945393182542372 ) ) ;
#198061=CARTESIAN_POINT ( 'NONE',  ( 4.745419391729821967, -1.590323190411299770, -1.310567541734160457 ) ) ;
#198062=CARTESIAN_POINT ( 'NONE',  ( 0.1462902992968219407, -1.560392365369901668, 1.155808223090015963 ) ) ;
#198067=CARTESIAN_POINT ( 'NONE',  ( 3.533539421053989660, -0.1523460092780377639, 2.115156586662121363 ) ) ;
#198069=CARTESIAN_POINT ( 'NONE',  ( 1.406875202279284753, -1.122500148236497575, -1.674886495921081631 ) ) ;
#198071=CARTESIAN_POINT ( 'NONE',  ( 4.296070028909639404, -0.8476096858263427736, 2.037697185916572007 ) ) ;
#198081=CARTESIAN_POINT ( 'NONE',  ( 4.241127833599818153, -1.794087422336073878, 1.013995622381487216 ) ) ;
#198084=CARTESIAN_POINT ( 'NONE',  ( 3.106122398345218638, -0.8164384046550461349, 1.847479848726358398 ) ) ;
#198087=CARTESIAN_POINT ( 'NONE',  ( 2.588805925060005730, -0.3509353788873382229, -2.030617818815634745 ) ) ;
#198091=CARTESIAN_POINT ( 'NONE',  ( -0.2409995289980003397, 4.087843961663322645, -2.555282842491034323 ) ) ;
#198092=CARTESIAN_POINT ( 'NONE',  ( 1.780954670855667388, 1.268887097626215876, 1.334285251370644021 ) ) ;
#198093=CARTESIAN_POINT ( 'NONE',  ( 6.305322857734435793, 1.832379230283949667, 1.229636283518860118 ) ) ;
#198095=CARTESIAN_POINT ( 'NONE',  ( 1.774925396934714295, -2.051924176137665423, -0.6798970441593693570 ) ) ;
#198097=CARTESIAN_POINT ( 'NONE',  ( 1.481658059775035952, -0.6748446255696785023, 1.900416712880992343 ) ) ;
#198099=CARTESIAN_POINT ( 'NONE',  ( 0.5318453760667535279, 0.9654296485097979552, -1.602142582367314549 ) ) ;
#198101=CARTESIAN_POINT ( 'NONE',  ( 4.926621433916460902, 1.886357061574754690, 0.5729670753305516895 ) ) ;
#198102=CARTESIAN_POINT ( 'NONE',  ( 4.294157853547872605, -0.8666056138363428252, -1.820986994602634024 ) ) ;
#198106=CARTESIAN_POINT ( 'NONE',  ( 6.692010077984027916, -0.9030311967607449475, 1.901034507416640373 ) ) ;
#198107=CARTESIAN_POINT ( 'NONE',  ( 5.283670394142272464, -1.967056725255760474, 0.6460906113585006549 ) ) ;
#198111=CARTESIAN_POINT ( 'NONE',  ( 5.625262229866254238, 1.783287769691415781, 0.9483128780355275511 ) ) ;
#198113=CARTESIAN_POINT ( 'NONE',  ( 3.651255599878608926, -1.887205614810626209, 1.327874790813722949 ) ) ;
#198114=CARTESIAN_POINT ( 'NONE',  ( 0.9716179518045722219, -0.3065469058200780972, 2.039571770164672504 ) ) ;
#198121=CARTESIAN_POINT ( 'NONE',  ( 4.369693832449129012, -0.3752608539947903665, 2.138364329090262306 ) ) ;
#198125=CARTESIAN_POINT ( 'NONE',  ( 2.788419073117563762, 1.577926727847511312, -0.9486480243563880643 ) ) ;
#198127=CARTESIAN_POINT ( 'NONE',  ( 4.827760788416924242, 1.126602223531171898, -1.879657820484957664 ) ) ;
#198129=CARTESIAN_POINT ( 'NONE',  ( 4.838899928913665605, 0.3820838354035635542, 2.229877907420589001 ) ) ;
#198135=CARTESIAN_POINT ( 'NONE',  ( 6.573528787226094572, 1.692674132781073260, -0.5166258990680439034 ) ) ;
#198136=CARTESIAN_POINT ( 'NONE',  ( 4.178388974671240597, 0.9510918172684652561, 1.774266679505158262 ) ) ;
#198138=CARTESIAN_POINT ( 'NONE',  ( 3.557739748072580088, 0.5135893094758836597, -2.042235538380641202 ) ) ;
#198139=CARTESIAN_POINT ( 'NONE',  ( 0.5971114826688945776, -0.2799204757548044986, 1.894894164429518746 ) ) ;
#198140=CARTESIAN_POINT ( 'NONE',  ( 2.488665619784910188, 1.909654154697162598, 0.4814545106021291265 ) ) ;
#198141=CARTESIAN_POINT ( 'NONE',  ( 0.5670072068131201126, 0.1877032549213939472, -1.861219751863735672 ) ) ;
#198142=CARTESIAN_POINT ( 'NONE',  ( 1.223018651738450480, -1.772137153356953432, -0.8420139538000551704 ) ) ;
#198143=CARTESIAN_POINT ( 'NONE',  ( 0.1582721923853447621, 1.907395734848855051, 0.1385995803297388196 ) ) ;
#198147=CARTESIAN_POINT ( 'NONE',  ( 5.717618200960679964, -1.824738551054584157, 0.4112096411929695994 ) ) ;
#198150=CARTESIAN_POINT ( 'NONE',  ( 6.350451050988413115, -2.059726887988411637, -0.2088473404622398499 ) ) ;
#198152=CARTESIAN_POINT ( 'NONE',  ( 1.205626512970816355, -1.630946839658468983, -1.275175305487465049 ) ) ;
#198157=CARTESIAN_POINT ( 'NONE',  ( 5.074906250706387567, -1.535530725987072298, 1.462626433913247093 ) ) ;
#198161=CARTESIAN_POINT ( 'NONE',  ( 6.127397123722368555, 0.1457569626216181913, -1.956525209266091192 ) ) ;
#198163=CARTESIAN_POINT ( 'NONE',  ( 3.251327214347735417, -1.985796489957316613, -0.3474142817363469748 ) ) ;
#198164=CARTESIAN_POINT ( 'NONE',  ( 3.854619899909034419, -1.789536248510626315, -0.6842995647342240417 ) ) ;
#198167=CARTESIAN_POINT ( 'NONE',  ( 1.646283778714407342, 0.6915601415973006150, 2.079641132013386517 ) ) ;
#198169=CARTESIAN_POINT ( 'NONE',  ( 3.163207368312019430, 0.2779861718534247794, -1.849665920529340646 ) ) ;
#198173=CARTESIAN_POINT ( 'NONE',  ( 6.099228927766127129, -0.2589519472634767006, 2.101251757753983984 ) ) ;
#198175=CARTESIAN_POINT ( 'NONE',  ( 6.654741963219192868, -0.5482099483974657295, -1.996413779700876301 ) ) ;
#198176=CARTESIAN_POINT ( 'NONE',  ( 2.191069407410517478, 1.617985365078830950, 1.324160459713573879 ) ) ;
#198177=CARTESIAN_POINT ( 'NONE',  ( 6.620655732516625314, 7.629137130509059617, 2.773739711112707340 ) ) ;
#198178=CARTESIAN_POINT ( 'NONE',  ( 0.3754632410046651048, 0.9867877818048297334, 1.414398233496700907 ) ) ;
#198187=CARTESIAN_POINT ( 'NONE',  ( 1.365539917532717196, 0.5261944252722695614, -1.733370571883424693 ) ) ;
#198192=CARTESIAN_POINT ( 'NONE',  ( 6.539320575229274901, 7.629137130509072051, 2.496737603865983424 ) ) ;
#198197=CARTESIAN_POINT ( 'NONE',  ( 2.664321193032999524, -0.7092454343347885937, -1.720814620647417303 ) ) ;
#198199=CARTESIAN_POINT ( 'NONE',  ( -0.08845379458875551881, -1.178863245278682026, -1.510317944339079732 ) ) ;
#198200=CARTESIAN_POINT ( 'NONE',  ( 6.106463915388694375, -0.6937866221692154944, -1.797298315204816310 ) ) ;
#198205=CARTESIAN_POINT ( 'NONE',  ( 5.172688686914132639, 1.361056241693802349, -1.423677202773800721 ) ) ;
#198206=CARTESIAN_POINT ( 'NONE',  ( 1.612141420133822223, -0.7113448269009944314, 1.997755531611951962 ) ) ;
#198210=CARTESIAN_POINT ( 'NONE',  ( 6.333935822332933618, 2.167035306593240840, 0.3253760364356065860 ) ) ;
#198212=CARTESIAN_POINT ( 'NONE',  ( 4.524389607583827910, 1.185449959155547850, -1.518358881950541139 ) ) ;
#198214=CARTESIAN_POINT ( 'NONE',  ( 0.1822601575737579360, -1.769359155225664226, -0.4491840103194589817 ) ) ;
#198215=CARTESIAN_POINT ( 'NONE',  ( 1.454063653991678473, 0.6380318336138122159, -2.112638918738508398 ) ) ;
#198216=FACE_OUTER_BOUND ( 'NONE', #42796, .T. ) ;
#198220=CARTESIAN_POINT ( 'NONE',  ( 6.139503339746209321, 1.821095124518475217, -0.7503768741054758218 ) ) ;
#198221=CARTESIAN_POINT ( 'NONE',  ( 1.892034919678585281, -0.5197426219408564085, -1.871140422112322232 ) ) ;
#198222=CARTESIAN_POINT ( 'NONE',  ( 6.643951024375948755, -0.1027215121673381443, -2.296211363497886460 ) ) ;
#198224=CARTESIAN_POINT ( 'NONE',  ( 4.768306509995578146, -0.7929947328253506011, -1.683642203456004127 ) ) ;
#198230=CARTESIAN_POINT ( 'NONE',  ( 0.02921319935947005314, -2.001080581411585513, 0.8940957790435491992 ) ) ;
#198235=CARTESIAN_POINT ( 'NONE',  ( 1.207329354700342305, -0.4456725867950651621, 1.770335049871730071 ) ) ;
#198237=CARTESIAN_POINT ( 'NONE',  ( 3.762146167370096883, 1.631196324480500115, -0.5889743285819144525 ) ) ;
#198239=CARTESIAN_POINT ( 'NONE',  ( 6.609000000000015973, 2.967897204652646614, 2.453190122791535366 ) ) ;
#198241=CARTESIAN_POINT ( 'NONE',  ( 0.02974079377688309753, -1.184178705181990532, -1.520296634558585547 ) ) ;
#198242=CARTESIAN_POINT ( 'NONE',  ( 4.557442073745519018, 1.573120015848201492, 1.171846803954358363 ) ) ;
#198245=CARTESIAN_POINT ( 'NONE',  ( 4.758503674095369007, 2.114844282287762667, 0.1552407789479764433 ) ) ;
#198248=CARTESIAN_POINT ( 'NONE',  ( 2.395452669547156077, -1.851176756146424074, 0.9269567275110508486 ) ) ;
#198252=CARTESIAN_POINT ( 'NONE',  ( 2.479437202158024878, -2.292751561675594907, -0.1657748548101884711 ) ) ;
#198258=ADVANCED_FACE ( 'NONE', ( #104783 ), #176949, .T. ) ;
#198259=CARTESIAN_POINT ( 'NONE',  ( 4.500206361630255003, -0.8965733778899236395, 1.689174240301967389 ) ) ;
#198261=CARTESIAN_POINT ( 'NONE',  ( 4.858271033065001632, 0.6623171007707692182, 1.592740567422048947 ) ) ;
#198262=CARTESIAN_POINT ( 'NONE',  ( 3.503138892209650024, -0.1435209762444041581, 2.011451614702438828 ) ) ;
#198263=CARTESIAN_POINT ( 'NONE',  ( 5.572921396849181974, -1.036564899910274784, 2.051751470549934453 ) ) ;
#198265=CARTESIAN_POINT ( 'NONE',  ( 0.5224629442122545875, -1.184049029929446828, -1.862174541895257995 ) ) ;
#198267=CARTESIAN_POINT ( 'NONE',  ( 5.360532716240259177, -1.281408969121943464, 1.220901466008792235 ) ) ;
#198269=CARTESIAN_POINT ( 'NONE',  ( 2.379227630831231011, 2.094957926495308875, -0.9307781363587577239 ) ) ;
#198270=CARTESIAN_POINT ( 'NONE',  ( 6.386648935047418263, 1.599332519906123462, -0.9119682274050244786 ) ) ;
#198278=CARTESIAN_POINT ( 'NONE',  ( 6.531696417657103737, 1.982406992490031383, -0.5971068152322634992 ) ) ;
#198279=CARTESIAN_POINT ( 'NONE',  ( 2.430875351317234756, -1.673853735218135741, 1.124246214196801485 ) ) ;
#198281=CARTESIAN_POINT ( 'NONE',  ( 5.408790948643045660, 1.457530049539386141, -1.259864545333173158 ) ) ;
#198283=CARTESIAN_POINT ( 'NONE',  ( 2.689914112924804090, 2.107969469017998421, -0.7009301692152307695 ) ) ;
#198288=CARTESIAN_POINT ( 'NONE',  ( 5.653775904655955920, 0.7130309894091393375, 1.587888939141286038 ) ) ;
#198289=CARTESIAN_POINT ( 'NONE',  ( 4.000408739481801312, 1.952204270133122810, 0.1946113827649766925 ) ) ;
#198293=CARTESIAN_POINT ( 'NONE',  ( 4.974029133664690683, 1.296991790296280422, 1.853570637303619817 ) ) ;
#198295=CARTESIAN_POINT ( 'NONE',  ( 1.434110160756268737, 1.226943730116908160, 1.657962230405624515 ) ) ;
#198298=CARTESIAN_POINT ( 'NONE',  ( 2.641812911801244113, -1.676132216910112493, -1.519885475924544593 ) ) ;
#198301=CARTESIAN_POINT ( 'NONE',  ( 2.460033746253722065, 0.7958763861501785275, 1.692906160045657860 ) ) ;
#198302=CARTESIAN_POINT ( 'NONE',  ( 1.283399958720226497, 1.417952419849175305, -0.9979722560638002449 ) ) ;
#198303=EDGE_CURVE ( 'NONE', #29350, #21442, #160168, .T. ) ;
#198304=CARTESIAN_POINT ( 'NONE',  ( 5.337503337980974649, 0.8888059580158399475, -2.003405333693850654 ) ) ;
#198305=CARTESIAN_POINT ( 'NONE',  ( 6.282281253371452934, -1.241832687457484985, 1.944794379655417682 ) ) ;
#198306=CARTESIAN_POINT ( 'NONE',  ( 1.727488365587977359, -1.940856233752264348, 0.6934696639643816996 ) ) ;
#198307=CARTESIAN_POINT ( 'NONE',  ( 3.591681417399609888, -1.939766604489696622, -0.09448766823863874453 ) ) ;
#198309=CARTESIAN_POINT ( 'NONE',  ( 5.325416506339426981, -1.776575524504428794, 0.5857008802128694791 ) ) ;
#198310=CARTESIAN_POINT ( 'NONE',  ( 0.8125000000000005551, 1.451031289061154306, 1.451031289061088136 ) ) ;
#198313=CARTESIAN_POINT ( 'NONE',  ( 6.380232485702068246, -0.2495653932444163448, 2.000551205290925783 ) ) ;
#198316=CARTESIAN_POINT ( 'NONE',  ( 4.219375079941334761, 1.978050461189932552, 0.3905991720301109082 ) ) ;
#198320=CARTESIAN_POINT ( 'NONE',  ( 2.631258204695927194, -1.703542010001803275, 0.6570300758180421807 ) ) ;
#198328=CARTESIAN_POINT ( 'NONE',  ( 0.3694064801790334918, -1.708597689296184274, -1.076810303892479226 ) ) ;
#198329=CARTESIAN_POINT ( 'NONE',  ( 6.393255305546848177, -0.1058262492604696708, -2.218914918540932035 ) ) ;
#198333=CARTESIAN_POINT ( 'NONE',  ( 6.262583990076592499, -1.459235794176002132, 1.455568404382314718 ) ) ;
#198334=CARTESIAN_POINT ( 'NONE',  ( 5.256482491209823138, 1.942542154241846619, -0.5404887192124521178 ) ) ;
#198342=ORIENTED_EDGE ( 'NONE', *, *, #34638, .T. ) ;
#198344=CARTESIAN_POINT ( 'NONE',  ( 5.132185397524263060, 0.2004025303571632666, -2.006139158026089220 ) ) ;
#198345=CARTESIAN_POINT ( 'NONE',  ( 4.839718430358881385, 1.836437689789902628, 0.1323948491315785347 ) ) ;
#198346=CARTESIAN_POINT ( 'NONE',  ( -0.02338929933909209349, 2.063686797106215387, -2.128951798380565918 ) ) ;
#198347=CARTESIAN_POINT ( 'NONE',  ( 3.053680222918000453, -1.886840229487633414, -1.328398743635789803 ) ) ;
#198349=CARTESIAN_POINT ( 'NONE',  ( 4.323607124742586016, -2.069909602744592014, 0.6229453038564189971 ) ) ;
#198351=CARTESIAN_POINT ( 'NONE',  ( 0.7494335824394976475, 1.939781244166354002, -0.09678450214786055161 ) ) ;
#198356=CARTESIAN_POINT ( 'NONE',  ( 2.957714569337116295, 1.861795396119047208, -0.1817069356538636715 ) ) ;
#198357=CARTESIAN_POINT ( 'NONE',  ( 1.687617486097678476, 1.829050272730630144, -0.5582976189952293389 ) ) ;
#198360=CARTESIAN_POINT ( 'NONE',  ( 3.071135375186518690, -2.039199700013223815, -0.8442704067812344393 ) ) ;
#198366=CARTESIAN_POINT ( 'NONE',  ( 0.9308618464644430324, 0.1408870404581187008, 1.966361230860876441 ) ) ;
#198367=CARTESIAN_POINT ( 'NONE',  ( 6.305331169356420240, 1.914788864002760160, 1.287784001537124468 ) ) ;
#198368=CARTESIAN_POINT ( 'NONE',  ( 1.187862215860764126, -1.241893603568875903, -1.518774446641702580 ) ) ;
#198369=CARTESIAN_POINT ( 'NONE',  ( 5.225460488781804358, 0.2076664479006613828, -2.052122333454815539 ) ) ;
#198376=CARTESIAN_POINT ( 'NONE',  ( 0.5851434883720012525, 2.077150299251043553, 0.6315224188822368134 ) ) ;
#198378=CARTESIAN_POINT ( 'NONE',  ( 6.409700764581637067, -0.8744420883355051854, -1.620376909479949390 ) ) ;
#198381=CARTESIAN_POINT ( 'NONE',  ( 1.141631569582121752, 0.7634220068381202262, -1.707866752806507460 ) ) ;
#198382=CARTESIAN_POINT ( 'NONE',  ( 5.887991582945824476, -0.9777203880148609416, 1.927937229880334113 ) ) ;
#198384=CARTESIAN_POINT ( 'NONE',  ( 0.07735805125223639556, 7.629137130509110243, -2.688903128390319530 ) ) ;
#198387=CARTESIAN_POINT ( 'NONE',  ( 0.8031952904608251620, 1.686239601473665140, -0.9019194118903075541 ) ) ;
#198389=CARTESIAN_POINT ( 'NONE',  ( 3.203702280051218931, -1.767899805609447261, 0.08541964596707474211 ) ) ;
#198390=CARTESIAN_POINT ( 'NONE',  ( 1.207504981961624813, 1.448612403150219885, 1.248453992567559512 ) ) ;
#198393=CARTESIAN_POINT ( 'NONE',  ( 5.853135685669797361, 0.1356727809044282473, -1.910850313501164743 ) ) ;
#198394=CARTESIAN_POINT ( 'NONE',  ( 6.004353349036935406, 1.967244357045078607, 0.09818725807526038074 ) ) ;
#198396=CARTESIAN_POINT ( 'NONE',  ( 0.9320672075895162223, -2.067649466203642206, 0.4702014512557165515 ) ) ;
#198398=CARTESIAN_POINT ( 'NONE',  ( 4.117926171558832671, -0.9613396577640184182, -1.604580606731422554 ) ) ;
#198399=CARTESIAN_POINT ( 'NONE',  ( 0.9085097582094739943, 1.384192474337717194, -1.190531929384466281 ) ) ;
#198401=CARTESIAN_POINT ( 'NONE',  ( 3.106307083854151774, -2.204334110825040494, 0.1085914373066959593 ) ) ;
#198404=CARTESIAN_POINT ( 'NONE',  ( 1.627463713854758298, 0.1539993984382737602, -2.057001629134532550 ) ) ;
#198410=CARTESIAN_POINT ( 'NONE',  ( 6.451426615364327155, -1.705040744490589066, 0.8662930942644477827 ) ) ;
#198412=CARTESIAN_POINT ( 'NONE',  ( 4.387213907293201487, 0.09840592021137170575, 2.068135374880715638 ) ) ;
#198414=CARTESIAN_POINT ( 'NONE',  ( 1.722176697685766200, -1.199285583244277253, -1.798187405066300038 ) ) ;
#198416=CARTESIAN_POINT ( 'NONE',  ( 2.385421078170113507, 0.09676420124534937384, -2.017471438767451275 ) ) ;
#198418=ORIENTED_EDGE ( 'NONE', *, *, #157150, .F. ) ;
#198422=CARTESIAN_POINT ( 'NONE',  ( 0.09298292169932984019, 1.756857073293972116, 0.9896806593640145033 ) ) ;
#198423=CARTESIAN_POINT ( 'NONE',  ( 6.639320575229257670, 3.688898292602959650, 2.617366112374151399 ) ) ;
#198424=CARTESIAN_POINT ( 'NONE',  ( 4.476244563333130699, -2.125884358948509689, -0.5320566845071761364 ) ) ;
#198426=CARTESIAN_POINT ( 'NONE',  ( 3.814637755342592307, -0.6046605605216844870, -1.814329123173196834 ) ) ;
#198430=CARTESIAN_POINT ( 'NONE',  ( 1.669546221992053603, 1.392560760841387246, 1.458543886677300394 ) ) ;
#198432=CARTESIAN_POINT ( 'NONE',  ( 0.9961154782066735658, -2.292545471836278992, 0.006648471028786878678 ) ) ;
#198434=CARTESIAN_POINT ( 'NONE',  ( 4.049579987339441800, 0.5806670320154716514, -1.624208954244592773 ) ) ;
#198438=CARTESIAN_POINT ( 'NONE',  ( 0.7308173252688826560, -1.846041318942293286, -0.6644482084196751126 ) ) ;
#198439=CARTESIAN_POINT ( 'NONE',  ( 0.6021629784135495989, -0.6261829430146518272, -1.762877433595814614 ) ) ;
#198441=CARTESIAN_POINT ( 'NONE',  ( 0.1753634416057497925, 6.947017063990798214, -2.739087685391654148 ) ) ;
#198443=CARTESIAN_POINT ( 'NONE',  ( 0.2392000317489213768, -0.1454578200970526591, -2.037356452166842580 ) ) ;
#198445=CARTESIAN_POINT ( 'NONE',  ( 4.775916358578648158, 1.790991888885495431, -0.2707881515907252234 ) ) ;
#198449=CARTESIAN_POINT ( 'NONE',  ( 5.795527448272657089, 1.671165027121311430, -0.6995385440057879656 ) ) ;
#198454=CARTESIAN_POINT ( 'NONE',  ( 6.074623017180313944, 1.249363044128497524, -1.379498876745478109 ) ) ;
#198456=CARTESIAN_POINT ( 'NONE',  ( 3.708511580433976107, 1.820041504565768742, 0.5977543794245043784 ) ) ;
#198463=CARTESIAN_POINT ( 'NONE',  ( 5.999228916948370127, -0.2569761400621084491, 2.101594505611179109 ) ) ;
#198464=CARTESIAN_POINT ( 'NONE',  ( 0.1984014031938194922, -2.161264429664040421, -0.05129915172277095536 ) ) ;
#198467=CARTESIAN_POINT ( 'NONE',  ( 1.272165501999738435, -1.161393580401563375, 1.408505525491813515 ) ) ;
#198469=CARTESIAN_POINT ( 'NONE',  ( 3.539906422930443775, 0.8216601389946125433, -1.630302437610211763 ) ) ;
#198472=ORIENTED_EDGE ( 'NONE', *, *, #178034, .F. ) ;
#198473=CARTESIAN_POINT ( 'NONE',  ( 2.506254056688070886, 1.969067392671639771, 0.05118484259234063610 ) ) ;
#198474=CARTESIAN_POINT ( 'NONE',  ( 4.616706917144582256, -0.09184519841067168011, 1.939997386343417896 ) ) ;
#198477=CARTESIAN_POINT ( 'NONE',  ( 4.957343421279006179, -1.817532610912236724, 1.092287347377165485 ) ) ;
#198481=EDGE_LOOP ( 'NONE', ( #152396, #100216 ) ) ;
#198486=CARTESIAN_POINT ( 'NONE',  ( 5.039593146249602640, -1.293522693445446015, -1.288650932716684849 ) ) ;
#198491=CARTESIAN_POINT ( 'NONE',  ( 5.260568668178753349, -1.354309965608934352, 1.290672426560689035 ) ) ;
#198499=CARTESIAN_POINT ( 'NONE',  ( 6.526262532640958902, 1.108799689610693751, 1.866440817598405966 ) ) ;
#198500=CARTESIAN_POINT ( 'NONE',  ( 2.724332569758937339, 2.101576450279537767, 0.2563457491038360070 ) ) ;
#198503=CARTESIAN_POINT ( 'NONE',  ( 6.297728486381423352, -1.495382609916453998, -1.431936454106122358 ) ) ;
#198508=CARTESIAN_POINT ( 'NONE',  ( 2.308868829589076022, 2.048438961056008090, 1.028902946192054912 ) ) ;
#198511=CARTESIAN_POINT ( 'NONE',  ( 2.320441991784210067, -0.7354482596747033973, -1.765520077574176394 ) ) ;
#198515=CARTESIAN_POINT ( 'NONE',  ( 0.1584477454876299096, 2.008078640038186258, 0.1440931537372847071 ) ) ;
#198516=CARTESIAN_POINT ( 'NONE',  ( 0.8308171121041010299, -1.845250773774274267, -0.6662997747023179373 ) ) ;
#198520=CARTESIAN_POINT ( 'NONE',  ( 4.224618542793646014, 0.1023655851960032920, 2.088258538514795593 ) ) ;
#198521=CARTESIAN_POINT ( 'NONE',  ( 2.236828121427667071, -1.582394523617111970, 0.7928310554637070240 ) ) ;
#198524=CARTESIAN_POINT ( 'NONE',  ( 5.367208288505312730, 2.210367218987763671, -0.6069939957479841830 ) ) ;
#198525=CARTESIAN_POINT ( 'NONE',  ( 3.503586914695429488, -0.7067764301678289840, -1.590537823618918711 ) ) ;
#198528=CARTESIAN_POINT ( 'NONE',  ( 3.549848462767680068, 1.568450346167485243, -0.7392937452721718428 ) ) ;
#198529=CARTESIAN_POINT ( 'NONE',  ( 3.279888855285200577, -2.093262694144955027, 0.5762538248230695270 ) ) ;
#198531=CARTESIAN_POINT ( 'NONE',  ( 5.524625123954316486, 0.3981063221985549072, 1.976670730632006601 ) ) ;
#198532=CARTESIAN_POINT ( 'NONE',  ( 6.593749840436431420, -1.895867669153237456, -0.7852924748296338242 ) ) ;
#198535=CARTESIAN_POINT ( 'NONE',  ( 1.993070439633041424, 1.677129747370089019, -0.9476047394562473469 ) ) ;
#198537=CARTESIAN_POINT ( 'NONE',  ( 6.205373625529961856, 1.933303589146176948, -1.094015395867214080 ) ) ;
#198539=CARTESIAN_POINT ( 'NONE',  ( 6.983263157960372780, 1.247263239625576059, 2.158450195331083510 ) ) ;
#198543=CARTESIAN_POINT ( 'NONE',  ( 1.454100989278300560, -1.612054358864203785, -1.528463602881096284 ) ) ;
#198549=CARTESIAN_POINT ( 'NONE',  ( 4.123522620141695683, 0.2556129913668835907, -2.046733346555211330 ) ) ;
#198553=CARTESIAN_POINT ( 'NONE',  ( 5.501189692264965458, 1.528658022856645315, 1.077728667985423661 ) ) ;
#198554=CARTESIAN_POINT ( 'NONE',  ( 4.834428552630634535, 0.5376618173574229109, -1.648781088846348108 ) ) ;
#198555=CARTESIAN_POINT ( 'NONE',  ( 3.966134247641060817, -1.625707123410979449, -0.6219663355369866586 ) ) ;
#198558=CARTESIAN_POINT ( 'NONE',  ( 1.628911237561550873, 0.2300632485819526785, 2.280818132175948421 ) ) ;
#198560=CARTESIAN_POINT ( 'NONE',  ( 6.058164993413670096, -1.477959563288837375, 1.479067623735799586 ) ) ;
#198561=CARTESIAN_POINT ( 'NONE',  ( 1.077780131904103156, -1.795810734350095750, -0.4053039038426772267 ) ) ;
#198563=CARTESIAN_POINT ( 'NONE',  ( 1.688125190044654556, 1.678006053171029688, 1.117831401076685660 ) ) ;
#198569=CARTESIAN_POINT ( 'NONE',  ( 3.035902975225315714, -2.043024508941180706, 0.5676086983019896781 ) ) ;
#198571=CARTESIAN_POINT ( 'NONE',  ( 5.215394836314163562, -0.2642288504575221464, 1.806346989861665087 ) ) ;
#198579=CARTESIAN_POINT ( 'NONE',  ( 3.515882793631277536, -0.5824337298786783634, 1.934013565619496999 ) ) ;
#198580=CARTESIAN_POINT ( 'NONE',  ( 6.809632187368197087, -0.4906261968062891055, 2.159508175712351541 ) ) ;
#198583=CARTESIAN_POINT ( 'NONE',  ( 4.873795578896718439, -1.825537460381383870, 0.3603196638213671532 ) ) ;
#198588=CARTESIAN_POINT ( 'NONE',  ( 6.262583990076592499, -1.459235794176002132, 1.455568404382314718 ) ) ;
#198592=CARTESIAN_POINT ( 'NONE',  ( 1.932526292592825046, 0.8863411937694037901, 1.489983018702551787 ) ) ;
#198593=CARTESIAN_POINT ( 'NONE',  ( 1.007268549873532981, -0.7791258169532075950, -1.556267712415648763 ) ) ;
#198594=CARTESIAN_POINT ( 'NONE',  ( 0.1304780226794301778, -1.424241760892838382, -1.816604428824322159 ) ) ;
#198597=CARTESIAN_POINT ( 'NONE',  ( 2.794271844819782302, -2.055044804604218456, -0.1548302833056774130 ) ) ;
#198599=CARTESIAN_POINT ( 'NONE',  ( 1.264999722075825561, -2.016288307338756525, -0.002813990012486000669 ) ) ;
#198604=CARTESIAN_POINT ( 'NONE',  ( 6.385618529757402406, 1.291587659170100766, 1.353439767483602285 ) ) ;
#198606=CARTESIAN_POINT ( 'NONE',  ( 4.922078805074791674, -1.902621863305080430, 0.1933406509087298719 ) ) ;
#198608=CARTESIAN_POINT ( 'NONE',  ( 6.463508838306311510, 0.3818026259072569983, -2.173449913608487716 ) ) ;
#198612=CARTESIAN_POINT ( 'NONE',  ( 6.551439628692993900, -1.894445571042557619, 0.9528467149547341641 ) ) ;
#198615=CARTESIAN_POINT ( 'NONE',  ( 3.522812192065057690, 1.465757825172078865, -1.782263946013421974 ) ) ;
#198616=CARTESIAN_POINT ( 'NONE',  ( 5.318788500806308051, -1.422220495204097546, 1.351624447685224162 ) ) ;
#198617=CARTESIAN_POINT ( 'NONE',  ( 1.375751926856683127, -1.915142299924106339, 0.4244507266663796741 ) ) ;
#198621=CARTESIAN_POINT ( 'NONE',  ( -0.1529269513586241080, -1.894431756695889923, -0.9458152384202949126 ) ) ;
#198623=CARTESIAN_POINT ( 'NONE',  ( 0.5504183687293667804, -1.553892155338543191, -0.9872222399871023457 ) ) ;
#198624=CARTESIAN_POINT ( 'NONE',  ( 4.786072553063510426, -1.330480670633835683, -1.715586834332043953 ) ) ;
#198626=CARTESIAN_POINT ( 'NONE',  ( 1.459403507577087700, -1.788631592985808538, 1.138920039206146928 ) ) ;
#198631=CARTESIAN_POINT ( 'NONE',  ( 2.460294058246147664, 0.8780975587320086762, 1.864460488959890139 ) ) ;
#198638=CARTESIAN_POINT ( 'NONE',  ( 4.371672787583542608, 0.4156390277068115480, -1.866406306929219605 ) ) ;
#198640=CARTESIAN_POINT ( 'NONE',  ( 1.423510532338147394, -0.05571650319935492202, 2.261890015172054458 ) ) ;
#198642=CARTESIAN_POINT ( 'NONE',  ( 0.8436869049191192405, -1.150191864323051982, -1.399547552825676666 ) ) ;
#198643=CARTESIAN_POINT ( 'NONE',  ( 1.973720722908858249, -0.8152147109428582450, 1.733722481544483163 ) ) ;
#198644=CARTESIAN_POINT ( 'NONE',  ( 3.086448098943677998, 1.152334561581969785, -1.719836228861029603 ) ) ;
#198646=CARTESIAN_POINT ( 'NONE',  ( 0.8484322082523039210, 0.5699466304493487900, 1.887293252202123739 ) ) ;
#198647=CARTESIAN_POINT ( 'NONE',  ( 5.338475953816137931, 1.898335173771143580, 0.3273637156304096130 ) ) ;
#198648=CARTESIAN_POINT ( 'NONE',  ( 1.401454987343775382, 1.884297621475890416, -1.332007787593261883 ) ) ;
#198651=CARTESIAN_POINT ( 'NONE',  ( 5.775849841709651322, -2.013224797598807569, 0.4483296186361291902 ) ) ;
#198655=CARTESIAN_POINT ( 'NONE',  ( 5.403390757083595730, 1.719820611593615656, 1.215146281773227921 ) ) ;
#198658=CARTESIAN_POINT ( 'NONE',  ( 4.429101881081805914, 0.1011787780425543737, 2.159334005894457231 ) ) ;
#198659=CARTESIAN_POINT ( 'NONE',  ( 5.830724911194343996, 1.354916080449189764, -1.497948107757952174 ) ) ;
#198668=CARTESIAN_POINT ( 'NONE',  ( 3.889861467948489082, -2.010801299972611478, 0.1531677096566556595 ) ) ;
#198674=CARTESIAN_POINT ( 'NONE',  ( 4.610339536224768331, -0.9213992672730475508, -1.955631277330005968 ) ) ;
#198679=CARTESIAN_POINT ( 'NONE',  ( 5.483999976877721672, -2.016598147233912730, 0.002826481282774962345 ) ) ;
#198681=CARTESIAN_POINT ( 'NONE',  ( 0.2227383504175127205, -0.09031333296150539924, 1.722639462886750517 ) ) ;
#198686=CARTESIAN_POINT ( 'NONE',  ( 6.450466390465378730, 0.5869013949594548141, 1.776180802621520005 ) ) ;
#198687=CARTESIAN_POINT ( 'NONE',  ( 0.9088405895168538695, -0.4911093815175514021, -1.952142171939993842 ) ) ;
#198693=CARTESIAN_POINT ( 'NONE',  ( 2.438272501909013901, -1.223040458498025673, -1.732039452853536776 ) ) ;
#198694=CARTESIAN_POINT ( 'NONE',  ( 1.546500145565052886, -1.423948579484592525, 1.427951870166991322 ) ) ;
#198695=CARTESIAN_POINT ( 'NONE',  ( 2.794932832814459811, -0.1373201097526421111, -1.806460840857474937 ) ) ;
#198697=CARTESIAN_POINT ( 'NONE',  ( 6.473507614529132148, 2.070149491355821159, -0.6224772505839873959 ) ) ;
#198701=CARTESIAN_POINT ( 'NONE',  ( 0.3388992355649001476, -1.619940322034026270, -1.022281207937189684 ) ) ;
#198708=CARTESIAN_POINT ( 'NONE',  ( 3.872077330825273389, 1.198917189070296541, 1.798566189592496034 ) ) ;
#198711=CARTESIAN_POINT ( 'NONE',  ( 1.600013431492643967, 1.466117565985028515, 1.532352819790145482 ) ) ;
#198713=CARTESIAN_POINT ( 'NONE',  ( 3.128153591792836252, 1.098079186366843985, -1.637025598404780791 ) ) ;
#198716=CARTESIAN_POINT ( 'NONE',  ( 5.863713558449636487, -0.4802757262234845226, 1.909948281557447114 ) ) ;
#198717=CARTESIAN_POINT ( 'NONE',  ( 2.097507970028670510, -1.941522886764552203, 0.04780177728339052301 ) ) ;
#198725=CARTESIAN_POINT ( 'NONE',  ( 6.252599623108594074, 1.892168639490459325, 0.2757424028280440753 ) ) ;
#198727=CARTESIAN_POINT ( 'NONE',  ( 4.283934280384479543, 1.440456688004333019, 1.672026782002330458 ) ) ;
#198728=CARTESIAN_POINT ( 'NONE',  ( 2.098912041516465266, -0.5885267676426220174, -2.126790307141281033 ) ) ;
#198730=CARTESIAN_POINT ( 'NONE',  ( 1.049298088506251947, -1.728493729547801117, 0.8183166869351958805 ) ) ;
#198733=CARTESIAN_POINT ( 'NONE',  ( 4.721179655770254335, -1.847879960204744432, -0.9338546512941485744 ) ) ;
#198736=CARTESIAN_POINT ( 'NONE',  ( 1.551884642779034262, 0.6273040060550126862, -2.068667048528524344 ) ) ;
#198737=CARTESIAN_POINT ( 'NONE',  ( 4.247736854543925133, 2.191053489037126045, -0.05455935714590579716 ) ) ;
#198744=CARTESIAN_POINT ( 'NONE',  ( 5.607993946907785521, -0.03366334548273764576, 1.734015701317252134 ) ) ;
#198746=CARTESIAN_POINT ( 'NONE',  ( 3.327070777303439364, -1.911029926764183040, -0.7966718667702379353 ) ) ;
#198747=CARTESIAN_POINT ( 'NONE',  ( 5.185217826725932788, 1.731529828693706641, 1.218147590116857026 ) ) ;
#198751=CARTESIAN_POINT ( 'NONE',  ( 3.344544815957225747, -1.939504806627976752, -0.3411970713738179395 ) ) ;
#198752=CARTESIAN_POINT ( 'NONE',  ( 6.105493113454719456, -2.275700256682281264, 0.2746985183333852110 ) ) ;
#198753=CARTESIAN_POINT ( 'NONE',  ( 2.437895498511342574, 0.8609710149188253281, -1.609920059450341778 ) ) ;
#198758=ORIENTED_EDGE ( 'NONE', *, *, #173375, .F. ) ;
#198759=CARTESIAN_POINT ( 'NONE',  ( 4.254156334807709605, 0.8570458487419434501, -1.821774543695050319 ) ) ;
#198760=CARTESIAN_POINT ( 'NONE',  ( 4.241029431094700541, -0.1880360549168894613, -1.952691919460777026 ) ) ;
#198764=CARTESIAN_POINT ( 'NONE',  ( 0.1520488688747126949, 0.8040222321012976403, 1.930173718738151578 ) ) ;
#198765=CARTESIAN_POINT ( 'NONE',  ( 5.506658716161647149, 1.338116961444441921, -1.158480101542769036 ) ) ;
#198767=CARTESIAN_POINT ( 'NONE',  ( 1.799034956846547795, 1.823213324544867397, 1.215573211712846158 ) ) ;
#198768=CARTESIAN_POINT ( 'NONE',  ( 0.5557209801456406417, -1.262220463910254331, 1.198535436172887714 ) ) ;
#198770=CARTESIAN_POINT ( 'NONE',  ( 0.2333690889706925564, 2.018283468528142777, -2.468684669820114586 ) ) ;
#198771=CARTESIAN_POINT ( 'NONE',  ( 0.8204219880046401681, 1.592052673282555286, 0.6642659308724234712 ) ) ;
#198772=CARTESIAN_POINT ( 'NONE',  ( 1.230279809073684172, -2.078304686880276808, -0.9817359432500573080 ) ) ;
#198773=CARTESIAN_POINT ( 'NONE',  ( 0.4686481397476391364, -2.065551408369214137, -0.7328327568804984260 ) ) ;
#198774=CARTESIAN_POINT ( 'NONE',  ( 6.239525021605913047, -1.647457779603450634, -0.5405594386218066649 ) ) ;
#198775=CARTESIAN_POINT ( 'NONE',  ( 3.018423772948013006, -1.088090592406821155, -1.919924466345590108 ) ) ;
#198776=CARTESIAN_POINT ( 'NONE',  ( 1.903425830921786188, -1.835712436893768063, 1.158886079418340875 ) ) ;
#198778=CARTESIAN_POINT ( 'NONE',  ( 1.850927149041701192, -1.938055702826226190, -0.8530577433697658085 ) ) ;
#198780=CARTESIAN_POINT ( 'NONE',  ( 5.631840744973369617, -1.222119163988559354, -1.489112003571291476 ) ) ;
#198782=CARTESIAN_POINT ( 'NONE',  ( 2.929518028021148357, -1.541346711875633435, -1.696969020646617476 ) ) ;
#198786=CARTESIAN_POINT ( 'NONE',  ( 4.864059028628820336, 0.6975124644323873468, -2.109029365712757897 ) ) ;
#198794=CARTESIAN_POINT ( 'NONE',  ( 3.059220373557011818, -1.198860207862334049, 1.621182619130703051 ) ) ;
#198796=CARTESIAN_POINT ( 'NONE',  ( 1.041928790383022774, 1.382269897723470642, 1.531051681482889393 ) ) ;
#198802=CARTESIAN_POINT ( 'NONE',  ( 3.908297495596550597, 1.550167135825938569, -1.549264980215167231 ) ) ;
#198803=CARTESIAN_POINT ( 'NONE',  ( 0.9498425221252141393, -1.824119990893595888, -0.8596288560165299408 ) ) ;
#198804=CARTESIAN_POINT ( 'NONE',  ( 0.6437974683802077935, 0.5340323341261629109, 1.762076181610471526 ) ) ;
#198805=CARTESIAN_POINT ( 'NONE',  ( 4.898102649693969468, -0.7706710736265044437, -2.159050251936722731 ) ) ;
#198806=CARTESIAN_POINT ( 'NONE',  ( 4.382634408885896171, 1.643497958660003144, -0.8300281608688080404 ) ) ;
#198810=CARTESIAN_POINT ( 'NONE',  ( 5.473610661177239933, 1.758888005172161373, -0.4887267171112125164 ) ) ;
#198811=CARTESIAN_POINT ( 'NONE',  ( 4.729138786257041538, 2.011204126674607462, 0.1455352507326590494 ) ) ;
#198813=CARTESIAN_POINT ( 'NONE',  ( 4.065478255348141445, 0.2803405965145295275, -2.245028738816820635 ) ) ;
#198815=CARTESIAN_POINT ( 'NONE',  ( 6.528360061338796427, 1.215782546000489850, -1.719372923949607390 ) ) ;
#198817=CARTESIAN_POINT ( 'NONE',  ( 5.020015195830264787, 2.048331326439792210, -0.3003445753073652469 ) ) ;
#198822=CARTESIAN_POINT ( 'NONE',  ( 1.928227594698066039, 1.109388971949121228, -1.574834034052971399 ) ) ;
#198828=CARTESIAN_POINT ( 'NONE',  ( 0.6859744409541921328, 2.042103856186634925, -0.5713114342573709648 ) ) ;
#198829=CARTESIAN_POINT ( 'NONE',  ( 1.336510806674645391, -1.239524924825789132, -1.843257696707498061 ) ) ;
#198830=CARTESIAN_POINT ( 'NONE',  ( 3.276497419027382563, -1.255868110884267530, 1.690353172608966448 ) ) ;
#198833=CARTESIAN_POINT ( 'NONE',  ( 2.752341281506097470, -1.956419249932477955, -0.1471676765215298721 ) ) ;
#198839=CARTESIAN_POINT ( 'NONE',  ( 2.724977724663907530, 1.532976055022855499, -1.465462182430438798 ) ) ;
#198841=CARTESIAN_POINT ( 'NONE',  ( 4.475024536774164119, 1.792854848340214025, 0.7970393728587571447 ) ) ;
#198842=CARTESIAN_POINT ( 'NONE',  ( 3.590839768554392908, -0.4196827604958653923, -2.120402733634827452 ) ) ;
#198843=CARTESIAN_POINT ( 'NONE',  ( 3.192734241421916419, 1.453351889590439816, 1.130385295574042104 ) ) ;
#198846=CARTESIAN_POINT ( 'NONE',  ( 4.294662974013852441, 1.399676235010495873, 1.034011069942197159 ) ) ;
#198850=CARTESIAN_POINT ( 'NONE',  ( 1.710078970767275885, -2.145365142986368934, 0.2646356489638818088 ) ) ;
#198851=CARTESIAN_POINT ( 'NONE',  ( 3.972029700707707445, 1.727737986437705819, 1.038833660170018769 ) ) ;
#198853=CARTESIAN_POINT ( 'NONE',  ( 1.604591590977550108, -0.7782141685120853580, -2.016947388195994062 ) ) ;
#198855=CARTESIAN_POINT ( 'NONE',  ( 3.291827724629258434, -0.8003651471039547882, 1.801871540228771273 ) ) ;
#198857=CARTESIAN_POINT ( 'NONE',  ( 3.351055748958339908, 0.4689680007726776401, -1.884483806560928398 ) ) ;
#198865=CARTESIAN_POINT ( 'NONE',  ( 0.6752036787147744912, -2.078553970830565145, -0.7415856106591719454 ) ) ;
#198867=CARTESIAN_POINT ( 'NONE',  ( 5.805508902378371694, -1.544246397408255866, -1.209716981170713357 ) ) ;
#198868=CARTESIAN_POINT ( 'NONE',  ( 2.443982611291168006, -1.755769474653746665, -0.9913988478210812305 ) ) ;
#198870=CARTESIAN_POINT ( 'NONE',  ( 3.028621024253768113, 0.5188578782318100657, 2.052648472271414448 ) ) ;
#198874=CARTESIAN_POINT ( 'NONE',  ( 4.048646477676579813, -1.531818510360350327, -1.021117339664041834 ) ) ;
#198877=CARTESIAN_POINT ( 'NONE',  ( 5.607717026683647354, 1.607092460389969446, 1.383685132418293495 ) ) ;
#198881=CARTESIAN_POINT ( 'NONE',  ( 5.290332094886032621, -2.044729594613464041, -0.2563108835951214970 ) ) ;
#198883=CARTESIAN_POINT ( 'NONE',  ( 0.4318009167844725771, 1.066696818439222039, 1.524822319796947934 ) ) ;
#198884=CARTESIAN_POINT ( 'NONE',  ( 2.841158510722852970, 0.6603703904487292498, -1.718939526767604420 ) ) ;
#198889=CARTESIAN_POINT ( 'NONE',  ( 2.578998426009218470, -2.112161100990978202, -0.6396139477699357423 ) ) ;
#198890=CARTESIAN_POINT ( 'NONE',  ( 5.044316441076016844, 2.255832582719615065, 0.1735265121041371095 ) ) ;
#198892=CARTESIAN_POINT ( 'NONE',  ( 4.693523411346745000, 1.687728755266065139, -0.6588045490927648684 ) ) ;
#198893=CARTESIAN_POINT ( 'NONE',  ( 5.489432593909100433, -0.4588279098093718256, 1.859853701273159743 ) ) ;
#198895=CARTESIAN_POINT ( 'NONE',  ( 5.453920962983416665, 1.868457504587007545, -0.09292587778651077712 ) ) ;
#198896=CARTESIAN_POINT ( 'NONE',  ( 4.826513810146395578, -1.216237885654298800, 1.408704720340781869 ) ) ;
#198899=CARTESIAN_POINT ( 'NONE',  ( 6.332837517263664395, 0.1779433324526000226, 1.760853854254845530 ) ) ;
#198900=CARTESIAN_POINT ( 'NONE',  ( -0.2058462039469660110, -0.8663896114125648751, -1.819200108291472606 ) ) ;
#198902=CARTESIAN_POINT ( 'NONE',  ( 2.315183273126443009, 1.881732686034083724, 0.9459776246590365645 ) ) ;
#198908=CARTESIAN_POINT ( 'NONE',  ( 1.424088383587719386, -2.004042310577313302, 0.2513328237187910652 ) ) ;
#198910=CARTESIAN_POINT ( 'NONE',  ( 6.720655732516650716, 2.993363686233801779, 2.180545405541700177 ) ) ;
#198913=CARTESIAN_POINT ( 'NONE',  ( 2.583474834239877449, 1.977432880963815309, -0.8734481387390122809 ) ) ;
#198914=CARTESIAN_POINT ( 'NONE',  ( 6.890000000000029878, 7.629137130509094256, 2.600000000000001421 ) ) ;
#198919=CARTESIAN_POINT ( 'NONE',  ( 6.503150282362620160, -0.1410805869419759218, 1.984311032119711715 ) ) ;
#198921=CARTESIAN_POINT ( 'NONE',  ( 0.7674258922165803076, 2.110627382301712540, -0.5898035449652739848 ) ) ;
#198923=CARTESIAN_POINT ( 'NONE',  ( 1.780510834742056847, -1.209543565243664798, 1.911899112700167880 ) ) ;
#198930=CARTESIAN_POINT ( 'NONE',  ( 2.776313302798124383, -1.692206278411222176, -0.5179841425143881795 ) ) ;
#198932=CARTESIAN_POINT ( 'NONE',  ( 6.774453055690137226, -1.363307072557031985, 1.735998097611628932 ) ) ;
#198937=CARTESIAN_POINT ( 'NONE',  ( 4.939077454563308933, -1.704950310733845065, -1.076300583479961048 ) ) ;
#198940=CARTESIAN_POINT ( 'NONE',  ( 2.447944060942487621, 1.870205405844455049, 0.04815357881200743595 ) ) ;
#198941=CARTESIAN_POINT ( 'NONE',  ( 2.131770371054972912, 1.982354287819853456, -0.5969549857752221023 ) ) ;
#198943=CARTESIAN_POINT ( 'NONE',  ( 2.162237915172473546, 1.912057200688283665, 0.04323261116381121871 ) ) ;
#198948=CARTESIAN_POINT ( 'NONE',  ( -0.03509584499547176162, -1.534781374734139670, 1.140672443274578729 ) ) ;
#198951=CARTESIAN_POINT ( 'NONE',  ( 2.664445928352857429, -0.7481792696971515388, -1.813797970468238985 ) ) ;
#198954=CARTESIAN_POINT ( 'NONE',  ( 5.801066647469003357, -0.3129311994157328303, -2.097281602037828208 ) ) ;
#198956=CARTESIAN_POINT ( 'NONE',  ( 6.925078400183515726, -0.002206826874838820583, 1.955452213090567160 ) ) ;
#198958=CARTESIAN_POINT ( 'NONE',  ( 1.933841784273998332, -1.951746473714164321, 0.4931059669559466063 ) ) ;
#198960=CARTESIAN_POINT ( 'NONE',  ( 0.5623061109219238407, -1.172325791230070857, 1.762859051686527012 ) ) ;
#198962=CARTESIAN_POINT ( 'NONE',  ( 2.189971326302230903, -1.350648006375281929, -1.569233719104834890 ) ) ;
#198966=CARTESIAN_POINT ( 'NONE',  ( 6.017543284830850325, -1.160447301756668104, -1.738784508216392855 ) ) ;
#198968=CARTESIAN_POINT ( 'NONE',  ( 4.225493254642153751, -1.746956894163293361, 0.5300125199643389573 ) ) ;
#198969=CARTESIAN_POINT ( 'NONE',  ( 3.088311256162243446, -1.077087438943722164, 1.456314016777765286 ) ) ;
#198973=CARTESIAN_POINT ( 'NONE',  ( 4.964015014492747291, 2.183396446337606989, -0.3195234977587738667 ) ) ;
#198976=CARTESIAN_POINT ( 'NONE',  ( 4.266199323752727146, 1.911794059647478949, -0.05023246155653331158 ) ) ;
#198984=CARTESIAN_POINT ( 'NONE',  ( 0.6789530235665336422, 1.236279375446739603, 1.364625092910062953 ) ) ;
#198986=CARTESIAN_POINT ( 'NONE',  ( 4.551927186349598031, 1.870183863439809357, -0.04390777100237578529 ) ) ;
#198991=CARTESIAN_POINT ( 'NONE',  ( 1.410928143256191092, -1.555772830594209788, 1.207522851012821308 ) ) ;
#198993=CARTESIAN_POINT ( 'NONE',  ( 1.985954055300429566, -2.015913623055834325, 0.05231662700833779323 ) ) ;
#198997=CARTESIAN_POINT ( 'NONE',  ( 2.923975034273151419, 1.216836049711809586, -1.822369523680394066 ) ) ;
#198998=CARTESIAN_POINT ( 'NONE',  ( 6.586557105272873969, -1.791547847876047594, -0.3505316570680468979 ) ) ;
#199008=CARTESIAN_POINT ( 'NONE',  ( 3.684953445348177148, 1.336164438771630714, 1.267087564277062484 ) ) ;
#199009=CARTESIAN_POINT ( 'NONE',  ( 0.9615884438243198495, -1.588399402277500760, -1.236662224066273019 ) ) ;
#199010=CARTESIAN_POINT ( 'NONE',  ( 2.706789001878449508, -1.702045039646230107, -1.544681222897727357 ) ) ;
#199011=CARTESIAN_POINT ( 'NONE',  ( 6.539320575229281118, 7.629137130509070275, 2.703262396134015866 ) ) ;
#199012=CARTESIAN_POINT ( 'NONE',  ( 0.8306204695724854759, -1.749664030167530138, -0.6342216345150762935 ) ) ;
#199015=CARTESIAN_POINT ( 'NONE',  ( 4.781465250580236415, 0.1816826923375300662, -1.903719681147630016 ) ) ;
#199018=CARTESIAN_POINT ( 'NONE',  ( 3.860945534362031140, 0.2537485593089708336, -2.075202752206976697 ) ) ;
#199019=CARTESIAN_POINT ( 'NONE',  ( 2.149089010626914931, -1.500894351328721621, -1.116326037436713881 ) ) ;
#199022=CARTESIAN_POINT ( 'NONE',  ( 6.356982874815331641, 0.3076174260261410054, -1.815216213958574132 ) ) ;
#199025=CARTESIAN_POINT ( 'NONE',  ( 3.756244407761480275, 0.6229016427463770489, 1.608663766957881824 ) ) ;
#199027=CARTESIAN_POINT ( 'NONE',  ( 6.586557750117827403, -2.163372447211810989, -0.4352210726449382006 ) ) ;
#199030=CARTESIAN_POINT ( 'NONE',  ( 5.137628997053973912, 2.028260002996465250, -0.7749071676581267276 ) ) ;
#199031=CARTESIAN_POINT ( 'NONE',  ( 3.404746562951189937, 1.438594061741470753, -1.123979961188771304 ) ) ;
#199032=CARTESIAN_POINT ( 'NONE',  ( 1.112071775475082402, 1.959765382314464732, -0.09068415226199526280 ) ) ;
#199033=CARTESIAN_POINT ( 'NONE',  ( 5.647700563513772920, 2.085583167219496215, -0.3645771090082204902 ) ) ;
#199035=CARTESIAN_POINT ( 'NONE',  ( 5.952705545545641463, -1.964087939335951827, -1.181845259310390306 ) ) ;
#199038=CARTESIAN_POINT ( 'NONE',  ( 1.453939175038564624, -1.538220317728825393, -1.459821603020584613 ) ) ;
#199044=CARTESIAN_POINT ( 'NONE',  ( 6.895391736652770831, -1.943277935985653349, 0.9682779983983346161 ) ) ;
#199045=CARTESIAN_POINT ( 'NONE',  ( 6.883263157960365142, -0.007059606330772279746, 2.153658854459541416 ) ) ;
#199048=CARTESIAN_POINT ( 'NONE',  ( 2.315342353584739055, 1.782219222887641674, -1.325647956807120220 ) ) ;
#199050=CARTESIAN_POINT ( 'NONE',  ( -0.08672817704761734414, -1.422268874607252043, -1.807091132531572608 ) ) ;
#199052=CARTESIAN_POINT ( 'NONE',  ( 4.961816841544592904, -0.5550570666568316325, 1.986392505239948036 ) ) ;
#199058=CARTESIAN_POINT ( 'NONE',  ( 0.1465796939425691170, -1.677718324701961361, 1.247191284554289625 ) ) ;
#199059=CARTESIAN_POINT ( 'NONE',  ( 4.236954046275762664, 2.015912997090345549, -0.05229627655192746472 ) ) ;
#199060=CARTESIAN_POINT ( 'NONE',  ( 3.983814121021773680, -1.821778379405362136, -0.2661574599523569007 ) ) ;
#199062=CARTESIAN_POINT ( 'NONE',  ( 2.045521581634631048, 0.6637456736250256784, -1.592148833096140192 ) ) ;
#199063=CARTESIAN_POINT ( 'NONE',  ( 0.6203277878081385754, 1.987498645412737908, 0.3399528957561820386 ) ) ;
#199064=CARTESIAN_POINT ( 'NONE',  ( 2.321245813631057864, 1.080353426350823209, -2.028982405110477227 ) ) ;
#199066=CARTESIAN_POINT ( 'NONE',  ( 1.529016648559086811, 2.180303969971490563, 0.6036265194416541302 ) ) ;
#199067=CARTESIAN_POINT ( 'NONE',  ( 3.721394855333003626, -0.1548319924524182156, 2.100431540652194062 ) ) ;
#199071=CARTESIAN_POINT ( 'NONE',  ( 6.718719045489192965, -0.7860540964614262105, 1.895863743164223347 ) ) ;
#199076=CARTESIAN_POINT ( 'NONE',  ( 5.185853984360066171, 2.140751028750527141, -0.5928278168529849124 ) ) ;
#199077=CARTESIAN_POINT ( 'NONE',  ( 3.504031732436951874, -0.8880451304637152488, -2.003635182500095535 ) ) ;
#199081=CARTESIAN_POINT ( 'NONE',  ( 6.890000000000010338, 2.965158640989657979, 2.452917560796507246 ) ) ;
#199083=CARTESIAN_POINT ( 'NONE',  ( 5.238584497427841491, 1.261362679698872169, -1.704546977916908457 ) ) ;
#199089=CARTESIAN_POINT ( 'NONE',  ( 5.882333747326812912, -0.2767177626767612919, -1.820229446528654371 ) ) ;
#199092=CARTESIAN_POINT ( 'NONE',  ( 0.9249085282522085949, -1.102964995092512890, -1.346285399390812598 ) ) ;
#199097=CARTESIAN_POINT ( 'NONE',  ( 5.471600609837615536, 2.084441204114939161, -0.5725544205837928002 ) ) ;
#199101=CARTESIAN_POINT ( 'NONE',  ( 5.172814640947125397, -2.034155943344346795, -0.7319064324283753864 ) ) ;
#199102=ORIENTED_EDGE ( 'NONE', *, *, #71220, .T. ) ;
#199104=CARTESIAN_POINT ( 'NONE',  ( 6.380149230842863339, -1.056690401097816867, 1.664064485322758635 ) ) ;
#199105=CARTESIAN_POINT ( 'NONE',  ( 4.798016402085652388, -1.585019518093808699, 0.7031974489903334291 ) ) ;
#199107=CARTESIAN_POINT ( 'NONE',  ( 1.786939262935317130, 1.904797134731281538, -1.083727916527020607 ) ) ;
#199108=CARTESIAN_POINT ( 'NONE',  ( 2.591229953566904776, -0.3941274307956154077, -2.273529888306951019 ) ) ;
#199109=CARTESIAN_POINT ( 'NONE',  ( 4.675106833541732954, 0.004019643978107888781, -2.060967561157340810 ) ) ;
#199110=CARTESIAN_POINT ( 'NONE',  ( 0.5505969416323712728, -1.640064848914600804, -1.039604180477508688 ) ) ;
#199115=CARTESIAN_POINT ( 'NONE',  ( 3.428091063814618700, -2.088597262255381448, 0.3661859999234198249 ) ) ;
#199117=CARTESIAN_POINT ( 'NONE',  ( 1.529922885524274134, -1.701946718671920600, 1.081067414773040802 ) ) ;
#199119=CARTESIAN_POINT ( 'NONE',  ( 4.647634198631804381, -1.703412986257560879, -1.402924735643434673 ) ) ;
#199121=CARTESIAN_POINT ( 'NONE',  ( 1.885388715806934679, -1.754394424870173719, 0.6211283009984622794 ) ) ;
#199126=CARTESIAN_POINT ( 'NONE',  ( 6.925078400183549476, 6.033022220673083247, 2.839235739982972184 ) ) ;
#199129=CARTESIAN_POINT ( 'NONE',  ( 3.291920626085430346, -0.8366078139741841557, 1.883634853023412825 ) ) ;
#199132=CARTESIAN_POINT ( 'NONE',  ( 3.598311091834342612, -0.9934155151001385908, 1.758370388466141465 ) ) ;
#199135=CARTESIAN_POINT ( 'NONE',  ( 1.868112839806375325, 1.058416689118582665, 1.768180007894581740 ) ) ;
#199139=( BOUNDED_SURFACE ( )  B_SPLINE_SURFACE ( 3, 3, ( 
 ( #209019, #58532, #46561, #112681, #190645, #193850, #109491, #176552, #175498, #207966, #10826 ),
 ( #127899, #111616, #27086, #108420, #192775, #95328, #76900, #59592, #158182, #161377, #45500 ),
 ( #143024, #144097, #110550, #60655, #28162, #94258, #160297, #11900, #210092, #61731, #42305 ),
 ( #9774, #12961, #177628, #29236, #75847, #79038, #141954, #26018, #145153, #211159, #62783 ),
 ( #128946, #30305, #96390, #63858, #149375, #118007, #32430, #165626, #131064, #115867, #200234 ),
 ( #50806, #16145, #82230, #180804, #17214, #67024, #214320, #146207, #213289, #98496, #47640 ),
 ( #167757, #35610, #101688, #64915, #134224, #34549, #148321, #182933, #48690, #197052, #958 ) ),
 .UNSPECIFIED., .T., .F., .T. ) 
 B_SPLINE_SURFACE_WITH_KNOTS ( ( 4, 3, 4 ),
 ( 4, 1, 1, 1, 1, 1, 1, 1, 4 ),
 ( 0.000000000000000000, 0.5000000000000000000, 1.000000000000000000 ),
 ( 0.000000000000000000, 0.2256777920876190668, 0.3978457394851813711, 0.5256768607792676740, 0.6183602023682204241, 0.6850295134299612121, 0.7345374503969632762, 0.7752450576501028756, 1.000000000000000000 ),
 .UNSPECIFIED. ) 
 GEOMETRIC_REPRESENTATION_ITEM ( )  RATIONAL_B_SPLINE_SURFACE ( (
 ( 1.000000000000000000, 1.000000000000000000, 1.000000000000000000, 1.000000000000000222, 0.9999999999999997780, 1.000000000000000444, 0.9999999999999997780, 1.000000000000000222, 0.9999999999999996669, 1.000000000000000222, 1.000000000000000222),
 ( 0.3333333333333333703, 0.3333333333333334259, 0.3333333333333333703, 0.3333333333333334259, 0.3333333333333333703, 0.3333333333333334259, 0.3333333333333333703, 0.3333333333333334259, 0.3333333333333333148, 0.3333333333333334259, 0.3333333333333334259),
 ( 0.3333333333333333703, 0.3333333333333334259, 0.3333333333333333703, 0.3333333333333334259, 0.3333333333333333703, 0.3333333333333334259, 0.3333333333333333703, 0.3333333333333334259, 0.3333333333333333148, 0.3333333333333334259, 0.3333333333333334259),
 ( 1.000000000000000000, 1.000000000000000000, 1.000000000000000000, 1.000000000000000222, 0.9999999999999997780, 1.000000000000000444, 0.9999999999999997780, 1.000000000000000222, 0.9999999999999996669, 1.000000000000000222, 1.000000000000000222),
 ( 0.3333333333333333703, 0.3333333333333334259, 0.3333333333333333703, 0.3333333333333334259, 0.3333333333333333703, 0.3333333333333334259, 0.3333333333333333703, 0.3333333333333334259, 0.3333333333333333148, 0.3333333333333334259, 0.3333333333333334259),
 ( 0.3333333333333333703, 0.3333333333333334259, 0.3333333333333333703, 0.3333333333333334259, 0.3333333333333333703, 0.3333333333333334259, 0.3333333333333333703, 0.3333333333333334259, 0.3333333333333333148, 0.3333333333333334259, 0.3333333333333334259),
 ( 1.000000000000000000, 1.000000000000000000, 1.000000000000000000, 1.000000000000000222, 0.9999999999999997780, 1.000000000000000444, 0.9999999999999997780, 1.000000000000000222, 0.9999999999999996669, 1.000000000000000222, 1.000000000000000222) ) ) 
 REPRESENTATION_ITEM ( '' )  SURFACE ( )  );
#199140=CARTESIAN_POINT ( 'NONE',  ( -0.2408018239684096284, -0.007136184528808932684, -2.100252307185761058 ) ) ;
#199141=CARTESIAN_POINT ( 'NONE',  ( 1.235996726672627943, 0.3573974351761283752, 1.805938768738392319 ) ) ;
#199142=CARTESIAN_POINT ( 'NONE',  ( 5.637410271038987730, -1.996576301129053377, 0.9405272304151901519 ) ) ;
#199144=CARTESIAN_POINT ( 'NONE',  ( 1.933122032479916985, 0.2097677157741582865, 2.151362962771664833 ) ) ;
#199146=CARTESIAN_POINT ( 'NONE',  ( 2.114470590943520634, 1.957170936680457052, 0.4852650170619755565 ) ) ;
#199152=CARTESIAN_POINT ( 'NONE',  ( 4.082859939823464401, -0.1922352567787863620, -1.962060651276048118 ) ) ;
#199153=CARTESIAN_POINT ( 'NONE',  ( 3.239470508323912146, 0.4852670486454255250, -1.957170429962351577 ) ) ;
#199157=CARTESIAN_POINT ( 'NONE',  ( 6.252575686221216955, 0.6590897193336446858, 2.000345064990595390 ) ) ;
#199158=CARTESIAN_POINT ( 'NONE',  ( 5.775854211382815073, -2.020734006234246927, 0.4499205674863211990 ) ) ;
#199162=CARTESIAN_POINT ( 'NONE',  ( 4.728773938389556619, 1.389870793851749164, -1.465793203850384030 ) ) ;
#199164=CARTESIAN_POINT ( 'NONE',  ( 0.5497677191402570163, 1.525909772416549126, 1.387868932477815065 ) ) ;
#199172=CARTESIAN_POINT ( 'NONE',  ( 2.822911419172136949, -1.498817844263359067, 1.571052884911597003 ) ) ;
#199176=CARTESIAN_POINT ( 'NONE',  ( 2.559893532628489954, -1.268187297466142338, 1.335118840784771166 ) ) ;
#199178=CARTESIAN_POINT ( 'NONE',  ( 4.212563348414651188, 2.004022095860341413, 0.8874167208733558798 ) ) ;
#199180=CARTESIAN_POINT ( 'NONE',  ( 4.294006694993548479, -0.8693707907260415091, 2.089011835857216948 ) ) ;
#199185=CARTESIAN_POINT ( 'NONE',  ( 6.784453145350711090, -1.736176628054094007, -0.3419908188336401311 ) ) ;
#199186=CARTESIAN_POINT ( 'NONE',  ( 3.809243135778153100, 1.699416117590052622, -1.078869421455890709 ) ) ;
#199188=CARTESIAN_POINT ( 'NONE',  ( 2.573382939595921570, 0.1044104795966259297, -2.103504788083962573 ) ) ;
#199189=CARTESIAN_POINT ( 'NONE',  ( 1.265090914671564759, 1.769361140067410521, -0.7345930670351871195 ) ) ;
#199192=CARTESIAN_POINT ( 'NONE',  ( 1.557020932125362078, 1.611981373198448253, -1.131376696270647075 ) ) ;
#199194=CARTESIAN_POINT ( 'NONE',  ( 0.3209005354254980680, -0.09642172165634513292, 1.868300368337752815 ) ) ;
#199195=CARTESIAN_POINT ( 'NONE',  ( 0.8538673084422104820, -0.7095216264049221122, 1.829241926910141203 ) ) ;
#199196=CARTESIAN_POINT ( 'NONE',  ( -0.1757481403069499348, -0.8193859263425256056, -1.726394157293544840 ) ) ;
#199202=CARTESIAN_POINT ( 'NONE',  ( 5.612129163471575310, -0.8422657237196762292, -1.670366365510121742 ) ) ;
#199205=CARTESIAN_POINT ( 'NONE',  ( 6.789897376884641567, -1.347643488625469121, -1.571692526165118009 ) ) ;
#199217=CARTESIAN_POINT ( 'NONE',  ( 5.951606347324345236, 1.484592722905058393, 1.282605414028796353 ) ) ;
#199219=CARTESIAN_POINT ( 'NONE',  ( 3.567732365556259388, 1.591074578583807853, -1.238131541301431326 ) ) ;
#199220=CARTESIAN_POINT ( 'NONE',  ( 4.065584057473277113, 1.255829935711678669, 1.446728075138058678 ) ) ;
#199222=CARTESIAN_POINT ( 'NONE',  ( 1.382659466718983543, -0.3261178763579902773, -2.167053615394160637 ) ) ;
#199224=CARTESIAN_POINT ( 'NONE',  ( 2.969827553264007047, 0.9974664638083343693, 1.582205488144486250 ) ) ;
#199228=CARTESIAN_POINT ( 'NONE',  ( 4.323895160615763622, 0.9038210025188663232, -1.914733396627795958 ) ) ;
#199230=CARTESIAN_POINT ( 'NONE',  ( 5.846161131210033446, -0.9342735719010831774, 1.847668428805064655 ) ) ;
#199231=CARTESIAN_POINT ( 'NONE',  ( 2.349268366499413840, 0.5549471352096692067, -2.015694315139557435 ) ) ;
#199232=CARTESIAN_POINT ( 'NONE',  ( 6.620655732516611103, 6.033324165176342291, 2.868629481857593255 ) ) ;
#199233=CARTESIAN_POINT ( 'NONE',  ( 0.3227381541650706787, -0.09231566880639123507, 1.722440863776145692 ) ) ;
#199243=CARTESIAN_POINT ( 'NONE',  ( 0.2580964568148482741, 1.806467626183925423, 0.1351022710447576103 ) ) ;
#199254=CARTESIAN_POINT ( 'NONE',  ( 3.314761293198214887, -1.410806105172614178, 1.213857476866337937 ) ) ;
#199255=CARTESIAN_POINT ( 'NONE',  ( 0.4564612863584472380, -1.804040949374663194, -0.6446129174930875783 ) ) ;
#199256=CARTESIAN_POINT ( 'NONE',  ( 0.6629299983115041206, 0.6194173074674096391, 2.027988828570789437 ) ) ;
#199259=CARTESIAN_POINT ( 'NONE',  ( -0.1399997263889559695, 7.629137130509076492, -2.600276787041354343 ) ) ;
#199263=CARTESIAN_POINT ( 'NONE',  ( 4.416829296269289884, -1.462161721869711384, 1.319618631580289581 ) ) ;
#199265=CARTESIAN_POINT ( 'NONE',  ( 1.629697543846151619, -0.2563088357964183883, 2.104862515383609800 ) ) ;
#199270=CARTESIAN_POINT ( 'NONE',  ( 5.455090197064776270, 0.4301712223657681022, -2.148646160378755443 ) ) ;
#199272=CARTESIAN_POINT ( 'NONE',  ( 4.454074118230034962, 1.925978650549282856, -0.04673309505795821689 ) ) ;
#199275=CARTESIAN_POINT ( 'NONE',  ( 0.6393319655835436599, -1.287349573739982933, -1.294668131371433661 ) ) ;
#199276=CARTESIAN_POINT ( 'NONE',  ( 1.049787907720298286, -1.741764784136769162, -1.355102641770723704 ) ) ;
#199280=ORIENTED_EDGE ( 'NONE', *, *, #185415, .T. ) ;
#199281=CARTESIAN_POINT ( 'NONE',  ( 6.069198383140281372, 1.735254367832469891, 0.9315073086425088578 ) ) ;
#199282=CARTESIAN_POINT ( 'NONE',  ( 1.821723684117615427, 1.116499850783551073, -1.588862189236692091 ) ) ;
#199283=CARTESIAN_POINT ( 'NONE',  ( 6.661448219487969169, -0.6026422599177021500, -2.217949877449727047 ) ) ;
#199285=CARTESIAN_POINT ( 'NONE',  ( 4.399146427517338864, -1.620787001191201560, 0.9142094169404291204 ) ) ;
#199289=CARTESIAN_POINT ( 'NONE',  ( 6.720655732516658709, 4.700665033810172311, 2.388972926809574737 ) ) ;
#199290=CARTESIAN_POINT ( 'NONE',  ( -0.09381621004311831158, -0.9424329983100244723, -1.976553698157037076 ) ) ;
#199294=CARTESIAN_POINT ( 'NONE',  ( 1.435882461153328515, 0.9014729512111450127, -1.587519582607027635 ) ) ;
#199296=CARTESIAN_POINT ( 'NONE',  ( 3.181945575597402431, 1.368952998951804556, 1.064414454346799266 ) ) ;
#199300=CARTESIAN_POINT ( 'NONE',  ( 0.1703666795057276195, -1.259402025324443564, 1.457936571737717735 ) ) ;
#199301=CARTESIAN_POINT ( 'NONE',  ( 4.856279117655732058, -1.961245242753749674, -0.05215834203427943683 ) ) ;
#199304=CARTESIAN_POINT ( 'NONE',  ( 4.459710115430675081, -1.639780234044617035, -1.344486126324248465 ) ) ;
#199308=CARTESIAN_POINT ( 'NONE',  ( 2.694261129275489886, 0.9798316074655871732, -1.823736424811234658 ) ) ;
#199312=CARTESIAN_POINT ( 'NONE',  ( 2.708015267422092531, 2.165615165066101966, 0.7711511238016451886 ) ) ;
#199320=CARTESIAN_POINT ( 'NONE',  ( 3.744317949583543470, 1.018843395500759197, -1.618198357137661469 ) ) ;
#199322=CARTESIAN_POINT ( 'NONE',  ( 5.666962058884261744, -1.561145826413099291, -0.7335915956277230254 ) ) ;
#199323=CARTESIAN_POINT ( 'NONE',  ( 3.116422982138194353, 1.968445132739887748, 0.4370783100892047801 ) ) ;
#199325=CARTESIAN_POINT ( 'NONE',  ( 5.151170688231202277, 1.131463054214848940, 2.000911673594136797 ) ) ;
#199327=CARTESIAN_POINT ( 'NONE',  ( 0.4873205249028254027, -0.2742316277877173691, -2.189713876267186166 ) ) ;
#199329=CARTESIAN_POINT ( 'NONE',  ( 5.659369745216535463, 0.3440881560464129629, -1.735765479537496603 ) ) ;
#199332=CARTESIAN_POINT ( 'NONE',  ( 1.623385997035782013, -2.157220310706788435, 0.7755101668525423708 ) ) ;
#199333=CARTESIAN_POINT ( 'NONE',  ( 6.667912628260062036, -1.128459271250933149, 1.455361883854713767 ) ) ;
#199335=CARTESIAN_POINT ( 'NONE',  ( 6.667925998804712151, -1.351855065013835455, 1.725503752137508284 ) ) ;
#199339=CARTESIAN_POINT ( 'NONE',  ( 6.461392557816405535, 1.719054114842766268, 1.153505076091146053 ) ) ;
#199340=CARTESIAN_POINT ( 'NONE',  ( 0.8136858238772455287, -1.282993010278702606, -1.555696519147983459 ) ) ;
#199342=CARTESIAN_POINT ( 'NONE',  ( 5.777940811437299651, 1.149350900142607879, 1.545952477797669200 ) ) ;
#199344=CARTESIAN_POINT ( 'NONE',  ( 1.846216761830053787, -1.455271069044868693, -1.678405531801461903 ) ) ;
#199351=DIRECTION ( 'NONE',  ( -0.9999980456341538426, 0.000000000000000000, -0.001977050295967298574 ) ) ;
#199352=CARTESIAN_POINT ( 'NONE',  ( 4.071615416877820692, -0.9979366678331093032, 1.425717084491331832 ) ) ;
#199353=CARTESIAN_POINT ( 'NONE',  ( 2.277722772326017608, -1.903703133612335341, 0.4737097981617058862 ) ) ;
#199359=CARTESIAN_POINT ( 'NONE',  ( 0.6079712386793578727, 0.6485803912554971573, -1.958102696269433673 ) ) ;
#199363=CARTESIAN_POINT ( 'NONE',  ( 1.182923723612337774, -2.207873014618145113, -0.4935663919954368373 ) ) ;
#199366=CARTESIAN_POINT ( 'NONE',  ( 2.266681450017640653, -1.708379500633325998, -0.7622673669660309237 ) ) ;
#199367=CARTESIAN_POINT ( 'NONE',  ( 1.388881788488422586, -0.6239178774879328149, -1.618199924151533686 ) ) ;
#199368=CARTESIAN_POINT ( 'NONE',  ( 5.407841436338867602, -0.9846607899807978681, -1.957994596084790206 ) ) ;
#199369=CARTESIAN_POINT ( 'NONE',  ( 5.790114358714919973, -1.044397830967594976, 2.057800239056095659 ) ) ;
#199370=CARTESIAN_POINT ( 'NONE',  ( 1.586866656640874451, -0.3012919939810917436, -2.038609575755165437 ) ) ;
#199371=CARTESIAN_POINT ( 'NONE',  ( 3.943253339372253308, 0.6530871051511869529, -1.828966769512891277 ) ) ;
#199373=CARTESIAN_POINT ( 'NONE',  ( 5.729731410239141454, -1.186140735684092284, -1.446405967604667886 ) ) ;
#199374=CARTESIAN_POINT ( 'NONE',  ( 1.875000000000001776, 2.052068128417950721, -1.077215146005767577E-13 ) ) ;
#199376=CARTESIAN_POINT ( 'NONE',  ( 6.608749954595573683, 0.7741944705832277673, -1.861732896133998727 ) ) ;
#199378=CARTESIAN_POINT ( 'NONE',  ( 4.324842380567116784, 0.8596320953860696612, -1.824118450417112847 ) ) ;
#199382=CARTESIAN_POINT ( 'NONE',  ( 2.490611698265518648, -0.3118145247060916114, -1.798701865878708839 ) ) ;
#199385=CARTESIAN_POINT ( 'NONE',  ( -0.1296875068448159751, 0.001480089298542403009, -1.826395826379861864 ) ) ;
#199391=CARTESIAN_POINT ( 'NONE',  ( 6.393224328948585722, -0.1011241736039915490, -2.017280362314947340 ) ) ;
#199392=CARTESIAN_POINT ( 'NONE',  ( 0.4344390223590781641, -1.137927343861804053, -1.789123301873453364 ) ) ;
#199396=CARTESIAN_POINT ( 'NONE',  ( 5.682513945847499137, -2.010110750271485447, -0.4539000206328601683 ) ) ;
#199397=CARTESIAN_POINT ( 'NONE',  ( 4.922500090287251773, -1.427935867408920645, -1.423962988533589158 ) ) ;
#199407=CARTESIAN_POINT ( 'NONE',  ( 5.114611164699836010, 0.6351010243071940620, -1.913510948406547563 ) ) ;
#199408=CARTESIAN_POINT ( 'NONE',  ( 5.103375755629981469, -1.831930319445294719, 0.1838923505294575433 ) ) ;
#199409=CARTESIAN_POINT ( 'NONE',  ( -0.02338929933911031503, 1.420967854922173368, -1.971839201816010911 ) ) ;
#199410=CARTESIAN_POINT ( 'NONE',  ( 2.860362167425280600, 2.296499369387979606, -0.2270692390979132391 ) ) ;
#199412=CARTESIAN_POINT ( 'NONE',  ( 5.167319818800252484, 0.2175342549677051207, -2.150644138106901693 ) ) ;
#199414=CARTESIAN_POINT ( 'NONE',  ( 0.3627036604622800864, 0.1893831815216796277, -1.932784825206189661 ) ) ;
#199421=CARTESIAN_POINT ( 'NONE',  ( 3.836663719693265584, 0.2738035037005565053, 1.850374562403465983 ) ) ;
#199422=CARTESIAN_POINT ( 'NONE',  ( 1.599720133015330337, 1.321132142916726204, 1.382909031182079307 ) ) ;
#199425=CARTESIAN_POINT ( 'NONE',  ( 2.473496279428960776, 0.1070396533628548558, -2.204406164007084445 ) ) ;
#199432=CARTESIAN_POINT ( 'NONE',  ( 0.2804619692761011751, -1.911105013696552168, -0.4832259537779006742 ) ) ;
#199433=CARTESIAN_POINT ( 'NONE',  ( 6.727182134110239353, -0.007837387828812587484, 2.289081727344749684 ) ) ;
#199434=CARTESIAN_POINT ( 'NONE',  ( 1.293326634533353170, -1.775083115552608559, 0.8357255594537355003 ) ) ;
#199435=CARTESIAN_POINT ( 'NONE',  ( 4.346570391463054683, -2.039393746373055372, -0.3077390332135512829 ) ) ;
#199443=CARTESIAN_POINT ( 'NONE',  ( 6.637192348400761333, -0.09982221633967082453, -2.168999452382541993 ) ) ;
#199445=CARTESIAN_POINT ( 'NONE',  ( 6.462460624273299814, -1.686435539877573220, -0.7394478613861471539 ) ) ;
#199448=CARTESIAN_POINT ( 'NONE',  ( 0.9834252619641962179, 1.251819791611600285, 1.390119989509101650 ) ) ;
#199450=CARTESIAN_POINT ( 'NONE',  ( -0.02244404828157658613, -0.004869073801674199918, -2.189079685368473527 ) ) ;
#199453=CARTESIAN_POINT ( 'NONE',  ( 1.031728963041964153, -1.865498905729731316, 0.4196304693004496156 ) ) ;
#199454=CARTESIAN_POINT ( 'NONE',  ( 3.414700241993049001, 1.599697164860384380, 0.7574896018788888075 ) ) ;
#199455=CARTESIAN_POINT ( 'NONE',  ( 0.8383554657987003500, 1.138622818284718008, -1.536203910471350298 ) ) ;
#199457=CARTESIAN_POINT ( 'NONE',  ( 3.866719127221716512, -0.1911932653220274059, -1.906053554140298756 ) ) ;
#199459=CARTESIAN_POINT ( 'NONE',  ( 5.600048008112708864, 0.7998006467024108002, -1.800045223161725660 ) ) ;
#199460=CARTESIAN_POINT ( 'NONE',  ( 1.178162429063234207, 2.088287186665960693, -0.3679680078583212333 ) ) ;
#199461=CARTESIAN_POINT ( 'NONE',  ( 6.720655732516625847, 7.629137130509076492, 2.426260288887295058 ) ) ;
#199462=CARTESIAN_POINT ( 'NONE',  ( 3.414787578387419309, 1.690673485743508619, 0.8009127983473337542 ) ) ;
#199463=CARTESIAN_POINT ( 'NONE',  ( 0.8908993799596062191, 1.611356928563783208, -0.8583080905386344384 ) ) ;
#199465=CARTESIAN_POINT ( 'NONE',  ( 3.422699507934781060, 1.400174360247144589, -1.705827624971032686 ) ) ;
#199468=CARTESIAN_POINT ( 'NONE',  ( 0.4673242579315056155, 1.793762616230053508, 1.018268840648499207 ) ) ;
#199475=CARTESIAN_POINT ( 'NONE',  ( 4.721179655770254335, -1.847879960204744432, -0.9338546512941485744 ) ) ;
#199477=CARTESIAN_POINT ( 'NONE',  ( 1.827627302340195437, -2.036028831988645926, 0.7264203155534704193 ) ) ;
#199479=CARTESIAN_POINT ( 'NONE',  ( 2.244791279253912197, 1.959548689066059168, 0.4886446307589187854 ) ) ;
#199481=EDGE_CURVE ( 'NONE', #124676, #30003, #103396, .T. ) ;
#199485=CARTESIAN_POINT ( 'NONE',  ( 0.3039231887648624619, -1.082844287645868375, -1.700959134490941160 ) ) ;
#199487=CARTESIAN_POINT ( 'NONE',  ( 5.003566749295822014, -2.181051155298455058, 0.2145382695054529609 ) ) ;
#199490=CARTESIAN_POINT ( 'NONE',  ( 3.638835171272115421, 1.817485770107383436, 0.5952672491930725007 ) ) ;
#199494=CARTESIAN_POINT ( 'NONE',  ( 1.616814774554303780, 0.2004563524992293566, 2.006445175307514095 ) ) ;
#199496=CARTESIAN_POINT ( 'NONE',  ( 0.1524363970008953684, 0.8851206712186098224, 2.114804356544320640 ) ) ;
#199498=CARTESIAN_POINT ( 'NONE',  ( 4.629763539376270387, -1.062658783613348534, -1.358442396976522248 ) ) ;
#199499=CARTESIAN_POINT ( 'NONE',  ( -0.1405533004718495238, 2.888985375434447889, -2.209311699518405447 ) ) ;
#199502=CARTESIAN_POINT ( 'NONE',  ( 0.9066075625437097774, 0.5660373911110065936, 1.878450800843839419 ) ) ;
#199506=CARTESIAN_POINT ( 'NONE',  ( 0.07536363704233051131, 7.629137130509080045, -2.744199452819145790 ) ) ;
#199510=CARTESIAN_POINT ( 'NONE',  ( 3.562975276761202181, -1.478990456472810910, 1.045639718295880094 ) ) ;
#199514=CARTESIAN_POINT ( 'NONE',  ( 4.371601898205011771, 0.3924986647133471007, -1.768265068870542800 ) ) ;
#199520=CARTESIAN_POINT ( 'NONE',  ( 6.109776933011930922, 0.5395433811187456685, -1.781096067677762962 ) ) ;
#199522=CARTESIAN_POINT ( 'NONE',  ( 4.147977739690055898, 0.9062469702798245930, 1.687694244345463224 ) ) ;
#199530=CARTESIAN_POINT ( 'NONE',  ( 0.7784641540938312954, -1.199969256800371697, 1.797863220954009744 ) ) ;
#199533=CARTESIAN_POINT ( 'NONE',  ( 0.4986989427119004059, 1.520756344202650601, -1.009667857431728599 ) ) ;
#199536=CARTESIAN_POINT ( 'NONE',  ( 3.188313505853744179, -1.798300186086329688, -0.3134973320952222364 ) ) ;
#199538=CARTESIAN_POINT ( 'NONE',  ( 1.705181254219298115, 1.662258477346746588, -0.9455041445245655485 ) ) ;
#199540=CARTESIAN_POINT ( 'NONE',  ( 2.277737068081890914, -1.911112558508936354, 0.4757300241334978530 ) ) ;
#199541=CARTESIAN_POINT ( 'NONE',  ( 5.319850173407331795, 1.153525655430783337, -1.562239502177962480 ) ) ;
#199544=CARTESIAN_POINT ( 'NONE',  ( 4.008146050417991546, -0.8085630067716749192, 1.960596031080278356 ) ) ;
#199553=CARTESIAN_POINT ( 'NONE',  ( 5.162654993523497993, -1.319871331358621669, 1.261628347558927166 ) ) ;
#199559=CARTESIAN_POINT ( 'NONE',  ( 5.682452175617663137, -1.825344843996518529, -0.4084625512627630406 ) ) ;
#199568=CARTESIAN_POINT ( 'NONE',  ( 6.438351068470751670, -1.168633322568404243, 1.829565972870864865 ) ) ;
#199569=CARTESIAN_POINT ( 'NONE',  ( 0.6853559850922884555, 1.733544695350475395, 1.215283626663875793 ) ) ;
#199572=CARTESIAN_POINT ( 'NONE',  ( 6.174686067066745387, 1.394736081427111030, -1.530067588329916850 ) ) ;
#199573=CARTESIAN_POINT ( 'NONE',  ( 1.997363575765517485, -1.840834563946552649, 0.04656924640939614363 ) ) ;
#199578=CARTESIAN_POINT ( 'NONE',  ( 1.500361222516993331, -0.8285058210528316591, -2.137470567302256708 ) ) ;
#199584=CARTESIAN_POINT ( 'NONE',  ( 0.9143154035033382865, -2.013376230895477903, 0.004183558276700528357 ) ) ;
#199585=CARTESIAN_POINT ( 'NONE',  ( 1.498799732657706718, 0.3773721054241683248, 1.924948185394937283 ) ) ;
#199586=CARTESIAN_POINT ( 'NONE',  ( 6.509000000000010999, 0.004788705324892603143, 2.000274819378269786 ) ) ;
#199590=CARTESIAN_POINT ( 'NONE',  ( 3.855486427358902013, 2.074851370404519280, -0.2558628111340756628 ) ) ;
#199591=CARTESIAN_POINT ( 'NONE',  ( 1.902845806929494232, 1.469307612142495723, 0.9863148084752764166 ) ) ;
#199594=CARTESIAN_POINT ( 'NONE',  ( 5.050848094970262991, -1.934468200101526758, -1.229489151810001735 ) ) ;
#199595=CARTESIAN_POINT ( 'NONE',  ( 3.626658729539467441, -1.607292185769314097, 0.6678421186538037180 ) ) ;
#199598=CARTESIAN_POINT ( 'NONE',  ( 3.831122626782780927, -1.165689738437695189, 1.283648893705439331 ) ) ;
#199599=CARTESIAN_POINT ( 'NONE',  ( 3.192005314569335894, -1.456082124923337995, -1.610717807342199048 ) ) ;
#199602=CARTESIAN_POINT ( 'NONE',  ( 4.909388789075159742, -1.913262893431907141, 0.6371506334161003426 ) ) ;
#199603=CARTESIAN_POINT ( 'NONE',  ( 6.750000000000005329, 3.320568569168067974, 2.600000000000000533 ) ) ;
#199605=CARTESIAN_POINT ( 'NONE',  ( 2.379798427543390105, 1.183398162072072823, 1.519983715915488531 ) ) ;
#199607=CARTESIAN_POINT ( 'NONE',  ( 6.222901868277154414, 1.646860780578407013, -1.490944794436506626 ) ) ;
#199609=CARTESIAN_POINT ( 'NONE',  ( -0.2106854629475425067, 4.089057744811007922, -2.552070079120628776 ) ) ;
#199617=CARTESIAN_POINT ( 'NONE',  ( 6.749321564901560322, -1.811022791033944257, -1.355814775124731808 ) ) ;
#199620=CARTESIAN_POINT ( 'NONE',  ( 3.965324414628346172, 1.767556376804786611, 1.063002922270523953 ) ) ;
#199624=CARTESIAN_POINT ( 'NONE',  ( 5.378141472655761923, -1.040010688794581029, 1.554561134376866161 ) ) ;
#199625=CARTESIAN_POINT ( 'NONE',  ( 4.518016650454199201, -1.583040169018738785, 0.7084668738900431473 ) ) ;
#199626=CARTESIAN_POINT ( 'NONE',  ( 5.038483826543846078, -1.489082695810162837, 0.9007512145987550678 ) ) ;
#199628=CARTESIAN_POINT ( 'NONE',  ( 1.505871038028598230, -2.274393761632488964, 0.2862045095256612326 ) ) ;
#199630=CARTESIAN_POINT ( 'NONE',  ( 6.146049400653379458, 0.6566722887273982456, 1.984991666494940743 ) ) ;
#199631=CARTESIAN_POINT ( 'NONE',  ( 6.562452659285362699, -1.776534117310492711, -0.7846822752179910543 ) ) ;
#199634=CARTESIAN_POINT ( 'NONE',  ( 1.565077508395201988, -1.076315722900993643, 1.704939445326451475 ) ) ;
#199635=CARTESIAN_POINT ( 'NONE',  ( 0.4983068789779531715, -0.7420642642406435341, -2.062120472104383317 ) ) ;
#199639=CARTESIAN_POINT ( 'NONE',  ( 3.651137946248568689, 0.3127203024623700367, 2.097190470537732221 ) ) ;
#199641=CARTESIAN_POINT ( 'NONE',  ( 5.408770660633122063, 1.379882519126625295, -1.195542987486551301 ) ) ;
#199647=CARTESIAN_POINT ( 'NONE',  ( 2.883074275722704360, -1.867829236092366951, -0.7691044946091238899 ) ) ;
#199648=CARTESIAN_POINT ( 'NONE',  ( 6.422910180798067969, 2.056742032306459578, 0.8002587082300142152 ) ) ;
#199651=CARTESIAN_POINT ( 'NONE',  ( 4.434314628233038569, -1.074157013132440275, 1.519412852752539678 ) ) ;
#199660=CARTESIAN_POINT ( 'NONE',  ( 1.809482579268039126, -1.467825596939468902, 0.9224971444230285478 ) ) ;
#199661=CARTESIAN_POINT ( 'NONE',  ( 1.745671189342316687, 0.5440799701325367277, 1.653152385070497887 ) ) ;
#199662=CARTESIAN_POINT ( 'NONE',  ( 6.674459784896970227, -1.426286490538879903, 1.815071943837057500 ) ) ;
#199665=CARTESIAN_POINT ( 'NONE',  ( 1.177107960601676551, -0.04769765464058715876, -2.060389331245067179 ) ) ;
#199668=EDGE_CURVE ( 'NONE', #78277, #97632, #105717, .T. ) ;
#199669=CARTESIAN_POINT ( 'NONE',  ( 6.626320313634256109, 0.4032262605214493312, -2.262638539848499164 ) ) ;
#199672=CARTESIAN_POINT ( 'NONE',  ( 0.2859245228041712439, -0.9316758688886862538, 1.737439158343912382 ) ) ;
#199674=CARTESIAN_POINT ( 'NONE',  ( 4.324404969281474109, -0.8226261416362996570, -1.726585468271451651 ) ) ;
#199676=CARTESIAN_POINT ( 'NONE',  ( 6.094375512030342001, -2.195847865938059140, -0.2203403561373064590 ) ) ;
#199681=CARTESIAN_POINT ( 'NONE',  ( 0.2233145766990596859, 1.758413993963375610, 0.9933387185240820649 ) ) ;
#199682=ORIENTED_EDGE ( 'NONE', *, *, #151247, .F. ) ;
#199683=CARTESIAN_POINT ( 'NONE',  ( 2.942713080207468579, 2.290027058972336604, 0.2837140972290051466 ) ) ;
#199684=CARTESIAN_POINT ( 'NONE',  ( 5.160583804383015227, -0.6592509027269661814, -1.847929681152965520 ) ) ;
#199685=CARTESIAN_POINT ( 'NONE',  ( 0.7780835697005837881, -1.044612314895682292, -1.660310580060719188 ) ) ;
#199689=CARTESIAN_POINT ( 'NONE',  ( 0.2865162857260491469, -0.7196341243457348158, -1.991407047551809750 ) ) ;
#199692=CARTESIAN_POINT ( 'NONE',  ( 0.1109373197970727476, -1.806229982939497436, 0.3559056038356380181 ) ) ;
#199693=CARTESIAN_POINT ( 'NONE',  ( 3.889651762418313119, -2.008042162167834377, 0.8258804214429303903 ) ) ;
#199695=CARTESIAN_POINT ( 'NONE',  ( 1.758217466200185042, 0.8068918862002281145, -1.961288232260410380 ) ) ;
#199701=CARTESIAN_POINT ( 'NONE',  ( 1.915377802959626230, -0.2551614870064948803, 2.044872660591416480 ) ) ;
#199705=CARTESIAN_POINT ( 'NONE',  ( 0.07735805125223899070, 6.946777552644263665, -2.683974465663693021 ) ) ;
#199708=CARTESIAN_POINT ( 'NONE',  ( 4.107995242876061326, -0.7289348763114507079, 1.768098669557085278 ) ) ;
#199711=CARTESIAN_POINT ( 'NONE',  ( 1.898125948304218547, -0.7631055018291610370, 2.129926759817270199 ) ) ;
#199713=CARTESIAN_POINT ( 'NONE',  ( 1.511653934090980034, -0.6084181080006717535, 1.706514628581125681 ) ) ;
#199714=CARTESIAN_POINT ( 'NONE',  ( 1.217839795352684273, 0.9409426854420616104, -1.668592810110066438 ) ) ;
#199715=CARTESIAN_POINT ( 'NONE',  ( 1.750525128138082254, -2.060206210462053988, -0.2049951091474821463 ) ) ;
#199718=CARTESIAN_POINT ( 'NONE',  ( 0.1453086613420169204, -1.522338971917249317, -1.252298935284136938 ) ) ;
#199719=CARTESIAN_POINT ( 'NONE',  ( 4.969325399568108814, 0.1871947810346066554, -1.917384544105669386 ) ) ;
#199720=CARTESIAN_POINT ( 'NONE',  ( 0.3820104410975051490, 2.150944695799131612, -0.8364647861166041309 ) ) ;
#199723=CARTESIAN_POINT ( 'NONE',  ( 4.773915743512389120, -2.023523412367009833, 0.3991901646795847913 ) ) ;
#199728=CARTESIAN_POINT ( 'NONE',  ( 5.245193717270952405, -1.807841653007141947, 1.079916013355223248 ) ) ;
#199730=CARTESIAN_POINT ( 'NONE',  ( 0.9772844579341716242, 2.006041157791297991, 0.8309993691856133458 ) ) ;
#199732=CARTESIAN_POINT ( 'NONE',  ( 5.026735257907362531, 2.066873009482797841, 0.6328083787210944111 ) ) ;
#199733=CARTESIAN_POINT ( 'NONE',  ( 5.180334445267184229, 0.9972254788270168424, 1.756242667785257172 ) ) ;
#199734=CARTESIAN_POINT ( 'NONE',  ( -0.02900071798684483726, 7.629137130509101361, -2.773797386654376584 ) ) ;
#199741=CARTESIAN_POINT ( 'NONE',  ( 3.327361509216096191, -1.530157842762596143, -1.313544516083162028 ) ) ;
#199745=CARTESIAN_POINT ( 'NONE',  ( 5.225516498768126183, -2.053876642077703707, 0.6744380372525200507 ) ) ;
#199751=CARTESIAN_POINT ( 'NONE',  ( 5.009388752257521560, -1.913799287717246500, 0.6352160319311253023 ) ) ;
#199753=CARTESIAN_POINT ( 'NONE',  ( 0.3809451599157384627, 1.611386624718774918, -0.6158283211408090985 ) ) ;
#199758=CARTESIAN_POINT ( 'NONE',  ( 5.835183367072669824, -1.691281831231405963, 0.7993005984755219284 ) ) ;
#199760=CARTESIAN_POINT ( 'NONE',  ( 6.345953593097265255, -1.318148336383131669, -1.521719194605136494 ) ) ;
#199764=CARTESIAN_POINT ( 'NONE',  ( 2.051582899450168362, -1.892833867889589960, 0.9560217657286762538 ) ) ;
#199765=CARTESIAN_POINT ( 'NONE',  ( 1.968375273883906429, -1.978056371059619511, -0.3905749819678172585 ) ) ;
#199766=CARTESIAN_POINT ( 'NONE',  ( 1.529274006537587161, -0.2194501901080987971, 1.798134050542072870 ) ) ;
#199768=CARTESIAN_POINT ( 'NONE',  ( 6.702040708066514085, -2.161345696851162845, 0.04751196314212167288 ) ) ;
#199771=CARTESIAN_POINT ( 'NONE',  ( 0.004910489962322779275, -0.09121751714964576596, 1.913643331117439672 ) ) ;
#199779=CARTESIAN_POINT ( 'NONE',  ( 4.522454563201145028, 1.332364063043835811, -1.702191164408660029 ) ) ;
#199782=CARTESIAN_POINT ( 'NONE',  ( 1.775790443353560732, 0.3575140072833471461, -2.090081039791711337 ) ) ;
#199783=CARTESIAN_POINT ( 'NONE',  ( 6.475623784153278883, 1.746001614453606576, -0.5331787911772439825 ) ) ;
#199784=CARTESIAN_POINT ( 'NONE',  ( 3.022686310138736676, 1.855048300136890482, 0.6674203052531629821 ) ) ;
#199785=CARTESIAN_POINT ( 'NONE',  ( 4.763870730211980487, 0.5944114921396548290, -1.817767169311027997 ) ) ;
#199789=CARTESIAN_POINT ( 'NONE',  ( 5.687944394218412469, -1.248225810400976465, -1.523521433493113308 ) ) ;
#199790=CARTESIAN_POINT ( 'NONE',  ( 1.781094086345108130, 1.339032250488644937, 1.406688339355038009 ) ) ;
#199798=CARTESIAN_POINT ( 'NONE',  ( 6.410809557875646547, -0.5148348048229570706, -1.841598127471068658 ) ) ;
#199800=CARTESIAN_POINT ( 'NONE',  ( 3.440233207309027375, 0.9924059104887033023, -1.971224004288201881 ) ) ;
#199801=CARTESIAN_POINT ( 'NONE',  ( 2.450463542074859280, 2.206263077450395738, 0.05474276496272853509 ) ) ;
#199803=CARTESIAN_POINT ( 'NONE',  ( 0.9789966485893276671, -1.729064073676725544, -0.8170501332188941923 ) ) ;
#199806=CARTESIAN_POINT ( 'NONE',  ( 3.561042923925850978, 1.633862107263984065, -1.271492733312264090 ) ) ;
#199811=CARTESIAN_POINT ( 'NONE',  ( 1.499129196564863209, 1.767075381950654611, -1.244890797856931686 ) ) ;
#199812=CARTESIAN_POINT ( 'NONE',  ( 3.614928802375876771, -0.1595779646587774658, 2.185787688459623901 ) ) ;
#199819=CARTESIAN_POINT ( 'NONE',  ( 5.502511934227880097, -1.689919030931926969, 0.3883318411201929776 ) ) ;
#199823=CARTESIAN_POINT ( 'NONE',  ( 4.030184149050713316, 1.145922430192683805, 1.723988044715178081 ) ) ;
#199824=CARTESIAN_POINT ( 'NONE',  ( 4.323895160615763622, 0.9038210025188663232, -1.914733396627795958 ) ) ;
#199827=CARTESIAN_POINT ( 'NONE',  ( 3.045709290742618425, 1.389371873615535602, 1.396104611999344769 ) ) ;
#199828=CARTESIAN_POINT ( 'NONE',  ( 0.4746845637013075159, -1.383529810647101455, 1.320479256824915071 ) ) ;
#199829=CARTESIAN_POINT ( 'NONE',  ( 4.593851424282248352, -2.291655481657675519, -0.05911330884650690953 ) ) ;
#199830=CARTESIAN_POINT ( 'NONE',  ( 2.930095790256614929, 1.013914413367119627, -1.518051517300327502 ) ) ;
#199836=CARTESIAN_POINT ( 'NONE',  ( 4.465094144989894431, -1.614439531090381408, 1.202519638469838226 ) ) ;
#199837=CARTESIAN_POINT ( 'NONE',  ( 4.680490258543752446, 1.210089798712219222, -1.543956201849092658 ) ) ;
#199840=CARTESIAN_POINT ( 'NONE',  ( 0.1751657365761703222, 0.2353161675953834020, -2.077853038718394885 ) ) ;
#199841=CARTESIAN_POINT ( 'NONE',  ( 0.9078953525096540300, -0.9432727566685695786, -1.865958795489220723 ) ) ;
#199842=CARTESIAN_POINT ( 'NONE',  ( 6.139478286200317214, -1.284810642169451622, -1.217457132491184035 ) ) ;
#199844=CARTESIAN_POINT ( 'NONE',  ( 2.291216553123593958, 1.694975396412688351, 1.389067552005143424 ) ) ;
#199845=CARTESIAN_POINT ( 'NONE',  ( 6.298757997817161502, 1.451094931915532404, 0.9604431249435537721 ) ) ;
#199848=CARTESIAN_POINT ( 'NONE',  ( 0.4688601960516668443, 0.1741500657085493509, -1.716052735907805937 ) ) ;
#199849=CARTESIAN_POINT ( 'NONE',  ( 0.7030180566853957425, -1.627119059678893587, -1.623510667393740725 ) ) ;
#199850=CARTESIAN_POINT ( 'NONE',  ( 0.7850416839378616674, 1.930235501049954339, -1.037882601892345713 ) ) ;
#199851=CARTESIAN_POINT ( 'NONE',  ( 3.299657469156279888, 1.739734091921738557, 1.357710657151039779 ) ) ;
#199853=CARTESIAN_POINT ( 'NONE',  ( 0.7608744453060071189, -0.7297706024342350828, -2.044895412143563185 ) ) ;
#199855=CARTESIAN_POINT ( 'NONE',  ( 2.800141503465008341, -1.047918259751862147, -1.839804015593812458 ) ) ;
#199856=CARTESIAN_POINT ( 'NONE',  ( 5.104483318454627216, -0.6487533354903095573, -1.814000550502705922 ) ) ;
#199858=CARTESIAN_POINT ( 'NONE',  ( 2.665910428807946708, 1.228978066529669899, 1.934933738419620575 ) ) ;
#199863=CARTESIAN_POINT ( 'NONE',  ( 4.354274701107041956, 0.9498992632326860308, -2.008065553403962422 ) ) ;
#199870=CARTESIAN_POINT ( 'NONE',  ( 2.953750172290268150, -1.864168560446223033, -0.7691209412190866956 ) ) ;
#199872=CARTESIAN_POINT ( 'NONE',  ( 1.059521212928912881, 1.683986000210126788, 1.190688086201870499 ) ) ;
#199877=CARTESIAN_POINT ( 'NONE',  ( 4.295009486468337023, 1.759388067201245187, 1.306329983072423984 ) ) ;
#199878=CARTESIAN_POINT ( 'NONE',  ( 1.055314813143366726, -1.277040974352643854, 1.560502084637045650 ) ) ;
#199879=CARTESIAN_POINT ( 'NONE',  ( 1.329379181053941483, 0.9071106928158387817, -1.602193565413398968 ) ) ;
#199880=CARTESIAN_POINT ( 'NONE',  ( 5.671479170183292950, 1.362789248821870025, 1.843150307845689229 ) ) ;
#199881=CARTESIAN_POINT ( 'NONE',  ( 3.714658492009088153, -0.1339090230784936997, 1.836323816731308067 ) ) ;
#199883=CARTESIAN_POINT ( 'NONE',  ( 4.155160913615768337, -1.517764731708035386, -1.014145119915064841 ) ) ;
#199884=CARTESIAN_POINT ( 'NONE',  ( 5.449842333688053486, -1.824117940560719298, -0.8596331684956670660 ) ) ;
#199886=CARTESIAN_POINT ( 'NONE',  ( 5.102513680054168610, -0.7571875712604788644, -2.132187818420825831 ) ) ;
#199888=CARTESIAN_POINT ( 'NONE',  ( 6.774446309029529267, -1.298820955785205955, 1.658247839749617869 ) ) ;
#199889=CARTESIAN_POINT ( 'NONE',  ( 3.578635096964689843, 1.315621898185691974, -1.598582974826658010 ) ) ;
#199894=CARTESIAN_POINT ( 'NONE',  ( 1.875490933414716288, 1.843686865663298091, -0.5587569667290130937 ) ) ;
#199896=CARTESIAN_POINT ( 'NONE',  ( 6.332857179708399009, -1.868906791504289844, -0.6213115537570863545 ) ) ;
#199901=CARTESIAN_POINT ( 'NONE',  ( 1.002369745560643510, -0.9483682245385971488, 1.896766750748935415 ) ) ;
#199902=CARTESIAN_POINT ( 'NONE',  ( 1.986886853112525442, -1.362214788617806649, 1.754679387841934002 ) ) ;
#199903=CARTESIAN_POINT ( 'NONE',  ( 3.030406611367501224, 1.171151514522270398, -1.750062178063223506 ) ) ;
#199906=CARTESIAN_POINT ( 'NONE',  ( 0.8712809235682484887, -0.2783187086575014679, 1.840006102165496982 ) ) ;
#199912=CARTESIAN_POINT ( 'NONE',  ( 1.283610819548046011, 0.1505422781087061845, -2.115291873224629082 ) ) ;
#199915=CARTESIAN_POINT ( 'NONE',  ( 4.088298575758734898, 1.051444423028622399, -1.656135347060924135 ) ) ;
#199916=CARTESIAN_POINT ( 'NONE',  ( 3.801785103514757846, -0.6297183656660889639, 2.067937956787009757 ) ) ;
#199917=CARTESIAN_POINT ( 'NONE',  ( 1.979791773625012352, -1.805961398883266344, -0.3578489297004632808 ) ) ;
#199920=CARTESIAN_POINT ( 'NONE',  ( 4.206796582046585797, -0.2943472477981134428, 1.715077512146965688 ) ) ;
#199926=CARTESIAN_POINT ( 'NONE',  ( 2.448304249002517974, 2.161202317112873139, 0.05382173394478938222 ) ) ;
#199927=CARTESIAN_POINT ( 'NONE',  ( 3.128279665134887644, 0.2985813455266342342, -1.993766061640166232 ) ) ;
#199929=CARTESIAN_POINT ( 'NONE',  ( 1.024558638192473170, 1.287004556549703693, -1.736669753874709343 ) ) ;
#199930=CARTESIAN_POINT ( 'NONE',  ( 3.625814716899962153, -1.173175478197308053, -1.584272814160747833 ) ) ;
#199931=CARTESIAN_POINT ( 'NONE',  ( 3.228005407155889461, 1.895358990768666096, 0.4226955006484037214 ) ) ;
#199940=CARTESIAN_POINT ( 'NONE',  ( 0.3236265600991515834, -0.1057403636935544400, 2.204373366691187108 ) ) ;
#199942=ADVANCED_FACE ( 'NONE', ( #166481 ), #119938, .T. ) ;
#199943=CARTESIAN_POINT ( 'NONE',  ( 4.838696733575553743, -1.901848327180942766, -0.4805237247276354928 ) ) ;
#199944=( BOUNDED_SURFACE ( )  B_SPLINE_SURFACE ( 3, 3, ( 
 ( #99189, #2705, #564, #69838, #50428, #53622, #119754, #116547, #35222, #85051, #86122 ),
 ( #169502, #150068, #185733, #184669, #21084, #200904, #87187, #213958, #101298, #82916, #182539 ),
 ( #34166, #151138, #115489, #68779, #100237, #134898, #102367, #197731, #1640, #67698, #165240 ),
 ( #131726, #133845, #49371, #16833, #148989, #73054, #203044, #107780, #139153, #24299, #4827 ),
 ( #57888, #141325, #74148, #89342, #55751, #75214, #125115, #106696, #205183, #138085, #190017 ),
 ( #56824, #204099, #23230, #120835, #121907, #124051, #70907, #186811, #172721, #173805, #105602 ),
 ( #137017, #41669, #26451, #54685, #170564, #122994, #187876, #39503, #171633, #38439, #154329 ) ),
 .UNSPECIFIED., .T., .F., .T. ) 
 B_SPLINE_SURFACE_WITH_KNOTS ( ( 4, 3, 4 ),
 ( 4, 1, 1, 1, 1, 1, 1, 1, 4 ),
 ( 0.000000000000000000, 0.5000000000000000000, 1.000000000000000000 ),
 ( 0.000000000000000000, 0.2256926809922864541, 0.3979886288388991278, 0.5260859906349554249, 0.6192013483571605637, 0.6864504996671639825, 0.7364865548622955282, 0.7772638159577213157, 1.000000000000000000 ),
 .UNSPECIFIED. ) 
 GEOMETRIC_REPRESENTATION_ITEM ( )  RATIONAL_B_SPLINE_SURFACE ( (
 ( 1.000000000000000222, 1.000000000000000222, 0.9999999999999997780, 1.000000000000000222, 0.9999999999999996669, 1.000000000000000000, 1.000000000000000222, 0.9999999999999996669, 1.000000000000000444, 1.000000000000000222, 1.000000000000000222),
 ( 0.3333333333333334259, 0.3333333333333334259, 0.3333333333333333148, 0.3333333333333333703, 0.3333333333333333703, 0.3333333333333332593, 0.3333333333333334814, 0.3333333333333332038, 0.3333333333333335924, 0.3333333333333334259, 0.3333333333333334259),
 ( 0.3333333333333334259, 0.3333333333333334259, 0.3333333333333333148, 0.3333333333333333703, 0.3333333333333333703, 0.3333333333333332593, 0.3333333333333334814, 0.3333333333333332038, 0.3333333333333335924, 0.3333333333333334259, 0.3333333333333334259),
 ( 1.000000000000000222, 1.000000000000000222, 0.9999999999999997780, 1.000000000000000222, 0.9999999999999996669, 1.000000000000000000, 1.000000000000000222, 0.9999999999999996669, 1.000000000000000444, 1.000000000000000222, 1.000000000000000222),
 ( 0.3333333333333334259, 0.3333333333333334259, 0.3333333333333333148, 0.3333333333333333703, 0.3333333333333333703, 0.3333333333333332593, 0.3333333333333334814, 0.3333333333333332038, 0.3333333333333335924, 0.3333333333333334259, 0.3333333333333334259),
 ( 0.3333333333333334259, 0.3333333333333334259, 0.3333333333333333148, 0.3333333333333333703, 0.3333333333333333703, 0.3333333333333332593, 0.3333333333333334814, 0.3333333333333332038, 0.3333333333333335924, 0.3333333333333334259, 0.3333333333333334259),
 ( 1.000000000000000222, 1.000000000000000222, 0.9999999999999997780, 1.000000000000000222, 0.9999999999999996669, 1.000000000000000000, 1.000000000000000222, 0.9999999999999996669, 1.000000000000000444, 1.000000000000000222, 1.000000000000000222) ) ) 
 REPRESENTATION_ITEM ( '' )  SURFACE ( )  );
#199945=CARTESIAN_POINT ( 'NONE',  ( 2.285779929129946098, 1.617817622347239803, -1.203354541732377658 ) ) ;
#199947=CARTESIAN_POINT ( 'NONE',  ( 2.923186261301851996, -1.865062457072470536, 1.002408848433397726 ) ) ;
#199949=CARTESIAN_POINT ( 'NONE',  ( 0.1747926744264677035, 1.388892567315727744, -2.112808070315982167 ) ) ;
#199951=CARTESIAN_POINT ( 'NONE',  ( 2.800538183361205302, 1.555518290611109800, 0.9846574483025126723 ) ) ;
#199956=CARTESIAN_POINT ( 'NONE',  ( 5.080389167821143026, 1.047295930500062866, 1.843893106414703054 ) ) ;
#199957=CARTESIAN_POINT ( 'NONE',  ( -0.2104748580754166598, -0.006608320950483163522, -2.103482951484026753 ) ) ;
#199959=CARTESIAN_POINT ( 'NONE',  ( 5.518845395222173877, 1.902436629287082237, 0.7926794616768815249 ) ) ;
#199960=CARTESIAN_POINT ( 'NONE',  ( 1.029495724655055344, 1.794938190532389788, -0.4914328765713778524 ) ) ;
#199961=CARTESIAN_POINT ( 'NONE',  ( 2.208333698829296310, 1.645431377724184463, 0.8263914577605266931 ) ) ;
#199966=CARTESIAN_POINT ( 'NONE',  ( 2.297764732281985633, 1.706874461811638044, 1.398895601573101111 ) ) ;
#199967=CARTESIAN_POINT ( 'NONE',  ( 4.499490165225078719, 1.813563011714003803, 1.352382200441957227 ) ) ;
#199969=CARTESIAN_POINT ( 'NONE',  ( 4.166123871162411341, 1.811061351045451850, -0.05074819156030555695 ) ) ;
#199970=CARTESIAN_POINT ( 'NONE',  ( 5.085127819360848456, 1.569905733240322343, 1.097627489654330990 ) ) ;
#199972=CARTESIAN_POINT ( 'NONE',  ( 3.625814716899962153, -1.173175478197308053, -1.584272814160747833 ) ) ;
#199973=CARTESIAN_POINT ( 'NONE',  ( 4.821099876132087125, -0.09137817997613774390, 1.868553921495450965 ) ) ;
#199974=CARTESIAN_POINT ( 'NONE',  ( 5.336322170104328855, -1.033901835001526104, 1.547212704913742520 ) ) ;
#199978=CARTESIAN_POINT ( 'NONE',  ( 0.6027503803631119039, 1.865048444749048739, 0.7672877736318934883 ) ) ;
#199980=CARTESIAN_POINT ( 'NONE',  ( 1.330846195043289493, 2.030104276556158549, 0.5602782565924493419 ) ) ;
#199983=CARTESIAN_POINT ( 'NONE',  ( 0.07479286986305369589, 0.2526433113205875935, -1.890777245541554796 ) ) ;
#199984=CARTESIAN_POINT ( 'NONE',  ( 3.428091063814618700, -2.088597262255381448, 0.3661859999234198249 ) ) ;
#199986=CARTESIAN_POINT ( 'NONE',  ( 1.793229165239007994, -0.1032543025433537293, -2.017296481459893709 ) ) ;
#199988=DIRECTION ( 'NONE',  ( 1.039099362110107450E-15, 1.000000000000000000, -4.583713267641621330E-32 ) ) ;
#199991=CARTESIAN_POINT ( 'NONE',  ( 2.530746307392011563, 2.096003997654236173, 0.5278882200696957128 ) ) ;
#199996=FACE_OUTER_BOUND ( 'NONE', #38374, .T. ) ;
#199998=CARTESIAN_POINT ( 'NONE',  ( 1.171705676731093604, 1.309414992938146893, 1.757219779060022580 ) ) ;
#200000=CARTESIAN_POINT ( 'NONE',  ( 1.376233744030544104, 1.349093794351564624, 1.816168808025316661 ) ) ;
#200003=CARTESIAN_POINT ( 'NONE',  ( 4.382046175016578005, -2.016188710442788246, -0.04465648322755921829 ) ) ;
#200008=CARTESIAN_POINT ( 'NONE',  ( 4.283650633623343751, 1.129305773815322711, 1.303882612223838500 ) ) ;
#200010=CARTESIAN_POINT ( 'NONE',  ( 2.336827959689928846, -1.583187595272864900, 0.7909824253358921364 ) ) ;
#200011=CARTESIAN_POINT ( 'NONE',  ( 5.069440727656137291, 0.2206807655098403653, -2.195719112144229879 ) ) ;
#200013=CARTESIAN_POINT ( 'NONE',  ( 4.640881595473839383, 1.934004784890541062, 0.5824627899903914718 ) ) ;
#200015=CARTESIAN_POINT ( 'NONE',  ( 4.851185501729457172, 0.1948232160459452411, -2.006962824030594561 ) ) ;
#200018=CARTESIAN_POINT ( 'NONE',  ( 2.272138710904994863, -1.152746988206950096, 1.473173409640892384 ) ) ;
#200020=CARTESIAN_POINT ( 'NONE',  ( 2.074333847954575205, 0.8209984392052707136, 1.727357542596375861 ) ) ;
#200025=CARTESIAN_POINT ( 'NONE',  ( 0.6680393924826667496, 1.910109291395128972, -0.09634788558426229943 ) ) ;
#200027=CARTESIAN_POINT ( 'NONE',  ( 2.137090596337941406, -0.09316805448006218460, -1.959763546484971197 ) ) ;
#200030=CARTESIAN_POINT ( 'NONE',  ( 5.537388447972660721, -0.05000006065614125139, 2.120159173171487055 ) ) ;
#200033=CARTESIAN_POINT ( 'NONE',  ( 6.766873944267649321, -1.801439555086775002, -0.8010921537245048185 ) ) ;
#200035=CARTESIAN_POINT ( 'NONE',  ( 1.793228464370033581, -0.1031022715946017104, -2.010704963445380411 ) ) ;
#200038=CARTESIAN_POINT ( 'NONE',  ( 1.300578652796330115, 1.418844934001600944, -1.571659118156268908 ) ) ;
#200041=CARTESIAN_POINT ( 'NONE',  ( 3.156751980976373329, -0.5984545454679365273, -1.982000093670479135 ) ) ;
#200045=CARTESIAN_POINT ( 'NONE',  ( 5.068349447220681370, -1.968310418947304408, -0.7050240649949056637 ) ) ;
#200047=CARTESIAN_POINT ( 'NONE',  ( 2.977373796215293300, 1.734057503958493118, -0.5710112477543202170 ) ) ;
#200048=CARTESIAN_POINT ( 'NONE',  ( 2.367557981294612812, 0.4819373766774863177, -1.746117998840409191 ) ) ;
#200050=CARTESIAN_POINT ( 'NONE',  ( 6.621690180768193379, -2.141820631849135292, 0.5315211216728524812 ) ) ;
#200054=CARTESIAN_POINT ( 'NONE',  ( 5.684669477433477169, -2.151827843693389308, -0.4886931181809702207 ) ) ;
#200057=CARTESIAN_POINT ( 'NONE',  ( 3.914637684252043393, -0.6027250981219151038, -1.814865640613130271 ) ) ;
#200067=CARTESIAN_POINT ( 'NONE',  ( 4.006994748872731549, 1.602975652146242380, 0.9638501484771769823 ) ) ;
#200073=CARTESIAN_POINT ( 'NONE',  ( 0.3386328343033001564, -1.908876393446774955, -0.4841592594212947298 ) ) ;
#200074=CARTESIAN_POINT ( 'NONE',  ( 1.722280025409760329, 1.994874335020242695, 0.2930476355553628953 ) ) ;
#200078=CARTESIAN_POINT ( 'NONE',  ( 3.064592470464472473, -2.024993410009158890, -0.8382372354380845936 ) ) ;
#200079=CARTESIAN_POINT ( 'NONE',  ( 6.059193749186201572, -1.568369423792463024, -0.9343120793870243190 ) ) ;
#200085=CARTESIAN_POINT ( 'NONE',  ( 3.966218424140379728, -1.719484690100345325, -0.6589542199007536460 ) ) ;
#200086=CARTESIAN_POINT ( 'NONE',  ( 0.5924399621960573237, -1.116526876179738226, 1.674895298907061569 ) ) ;
#200087=CARTESIAN_POINT ( 'NONE',  ( 3.304404366906594337, -2.028264134497267168, 1.081039266028597234 ) ) ;
#200089=CARTESIAN_POINT ( 'NONE',  ( 1.111883761159220496, 1.859168010044176311, -0.08395930885315286418 ) ) ;
#200093=CARTESIAN_POINT ( 'NONE',  ( 4.482611839828003930, -1.244964735940889522, 1.451779576051547282 ) ) ;
#200097=CARTESIAN_POINT ( 'NONE',  ( 4.300388110500093397, 1.614917507917512207, -1.327843252744983049 ) ) ;
#200098=CARTESIAN_POINT ( 'NONE',  ( 2.236979667955760309, -1.672073921526989748, 0.8388852543278202401 ) ) ;
#200101=CARTESIAN_POINT ( 'NONE',  ( 3.052039328023182119, -1.315916573227500219, 1.139148930295554862 ) ) ;
#200104=CARTESIAN_POINT ( 'NONE',  ( 4.090264520950432470, -1.706510830129988499, -0.2501320830878352997 ) ) ;
#200106=CARTESIAN_POINT ( 'NONE',  ( 6.322910218073367616, 2.057572540570989261, 0.7984293639632376038 ) ) ;
#200110=CARTESIAN_POINT ( 'NONE',  ( 3.063509990063197019, 1.831722579244631666, 1.165231348177008242 ) ) ;
#200111=CARTESIAN_POINT ( 'NONE',  ( 1.928079105319381314, 1.052063804484974385, -1.491885150056403431 ) ) ;
#200112=CARTESIAN_POINT ( 'NONE',  ( 0.4792544977638459880, -0.1021076105021078151, 1.959249876678282209 ) ) ;
#200113=CARTESIAN_POINT ( 'NONE',  ( 5.173117096678320870, 1.865890646727845326, -1.000864459693462383 ) ) ;
#200115=CARTESIAN_POINT ( 'NONE',  ( 5.530919501969752794, -2.073650524585127997, 0.9775372349926645388 ) ) ;
#200118=CARTESIAN_POINT ( 'NONE',  ( 1.067215373428985092, -1.669322716927954753, 1.307481345630675529 ) ) ;
#200123=CARTESIAN_POINT ( 'NONE',  ( 6.420782495146515778, -1.541274310347956922, 1.529322475779694601 ) ) ;
#200126=CARTESIAN_POINT ( 'NONE',  ( 1.594693315975799441, -1.184698573716694847, 1.878835628132907054 ) ) ;
#200128=CARTESIAN_POINT ( 'NONE',  ( 6.592432824109000222, -0.4393352932590722792, 1.975308225066509049 ) ) ;
#200130=CARTESIAN_POINT ( 'NONE',  ( 4.698127260392297444, 0.8867148737545665904, -1.862399597460895784 ) ) ;
#200136=CARTESIAN_POINT ( 'NONE',  ( 1.025464405625675646, -1.327728713622891688, -1.614889332886438655 ) ) ;
#200137=CARTESIAN_POINT ( 'NONE',  ( 4.641250102003463773, 0.7743139518727223392, 1.862017545363145565 ) ) ;
#200138=CARTESIAN_POINT ( 'NONE',  ( 4.757273854911123756, 1.820453720981948242, -0.2752165127944474210 ) ) ;
#200140=CARTESIAN_POINT ( 'NONE',  ( 0.7094338256347174632, -1.717145877019264022, 0.1620263704987124354 ) ) ;
#200143=CARTESIAN_POINT ( 'NONE',  ( 1.669569175971203023, 0.1671416771932125456, -2.256311322606067371 ) ) ;
#200144=CARTESIAN_POINT ( 'NONE',  ( 3.176497522518567873, -1.254329069944852382, 1.691643483388256985 ) ) ;
#200148=CARTESIAN_POINT ( 'NONE',  ( 5.937500000000004441, 1.451031289060873863, -1.451031289061349927 ) ) ;
#200153=CARTESIAN_POINT ( 'NONE',  ( 4.957398421247804166, -1.904820672624758515, 1.142771788014641743 ) ) ;
#200154=CARTESIAN_POINT ( 'NONE',  ( 3.416156609664961152, 1.390242785425911620, -1.694013327489252152 ) ) ;
#200159=CARTESIAN_POINT ( 'NONE',  ( 6.609999999999968345, 7.051749200714771959, 2.878153929105996323 ) ) ;
#200161=CARTESIAN_POINT ( 'NONE',  ( 4.377262645480927361, -1.895543854172193399, -0.9507902649282941043 ) ) ;
#200167=CARTESIAN_POINT ( 'NONE',  ( 4.616662711240536510, -0.08544939198026380023, 1.839383977539174264 ) ) ;
#200170=CARTESIAN_POINT ( 'NONE',  ( 1.206182128890446403, 1.534490571913693868, 0.8211921505957423539 ) ) ;
#200175=CARTESIAN_POINT ( 'NONE',  ( 5.383715653711652394, 1.448795075966866852, 1.604530791579752202 ) ) ;
#200178=CARTESIAN_POINT ( 'NONE',  ( 4.188458007013862172, -2.137797052781073237, -0.3198388112101158143 ) ) ;
#200180=CARTESIAN_POINT ( 'NONE',  ( 6.450460791689297757, 0.6159929566152704261, 1.872736359496610659 ) ) ;
#200181=CARTESIAN_POINT ( 'NONE',  ( 4.587041898695760622, 1.066698363585473652, -1.366732696162711314 ) ) ;
#200182=CARTESIAN_POINT ( 'NONE',  ( 2.208753784402537335, 1.959192758111829136, 0.9821998110004714899 ) ) ;
#200183=CARTESIAN_POINT ( 'NONE',  ( 1.975998049093165232, 2.207973392102855925, -0.6707195784038646469 ) ) ;
#200184=CARTESIAN_POINT ( 'NONE',  ( 5.096976104305405819, 1.715636550957209794, -1.141348886549067077 ) ) ;
#200185=CARTESIAN_POINT ( 'NONE',  ( 0.2517628464389579102, 0.7423079377118102506, 1.794666626680625932 ) ) ;
#200190=CARTESIAN_POINT ( 'NONE',  ( 1.020157974382044364, -1.821741137083273010, 0.8647263380179845971 ) ) ;
#200192=CARTESIAN_POINT ( 'NONE',  ( 2.942613154609276638, 2.189964478704994555, 0.2713889102748042736 ) ) ;
#200194=CARTESIAN_POINT ( 'NONE',  ( 2.359995855038379720, -1.860683555027684788, 0.03984664071272727565 ) ) ;
#200199=CARTESIAN_POINT ( 'NONE',  ( 6.925078400183531713, -0.004750840071900476122, 2.044148492825672569 ) ) ;
#200202=CARTESIAN_POINT ( 'NONE',  ( 3.344654342685839499, 0.4992920947068257842, 1.999368073990233308 ) ) ;
#200205=CARTESIAN_POINT ( 'NONE',  ( 1.910812834059022469, -0.5409473409442880909, -1.945794739053583466 ) ) ;
#200209=CARTESIAN_POINT ( 'NONE',  ( 2.149359023125880341, -1.654445155856735905, -1.228624528962230400 ) ) ;
#200213=CARTESIAN_POINT ( 'NONE',  ( -0.2411972340276204718, 2.032951786628557134, -2.316127775276015655 ) ) ;
#200214=CARTESIAN_POINT ( 'NONE',  ( 0.2515690823673248921, 0.7017594223384625574, 1.702352774230586618 ) ) ;
#200215=CARTESIAN_POINT ( 'NONE',  ( 5.848300530743933301, 2.204158087718602221, 0.1119919437090263481 ) ) ;
#200217=CARTESIAN_POINT ( 'NONE',  ( 1.212450271513715094, -0.9707322288472041150, -1.931405299116681018 ) ) ;
#200220=CARTESIAN_POINT ( 'NONE',  ( 1.815639016007553730, -1.320828798922760949, -1.523793687088881299 ) ) ;
#200221=CARTESIAN_POINT ( 'NONE',  ( 1.950936211155746447, 1.584691988697755960, 1.664941613344946836 ) ) ;
#200223=CARTESIAN_POINT ( 'NONE',  ( 0.1450994221751950586, -1.442925249786636943, -1.190247126510869613 ) ) ;
#200225=CARTESIAN_POINT ( 'NONE',  ( 2.043623373375623942, 0.7184291972081280342, -1.727395513401897453 ) ) ;
#200226=CARTESIAN_POINT ( 'NONE',  ( 3.731657894805060938, 0.6748485617756972976, -1.900415309456899182 ) ) ;
#200231=CARTESIAN_POINT ( 'NONE',  ( 5.320966398826527666, 1.945490409060679049, 0.8070863781705228668 ) ) ;
#200234=CARTESIAN_POINT ( 'NONE',  ( 6.639320575229294086, 0.002105643433562148347, 2.003388605011639179 ) ) ;
#200235=CARTESIAN_POINT ( 'NONE',  ( 5.537369811128121988, -0.04535447194144863470, 2.019437878860441238 ) ) ;
#200237=CARTESIAN_POINT ( 'NONE',  ( 0.6200784347700560861, 2.040642744413103671, -0.2990284185609564105 ) ) ;
#200245=CARTESIAN_POINT ( 'NONE',  ( 2.559224761666531567, 1.745036862030847624, -1.291676481929154408 ) ) ;
#200247=CARTESIAN_POINT ( 'NONE',  ( 2.454439063956286304, -1.602943312447857593, -0.9057913635923324769 ) ) ;
#200249=CARTESIAN_POINT ( 'NONE',  ( 3.984055765753656164, -2.167877601896048390, -0.3204034371554059235 ) ) ;
#200251=CARTESIAN_POINT ( 'NONE',  ( 5.172873261720807747, -2.128565284095069288, -0.7672878325792488186 ) ) ;
#200257=CARTESIAN_POINT ( 'NONE',  ( 6.520749347316099787, 1.652272609716086249, 0.6344386834381664508 ) ) ;
#200259=CARTESIAN_POINT ( 'NONE',  ( 4.090493406365951934, -1.157184705539246794, 1.647087716845529126 ) ) ;
#200261=CARTESIAN_POINT ( 'NONE',  ( 2.503073473877976518, 1.692030140557040152, -1.253631523096561784 ) ) ;
#200262=CARTESIAN_POINT ( 'NONE',  ( 0.4388990752801218975, -1.618778001572194647, -1.023919763412997286 ) ) ;
#200265=CARTESIAN_POINT ( 'NONE',  ( 2.330458462945466547, -1.214122947426389709, 1.550707797581540204 ) ) ;
#200266=CARTESIAN_POINT ( 'NONE',  ( 0.7252172114964609007, -1.777616610744123804, 0.5828384007960025759 ) ) ;
#200267=CARTESIAN_POINT ( 'NONE',  ( 1.398799877119625501, 0.3793605821263335565, 1.924665094374561791 ) ) ;
#200268=CARTESIAN_POINT ( 'NONE',  ( -0.08783152977152529350, -1.912005390248720627, -0.04503566501021933483 ) ) ;
#200272=CARTESIAN_POINT ( 'NONE',  ( 5.453920962983416665, 1.868457504587007545, -0.09292587778651076325 ) ) ;
#200275=CARTESIAN_POINT ( 'NONE',  ( 5.278213287142951238, -1.102824678039602269, -1.751873656341627505 ) ) ;
#200279=CARTESIAN_POINT ( 'NONE',  ( 0.1392002015415672034, -0.1474423581745692435, -2.037351525059682977 ) ) ;
#200286=CARTESIAN_POINT ( 'NONE',  ( 5.617619635959271385, 0.3843197845415853853, -1.923678648292715732 ) ) ;
#200288=CARTESIAN_POINT ( 'NONE',  ( 2.688827190807027367, -1.158510681541668141, -1.649829502315000251 ) ) ;
#200289=CARTESIAN_POINT ( 'NONE',  ( 2.096773827148257219, 1.713186613203399489, 0.8573791853930428086 ) ) ;
#200291=CARTESIAN_POINT ( 'NONE',  ( -0.09381621004311831158, -0.9424329983100244723, -1.976553698157037298 ) ) ;
#200292=CARTESIAN_POINT ( 'NONE',  ( 0.1333692844072801587, 4.087911462428309051, -2.608372271572469092 ) ) ;
#200293=CARTESIAN_POINT ( 'NONE',  ( 3.391731324245280010, -0.7611128710301139355, 1.708892184765831157 ) ) ;
#200297=CARTESIAN_POINT ( 'NONE',  ( 4.236029508982094072, 2.116713919566749702, -0.05380437090627546853 ) ) ;
#200300=CARTESIAN_POINT ( 'NONE',  ( 6.109843426155951107, 0.6047356833836557977, -1.980059631771100781 ) ) ;
#200301=CARTESIAN_POINT ( 'NONE',  ( 2.032869862874300271, -1.866249813966861515, 0.9426962998228316515 ) ) ;
#200302=CARTESIAN_POINT ( 'NONE',  ( 6.620655732516610215, 1.221631503675042030, 2.386181433960798071 ) ) ;
#200303=CARTESIAN_POINT ( 'NONE',  ( 0.6040130627208201153, -0.5744563726430768069, -1.626443300898507305 ) ) ;
#200313=CARTESIAN_POINT ( 'NONE',  ( 0.2053161149570548183, 1.340855080820763545, 1.218213988936674763 ) ) ;
#200323=CARTESIAN_POINT ( 'NONE',  ( 0.5267775621587212909, -1.642505510697172655, 0.9855279480080190169 ) ) ;
#200324=CARTESIAN_POINT ( 'NONE',  ( -0.1046615654881309365, -0.1561857951268459388, -2.086345279447648693 ) ) ;
#200325=CARTESIAN_POINT ( 'NONE',  ( -0.1399997263889612154, 1.357298622859518078, -2.254419820505838334 ) ) ;
#200330=CARTESIAN_POINT ( 'NONE',  ( 3.450015926008513478, -0.8023341227383492535, 1.798807795796441678 ) ) ;
#200331=CARTESIAN_POINT ( 'NONE',  ( 1.084817099560590803, -1.342388549496125627, 1.641497191572589776 ) ) ;
#200333=CARTESIAN_POINT ( 'NONE',  ( 6.727182134110196721, 7.051813866762763006, 2.787205683092201181 ) ) ;
#200334=CARTESIAN_POINT ( 'NONE',  ( 5.929655999079199269, 1.083026401007038952, -1.905042663481799403 ) ) ;
#200336=CARTESIAN_POINT ( 'NONE',  ( 3.715773558573881363, -1.898061356504710639, 0.3282749975898023309 ) ) ;
#200338=CARTESIAN_POINT ( 'NONE',  ( 0.3580656308817786737, 0.6935259069400133702, 1.688922952486398454 ) ) ;
#200339=CARTESIAN_POINT ( 'NONE',  ( 0.9970219447392356660, -0.5395372827587068265, -2.139793933917451874 ) ) ;
#200343=( BOUNDED_SURFACE ( )  B_SPLINE_SURFACE ( 3, 3, ( 
 ( #70665, #4591, #200666, #166065, #17651, #53376, #119511, #170319, #168198, #52315 ),
 ( #54453, #68535, #120596, #71736, #121670, #186573, #199609, #83735, #133604, #118445 ),
 ( #69601, #37122, #103201, #169263, #149827, #20849, #38201, #19797, #187637, #1397 ),
 ( #51252, #167140, #101050, #21907, #67458, #184432, #85881, #151957, #36049, #88017 ),
 ( #150898, #5656, #135709, #201735, #137850, #117377, #203871, #183374, #34979, #18725 ),
 ( #2459, #24066, #208149, #74968, #43557, #125937, #171395, #76032, #60846, #105358 ),
 ( #6740, #42491, #139998, #157299, #107534, #123814, #142135, #141078, #77089, #26204 ) ),
 .UNSPECIFIED., .T., .F., .F. ) 
 B_SPLINE_SURFACE_WITH_KNOTS ( ( 4, 3, 4 ),
 ( 4, 1, 1, 1, 1, 1, 1, 4 ),
 ( 0.000000000000000000, 0.5000000000000000000, 1.000000000000000000 ),
 ( 0.000000000000000000, 0.09705918685507786137, 0.1907419858981972138, 0.2602182418918835838, 0.3625179829595637226, 0.5215049497019805802, 0.7338397267804015467, 1.000000000000000000 ),
 .UNSPECIFIED. ) 
 GEOMETRIC_REPRESENTATION_ITEM ( )  RATIONAL_B_SPLINE_SURFACE ( (
 ( 1.000000000000000000, 1.000000000000000000, 1.000000000000000000, 1.000000000000000222, 1.000000000000000222, 0.9999999999999994449, 1.000000000000000444, 0.9999999999999997780, 1.000000000000000000, 1.000000000000000000),
 ( 0.3333333333333333703, 0.3333333333333333703, 0.3333333333333333703, 0.3333333333333334259, 0.3333333333333333703, 0.3333333333333332038, 0.3333333333333335369, 0.3333333333333332038, 0.3333333333333333703, 0.3333333333333333703),
 ( 0.3333333333333333703, 0.3333333333333333703, 0.3333333333333333703, 0.3333333333333334259, 0.3333333333333333703, 0.3333333333333332038, 0.3333333333333335369, 0.3333333333333332038, 0.3333333333333333703, 0.3333333333333333703),
 ( 1.000000000000000000, 1.000000000000000000, 1.000000000000000000, 1.000000000000000222, 1.000000000000000222, 0.9999999999999994449, 1.000000000000000444, 0.9999999999999997780, 1.000000000000000000, 1.000000000000000000),
 ( 0.3333333333333333703, 0.3333333333333333703, 0.3333333333333333703, 0.3333333333333334259, 0.3333333333333333703, 0.3333333333333332038, 0.3333333333333335369, 0.3333333333333332038, 0.3333333333333333703, 0.3333333333333333703),
 ( 0.3333333333333333703, 0.3333333333333333703, 0.3333333333333333703, 0.3333333333333334259, 0.3333333333333333703, 0.3333333333333332038, 0.3333333333333335369, 0.3333333333333332038, 0.3333333333333333703, 0.3333333333333333703),
 ( 1.000000000000000000, 1.000000000000000000, 1.000000000000000000, 1.000000000000000222, 1.000000000000000222, 0.9999999999999994449, 1.000000000000000444, 0.9999999999999997780, 1.000000000000000000, 1.000000000000000000) ) ) 
 REPRESENTATION_ITEM ( '' )  SURFACE ( )  );
#200344=CARTESIAN_POINT ( 'NONE',  ( 6.649268376821393822, 1.715264285883275397, -0.9675598167100638580 ) ) ;
#200345=CARTESIAN_POINT ( 'NONE',  ( 0.8373251867893832801, 0.7858318893144546902, -1.776134337346139125 ) ) ;
#200346=CARTESIAN_POINT ( 'NONE',  ( 6.485746271079104730, 2.140961846981633609, 0.8364165754714718570 ) ) ;
#200348=CARTESIAN_POINT ( 'NONE',  ( 4.838624485402447384, -1.804320056961044694, -0.4549315660777561443 ) ) ;
#200352=CARTESIAN_POINT ( 'NONE',  ( 6.720655732516652492, 7.053303974100803231, 2.424416723604695179 ) ) ;
#200353=CARTESIAN_POINT ( 'NONE',  ( 6.614806893291146572, -0.1579704184760947761, 2.055781730312715272 ) ) ;
#200360=CARTESIAN_POINT ( 'NONE',  ( 0.1526014871912773629, -1.468541917219987836, 1.084465738218153064 ) ) ;
#200362=CARTESIAN_POINT ( 'NONE',  ( 2.039351246016813501, -1.339629256360101106, 1.101148611782216014 ) ) ;
#200365=CARTESIAN_POINT ( 'NONE',  ( 0.3813102713988948955, 1.798072043455358981, -0.6920631024385316410 ) ) ;
#200366=CARTESIAN_POINT ( 'NONE',  ( 3.660947809037872425, 1.549288415169544963, -1.203348422379519667 ) ) ;
#200372=CARTESIAN_POINT ( 'NONE',  ( 5.022192282182047940, -2.110239842997441606, 0.2083548542347323507 ) ) ;
#200375=CARTESIAN_POINT ( 'NONE',  ( 3.432542862244458703, -1.236986750340131946, 1.659893174209552624 ) ) ;
#200378=CARTESIAN_POINT ( 'NONE',  ( 4.758541215226599341, 2.215266761731282674, 0.1642064029221591559 ) ) ;
#200380=CARTESIAN_POINT ( 'NONE',  ( 2.795839995030196423, 1.662961046791612940, -1.587192879829945946 ) ) ;
#200387=CARTESIAN_POINT ( 'NONE',  ( 3.972844611716894736, -1.413603510852480927, 1.288168406687495215 ) ) ;
#200389=CARTESIAN_POINT ( 'NONE',  ( 3.838627834895870450, 0.2530714650476103555, 1.705954220825799617 ) ) ;
#200390=CARTESIAN_POINT ( 'NONE',  ( 2.940638933469359895, -1.523795050681177710, 1.320827213682006285 ) ) ;
#200391=CARTESIAN_POINT ( 'NONE',  ( 4.395370282159323239, -0.9827166871091972400, -2.078181120130776272 ) ) ;
#200393=CARTESIAN_POINT ( 'NONE',  ( 6.621705515693503408, -2.043321748007483674, 0.5098342655636013410 ) ) ;
#200395=CARTESIAN_POINT ( 'NONE',  ( 5.835142003873758476, -1.599326089537930873, 0.7579421051841316315 ) ) ;
#200397=CARTESIAN_POINT ( 'NONE',  ( 1.412523707164672127, 1.536465969362065476, -1.701261851757162269 ) ) ;
#200398=CARTESIAN_POINT ( 'NONE',  ( 0.1459185412583801633, -1.400943258209320863, 1.032289493613134823 ) ) ;
#200404=CARTESIAN_POINT ( 'NONE',  ( 0.6608746330511162670, -0.7316962540516893654, -2.044312434917434640 ) ) ;
#200405=CARTESIAN_POINT ( 'NONE',  ( 1.376185782568883020, -2.007256511855738612, -0.1928315418098166534 ) ) ;
#200407=AXIS2_PLACEMENT_3D ( 'NONE', #95216, #132002, #161266 ) ;
#200409=CARTESIAN_POINT ( 'NONE',  ( 5.690048631714204497, -0.8642791622572744137, 1.721823430457876780 ) ) ;
#200411=CARTESIAN_POINT ( 'NONE',  ( 2.707538781118669302, 1.902989223989959067, -1.145821276547890122 ) ) ;
#200419=CARTESIAN_POINT ( 'NONE',  ( 3.983749006537410153, -1.722186279587777369, -0.2504274415035238621 ) ) ;
#200420=CARTESIAN_POINT ( 'NONE',  ( 2.154674626568295892, -0.5202524484802829585, -1.891573884155263396 ) ) ;
#200425=CARTESIAN_POINT ( 'NONE',  ( 0.9067701044400799937, 0.5968461685175918685, 1.974459182335401186 ) ) ;
#200428=CARTESIAN_POINT ( 'NONE',  ( 1.604739632818411144, -0.8155265934593752819, -2.110601385940619412 ) ) ;
#200431=CARTESIAN_POINT ( 'NONE',  ( 2.407302635362520427, -0.4140892318466664057, 1.823965488845371796 ) ) ;
#200432=CARTESIAN_POINT ( 'NONE',  ( 0.8614527929159084829, -0.04078779759817893064, -1.733857029152048757 ) ) ;
#200433=CARTESIAN_POINT ( 'NONE',  ( 5.003566749295822014, -2.181051155298455058, 0.2145382695054529609 ) ) ;
#200434=CARTESIAN_POINT ( 'NONE',  ( 5.544061457994609476, 0.9416624597364110505, -2.106895457712253616 ) ) ;
#200435=CARTESIAN_POINT ( 'NONE',  ( 1.411086320874027855, 1.817183042272657145, 0.9721812696896633410 ) ) ;
#200436=CARTESIAN_POINT ( 'NONE',  ( 3.644416830925560014, -1.587075459539259992, 1.118831915631451013 ) ) ;
#200439=CARTESIAN_POINT ( 'NONE',  ( 6.081297793977560318, 1.728434112010367674, -0.7156336962577531935 ) ) ;
#200441=CARTESIAN_POINT ( 'NONE',  ( 6.696638777208028692, -1.314797947003863543, -1.528504179509587280 ) ) ;
#200444=CARTESIAN_POINT ( 'NONE',  ( 4.061172775696818782, -1.158689426361030561, 1.650081270007992318 ) ) ;
#200448=CARTESIAN_POINT ( 'NONE',  ( 1.734698295210383767, 0.1775668987445792879, 1.817036636966688823 ) ) ;
#200457=CARTESIAN_POINT ( 'NONE',  ( 6.041667287826984811, -1.900962894602696185, 0.6825640075473203838 ) ) ;
#200458=CARTESIAN_POINT ( 'NONE',  ( -0.09290056220616692284, -0.4702265987995763452, -2.075310686570643437 ) ) ;
#200463=CARTESIAN_POINT ( 'NONE',  ( 4.803620198249330286, -0.5517947341296326469, 1.985563166520041278 ) ) ;
#200464=CARTESIAN_POINT ( 'NONE',  ( 5.467422714486909641, -1.967887220244109558, -0.4390321945699494632 ) ) ;
#200465=VERTEX_POINT ( 'NONE', #13847 ) ;
#200472=CARTESIAN_POINT ( 'NONE',  ( 4.622422610786712127, 0.4444332032229811325, -1.966343831704894907 ) ) ;
#200473=CARTESIAN_POINT ( 'NONE',  ( 4.259580805731934205, 0.8699401392010926992, 1.622648742527862620 ) ) ;
#200475=CARTESIAN_POINT ( 'NONE',  ( 0.07661050522434449672, 6.948789054712463553, -2.305832378935098514 ) ) ;
#200476=CARTESIAN_POINT ( 'NONE',  ( 2.086955060466778811, -2.263696646927360501, -0.4477047476570076290 ) ) ;
#200478=CARTESIAN_POINT ( 'NONE',  ( 5.044278900083454253, 2.155409826167026477, 0.1645634770654491874 ) ) ;
#200480=CARTESIAN_POINT ( 'NONE',  ( 0.2044968316872765035, 1.690132753820037692, 0.9564217018903762302 ) ) ;
#200485=CARTESIAN_POINT ( 'NONE',  ( 3.537841792810627606, 0.8420186812403904764, -1.670516725672297031 ) ) ;
#200489=CARTESIAN_POINT ( 'NONE',  ( 2.948105999307056635, 0.7938017206191756436, -2.059354589195587337 ) ) ;
#200495=CARTESIAN_POINT ( 'NONE',  ( 0.4738186427182951577, 1.131346554974651086, 1.614239802345132757 ) ) ;
#200497=CARTESIAN_POINT ( 'NONE',  ( 6.393248246410252911, 2.011339380631727458, -1.131280203180404342 ) ) ;
#200498=CARTESIAN_POINT ( 'NONE',  ( 1.433958818539453395, 1.165882187713672247, 1.577721859592796205 ) ) ;
#200499=CARTESIAN_POINT ( 'NONE',  ( 4.539923930118438200, 1.343280314546798637, 1.565306332949261803 ) ) ;
#200507=CARTESIAN_POINT ( 'NONE',  ( 6.145025799957537060, -0.3124719705198654718, -2.148460482323500731 ) ) ;
#200511=CARTESIAN_POINT ( 'NONE',  ( 1.704156511045151978, -0.6684128243485131238, -1.747238085743174185 ) ) ;
#200516=CARTESIAN_POINT ( 'NONE',  ( 0.6449871831117167664, 0.1410837285014763798, 1.907147727228817535 ) ) ;
#200517=CARTESIAN_POINT ( 'NONE',  ( 3.309201167148849265, -0.3463371335676104223, 1.735430568453823374 ) ) ;
#200518=CARTESIAN_POINT ( 'NONE',  ( 0.1703706300211875746, 0.7318840393725855042, 1.766877091004593225 ) ) ;
#200520=CARTESIAN_POINT ( 'NONE',  ( 4.868704338522531039, -0.2386889102116992178, -1.900620109961237203 ) ) ;
#200522=CARTESIAN_POINT ( 'NONE',  ( 4.896905686981484429, 0.3346149513497528871, 1.940740247813901087 ) ) ;
#200523=CARTESIAN_POINT ( 'NONE',  ( 0.4398875993102538962, -2.011672884243600024, 0.6710486789910232730 ) ) ;
#200525=CARTESIAN_POINT ( 'NONE',  ( 3.502682687546424312, 1.475339254275360279, -1.149998991230333223 ) ) ;
#200526=CARTESIAN_POINT ( 'NONE',  ( 0.3108172448005979138, 1.586703044182024458, 0.9029097728878652251 ) ) ;
#200528=CARTESIAN_POINT ( 'NONE',  ( 3.879664727460280904, 2.078262106501146622, -0.7427522710690689367 ) ) ;
#200532=CARTESIAN_POINT ( 'NONE',  ( 0.5024796060203519099, 2.057031790779086045, 0.1535979213492833784 ) ) ;
#200539=CARTESIAN_POINT ( 'NONE',  ( 3.016144355299533952, 2.060630728401948275, -0.2003171163396169074 ) ) ;
#200541=CARTESIAN_POINT ( 'NONE',  ( 1.142116303652768172, 0.8771353898661786719, -1.975824051420910221 ) ) ;
#200543=CARTESIAN_POINT ( 'NONE',  ( 0.6276103948988649428, -0.2939658443398012744, 1.998026100167526575 ) ) ;
#200548=CARTESIAN_POINT ( 'NONE',  ( 6.538435458278026857, 1.930121188254026787, -0.5825698962980339068 ) ) ;
#200549=CARTESIAN_POINT ( 'NONE',  ( 5.735529463276822781, 0.5494309942872098729, -1.835271804430014919 ) ) ;
#200550=CARTESIAN_POINT ( 'NONE',  ( 4.318054327947466575, 1.347776305887092185, -1.728067674571641898 ) ) ;
#200552=CARTESIAN_POINT ( 'NONE',  ( 3.515784362865181478, -0.5505564139345071606, 1.831456330389509501 ) ) ;
#200556=CARTESIAN_POINT ( 'NONE',  ( 1.564077599769473803, -1.076297475396456704, 1.704952281334138675 ) ) ;
#200559=CARTESIAN_POINT ( 'NONE',  ( 0.9434182766495626815, -1.811351811004081158, -1.404917595322150659 ) ) ;
#200561=CARTESIAN_POINT ( 'NONE',  ( 4.260587326446613865, -1.277293937326873019, 1.159233799866489889 ) ) ;
#200562=CARTESIAN_POINT ( 'NONE',  ( 0.1399997263886020860, 0.7221123407896400392, -2.083281383436136558 ) ) ;
#200566=CARTESIAN_POINT ( 'NONE',  ( 1.170277241841523264, -0.8789641444944886750, -1.754005360843587047 ) ) ;
#200568=CARTESIAN_POINT ( 'NONE',  ( 0.07516593201269992919, 2.015085533825950126, -2.458757630349134082 ) ) ;
#200572=CARTESIAN_POINT ( 'NONE',  ( 4.318897000252651885, 1.397372457865418083, -1.152701029936139099 ) ) ;
#200576=CARTESIAN_POINT ( 'NONE',  ( 4.846265894328573687, 0.9266178045349574566, -1.556377301703376625 ) ) ;
#200580=CARTESIAN_POINT ( 'NONE',  ( 5.723074792265875566, -1.682715607417185399, -0.7953119777529999990 ) ) ;
#200582=CARTESIAN_POINT ( 'NONE',  ( 3.884325381594720739, -0.6044542036256529416, -1.817792542802825428 ) ) ;
#200589=CARTESIAN_POINT ( 'NONE',  ( 0.4269344243218140544, 2.069031678568326704, 0.6260965431626740463 ) ) ;
#200592=CARTESIAN_POINT ( 'NONE',  ( 0.7975364289293709330, -0.6616875547802402169, 1.701626729119443127 ) ) ;
#200595=CARTESIAN_POINT ( 'NONE',  ( 3.469579810302122702, 1.781292651720441711, -0.3989491859636914994 ) ) ;
#200598=CARTESIAN_POINT ( 'NONE',  ( 2.400782916097830455, 0.4286735998642232648, 1.922169311629307931 ) ) ;
#200599=CARTESIAN_POINT ( 'NONE',  ( 3.509261751715045730, -1.912814363422868480, 0.3349611914155846693 ) ) ;
#200603=CARTESIAN_POINT ( 'NONE',  ( 4.377262645480927361, -1.895543854172193399, -0.9507902649282941043 ) ) ;
#200613=CARTESIAN_POINT ( 'NONE',  ( 4.125493313500066428, -1.746467973620144942, 0.5319596651164605339 ) ) ;
#200618=CARTESIAN_POINT ( 'NONE',  ( 4.979306205331720747, 1.745251617482036943, -0.6738592683939447214 ) ) ;
#200620=CARTESIAN_POINT ( 'NONE',  ( 3.492722931844041145, -0.3765888977748827471, -1.889173544197232824 ) ) ;
#200629=CARTESIAN_POINT ( 'NONE',  ( 0.9314518356654817310, -1.671823418590481447, -1.299033474062233351 ) ) ;
#200632=CARTESIAN_POINT ( 'NONE',  ( 6.789897376884641567, -1.347643488625469121, -1.571692526165118009 ) ) ;
#200633=CARTESIAN_POINT ( 'NONE',  ( 1.505144418776669601, -1.827259764946763454, 0.2261131901925839127 ) ) ;
#200638=CARTESIAN_POINT ( 'NONE',  ( 1.113678556162515543, -2.235424308229993162, 0.5066684154252357741 ) ) ;
#200640=CARTESIAN_POINT ( 'NONE',  ( 5.507742394360604088, -0.8750994344452074358, -1.733673826448577593 ) ) ;
#200643=CARTESIAN_POINT ( 'NONE',  ( 0.4221356392010866543, -2.003110517487953324, 0.2016333174496009462 ) ) ;
#200648=CARTESIAN_POINT ( 'NONE',  ( 3.837900784552390476, 2.080585211200749018, 0.2046572434392830431 ) ) ;
#200649=CARTESIAN_POINT ( 'NONE',  ( 2.606023559441010828, -0.6750964425338638053, -1.636234759011189421 ) ) ;
#200651=CARTESIAN_POINT ( 'NONE',  ( 5.314510991623739855, 2.116275055252315074, 0.8812819573641057502 ) ) ;
#200652=CARTESIAN_POINT ( 'NONE',  ( 3.749730547248275148, 0.6284987560769598192, 1.623061768561576468 ) ) ;
#200656=CARTESIAN_POINT ( 'NONE',  ( 3.321388563693925544, -1.314311947043474538, 1.130952296748084951 ) ) ;
#200657=CARTESIAN_POINT ( 'NONE',  ( 4.018178019744323315, 2.155211776303669335, -0.2622048733134130782 ) ) ;
#200659=CARTESIAN_POINT ( 'NONE',  ( 4.645720405014278853, 1.993893748393640086, -0.3006458143828410479 ) ) ;
#200660=CARTESIAN_POINT ( 'NONE',  ( 1.281250000000000444, 0.7852924748300526003, 1.895863743164061255 ) ) ;
#200662=CARTESIAN_POINT ( 'NONE',  ( 2.239170187357332420, -1.721643101494104044, 0.8643732543716446948 ) ) ;
#200664=CARTESIAN_POINT ( 'NONE',  ( 6.047183177241617358, 0.2169752325061699572, 2.210822359046988428 ) ) ;
#200666=CARTESIAN_POINT ( 'NONE',  ( -0.2108831679771203116, 0.7314853703891763814, -1.979988191570913880 ) ) ;
#200671=CARTESIAN_POINT ( 'NONE',  ( 0.9794852244889130644, -2.010350447809361896, -0.9450808295136583492 ) ) ;
#200672=AXIS2_PLACEMENT_3D ( 'NONE', #18924, #118644, #67657 ) ;
#200673=CARTESIAN_POINT ( 'NONE',  ( 5.828557447170540584, -1.245780601409246957, 1.515539014345569147 ) ) ;
#200676=CARTESIAN_POINT ( 'NONE',  ( 0.1929406647830470833, -0.4748886411078504510, -2.116594070111991410 ) ) ;
#200679=CARTESIAN_POINT ( 'NONE',  ( 3.859879052112312969, -0.6014189565349871147, 1.973034901002912678 ) ) ;
#200683=CARTESIAN_POINT ( 'NONE',  ( 5.870339087135666212, -1.187030499695044039, 1.445606174157453738 ) ) ;
#200684=CARTESIAN_POINT ( 'NONE',  ( 4.289544331642456854, 1.336530783054422189, -1.104934575851760137 ) ) ;
#200685=CARTESIAN_POINT ( 'NONE',  ( 3.790341827058436142, 1.467891733132551613, -0.9347920342070329403 ) ) ;
#200687=CARTESIAN_POINT ( 'NONE',  ( 1.839794590071419211, 0.8728355696882350578, -2.119893007042342958 ) ) ;
#200689=CARTESIAN_POINT ( 'NONE',  ( 5.460518745505165583, -1.890641411385725501, -0.8928391682238371319 ) ) ;
#200690=CARTESIAN_POINT ( 'NONE',  ( 6.544875487120448199, -1.561333999131156780, -1.154546517916557269 ) ) ;
#200693=CARTESIAN_POINT ( 'NONE',  ( 1.617814789376757156, 0.2004366740697149929, 2.006445999502483257 ) ) ;
#200694=CARTESIAN_POINT ( 'NONE',  ( 0.4631483011842302822, 0.2107759881739782182, -2.181290363801504650 ) ) ;
#200698=CARTESIAN_POINT ( 'NONE',  ( 2.157031413788193852, 0.4673396547767159070, 2.068183735011968505 ) ) ;
#200700=CARTESIAN_POINT ( 'NONE',  ( 5.092344371507952161, -1.812320225013038133, -0.2200062734805732223 ) ) ;
#200707=CARTESIAN_POINT ( 'NONE',  ( 2.760026041568770072, 0.7230886973167930387, -1.886116010022680589 ) ) ;
#200708=CARTESIAN_POINT ( 'NONE',  ( 6.282275147445602670, -1.185768659569720329, 1.860957768143455038 ) ) ;
#200710=CARTESIAN_POINT ( 'NONE',  ( 4.170637490619288457, 1.318561355513592215, -1.313476238859044409 ) ) ;
#200720=CARTESIAN_POINT ( 'NONE',  ( 1.457864220016273693, 1.308402020977760261, 1.137755859488085886 ) ) ;
#200721=CARTESIAN_POINT ( 'NONE',  ( 1.376469814831126071, 1.609123190100629985, -0.6634216792447115152 ) ) ;
#200722=CARTESIAN_POINT ( 'NONE',  ( 5.233197408665407835, 0.1653354203888204033, 2.301840570688079790 ) ) ;
#200725=CARTESIAN_POINT ( 'NONE',  ( 1.159529407832321501, 0.4047576141815812378, -2.020457351226915055 ) ) ;
#200727=CARTESIAN_POINT ( 'NONE',  ( 6.591202130252849400, 1.331619970128885777, -1.873199602832905430 ) ) ;
#200730=CARTESIAN_POINT ( 'NONE',  ( 0.1628737759792201201, -1.759808232078699630, -0.8888803535714930870 ) ) ;
#200731=CARTESIAN_POINT ( 'NONE',  ( 4.306835718904429733, -0.4242474483713705169, -1.864571660543254961 ) ) ;
#200734=CARTESIAN_POINT ( 'NONE',  ( 6.217417563691929772, -0.2743312036321900460, 2.189694890431858276 ) ) ;
#200739=CARTESIAN_POINT ( 'NONE',  ( 6.375647721065083928, 0.3630326626483972308, -2.089014862189771726 ) ) ;
#200742=CARTESIAN_POINT ( 'NONE',  ( 3.716130297413534844, -2.273962828982917017, 0.3916390033968617512 ) ) ;
#200743=CARTESIAN_POINT ( 'NONE',  ( 4.809014631063706524, -1.576880339463518022, 1.167019128429528374 ) ) ;
#200744=CARTESIAN_POINT ( 'NONE',  ( 0.6198768371072012062, 1.941228818809427104, -0.2821078022595123747 ) ) ;
#200748=CARTESIAN_POINT ( 'NONE',  ( 0.4623062725150044461, -1.170719190667910414, 1.764065175548671593 ) ) ;
#200751=CARTESIAN_POINT ( 'NONE',  ( 0.2691533882960769897, 1.057504993221158873, 1.506941669042777265 ) ) ;
#200752=CARTESIAN_POINT ( 'NONE',  ( 3.204148022151423802, 0.7856563700287253482, -2.024084340642897661 ) ) ;
#200754=CARTESIAN_POINT ( 'NONE',  ( 1.195735321641926197, 1.957225868588155837, -0.8166992996602240318 ) ) ;
#200759=CARTESIAN_POINT ( 'NONE',  ( 2.231779466116891708, -1.343800923419868010, -1.562491722542774797 ) ) ;
#200766=CARTESIAN_POINT ( 'NONE',  ( 4.688094572372190960, 1.103980140559155831, 1.561224650464939190 ) ) ;
#200768=CARTESIAN_POINT ( 'NONE',  ( 1.036823874139713997, 2.229064601995099260, 0.3862009557947677640 ) ) ;
#200770=CARTESIAN_POINT ( 'NONE',  ( 1.335881098409009704, -1.007921504507871102, -1.505067075931452392 ) ) ;
#200771=CARTESIAN_POINT ( 'NONE',  ( 0.5498253489954890716, 0.9468162992772524156, 1.665335589065963129 ) ) ;
#200772=CARTESIAN_POINT ( 'NONE',  ( 1.609917502266303480, 0.6029389078928657497, -1.980602105166151095 ) ) ;
#200774=CARTESIAN_POINT ( 'NONE',  ( 6.789956943122251509, -0.7972922127613899512, 1.690610701080223821 ) ) ;
#200775=CARTESIAN_POINT ( 'NONE',  ( 5.690048631714204497, -0.8642791622572744137, 1.721823430457876780 ) ) ;
#200776=CARTESIAN_POINT ( 'NONE',  ( 0.2414294658986924358, 0.4011018576653562207, 2.272434410966933438 ) ) ;
#200779=CARTESIAN_POINT ( 'NONE',  ( 3.877431937021211361, -0.1548021625025173265, 2.056941320008953245 ) ) ;
#200784=CARTESIAN_POINT ( 'NONE',  ( 4.876057405804426814, 1.210321851207227795, 1.723226277364843462 ) ) ;
#200787=CARTESIAN_POINT ( 'NONE',  ( 6.602015318333181781, 0.7961593463888805289, -1.911361562896146671 ) ) ;
#200789=CARTESIAN_POINT ( 'NONE',  ( 4.552137767457805850, 2.161219302129935738, -0.04802546048104232301 ) ) ;
#200790=CARTESIAN_POINT ( 'NONE',  ( 5.127605754342813960, -0.2940821729933600914, 1.998008755081616572 ) ) ;
#200791=CARTESIAN_POINT ( 'NONE',  ( -0.1399997263889663501, 0.2375346743129815030, -2.034463206964792548 ) ) ;
#200796=CARTESIAN_POINT ( 'NONE',  ( 3.995327539805045181, -0.3399590882401174463, 1.987497567597557468 ) ) ;
#200803=CARTESIAN_POINT ( 'NONE',  ( 4.288685525864014636, 1.556897452430844320, -1.281376678550147474 ) ) ;
#200805=CARTESIAN_POINT ( 'NONE',  ( 0.2754634098539961440, 0.9884889332615778290, 1.413329177942000303 ) ) ;
#200809=CIRCLE ( 'NONE', #194361, 0.04999999999999969746 ) ;
#200811=CARTESIAN_POINT ( 'NONE',  ( 5.448468942325162878, 0.5420331153751513087, 1.790312535500695024 ) ) ;
#200812=CARTESIAN_POINT ( 'NONE',  ( 5.976820168803962829, -1.420628428873932814, 1.426715538211227763 ) ) ;
#200816=CARTESIAN_POINT ( 'NONE',  ( 1.071888921174158016, -0.9040910708146729924, 1.802427947461216373 ) ) ;
#200817=CARTESIAN_POINT ( 'NONE',  ( 1.072181177352715453, 0.7354878280073854357, 1.655762779942154372 ) ) ;
#200819=CARTESIAN_POINT ( 'NONE',  ( 6.561405286136596793, 0.3748316153167964848, -2.128808860954830795 ) ) ;
#200823=CARTESIAN_POINT ( 'NONE',  ( -0.1181432109131977104, -1.915350881444439102, -0.04437447078771068754 ) ) ;
#200829=CARTESIAN_POINT ( 'NONE',  ( 3.784175263432405956, -1.067420458145739826, 1.879713924940962677 ) ) ;
#200832=CARTESIAN_POINT ( 'NONE',  ( 0.5980879788009090259, 1.428637019467562830, 1.567290143595565066 ) ) ;
#200834=CARTESIAN_POINT ( 'NONE',  ( 2.530492563074437928, 1.911271491015430035, 0.4824842627236708426 ) ) ;
#200835=CARTESIAN_POINT ( 'NONE',  ( 4.394721148579957770, -1.856311205515799312, -0.4593126252911489127 ) ) ;
#200838=CARTESIAN_POINT ( 'NONE',  ( 6.584429662329396749, 1.135205087083859476, -1.609268749140836618 ) ) ;
#200839=CARTESIAN_POINT ( 'NONE',  ( 1.165847801482827517, -1.232189268765693235, 1.500965459471349961 ) ) ;
#200846=CARTESIAN_POINT ( 'NONE',  ( 4.723256143441832755, 1.665581346147155806, 0.9393396248940300008 ) ) ;
#200848=CARTESIAN_POINT ( 'NONE',  ( 3.563272299071856164, -1.946135509614330239, -1.040604674307284316 ) ) ;
#200850=CARTESIAN_POINT ( 'NONE',  ( 1.677102584378454608, -2.095606157416990190, -0.6917391671936305997 ) ) ;
#200852=CARTESIAN_POINT ( 'NONE',  ( 1.137202173061176547, -0.04613941135153502154, 1.911881008470908139 ) ) ;
#200858=CARTESIAN_POINT ( 'NONE',  ( 3.490741092712910998, 2.019281663078629219, 0.4563312328872349277 ) ) ;
#200862=CARTESIAN_POINT ( 'NONE',  ( 0.5323697292517782786, 1.110078392871534314, -1.854780036684190669 ) ) ;
#200863=CARTESIAN_POINT ( 'NONE',  ( 3.228257827484398490, 2.138632370135685523, 0.4780590757816546854 ) ) ;
#200872=CARTESIAN_POINT ( 'NONE',  ( 5.713412806352172524, 1.673543110082301721, 0.4542079487798825199 ) ) ;
#200874=CARTESIAN_POINT ( 'NONE',  ( 3.379797469122407083, -1.996479967689598789, 0.5476083754193948883 ) ) ;
#200875=CARTESIAN_POINT ( 'NONE',  ( 4.341493734318905950, 0.4621530863439751724, -2.066033417628045932 ) ) ;
#200878=CARTESIAN_POINT ( 'NONE',  ( 3.309381622104785148, -1.607321225346239668, -1.137771303188861660 ) ) ;
#200879=CARTESIAN_POINT ( 'NONE',  ( 0.4219365929402639215, -1.902980170924161385, 0.1897552588234762416 ) ) ;
#200880=CARTESIAN_POINT ( 'NONE',  ( 4.998102599042142380, -0.7687487195138610341, -2.159632177038037337 ) ) ;
#200881=CARTESIAN_POINT ( 'NONE',  ( 2.859763506297557711, 1.816872213737670938, -0.1792109616642542924 ) ) ;
#200885=CARTESIAN_POINT ( 'NONE',  ( 4.236591777569945982, 1.235091891264840314, -1.589779643154372701 ) ) ;
#200886=CARTESIAN_POINT ( 'NONE',  ( 4.030091663008243508, 1.086175826233202857, 1.633415718976807041 ) ) ;
#200889=CARTESIAN_POINT ( 'NONE',  ( 0.1755611466353447780, 1.308645672766622914, -2.493865953706751792 ) ) ;
#200890=CARTESIAN_POINT ( 'NONE',  ( 0.08173368997131927327, -0.9817114319007680390, 1.845913477919949086 ) ) ;
#200891=CARTESIAN_POINT ( 'NONE',  ( 5.981276632755388789, 1.633781900041403334, -0.6810181619275444964 ) ) ;
#200893=CARTESIAN_POINT ( 'NONE',  ( 1.517799938645987057, -1.219565478727736574, -1.820545776841306029 ) ) ;
#200894=CARTESIAN_POINT ( 'NONE',  ( 6.246048974015395494, 0.5531718476652900396, 1.650163303580793217 ) ) ;
#200896=CARTESIAN_POINT ( 'NONE',  ( 0.2335667940002632559, 2.006215057630795773, -2.568298294197084886 ) ) ;
#200897=CARTESIAN_POINT ( 'NONE',  ( 0.6973489402126078485, -0.6253137818992074992, 1.607738891190332753 ) ) ;
#200898=CARTESIAN_POINT ( 'NONE',  ( 0.4921457485732755321, 2.200376924867069484, 0.6639341530902067579 ) ) ;
#200899=CARTESIAN_POINT ( 'NONE',  ( 0.6268464039562298140, 0.1668571106153530770, 2.185281662807083691 ) ) ;
#200900=CARTESIAN_POINT ( 'NONE',  ( 2.702037527177497012, -0.6914408288211832954, 2.095836555436859872 ) ) ;
#200901=CARTESIAN_POINT ( 'NONE',  ( 6.672352044927558623, -1.017530931492259816, -1.917974758356699505 ) ) ;
#200903=CARTESIAN_POINT ( 'NONE',  ( 0.8841682305550628840, -2.117513412274423690, 0.006320426156874307463 ) ) ;
#200904=CARTESIAN_POINT ( 'NONE',  ( 6.727182134110237577, 2.938513203633616566, 2.740843696613648017 ) ) ;
#200905=CARTESIAN_POINT ( 'NONE',  ( 5.262690832784179484, -1.395389315813623909, 1.328347855495640273 ) ) ;
#200907=CARTESIAN_POINT ( 'NONE',  ( 1.171857018789014271, 1.370485515009724820, 1.837452469633732210 ) ) ;
#200912=CARTESIAN_POINT ( 'NONE',  ( 3.844553043330910747, 1.187701353711614338, -1.876932147738763268 ) ) ;
#200919=CARTESIAN_POINT ( 'NONE',  ( 1.916638904718031000, -1.319229391439219246, -1.525043083973671498 ) ) ;
#200921=CARTESIAN_POINT ( 'NONE',  ( 0.6552251538811122433, 1.716912266053271408, -1.142698840430116602 ) ) ;
#200926=CARTESIAN_POINT ( 'NONE',  ( 4.242245924764226572, 0.5834501570099770440, 2.112278566661344392 ) ) ;
#200927=CARTESIAN_POINT ( 'NONE',  ( 0.9850002542920628379, -2.016597020373378513, 0.002813405579435435122 ) ) ;
#200928=CARTESIAN_POINT ( 'NONE',  ( 0.7668492355173107677, 1.774547462407764842, -0.4907661837717376407 ) ) ;
#200929=CARTESIAN_POINT ( 'NONE',  ( 5.161814014510654580, 1.128026202373041853, 1.995582457067740068 ) ) ;
#200930=CARTESIAN_POINT ( 'NONE',  ( 3.011469152984513009, -0.9080073089506625061, -1.601583425259824001 ) ) ;
#200933=CARTESIAN_POINT ( 'NONE',  ( 4.190329584092522097, -1.805708503706305423, -0.2678305112727846771 ) ) ;
#200934=CARTESIAN_POINT ( 'NONE',  ( 4.623672751230786027, 0.3474658942751900903, 1.986100912583692812 ) ) ;
#200936=CARTESIAN_POINT ( 'NONE',  ( 4.241306175801488720, -1.970289653591940970, 1.112044505652502346 ) ) ;
#200938=CARTESIAN_POINT ( 'NONE',  ( 6.651405291617982662, -1.688965747674558759, -1.257743519153362355 ) ) ;
#200940=CARTESIAN_POINT ( 'NONE',  ( 3.719242722441223226, -1.824546119899137731, -0.9785211796824041519 ) ) ;
#200945=CARTESIAN_POINT ( 'NONE',  ( 1.594233254470639238, -1.917152233794093164, -0.1895178900164773139 ) ) ;
#200947=CARTESIAN_POINT ( 'NONE',  ( 6.543809977506837683, 1.355650292293397507, 1.428865145875155340 ) ) ;
#200952=CARTESIAN_POINT ( 'NONE',  ( 2.092296997076743548, 1.370790743785160970, 1.747926019109148799 ) ) ;
#200953=CARTESIAN_POINT ( 'NONE',  ( 3.452270085047473458, 2.106147100029008179, 0.001788861226008006461 ) ) ;
#200957=CARTESIAN_POINT ( 'NONE',  ( 1.011883965753940018, 1.859189825682316277, -0.08597224477241424689 ) ) ;
#200963=CARTESIAN_POINT ( 'NONE',  ( 0.8793290508635929204, -1.919567575575848339, -0.9014759086384205311 ) ) ;
#200966=CARTESIAN_POINT ( 'NONE',  ( 4.914483161888778540, 0.7490505147796695518, 1.813437088826752142 ) ) ;
#200967=CARTESIAN_POINT ( 'NONE',  ( 3.766626874709140704, -1.453462046928340579, 1.600284095077113333 ) ) ;
#200968=CARTESIAN_POINT ( 'NONE',  ( 1.505144418776669601, -1.827259764946763454, 0.2261131901925839127 ) ) ;
#200971=CARTESIAN_POINT ( 'NONE',  ( 5.068161541800582093, -1.640353732806285825, -0.5817517365288951137 ) ) ;
#200976=CARTESIAN_POINT ( 'NONE',  ( 1.534274790466340299, 1.065227450066742687, -1.880959520452238465 ) ) ;
#200977=CARTESIAN_POINT ( 'NONE',  ( 2.987657498945671897, 1.897406709466815444, 0.6818930838706839248 ) ) ;
#200979=CARTESIAN_POINT ( 'NONE',  ( 1.569428280142046717, 0.1587979871724466974, -2.155937297210829495 ) ) ;
#200980=CARTESIAN_POINT ( 'NONE',  ( 3.028153684870387607, 1.096474020163393792, -1.638230769948149534 ) ) ;
#200981=CARTESIAN_POINT ( 'NONE',  ( 6.509000000000047415, 2.458121647476101401, 2.283885694139938138 ) ) ;
#200982=CARTESIAN_POINT ( 'NONE',  ( 3.509261751715045730, -1.912814363422868480, 0.3349611914155846693 ) ) ;
#200988=CARTESIAN_POINT ( 'NONE',  ( -0.1108833634137010582, 5.723767666350643601, -2.491012016648496363 ) ) ;
#200994=CARTESIAN_POINT ( 'NONE',  ( 6.721674876502457430, -2.240710703332372766, 0.5512419492274822641 ) ) ;
#200996=CARTESIAN_POINT ( 'NONE',  ( 4.065250617491710905, 1.680331827152386159, 1.012218702928203706 ) ) ;
#200998=CARTESIAN_POINT ( 'NONE',  ( 2.092422861153935276, -0.4390285686692517175, 1.967888031366466395 ) ) ;
#200999=ORIENTED_EDGE ( 'NONE', *, *, #34638, .F. ) ;
#201000=CARTESIAN_POINT ( 'NONE',  ( 3.186815374238487930, 1.666415522689016049, -1.306070977860743110 ) ) ;
#201002=CARTESIAN_POINT ( 'NONE',  ( 0.07459516483346650961, 6.948550711820903558, -2.350542341214032493 ) ) ;
#201004=CARTESIAN_POINT ( 'NONE',  ( 2.958754162918545205, 0.2696264243384552950, -1.821159755858774654 ) ) ;
#201008=CARTESIAN_POINT ( 'NONE',  ( 3.937823072884456099, -2.028283017459261650, 0.6187693826033290323 ) ) ;
#201011=CARTESIAN_POINT ( 'NONE',  ( 5.202442474109128412, -0.6904536177961515531, -1.941828258638809368 ) ) ;
#201012=CARTESIAN_POINT ( 'NONE',  ( 1.205250485101029723, -1.463924481597483007, -1.148973905474151014 ) ) ;
#201013=CARTESIAN_POINT ( 'NONE',  ( 2.542321706073047416, -1.529623444112483632, 1.024600984555257277 ) ) ;
#201020=CARTESIAN_POINT ( 'NONE',  ( 1.963769682107346037, 0.3752889857368995608, -2.174583152744386627 ) ) ;
#201021=CARTESIAN_POINT ( 'NONE',  ( 4.991644252507740021, 1.671830779756987573, 1.524457814443666903 ) ) ;
#201024=CARTESIAN_POINT ( 'NONE',  ( 4.552869461240817373, 0.3164949366275445208, 1.783561479213832346 ) ) ;
#201025=CARTESIAN_POINT ( 'NONE',  ( 4.294081978838642399, -0.8244651323695743050, -1.729401801750865442 ) ) ;
#201028=CARTESIAN_POINT ( 'NONE',  ( 4.030118584743531684, 1.055711351780568741, -1.664808796107832389 ) ) ;
#201029=CARTESIAN_POINT ( 'NONE',  ( 5.155093292349416600, -1.580716073637401076, -1.000049079914612449 ) ) ;
#201030=CARTESIAN_POINT ( 'NONE',  ( 5.072628826387419743, 1.283713728693743894, -1.347665127999774448 ) ) ;
#201032=CARTESIAN_POINT ( 'NONE',  ( 0.02267320670834571672, 0.3494893071277604402, 1.985867805234131644 ) ) ;
#201034=CARTESIAN_POINT ( 'NONE',  ( 1.594499780405156830, -2.096077427685174577, -0.2048490792218547185 ) ) ;
#201038=CARTESIAN_POINT ( 'NONE',  ( 3.375340920106313813, -1.871962376360849056, -0.9962781187466958066 ) ) ;
#201040=CARTESIAN_POINT ( 'NONE',  ( 1.582292005822239167, 1.041880795974026608, 1.730197787189115433 ) ) ;
#201045=CARTESIAN_POINT ( 'NONE',  ( 2.636181727411972098, 1.021492356387411427, -1.905029093917938399 ) ) ;
#201046=CARTESIAN_POINT ( 'NONE',  ( 6.890000000000005898, 2.048573291599069091, 2.305811639209849773 ) ) ;
#201054=CARTESIAN_POINT ( 'NONE',  ( 0.5038066827526345159, -2.180447833630628107, 0.2205874978757973448 ) ) ;
#201056=CARTESIAN_POINT ( 'NONE',  ( 1.393865445735403830, 1.714438158727617179, 1.476448846179352348 ) ) ;
#201063=CARTESIAN_POINT ( 'NONE',  ( 3.668305164303451882, -1.157086425697685828, 1.279375231203205621 ) ) ;
#201065=CARTESIAN_POINT ( 'NONE',  ( 2.371989033382770895, -1.092842237840240482, 1.391882982410238556 ) ) ;
#201066=CARTESIAN_POINT ( 'NONE',  ( 2.912746486309669258, -0.5863433081114779455, -1.925794048158388394 ) ) ;
#201068=CARTESIAN_POINT ( 'NONE',  ( 4.876106637443972325, 1.267215935518750669, 1.806476597341267087 ) ) ;
#201070=CARTESIAN_POINT ( 'NONE',  ( 4.148698013468838930, 1.981613772426650266, 0.3898967627796907642 ) ) ;
#201072=CARTESIAN_POINT ( 'NONE',  ( 4.183220377109976518, 1.621195451842275315, 1.198844725951081047 ) ) ;
#201073=CARTESIAN_POINT ( 'NONE',  ( 4.412255891540381114, -1.811360455869342578, -0.03765339742955660374 ) ) ;
#201075=CARTESIAN_POINT ( 'NONE',  ( 2.975316878787794828, 1.776827963633962559, -0.5852370025475408521 ) ) ;
#201078=CARTESIAN_POINT ( 'NONE',  ( 1.511816067030671729, -0.6413169068853613597, 1.801808535584384252 ) ) ;
#201083=CARTESIAN_POINT ( 'NONE',  ( -0.2049973002360427898, -0.1418364932926942379, -1.881151990943498387 ) ) ;
#201085=CARTESIAN_POINT ( 'NONE',  ( 1.223018651738450480, -1.772137153356953432, -0.8420139538000551704 ) ) ;
#201086=CARTESIAN_POINT ( 'NONE',  ( 0.1458495181914116201, -0.1430550213798176262, -1.983920851313693223 ) ) ;
#201088=CARTESIAN_POINT ( 'NONE',  ( 5.203433420164765622, 1.869144303625443371, -1.001675624404389620 ) ) ;
#201091=CARTESIAN_POINT ( 'NONE',  ( 6.063742386902314152, 1.942598920255795392, -0.3345802184639041776 ) ) ;
#201093=CARTESIAN_POINT ( 'NONE',  ( 0.2990880961862537601, -0.2507095357664780866, -1.997497332983847906 ) ) ;
#201095=CARTESIAN_POINT ( 'NONE',  ( 1.652128961607162827, 1.091750937195800519, 1.813926670343589898 ) ) ;
#201097=CARTESIAN_POINT ( 'NONE',  ( 2.787621587699981696, -1.932700977737045633, 0.7428295258242522126 ) ) ;
#201102=CARTESIAN_POINT ( 'NONE',  ( 4.910148475136437263, 1.442109633637311372, -1.513870239069979196 ) ) ;
#201104=CARTESIAN_POINT ( 'NONE',  ( 3.469579810302122702, 1.781292651720441711, -0.3989491859636914994 ) ) ;
#201105=CARTESIAN_POINT ( 'NONE',  ( 1.857782056280156580, 0.6927856907082428073, -1.673962145341382435 ) ) ;
#201107=CARTESIAN_POINT ( 'NONE',  ( 6.147136880733683917, -1.866598994669690148, 1.177069016086537356 ) ) ;
#201110=CARTESIAN_POINT ( 'NONE',  ( 5.491335294905154818, 1.948586811899848614, -1.035780281143129811 ) ) ;
#201112=ORIENTED_EDGE ( 'NONE', *, *, #30212, .F. ) ;
#201113=CARTESIAN_POINT ( 'NONE',  ( 3.932203299393256302, -0.9856607118853939475, -1.638553295466014248 ) ) ;
#201116=CARTESIAN_POINT ( 'NONE',  ( 6.848098043024292814, -0.8888149443028300345, 1.868052569137634400 ) ) ;
#201126=CARTESIAN_POINT ( 'NONE',  ( 4.165207536865437099, 0.2314014899743311315, -1.856129391651973215 ) ) ;
#201132=CARTESIAN_POINT ( 'NONE',  ( 6.702015291077846548, 0.7979701500827086624, -1.910492173269620508 ) ) ;
#201133=CARTESIAN_POINT ( 'NONE',  ( 1.071888921174158016, -0.9040910708146729924, 1.802427947461216373 ) ) ;
#201136=DIRECTION ( 'NONE',  ( 2.949029909160572061E-17, 1.000000000000000000, -8.673600428462616880E-15 ) ) ;
#201137=CARTESIAN_POINT ( 'NONE',  ( 1.429895766826321690, 1.077743243251317429, -1.908043295719801025 ) ) ;
#201138=CARTESIAN_POINT ( 'NONE',  ( 6.463509179248936753, 0.3066564278407272193, -1.799597105106438777 ) ) ;
#201146=CARTESIAN_POINT ( 'NONE',  ( 3.948646536499214932, -1.533023199436277961, -1.019512891124202403 ) ) ;
#201147=CARTESIAN_POINT ( 'NONE',  ( 0.8385398129025347647, 1.197303422201956957, -1.618206657969661011 ) ) ;
#201148=CARTESIAN_POINT ( 'NONE',  ( 2.548584303619909175, 2.101849941811538169, -0.9302779420137051725 ) ) ;
#201150=CARTESIAN_POINT ( 'NONE',  ( 1.287708147089029032, -1.175244795098003614, -1.442924398407473108 ) ) ;
#201153=CARTESIAN_POINT ( 'NONE',  ( 4.271672842113056312, 0.4137096367802223784, -1.866957553337177611 ) ) ;
#201157=CARTESIAN_POINT ( 'NONE',  ( 3.298458272841266137, 1.646618950329106434, -1.288217307904614639 ) ) ;
#201158=CARTESIAN_POINT ( 'NONE',  ( 1.762360912074714125, -1.325010844092512796, 1.320751239342173200 ) ) ;
#201161=CARTESIAN_POINT ( 'NONE',  ( 3.720004753662985664, 1.653986544816415494, 0.5419736716202552262 ) ) ;
#201165=CARTESIAN_POINT ( 'NONE',  ( 4.301177763854931335, 1.387281528384849860, 1.024788870506128990 ) ) ;
#201167=CARTESIAN_POINT ( 'NONE',  ( 3.913774547416096095, -1.127657808996849198, -1.879056921112078893 ) ) ;
#201168=CARTESIAN_POINT ( 'NONE',  ( 6.358075476802443227, 2.201304964888863402, -0.1578768562689457922 ) ) ;
#201169=AXIS2_PLACEMENT_3D ( 'NONE', #43328, #9729, #111572 ) ;
#201171=CARTESIAN_POINT ( 'NONE',  ( 3.555704413576792788, 1.708454066091537493, 1.339533783212579099 ) ) ;
#201172=CARTESIAN_POINT ( 'NONE',  ( 2.560947663861262491, -1.588335953301520220, -0.9000364273514869229 ) ) ;
#201174=CARTESIAN_POINT ( 'NONE',  ( 4.399685268140280492, -2.075804279169701339, 0.4165508703993703876 ) ) ;
#201177=CARTESIAN_POINT ( 'NONE',  ( 4.370831947049586219, 0.0005328150827835219676, -2.292545470631628390 ) ) ;
#201179=CARTESIAN_POINT ( 'NONE',  ( 6.720655732516679137, 4.703287744343486843, 2.289001594030832365 ) ) ;
#201181=CARTESIAN_POINT ( 'NONE',  ( 0.9793288802587530872, -1.918618388578940737, -0.9032494106611321794 ) ) ;
#201188=CARTESIAN_POINT ( 'NONE',  ( 5.871720251644387822, -0.2986239867289949834, -1.994071864161291119 ) ) ;
#201190=CARTESIAN_POINT ( 'NONE',  ( 4.627816428071820809, 2.001945081875619259, -0.4960309448565465851 ) ) ;
#201195=CARTESIAN_POINT ( 'NONE',  ( 0.1331565106231571705, 6.948071080078889850, -2.540993614958915181 ) ) ;
#201196=CARTESIAN_POINT ( 'NONE',  ( 0.3223637989299525941, 2.001183132641819906, 0.6049928108779398794 ) ) ;
#201197=CARTESIAN_POINT ( 'NONE',  ( 4.904922738988922504, -1.081064280317966420, -1.701948707654332704 ) ) ;
#201198=CARTESIAN_POINT ( 'NONE',  ( 4.229911503591711863, 1.806553461410321582, 0.3548724298726435022 ) ) ;
#201201=CARTESIAN_POINT ( 'NONE',  ( 1.271983708484729636, -1.098657341177114999, 1.329575768613028286 ) ) ;
#201202=CARTESIAN_POINT ( 'NONE',  ( 0.3215004009857677092, -1.429452135790244549, -1.422604240635255479 ) ) ;
#201204=CARTESIAN_POINT ( 'NONE',  ( 1.337049673779285852, 0.6609975811289883207, -2.201632501652720286 ) ) ;
#201206=CARTESIAN_POINT ( 'NONE',  ( 1.564152511173346749, 2.229009205740081434, -0.3863987453041685116 ) ) ;
#201207=CARTESIAN_POINT ( 'NONE',  ( 3.106188079018203041, -2.103647721026543405, 0.1036251941764678303 ) ) ;
#201212=SURFACE_SIDE_STYLE ('',( #153563 ) ) ;
#201217=CARTESIAN_POINT ( 'NONE',  ( 4.922253396635227318, -2.210645704158546554, 0.2187456033138199529 ) ) ;
#201218=CARTESIAN_POINT ( 'NONE',  ( 2.203317661949526052, -0.4785072280911427667, 2.138412878249687399 ) ) ;
#201221=CARTESIAN_POINT ( 'NONE',  ( 5.494571831323358246, 1.932540981948445147, 0.3370517209014682325 ) ) ;
#201225=CARTESIAN_POINT ( 'NONE',  ( 4.271814301144261528, 0.4616217191124799002, -2.069597271375968273 ) ) ;
#201229=CARTESIAN_POINT ( 'NONE',  ( 6.491117449447131982, 1.883434485765375310, -1.060826435891427666 ) ) ;
#201231=CARTESIAN_POINT ( 'NONE',  ( 5.442854017605395889, -1.455216020186438364, -1.127989967910733693 ) ) ;
#201233=CARTESIAN_POINT ( 'NONE',  ( 1.557743604271996762, -1.230989698698783608, 1.230628217043183925 ) ) ;
#201237=CARTESIAN_POINT ( 'NONE',  ( 5.295850518597075229, -0.7817450549502875656, 2.015575934489414411 ) ) ;
#201241=CARTESIAN_POINT ( 'NONE',  ( 4.909125497034264818, 1.879091090907711425, 1.068517025386829467 ) ) ;
#201243=CARTESIAN_POINT ( 'NONE',  ( 5.219980872528355853, -1.052265754357907701, -1.666845346888909729 ) ) ;
#201244=CARTESIAN_POINT ( 'NONE',  ( 3.549848462767680068, 1.568450346167485243, -0.7392937452721718428 ) ) ;
#201245=CARTESIAN_POINT ( 'NONE',  ( 1.031118135130421498, -1.979082047791239418, 0.9416876394413642437 ) ) ;
#201246=CARTESIAN_POINT ( 'NONE',  ( 2.626355190031507192, -1.328241637659173247, -1.886819894403545028 ) ) ;
#201247=CARTESIAN_POINT ( 'NONE',  ( 4.393860645892766037, -0.7923225987812362314, 1.902584447174461291 ) ) ;
#201248=CARTESIAN_POINT ( 'NONE',  ( 6.304245038521663957, 1.436082020041820506, -1.307557180447990186 ) ) ;
#201253=CARTESIAN_POINT ( 'NONE',  ( 0.9498425221252141393, -1.824119990893595888, -0.8596288560165299408 ) ) ;
#201255=CARTESIAN_POINT ( 'NONE',  ( 3.223846859376262142, -2.127229092858519799, 0.5869343725257711863 ) ) ;
#201257=CARTESIAN_POINT ( 'NONE',  ( 6.948121807170864805, -0.8414398651286276731, 1.770450887113049099 ) ) ;
#201262=CARTESIAN_POINT ( 'NONE',  ( 6.825078400183551608, 1.261667030487168439, 2.159888225955305163 ) ) ;
#201263=CARTESIAN_POINT ( 'NONE',  ( 6.052668933152094866, -1.581501214056714177, -0.9424504099920794076 ) ) ;
#201265=CARTESIAN_POINT ( 'NONE',  ( 3.151298293300933029, -1.683901109147158737, -1.187873040408020886 ) ) ;
#201269=CARTESIAN_POINT ( 'NONE',  ( 1.787766293494430725, 1.931992495155916867, -0.5885693585916639270 ) ) ;
#201272=CARTESIAN_POINT ( 'NONE',  ( 2.096624111547572777, -0.5486670241920866831, -1.986447216630163659 ) ) ;
#201278=CARTESIAN_POINT ( 'NONE',  ( 5.197975494389605267, -0.7968864405506062010, 2.058166701804148957 ) ) ;
#201279=CARTESIAN_POINT ( 'NONE',  ( 1.247603677004164746, -1.703183937513498281, -1.330886036463780009 ) ) ;
#201281=CARTESIAN_POINT ( 'NONE',  ( 0.4621254960020632074, -1.116205757145168231, 1.679226196708947239 ) ) ;
#201286=CARTESIAN_POINT ( 'NONE',  ( 1.656895194024514906, -1.602792776363659133, -0.9643473572949823325 ) ) ;
#201287=CARTESIAN_POINT ( 'NONE',  ( 4.048064755690682581, 0.9548552675892291175, 1.776167154503265566 ) ) ;
#201291=CARTESIAN_POINT ( 'NONE',  ( 5.004563900840214963, -0.7087877200973876635, -1.983347251131000855 ) ) ;
#201295=CARTESIAN_POINT ( 'NONE',  ( 5.291273337336410698, -0.05367003302336400411, -2.019259759236047280 ) ) ;
#201297=CARTESIAN_POINT ( 'NONE',  ( 1.200133799977639137, 0.8395725688425963451, -1.884152621438263342 ) ) ;
#201305=CARTESIAN_POINT ( 'NONE',  ( 3.297511149327167601, -1.916070068265750992, 1.021083071776592410 ) ) ;
#201308=CARTESIAN_POINT ( 'NONE',  ( 1.768857366986800184, 1.761637791510446860, -0.5354853023365884201 ) ) ;
#201310=CARTESIAN_POINT ( 'NONE',  ( 4.810206850810132551, 1.511280187219691928, -1.587364365194674498 ) ) ;
#201312=CARTESIAN_POINT ( 'NONE',  ( 4.592800228568824750, -0.4914316458759260264, -2.208360408168393629 ) ) ;
#201319=CARTESIAN_POINT ( 'NONE',  ( 5.553870903591159092, 1.767663364219349553, -0.08767779694792036949 ) ) ;
#201322=CARTESIAN_POINT ( 'NONE',  ( 2.204260208318520764, -2.105514897310766020, 0.05069945311739902649 ) ) ;
#201326=CARTESIAN_POINT ( 'NONE',  ( 1.644903635585378554, -0.2856866470503526823, -1.948579891484893079 ) ) ;
#201327=CARTESIAN_POINT ( 'NONE',  ( 0.4439547499465161251, 1.865322535695708606, 0.1421067652795371117 ) ) ;
#201328=CARTESIAN_POINT ( 'NONE',  ( 1.170277241841523264, -0.8789641444944886750, -1.754005360843587047 ) ) ;
#201329=CARTESIAN_POINT ( 'NONE',  ( 6.187769672300552415, 1.730736780639136496, -0.5351268960485565662 ) ) ;
#201333=CARTESIAN_POINT ( 'NONE',  ( 5.858239598252557023, 0.7595784280203802252, 1.709674162104061423 ) ) ;
#201336=CARTESIAN_POINT ( 'NONE',  ( 5.524307029080701703, 1.015476208609331188, 1.803995072556117352 ) ) ;
#201339=CARTESIAN_POINT ( 'NONE',  ( 0.2915762745691782287, -1.893489616766583339, 0.8377075429084477332 ) ) ;
#201346=CARTESIAN_POINT ( 'NONE',  ( 5.283633159863808437, -1.863482887291990409, 0.6137318589548645953 ) ) ;
#201348=CARTESIAN_POINT ( 'NONE',  ( 3.040388574052850235, 1.915307028720541371, -0.6297779509270851062 ) ) ;
#201349=CARTESIAN_POINT ( 'NONE',  ( 2.501083532561697798, -0.1830384092258540707, 1.906917772027187929 ) ) ;
#201351=CARTESIAN_POINT ( 'NONE',  ( 0.3104468679729632807, 1.506874830639578056, -1.591553791636945991 ) ) ;
#201352=CARTESIAN_POINT ( 'NONE',  ( 0.2333690889706820926, 2.873202992247088083, -2.541887414127189881 ) ) ;
#201353=CARTESIAN_POINT ( 'NONE',  ( 2.706148147531197701, -0.7121320899835179574, -1.729884524348634933 ) ) ;
#201355=CARTESIAN_POINT ( 'NONE',  ( 4.535406599088565471, -0.09463749723611977749, 2.011077795214308406 ) ) ;
#201358=CARTESIAN_POINT ( 'NONE',  ( 4.903976463145187203, -1.133744943205544642, -1.787932202283550875 ) ) ;
#201360=CARTESIAN_POINT ( 'NONE',  ( 6.232888004217203459, -1.964670499678453197, -0.6532144590316590893 ) ) ;
#201361=CARTESIAN_POINT ( 'NONE',  ( 1.610996488345920907, -0.2524672473064055733, 2.075362222853482930 ) ) ;
#201362=CARTESIAN_POINT ( 'NONE',  ( 6.720655732516655156, 7.629137130509086262, 2.873739711112702544 ) ) ;
#201363=CARTESIAN_POINT ( 'NONE',  ( 6.563509198815889789, 0.3086105522638156184, -1.799150958419073909 ) ) ;
#201373=CARTESIAN_POINT ( 'NONE',  ( 0.6624192275643402406, 0.5246805835648783445, 1.733790746550630146 ) ) ;
#201381=CARTESIAN_POINT ( 'NONE',  ( 5.659779856126235131, 1.203369751103126717, 1.617807692209995984 ) ) ;
#201382=CARTESIAN_POINT ( 'NONE',  ( -0.07530339154229391541, -0.9103892951793614019, -1.913193754492636067 ) ) ;
#201386=CARTESIAN_POINT ( 'NONE',  ( -0.1399997263889819765, 0.7174702203470960660, -2.082715917450683740 ) ) ;
#201390=CARTESIAN_POINT ( 'NONE',  ( 3.133609412646401360, 1.871568317120005265, -0.6134489921753321084 ) ) ;
#201391=CARTESIAN_POINT ( 'NONE',  ( 4.429314653828757109, -1.560513098751922900, -1.277029310785951388 ) ) ;
#201395=CARTESIAN_POINT ( 'NONE',  ( 4.576244502665470115, -2.125281509430646754, -0.5339713055512520512 ) ) ;
#201397=CARTESIAN_POINT ( 'NONE',  ( 2.643477790179576292, -1.426271481392614948, -1.295054687222449541 ) ) ;
#201399=CARTESIAN_POINT ( 'NONE',  ( -0.1296875068447882473, 5.724785194352729256, -2.420566058096422779 ) ) ;
#201404=CARTESIAN_POINT ( 'NONE',  ( 5.471530992243406999, -0.2926990004611991214, 1.947462276923512370 ) ) ;
#201405=CARTESIAN_POINT ( 'NONE',  ( 0.2748124788713289246, 1.811699325429259488, -0.6999492020843509632 ) ) ;
#201406=CARTESIAN_POINT ( 'NONE',  ( 3.932292794061467589, -1.036904606752734326, -1.725386108540658103 ) ) ;
#201407=CARTESIAN_POINT ( 'NONE',  ( 5.958471553546731414, 1.734833135700924345, 1.507719323494296937 ) ) ;
#201409=CARTESIAN_POINT ( 'NONE',  ( 4.047575586610673071, 1.345269348194571668, 1.286062638920927537 ) ) ;
#201415=CARTESIAN_POINT ( 'NONE',  ( 0.5740950506661415265, -1.212703583203307511, 1.825263377225619266 ) ) ;
#201420=CARTESIAN_POINT ( 'NONE',  ( 0.5217476098421744979, -0.9739702522407606144, -1.544006022310390192 ) ) ;
#201422=CARTESIAN_POINT ( 'NONE',  ( 3.076526641549358398, -0.6997103666757237272, 1.586905598789583482 ) ) ;
#201424=CARTESIAN_POINT ( 'NONE',  ( 6.509000000000011887, 3.696273625755361447, 2.514342382328867753 ) ) ;
#201426=CARTESIAN_POINT ( 'NONE',  ( 5.145057536039753465, -1.563975785779356587, 0.9416349707431559413 ) ) ;
#201427=CARTESIAN_POINT ( 'NONE',  ( 3.221486639279776298, 0.2924833653642990861, -1.939731193138781951 ) ) ;
#201431=CARTESIAN_POINT ( 'NONE',  ( 5.320985837513584116, 1.605487267134264595, -1.385306402853322405 ) ) ;
#201434=CARTESIAN_POINT ( 'NONE',  ( 2.729418486472269922, 0.1060373921930452268, -2.067687848736274869 ) ) ;
#201437=CARTESIAN_POINT ( 'NONE',  ( 4.776165916792348476, 2.197254790419100434, -0.3252806346676767046 ) ) ;
#201439=CARTESIAN_POINT ( 'NONE',  ( 3.340769233699531604, 0.5564940052410914939, -2.230230389815818892 ) ) ;
#201446=CARTESIAN_POINT ( 'NONE',  ( 3.199369407753744454, 1.726971514772487559, -0.8218122705464236954 ) ) ;
#201448=CARTESIAN_POINT ( 'NONE',  ( 4.612129873793564094, -0.7390372460917455921, -1.558541145072767975 ) ) ;
#201449=CARTESIAN_POINT ( 'NONE',  ( 2.905482715143858030, -1.942096844255640109, 0.5424705965835219246 ) ) ;
#201450=CARTESIAN_POINT ( 'NONE',  ( 3.955939753277417648, -2.145046849925678956, -0.8267234532119535073 ) ) ;
#201452=CARTESIAN_POINT ( 'NONE',  ( 6.041652760897754604, -1.524265013729691143, -1.453574456173498231 ) ) ;
#201455=CARTESIAN_POINT ( 'NONE',  ( 4.551851636600127371, 1.769384361346277856, -0.04241240985469392488 ) ) ;
#201457=CARTESIAN_POINT ( 'NONE',  ( 0.5336625369133874974, -1.625122730996070297, -1.616870241932764074 ) ) ;
#201458=CARTESIAN_POINT ( 'NONE',  ( 0.1810874682179625661, -0.8250252819957092365, 1.532327275369157915 ) ) ;
#201460=CARTESIAN_POINT ( 'NONE',  ( 6.439412520197737244, 0.8424478218750917069, -2.023249321508275855 ) ) ;
#201464=CARTESIAN_POINT ( 'NONE',  ( 0.7312207505087648940, -2.044463659613379392, -0.7311735514200778940 ) ) ;
#201465=CARTESIAN_POINT ( 'NONE',  ( 0.9543149826918421175, -1.275552737861269437, 1.561884623745241951 ) ) ;
#201468=CARTESIAN_POINT ( 'NONE',  ( 4.899011302651929078, 1.600714092801895472, -1.071686876026227475 ) ) ;
#201470=CARTESIAN_POINT ( 'NONE',  ( 0.8268048150999330881, -1.005496690709275720, -1.980927387359689318 ) ) ;
#201480=CARTESIAN_POINT ( 'NONE',  ( 4.651753270297207976, 0.6719488171132372845, 1.605710474869048499 ) ) ;
#201481=CARTESIAN_POINT ( 'NONE',  ( 1.908577322519442454, 0.6123880975643314351, 1.863924812142327747 ) ) ;
#201485=CARTESIAN_POINT ( 'NONE',  ( 6.531700620877029628, 1.877769495358465157, -0.5682946464737671510 ) ) ;
#201488=CARTESIAN_POINT ( 'NONE',  ( 1.288340396327339432, -1.015645312862264227, 2.021827887327799722 ) ) ;
#201492=CARTESIAN_POINT ( 'NONE',  ( 1.387741975113141235, -0.8460221195879283895, 1.668388151239764028 ) ) ;
#201493=CARTESIAN_POINT ( 'NONE',  ( 0.3165338080420940781, 0.8936020571472038654, -1.485981903106075031 ) ) ;
#201494=CARTESIAN_POINT ( 'NONE',  ( 3.931328349035985603, -1.512150646884598215, -1.586510368271301541 ) ) ;
#201495=CARTESIAN_POINT ( 'NONE',  ( 5.051972272063284031, 0.7293918257267332228, -2.189345848185173082 ) ) ;
#201497=CARTESIAN_POINT ( 'NONE',  ( 1.077108160694364214, -0.04970969036830223675, -2.060456431261459276 ) ) ;
#201498=CARTESIAN_POINT ( 'NONE',  ( 3.468632250064273670, 0.04687378517908299957, -1.941542025766171298 ) ) ;
#201500=CARTESIAN_POINT ( 'NONE',  ( 5.413307058180727438, -0.2754873708227522644, 1.850039175317084617 ) ) ;
#201502=CARTESIAN_POINT ( 'NONE',  ( 0.1745346383498986020, -0.7352478164647980874, -1.569626033853884106 ) ) ;
#201505=CARTESIAN_POINT ( 'NONE',  ( 5.080704010962952211, -0.7231418808758652839, 1.882473355234378865 ) ) ;
#201508=CARTESIAN_POINT ( 'NONE',  ( 1.664397423953474009, -1.292156093668932693, 1.290017532847971271 ) ) ;
#201518=CARTESIAN_POINT ( 'NONE',  ( 5.742833863956755103, 1.946992082993486584, 0.5367204025522700483 ) ) ;
#201519=CARTESIAN_POINT ( 'NONE',  ( 0.1531979293848736434, 0.3668625560977051281, 2.088361607889513305 ) ) ;
#201523=CARTESIAN_POINT ( 'NONE',  ( 5.172756020173422620, -1.939746602593624081, -0.6965250322775017322 ) ) ;
#201524=CARTESIAN_POINT ( 'NONE',  ( 4.641250102003462885, 0.7743139518727222281, 1.862017545363145343 ) ) ;
#201532=CARTESIAN_POINT ( 'NONE',  ( 5.044295983762377311, 1.882185518538554314, -0.7230303062365079914 ) ) ;
#201533=CARTESIAN_POINT ( 'NONE',  ( 3.767381502543519112, 1.024135474229198151, 1.529801857347697025 ) ) ;
#201535=CARTESIAN_POINT ( 'NONE',  ( 2.719673384174253972, -0.2251885735481904405, 2.296679687964820360 ) ) ;
#201537=CARTESIAN_POINT ( 'NONE',  ( 4.411504763889100289, -0.3743020017868466387, 2.128795073437335095 ) ) ;
#201539=CARTESIAN_POINT ( 'NONE',  ( -0.04160512940111232155, -1.735061556407999417, -0.8725848562033207134 ) ) ;
#201541=CARTESIAN_POINT ( 'NONE',  ( 3.972236164830291738, 1.968842830503451991, 1.185689330230592642 ) ) ;
#201544=CARTESIAN_POINT ( 'NONE',  ( 3.924554409752772699, 1.776107677202539925, 0.5873546117282567591 ) ) ;
#201547=CARTESIAN_POINT ( 'NONE',  ( 0.2804619692761011751, -1.911105013696552168, -0.4832259537779006742 ) ) ;
#201550=CARTESIAN_POINT ( 'NONE',  ( 1.436444770134176485, 1.085300811998829662, -1.921501399296850821 ) ) ;
#201556=CARTESIAN_POINT ( 'NONE',  ( 6.702032618711820433, -1.971027473680329045, 0.04818573739380492549 ) ) ;
#201557=CARTESIAN_POINT ( 'NONE',  ( 0.5523711044835468709, 0.7197940642212009577, -2.192503933474987843 ) ) ;
#201558=CARTESIAN_POINT ( 'NONE',  ( 0.3792546940144908563, -0.1001052471676349837, 1.959448305358338693 ) ) ;
#201559=CARTESIAN_POINT ( 'NONE',  ( 4.557522945366278222, 1.653560713460072051, 1.232637662666216549 ) ) ;
#201568=CARTESIAN_POINT ( 'NONE',  ( 6.443812750726708671, 1.492410320797844747, 1.577172898185905670 ) ) ;
#201570=CARTESIAN_POINT ( 'NONE',  ( 5.126429434416579056, 0.1410513515392505246, 1.835921608166577013 ) ) ;
#201578=CARTESIAN_POINT ( 'NONE',  ( 0.9438406676962156627, -1.213610516764839664, -1.477797202995428938 ) ) ;
#201579=CARTESIAN_POINT ( 'NONE',  ( 1.814973546968738027, -0.2204486908502552300, 1.755991699180702748 ) ) ;
#201580=CARTESIAN_POINT ( 'NONE',  ( 0.1352199593073095951, -0.09384731153385186819, 1.910084486482076294 ) ) ;
#201582=CARTESIAN_POINT ( 'NONE',  ( 4.886306726311728355, -0.6496138446146214607, -1.802220356481977204 ) ) ;
#201584=CARTESIAN_POINT ( 'NONE',  ( 5.775830853014204180, -1.921903692836058886, 0.4298591908668251138 ) ) ;
#201585=CARTESIAN_POINT ( 'NONE',  ( 0.2289750728588327566, 1.457791096766167360, -1.540313549178488284 ) ) ;
#201587=CARTESIAN_POINT ( 'NONE',  ( 4.399188623838041323, 1.502396186649012311, 1.114296746780506497 ) ) ;
#201588=CARTESIAN_POINT ( 'NONE',  ( 6.727182134110236689, 0.008744176509112643741, 1.710970312420513562 ) ) ;
#201590=CARTESIAN_POINT ( 'NONE',  ( 3.334799921508072806, 2.153101868192684343, 0.4835390122766567433 ) ) ;
#201593=CARTESIAN_POINT ( 'NONE',  ( 0.8716181059342765769, -0.3045769538833371648, 2.039966307373513033 ) ) ;
#201600=CARTESIAN_POINT ( 'NONE',  ( 3.104029480343179603, 0.7476448069429382226, -1.930825944200013966 ) ) ;
#201604=CARTESIAN_POINT ( 'NONE',  ( 0.7330764811492549438, 1.866981473359119237, 0.7708630573498123084 ) ) ;
#201606=CARTESIAN_POINT ( 'NONE',  ( 0.07479286986305369589, 4.095183424177953668, -2.410510762676120411 ) ) ;
#201608=CARTESIAN_POINT ( 'NONE',  ( 6.890000000000050306, -0.002781820520068867264, 1.999840353888074240 ) ) ;
#201609=CARTESIAN_POINT ( 'NONE',  ( 5.893738820153655134, -1.900388249151972353, 0.2415585323580979049 ) ) ;
#201610=CARTESIAN_POINT ( 'NONE',  ( 4.353197867323560288, 0.4795420089713005041, -2.138300074133951068 ) ) ;
#201613=CARTESIAN_POINT ( 'NONE',  ( 3.955252344019274169, -1.661368509396843995, 0.9470704235666274062 ) ) ;
#201617=CARTESIAN_POINT ( 'NONE',  ( 0.7203276360899166786, 1.987051886588153682, 0.3419113104980234241 ) ) ;
#201619=CARTESIAN_POINT ( 'NONE',  ( 6.216381822182693639, 2.044192415450503120, 0.7905562269360306704 ) ) ;
#201621=CARTESIAN_POINT ( 'NONE',  ( 3.504663807952506538, 1.359994529648723249, -1.060664293495124477 ) ) ;
#201623=CARTESIAN_POINT ( 'NONE',  ( -0.1399997263889611598, 2.874570648431204578, -2.488748559936367233 ) ) ;
#201627=CARTESIAN_POINT ( 'NONE',  ( 1.346068015636435522, -0.8851805579040676886, 1.750911360861057142 ) ) ;
#201630=CARTESIAN_POINT ( 'NONE',  ( 0.1755611466353446948, 4.081716065625639267, -2.798746370182193743 ) ) ;
#201631=EDGE_LOOP ( 'NONE', ( #111854, #32551, #186346, #76430 ) ) ;
#201634=CARTESIAN_POINT ( 'NONE',  ( 4.195841788199461853, 1.186545534222239962, 1.368844175430401933 ) ) ;
#201638=CARTESIAN_POINT ( 'NONE',  ( 5.232992382607310589, 1.676000702356477134, 0.6878641890804160219 ) ) ;
#201643=CARTESIAN_POINT ( 'NONE',  ( 4.703460533163725366, -1.437978410778781857, -1.181371033526560144 ) ) ;
#201645=CARTESIAN_POINT ( 'NONE',  ( 2.776846452629442297, 1.641606522343663555, -0.9870246354491112317 ) ) ;
#201651=CARTESIAN_POINT ( 'NONE',  ( 0.4093245661422850179, 1.881582470445356314, 1.064130679222355491 ) ) ;
#201654=CARTESIAN_POINT ( 'NONE',  ( 1.939510448661335484, 0.7990184383764920018, -1.932127011870365951 ) ) ;
#201656=CARTESIAN_POINT ( 'NONE',  ( 0.5162701059127188241, 1.262803565755654001, -1.318596375272471199 ) ) ;
#201658=CARTESIAN_POINT ( 'NONE',  ( 2.924607851032960504, 1.718362407962298111, 0.6167639819729957562 ) ) ;
#201660=CARTESIAN_POINT ( 'NONE',  ( 2.127084423382288314, 1.709874882824816478, 0.8565708355050825062 ) ) ;
#201661=CARTESIAN_POINT ( 'NONE',  ( 2.576555279139204568, 1.288776560207754551, -1.489423508990360023 ) ) ;
#201663=CARTESIAN_POINT ( 'NONE',  ( 3.649888709942475273, 0.7017510601828327310, 1.811005675494174350 ) ) ;
#201667=CARTESIAN_POINT ( 'NONE',  ( 4.711248855110969913, 1.761570823303935551, -1.180294879073326308 ) ) ;
#201671=CARTESIAN_POINT ( 'NONE',  ( 0.2331563151865486683, 2.034376611827843906, -2.362208330281903024 ) ) ;
#201675=CARTESIAN_POINT ( 'NONE',  ( 4.019992336727182369, -0.9402185374879183932, -1.564826772493657536 ) ) ;
#201681=CARTESIAN_POINT ( 'NONE',  ( 5.067206508511894469, 0.1826785619755930679, -1.861722072867748823 ) ) ;
#201683=CARTESIAN_POINT ( 'NONE',  ( 2.631371740967450634, -1.797512724518410598, 0.6935160474876176373 ) ) ;
#201685=CARTESIAN_POINT ( 'NONE',  ( 6.262552437187629550, -0.7028992384056665932, -1.831702256219314151 ) ) ;
#201693=CARTESIAN_POINT ( 'NONE',  ( 1.740021635027885649, 2.111287947816307575, -0.1595968877764943616 ) ) ;
#201697=CARTESIAN_POINT ( 'NONE',  ( 6.086797785588474063, 1.993605056338519699, 0.5577928598018768724 ) ) ;
#201698=CARTESIAN_POINT ( 'NONE',  ( -0.02423404108400224743, -1.785672699080865788, -0.4486397487279417118 ) ) ;
#201700=CARTESIAN_POINT ( 'NONE',  ( 6.381448165025822128, -0.6081200552338487109, -2.216719476268604438 ) ) ;
#201703=CARTESIAN_POINT ( 'NONE',  ( 1.394904949290655116, 1.871713452925367616, -1.323071089866036276 ) ) ;
#201707=CARTESIAN_POINT ( 'NONE',  ( 6.122988667457554435, -1.827782563270570648, 0.6563872640158885385 ) ) ;
#201711=CARTESIAN_POINT ( 'NONE',  ( 0.3869771421881840201, -1.897093440144840937, -0.6742409396158774992 ) ) ;
#201716=CARTESIAN_POINT ( 'NONE',  ( 2.871125768194443761, 1.984923283205226818, -0.6565763796619171755 ) ) ;
#201717=CARTESIAN_POINT ( 'NONE',  ( 0.9359865740741512008, 1.742660192269055663, 0.3080425777817352162 ) ) ;
#201720=CARTESIAN_POINT ( 'NONE',  ( 4.136908408643169111, -1.995281682711878668, 1.128303315244700178 ) ) ;
#201721=CARTESIAN_POINT ( 'NONE',  ( 3.081702191724482454, -1.714667182045168214, -0.2967042344550906985 ) ) ;
#201725=CARTESIAN_POINT ( 'NONE',  ( 3.461945267817592597, 1.365228559796902719, 1.068630620724864588 ) ) ;
#201726=CARTESIAN_POINT ( 'NONE',  ( 4.123599099448671090, 0.2696675481538573504, -2.154320840723603414 ) ) ;
#201728=CARTESIAN_POINT ( 'NONE',  ( 4.944546133779973651, -1.457238331152037825, 1.394083050251286870 ) ) ;
#201729=CARTESIAN_POINT ( 'NONE',  ( 3.156250000000002665, -1.895863743164019288, 0.7852924748301466362 ) ) ;
#201731=CARTESIAN_POINT ( 'NONE',  ( 1.588762598846172436, -0.2802010128373257913, -1.905785462699102206 ) ) ;
#201733=CARTESIAN_POINT ( 'NONE',  ( 4.588250468535750137, 1.280153277506433707, 1.815263839992816042 ) ) ;
#201735=CARTESIAN_POINT ( 'NONE',  ( -0.1110810684432777806, 1.403644835841436400, -2.056232460864733103 ) ) ;
#201740=CARTESIAN_POINT ( 'NONE',  ( 1.120143885658178906, -0.5347273011463581360, 2.155877112962206965 ) ) ;
#201741=CARTESIAN_POINT ( 'NONE',  ( 5.775826483351648832, -1.914393393812302113, 0.4282712878391075062 ) ) ;
#201743=CARTESIAN_POINT ( 'NONE',  ( 6.819576192995205233, -2.197070018990463502, 0.5395731105267542738 ) ) ;
#201746=CARTESIAN_POINT ( 'NONE',  ( 3.437984354829794142, 1.306305779046763149, 1.596332929251530253 ) ) ;
#201750=CARTESIAN_POINT ( 'NONE',  ( 5.923093557443566581, -0.04637014295935313474, 1.870147476527424635 ) ) ;
#201751=CARTESIAN_POINT ( 'NONE',  ( 4.430095426116970714, -1.344173880920132458, -1.095666204706043700 ) ) ;
#201752=CARTESIAN_POINT ( 'NONE',  ( 3.509068237933731016, -1.713987098263862086, 0.3013083454645076875 ) ) ;
#201753=CARTESIAN_POINT ( 'NONE',  ( 1.365189820700737577, 0.1628935585381158235, -2.286633867385555519 ) ) ;
#201755=CARTESIAN_POINT ( 'NONE',  ( 6.233939691744167177, 2.068093053085200417, 0.3059697267470474769 ) ) ;
#201756=CARTESIAN_POINT ( 'NONE',  ( 6.632770897174698810, -1.733374817101345000, 0.8757406700844807546 ) ) ;
#201759=CARTESIAN_POINT ( 'NONE',  ( 1.442029965644067158, -1.730867108953790590, -1.034163949609874233 ) ) ;
#201760=CARTESIAN_POINT ( 'NONE',  ( 0.2346725361867564585, 0.3788711812165134196, 2.158297013397599162 ) ) ;
#201764=CARTESIAN_POINT ( 'NONE',  ( 2.877707679121459527, 0.3088738507561124003, -2.097740099398600400 ) ) ;
#201767=CARTESIAN_POINT ( 'NONE',  ( 5.602125774977974260, -1.825872481414937853, 0.004271240736861136277 ) ) ;
#201774=CARTESIAN_POINT ( 'NONE',  ( 1.652609354460622626, 1.998416004623180697, 0.2920258124684270706 ) ) ;
#201775=CARTESIAN_POINT ( 'NONE',  ( 0.5168062790325059774, 1.452128344422070283, -1.525477944039640432 ) ) ;
#201777=CARTESIAN_POINT ( 'NONE',  ( 4.100341000477321529, 1.851659804611929472, 0.1859286059659806256 ) ) ;
#201782=CARTESIAN_POINT ( 'NONE',  ( 5.022008369909983116, -0.9795521577263366364, -1.540466923627185292 ) ) ;
#201787=CARTESIAN_POINT ( 'NONE',  ( 2.002904151241869712, 1.714182390810105927, 0.2594085799107764823 ) ) ;
#201788=CARTESIAN_POINT ( 'NONE',  ( 6.456982894382444549, 0.3095715517048603371, -1.814770079682447967 ) ) ;
#201789=CARTESIAN_POINT ( 'NONE',  ( 5.110162711920646750, -2.297000869944005430, 0.2220405423442091408 ) ) ;
#201792=CARTESIAN_POINT ( 'NONE',  ( 1.141951006405941715, 0.8376953415718463303, -1.883039458060199900 ) ) ;
#201794=CARTESIAN_POINT ( 'NONE',  ( 6.450549897212096262, 1.577601184540510681, 1.671684124095852653 ) ) ;
#201797=CARTESIAN_POINT ( 'NONE',  ( 6.596569749568344854, -0.5012203084251048990, -1.802199723311518786 ) ) ;
#201798=CARTESIAN_POINT ( 'NONE',  ( 3.550944491985886575, 0.2853618425060593378, 1.890879049853078087 ) ) ;
#201800=CARTESIAN_POINT ( 'NONE',  ( 4.653060005753134831, -1.773635849817876586, 1.313014255023836618 ) ) ;
#201805=CARTESIAN_POINT ( 'NONE',  ( 6.059260758684835046, -1.791542317298041365, 1.134111293253435182 ) ) ;
#201807=CARTESIAN_POINT ( 'NONE',  ( 3.434905211628926480, 2.250879548190734436, 0.5077644651142860788 ) ) ;
#201808=CARTESIAN_POINT ( 'NONE',  ( 4.246505328441081417, -1.940195102956907336, -0.2900488188990399396 ) ) ;
#201809=CARTESIAN_POINT ( 'NONE',  ( 0.6726124357511429341, 1.356994209013298036, -1.416925378234991095 ) ) ;
#201813=CARTESIAN_POINT ( 'NONE',  ( 6.210172754313918908, 1.157103754073171675, -1.651340222398114843 ) ) ;
#201816=CARTESIAN_POINT ( 'NONE',  ( 2.764704757504053756, -0.8271204958998740198, -2.007528505447711886 ) ) ;
#201818=CARTESIAN_POINT ( 'NONE',  ( 0.6508261300204335464, 2.090236094481153550, 0.3566229023672163878 ) ) ;
#201823=CARTESIAN_POINT ( 'NONE',  ( 1.651711298185059684, 0.6011997390959940013, -1.971106496394055885 ) ) ;
#201829=CARTESIAN_POINT ( 'NONE',  ( 4.811142580195256535, 1.587781804131962682, -1.065416552848017062 ) ) ;
#201830=CARTESIAN_POINT ( 'NONE',  ( 2.958220528980558761, -1.197304571117228100, 1.622486353517027968 ) ) ;
#201833=CARTESIAN_POINT ( 'NONE',  ( -0.1231740688493014324, -1.618022042794277748, -0.8147913963296258277 ) ) ;
#201835=CARTESIAN_POINT ( 'NONE',  ( 0.3213152726999657927, -1.356817153130492004, -1.352679412961822925 ) ) ;
#201836=CARTESIAN_POINT ( 'NONE',  ( 1.961466609329724164, 1.720096886549182136, 1.151944459977225055 ) ) ;
#201838=CARTESIAN_POINT ( 'NONE',  ( 0.4968692282744023303, 1.640418903650592508, -1.093199247851096789 ) ) ;
#201839=CARTESIAN_POINT ( 'NONE',  ( 3.141029808440584326, -1.609794727316344209, 0.8612202190056221784 ) ) ;
#201841=CARTESIAN_POINT ( 'NONE',  ( 0.04808971849027363077, -1.788275647358487985, -1.458162290246179715 ) ) ;
#201844=CARTESIAN_POINT ( 'NONE',  ( 3.789554774376595159, -1.906935327315992579, 0.7867413014382127479 ) ) ;
#201850=CARTESIAN_POINT ( 'NONE',  ( 5.807678370005410429, -0.5150985282868367765, 2.041858835689168927 ) ) ;
#201852=CARTESIAN_POINT ( 'NONE',  ( 6.654741963219192868, -0.5482099483974657295, -1.996413779700876301 ) ) ;
#201855=CARTESIAN_POINT ( 'NONE',  ( 3.725982817344280829, -1.284327275973631277, -1.738548686538298416 ) ) ;
#201856=CARTESIAN_POINT ( 'NONE',  ( 4.565106334443884251, -1.620744288901782904, 1.204869856736161537 ) ) ;
#201862=CARTESIAN_POINT ( 'NONE',  ( 2.659388954101277847, 1.913261587491304150, -0.6371546050257800298 ) ) ;
#201868=CARTESIAN_POINT ( 'NONE',  ( 4.446888776373093322, -1.802426293348384334, -0.9040943451460029534 ) ) ;
#201870=CARTESIAN_POINT ( 'NONE',  ( 0.5040132504689893711, -0.5763820916803040761, -1.625860608634047244 ) ) ;
#201875=CARTESIAN_POINT ( 'NONE',  ( 5.413307058180727438, -0.2754873708227522644, 1.850039175317084617 ) ) ;
#201876=CARTESIAN_POINT ( 'NONE',  ( 6.205343618373656334, 1.749435416034326618, -0.9961562333783975376 ) ) ;
#201880=CARTESIAN_POINT ( 'NONE',  ( 0.4742327405582689170, -2.001515332587662233, -0.2440062454662216829 ) ) ;
#201881=CARTESIAN_POINT ( 'NONE',  ( 1.546807606353679754, 0.1796435140209233228, 1.802673299184972322 ) ) ;
#201887=CARTESIAN_POINT ( 'NONE',  ( 5.993738795899758998, -1.900512161056673088, 0.2395553810000446704 ) ) ;
#201894=CARTESIAN_POINT ( 'NONE',  ( 4.188458007013862172, -2.137797052781073237, -0.3198388112101158143 ) ) ;
#201898=CARTESIAN_POINT ( 'NONE',  ( 0.2992908618118708675, -0.2657624787030036240, -2.103842954668332599 ) ) ;
#201899=CARTESIAN_POINT ( 'NONE',  ( 5.543921259432438298, 0.7380120197021734496, -1.669944898041133774 ) ) ;
#201900=CARTESIAN_POINT ( 'NONE',  ( 2.653541938639871756, 0.5291849669812850321, -1.898919477364902741 ) ) ;
#201901=CARTESIAN_POINT ( 'NONE',  ( 4.201352949932454450, 1.705870964349815333, -0.8646410313453978258 ) ) ;
#201904=CARTESIAN_POINT ( 'NONE',  ( 6.057084849134293236, 1.611049215779712940, -1.132701646639628246 ) ) ;
#201905=CARTESIAN_POINT ( 'NONE',  ( 0.4802856102240244951, -0.2370191179813440352, -1.927374317010506877 ) ) ;
#201911=CARTESIAN_POINT ( 'NONE',  ( 4.846305138012901637, 0.9798207982155520135, -1.642033262021398654 ) ) ;
#201913=CARTESIAN_POINT ( 'NONE',  ( 0.3939699847536023980, 1.636818068892214262, 1.480257586202008646 ) ) ;
#201915=CARTESIAN_POINT ( 'NONE',  ( 0.1176276963383571517, -0.5100272734060510293, 1.842954807014775653 ) ) ;
#201916=CARTESIAN_POINT ( 'NONE',  ( -0.02319159430947368913, 6.948789054712430691, -2.406029888528108618 ) ) ;
#201920=CARTESIAN_POINT ( 'NONE',  ( 2.770052221688572125, -2.048192801557855436, 0.3012726569043902569 ) ) ;
#201924=CARTESIAN_POINT ( 'NONE',  ( 0.07536363704235826688, -0.001874865094115066300, -2.144269471569634877 ) ) ;
#201929=CARTESIAN_POINT ( 'NONE',  ( 5.695915039874445362, 1.533740007788013449, 0.8092579662780824412 ) ) ;
#201931=CARTESIAN_POINT ( 'NONE',  ( 3.555589372526322123, 1.629040189086952362, 1.277421477176057474 ) ) ;
#201932=CARTESIAN_POINT ( 'NONE',  ( 4.271193901148872207, 1.890388351848461657, -0.9536453560208182356 ) ) ;
#201936=CARTESIAN_POINT ( 'NONE',  ( 2.764455286864405004, -0.7492524419267130309, -1.821560881719074709 ) ) ;
#201937=CARTESIAN_POINT ( 'NONE',  ( 1.072351618572921605, 0.7776387867773439933, 1.747342548420704800 ) ) ;
#201938=CARTESIAN_POINT ( 'NONE',  ( 4.681715291062889861, -1.083280430520225046, 2.020132927424389102 ) ) ;
#201939=CARTESIAN_POINT ( 'NONE',  ( 3.228933428962964758, 0.04559371896543929631, 1.825288036790246204 ) ) ;
#201944=CARTESIAN_POINT ( 'NONE',  ( 3.937747632521654495, -1.925297015496162611, 0.5883167919090799280 ) ) ;
#201945=CARTESIAN_POINT ( 'NONE',  ( 3.239059677355364375, -0.1396402669299641186, -1.956817938210092089 ) ) ;
#201949=CARTESIAN_POINT ( 'NONE',  ( 6.263634082940216175, 1.073540726731788908, 1.793809194602818735 ) ) ;
#201950=CARTESIAN_POINT ( 'NONE',  ( 5.155052684544634722, -1.496415494590461748, -0.9447146595812674352 ) ) ;
#201951=DIRECTION ( 'NONE',  ( 1.014813233446432150E-15, 1.000000000000000000, -4.583713267641621330E-32 ) ) ;
#201952=CARTESIAN_POINT ( 'NONE',  ( 2.168174125648382411, -1.346884454587377711, 1.728604079486287137 ) ) ;
#201953=CARTESIAN_POINT ( 'NONE',  ( 6.720655732516681802, 0.008434553976941013345, 1.726293928996263549 ) ) ;
#201956=CARTESIAN_POINT ( 'NONE',  ( 0.02935885042023527250, -1.056071399167260783, -1.364091372971764748 ) ) ;
#201957=CARTESIAN_POINT ( 'NONE',  ( 0.7205771127097709838, -1.942975266472912299, -1.227557580038857399 ) ) ;
#201958=CARTESIAN_POINT ( 'NONE',  ( 0.3807642395799659130, -0.2741851280289032688, -2.174293136291181483 ) ) ;
#201959=CARTESIAN_POINT ( 'NONE',  ( 6.784571902810725419, -1.680486618648807218, 0.4264331113166124343 ) ) ;
#201960=CARTESIAN_POINT ( 'NONE',  ( 3.194164748978207680, -0.8942147705085048415, 2.017778291555922809 ) ) ;
#201961=CARTESIAN_POINT ( 'NONE',  ( 0.7784788067067629491, -1.160020112895485456, -1.834993543685500939 ) ) ;
#201963=CARTESIAN_POINT ( 'NONE',  ( 0.6029268795967283046, 1.958829854606686904, 0.8042956034161384826 ) ) ;
#201964=CARTESIAN_POINT ( 'NONE',  ( 6.620655732516649294, 0.5674144795907026806, 2.226195167976598110 ) ) ;
#201965=CARTESIAN_POINT ( 'NONE',  ( 5.227533229383872104, -1.829308364520453978, 0.6040709075912870096 ) ) ;
#201967=CARTESIAN_POINT ( 'NONE',  ( 1.083963445724302588, -1.025016635393001252, 2.050507297876194901 ) ) ;
#201971=CARTESIAN_POINT ( 'NONE',  ( 3.282088111431053612, 2.166828800601192206, -0.4882270792503102808 ) ) ;
#201978=CARTESIAN_POINT ( 'NONE',  ( 2.250625165576759290, 1.976955744075848065, -0.3961026872240576702 ) ) ;
#201980=CARTESIAN_POINT ( 'NONE',  ( 1.112259789790952746, 2.060362754584772471, -0.09740899567091049205 ) ) ;
#201983=CARTESIAN_POINT ( 'NONE',  ( 6.550362485727940332, -1.338708790221679656, 1.112040286498132025 ) ) ;
#201985=CARTESIAN_POINT ( 'NONE',  ( 2.829092851278795617, -1.652813950429321999, 0.6331040572071617856 ) ) ;
#201986=CARTESIAN_POINT ( 'NONE',  ( 1.442029965644067158, -1.730867108953790590, -1.034163949609874233 ) ) ;
#201987=CARTESIAN_POINT ( 'NONE',  ( 0.4152503475762688856, -0.9843521281015167324, -1.555853522519357934 ) ) ;
#201988=CARTESIAN_POINT ( 'NONE',  ( 5.601222333718593127, -0.5599829797399961118, 2.222829207915150374 ) ) ;
#201989=CARTESIAN_POINT ( 'NONE',  ( 3.925598083870453614, 0.9833751987384667936, -1.556331266066004027 ) ) ;
#201991=CARTESIAN_POINT ( 'NONE',  ( 3.662960631648714216, -1.609669772967847079, -0.8612380056681954166 ) ) ;
#201992=CARTESIAN_POINT ( 'NONE',  ( 5.291638762709002464, 1.525045427759319727, -1.319226660814104335 ) ) ;
#201994=CARTESIAN_POINT ( 'NONE',  ( 3.450319916561462197, 2.262689076145682598, 0.002162386163321801912 ) ) ;
#201996=CARTESIAN_POINT ( 'NONE',  ( 6.018611168240656006, 1.417078199399327332, -1.558035186251781612 ) ) ;
#201997=CARTESIAN_POINT ( 'NONE',  ( 3.613788337741298040, 0.5058112091442801272, -2.007490274132675445 ) ) ;
#202000=CARTESIAN_POINT ( 'NONE',  ( 5.426475896148662770, -0.9536019125786737716, -1.894055658958586852 ) ) ;
#202004=CARTESIAN_POINT ( 'NONE',  ( 2.508321089405711746, -0.7374124507862482858, -1.779973396525496909 ) ) ;
#202006=CARTESIAN_POINT ( 'NONE',  ( 6.614111185624225620, 1.964402775464332507, -0.1412838390872969141 ) ) ;
#202011=CARTESIAN_POINT ( 'NONE',  ( 0.4928134435002875513, -1.227493105415909946, 1.851297100075269153 ) ) ;
#202012=CARTESIAN_POINT ( 'NONE',  ( 2.924945619078959336, 1.982447918529605557, 0.7109604360746536456 ) ) ;
#202015=CARTESIAN_POINT ( 'NONE',  ( 0.9064450206472760563, 0.5352286137044174330, 1.782442419352270102 ) ) ;
#202020=CARTESIAN_POINT ( 'NONE',  ( 1.705496241919310707, 1.842552997918958768, -1.049655202612943095 ) ) ;
#202023=CARTESIAN_POINT ( 'NONE',  ( 4.141029529442549872, -0.1900441490861082827, -1.952618137025011746 ) ) ;
#202024=CARTESIAN_POINT ( 'NONE',  ( 2.149508875876861236, -1.735919364271593768, -1.288018159417112729 ) ) ;
#202025=CARTESIAN_POINT ( 'NONE',  ( 1.575478407343299692, -0.9843019613302635973, 1.555867251595323353 ) ) ;
#202028=CARTESIAN_POINT ( 'NONE',  ( 2.958654558096874609, 0.2547609298257165200, -1.721438497358678932 ) ) ;
#202032=CARTESIAN_POINT ( 'NONE',  ( 1.358524781292804517, 0.8764843271744371389, 1.976213614152767750 ) ) ;
#202033=CARTESIAN_POINT ( 'NONE',  ( 3.409529676982744562, 0.4871283372531940992, 1.956261718130556382 ) ) ;
#202035=CARTESIAN_POINT ( 'NONE',  ( 0.8839147992780393981, 1.452536163361785260, 1.601146772000871188 ) ) ;
#202036=CARTESIAN_POINT ( 'NONE',  ( 3.819176294577591779, -0.1464417209034867828, 1.966092509880690065 ) ) ;
#202038=CARTESIAN_POINT ( 'NONE',  ( 6.509000000000039421, 4.695815278351551214, 2.562658139094181386 ) ) ;
#202039=CARTESIAN_POINT ( 'NONE',  ( 2.630336588288070043, 0.2403035443280654992, 1.927090367541855365 ) ) ;
#202044=CARTESIAN_POINT ( 'NONE',  ( -0.1110810684433142237, 6.948330828014858795, -2.391984312838004278 ) ) ;
#202050=CARTESIAN_POINT ( 'NONE',  ( 6.581126798121099242, -0.1039769691308822797, -2.305377512668804751 ) ) ;
#202052=CARTESIAN_POINT ( 'NONE',  ( 4.117980938109369937, 1.947433809354440326, -0.2358448244534834815 ) ) ;
#202054=CARTESIAN_POINT ( 'NONE',  ( 2.110000207431836472, 0.002812218110825881467, 2.016597019944998959 ) ) ;
#202056=CARTESIAN_POINT ( 'NONE',  ( 3.925106927653505995, -1.840236814299311741, 1.047156446301507948 ) ) ;
#202060=CARTESIAN_POINT ( 'NONE',  ( 3.538839456958355889, -1.395042877683351890, -1.201619466480362108 ) ) ;
#202064=CARTESIAN_POINT ( 'NONE',  ( 3.551138032611600437, 0.3147205237276836653, 2.097014573754731881 ) ) ;
#202068=CARTESIAN_POINT ( 'NONE',  ( 4.991509756128800213, 1.524171611017493655, 1.387147876433484806 ) ) ;
#202070=CARTESIAN_POINT ( 'NONE',  ( 2.067674361007607597, -1.131582805410412673, 1.452419944642673100 ) ) ;
#202076=CARTESIAN_POINT ( 'NONE',  ( 2.315298440750997777, 1.971968782506158924, 0.9909306302095726160 ) ) ;
#202077=CARTESIAN_POINT ( 'NONE',  ( 3.479979345725477291, 1.432071248269211505, 1.751504329374527158 ) ) ;
#202079=CARTESIAN_POINT ( 'NONE',  ( 4.254050669898622239, 0.7686244906546428890, -1.640568623306848606 ) ) ;
#202080=CARTESIAN_POINT ( 'NONE',  ( 4.364398177449787752, -1.859642558872817375, -0.4596742015197906595 ) ) ;
#202083=CARTESIAN_POINT ( 'NONE',  ( 3.801606108737245471, -0.5733388152893458267, 1.886244881718708521 ) ) ;
#202084=CARTESIAN_POINT ( 'NONE',  ( 4.627732503263369601, -1.150995203733524930, -1.474563928533303869 ) ) ;
#202086=CARTESIAN_POINT ( 'NONE',  ( 3.299772510450727836, 1.819142665603549425, 1.419829399881943566 ) ) ;
#202087=CARTESIAN_POINT ( 'NONE',  ( 4.492532346964829060, 1.824898331334467549, 0.3640980636450250052 ) ) ;
#202089=CLOSED_SHELL ( 'NONE', ( #188055, #35218, #193152, #114894, #105435, #132377, #24000, #145997 ) ) ;
#202090=CARTESIAN_POINT ( 'NONE',  ( -0.1355283706049141557, -1.957205112593700003, -0.4852584411360050254 ) ) ;
#202092=CARTESIAN_POINT ( 'NONE',  ( 1.735132801782751200, 0.2076089413485527335, 2.095809512812545350 ) ) ;
#202097=CARTESIAN_POINT ( 'NONE',  ( 3.006218798242997980, -0.8556837461295877523, 1.940463308995137526 ) ) ;
#202099=CARTESIAN_POINT ( 'NONE',  ( 1.301042304527067817, -0.3004618026806615272, -1.997203725593140078 ) ) ;
#202104=CARTESIAN_POINT ( 'NONE',  ( 1.880366631079612549, -1.158069840294423392, 1.825029014904603342 ) ) ;
#202107=CARTESIAN_POINT ( 'NONE',  ( 6.925078400183550364, 4.698656493127392864, 2.418320467900983761 ) ) ;
#202108=CARTESIAN_POINT ( 'NONE',  ( 6.639320575229294974, 0.002105643433562139673, 2.003388605011639179 ) ) ;
#202110=CARTESIAN_POINT ( 'NONE',  ( 5.964077395145578109, -1.074666730956087335, 1.706109649615504154 ) ) ;
#202112=CARTESIAN_POINT ( 'NONE',  ( 6.480031082513550089, -2.050496881725831777, -0.4073240614407472315 ) ) ;
#202114=CARTESIAN_POINT ( 'NONE',  ( 1.358695222972395422, 0.9186288065576648787, 2.067797507578944760 ) ) ;
#202121=CARTESIAN_POINT ( 'NONE',  ( 3.844159338287247429, 1.716807015663003311, 0.1666082703000223986 ) ) ;
#202124=CARTESIAN_POINT ( 'NONE',  ( 2.178617772012156006, -0.08127397458944020381, -1.767985329221566815 ) ) ;
#202125=CARTESIAN_POINT ( 'NONE',  ( 3.070950286465543577, -1.523008450377001832, 1.316504112208529920 ) ) ;
#202126=CARTESIAN_POINT ( 'NONE',  ( 5.667066814448853407, -1.992748536412903615, -0.9483587796220711574 ) ) ;
#202128=CARTESIAN_POINT ( 'NONE',  ( 3.902606965841335818, -1.998407076283228223, -0.2920856897847978195 ) ) ;
#202130=CARTESIAN_POINT ( 'NONE',  ( 5.444028431581452665, -1.345373016635186714, -1.639009079359869725 ) ) ;
#202131=CARTESIAN_POINT ( 'NONE',  ( 4.130482583401101415, 0.5405105419177670401, 1.942537254285629178 ) ) ;
#202132=CARTESIAN_POINT ( 'NONE',  ( 4.271601952734533469, 0.3905692737867596520, -1.768816315278500584 ) ) ;
#202135=CARTESIAN_POINT ( 'NONE',  ( 1.990876257202532695, 1.628914321797021669, -0.9196232060951770038 ) ) ;
#202138=CARTESIAN_POINT ( 'NONE',  ( 6.129554203544218538, -0.2143803907406968412, 1.798669436738309368 ) ) ;
#202144=CARTESIAN_POINT ( 'NONE',  ( 0.6504702201592416078, 1.884490048413577368, 0.3244712162126031085 ) ) ;
#202146=CARTESIAN_POINT ( 'NONE',  ( 1.961309178647975715, 1.629323162926434199, 1.092499269706406428 ) ) ;
#202148=EDGE_CURVE ( 'NONE', #190431, #90194, #151013, .T. ) ;
#202150=CARTESIAN_POINT ( 'NONE',  ( 3.779626292077962191, 0.2561244552635975058, -2.104982076983111572 ) ) ;
#202153=CARTESIAN_POINT ( 'NONE',  ( 5.290288327143207958, -1.956129722686357431, -0.2442305991610035365 ) ) ;
#202156=CARTESIAN_POINT ( 'NONE',  ( 0.8967405870976161708, -1.965081358092489516, -0.4369277762777488139 ) ) ;
#202159=CARTESIAN_POINT ( 'NONE',  ( 1.036884384669316539, -1.666496236897334615, 1.305811245984341173 ) ) ;
#202161=CARTESIAN_POINT ( 'NONE',  ( 2.330607996690749140, -1.275545549462468120, 1.630658604070814199 ) ) ;
#202165=CARTESIAN_POINT ( 'NONE',  ( 4.945306066807232170, 0.6564501001628511023, -1.984974157428524899 ) ) ;
#202167=CARTESIAN_POINT ( 'NONE',  ( 3.047666980291532823, 0.6586017179070653427, -1.702814618940437619 ) ) ;
#202168=CARTESIAN_POINT ( 'NONE',  ( 2.139049582973771457, 0.0009909630806471080022, 1.811656970554485602 ) ) ;
#202170=CARTESIAN_POINT ( 'NONE',  ( 6.586557750117827403, -2.163372447211810989, -0.4352210726449382006 ) ) ;
#202173=CARTESIAN_POINT ( 'NONE',  ( 5.772568991252683190, -1.404203161598962968, 1.702366421003978392 ) ) ;
#202176=VERTEX_POINT ( 'NONE', #85585 ) ;
#202177=CARTESIAN_POINT ( 'NONE',  ( 3.650944405621194377, 0.2833616294029631111, 1.891055170903446658 ) ) ;
#202180=CARTESIAN_POINT ( 'NONE',  ( 6.373496627357888578, -0.2573980274669443458, 2.054251119134167691 ) ) ;
#202182=CARTESIAN_POINT ( 'NONE',  ( 5.495707582769355781, -2.191739722525353429, -0.0009102486706394352645 ) ) ;
#202186=CARTESIAN_POINT ( 'NONE',  ( 3.585083614955932863, 1.692364770286663322, -0.7970176776704934740 ) ) ;
#202187=CARTESIAN_POINT ( 'NONE',  ( -0.02319159430947542039, 1.394398620246390275, -2.068318759734718792 ) ) ;
#202194=CARTESIAN_POINT ( 'NONE',  ( 6.596543124887806364, 2.046857425119428697, 0.3097440254393943881 ) ) ;
#202195=CARTESIAN_POINT ( 'NONE',  ( 0.8433753223025289847, 0.3905737783656983431, -1.978056610397058712 ) ) ;
#202199=CARTESIAN_POINT ( 'NONE',  ( 0.8674257402763450031, 2.111068143204323455, -0.5878430487569612506 ) ) ;
#202200=CARTESIAN_POINT ( 'NONE',  ( 5.813091150998386247, 1.612263477354998864, 0.8566026058636074803 ) ) ;
#202209=CARTESIAN_POINT ( 'NONE',  ( 3.280630368989821743, 1.663260157205956880, -0.7901080472864712156 ) ) ;
#202210=CARTESIAN_POINT ( 'NONE',  ( 1.031890287230966985, -1.963566467742537069, 0.4430998199175004704 ) ) ;
#202211=CARTESIAN_POINT ( 'NONE',  ( 2.530986164375541581, 2.254368048762548593, -0.4469772407268405301 ) ) ;
#202213=CARTESIAN_POINT ( 'NONE',  ( 0.9888277058803507380, 0.1293858107240040412, 1.856492687334237335 ) ) ;
#202217=CARTESIAN_POINT ( 'NONE',  ( 4.412309042748480792, -1.912102599942141268, -0.04143165621695726192 ) ) ;
#202221=CARTESIAN_POINT ( 'NONE',  ( 3.263305109790759939, 2.039240668410980284, -0.4604351538632973639 ) ) ;
#202222=CARTESIAN_POINT ( 'NONE',  ( 2.500682550815761740, 1.503739811390795378, -1.112508705057350999 ) ) ;
#202226=CARTESIAN_POINT ( 'NONE',  ( 2.893823712666950598, -0.5078125688623453815, -1.664683006417116751 ) ) ;
#202230=CARTESIAN_POINT ( 'NONE',  ( 3.474969472568560480, 0.04075424684168299505, -1.724569731432665121 ) ) ;
#202231=CARTESIAN_POINT ( 'NONE',  ( 4.318054327947466575, 1.347776305887092185, -1.728067674571641898 ) ) ;
#202232=CARTESIAN_POINT ( 'NONE',  ( 6.621690180768193379, -2.141820631849135292, 0.5315211216728524812 ) ) ;
#202234=CARTESIAN_POINT ( 'NONE',  ( 3.221698175004498399, 0.3232067185854271552, -2.146787281877101439 ) ) ;
#202235=CARTESIAN_POINT ( 'NONE',  ( 2.279681363911123970, 1.122676072794186908, 1.439608767588994365 ) ) ;
#202236=CARTESIAN_POINT ( 'NONE',  ( 0.2390249890181182224, -0.1369461163322066299, -1.930431041017650395 ) ) ;
#202237=CARTESIAN_POINT ( 'NONE',  ( 4.557876730116875663, 1.221875164117897539, 1.729014733294547801 ) ) ;
#202239=CARTESIAN_POINT ( 'NONE',  ( 5.161814014510654580, 1.128026202373041853, 1.995582457067740068 ) ) ;
#202241=CARTESIAN_POINT ( 'NONE',  ( 6.620655732516647518, 0.01042156863438310939, 1.726407961933309920 ) ) ;
#202244=CARTESIAN_POINT ( 'NONE',  ( -0.1046615654881309365, -0.1561857951268459388, -2.086345279447648249 ) ) ;
#202253=CARTESIAN_POINT ( 'NONE',  ( 5.256482491209823138, 1.942542154241846397, -0.5404887192124520068 ) ) ;
#202255=CARTESIAN_POINT ( 'NONE',  ( 4.223522562419862680, 0.2575905095270197287, -2.046390306194557418 ) ) ;
#202257=CARTESIAN_POINT ( 'NONE',  ( -0.2408018239684408812, 2.868499929943384874, -2.588695376639174484 ) ) ;
#202261=CARTESIAN_POINT ( 'NONE',  ( 0.7266515212380560973, 0.1555473773823950467, 2.084908828405390491 ) ) ;
#202262=CARTESIAN_POINT ( 'NONE',  ( 4.447888798048591497, -1.802416534049579910, -0.9041112711936499791 ) ) ;
#202263=CARTESIAN_POINT ( 'NONE',  ( 3.720104550828434942, 1.749555917645674530, 0.5740644926693627692 ) ) ;
#202265=CARTESIAN_POINT ( 'NONE',  ( 0.9731894095723004900, 1.663878915475509812, -0.4539961392346722469 ) ) ;
#202267=CARTESIAN_POINT ( 'NONE',  ( 1.354533853113936814, 0.1633331948888619711, -2.292934881128176450 ) ) ;
#202269=CARTESIAN_POINT ( 'NONE',  ( 0.2107632190684857465, -0.9678151086435597961, -2.042474306115627414 ) ) ;
#202270=CARTESIAN_POINT ( 'NONE',  ( 2.983145545965359080, -0.1552688264333592638, -2.100405815202969873 ) ) ;
#202274=CARTESIAN_POINT ( 'NONE',  ( 5.500000000000004441, -3.262149103155007084E-13, -2.052068128417942283 ) ) ;
#202279=CARTESIAN_POINT ( 'NONE',  ( 5.502238596801645620, -0.9988962762179309784, 1.984187878789472892 ) ) ;
#202280=CARTESIAN_POINT ( 'NONE',  ( 2.484552680892829546, -0.3758780662847274190, -2.158817762932266682 ) ) ;
#202283=CARTESIAN_POINT ( 'NONE',  ( 5.459412808053472510, 1.602871733476991079, 1.130958114227413436 ) ) ;
#202286=CARTESIAN_POINT ( 'NONE',  ( 6.610000000000028741, 1.211438232176115237, 2.390254139237833808 ) ) ;
#202288=CARTESIAN_POINT ( 'NONE',  ( 4.060867369437678676, 0.5686956411946364476, 2.042824496258560441 ) ) ;
#202294=CARTESIAN_POINT ( 'NONE',  ( 5.214338956685346638, 1.703448749313410282, 0.6994016148276982481 ) ) ;
#202297=CARTESIAN_POINT ( 'NONE',  ( 0.6611568445531558202, 0.8558493542428649015, 1.515405575314775044 ) ) ;
#202301=CARTESIAN_POINT ( 'NONE',  ( 5.418883921851007202, 1.995750516393671514, 0.8311057252617033431 ) ) ;
#202305=CARTESIAN_POINT ( 'NONE',  ( 4.399409362686744096, 1.734418756986338295, 1.290045131933370781 ) ) ;
#202307=CARTESIAN_POINT ( 'NONE',  ( 4.903572647403447782, -0.5284346980384787562, 1.899126047080600621 ) ) ;
#202308=CARTESIAN_POINT ( 'NONE',  ( 4.499182623014930549, 1.700326773844270667, 0.3381245445180857123 ) ) ;
#202310=CARTESIAN_POINT ( 'NONE',  ( 0.4861908890553789941, -2.175720422541329580, -0.2624175912114696252 ) ) ;
#202311=CARTESIAN_POINT ( 'NONE',  ( 2.766999470516241288, -1.591810197153446182, 1.670866638877396060 ) ) ;
#202312=CARTESIAN_POINT ( 'NONE',  ( 4.218082229858637788, -1.055972844705153291, -1.769506188133779467 ) ) ;
#202313=CARTESIAN_POINT ( 'NONE',  ( 6.321825213571911739, 1.114395046473240392, -1.590342819258899532 ) ) ;
#202321=CARTESIAN_POINT ( 'NONE',  ( 3.821466819111440927, -0.1649144712266135959, 2.200675313789305143 ) ) ;
#202323=CARTESIAN_POINT ( 'NONE',  ( 0.8306204695724854759, -1.749664030167530138, -0.6342216345150762935 ) ) ;
#202328=CARTESIAN_POINT ( 'NONE',  ( 6.925078400183521055, 4.691537398408025972, 2.606905763235977336 ) ) ;
#202330=CARTESIAN_POINT ( 'NONE',  ( 3.133719265644947960, -1.383057153600345535, -1.528062560492246202 ) ) ;
#202335=CARTESIAN_POINT ( 'NONE',  ( 2.131779597171743923, -1.345384690298248698, -1.561254108789570827 ) ) ;
#202340=CARTESIAN_POINT ( 'NONE',  ( 5.971336403843030105, 0.1662174427981797931, -2.200672837095698497 ) ) ;
#202341=CARTESIAN_POINT ( 'NONE',  ( 1.528841242883504981, 2.082761121880230881, 0.5781018612496248155 ) ) ;
#202343=CARTESIAN_POINT ( 'NONE',  ( 0.9894706735516716201, -0.4852629857438545691, 1.957171443305204761 ) ) ;
#202347=CARTESIAN_POINT ( 'NONE',  ( 6.235011639695051677, 1.786057601157978958, 0.6837302122261401660 ) ) ;
#202350=CARTESIAN_POINT ( 'NONE',  ( 2.219420098953532428, -1.815089452277141691, 0.4520615115926190919 ) ) ;
#202352=CARTESIAN_POINT ( 'NONE',  ( 3.432827581131673522, -1.645759781613131967, 1.164986487700324425 ) ) ;
#202356=CARTESIAN_POINT ( 'NONE',  ( 4.617860632714274161, -2.065554989951523535, 0.4101935312739966588 ) ) ;
#202361=CARTESIAN_POINT ( 'NONE',  ( 4.922131295886445379, -2.009687048479208205, 0.2019785858936548328 ) ) ;
#202364=CARTESIAN_POINT ( 'NONE',  ( 1.129816159781659390, 1.988900438959967376, -0.5462022044933153575 ) ) ;
#202367=CARTESIAN_POINT ( 'NONE',  ( 6.011032505573889573, 1.903242638633116712, 1.024824547371510075 ) ) ;
#202373=CARTESIAN_POINT ( 'NONE',  ( 3.033805354627703288, 2.062495667156949430, -0.6785788507157832772 ) ) ;
#202376=CARTESIAN_POINT ( 'NONE',  ( 1.733694375844633706, 1.821329977863223926, 0.2691589665217360983 ) ) ;
#202378=CARTESIAN_POINT ( 'NONE',  ( 2.982162443640325566, -2.159563097825706990, -0.3721831821169723775 ) ) ;
#202379=CARTESIAN_POINT ( 'NONE',  ( 6.883263157960358924, 4.692138088316172073, 2.616388454592593504 ) ) ;
#202380=CARTESIAN_POINT ( 'NONE',  ( 5.014671263542332724, 1.563880152264264245, -1.635232377595864595 ) ) ;
#202387=CARTESIAN_POINT ( 'NONE',  ( 5.255052661293587946, -1.495254947996208950, -0.9463502368073344329 ) ) ;
#202389=CARTESIAN_POINT ( 'NONE',  ( 2.380028573532027458, 1.294904889207445509, 1.660730631172540495 ) ) ;
#202392=CARTESIAN_POINT ( 'NONE',  ( 2.242574321144190641, -1.930940592676654965, -0.3871509593617681322 ) ) ;
#202395=CARTESIAN_POINT ( 'NONE',  ( 6.047087830114247886, 0.1867083960328217995, 1.801967238635309165 ) ) ;
#202399=CARTESIAN_POINT ( 'NONE',  ( 5.383624799460786647, 1.257121276536907750, 1.385457850027263405 ) ) ;
#202401=CARTESIAN_POINT ( 'NONE',  ( 5.260626886859606444, -0.6923115906582855139, -1.951227211109484383 ) ) ;
#202410=CARTESIAN_POINT ( 'NONE',  ( 5.424254290899477304, 0.9654600744411747648, 1.707767180430696641 ) ) ;
#202412=CARTESIAN_POINT ( 'NONE',  ( 3.181017370561005198, -0.9912469002804729090, -1.755500664876320727 ) ) ;
#202414=CARTESIAN_POINT ( 'NONE',  ( 2.588968054610871317, 1.620874238694985925, 1.020808031020562501 ) ) ;
#202416=CARTESIAN_POINT ( 'NONE',  ( 0.9080814035550346386, -0.9900877184637231210, -1.955254813705724404 ) ) ;
#202417=CARTESIAN_POINT ( 'NONE',  ( 0.2331713839410602396, 2.030351879425442707, -2.369071045443218004 ) ) ;
#202418=CARTESIAN_POINT ( 'NONE',  ( 2.108475139129362574, 1.389272611029747750, -1.252756881873963168 ) ) ;
#202420=CARTESIAN_POINT ( 'NONE',  ( 4.131111929362305091, 1.842322257054655354, 0.8120569753113301426 ) ) ;
#202423=CARTESIAN_POINT ( 'NONE',  ( 4.534827772108455335, -1.699605468249162588, 1.262326912638973786 ) ) ;
#202425=CARTESIAN_POINT ( 'NONE',  ( 6.320769956279724155, -1.466918727022302971, 1.461273828345016845 ) ) ;
#202426=CARTESIAN_POINT ( 'NONE',  ( 1.716468666696397971, 1.951974251796151583, 0.7495149520271927601 ) ) ;
#202428=CARTESIAN_POINT ( 'NONE',  ( 6.088856429251793934, -0.2706771573857471580, -1.805266125362497531 ) ) ;
#202433=( NAMED_UNIT ( * ) SI_UNIT ( $, .STERADIAN. ) SOLID_ANGLE_UNIT ( ) );
#202437=CARTESIAN_POINT ( 'NONE',  ( 0.3635249777022043771, 0.5700983740567664437, -1.719507965497588220 ) ) ;
#202444=CARTESIAN_POINT ( 'NONE',  ( 5.905875104417894761, -1.122515283938491537, -1.674877678029200068 ) ) ;
#202445=CARTESIAN_POINT ( 'NONE',  ( 0.8562900302464396818, 0.8558255631127343888, -1.940287777186230578 ) ) ;
#202453=CARTESIAN_POINT ( 'NONE',  ( 2.975404341296074229, -0.1976578167360588389, 1.959527558586687146 ) ) ;
#202454=CARTESIAN_POINT ( 'NONE',  ( 4.886342304379579282, -0.6820123065829878373, -1.897693145932321857 ) ) ;
#202458=CARTESIAN_POINT ( 'NONE',  ( 5.244143516318892750, 0.6338322011035132375, 2.097776330851252258 ) ) ;
#202460=CARTESIAN_POINT ( 'NONE',  ( 3.434515876041916105, 1.879162883219337665, 0.4232601004234298747 ) ) ;
#202462=CARTESIAN_POINT ( 'NONE',  ( -0.02948999725177046949, 0.7228889410342426158, -2.008564694272568563 ) ) ;
#202468=CARTESIAN_POINT ( 'NONE',  ( 5.155114233317533490, 1.639596689546858777, -1.090739528099492928 ) ) ;
#202470=CARTESIAN_POINT ( 'NONE',  ( 0.9252163604592329449, -1.233020167302405490, -1.500395619358737553 ) ) ;
#202471=CARTESIAN_POINT ( 'NONE',  ( 4.283843839860628222, 1.952122219449687668, -0.4911893120533029622 ) ) ;
#202472=CARTESIAN_POINT ( 'NONE',  ( 5.237821733363889010, -2.161759915733433068, -0.7809387408506673900 ) ) ;
#202474=CARTESIAN_POINT ( 'NONE',  ( 3.906960136656021376, -1.523566986099005316, 1.068299854780943692 ) ) ;
#202481=CARTESIAN_POINT ( 'NONE',  ( 0.3280006606478855224, 1.121390616443746602, -1.882787531365101685 ) ) ;
#202486=CARTESIAN_POINT ( 'NONE',  ( 0.2053145577999641036, -0.4904175937916722128, 1.758528939493007481 ) ) ;
#202488=CARTESIAN_POINT ( 'NONE',  ( 2.707300540323886562, 1.633622375412818073, 0.5822755513817943207 ) ) ;
#202493=CARTESIAN_POINT ( 'NONE',  ( 6.111906964637446649, -1.811269838261083232, 0.2284818145076653595 ) ) ;
#202494=CARTESIAN_POINT ( 'NONE',  ( 3.731260466781026963, 0.05263058604075031982, -1.961233346245725429 ) ) ;
#202499=CARTESIAN_POINT ( 'NONE',  ( 3.633539341399088407, -0.1543397204060332761, 2.114911865293423787 ) ) ;
#202502=ADVANCED_FACE ( 'NONE', ( #124583 ), #180104, .T. ) ;
#202503=CARTESIAN_POINT ( 'NONE',  ( 1.446235060908855008, -0.9343481645287862181, 1.847524432027500385 ) ) ;
#202506=CARTESIAN_POINT ( 'NONE',  ( 4.916739609850255377, -0.7473993280511237458, -2.091895594778249379 ) ) ;
#202508=CARTESIAN_POINT ( 'NONE',  ( 1.249136956142880894, 2.263619502511230230, -0.3993902815438779563 ) ) ;
#202516=CARTESIAN_POINT ( 'NONE',  ( 2.689602200614676697, 1.814610489020528350, -0.6038049036062518304 ) ) ;
#202517=CARTESIAN_POINT ( 'NONE',  ( 4.242953580973901850, -1.500179917044243139, 0.8508681493539415053 ) ) ;
#202518=CARTESIAN_POINT ( 'NONE',  ( 2.817592499383800408, -1.357869084745389587, -1.490969456672403659 ) ) ;
#202519=CARTESIAN_POINT ( 'NONE',  ( 3.516502792989243176, -2.123307701433849282, 0.8810689989526691024 ) ) ;
#202521=CARTESIAN_POINT ( 'NONE',  ( 6.709622069694824553, -0.4604308047033068840, 2.062537096560501659 ) ) ;
#202523=CARTESIAN_POINT ( 'NONE',  ( 4.973781575966475188, 1.018845774273930749, 1.446830399915491006 ) ) ;
#202525=CARTESIAN_POINT ( 'NONE',  ( 1.008267258593512183, -1.035053087846869335, -2.045343892876672065 ) ) ;
#202526=CARTESIAN_POINT ( 'NONE',  ( 6.316338248019477852, 1.719745045379994286, 0.6579504788090041467 ) ) ;
#202528=CARTESIAN_POINT ( 'NONE',  ( 5.542994302928621053, -1.725804593724251657, -1.350479894307685225 ) ) ;
#202532=CARTESIAN_POINT ( 'NONE',  ( 6.689897370947560873, -1.349224794794257720, -1.570457413003906177 ) ) ;
#202533=CARTESIAN_POINT ( 'NONE',  ( 0.9191581010105540628, -1.820984308097562954, 0.8666112775468015617 ) ) ;
#202535=CARTESIAN_POINT ( 'NONE',  ( 4.283760221956850245, 1.259274395394771817, 1.458037640750938779 ) ) ;
#202537=CARTESIAN_POINT ( 'NONE',  ( 0.8794853950937852050, -2.011299634806243741, -0.9433073274909502537 ) ) ;
#202546=CARTESIAN_POINT ( 'NONE',  ( 4.229842819227870976, 1.707864474872609062, 0.3341882380870179192 ) ) ;
#202547=CARTESIAN_POINT ( 'NONE',  ( 2.769914238037580745, -1.940913097850523128, 0.2850433363836765155 ) ) ;
#202552=CARTESIAN_POINT ( 'NONE',  ( 0.2036765287981847083, -1.593398458586914757, -1.309455759714562850 ) ) ;
#202555=CARTESIAN_POINT ( 'NONE',  ( 5.260953973667149342, -0.05432152012316109058, -2.015980820358989511 ) ) ;
#202556=CARTESIAN_POINT ( 'NONE',  ( 0.8137758769373629741, -0.3292158159766758185, 2.238336236828967429 ) ) ;
#202560=CARTESIAN_POINT ( 'NONE',  ( 1.897508810457830153, -0.6348907881138059484, 1.759622905829677508 ) ) ;
#202561=CARTESIAN_POINT ( 'NONE',  ( -0.07027205189932134166, -1.338084538058325279, -1.103043951268277478 ) ) ;
#202563=CARTESIAN_POINT ( 'NONE',  ( 3.843468145482428877, 0.7371271433744167600, -2.064019554291535830 ) ) ;
#202564=CARTESIAN_POINT ( 'NONE',  ( 6.088978940744814494, -0.3304744056438710387, -2.283700556900492451 ) ) ;
#202565=CARTESIAN_POINT ( 'NONE',  ( 6.643830136542335119, 0.7930364421293911725, -1.902288772117090687 ) ) ;
#202566=CARTESIAN_POINT ( 'NONE',  ( 3.714730536668510830, -0.1420231480665778423, 1.936809614188730544 ) ) ;
#202568=CARTESIAN_POINT ( 'NONE',  ( 5.553920895479774522, 1.868435625992425742, -0.09091641586010666687 ) ) ;
#202572=CARTESIAN_POINT ( 'NONE',  ( 4.236954046275762664, 2.015912997090345549, -0.05229627655192746472 ) ) ;
#202576=CARTESIAN_POINT ( 'NONE',  ( 1.031563979315492485, -1.156294252604734396, -1.412831148817683680 ) ) ;
#202582=CARTESIAN_POINT ( 'NONE',  ( 0.4269344243218140544, 2.069031678568326704, 0.6260965431626740463 ) ) ;
#202586=CARTESIAN_POINT ( 'NONE',  ( 5.901037506996139825, -0.2983434833860042490, -1.997397228102874234 ) ) ;
#202587=CARTESIAN_POINT ( 'NONE',  ( 5.848318881832833327, 1.097015000334870649, -1.931420017644119635 ) ) ;
#202588=ORIENTED_EDGE ( 'NONE', *, *, #52718, .F. ) ;
#202591=CARTESIAN_POINT ( 'NONE',  ( 5.155176885484381799, -1.739861089072095357, -1.104300716835506346 ) ) ;
#202592=CARTESIAN_POINT ( 'NONE',  ( 4.166638809851969327, 1.319227567334404494, 1.525044649537968589 ) ) ;
#202600=CARTESIAN_POINT ( 'NONE',  ( 4.130232389481975908, 0.2495678132241747338, -2.000550906993769473 ) ) ;
#202601=CARTESIAN_POINT ( 'NONE',  ( 3.556447125109524876, -1.624355972047783148, -0.8667379164201680641 ) ) ;
#202603=CARTESIAN_POINT ( 'NONE',  ( 2.245130213409586961, 0.5076759487793567338, 2.251015715305480391 ) ) ;
#202605=CARTESIAN_POINT ( 'NONE',  ( 4.446650332099550518, 0.5718123500428309303, 2.084546224624775679 ) ) ;
#202607=CARTESIAN_POINT ( 'NONE',  ( 6.532758020889952277, -1.641319963461195464, 0.8346263169811756200 ) ) ;
#202608=CARTESIAN_POINT ( 'NONE',  ( 2.729704159269104924, 0.7212915320151757070, -1.883313052590728454 ) ) ;
#202614=CARTESIAN_POINT ( 'NONE',  ( 2.008475284031425723, 1.387998011844304491, -1.254312187223500796 ) ) ;
#202615=CARTESIAN_POINT ( 'NONE',  ( 6.702032618711820433, -1.971027473680329045, 0.04818573739380492549 ) ) ;
#202619=CARTESIAN_POINT ( 'NONE',  ( 1.840723031453334935, 2.183200880077686978, 0.3216222850719457349 ) ) ;
#202625=CARTESIAN_POINT ( 'NONE',  ( 5.629747345311447937, -1.250075164085572954, -1.524477324586423377 ) ) ;
#202626=CARTESIAN_POINT ( 'NONE',  ( 6.322925365441865786, 2.150718969097795696, 0.8370602354567517889 ) ) ;
#202627=CARTESIAN_POINT ( 'NONE',  ( 0.5198770262540284293, 1.941052373433370448, -0.2841105942011297736 ) ) ;
#202628=CARTESIAN_POINT ( 'NONE',  ( 3.748931555198372845, -0.3975983499134613242, -2.023727603370987449 ) ) ;
#202637=CARTESIAN_POINT ( 'NONE',  ( 5.951682048281027981, 1.640226396406889942, 1.422642917226999426 ) ) ;
#202639=CARTESIAN_POINT ( 'NONE',  ( 4.985823801847525161, -1.827980399782932697, -0.2200341325891697619 ) ) ;
#202642=CARTESIAN_POINT ( 'NONE',  ( 0.6142526126209288950, 1.294576594435635108, -1.350420462534522859 ) ) ;
#202648=CARTESIAN_POINT ( 'NONE',  ( 2.324752472428833983, -0.002986221762550990942, 1.770032028303660576 ) ) ;
#202650=CARTESIAN_POINT ( 'NONE',  ( 6.164703283132928924, 0.6335332109005767931, 1.910856914995302303 ) ) ;
#202652=CARTESIAN_POINT ( 'NONE',  ( 4.534732036847580083, -1.536008458380673458, 1.144414559590371638 ) ) ;
#202654=CARTESIAN_POINT ( 'NONE',  ( 5.564895475732142494, 1.492515675241333772, -1.285245034736775649 ) ) ;
#202655=CARTESIAN_POINT ( 'NONE',  ( 0.1059362375676886209, 1.575662574916199210, 1.419458935296296520 ) ) ;
#202657=CARTESIAN_POINT ( 'NONE',  ( 3.063207453921251489, 0.2760179531714930246, -1.850060308400132358 ) ) ;
#202658=CARTESIAN_POINT ( 'NONE',  ( 6.463511695382619493, 0.2867160277617316622, -1.700725516685620553 ) ) ;
#202660=CARTESIAN_POINT ( 'NONE',  ( 3.545738602337618506, -1.670889076328873069, -1.441789439710974063 ) ) ;
#202662=CARTESIAN_POINT ( 'NONE',  ( 0.3618804954101816906, -0.5516051106895186740, 1.987472385349927428 ) ) ;
#202671=CARTESIAN_POINT ( 'NONE',  ( 2.787621587699981696, -1.932700977737045633, 0.7428295258242522126 ) ) ;
#202675=CARTESIAN_POINT ( 'NONE',  ( 1.102219918440990876, -0.9059408578524772437, 1.805149201161629025 ) ) ;
#202680=CARTESIAN_POINT ( 'NONE',  ( 0.1747926744264677590, 2.047238405490480861, -2.272669950590770149 ) ) ;
#202682=CARTESIAN_POINT ( 'NONE',  ( 6.098982473628085543, 0.9961464269193781584, -1.752763620266280187 ) ) ;
#202683=CARTESIAN_POINT ( 'NONE',  ( 6.227746030346171580, 0.7262518248569529433, -1.772935525165220128 ) ) ;
#202685=CARTESIAN_POINT ( 'NONE',  ( 3.456733517523990606, -1.933646301634945885, -1.031433503814835007 ) ) ;
#202687=CARTESIAN_POINT ( 'NONE',  ( 2.513799616133075343, -0.5961229146635020903, 1.817204401178821760 ) ) ;
#202691=CARTESIAN_POINT ( 'NONE',  ( 1.230092461119953517, 2.014234866427236259, 0.09611455020034495589 ) ) ;
#202693=CARTESIAN_POINT ( 'NONE',  ( 6.146043800834426918, 0.6857851511376764631, 2.081541312870714311 ) ) ;
#202695=CARTESIAN_POINT ( 'NONE',  ( 3.276077977556953513, -1.028358954114884094, 1.384488693430762085 ) ) ;
#202697=CARTESIAN_POINT ( 'NONE',  ( 0.1394461523057137220, 2.891244824116427470, -2.208899952336295325 ) ) ;
#202701=CARTESIAN_POINT ( 'NONE',  ( 0.9769180011504545735, 1.811320799089161993, 0.7541596914439269161 ) ) ;
#202704=CARTESIAN_POINT ( 'NONE',  ( 0.1399997263886037790, 2.025166351305721868, -2.415484119839182320 ) ) ;
#202707=CARTESIAN_POINT ( 'NONE',  ( 4.266123773889715309, 1.810994338341217480, -0.04873877536224096446 ) ) ;
#202711=CARTESIAN_POINT ( 'NONE',  ( 4.617698128633199062, -0.4785133679615029556, 1.747060762061508621 ) ) ;
#202715=CARTESIAN_POINT ( 'NONE',  ( 5.529708137783917898, 1.793509118821761561, -0.4966223845426844252 ) ) ;
#202717=CARTESIAN_POINT ( 'NONE',  ( 2.530754833220005384, -1.591195339209892312, 1.066270812275710966 ) ) ;
#202725=CARTESIAN_POINT ( 'NONE',  ( 1.166094707548096965, -1.325134400199390550, 1.617025002462493921 ) ) ;
#202727=CARTESIAN_POINT ( 'NONE',  ( 6.018570082959111112, 1.293320673360508488, -1.427839425051903532 ) ) ;
#202729=CARTESIAN_POINT ( 'NONE',  ( 2.959763373685084353, 1.816946311034864703, -0.1772020141349931188 ) ) ;
#202731=CARTESIAN_POINT ( 'NONE',  ( 2.250135261179100343, 0.8981609309555339538, -1.688322754368525747 ) ) ;
#202733=CARTESIAN_POINT ( 'NONE',  ( 1.328490337915340991, -1.252144239891037403, 1.520259730874585768 ) ) ;
#202734=CARTESIAN_POINT ( 'NONE',  ( 3.368632357871951033, 0.04486925901568206143, -1.941695523777670740 ) ) ;
#202739=CARTESIAN_POINT ( 'NONE',  ( 4.412424163657523657, -2.120181911468725033, -0.04909571644767100895 ) ) ;
#202746=CARTESIAN_POINT ( 'NONE',  ( 4.178209475066913647, -1.049361115903378883, 1.493786327181771068 ) ) ;
#202747=CARTESIAN_POINT ( 'NONE',  ( 0.1861046438572169226, -1.272802160389638892, -1.633586439835111648 ) ) ;
#202751=CARTESIAN_POINT ( 'NONE',  ( 4.926551758443064699, 1.790249073151507497, 0.5424879929923772659 ) ) ;
#202753=CARTESIAN_POINT ( 'NONE',  ( 2.596214140771450296, -1.921342217666447860, -0.1417109463846803752 ) ) ;
#202761=CARTESIAN_POINT ( 'NONE',  ( 1.599367111750239934, -0.2554771505851380908, 2.101684664062503316 ) ) ;
#202764=CARTESIAN_POINT ( 'NONE',  ( 4.891501605334720004, -1.894957309059261297, 0.8341102180390786991 ) ) ;
#202765=CARTESIAN_POINT ( 'NONE',  ( 0.6613494997313728030, 0.9071737413179328247, 1.602200521169500957 ) ) ;
#202768=CARTESIAN_POINT ( 'NONE',  ( 5.906922434318937931, -1.273882657197453305, -1.913274281643152941 ) ) ;
#202772=CARTESIAN_POINT ( 'NONE',  ( 1.183963288966838334, -1.026766722195756376, 2.049517438521175183 ) ) ;
#202775=CARTESIAN_POINT ( 'NONE',  ( 6.087830645824786835, -1.932811661901209010, -0.1881662411436606785 ) ) ;
#202779=CARTESIAN_POINT ( 'NONE',  ( 6.486579876843341808, -1.171037552013409089, 1.512559164390047783 ) ) ;
#202780=CARTESIAN_POINT ( 'NONE',  ( 0.1335669894368500532, -0.0009366757763962071850, -2.153671288142432694 ) ) ;
#202785=CARTESIAN_POINT ( 'NONE',  ( 3.046908718545093819, -1.709425224762064266, -1.203301715110078662 ) ) ;
#202786=CARTESIAN_POINT ( 'NONE',  ( 1.568863545881917343, 0.1344791104000986337, -1.764800092583326929 ) ) ;
#202789=CARTESIAN_POINT ( 'NONE',  ( 3.978722188455630082, -0.2232912938500397904, -2.281366727860510313 ) ) ;
#202790=CARTESIAN_POINT ( 'NONE',  ( 3.011345489304529277, -0.8582029173807427247, -1.513924679874333767 ) ) ;
#202793=CARTESIAN_POINT ( 'NONE',  ( 3.374086008222790589, -0.3405263371191130095, 1.699849027820112823 ) ) ;
#202794=CARTESIAN_POINT ( 'NONE',  ( 3.385384905382606391, 0.05040654291960967176, 2.170743301239473233 ) ) ;
#202796=CARTESIAN_POINT ( 'NONE',  ( 5.102750050473856547, 1.865045247124358818, 0.7672954931761333253 ) ) ;
#202797=CARTESIAN_POINT ( 'NONE',  ( 2.406250000000001776, 1.895863743164033277, -0.7852924748301132185 ) ) ;
#202800=CARTESIAN_POINT ( 'NONE',  ( 0.9383530073892000223, 1.897354475554638320, 0.3323884044314562858 ) ) ;
#202802=CARTESIAN_POINT ( 'NONE',  ( 3.990652734535464319, -1.277060150153148221, 1.817470393784472948 ) ) ;
#202804=CARTESIAN_POINT ( 'NONE',  ( 6.883263157960364254, 2.447565407927353220, 2.329071302269662080 ) ) ;
#202809=CARTESIAN_POINT ( 'NONE',  ( 0.9970955524637573619, -2.168350899310825586, -0.4814931055744512411 ) ) ;
#202810=CARTESIAN_POINT ( 'NONE',  ( 5.424254290899477304, 0.9654600744411747648, 1.707767180430696641 ) ) ;
#202813=CARTESIAN_POINT ( 'NONE',  ( 0.5444778865218368180, 2.155786741090206959, 0.1595364878888144988 ) ) ;
#202815=CARTESIAN_POINT ( 'NONE',  ( 3.350102204537624306, -0.8385132117052511713, 1.884735577694598430 ) ) ;
#202819=CARTESIAN_POINT ( 'NONE',  ( 4.551927186349598031, 1.870183863439809357, -0.04390777100237578529 ) ) ;
#202820=CARTESIAN_POINT ( 'NONE',  ( 3.850049338483009009, 0.2070581644968480517, -1.721641829124469059 ) ) ;
#202821=CARTESIAN_POINT ( 'NONE',  ( 3.104748464929545371, -0.3365338927540823533, 1.707397895346264738 ) ) ;
#202822=CARTESIAN_POINT ( 'NONE',  ( 1.277341847617214476, 2.115720621435190907, -0.8829085993839781432 ) ) ;
#202824=CARTESIAN_POINT ( 'NONE',  ( 4.669523271137602904, 1.205110262999141701, 1.708276167780866661 ) ) ;
#202825=CARTESIAN_POINT ( 'NONE',  ( 0.4976878544296211015, -0.6176706345307936274, -1.734562967469073236 ) ) ;
#202828=CARTESIAN_POINT ( 'NONE',  ( 1.705704151892040832, 1.882474636155605507, 0.7231385473688843879 ) ) ;
#202833=CARTESIAN_POINT ( 'NONE',  ( 2.649219347560148208, 0.2619616101627724736, 2.104190563435456518 ) ) ;
#202835=CARTESIAN_POINT ( 'NONE',  ( 5.865807274569020180, 1.797851641234180509, -0.3166982042408575948 ) ) ;
#202842=CARTESIAN_POINT ( 'NONE',  ( 1.898700399197379651, -1.981625571768164340, -0.3898374508689693152 ) ) ;
#202843=CARTESIAN_POINT ( 'NONE',  ( 0.1300960903409088820, -1.296115720595720333, -1.660425602283533308 ) ) ;
#202845=CARTESIAN_POINT ( 'NONE',  ( 4.574962676454192412, 1.700228875758927671, 0.7569903647998057483 ) ) ;
#202851=CARTESIAN_POINT ( 'NONE',  ( 4.793472150574508817, 1.354911484294840429, 1.223852735664505698 ) ) ;
#202855=CARTESIAN_POINT ( 'NONE',  ( 0.5613444508567478897, 1.446164810419462432, -0.9560955100236142590 ) ) ;
#202856=CARTESIAN_POINT ( 'NONE',  ( 0.04040834310030903126, -1.341606091951352164, -1.108378290077848494 ) ) ;
#202857=CARTESIAN_POINT ( 'NONE',  ( 4.987122935671228774, -0.2785958505117277495, -2.290767236937583995 ) ) ;
#202859=CARTESIAN_POINT ( 'NONE',  ( 1.264995835974036975, -1.861883480270887903, -0.8836341380922418942 ) ) ;
#202862=CARTESIAN_POINT ( 'NONE',  ( 0.5267199648841465187, 1.994564833640038781, -0.2930222482238133419 ) ) ;
#202865=CARTESIAN_POINT ( 'NONE',  ( 5.594569530875262764, -0.4557361262383100020, -1.814172972432124720 ) ) ;
#202866=CARTESIAN_POINT ( 'NONE',  ( 3.832203377193269755, -0.9874410831685247469, -1.637625244210038300 ) ) ;
#202868=CARTESIAN_POINT ( 'NONE',  ( 4.547634279845023109, -1.704780727694398479, -1.401453192282381188 ) ) ;
#202873=CARTESIAN_POINT ( 'NONE',  ( 6.024112365460934981, -2.104525519549589330, 0.2592714029671301934 ) ) ;
#202875=CARTESIAN_POINT ( 'NONE',  ( 3.751255533806226339, -1.888273344036644819, 1.326175916821286105 ) ) ;
#202876=CARTESIAN_POINT ( 'NONE',  ( 3.560947883890089649, 1.548132398191165882, -1.204989647596923508 ) ) ;
#202878=CARTESIAN_POINT ( 'NONE',  ( 1.059338230090471011, 1.600537254139059673, 1.134074526779847769 ) ) ;
#202882=CARTESIAN_POINT ( 'NONE',  ( 5.911342272548038679, -1.897112096406332382, 0.6839327336411115121 ) ) ;
#202885=CARTESIAN_POINT ( 'NONE',  ( 2.694371920525945097, 1.027083080403013993, -1.912793749723267211 ) ) ;
#202888=CARTESIAN_POINT ( 'NONE',  ( 1.019968326173793960, -0.5097545255977399270, 2.058319881341897695 ) ) ;
#202894=CARTESIAN_POINT ( 'NONE',  ( 0.5618817370758311114, 2.038728707766800596, -0.2996719410968719521 ) ) ;
#202896=CARTESIAN_POINT ( 'NONE',  ( 6.827182134110195477, 7.052946558436035573, 2.509100386683714490 ) ) ;
#202900=VERTEX_POINT ( 'NONE', #176693 ) ;
#202901=CARTESIAN_POINT ( 'NONE',  ( 4.723256143441832755, 1.665581346147155806, 0.9393396248940298898 ) ) ;
#202902=CARTESIAN_POINT ( 'NONE',  ( 5.207753166488873653, -1.761066459785052274, 0.1758167199723305041 ) ) ;
#202905=CARTESIAN_POINT ( 'NONE',  ( -0.05289022600267567070, -1.656485410061825592, 0.7338673832079073422 ) ) ;
#202908=CARTESIAN_POINT ( 'NONE',  ( 1.376049117821566137, -1.906831126389372022, -0.1839060664316337634 ) ) ;
#202909=CARTESIAN_POINT ( 'NONE',  ( 1.943885480841448965, 1.426152643941134501, 1.501071833787496645 ) ) ;
#202911=CARTESIAN_POINT ( 'NONE',  ( 0.2507688454781953902, -1.584965806562924628, 1.172240258958085146 ) ) ;
#202912=CARTESIAN_POINT ( 'NONE',  ( 2.631258204695927194, -1.703542010001803275, 0.6570300758180421807 ) ) ;
#202913=CARTESIAN_POINT ( 'NONE',  ( 0.5754005350990994971, -2.174928102591418888, -0.7718245971977951703 ) ) ;
#202917=CARTESIAN_POINT ( 'NONE',  ( 4.580570881008502404, 1.271380961112581032, -1.624167499240388057 ) ) ;
#202922=CARTESIAN_POINT ( 'NONE',  ( 5.508848719172433128, 1.596710022150628294, -1.373279487321391379 ) ) ;
#202926=CARTESIAN_POINT ( 'NONE',  ( 6.268043187460373922, -2.055199631210803624, 0.2494731385529954104 ) ) ;
#202928=CARTESIAN_POINT ( 'NONE',  ( 4.077527805175058973, 2.036875575534887961, -0.7240464584713502960 ) ) ;
#202929=CARTESIAN_POINT ( 'NONE',  ( 4.072919328976184694, -1.495020084728536203, 1.358112258667160344 ) ) ;
#202934=CARTESIAN_POINT ( 'NONE',  ( 2.624232735793774030, 2.001858099149746550, 0.2420302859193757539 ) ) ;
#202939=CARTESIAN_POINT ( 'NONE',  ( 5.308822938259078583, -0.4706598425541131947, -1.853433239416848677 ) ) ;
#202942=CARTESIAN_POINT ( 'NONE',  ( 4.200796113533305842, 1.844717850457804120, 0.8146114232021259838 ) ) ;
#202945=CARTESIAN_POINT ( 'NONE',  ( 6.827182134110228340, 0.006757161851634120239, 1.710856279483467191 ) ) ;
#202950=CARTESIAN_POINT ( 'NONE',  ( 5.747288119592351308, -1.474170506619469023, -1.151262835514428540 ) ) ;
#202951=CARTESIAN_POINT ( 'NONE',  ( 6.310797300923185915, -0.5409384057308598281, -1.939081195975641769 ) ) ;
#202954=CARTESIAN_POINT ( 'NONE',  ( 1.903268718874175480, -1.751121435885591548, 1.104011288380807532 ) ) ;
#202958=CARTESIAN_POINT ( 'NONE',  ( 0.7554827284574801016, 1.942536278707338360, -0.5405140857882018146 ) ) ;
#202959=CARTESIAN_POINT ( 'NONE',  ( 1.001899194773261170, -0.8131845483106721062, 1.618847804792804324 ) ) ;
#202966=CARTESIAN_POINT ( 'NONE',  ( 6.081633583971849610, -0.6405020660514448849, 1.805506905929341821 ) ) ;
#202973=CARTESIAN_POINT ( 'NONE',  ( 3.362350911093567873, 0.9703303321016673033, 1.931748911306984784 ) ) ;
#202976=CARTESIAN_POINT ( 'NONE',  ( 0.8793290508635929204, -1.919567575575848339, -0.9014759086384204201 ) ) ;
#202977=CARTESIAN_POINT ( 'NONE',  ( 6.194357462883205656, -1.817092693925309810, -0.1759843941628037312 ) ) ;
#202978=CARTESIAN_POINT ( 'NONE',  ( 1.809780422520257170, -1.956919260803160032, 0.2374922769308157044 ) ) ;
#202979=CARTESIAN_POINT ( 'NONE',  ( 5.133030909251353968, 1.769313487831367659, 0.7262901588861517821 ) ) ;
#202981=PLANE ( 'NONE',  #163525 ) ;
#202982=CARTESIAN_POINT ( 'NONE',  ( 5.336368261742150843, -1.095693791129894956, 1.636418990172120003 ) ) ;
#202983=CARTESIAN_POINT ( 'NONE',  ( 0.4627034902389154936, 0.1913720229725413835, -1.932491135362510715 ) ) ;
#202991=CARTESIAN_POINT ( 'NONE',  ( 5.057238878282278804, -1.638088962530854786, 0.9864336689310859718 ) ) ;
#202993=CARTESIAN_POINT ( 'NONE',  ( 1.378255502416311895, 1.315327575222959622, 1.771799650011764538 ) ) ;
#202995=CARTESIAN_POINT ( 'NONE',  ( 6.094395157121155648, -1.075028013068216604, 1.701836141867618446 ) ) ;
#202998=DIRECTION ( 'NONE',  ( 1.908195823574487804E-17, 1.000000000000000000, -3.097714438736600596E-15 ) ) ;
#202999=CARTESIAN_POINT ( 'NONE',  ( 2.523957353938070192, 2.030885678308389952, -0.4015143504868187718 ) ) ;
#203003=CARTESIAN_POINT ( 'NONE',  ( 0.1984014031938194922, -2.161264429664040421, -0.05129915172277095536 ) ) ;
#203008=CARTESIAN_POINT ( 'NONE',  ( 6.925078400183546812, 3.702220002068328242, 2.370079373711677206 ) ) ;
#203010=CARTESIAN_POINT ( 'NONE',  ( 5.432138663567621428, -1.371958567392589146, -1.060553414760868618 ) ) ;
#203012=CARTESIAN_POINT ( 'NONE',  ( 3.098552089154332556, 2.054082100768514607, 0.2579794602402472603 ) ) ;
#203013=CARTESIAN_POINT ( 'NONE',  ( 4.288735948182021751, 1.635604132441673020, -1.344385869115312770 ) ) ;
#203016=CARTESIAN_POINT ( 'NONE',  ( 2.817198160248539196, -1.711224680871022086, -0.9748066430285988737 ) ) ;
#203017=CARTESIAN_POINT ( 'NONE',  ( 0.5625819312903357350, 0.5574351770905332515, 1.829310545699929458 ) ) ;
#203018=CARTESIAN_POINT ( 'NONE',  ( 5.085981902069889315, -2.274473487728204013, -0.2844877896996683142 ) ) ;
#203019=CARTESIAN_POINT ( 'NONE',  ( 1.875362892791394787, 1.747422460009705913, -0.5287960245906262458 ) ) ;
#203023=CARTESIAN_POINT ( 'NONE',  ( 2.373293634344127767, -1.753592693251155632, -0.9887173157705446691 ) ) ;
#203024=CARTESIAN_POINT ( 'NONE',  ( 3.678520109711844732, 1.247982904293298168, -1.513573691770610186 ) ) ;
#203028=CARTESIAN_POINT ( 'NONE',  ( 0.07556134207192634344, 1.307170157424314638, -2.493659143521540500 ) ) ;
#203029=CARTESIAN_POINT ( 'NONE',  ( 6.105435528804215473, -2.075010666747591159, 0.2545828925317530911 ) ) ;
#203030=CARTESIAN_POINT ( 'NONE',  ( 5.102326758870145973, -0.5985492928855026262, -1.665706573615277852 ) ) ;
#203032=CARTESIAN_POINT ( 'NONE',  ( 1.289316216709124996, 1.661312375189183399, 1.429258102917586815 ) ) ;
#203033=CARTESIAN_POINT ( 'NONE',  ( 6.456985410506528744, 0.2896317775202154610, -1.715898445072817413 ) ) ;
#203036=CARTESIAN_POINT ( 'NONE',  ( 0.3866022076702098076, -0.1098403002397010941, 2.295889243394435564 ) ) ;
#203037=CARTESIAN_POINT ( 'NONE',  ( -0.005964567173097347699, -2.191213315851054944, -0.04726126812268362232 ) ) ;
#203038=CARTESIAN_POINT ( 'NONE',  ( 6.380242484794338864, -0.2077342984398328762, 1.721287130621736772 ) ) ;
#203039=CARTESIAN_POINT ( 'NONE',  ( 2.842613246588860942, 2.190307313262893185, 0.2694104812042824038 ) ) ;
#203040=CARTESIAN_POINT ( 'NONE',  ( 0.3741910912563637948, -2.129432730031981080, 0.4223156635175562279 ) ) ;
#203042=CARTESIAN_POINT ( 'NONE',  ( 1.059931528796464129, 1.266109226500349960, 1.696929307225014449 ) ) ;
#203043=CARTESIAN_POINT ( 'NONE',  ( 3.375000000000002665, 2.052068128417946724, -1.927395870058053847E-13 ) ) ;
#203044=CARTESIAN_POINT ( 'NONE',  ( 6.827182134110194589, 2.412578537245218424, 2.569476350730160785 ) ) ;
#203045=CARTESIAN_POINT ( 'NONE',  ( 5.754890659886483739, -1.518548266084504439, 1.185242666505934572 ) ) ;
#203046=ORIENTED_EDGE ( 'NONE', *, *, #83250, .F. ) ;
#203047=CARTESIAN_POINT ( 'NONE',  ( 1.962814135067984411, -2.097685689255949448, -0.9248770880663819138 ) ) ;
#203051=CARTESIAN_POINT ( 'NONE',  ( 3.176664282717697851, 1.000473465829452735, 1.983322933999843052 ) ) ;
#203058=CARTESIAN_POINT ( 'NONE',  ( 1.424454163599726320, -1.462446849824734274, -1.388484543128357229 ) ) ;
#203060=CARTESIAN_POINT ( 'NONE',  ( 6.268047042621852860, -2.047536660891946525, 0.2488583125946699504 ) ) ;
#203062=CARTESIAN_POINT ( 'NONE',  ( 6.022986557963563747, -1.635662919198093812, 0.5951793741951169059 ) ) ;
#203065=CARTESIAN_POINT ( 'NONE',  ( 1.580939025779507956, 1.637719487297364163, -0.6712238910871449749 ) ) ;
#203066=CARTESIAN_POINT ( 'NONE',  ( -0.01695367945527340853, -2.016028864686558730, -0.04667425414178058563 ) ) ;
#203067=CARTESIAN_POINT ( 'NONE',  ( 6.444851825500396814, -1.403812859381381895, -1.028626497576446086 ) ) ;
#203068=CARTESIAN_POINT ( 'NONE',  ( 4.687240393977892161, 1.697883010200517129, 1.540384229137826466 ) ) ;
#203069=CARTESIAN_POINT ( 'NONE',  ( 3.503688343963583307, -0.7473321665184139428, -1.682825604429179833 ) ) ;
#203072=CARTESIAN_POINT ( 'NONE',  ( 3.786012796616508247, -0.9002957760516903107, 1.588078298607284111 ) ) ;
#203073=CARTESIAN_POINT ( 'NONE',  ( 4.799454022740247794, 1.388487131293577592, -1.462444391756134943 ) ) ;
#203075=CARTESIAN_POINT ( 'NONE',  ( 3.643696890507712283, -1.711652922788420739, -1.479685619365896265 ) ) ;
#203077=CARTESIAN_POINT ( 'NONE',  ( 6.563511373971260277, 0.3638278135829931537, -2.074131770586047363 ) ) ;
#203078=CARTESIAN_POINT ( 'NONE',  ( 3.877443546529443452, -0.1552652338182025915, 2.064615508632794860 ) ) ;
#203081=CARTESIAN_POINT ( 'NONE',  ( 5.654972079148370412, 0.4136758123431219514, 2.079573305287989893 ) ) ;
#203083=CARTESIAN_POINT ( 'NONE',  ( 1.699704897782030377, -0.6493637136964022227, 1.813892859743936103 ) ) ;
#203086=CARTESIAN_POINT ( 'NONE',  ( 6.737161338948785883, -0.09310609838950174855, -1.967343120315911298 ) ) ;
#203091=CARTESIAN_POINT ( 'NONE',  ( 0.4225341819744453664, -2.209939313495157265, 0.2258247597332131984 ) ) ;
#203092=CARTESIAN_POINT ( 'NONE',  ( 2.995255089933103854, 1.807040913553149997, -1.081249443666182808 ) ) ;
#203095=CARTESIAN_POINT ( 'NONE',  ( 0.8361097980106885208, -1.038377568841988063, 1.544222109484013172 ) ) ;
#203100=CARTESIAN_POINT ( 'NONE',  ( 1.178162429063234207, 2.088287186665960693, -0.3679680078583212333 ) ) ;
#203103=CARTESIAN_POINT ( 'NONE',  ( 3.314850587115983238, -1.487306837207631238, 1.279512770686676681 ) ) ;
#203104=CARTESIAN_POINT ( 'NONE',  ( 1.885829143180400624, 1.490600019384461072, 1.565824011241300440 ) ) ;
#203105=CARTESIAN_POINT ( 'NONE',  ( 1.259045258496578557, 1.813921241667546758, -0.3151448728593714277 ) ) ;
#203109=CARTESIAN_POINT ( 'NONE',  ( 3.995860056160570384, -0.5486252962480555606, -1.651658045138884257 ) ) ;
#203115=CARTESIAN_POINT ( 'NONE',  ( 0.5675189469334164238, 0.2105291993744831114, -2.151437729447757796 ) ) ;
#203117=CARTESIAN_POINT ( 'NONE',  ( 3.391953724946984661, 0.04666865176591524639, 2.015725201127672506 ) ) ;
#203120=CARTESIAN_POINT ( 'NONE',  ( 3.643400374902918681, -1.492087795311855425, -1.288628176122036839 ) ) ;
#203121=CARTESIAN_POINT ( 'NONE',  ( 6.509000000000037645, 2.054060622569788386, 2.307050226316338382 ) ) ;
#203122=CARTESIAN_POINT ( 'NONE',  ( 2.647912457843327960, 0.6564901929842799078, 1.827849683178353057 ) ) ;
#203128=CARTESIAN_POINT ( 'NONE',  ( -0.2106854629475425067, 4.089057744811007922, -2.552070079120628776 ) ) ;
#203134=CARTESIAN_POINT ( 'NONE',  ( 0.2005908178989434243, -2.206344910233990486, -0.05143828380192031619 ) ) ;
#203136=CARTESIAN_POINT ( 'NONE',  ( 4.539869136473917877, 1.278287603951251183, 1.488235606430035274 ) ) ;
#203138=CARTESIAN_POINT ( 'NONE',  ( 2.074842474778653578, -0.8596299393073092432, 1.824119475507138821 ) ) ;
#203140=CARTESIAN_POINT ( 'NONE',  ( 2.290374991995058895, -0.8151648431981967091, -1.954327666539334762 ) ) ;
#203144=CARTESIAN_POINT ( 'NONE',  ( 3.116968920156853340, -1.774181764490849744, 0.4917334186493869108 ) ) ;
#203148=CARTESIAN_POINT ( 'NONE',  ( 4.113620189327307664, 1.705085180707970771, 1.260635662952174663 ) ) ;
#203151=CARTESIAN_POINT ( 'NONE',  ( 4.569639033146696505, 1.999850647628642175, -0.4969485059727016263 ) ) ;
#203153=CARTESIAN_POINT ( 'NONE',  ( 2.138008341990283778, 0.4048980806483238326, 1.796005048712509655 ) ) ;
#203159=CARTESIAN_POINT ( 'NONE',  ( 2.174722684859807575, -1.356406721008751814, 1.740749382485320407 ) ) ;
#203160=CARTESIAN_POINT ( 'NONE',  ( 3.216390312923810502, -1.112095606969863759, -1.970117241612897363 ) ) ;
#203162=CARTESIAN_POINT ( 'NONE',  ( 4.043061577595566725, 0.09493798274137112136, 1.809245059475625750 ) ) ;
#203163=CARTESIAN_POINT ( 'NONE',  ( 3.889770295363860431, -1.910208526776317806, 0.1464741861031873538 ) ) ;
#203164=CARTESIAN_POINT ( 'NONE',  ( 5.652806998763869828, -0.4994405740583847675, -2.009109930559597856 ) ) ;
#203166=CARTESIAN_POINT ( 'NONE',  ( 3.555508008102294060, 0.4801912113073670829, -1.911968381370426684 ) ) ;
#203167=CARTESIAN_POINT ( 'NONE',  ( 1.131717742382963632, -1.219707097817297692, -1.491085513105432581 ) ) ;
#203168=CARTESIAN_POINT ( 'NONE',  ( 3.696050037196423332, -1.868490534004090931, -0.09263902202472777681 ) ) ;
#203169=CARTESIAN_POINT ( 'NONE',  ( 3.088805445243738568, -2.273621702497233166, -0.3942619731671925254 ) ) ;
#203170=CARTESIAN_POINT ( 'NONE',  ( 4.721077684499490168, -1.662108436276054091, -0.8373904101051653504 ) ) ;
#203173=CARTESIAN_POINT ( 'NONE',  ( 1.717544045074904213, -0.2563126921724939167, 2.090340884163774948 ) ) ;
#203179=CARTESIAN_POINT ( 'NONE',  ( 0.6506561817731060238, 1.990614601344290691, 0.3409984238087642727 ) ) ;
#203185=CARTESIAN_POINT ( 'NONE',  ( 1.616726252867954683, 1.452999108549270169, -1.600537328674697779 ) ) ;
#203186=CARTESIAN_POINT ( 'NONE',  ( 6.610000000000001208, 3.709748940453510446, 2.234587373521100151 ) ) ;
#203188=CARTESIAN_POINT ( 'NONE',  ( 6.825078400183584471, 2.055285645424239416, 2.261848697290469445 ) ) ;
#203191=CARTESIAN_POINT ( 'NONE',  ( 5.594935472981866553, 1.780666063871166882, 0.9463038388278843804 ) ) ;
#203193=CARTESIAN_POINT ( 'NONE',  ( 6.427293192253748622, -1.366186911818557226, -1.582700853868714397 ) ) ;
#203195=CARTESIAN_POINT ( 'NONE',  ( 0.6732104281652334654, -2.131434628316424273, -0.7592435237872022791 ) ) ;
#203202=CARTESIAN_POINT ( 'NONE',  ( 2.508071618744921238, -0.6595455166902574051, -1.594007932167235131 ) ) ;
#203204=CARTESIAN_POINT ( 'NONE',  ( 2.389615768203833479, -0.7611923103308501082, 1.597832513397597021 ) ) ;
#203205=CARTESIAN_POINT ( 'NONE',  ( 2.649090073008007362, 0.2487567141898557876, 1.997615136964459470 ) ) ;
#203206=CARTESIAN_POINT ( 'NONE',  ( 5.315527377757141458, -0.3284926246858720922, 2.182075488366498117 ) ) ;
#203208=CARTESIAN_POINT ( 'NONE',  ( 4.447524238883529435, -1.845004865869297905, 0.8223427699834483517 ) ) ;
#203210=CARTESIAN_POINT ( 'NONE',  ( 4.477262591527907176, -1.894555094343739476, -0.9525379817736513433 ) ) ;
#203211=CARTESIAN_POINT ( 'NONE',  ( 4.499625164952708367, -1.976952908697379607, 0.3961224619316304763 ) ) ;
#203212=CARTESIAN_POINT ( 'NONE',  ( 4.078215212670958323, 0.8593412415473808963, 1.594818892651229891 ) ) ;
#203217=CARTESIAN_POINT ( 'NONE',  ( 1.234984068473435670, -1.692697435815498919, 0.7966027930108382504 ) ) ;
#203219=CARTESIAN_POINT ( 'NONE',  ( 5.654893700716965732, 0.3597771647365927694, 1.775199357419085411 ) ) ;
#203225=CARTESIAN_POINT ( 'NONE',  ( 0.3164790345465406385, -0.6463921985436007489, -1.799943259716822341 ) ) ;
#203227=CARTESIAN_POINT ( 'NONE',  ( 2.260140581184489239, -1.961506502764579052, 0.04509734162668613960 ) ) ;
#203230=CARTESIAN_POINT ( 'NONE',  ( 4.271814301144261528, 0.4616217191124799002, -2.069597271375968273 ) ) ;
#203231=CARTESIAN_POINT ( 'NONE',  ( -0.02968770228137588424, 4.095675376368371090, -2.381331788581673159 ) ) ;
#203233=CARTESIAN_POINT ( 'NONE',  ( 5.325445421541009416, -1.872857986210634484, 0.6156230612282005410 ) ) ;
#203235=CARTESIAN_POINT ( 'NONE',  ( 1.230727935554910557, 1.348888731755660153, -1.494678444409401896 ) ) ;
#203237=CARTESIAN_POINT ( 'NONE',  ( 1.529080078018136390, -1.786526079506415288, 1.135962973836294854 ) ) ;
#203239=CARTESIAN_POINT ( 'NONE',  ( 2.242711981562468093, -2.029969483702593003, -0.4061203719310027549 ) ) ;
#203243=CARTESIAN_POINT ( 'NONE',  ( 4.277343952648727132, 1.365583793738689655, 1.583094835029410063 ) ) ;
#203245=CARTESIAN_POINT ( 'NONE',  ( 2.924607851032960504, 1.718362407962298333, 0.6167639819729958672 ) ) ;
#203246=CARTESIAN_POINT ( 'NONE',  ( 1.646807439477548707, 0.1776336960073976179, 1.802747333403993402 ) ) ;
#203248=CARTESIAN_POINT ( 'NONE',  ( 6.322910218073367616, 2.057572540570989261, 0.7984293639632376038 ) ) ;
#203250=CARTESIAN_POINT ( 'NONE',  ( 3.962124768131184638, 2.190450126196175074, -0.2673064950309556043 ) ) ;
#203253=CARTESIAN_POINT ( 'NONE',  ( 2.877492880751183257, 0.2784179829431778219, -1.891769048003589138 ) ) ;
#203257=CARTESIAN_POINT ( 'NONE',  ( 6.478973898625433492, 1.930320082341809629, 0.7489585856828018251 ) ) ;
#203259=CARTESIAN_POINT ( 'NONE',  ( 5.864808805604324604, 0.1626094438406736342, -2.185560445749204828 ) ) ;
#203264=CARTESIAN_POINT ( 'NONE',  ( 3.637841704585748293, 0.8437669887123750989, -1.669527271503386201 ) ) ;
#203269=CARTESIAN_POINT ( 'NONE',  ( 6.895378825052528526, -1.852007112603266670, 0.9253362530580526712 ) ) ;
#203270=CARTESIAN_POINT ( 'NONE',  ( 1.247672978039487734, 1.986097573956084439, -0.3474914183895366215 ) ) ;
#203273=CARTESIAN_POINT ( 'NONE',  ( 1.552940555598739891, -1.880887156831068552, -1.124362282834884263 ) ) ;
#203274=CARTESIAN_POINT ( 'NONE',  ( 6.709597972018079837, -0.3944863986210072060, 1.789098616620278470 ) ) ;
#203282=CARTESIAN_POINT ( 'NONE',  ( 3.860763913883006992, 0.2215400755124704024, -1.827792592973469743 ) ) ;
#203283=CARTESIAN_POINT ( 'NONE',  ( 0.9967404297962767501, -1.964529542677856622, -0.4388597091333420463 ) ) ;
#203284=CARTESIAN_POINT ( 'NONE',  ( 2.407932310410058285, 0.5022953597978959683, 2.242707597164790734 ) ) ;
#203286=CARTESIAN_POINT ( 'NONE',  ( 0.2680791809135505410, -0.7890318081985218113, -1.684091100025336463 ) ) ;
#203289=CARTESIAN_POINT ( 'NONE',  ( 3.797043250571481732, -0.1924442655423033721, -1.902711443722324258 ) ) ;
#203293=CARTESIAN_POINT ( 'NONE',  ( 2.384421550557855429, -0.3601958963256215451, -2.059324561056875336 ) ) ;
#203294=CARTESIAN_POINT ( 'NONE',  ( 0.8658264364783776479, 0.9185255527898968930, 1.629538061279064642 ) ) ;
#203295=CARTESIAN_POINT ( 'NONE',  ( 2.460314346279086628, 1.556669099887195484, 1.281166478716524670 ) ) ;
#203298=CARTESIAN_POINT ( 'NONE',  ( 3.684860642351639903, 1.263529365103865709, 1.197186439443503003 ) ) ;
#203301=CARTESIAN_POINT ( 'NONE',  ( 4.336358584672225902, 1.692218828317056278, 0.3330917469099390904 ) ) ;
#203302=CARTESIAN_POINT ( 'NONE',  ( 3.368858348882136422, 0.05182064297618373117, -2.191103300807801801 ) ) ;
#203303=CARTESIAN_POINT ( 'NONE',  ( 5.953802724510455668, 0.6443607167232848765, -2.110727517106169682 ) ) ;
#203305=CARTESIAN_POINT ( 'NONE',  ( 3.784171691162826701, -1.288926714175726129, -1.746948845794197958 ) ) ;
#203306=CARTESIAN_POINT ( 'NONE',  ( 2.719161800852238464, -0.1789327596440904167, 1.816892639718168390 ) ) ;
#203308=CARTESIAN_POINT ( 'NONE',  ( 4.891875743818586919, -2.106850654347144580, 0.2108507618673941542 ) ) ;
#203311=CARTESIAN_POINT ( 'NONE',  ( 4.757543194620796889, 2.267657608012829673, -0.3350592807548398722 ) ) ;
#203315=CARTESIAN_POINT ( 'NONE',  ( 0.5223349339509277822, -2.109880975928311031, 0.2119513895993754005 ) ) ;
#203319=CARTESIAN_POINT ( 'NONE',  ( 6.883263157960381129, 0.5832772681763243039, 2.006853359411898463 ) ) ;
#203321=CARTESIAN_POINT ( 'NONE',  ( 5.080704010962952211, -0.7231418808758652839, 1.882473355234378865 ) ) ;
#203323=CARTESIAN_POINT ( 'NONE',  ( 3.116140835343351956, 2.053043485406472080, -0.1977005638095686579 ) ) ;
#203327=CARTESIAN_POINT ( 'NONE',  ( 6.105464321129510097, -2.175355461714892691, 0.2646407054325700670 ) ) ;
#203328=CARTESIAN_POINT ( 'NONE',  ( 4.922500090287251773, -1.427935867408920645, -1.423962988533589158 ) ) ;
#203329=CARTESIAN_POINT ( 'NONE',  ( 3.772867777003403589, 1.732451475078290448, -0.6238847238279123797 ) ) ;
#203332=CARTESIAN_POINT ( 'NONE',  ( 0.8501349688851227437, 0.4944664728778884744, 1.652377535151504206 ) ) ;
#203334=CARTESIAN_POINT ( 'NONE',  ( 0.9502802867703894485, -2.080962668894706269, -0.9767702978288366200 ) ) ;
#203336=CARTESIAN_POINT ( 'NONE',  ( 0.6676899448993807162, 0.2205636587761065359, -2.251657551468993379 ) ) ;
#203337=CARTESIAN_POINT ( 'NONE',  ( 3.334694542603059642, 2.054772597177223936, 0.4612437286577449891 ) ) ;
#203341=CARTESIAN_POINT ( 'NONE',  ( 6.250000000000084377, 2.349784478886278158E-12, 2.052068128417940063 ) ) ;
#203347=CARTESIAN_POINT ( 'NONE',  ( 4.517978939158282969, -0.5908935252547321548, 2.141346583060988351 ) ) ;
#203348=CARTESIAN_POINT ( 'NONE',  ( 2.695491272475036837, -0.6865090956127660737, 2.081212476921667776 ) ) ;
#203352=CARTESIAN_POINT ( 'NONE',  ( 5.230891786122516152, -1.846674803186045821, -0.6626716404555529349 ) ) ;
#203354=CARTESIAN_POINT ( 'NONE',  ( 6.609999999999995879, 0.01081285896096205283, 1.720159828161060833 ) ) ;
#203358=CARTESIAN_POINT ( 'NONE',  ( 4.465154236216789307, -1.701427117168831549, 1.265499569954648962 ) ) ;
#203361=CARTESIAN_POINT ( 'NONE',  ( 5.102478102407745908, -0.7247817745383768884, -2.036717088958202471 ) ) ;
#203363=CARTESIAN_POINT ( 'NONE',  ( 5.478019777291557979, -1.797689181224306321, -0.3974485807837144224 ) ) ;
#203366=CARTESIAN_POINT ( 'NONE',  ( 6.404260164931634414, 1.284261220195097808, -1.174706115135275342 ) ) ;
#203369=CARTESIAN_POINT ( 'NONE',  ( 3.942369626403975147, 2.151062187213080623, 0.2142938780915065733 ) ) ;
#203374=CARTESIAN_POINT ( 'NONE',  ( 3.379894511112140787, 1.369989894601089775, 1.672159933133889442 ) ) ;
#203375=CARTESIAN_POINT ( 'NONE',  ( 4.552002736099131752, 1.970983365533407694, -0.04540313215006633318 ) ) ;
#203376=CARTESIAN_POINT ( 'NONE',  ( 3.778401656274816389, -1.708383637232064878, 0.2947856008331130040 ) ) ;
#203377=CARTESIAN_POINT ( 'NONE',  ( 0.9080814035550346386, -0.9900877184637231210, -1.955254813705724404 ) ) ;
#203378=CARTESIAN_POINT ( 'NONE',  ( 1.729934149615200312, -2.172323606337727142, 0.7788181121253530126 ) ) ;
#203379=CARTESIAN_POINT ( 'NONE',  ( 3.919256602636957076, -0.1552153454438681413, 2.055015938418188526 ) ) ;
#203380=CARTESIAN_POINT ( 'NONE',  ( 5.460475975554013317, -1.757383149004720924, -0.8268225932778446863 ) ) ;
#203386=CARTESIAN_POINT ( 'NONE',  ( 3.065657736429776126, 0.3252250816505456998, -2.182562984848686938 ) ) ;
#203389=CARTESIAN_POINT ( 'NONE',  ( 0.9361096364171941353, -1.039984170849604039, 1.543015978488631923 ) ) ;
#203390=CARTESIAN_POINT ( 'NONE',  ( -0.1290005225502675879, -0.006633637972621592160, -2.173875058097324064 ) ) ;
#203394=CARTESIAN_POINT ( 'NONE',  ( 6.386648935047418263, 1.599332519906123462, -0.9119682274050244786 ) ) ;
#203396=CARTESIAN_POINT ( 'NONE',  ( 2.694271958740936945, -2.055289539400024790, -0.1528356987768857700 ) ) ;
#203401=CARTESIAN_POINT ( 'NONE',  ( 1.903268112024224523, 1.712809940758196259, 1.145777703309367457 ) ) ;
#203408=CARTESIAN_POINT ( 'NONE',  ( 6.076841795016812320, -2.094286673724785164, -0.6961510500591641115 ) ) ;
#203409=CARTESIAN_POINT ( 'NONE',  ( 6.766858430912646938, -2.064281441484459023, -0.9263300772878214628 ) ) ;
#203411=CARTESIAN_POINT ( 'NONE',  ( 6.433875545303581411, -1.754733077360526972, 0.4498553729834730008 ) ) ;
#203412=CARTESIAN_POINT ( 'NONE',  ( 0.8136858238772455287, -1.282993010278702606, -1.555696519147983459 ) ) ;
#203416=CARTESIAN_POINT ( 'NONE',  ( 2.078771448894382701, -0.08914341469279044028, -1.868647664167771616 ) ) ;
#203417=CARTESIAN_POINT ( 'NONE',  ( 3.960172920142067898, -1.157100329752266621, 1.651342637023434090 ) ) ;
#203421=CARTESIAN_POINT ( 'NONE',  ( 5.408848747418643299, 1.595474064493606514, -1.374861248814135628 ) ) ;
#203422=EDGE_CURVE ( 'NONE', #139360, #113025, #136368, .T. ) ;
#203427=CARTESIAN_POINT ( 'NONE',  ( 3.709244008563481465, 1.704072514596865817, -1.083995235011512515 ) ) ;
#203430=CARTESIAN_POINT ( 'NONE',  ( 6.057095868330090838, 1.688466812627244185, -1.184547966247089912 ) ) ;
#203432=CARTESIAN_POINT ( 'NONE',  ( 5.114612887932482366, 1.494710344919391476, -1.561737693111686642 ) ) ;
#203438=CARTESIAN_POINT ( 'NONE',  ( 2.805323142837768291, -1.806386208845015995, 1.204286856753070456 ) ) ;
#203441=CARTESIAN_POINT ( 'NONE',  ( 1.663359199420410883, 0.9473472845980964729, 1.578708189602283873 ) ) ;
#203443=CARTESIAN_POINT ( 'NONE',  ( 3.509492838045696672, -2.158849082856160173, 0.3763758916049686487 ) ) ;
#203444=CARTESIAN_POINT ( 'NONE',  ( 6.883263157960358924, 7.052235917045241997, 2.651962373728885325 ) ) ;
#203445=CARTESIAN_POINT ( 'NONE',  ( 4.012777769421401963, 1.602246665114055002, -1.597678914196493771 ) ) ;
#203451=CARTESIAN_POINT ( 'NONE',  ( 5.852768638770064591, -1.394116391329143667, 1.090054309861036241 ) ) ;
#203452=CARTESIAN_POINT ( 'NONE',  ( 3.369792252087350892, 0.4868432662692974144, -1.953231169037449533 ) ) ;
#203454=CARTESIAN_POINT ( 'NONE',  ( 1.342952632442768302, 0.4104956981533373628, 2.065382446648211801 ) ) ;
#203457=CARTESIAN_POINT ( 'NONE',  ( 0.9066264771708797410, 0.5685364763899096729, 1.885722953041415906 ) ) ;
#203461=CARTESIAN_POINT ( 'NONE',  ( 5.572461477490294968, 0.7419763400571472989, 1.652881490725614189 ) ) ;
#203465=CARTESIAN_POINT ( 'NONE',  ( 4.451927283622527654, 1.870250842541102410, -0.04591718433973044494 ) ) ;
#203466=CARTESIAN_POINT ( 'NONE',  ( 5.067269747081383890, 1.798595138155818063, 1.025117745595036656 ) ) ;
#203478=CARTESIAN_POINT ( 'NONE',  ( 4.668382477721988444, -0.8370036265390871089, -1.774476930476886594 ) ) ;
#203480=CARTESIAN_POINT ( 'NONE',  ( 2.513045873335067792, 2.015604327017831654, 0.05229110803010170866 ) ) ;
#203482=CARTESIAN_POINT ( 'NONE',  ( -0.02351032182101517320, -2.127384168920816165, -0.5261613093957145937 ) ) ;
#203484=CARTESIAN_POINT ( 'NONE',  ( 2.460033746253722065, 0.7958763861501785275, 1.692906160045657860 ) ) ;
#203486=CARTESIAN_POINT ( 'NONE',  ( 4.552993993533384298, 0.3484205210483002357, 1.982688671860346252 ) ) ;
#203489=CARTESIAN_POINT ( 'NONE',  ( 4.025106843427800563, -1.841118617500647314, 1.045351873429276601 ) ) ;
#203491=CARTESIAN_POINT ( 'NONE',  ( 6.127406499145813257, 0.1562011534181114436, -2.064545280851529885 ) ) ;
#203492=CARTESIAN_POINT ( 'NONE',  ( 1.083664105429899216, -0.9366695517310281716, 1.869248094466950949 ) ) ;
#203493=CARTESIAN_POINT ( 'NONE',  ( 6.720655732516647163, 1.258879151752972048, 2.189434846530075252 ) ) ;
#203494=CARTESIAN_POINT ( 'NONE',  ( 0.08252656676070461994, -0.1270158569062987686, -1.696106202995291357 ) ) ;
#203503=CARTESIAN_POINT ( 'NONE',  ( 6.129550632656369125, -0.2293275368827427663, 1.898405681093485953 ) ) ;
#203511=CARTESIAN_POINT ( 'NONE',  ( 5.607046053289695742, -0.04666138757647777385, 2.016035322322209389 ) ) ;
#203518=CARTESIAN_POINT ( 'NONE',  ( 4.012523933672189180, 0.7048025691861439235, 1.839212210364450151 ) ) ;
#203519=CARTESIAN_POINT ( 'NONE',  ( 4.271111354109316416, 1.799915745204151429, -0.9091612155255476280 ) ) ;
#203522=CARTESIAN_POINT ( 'NONE',  ( 4.769572470968366673, 1.260305947291120221, 1.792593939366843303 ) ) ;
#203524=CARTESIAN_POINT ( 'NONE',  ( 3.680616551068579767, -1.856277683350136432, -0.5147254836462693550 ) ) ;
#203526=CARTESIAN_POINT ( 'NONE',  ( -0.1294898018152383368, 5.723764454335155349, -2.520545915250469893 ) ) ;
#203527=CARTESIAN_POINT ( 'NONE',  ( 0.4345545588612038101, 1.130843733186673639, -1.894998796914903139 ) ) ;
#203532=CARTESIAN_POINT ( 'NONE',  ( 4.768383308330760961, -0.8382467442454040185, -1.782262242837754807 ) ) ;
#203534=CARTESIAN_POINT ( 'NONE',  ( -0.02402099761080173090, -1.884047281740467872, -0.4708274727777494451 ) ) ;
#203535=CARTESIAN_POINT ( 'NONE',  ( 4.582685675920167512, -1.313125608480088635, 1.525959163679012187 ) ) ;
#203536=CARTESIAN_POINT ( 'NONE',  ( 5.255319057710332586, -2.280117823540278366, -0.2889680969316887893 ) ) ;
#203538=CARTESIAN_POINT ( 'NONE',  ( 3.133497910287503796, 1.768579976953125632, -0.5793101531420452588 ) ) ;
#203543=CARTESIAN_POINT ( 'NONE',  ( 6.321832389622432657, 1.203313566387714584, -1.709558936785739780 ) ) ;
#203548=CARTESIAN_POINT ( 'NONE',  ( 0.2756506080626683342, 1.048234779247591453, 1.494575289200591239 ) ) ;
#203552=CARTESIAN_POINT ( 'NONE',  ( 2.285452750267936484, 1.391693986029099772, -1.034342955966370603 ) ) ;
#203554=CARTESIAN_POINT ( 'NONE',  ( 6.509000000000035868, 7.629137130509092479, 2.600000000000000977 ) ) ;
#203557=CARTESIAN_POINT ( 'NONE',  ( 0.6552395816744536194, 1.723207459482085202, -1.147090658606984892 ) ) ;
#203558=CARTESIAN_POINT ( 'NONE',  ( 5.074738461036464088, -1.720261882950037124, -0.6118011564382742629 ) ) ;
#203559=CARTESIAN_POINT ( 'NONE',  ( 3.028120845615461132, 1.045410262836780069, 1.659804706804830277 ) ) ;
#203564=CARTESIAN_POINT ( 'NONE',  ( 4.160867320283115234, 0.5667376361006767338, 2.043264482828925033 ) ) ;
#203568=CARTESIAN_POINT ( 'NONE',  ( 1.270471156847551075, -0.9273748054965322840, -1.850965650132020635 ) ) ;
#203571=CARTESIAN_POINT ( 'NONE',  ( 4.723389051577030706, 1.932298245749045629, 1.095468883668549553 ) ) ;
#203573=CARTESIAN_POINT ( 'NONE',  ( 1.284255082537180570, 1.875723515222413207, -1.328569176028525645 ) ) ;
#203575=CARTESIAN_POINT ( 'NONE',  ( 1.164813196467245904, 1.489159823276710926, -1.277213275948145599 ) ) ;
#203581=CARTESIAN_POINT ( 'NONE',  ( 2.584119536544440265, 1.026460374567798484, 1.613398670029235538 ) ) ;
#203583=CARTESIAN_POINT ( 'NONE',  ( 3.645241786196154354, -1.305741510076625644, -1.126962775032739339 ) ) ;
#203584=CARTESIAN_POINT ( 'NONE',  ( 2.202361591730035428, 1.313542931311746598, -1.530159205979222392 ) ) ;
#203585=CARTESIAN_POINT ( 'NONE',  ( 4.360180292246352174, 0.0003893357360621601550, -2.298851035006874266 ) ) ;
#203586=CARTESIAN_POINT ( 'NONE',  ( 3.761208288054026738, -1.993080904335465142, -1.070619287061522318 ) ) ;
#203587=CARTESIAN_POINT ( 'NONE',  ( 6.129533150132032482, -1.983608965904083421, 0.7080540597134558078 ) ) ;
#203590=CARTESIAN_POINT ( 'NONE',  ( 5.255052661293587946, -1.495254947996208950, -0.9463502368073344329 ) ) ;
#203592=CARTESIAN_POINT ( 'NONE',  ( 0.9379084653730703769, 0.9244841788896654977, -2.097747560502453812 ) ) ;
#203593=CARTESIAN_POINT ( 'NONE',  ( 5.876868881424701208, 1.699447150514224125, -0.7087742222662285485 ) ) ;
#203595=CARTESIAN_POINT ( 'NONE',  ( 5.859372887940716090, 2.159598860408561194, -0.3713886045505072619 ) ) ;
#203599=CARTESIAN_POINT ( 'NONE',  ( 5.336411075974297979, -1.153114810915600641, 1.719314882265559286 ) ) ;
#203600=CARTESIAN_POINT ( 'NONE',  ( 1.710173085450257924, 1.157096902994741772, -1.651345047625000007 ) ) ;
#203602=CARTESIAN_POINT ( 'NONE',  ( 3.984924265943972532, -0.1901312170250069600, -1.917098255223735004 ) ) ;
#203604=CARTESIAN_POINT ( 'NONE',  ( 0.9322285317887604172, -2.165714743787349406, 0.4936765188615526712 ) ) ;
#203614=CARTESIAN_POINT ( 'NONE',  ( 1.943732651021431224, 1.350599318427040840, 1.423195245143428433 ) ) ;
#203619=CARTESIAN_POINT ( 'NONE',  ( 6.514115657861259123, 1.956686900881845714, -0.1430618042221123987 ) ) ;
#203622=CARTESIAN_POINT ( 'NONE',  ( 6.332923096303629151, 0.2067577541180857514, 2.151790036905242953 ) ) ;
#203626=CARTESIAN_POINT ( 'NONE',  ( 1.229531971273215341, -1.182229855178434930, -1.449605969065965949 ) ) ;
#203627=CARTESIAN_POINT ( 'NONE',  ( 6.889999999999967706, 0.005249217920031550542, 1.719840535937327664 ) ) ;
#203629=CARTESIAN_POINT ( 'NONE',  ( 4.528971853086540378, -2.003544689622422936, 0.8885388601788182239 ) ) ;
#203630=CARTESIAN_POINT ( 'NONE',  ( 6.001056180859140277, 1.891180833080384982, -1.322043635676501072 ) ) ;
#203631=CARTESIAN_POINT ( 'NONE',  ( 6.819606862646741874, -2.000071036334325036, 0.4962039222910428760 ) ) ;
#203632=CARTESIAN_POINT ( 'NONE',  ( 2.783070106938976274, 1.373617692895822806, 1.372961415081490610 ) ) ;
#203638=CARTESIAN_POINT ( 'NONE',  ( 2.936172824561166905, -1.650081981912490336, -1.158688413653415239 ) ) ;
#203642=CARTESIAN_POINT ( 'NONE',  ( 1.471042373949003501, 0.1361147407585860392, -1.820667060309004937 ) ) ;
#203648=CARTESIAN_POINT ( 'NONE',  ( 0.4620835240300471547, 2.137967531602209981, -0.3185850937674692407 ) ) ;
#203654=CARTESIAN_POINT ( 'NONE',  ( 5.285809349500922849, 1.945818207184028426, -0.5408622128197750900 ) ) ;
#203655=CARTESIAN_POINT ( 'NONE',  ( 5.444044349889116674, -1.407711435423303792, -1.718264895412445536 ) ) ;
#203659=CARTESIAN_POINT ( 'NONE',  ( 5.348532861604016198, 0.5962098156395375659, 1.972770010162463228 ) ) ;
#203660=CARTESIAN_POINT ( 'NONE',  ( 4.219375079941334761, 1.978050461189932552, 0.3905991720301109082 ) ) ;
#203661=ORIENTED_EDGE ( 'NONE', *, *, #90488, .T. ) ;
#203668=CARTESIAN_POINT ( 'NONE',  ( 4.059922587279920947, 1.704677108394496043, -1.076152822228809480 ) ) ;
#203669=CARTESIAN_POINT ( 'NONE',  ( 3.099365256270599112, -1.839010575856118823, 0.09107247011905240941 ) ) ;
#203671=CARTESIAN_POINT ( 'NONE',  ( 2.315413608375629817, 2.062204878978285194, 1.035883635760030508 ) ) ;
#203673=CARTESIAN_POINT ( 'NONE',  ( 4.130267194010744269, 1.160198474277823300, -1.823679694223250491 ) ) ;
#203676=CARTESIAN_POINT ( 'NONE',  ( 3.357065504480163387, -0.9345643552367989271, 2.099969358187879109 ) ) ;
#203679=CARTESIAN_POINT ( 'NONE',  ( 2.324885834233282544, -0.002380789299309681549, 1.870836310375329381 ) ) ;
#203681=CARTESIAN_POINT ( 'NONE',  ( 0.3156150085598420363, -1.934196717871897953, 0.3801348212975861895 ) ) ;
#203684=CARTESIAN_POINT ( 'NONE',  ( 2.069229996397306426, -2.018448871333050842, -0.8927042923378907258 ) ) ;
#203690=CARTESIAN_POINT ( 'NONE',  ( 5.981319044003478247, 1.821754654810204599, -0.7540403668018207384 ) ) ;
#203691=CARTESIAN_POINT ( 'NONE',  ( 5.531924057230363623, -1.459877215294088204, -1.787231782134098168 ) ) ;
#203692=CARTESIAN_POINT ( 'NONE',  ( 0.1858947801188018389, -1.204007190563995078, -1.549573762531175625 ) ) ;
#203694=CARTESIAN_POINT ( 'NONE',  ( 4.680570805348211572, 1.272886101012826288, -1.622837931747274975 ) ) ;
#203701=CARTESIAN_POINT ( 'NONE',  ( 5.969212972359552616, 1.911920703953375655, 1.028910892658722265 ) ) ;
#203703=CARTESIAN_POINT ( 'NONE',  ( 5.688959394570705541, 1.398425918548395153, 1.197878823674280779 ) ) ;
#203704=CARTESIAN_POINT ( 'NONE',  ( 6.620655732516659064, 6.039214117936751336, 2.421170424969817603 ) ) ;
#203710=CARTESIAN_POINT ( 'NONE',  ( 0.3813228709106940006, 0.1872568833237615027, -1.903067810102520241 ) ) ;
#203711=CARTESIAN_POINT ( 'NONE',  ( 1.797346856567107798, -0.6001438452145327895, 1.665118380002019283 ) ) ;
#203712=CARTESIAN_POINT ( 'NONE',  ( -0.09332341176954485340, -0.4182270256129701491, -1.872751671355552983 ) ) ;
#203714=CARTESIAN_POINT ( 'NONE',  ( 4.394081885627950435, -0.8225995951327015332, -1.730150695830068308 ) ) ;
#203716=CARTESIAN_POINT ( 'NONE',  ( 5.301205566836260985, -1.690247886301226909, 1.010757534590230433 ) ) ;
#203717=CARTESIAN_POINT ( 'NONE',  ( 6.258070668236964451, 0.7691888804484037223, -1.867794269369964066 ) ) ;
#203719=CARTESIAN_POINT ( 'NONE',  ( 3.309304339999539657, -0.3661640501408692794, 1.834289908569000538 ) ) ;
#203720=CARTESIAN_POINT ( 'NONE',  ( 6.481054518252093111, -0.09278056567359710405, -1.722521162943893014 ) ) ;
#203722=CARTESIAN_POINT ( 'NONE',  ( 2.368051099418837069, 2.164043333312406503, -0.4318774905316472013 ) ) ;
#203725=CARTESIAN_POINT ( 'NONE',  ( 0.3442780524403609155, -0.9739420414685855398, 1.818282578471181132 ) ) ;
#203730=CARTESIAN_POINT ( 'NONE',  ( 0.1747926744264920174, 4.095712681614646300, -2.410328719303979739 ) ) ;
#203731=ADVANCED_FACE ( 'NONE', ( #49623 ), #54205, .F. ) ;
#203734=CARTESIAN_POINT ( 'NONE',  ( 3.420434311836465291, 0.9283866757503267397, 1.850595421526677775 ) ) ;
#203738=CARTESIAN_POINT ( 'NONE',  ( 0.4342474147537092044, -1.082315208530496786, -1.704999936850047249 ) ) ;
#203742=CARTESIAN_POINT ( 'NONE',  ( 0.07479286986305544449, 6.948552162806721277, -2.450557996216149892 ) ) ;
#203745=CARTESIAN_POINT ( 'NONE',  ( 6.157445398352582977, 1.830988975552667153, -0.5633538272611648967 ) ) ;
#203746=CARTESIAN_POINT ( 'NONE',  ( 6.539320575229247368, 1.272291865413360812, 2.120198356887960767 ) ) ;
#203747=CARTESIAN_POINT ( 'NONE',  ( 4.335597073515660149, 0.9364531651635084053, -1.981528385891350386 ) ) ;
#203750=CARTESIAN_POINT ( 'NONE',  ( 2.531394148431935776, -0.1834752923718512840, 1.903540536635806912 ) ) ;
#203754=CARTESIAN_POINT ( 'NONE',  ( 0.8785300617164049086, -0.4926655378557908138, -1.955167820405806056 ) ) ;
#203757=CARTESIAN_POINT ( 'NONE',  ( 6.321842903100939104, 1.263506803105146847, -1.790488031206059372 ) ) ;
#203759=CARTESIAN_POINT ( 'NONE',  ( 3.258550815082728036, -1.306766610546957530, 1.125807055032159054 ) ) ;
#203761=CARTESIAN_POINT ( 'NONE',  ( -0.1399997263889819488, 4.088450529495776919, -2.555104583160577203 ) ) ;
#203765=CARTESIAN_POINT ( 'NONE',  ( 0.3968290921660848070, 0.3316028935436679537, 1.933473477243151439 ) ) ;
#203771=CARTESIAN_POINT ( 'NONE',  ( 3.703588720873185469, 1.314418127562553940, 1.246746269480051073 ) ) ;
#203775=CARTESIAN_POINT ( 'NONE',  ( 4.459482644723921752, -1.403152132390030449, -1.145693287117461656 ) ) ;
#203779=( GEOMETRIC_REPRESENTATION_CONTEXT ( 3 ) GLOBAL_UNCERTAINTY_ASSIGNED_CONTEXT ( ( #120119 ) ) GLOBAL_UNIT_ASSIGNED_CONTEXT ( ( #30165, #79972, #114681 ) ) REPRESENTATION_CONTEXT ( 'NONE', 'WORKASPACE' ) );
#203780=CARTESIAN_POINT ( 'NONE',  ( 5.019887821480574885, 1.840843491799005527, -0.2725137592536843734 ) ) ;
#203782=CARTESIAN_POINT ( 'NONE',  ( 2.407709352951839854, -1.104968261951447595, -1.564578956373291696 ) ) ;
#203783=DIRECTION ( 'NONE',  ( 1.016547956922408957E-15, 1.000000000000000000, -4.622230424712075819E-32 ) ) ;
#203789=CARTESIAN_POINT ( 'NONE',  ( 1.447338344653009701, 0.6056102050338266762, -2.000996673686726179 ) ) ;
#203791=CARTESIAN_POINT ( 'NONE',  ( 6.598663746767657656, -0.5144617408539242653, -1.856373320315672037 ) ) ;
#203793=CARTESIAN_POINT ( 'NONE',  ( 2.942213871598579722, 1.811567870905493205, 0.2252638538085757203 ) ) ;
#203795=CARTESIAN_POINT ( 'NONE',  ( 2.302860652515530848, -0.3306829512400177862, -1.883434002855538081 ) ) ;
#203796=CARTESIAN_POINT ( 'NONE',  ( 2.031642458604762780, 1.885605923395494044, -0.5689241207685117319 ) ) ;
#203797=CARTESIAN_POINT ( 'NONE',  ( 3.210425159823264707, 1.756831471361683494, 0.8279855452232912638 ) ) ;
#203801=CARTESIAN_POINT ( 'NONE',  ( 6.491040186595096628, 0.1814514006053032646, 1.852032668777810587 ) ) ;
#203803=CARTESIAN_POINT ( 'NONE',  ( 4.166350089634453191, 2.120059694336435374, -0.05518752902338577848 ) ) ;
#203812=CARTESIAN_POINT ( 'NONE',  ( 4.424309136736732206, 1.121156565774838354, -1.440799707636587712 ) ) ;
#203817=CARTESIAN_POINT ( 'NONE',  ( 4.117926171558832671, -0.9613396577640184182, -1.604580606731422554 ) ) ;
#203819=CARTESIAN_POINT ( 'NONE',  ( 2.191906549581578822, -0.8239416835312768361, 1.741544141456285555 ) ) ;
#203820=CARTESIAN_POINT ( 'NONE',  ( 6.807479307002794577, -1.573682814073861902, -1.171087784426767753 ) ) ;
#203826=CARTESIAN_POINT ( 'NONE',  ( 0.6502104730865595483, 1.047635159188778031, 1.839821444870335165 ) ) ;
#203830=CARTESIAN_POINT ( 'NONE',  ( 5.295788417638883416, -1.460108768623759712, -1.467927865959644862 ) ) ;
#203831=CARTESIAN_POINT ( 'NONE',  ( 0.1515692981730529243, 0.7036590017722235135, 1.701685288394996665 ) ) ;
#203833=CARTESIAN_POINT ( 'NONE',  ( 5.379591378607442742, -0.5557209876673010474, -2.230391596181950042 ) ) ;
#203837=CARTESIAN_POINT ( 'NONE',  ( 1.887097267728707894, 1.992918150068530014, -1.132464722766779675 ) ) ;
#203840=CARTESIAN_POINT ( 'NONE',  ( 5.419850138435895914, 1.155063568626579995, -1.560950513000541662 ) ) ;
#203845=CARTESIAN_POINT ( 'NONE',  ( -0.1403655429255863119, -1.558841978801903894, -1.273620833657141072 ) ) ;
#203847=CARTESIAN_POINT ( 'NONE',  ( 5.911342272548039567, -1.897112096406332382, 0.6839327336411114011 ) ) ;
#203851=CARTESIAN_POINT ( 'NONE',  ( 2.906283313408718705, 1.513773858955402618, -1.442204806208322809 ) ) ;
#203852=CARTESIAN_POINT ( 'NONE',  ( 0.8832604684265840111, 1.184483277375179666, 1.315230855816750921 ) ) ;
#203853=FACE_OUTER_BOUND ( 'NONE', #160516, .T. ) ;
#203855=CARTESIAN_POINT ( 'NONE',  ( 4.418134799529137346, 1.412088972526281072, -1.805610035947482039 ) ) ;
#203856=CARTESIAN_POINT ( 'NONE',  ( 2.642201187982503363, -1.446964261146063802, 0.9666251106823405825 ) ) ;
#203860=CARTESIAN_POINT ( 'NONE',  ( 2.038076752987047602, 1.660595340560795607, -0.4986328326925906773 ) ) ;
#203861=CARTESIAN_POINT ( 'NONE',  ( 2.084662720398474001, 1.251192046665784208, -1.774223565721672724 ) ) ;
#203863=CARTESIAN_POINT ( 'NONE',  ( 4.575407832915947104, 1.497500392235491029, 1.350737390116145242 ) ) ;
#203864=CARTESIAN_POINT ( 'NONE',  ( 2.937500000000001776, 1.451031289060998430, -1.451031289061236018 ) ) ;
#203867=CARTESIAN_POINT ( 'NONE',  ( 0.6746739519505640104, -1.812841073067989361, -0.6519485973254712796 ) ) ;
#203869=CARTESIAN_POINT ( 'NONE',  ( 5.080443840416010381, 1.095562506470529884, 1.932424796230156616 ) ) ;
#203871=CARTESIAN_POINT ( 'NONE',  ( -0.1110810684433141682, 4.095429159110416606, -2.351882046268341409 ) ) ;
#203876=CARTESIAN_POINT ( 'NONE',  ( 0.5928132819080602633, -1.229099697874297181, 1.850090981381287358 ) ) ;
#203877=CARTESIAN_POINT ( 'NONE',  ( 5.476992472119650124, 1.812042599547862176, 0.7524171098330990626 ) ) ;
#203881=CARTESIAN_POINT ( 'NONE',  ( 6.485631321617453260, 1.553040037441177690, 1.645414220380213788 ) ) ;
#203883=CARTESIAN_POINT ( 'NONE',  ( 3.262228214153365169, -2.060424958539575524, 0.09861793142403557644 ) ) ;
#203887=CARTESIAN_POINT ( 'NONE',  ( 4.780451015977909002, -1.813929833846049666, -0.4561423458772846939 ) ) ;
#203888=CARTESIAN_POINT ( 'NONE',  ( 3.375360373764887179, -0.3420621250952958214, -1.699858368971490563 ) ) ;
#203889=CARTESIAN_POINT ( 'NONE',  ( 3.737644501653397455, 1.732476483319781657, 0.1661042753308156761 ) ) ;
#203890=CARTESIAN_POINT ( 'NONE',  ( 0.4512259348973605699, -1.940755322566484642, -1.219765617878470376 ) ) ;
#203892=CARTESIAN_POINT ( 'NONE',  ( 4.687105897418362588, 1.550225779131916726, 1.403071992899749931 ) ) ;
#203893=CARTESIAN_POINT ( 'NONE',  ( 0.3570341529223716726, 1.821527202347131169, -0.2672101559373847857 ) ) ;
#203896=CARTESIAN_POINT ( 'NONE',  ( 0.3873425458618062200, -0.6819987885887256462, -1.897696807414723796 ) ) ;
#203898=CARTESIAN_POINT ( 'NONE',  ( 0.7738737444688469358, 0.4079195088417563730, -2.080830740624163955 ) ) ;
#203899=CARTESIAN_POINT ( 'NONE',  ( 6.604150280000163242, -0.1430408514614608939, 1.983920101186954721 ) ) ;
#203902=CARTESIAN_POINT ( 'NONE',  ( 2.209781436637091367, 1.640924847721588975, 1.343087772177023353 ) ) ;
#203904=CARTESIAN_POINT ( 'NONE',  ( 4.336427269025699971, 1.790907886515300085, 0.3537760332646966432 ) ) ;
#203910=CARTESIAN_POINT ( 'NONE',  ( 1.828384590600404591, -0.9557513975326953348, -1.779375440769872752 ) ) ;
#203911=CARTESIAN_POINT ( 'NONE',  ( 5.965903178300210108, 2.175115270774199416, -0.3715683035191638117 ) ) ;
#203913=CARTESIAN_POINT ( 'NONE',  ( 4.240933880512650411, -0.1787712432332102808, -1.852300418306342955 ) ) ;
#203918=CARTESIAN_POINT ( 'NONE',  ( 5.232948167349782409, 0.1380416123818763163, 1.820529236867339584 ) ) ;
#203922=CARTESIAN_POINT ( 'NONE',  ( 0.2625146791020065984, -1.733275965524210482, -0.05152637578398518159 ) ) ;
#203923=CARTESIAN_POINT ( 'NONE',  ( 6.580030785786400216, -1.806642183828395920, -0.3538341520857649081 ) ) ;
#203924=CARTESIAN_POINT ( 'NONE',  ( 5.496783081331708232, -0.5556612750647730303, -2.239684525637525514 ) ) ;
#203926=CARTESIAN_POINT ( 'NONE',  ( 1.581398767000765426, 1.905217558097069386, -0.7859657096468860571 ) ) ;
#203928=CARTESIAN_POINT ( 'NONE',  ( 6.345094440775825184, -1.237889906630392334, 1.936425090000978289 ) ) ;
#203931=CARTESIAN_POINT ( 'NONE',  ( 5.928550619183988957, 1.803260976426118489, 0.4972845834502263584 ) ) ;
#203932=CARTESIAN_POINT ( 'NONE',  ( 4.078302138561982204, 0.9061299177482335931, 1.684124486321957104 ) ) ;
#203934=CARTESIAN_POINT ( 'NONE',  ( 5.110101661328442901, -2.196521081226535443, 0.2136625748923453583 ) ) ;
#203939=CARTESIAN_POINT ( 'NONE',  ( 5.672555391165950311, 0.8593836824349295744, 1.938725756316476589 ) ) ;
#203940=CARTESIAN_POINT ( 'NONE',  ( 2.573609363736366618, 0.1136701668994527237, -2.304911326000145699 ) ) ;
#203941=CARTESIAN_POINT ( 'NONE',  ( 3.490630252122446375, 1.913478943654752129, 0.4322817992908413176 ) ) ;
#203943=CARTESIAN_POINT ( 'NONE',  ( 0.2858946156298440844, -1.202361161835348025, -1.550730028719159215 ) ) ;
#203947=CARTESIAN_POINT ( 'NONE',  ( 6.069546051295945155, 1.394081536189460069, 1.457239770841619597 ) ) ;
#203950=CARTESIAN_POINT ( 'NONE',  ( 3.045941508711128787, 1.532170317875800603, 1.538426465386952380 ) ) ;
#203952=CARTESIAN_POINT ( 'NONE',  ( 1.178162429063234207, 2.088287186665960693, -0.3679680078583212333 ) ) ;
#203958=CARTESIAN_POINT ( 'NONE',  ( 0.6849272659917711170, -0.2494827685093256309, -2.045528899044207982 ) ) ;
#203964=CARTESIAN_POINT ( 'NONE',  ( 3.316961667764028121, 1.505919282548912719, -1.178437403786938731 ) ) ;
#203966=CARTESIAN_POINT ( 'NONE',  ( 5.647242114940491220, -1.397150190615953358, -1.086277386216354168 ) ) ;
#203969=CARTESIAN_POINT ( 'NONE',  ( 0.3865838573892222962, -1.705918499434391444, -0.6100900862041622741 ) ) ;
#203970=CARTESIAN_POINT ( 'NONE',  ( 0.9189787140968961321, -1.730522700298501304, 0.8221016984403562988 ) ) ;
#203971=CARTESIAN_POINT ( 'NONE',  ( 1.873570696236816158, -0.2555354716398828274, 2.054483085851127377 ) ) ;
#203973=CARTESIAN_POINT ( 'NONE',  ( 6.684453402082996654, -1.835023323784425564, -0.3624468955198830722 ) ) ;
#203974=CARTESIAN_POINT ( 'NONE',  ( 3.176193443437186126, -1.086901434622984830, 1.466744820640853098 ) ) ;
#203975=CARTESIAN_POINT ( 'NONE',  ( 6.691986956589398794, -0.9478133180038283978, 1.990996264204819122 ) ) ;
#203978=CARTESIAN_POINT ( 'NONE',  ( 4.053227687556320014, 1.744102858319864113, -1.100964799198749455 ) ) ;
#203983=CARTESIAN_POINT ( 'NONE',  ( 0.3862812426984676972, -1.019270635400490121, 1.906220128828392646 ) ) ;
#203984=CARTESIAN_POINT ( 'NONE',  ( 6.514133371570012265, 2.065101995627930620, -0.1482383472809906122 ) ) ;
#203986=CARTESIAN_POINT ( 'NONE',  ( 4.253314833958360630, -1.794556715717060769, -1.204719293387515489 ) ) ;
#203987=CARTESIAN_POINT ( 'NONE',  ( 3.809243936906735239, 1.705047127353828351, -1.082240749027115978 ) ) ;
#203992=CARTESIAN_POINT ( 'NONE',  ( 3.010954138651841916, 0.05432569772663429358, 2.015980714967258614 ) ) ;
#203996=CARTESIAN_POINT ( 'NONE',  ( 5.291234991620993533, -0.05314252713351996088, -1.911838368980276703 ) ) ;
#204000=CARTESIAN_POINT ( 'NONE',  ( 4.323842328482737862, 0.8596156136044874607, -1.824127480631778653 ) ) ;
#204003=CARTESIAN_POINT ( 'NONE',  ( 0.04690384546136848465, -1.329360633743952746, -1.098954345569080893 ) ) ;
#204008=CARTESIAN_POINT ( 'NONE',  ( 5.395714598229544023, -0.6742385858747660388, 1.744967798948720228 ) ) ;
#204009=CARTESIAN_POINT ( 'NONE',  ( 5.924093355334532518, -1.997480882691978987, 0.2508417921044738819 ) ) ;
#204011=CARTESIAN_POINT ( 'NONE',  ( 2.079047829753433163, 1.930162853665925216, 0.7490395704240898622 ) ) ;
#204015=CARTESIAN_POINT ( 'NONE',  ( 0.6500178175347062215, 0.9963223104369985927, 1.753020061881369829 ) ) ;
#204016=CARTESIAN_POINT ( 'NONE',  ( 1.019438801881300316, -0.4388897500222695425, 1.757493349343726585 ) ) ;
#204021=CARTESIAN_POINT ( 'NONE',  ( 6.028903631427566800, -1.615475894945080926, 1.029159534634891626 ) ) ;
#204028=CARTESIAN_POINT ( 'NONE',  ( 3.274459119871219848, -1.289031633699177171, 1.735169069618908599 ) ) ;
#204031=CARTESIAN_POINT ( 'NONE',  ( 0.3695850531008069706, -1.794773754367712693, -1.129184308951653781 ) ) ;
#204032=CARTESIAN_POINT ( 'NONE',  ( 6.264658373536383884, -1.288822541704701230, 1.293195164663100361 ) ) ;
#204033=CARTESIAN_POINT ( 'NONE',  ( 2.178924785135676334, -0.09298872875643586500, -1.969266502737290425 ) ) ;
#204034=CARTESIAN_POINT ( 'NONE',  ( 5.045129621168108258, 0.1466893748028277877, 1.906852434080000824 ) ) ;
#204037=CARTESIAN_POINT ( 'NONE',  ( 4.527769023902194157, 1.910916496070225179, -0.4765158004534468805 ) ) ;
#204038=CARTESIAN_POINT ( 'NONE',  ( 6.614805133705309537, -0.1285734799129842065, 1.912263277720785970 ) ) ;
#204044=CARTESIAN_POINT ( 'NONE',  ( 5.479139036522528983, -1.730609802697373079, -0.8137914003483390779 ) ) ;
#204046=CARTESIAN_POINT ( 'NONE',  ( 0.7982362974770088604, -0.7925503509537080715, 2.059710425106767939 ) ) ;
#204048=CARTESIAN_POINT ( 'NONE',  ( 5.795569859559966730, 1.859138327062941132, -0.7725605513991992135 ) ) ;
#204049=CARTESIAN_POINT ( 'NONE',  ( 0.07661050522435489119, 2.064768137775649048, -2.128874817076317871 ) ) ;
#204051=CARTESIAN_POINT ( 'NONE',  ( -1.786765180256111307E-13, 7.629137130509076492, -2.599999999999921929 ) ) ;
#204052=CARTESIAN_POINT ( 'NONE',  ( 2.576698201331685922, 1.354182300986291887, -1.566139152919379329 ) ) ;
#204056=CARTESIAN_POINT ( 'NONE',  ( 0.8839147992780393981, 1.452536163361785260, 1.601146772000871188 ) ) ;
#204062=CARTESIAN_POINT ( 'NONE',  ( 6.825078400183545391, 0.005516643811322509937, 1.755566376062764222 ) ) ;
#204064=CARTESIAN_POINT ( 'NONE',  ( 4.394945383863869459, -0.7467295182301251222, -1.565304230221546300 ) ) ;
#204066=CARTESIAN_POINT ( 'NONE',  ( 2.799741537105740363, -1.531010120401912200, -1.393694001666223814 ) ) ;
#204067=CARTESIAN_POINT ( 'NONE',  ( 4.499685226448436381, -2.076086866053193258, 0.4145649545581850393 ) ) ;
#204070=CARTESIAN_POINT ( 'NONE',  ( 1.780066195911081284, -1.089727156841081346, -1.640273131265007844 ) ) ;
#204072=CARTESIAN_POINT ( 'NONE',  ( 1.125099709691119276, 1.687896996356451629, 0.8989547360247207575 ) ) ;
#204073=CARTESIAN_POINT ( 'NONE',  ( 5.121132688944100231, -2.177879115872250360, 0.7152381750462534216 ) ) ;
#204074=CARTESIAN_POINT ( 'NONE',  ( 1.699542765152612711, -0.6164703606487755838, 1.718597393154073671 ) ) ;
#204078=CARTESIAN_POINT ( 'NONE',  ( 3.181892525975566155, 1.963218260121324166, -0.4451317699624996460 ) ) ;
#204079=CARTESIAN_POINT ( 'NONE',  ( 3.573055779259231457, 1.771592698278463107, 0.8429337356923997104 ) ) ;
#204082=CARTESIAN_POINT ( 'NONE',  ( 0.07516593201273635838, 1.359561921253334749, -2.300590921312398951 ) ) ;
#204083=CARTESIAN_POINT ( 'NONE',  ( 5.683562130502735954, -0.9407222913834032418, 1.867095764824426851 ) ) ;
#204084=CARTESIAN_POINT ( 'NONE',  ( 4.486996778590452983, 1.580468086399078542, -0.7966448122273452892 ) ) ;
#204086=CARTESIAN_POINT ( 'NONE',  ( 1.060776890969020059, -1.982532595227912475, -0.9341070725938580566 ) ) ;
#204087=CARTESIAN_POINT ( 'NONE',  ( -0.1239745564502250652, -0.1323307239476738673, -1.711383809018538038 ) ) ;
#204089=CARTESIAN_POINT ( 'NONE',  ( 0.2331713839410602396, 7.629137130509072939, -2.553349835631549603 ) ) ;
#204090=CARTESIAN_POINT ( 'NONE',  ( 5.836663081169705336, 0.6703748249779170054, -2.198801845021758350 ) ) ;
#204092=CARTESIAN_POINT ( 'NONE',  ( 5.641838915941918664, -0.04494510194943436565, -1.733422878500885167 ) ) ;
#204093=CARTESIAN_POINT ( 'NONE',  ( 1.805583701156989518, 1.836052299496168771, 1.224139149458243425 ) ) ;
#204095=CARTESIAN_POINT ( 'NONE',  ( 0.4796376738960402841, -0.1079922143863345368, 2.168524981076371372 ) ) ;
#204097=CARTESIAN_POINT ( 'NONE',  ( 0.9544967768389999163, -1.338301201188813572, 1.640804622059524043 ) ) ;
#204098=CARTESIAN_POINT ( 'NONE',  ( 3.812500000000003109, 1.451031289061270213, 1.451031289060960905 ) ) ;
#204099=CARTESIAN_POINT ( 'NONE',  ( 6.727182134110199385, 7.052145554274142469, 2.687205589382557491 ) ) ;
#204100=CARTESIAN_POINT ( 'NONE',  ( 4.260710244665906643, -1.428042822336324846, 1.293124370783913735 ) ) ;
#204101=CARTESIAN_POINT ( 'NONE',  ( 0.9443249964648057215, -1.413213925058560028, -1.713760899525147874 ) ) ;
#204103=CARTESIAN_POINT ( 'NONE',  ( 1.857357856600039048, 0.3871700131025680447, -2.259295229882941403 ) ) ;
#204107=CARTESIAN_POINT ( 'NONE',  ( 4.248835331960220785, 2.178490119157860061, 0.4332075398792554766 ) ) ;
#204113=CARTESIAN_POINT ( 'NONE',  ( 1.336564801266389990, 0.5826540126645517459, -1.930418273149013153 ) ) ;
#204115=CARTESIAN_POINT ( 'NONE',  ( 6.355934510867760956, -0.6984221382469282258, 1.940952099462374569 ) ) ;
#204118=CARTESIAN_POINT ( 'NONE',  ( 0.1339853816830008371, 0.3136495386693045062, 1.814181566856580607 ) ) ;
#204121=CARTESIAN_POINT ( 'NONE',  ( 1.668863397688532091, 0.1364744985549205814, -1.764554890378322805 ) ) ;
#204122=CARTESIAN_POINT ( 'NONE',  ( 0.3170300144729014669, 1.034162889623980286, -1.730867746391979933 ) ) ;
#204123=CARTESIAN_POINT ( 'NONE',  ( 6.233937787808796038, 1.722893207988238862, 0.2456954999437432341 ) ) ;
#204124=CARTESIAN_POINT ( 'NONE',  ( 4.669621734427405357, 1.318897967798425608, 1.874777261101326920 ) ) ;
#204125=CARTESIAN_POINT ( 'NONE',  ( 3.626748959588219634, -1.700609458330613055, 0.7059681596332522124 ) ) ;
#204127=CARTESIAN_POINT ( 'NONE',  ( 3.311362000969253039, -0.3573404788377897989, 1.790086433339547201 ) ) ;
#204128=CARTESIAN_POINT ( 'NONE',  ( 3.340470361411255418, 0.4872029778183216697, -1.956561305313428978 ) ) ;
#204130=CARTESIAN_POINT ( 'NONE',  ( 3.889755562772099662, 1.636703778197702075, 1.562332884182315196 ) ) ;
#204132=CARTESIAN_POINT ( 'NONE',  ( 5.790091041381728587, -0.9498100376258570288, 1.879691625423451029 ) ) ;
#204134=CARTESIAN_POINT ( 'NONE',  ( 3.525891238081061640, 2.020528833579691597, -0.4508363271973143682 ) ) ;
#204137=CARTESIAN_POINT ( 'NONE',  ( 5.285831659486547984, 2.043504495962459977, -0.5658664308652374686 ) ) ;
#204139=CARTESIAN_POINT ( 'NONE',  ( 0.8031968939124977114, 1.574386321349549700, 1.110025428916910917 ) ) ;
#204141=CARTESIAN_POINT ( 'NONE',  ( 6.842638217859555283, -1.930751226189564962, -0.3875045943893626887 ) ) ;
#204146=CARTESIAN_POINT ( 'NONE',  ( 0.9322285317887604172, -2.165714743787349406, 0.4936765188615526712 ) ) ;
#204147=CARTESIAN_POINT ( 'NONE',  ( 2.380028573532027458, 1.294904889207445509, 1.660730631172540495 ) ) ;
#204150=CARTESIAN_POINT ( 'NONE',  ( 0.1680794356360598985, -0.7909032441709142880, -1.683366987590989350 ) ) ;
#204156=CARTESIAN_POINT ( 'NONE',  ( 0.6684183810189650021, 2.117893379942568988, -0.1100008709709817956 ) ) ;
#204159=CARTESIAN_POINT ( 'NONE',  ( 3.719154087244529894, -1.729071306366702698, -0.9269775827704658244 ) ) ;
#204160=CARTESIAN_POINT ( 'NONE',  ( 1.956163130892615731, 2.155914767609674598, -0.1587918856347721730 ) ) ;
#204161=CARTESIAN_POINT ( 'NONE',  ( 2.278628554356322500, 1.682734121078124812, -0.7478279864501293783 ) ) ;
#204164=CARTESIAN_POINT ( 'NONE',  ( 3.943067085940495264, 0.5840054040482050013, -1.639550319303827219 ) ) ;
#204167=CARTESIAN_POINT ( 'NONE',  ( 0.4972265960483426284, 1.796464302094663346, -1.202062886709959422 ) ) ;
#204168=CARTESIAN_POINT ( 'NONE',  ( 3.216172551982798833, -1.646586737935524125, -1.163091166099708529 ) ) ;
#204170=CARTESIAN_POINT ( 'NONE',  ( 0.2159880523044250267, -2.119658899406823505, 0.4233941889316418239 ) ) ;
#204171=CARTESIAN_POINT ( 'NONE',  ( 2.782053229633123959, -1.014971971657689709, 1.689997848710776740 ) ) ;
#204172=CARTESIAN_POINT ( 'NONE',  ( 6.508999999999982577, 2.977730662443831111, 2.353651457310241835 ) ) ;
#204173=CARTESIAN_POINT ( 'NONE',  ( 2.472129730261590552, -1.859182766463037151, -0.5613441811427360983 ) ) ;
#204179=CARTESIAN_POINT ( 'NONE',  ( -0.1108833634136767998, 2.883350581177961391, -2.385667623150728556 ) ) ;
#204184=CARTESIAN_POINT ( 'NONE',  ( 0.3412290553763823175, 0.3797058362894655814, 2.173699509851903855 ) ) ;
#204186=CARTESIAN_POINT ( 'NONE',  ( 3.696105151714265347, 0.8860871710942277435, -1.750347149911928968 ) ) ;
#204188=CARTESIAN_POINT ( 'NONE',  ( 1.477185633673218312, -2.006960102380969779, -0.1948397147320118372 ) ) ;
#204190=CARTESIAN_POINT ( 'NONE',  ( 1.833370464255643206, -1.703966518588348578, -1.256690760101538240 ) ) ;
#204194=CARTESIAN_POINT ( 'NONE',  ( 3.204851553285171573, -0.3583046703147829692, 1.805758307424263354 ) ) ;
#204198=CARTESIAN_POINT ( 'NONE',  ( 4.254221937059123881, 0.9039275175388861161, -1.918405034562712830 ) ) ;
#204200=CARTESIAN_POINT ( 'NONE',  ( 0.005434845660363255178, -0.7843016415976924449, -1.664241202765592176 ) ) ;
#204204=CARTESIAN_POINT ( 'NONE',  ( 4.007146649590315413, 1.765602988722612565, 1.062546815679512369 ) ) ;
#204207=CARTESIAN_POINT ( 'NONE',  ( 1.382094229771430705, -0.2707140722739818650, -1.821126350552772610 ) ) ;
#204213=CARTESIAN_POINT ( 'NONE',  ( 0.9091299924109221831, 1.668792687453458878, -1.444214864661397035 ) ) ;
#204214=CARTESIAN_POINT ( 'NONE',  ( 4.183118113821016948, -0.2165105290278953043, -2.252005913828499573 ) ) ;
#204216=CARTESIAN_POINT ( 'NONE',  ( 3.550846374533889183, 0.2710319999918932021, 1.791078082347187683 ) ) ;
#204217=CARTESIAN_POINT ( 'NONE',  ( 4.592943030449060160, 1.669885041223855060, 0.9386680909919845606 ) ) ;
#204218=CARTESIAN_POINT ( 'NONE',  ( 5.020015195830264787, 2.048331326439792210, -0.3003445753073652469 ) ) ;
#204221=CARTESIAN_POINT ( 'NONE',  ( 3.098462860235187133, -0.5706901479570201108, -1.887068881103808327 ) ) ;
#204222=CARTESIAN_POINT ( 'NONE',  ( 1.061403713111798153, 0.3786953092320010650, -1.888642112844605592 ) ) ;
#204223=CARTESIAN_POINT ( 'NONE',  ( 3.449935675575486638, 1.870836310073907827, 0.001118452434160921221 ) ) ;
#204224=CARTESIAN_POINT ( 'NONE',  ( 3.598509747979701690, -2.304983022191483766, -0.1141929325871558626 ) ) ;
#204225=CARTESIAN_POINT ( 'NONE',  ( 3.209261600960995775, -1.519886386175553605, -1.073685847751577604 ) ) ;
#204229=CARTESIAN_POINT ( 'NONE',  ( 1.418734189139436275, 1.413363300903627717, -1.561561204404242842 ) ) ;
#204234=CARTESIAN_POINT ( 'NONE',  ( 2.672263739372262137, 2.109986773948614225, -0.2121620573234672125 ) ) ;
#204236=CARTESIAN_POINT ( 'NONE',  ( 0.9143263792395848188, -2.019972748253701322, 0.004280675582559247648 ) ) ;
#204241=CARTESIAN_POINT ( 'NONE',  ( 0.7378453340087381962, -1.528073262844112268, -1.529135702860604074 ) ) ;
#204244=CARTESIAN_POINT ( 'NONE',  ( 6.825078400183548055, 2.447738240532343124, 2.338733633852312366 ) ) ;
#204247=CARTESIAN_POINT ( 'NONE',  ( 5.542203953035277131, 0.8216685229280199509, 1.841735684200429990 ) ) ;
#204249=CARTESIAN_POINT ( 'NONE',  ( 0.2928600448571066495, 1.818678932476354149, -1.222557900829209121 ) ) ;
#204251=CARTESIAN_POINT ( 'NONE',  ( 0.3568017664055183613, 0.8693207686717405736, 2.089032543936353736 ) ) ;
#204254=CARTESIAN_POINT ( 'NONE',  ( 4.294157853547872605, -0.8666056138363428252, -1.820986994602634024 ) ) ;
#204256=CARTESIAN_POINT ( 'NONE',  ( 1.335391617855705926, 0.5546556490612590817, -1.833562831147776739 ) ) ;
#204260=CARTESIAN_POINT ( 'NONE',  ( 3.000334558935643603, -0.5012536917932303160, -1.650428355875031228 ) ) ;
#204262=CARTESIAN_POINT ( 'NONE',  ( 2.284116761108864413, -1.734514481284253007, -0.3503773294724100706 ) ) ;
#204263=CARTESIAN_POINT ( 'NONE',  ( 2.526041439118778431, -1.990860190764773829, 0.2976642988744558904 ) ) ;
#204264=CARTESIAN_POINT ( 'NONE',  ( 5.596761079150560647, -0.5311557606857522096, -2.141783596114990917 ) ) ;
#204267=CARTESIAN_POINT ( 'NONE',  ( 3.985108911058360182, -1.979049277059058864, -0.7619450576143712572 ) ) ;
#204268=CARTESIAN_POINT ( 'NONE',  ( 3.796500049179197589, 1.423950305759081214, -1.427950143821264506 ) ) ;
#204269=CARTESIAN_POINT ( 'NONE',  ( 4.359482725938978120, -1.404519563743265920, -1.144221460762798737 ) ) ;
#204273=CARTESIAN_POINT ( 'NONE',  ( 1.340467186903429253, 0.3614942610149494695, 1.835218787103513050 ) ) ;
#204275=CARTESIAN_POINT ( 'NONE',  ( 6.428355384240774129, -0.8606449381524762243, -1.593976378398887173 ) ) ;
#204285=CARTESIAN_POINT ( 'NONE',  ( 4.306960158517386894, -0.4675538901007176285, -2.068242682749166672 ) ) ;
#204286=CARTESIAN_POINT ( 'NONE',  ( -0.1296875068448125334, 2.048176110289974261, -2.243787855586779401 ) ) ;
#204288=CARTESIAN_POINT ( 'NONE',  ( 5.448493488195655488, 0.5694873833897282633, 1.887333253073280703 ) ) ;
#204290=CARTESIAN_POINT ( 'NONE',  ( 0.4924401237900773443, -1.114920267122095021, 1.676101429157205613 ) ) ;
#204292=CARTESIAN_POINT ( 'NONE',  ( 6.491443032814855130, -0.4656331456187530748, 2.073361762655197893 ) ) ;
#204295=CARTESIAN_POINT ( 'NONE',  ( 1.416557266959647787, 0.8372786474034592530, 1.893679232998768391 ) ) ;
#204299=CARTESIAN_POINT ( 'NONE',  ( 4.962875334715753262, 0.2052988877573138915, -2.080521221900538009 ) ) ;
#204302=CARTESIAN_POINT ( 'NONE',  ( 2.836711209001481659, 0.2215568149019596367, 1.812007907362273018 ) ) ;
#204303=CARTESIAN_POINT ( 'NONE',  ( 1.260107830910334181, 1.809384220011617028, 0.08917393313457448734 ) ) ;
#204305=CARTESIAN_POINT ( 'NONE',  ( 6.428370569364434850, 1.274405893209800356, -1.801548588985131039 ) ) ;
#204307=CARTESIAN_POINT ( 'NONE',  ( 4.085166796624926100, -0.2132991444873769959, -2.196430506890618695 ) ) ;
#204310=CARTESIAN_POINT ( 'NONE',  ( 2.912652942483742180, -0.5572119909246497915, -1.829279355302193544 ) ) ;
#204312=CARTESIAN_POINT ( 'NONE',  ( 6.127406499145813257, 0.1562011534181114436, -2.064545280851529885 ) ) ;
#204314=CARTESIAN_POINT ( 'NONE',  ( 5.425378541715013547, -1.389685604419872655, -1.694579525865948844 ) ) ;
#204318=EDGE_CURVE ( 'NONE', #180616, #185672, #81857, .T. ) ;
#204325=CARTESIAN_POINT ( 'NONE',  ( 6.983263157960365675, -0.006178392973848687020, 2.053544886540019210 ) ) ;
#204326=CARTESIAN_POINT ( 'NONE',  ( 1.194935658704935566, 1.779638138761422628, 0.9480210990304924756 ) ) ;
#204329=CARTESIAN_POINT ( 'NONE',  ( 1.869323357045350686, 2.096458975851514861, -0.6381942758529115522 ) ) ;
#204330=CARTESIAN_POINT ( 'NONE',  ( 5.461492464141177727, 0.3521552718798379722, -1.791230276788812414 ) ) ;
#204339=CARTESIAN_POINT ( 'NONE',  ( 2.841158510722852970, 0.6603703904487292498, -1.718939526767604420 ) ) ;
#204340=CARTESIAN_POINT ( 'NONE',  ( 0.02993902094421736770, -1.973830418800892161, 0.3948085296872869687 ) ) ;
#204341=CARTESIAN_POINT ( 'NONE',  ( 2.460726772196987433, 1.776095029035225537, 1.458756201258274210 ) ) ;
#204343=CARTESIAN_POINT ( 'NONE',  ( 0.3384086464433467278, -1.803039684303367141, -0.4601552930486965121 ) ) ;
#204346=CARTESIAN_POINT ( 'NONE',  ( 2.935702856749936362, -1.841876368404654629, 0.5141854427313449216 ) ) ;
#204350=CARTESIAN_POINT ( 'NONE',  ( 2.823863332701610940, 1.159264052448713889, -1.739707760033171180 ) ) ;
#204351=CARTESIAN_POINT ( 'NONE',  ( 0.7252172114964609007, -1.777616610744123804, 0.5828384007960025759 ) ) ;
#204352=CARTESIAN_POINT ( 'NONE',  ( 2.442732317853496760, 1.238130588059358717, 1.591075322344523535 ) ) ;
#204356=CARTESIAN_POINT ( 'NONE',  ( 2.700428686635591546, 1.471443353139300081, 0.9291617766199999906 ) ) ;
#204357=AXIS2_PLACEMENT_3D ( 'NONE', #99355, #148110, #210946 ) ;
#204361=CARTESIAN_POINT ( 'NONE',  ( 3.193694537771115449, -0.6981934656059236577, 1.577442374586303320 ) ) ;
#204362=CARTESIAN_POINT ( 'NONE',  ( 3.052458795248469414, -1.657928338269051505, 1.433322580492613296 ) ) ;
#204363=CARTESIAN_POINT ( 'NONE',  ( 5.250674450588199704, 0.6379336648693231249, 2.112661011922472021 ) ) ;
#204365=CARTESIAN_POINT ( 'NONE',  ( 3.256845431185355633, -0.6256494993409821292, -2.079000826131827129 ) ) ;
#204366=CARTESIAN_POINT ( 'NONE',  ( 2.420285107995377327, 1.192830232448302441, -1.382225081888274643 ) ) ;
#204368=CARTESIAN_POINT ( 'NONE',  ( 4.311780797230674089, -1.305379566919599332, -1.666953740739559819 ) ) ;
#204369=CARTESIAN_POINT ( 'NONE',  ( 6.639320575229291421, 7.052752469465089824, 2.594893258668645952 ) ) ;
#204372=CARTESIAN_POINT ( 'NONE',  ( 4.476316811684385222, -2.223409025971525121, -0.5576598666321966880 ) ) ;
#204377=CARTESIAN_POINT ( 'NONE',  ( 0.1531979293848736434, 0.3668625560977051281, 2.088361607889513305 ) ) ;
#204383=CARTESIAN_POINT ( 'NONE',  ( 5.572888750952301073, -0.9041123360693378297, 1.802415994888312722 ) ) ;
#204385=CARTESIAN_POINT ( 'NONE',  ( 3.836832695767174783, -1.986499165045521265, -0.5546697284559941599 ) ) ;
#204387=CARTESIAN_POINT ( 'NONE',  ( -0.1411974294642098227, 4.091293698307607585, -2.455098582995118406 ) ) ;
#204392=CARTESIAN_POINT ( 'NONE',  ( 6.333935822332933618, 2.167035306593240840, 0.3253760364356065860 ) ) ;
#204393=CARTESIAN_POINT ( 'NONE',  ( 3.463517678199812266, -1.944071305346905643, -0.5350885120067662148 ) ) ;
#204394=CARTESIAN_POINT ( 'NONE',  ( 2.929072846782492245, -1.238530643895646488, -1.362589426554157157 ) ) ;
#204398=CARTESIAN_POINT ( 'NONE',  ( 0.4809449578498920519, 1.612012756419522352, -0.6139154093185476002 ) ) ;
#204400=CARTESIAN_POINT ( 'NONE',  ( 1.231506118810040018, 2.296321937838792238, 0.1066795702680169711 ) ) ;
#204402=CARTESIAN_POINT ( 'NONE',  ( 0.3337811221923889793, -2.067640401758659596, 0.9186946961548744239 ) ) ;
#204403=CARTESIAN_POINT ( 'NONE',  ( 3.264387862500417903, 0.9470664325190655264, 1.881190857022313478 ) ) ;
#204412=CARTESIAN_POINT ( 'NONE',  ( 3.656649667753679278, 2.210956852819144114, 0.2149545701610345305 ) ) ;
#204413=CARTESIAN_POINT ( 'NONE',  ( 2.466951935624495107, 0.1062163371072753354, -2.188993582743845590 ) ) ;
#204416=CARTESIAN_POINT ( 'NONE',  ( 5.758247127753066685, -1.962046631956643195, -0.001586170976335121285 ) ) ;
#204422=CARTESIAN_POINT ( 'NONE',  ( 4.324552338190708056, -0.9094542848507057853, -1.915842285305848769 ) ) ;
#204425=CARTESIAN_POINT ( 'NONE',  ( 5.049776242366147194, 0.6816224847111511664, -2.051488706027407183 ) ) ;
#204427=CARTESIAN_POINT ( 'NONE',  ( 4.651808992177354440, 0.7092673950449077669, 1.699362209096597187 ) ) ;
#204432=CARTESIAN_POINT ( 'NONE',  ( 0.1689663589281220069, 0.9994598401263864451, 1.424626921871420926 ) ) ;
#204433=CARTESIAN_POINT ( 'NONE',  ( 6.827182134110233669, 2.063332311267600971, 2.217821918593851027 ) ) ;
#204436=CARTESIAN_POINT ( 'NONE',  ( 4.627887939457571598, -1.327398817707679868, -1.706084338546076662 ) ) ;
#204439=CARTESIAN_POINT ( 'NONE',  ( 2.993221558690632556, 1.854768100113469265, -1.110066390340218367 ) ) ;
#204440=CARTESIAN_POINT ( 'NONE',  ( 4.411372364376418886, -0.3401156029278085136, 1.941656249039567905 ) ) ;
#204441=CARTESIAN_POINT ( 'NONE',  ( 3.409274926616968404, 0.4192967605245543905, 1.682228440661166502 ) ) ;
#204442=CARTESIAN_POINT ( 'NONE',  ( 0.7850416839378616674, 1.930235501049954339, -1.037882601892345713 ) ) ;
#204443=CARTESIAN_POINT ( 'NONE',  ( 1.606910496583548786, -0.8321943236449917958, -2.152478949753482862 ) ) ;
#204444=CARTESIAN_POINT ( 'NONE',  ( 3.796211532432732572, -2.058264701994051649, -0.1047273801592675524 ) ) ;
#204445=CARTESIAN_POINT ( 'NONE',  ( 5.899939537456503125, -0.7029524595547633758, -1.810543181819963321 ) ) ;
#204452=CARTESIAN_POINT ( 'NONE',  ( 3.188704395469597497, -2.173853526369253331, -0.3788738375181537332 ) ) ;
#204455=CARTESIAN_POINT ( 'NONE',  ( 0.7778919621034340315, -0.9889961724188134351, -1.576189065804904477 ) ) ;
#204456=CARTESIAN_POINT ( 'NONE',  ( -0.02919842301644676522, 2.866066704180502800, -2.562138095921069780 ) ) ;
#204461=CARTESIAN_POINT ( 'NONE',  ( 6.246043375366982175, 0.5822610321466625827, 1.746719530172704760 ) ) ;
#204463=CARTESIAN_POINT ( 'NONE',  ( 2.043891306636512528, 0.7897949731258145922, -1.903750762553678921 ) ) ;
#204469=CARTESIAN_POINT ( 'NONE',  ( 1.270465292308793126, -1.308197635955485216, 1.592426268366262665 ) ) ;
#204471=CARTESIAN_POINT ( 'NONE',  ( 4.440845869443198701, -1.426288408191313639, -1.164454570719307469 ) ) ;
#204475=CARTESIAN_POINT ( 'NONE',  ( 4.055453297694236348, -1.834216022232620702, -1.226887332174103173 ) ) ;
#204476=CARTESIAN_POINT ( 'NONE',  ( 6.731690493876715919, -1.469984723218084488, -1.719904613669322790 ) ) ;
#204478=CARTESIAN_POINT ( 'NONE',  ( 0.5274218815167727170, -0.2782315536139517431, 1.891897276498944347 ) ) ;
#204479=CARTESIAN_POINT ( 'NONE',  ( 1.112517963266421939, 1.944731545904467396, 0.5331650539944567946 ) ) ;
#204481=CARTESIAN_POINT ( 'NONE',  ( 1.740083653633100580, -2.182622149841602521, -0.7203450084119922270 ) ) ;
#204482=CARTESIAN_POINT ( 'NONE',  ( 6.789956943122251509, -0.7972922127613899512, 1.690610701080223821 ) ) ;
#204487=CARTESIAN_POINT ( 'NONE',  ( 2.201827603038747139, -1.870314503716500099, 0.04339327950253490246 ) ) ;
#204488=CARTESIAN_POINT ( 'NONE',  ( 2.132046339962359038, 2.016188815772378629, 0.04465230659478347519 ) ) ;
#204492=CARTESIAN_POINT ( 'NONE',  ( 4.811209553025526553, 1.832079168721172380, 1.038602630702612384 ) ) ;
#204497=CARTESIAN_POINT ( 'NONE',  ( 4.377216478116826792, -1.806098078589046807, -0.9042721688041258643 ) ) ;
#204499=CARTESIAN_POINT ( 'NONE',  ( 6.092244811693771744, 1.020019244021443727, -1.792768071708307431 ) ) ;
#204501=CARTESIAN_POINT ( 'NONE',  ( 4.200566210393744448, -0.6737006675727378324, -2.054019326127386691 ) ) ;
#204507=CARTESIAN_POINT ( 'NONE',  ( 1.557326333469456481, 1.775469013113859074, -1.249449068179921518 ) ) ;
#204510=CARTESIAN_POINT ( 'NONE',  ( 1.452429406588066740, -1.579491434881035827, -0.9459884711465746943 ) ) ;
#204512=CARTESIAN_POINT ( 'NONE',  ( 2.736070936638954176, 2.175344985778558726, 0.2654339622269741295 ) ) ;
#204513=CARTESIAN_POINT ( 'NONE',  ( 6.883263157960367806, 6.035304072343574688, 2.648703854151325032 ) ) ;
#204514=CARTESIAN_POINT ( 'NONE',  ( 3.784249319668216760, -1.117672106238891461, 1.967118024168002410 ) ) ;
#204521=CARTESIAN_POINT ( 'NONE',  ( 5.923074920120706466, -0.04171666621876138348, 1.769427632397130079 ) ) ;
#204522=CARTESIAN_POINT ( 'NONE',  ( 3.563142721848435279, -1.644496397275853505, 1.160845683069864798 ) ) ;
#204524=CARTESIAN_POINT ( 'NONE',  ( 2.010898292529788467, 1.560970962663108752, -1.413861550561988922 ) ) ;
#204527=CARTESIAN_POINT ( 'NONE',  ( 1.451539297965124264, 1.489159454907125646, 1.289083465231783299 ) ) ;
#204530=CARTESIAN_POINT ( 'NONE',  ( 5.431847905162764611, -1.765542832439458198, 0.4050695418617160648 ) ) ;
#204536=CARTESIAN_POINT ( 'NONE',  ( 4.908994958506140094, 1.627828031611065152, 0.9215782234750914403 ) ) ;
#204538=CARTESIAN_POINT ( 'NONE',  ( 5.243061650278370678, -0.2479348644398685908, -2.055265572831247667 ) ) ;
#204547=CARTESIAN_POINT ( 'NONE',  ( 5.266048140081638351, -1.952571265509401854, 0.1905133553196102503 ) ) ;
#204549=CARTESIAN_POINT ( 'NONE',  ( 2.003279617838377824, 1.993765885540278004, 0.2985825316763612847 ) ) ;
#204551=CARTESIAN_POINT ( 'NONE',  ( 0.1874131419884322858, 1.628132678060219884, 1.467219630700428157 ) ) ;
#204552=CARTESIAN_POINT ( 'NONE',  ( 4.019144481351099252, -2.000086177330139492, 0.6089195546459759134 ) ) ;
#204553=CARTESIAN_POINT ( 'NONE',  ( 1.809613641711980359, -1.857008771552502768, 0.2239427725650791623 ) ) ;
#204555=CARTESIAN_POINT ( 'NONE',  ( 4.008068315354725186, -0.7665524943986418149, 1.861746286504823988 ) ) ;
#204558=CARTESIAN_POINT ( 'NONE',  ( 3.093478398350542946, -0.4104027421963015732, 2.076914780291692519 ) ) ;
#204560=CARTESIAN_POINT ( 'NONE',  ( 4.809070886388271404, -1.664838503569150419, 1.230558894880565246 ) ) ;
#204562=CARTESIAN_POINT ( 'NONE',  ( 0.9606207175340542026, -1.891748053602306578, -0.8905051939756128965 ) ) ;
#204563=CARTESIAN_POINT ( 'NONE',  ( 6.620655732516625314, 7.629137130509059617, 2.773739711112707340 ) ) ;
#204564=CARTESIAN_POINT ( 'NONE',  ( 6.176747059734421619, -1.734417727105644680, -0.5698399933231483860 ) ) ;
#204572=CARTESIAN_POINT ( 'NONE',  ( 6.498695769366850783, -1.876353784076413067, -0.3680397143606057853 ) ) ;
#204580=CARTESIAN_POINT ( 'NONE',  ( 5.589470316598125876, -0.4871849528341637425, 1.956566939648955339 ) ) ;
#204583=CARTESIAN_POINT ( 'NONE',  ( 0.1394461523056798324, 0.009327122704651937685, -1.719853553173174232 ) ) ;
#204586=CARTESIAN_POINT ( 'NONE',  ( 3.203910658309446990, 0.7132968404394635087, -1.835904812064126590 ) ) ;
#204587=CARTESIAN_POINT ( 'NONE',  ( 4.710564641745673242, 1.930423983604495630, 0.5826390268678026674 ) ) ;
#204590=CARTESIAN_POINT ( 'NONE',  ( 4.611385148785618782, -2.149487334021232599, 0.4259423572047504880 ) ) ;
#204592=CARTESIAN_POINT ( 'NONE',  ( 2.924735480247532937, 1.813364411391896969, 0.6504805730627157834 ) ) ;
#204594=CARTESIAN_POINT ( 'NONE',  ( -0.1298852118743893114, 2.060165343084968459, -2.144168685196511159 ) ) ;
#204596=EDGE_CURVE ( 'NONE', #89693, #200465, #27783, .T. ) ;
#204604=CARTESIAN_POINT ( 'NONE',  ( 0.1517630622446651534, 0.7442075171455504456, 1.793999140845178530 ) ) ;
#204605=CARTESIAN_POINT ( 'NONE',  ( 2.508449741805112154, -2.007837557984166299, -0.1460343770829114485 ) ) ;
#204606=CARTESIAN_POINT ( 'NONE',  ( 4.991759546967353245, 2.197549137908102246, 0.6733019004761026105 ) ) ;
#204608=CARTESIAN_POINT ( 'NONE',  ( 3.256551146222384396, -0.5358571751262303229, -1.782154170384263603 ) ) ;
#204611=CARTESIAN_POINT ( 'NONE',  ( 6.205323455156911194, 1.660478276859885582, -0.9486371710855368011 ) ) ;
#204614=CARTESIAN_POINT ( 'NONE',  ( 6.181206942494069878, 1.442326931096184151, 1.513799708994074900 ) ) ;
#204619=CARTESIAN_POINT ( 'NONE',  ( 0.9788029507734037349, -0.04229004422508231970, -1.825371421953936757 ) ) ;
#204621=CARTESIAN_POINT ( 'NONE',  ( 2.654579492894239223, 0.9294799389642364185, 1.463784073337747849 ) ) ;
#204626=CARTESIAN_POINT ( 'NONE',  ( 0.2333690889706682703, 0.003390530909083006028, -2.053566628440507635 ) ) ;
#204627=CARTESIAN_POINT ( 'NONE',  ( 6.006453938882227561, -0.6616566355047011072, -1.701761020394356283 ) ) ;
#204628=CARTESIAN_POINT ( 'NONE',  ( 3.274216958324972726, -0.9628348462043828659, -1.709115330885315309 ) ) ;
#204632=CARTESIAN_POINT ( 'NONE',  ( 4.108145954595856075, -0.8103754143699601897, 1.959725966023172727 ) ) ;
#204636=CARTESIAN_POINT ( 'NONE',  ( 2.114207291064807759, 2.064986537539798661, -0.1480984254652456533 ) ) ;
#204638=CARTESIAN_POINT ( 'NONE',  ( 5.092532722643547061, -1.235012376581679172, 1.846140261684477091 ) ) ;
#204639=ORIENTED_EDGE ( 'NONE', *, *, #9755, .T. ) ;
#204640=CARTESIAN_POINT ( 'NONE',  ( 2.268584743917153368, 2.099868620093465754, -0.9355518099330699666 ) ) ;
#204642=CARTESIAN_POINT ( 'NONE',  ( 6.473490848629269045, -0.2583879851764906976, 2.046290913384725130 ) ) ;
#204647=CARTESIAN_POINT ( 'NONE',  ( 6.614805131849967879, -0.1256686391097518729, 1.812046779126045726 ) ) ;
#204650=CARTESIAN_POINT ( 'NONE',  ( 3.146637304467227558, 1.866760668956708447, 0.4145885930168375921 ) ) ;
#204651=CARTESIAN_POINT ( 'NONE',  ( -0.2106725631050176961, 4.086973797293973476, -2.558389695104481554 ) ) ;
#204652=CARTESIAN_POINT ( 'NONE',  ( 4.313312247719586878, -0.2936513069345859650, 1.699412160066446909 ) ) ;
#204653=CARTESIAN_POINT ( 'NONE',  ( 2.466030083290056130, -1.032479112849067793, 1.731996155473938481 ) ) ;
#204654=CARTESIAN_POINT ( 'NONE',  ( 4.096513536321761073, -0.3929280286100769182, 2.264727396410810556 ) ) ;
#204655=CARTESIAN_POINT ( 'NONE',  ( 3.462467831702148668, 1.013738371934786331, 2.022624228200241348 ) ) ;
#204656=CARTESIAN_POINT ( 'NONE',  ( 6.199853529602823876, -0.7113111419616345854, 1.982453129600779462 ) ) ;
#204658=CARTESIAN_POINT ( 'NONE',  ( 4.833122733705673468, -1.618250600028045216, 0.7167863974541763827 ) ) ;
#204660=CARTESIAN_POINT ( 'NONE',  ( 1.131297326486919497, -2.070297854115164871, 0.9843215409001818683 ) ) ;
#204661=CARTESIAN_POINT ( 'NONE',  ( 6.070224334863941529, -1.749758606415029449, -0.5730458292283467925 ) ) ;
#204664=CARTESIAN_POINT ( 'NONE',  ( 5.701184558104195332, -0.5354452791076976803, 2.124913622581547479 ) ) ;
#204667=CARTESIAN_POINT ( 'NONE',  ( 6.391088794356012848, 0.1989163192229244648, 2.060770550043041993 ) ) ;
#204671=CARTESIAN_POINT ( 'NONE',  ( 3.844294682379956640, 1.917307101836130512, 0.1879692045662837430 ) ) ;
#204674=CARTESIAN_POINT ( 'NONE',  ( 1.406790049154776234, -2.211310019597735987, -0.2114152780076440363 ) ) ;
#204684=CARTESIAN_POINT ( 'NONE',  ( 1.680054527999317759, -1.087118939145682583, -1.632918184844594611 ) ) ;
#204687=CARTESIAN_POINT ( 'NONE',  ( 6.373494408814909917, -0.2414686440028299685, 1.946897059556201848 ) ) ;
#204690=CARTESIAN_POINT ( 'NONE',  ( 0.4622851218389683603, 2.237382594954186565, -0.3354954470186234383 ) ) ;
#204694=CARTESIAN_POINT ( 'NONE',  ( 1.088877184111051832, 1.652420591378000791, -0.8765777015899289815 ) ) ;
#204695=CARTESIAN_POINT ( 'NONE',  ( 6.884150274805287850, -0.1404709382532287054, 1.702994612897957394 ) ) ;
#204697=CARTESIAN_POINT ( 'NONE',  ( 4.265290774032561849, 2.125562838249666964, -0.5332280334861272397 ) ) ;
#204698=CARTESIAN_POINT ( 'NONE',  ( 4.436755630409714435, 2.262211819008316027, 0.4546042144240244887 ) ) ;
#204699=CARTESIAN_POINT ( 'NONE',  ( 0.1630570004950296636, -1.840724325608022127, -0.9269800520197747362 ) ) ;
#204700=CARTESIAN_POINT ( 'NONE',  ( 2.818227900350485982, 1.828750386608999356, 0.6536940613037258707 ) ) ;
#204704=CARTESIAN_POINT ( 'NONE',  ( 3.938125092175647879, -1.678004675797317713, -1.117833462672225497 ) ) ;
#204708=CARTESIAN_POINT ( 'NONE',  ( 0.5920835508136900183, -1.811502216344462735, -0.2265648652611390590 ) ) ;
#204713=CARTESIAN_POINT ( 'NONE',  ( 5.981337812661591258, 1.905142945929317211, -0.7864339424841911841 ) ) ;
#204719=CARTESIAN_POINT ( 'NONE',  ( 5.813150814160550794, 1.649844410012293539, -1.164645984317608463 ) ) ;
#204720=CARTESIAN_POINT ( 'NONE',  ( 5.197972062552532080, 1.490711083722006780, 1.646940351458234808 ) ) ;
#204723=CARTESIAN_POINT ( 'NONE',  ( 4.276283029400809177, -1.188189442049456535, 1.683678490072185285 ) ) ;
#204724=CARTESIAN_POINT ( 'NONE',  ( 3.604138833494671346, -0.1455340571130462057, 2.011204217620660373 ) ) ;
#204732=CARTESIAN_POINT ( 'NONE',  ( 4.499374939222855474, 1.976653413780619761, 0.3960398538903551757 ) ) ;
#204733=CARTESIAN_POINT ( 'NONE',  ( 3.732213890823964597, 0.2717154217161937280, 1.820854149191558635 ) ) ;
#204736=CARTESIAN_POINT ( 'NONE',  ( 1.893647147081824356, 2.006347305559322169, -1.140069799644787940 ) ) ;
#204738=CARTESIAN_POINT ( 'NONE',  ( 3.181113218772323226, -0.1555236193923059951, -2.156033859764289407 ) ) ;
#204741=CARTESIAN_POINT ( 'NONE',  ( 3.304404366906594337, -2.028264134497267168, 1.081039266028597234 ) ) ;
#204743=CARTESIAN_POINT ( 'NONE',  ( 2.061206331123175861, 0.3224310286589862629, -1.842498087946140561 ) ) ;
#204745=CARTESIAN_POINT ( 'NONE',  ( 6.491095702449441340, 1.715375089605765124, -0.9715357305846801239 ) ) ;
#204749=CARTESIAN_POINT ( 'NONE',  ( 1.418904949497600487, 1.480075412272121582, -1.637148382315711359 ) ) ;
#204754=CARTESIAN_POINT ( 'NONE',  ( 5.893431036533754330, 1.492594341498763466, 1.288039297220463730 ) ) ;
#204755=CARTESIAN_POINT ( 'NONE',  ( 5.215558013723960329, -0.3431011331927047991, 2.281934296042067878 ) ) ;
#204756=CARTESIAN_POINT ( 'NONE',  ( 0.6956633456795427994, -1.384754418207832405, -1.389998539416361423 ) ) ;
#204757=CARTESIAN_POINT ( 'NONE',  ( 2.764570516439817549, -0.7852151221510113022, -1.907448154738192514 ) ) ;
#204764=CARTESIAN_POINT ( 'NONE',  ( 5.406739488685087025, 0.6250254011054052761, 2.079287783280135304 ) ) ;
#204766=CARTESIAN_POINT ( 'NONE',  ( 5.513187957602974976, -1.795010045117376496, 0.4093405989887277663 ) ) ;
#204769=CARTESIAN_POINT ( 'NONE',  ( 0.4384654110765589530, 0.3132546388123040870, 1.843968665737522050 ) ) ;
#204770=CARTESIAN_POINT ( 'NONE',  ( 0.3864610594027502732, -1.064975819449946126, 1.996106434226818216 ) ) ;
#204775=CARTESIAN_POINT ( 'NONE',  ( -0.05814382529654647802, -1.176414490726215734, -1.508152472379259867 ) ) ;
#204776=CARTESIAN_POINT ( 'NONE',  ( 2.025891818203702233, 1.021928659931588435, -1.444778566663025954 ) ) ;
#204777=CARTESIAN_POINT ( 'NONE',  ( -0.1108833634136767443, 0.0002062650063822807356, -1.896853557917008271 ) ) ;
#204779=CARTESIAN_POINT ( 'NONE',  ( 2.899894056866093361, -0.9465274319002868753, -1.665356295385928442 ) ) ;
#204781=CARTESIAN_POINT ( 'NONE',  ( 4.193778028305522376, -1.356587754280412339, -1.428115657216560974 ) ) ;
#204782=CARTESIAN_POINT ( 'NONE',  ( 0.1410940620840978044, 2.031152781523197337, 0.6094965309384676733 ) ) ;
#204785=CARTESIAN_POINT ( 'NONE',  ( 2.623731232481395725, -1.075365945362505293, -1.530472918023266571 ) ) ;
#204786=CARTESIAN_POINT ( 'NONE',  ( 6.270102258788001315, 0.8933021238881621029, 1.475393591635131507 ) ) ;
#204788=CARTESIAN_POINT ( 'NONE',  ( 2.772332522587173997, 1.181257105606844160, 1.863944272329665086 ) ) ;
#204791=CARTESIAN_POINT ( 'NONE',  ( 6.514115657861259123, 1.956686900881845714, -0.1430618042221123987 ) ) ;
#204800=CARTESIAN_POINT ( 'NONE',  ( 3.543477799061961253, 1.872898848466747479, -0.8826743078152868849 ) ) ;
#204804=CARTESIAN_POINT ( 'NONE',  ( 0.3815177477655702920, 0.1955376695662625619, -2.010167716959633033 ) ) ;
#204807=CARTESIAN_POINT ( 'NONE',  ( 0.1745949693968510408, 0.7659234433113177865, -1.841618699378000601 ) ) ;
#204809=CARTESIAN_POINT ( 'NONE',  ( 4.903672622533054692, 0.3418847601762939337, 1.986741992616162245 ) ) ;
#204810=CARTESIAN_POINT ( 'NONE',  ( 5.366386423658583205, -1.870495304593930097, -0.4130858509987145877 ) ) ;
#204811=CARTESIAN_POINT ( 'NONE',  ( 6.539320575229276677, 6.035451701470580410, 2.698157228745074576 ) ) ;
#204812=CARTESIAN_POINT ( 'NONE',  ( 4.265290774032561849, 2.125562838249666964, -0.5332280334861272397 ) ) ;
#204814=CARTESIAN_POINT ( 'NONE',  ( 2.812653035604309348, -0.5591599321941118639, -1.828790038765286452 ) ) ;
#204818=CARTESIAN_POINT ( 'NONE',  ( 6.603150282362637569, -0.1459358296138096867, 2.084196934165093662 ) ) ;
#204820=CARTESIAN_POINT ( 'NONE',  ( 5.724229345562060089, 2.111793275502030554, 0.5857118945327836057 ) ) ;
#204822=CARTESIAN_POINT ( 'NONE',  ( 2.608071471510875039, -0.6576475463303601554, -1.594674760072743114 ) ) ;
#204828=CARTESIAN_POINT ( 'NONE',  ( 0.5726126529861442771, 1.355618539282506640, -1.418395753018865113 ) ) ;
#204836=CARTESIAN_POINT ( 'NONE',  ( 2.490610001455384470, -1.733883600701890737, -0.5244944224890700779 ) ) ;
#204840=CARTESIAN_POINT ( 'NONE',  ( 4.055163089163640322, -1.574157218682000758, 0.8962264629079966793 ) ) ;
#204844=CARTESIAN_POINT ( 'NONE',  ( 5.265987090187672415, -1.852092866064008803, 0.1821183643400964280 ) ) ;
#204846=CARTESIAN_POINT ( 'NONE',  ( 2.179167455442470480, 1.482148263166820801, 1.213602503745815353 ) ) ;
#204854=CARTESIAN_POINT ( 'NONE',  ( 0.9727375897880451427, -0.05299885879509737968, -2.090136731789421276 ) ) ;
#204855=CARTESIAN_POINT ( 'NONE',  ( 0.1647065507319189492, -1.628042339203483957, -0.8261295386280396169 ) ) ;
#204857=CARTESIAN_POINT ( 'NONE',  ( 2.625780896952558674, -1.049238153381076177, -1.493741879923994542 ) ) ;
#204858=CARTESIAN_POINT ( 'NONE',  ( 3.633602750639616019, -2.039237483250630589, 0.8441791899983088765 ) ) ;
#204861=CARTESIAN_POINT ( 'NONE',  ( 1.318461241437279607, -0.6911404020932455650, -1.783297644634279200 ) ) ;
#204862=CARTESIAN_POINT ( 'NONE',  ( 1.258185455790395979, -1.969739565659900160, -0.003359478883382254876 ) ) ;
#204863=CARTESIAN_POINT ( 'NONE',  ( 4.124509801231989847, 0.09871269697571230517, 1.939684287242355420 ) ) ;
#204867=CARTESIAN_POINT ( 'NONE',  ( 6.526204204079649962, 0.9558936715202811518, 1.596491800297286545 ) ) ;
#204872=CARTESIAN_POINT ( 'NONE',  ( 2.753686713869853531, 2.180749500395392282, -0.2175628297749406803 ) ) ;
#204876=CARTESIAN_POINT ( 'NONE',  ( 3.457459740917231628, 0.4424662778084071935, -1.771134634090239190 ) ) ;
#204877=CARTESIAN_POINT ( 'NONE',  ( 5.841029835422532734, -1.731992920607817288, -1.032484497598872064 ) ) ;
#204884=CARTESIAN_POINT ( 'NONE',  ( 4.065207594588423845, 0.2294239933214488880, -1.856472568989680161 ) ) ;
#204887=CARTESIAN_POINT ( 'NONE',  ( 1.928227594698066039, 1.109388971949121228, -1.574834034052971399 ) ) ;
#204888=CARTESIAN_POINT ( 'NONE',  ( 6.754749089495472703, -0.5201146403621333958, -1.891512521893109700 ) ) ;
#204893=CARTESIAN_POINT ( 'NONE',  ( 0.5095558700928676243, -2.008984845895735116, 0.6684745883070477568 ) ) ;
#204896=CARTESIAN_POINT ( 'NONE',  ( 4.645415698524104187, 1.851598927129451955, -0.9261206523473937136 ) ) ;
#204897=CARTESIAN_POINT ( 'NONE',  ( 0.01093749962182561514, -1.805946196879631094, 0.3578947576599255664 ) ) ;
#204900=CARTESIAN_POINT ( 'NONE',  ( 5.203857780826313117, 2.123009612837105209, 0.8817886472500915396 ) ) ;
#204904=CARTESIAN_POINT ( 'NONE',  ( 0.4633194693007875453, 0.2188196410306940398, -2.281803551658576179 ) ) ;
#204908=CARTESIAN_POINT ( 'NONE',  ( 4.962805208576138938, 0.1888075513713943498, -1.932747541012701964 ) ) ;
#204913=CARTESIAN_POINT ( 'NONE',  ( 6.099862406061942188, 1.323743610676546334, 1.380425988546908567 ) ) ;
#204914=CARTESIAN_POINT ( 'NONE',  ( 5.682827415814322158, 1.645762192317705486, -1.164983060713747909 ) ) ;
#204918=CARTESIAN_POINT ( 'NONE',  ( 2.396528757545500099, 1.678484640409601436, -1.246154833996036437 ) ) ;
#204919=CARTESIAN_POINT ( 'NONE',  ( 0.7601953647339227960, -1.285989511019115517, 1.216233164963770763 ) ) ;
#204922=CARTESIAN_POINT ( 'NONE',  ( 4.101757505036166762, -2.286240945789700607, 0.1669829803510776423 ) ) ;
#204923=CARTESIAN_POINT ( 'NONE',  ( 2.765247366594007605, 0.9310170973755277357, 1.470147560556547273 ) ) ;
#204926=CARTESIAN_POINT ( 'NONE',  ( 2.707414796094851361, 1.816601298730673220, -1.093838055662835096 ) ) ;
#204928=CARTESIAN_POINT ( 'NONE',  ( 1.774300323613137165, -1.721452415463576635, 0.2060816229845687519 ) ) ;
#204930=CARTESIAN_POINT ( 'NONE',  ( 1.961162895873772127, 1.544969826164013238, 1.037258533166736996 ) ) ;
#204931=CARTESIAN_POINT ( 'NONE',  ( 2.594372030776093574, 1.025359171358769306, -1.913825152921688311 ) ) ;
#204933=CARTESIAN_POINT ( 'NONE',  ( 3.872279980006509970, -1.995268062538615883, -0.2910826752766728642 ) ) ;
#204934=CARTESIAN_POINT ( 'NONE',  ( 2.187500000000001332, -1.451031289061030849, 1.451031289061208041 ) ) ;
#204936=CARTESIAN_POINT ( 'NONE',  ( 0.5164664324388609229, 1.330803901959699997, -1.393038531337851493 ) ) ;
#204938=CARTESIAN_POINT ( 'NONE',  ( 4.834350099735578610, -1.189287197132185669, -1.876079791293260079 ) ) ;
#204943=CARTESIAN_POINT ( 'NONE',  ( 0.7509959265504009274, 2.189410886431830239, 0.3742058002541984729 ) ) ;
#204944=CARTESIAN_POINT ( 'NONE',  ( 5.934033239752054989, 1.167398200610193282, 1.576599764842034457 ) ) ;
#204947=CARTESIAN_POINT ( 'NONE',  ( 5.448581927027607463, 0.6492139302081233465, 2.167288725150788409 ) ) ;
#204952=CARTESIAN_POINT ( 'NONE',  ( 3.402832357982612077, 0.4983898525147857361, 2.001458950477213339 ) ) ;
#204956=CARTESIAN_POINT ( 'NONE',  ( 4.305816765424046011, -1.865681898550693107, 0.1353468896250972775 ) ) ;
#204957=CARTESIAN_POINT ( 'NONE',  ( 3.639074924717408788, 0.6284830325712500443, 1.616442243290783232 ) ) ;
#204958=CARTESIAN_POINT ( 'NONE',  ( 3.491524089112467699, -1.738650433694358233, -0.08144215361822156052 ) ) ;
#204959=CARTESIAN_POINT ( 'NONE',  ( 0.5742758271649881507, -1.267216683205124150, 1.910101658145799020 ) ) ;
#204961=CARTESIAN_POINT ( 'NONE',  ( 4.774988821994140764, 1.950233014344885385, -0.7539837885136254636 ) ) ;
#204963=CARTESIAN_POINT ( 'NONE',  ( 5.560475942038150876, -1.756435177671934911, -0.8285927890409640062 ) ) ;
#204965=CARTESIAN_POINT ( 'NONE',  ( 2.468750000000001776, 0.7852924748298570901, -1.895863743164139859 ) ) ;
#204966=CARTESIAN_POINT ( 'NONE',  ( 0.5455463417442986129, -1.458554840210561476, 1.392547631435703037 ) ) ;
#204967=CARTESIAN_POINT ( 'NONE',  ( 0.8090202166558431163, -0.5209130535433897924, -2.055487714681260236 ) ) ;
#204973=CARTESIAN_POINT ( 'NONE',  ( 4.688025921862073453, -0.8580590012943272171, 1.611482198803436905 ) ) ;
#204980=CARTESIAN_POINT ( 'NONE',  ( 2.549087187268097576, 0.2513027392179004171, 2.004046050866041817 ) ) ;
#204981=CARTESIAN_POINT ( 'NONE',  ( 5.579209114504255496, -0.04897750150410771358, -2.206396493298476980 ) ) ;
#204984=CARTESIAN_POINT ( 'NONE',  ( 3.326847623520872155, -1.717698991579403422, -0.7164791247627964044 ) ) ;
#204987=EDGE_LOOP ( 'NONE', ( #46819, #197812, #70076, #129140 ) ) ;
#204991=CARTESIAN_POINT ( 'NONE',  ( 4.898959864523320107, 1.516061528642864253, -1.016892643307308441 ) ) ;
#204996=CARTESIAN_POINT ( 'NONE',  ( 0.2976278659034147789, -1.588993460933589841, 0.6942472086189295233 ) ) ;
#204997=CARTESIAN_POINT ( 'NONE',  ( 0.1634481287224815171, -1.141006008805772298, 1.314205411033820381 ) ) ;
#204998=CARTESIAN_POINT ( 'NONE',  ( 5.373738807407080209, 2.225351779437909183, -0.6107155785605354881 ) ) ;
#205000=CARTESIAN_POINT ( 'NONE',  ( 0.2454759580562664856, -1.591291808662575580, -1.309149871672641297 ) ) ;
#205002=CARTESIAN_POINT ( 'NONE',  ( 5.765083458594993715, -2.298542321979883507, -0.008455817729055568541 ) ) ;
#205005=CARTESIAN_POINT ( 'NONE',  ( 5.735183426005796115, -1.690533149647139410, 0.8011652756413772947 ) ) ;
#205006=CARTESIAN_POINT ( 'NONE',  ( 3.920094060441734030, -1.906919942518231936, 0.1457910263855527466 ) ) ;
#205008=CARTESIAN_POINT ( 'NONE',  ( 5.619807753665406302, -2.153844256707802440, 0.4802137346974973409 ) ) ;
#205009=CARTESIAN_POINT ( 'NONE',  ( 4.716069161646245789, 1.085680477651463915, -1.817652797078447735 ) ) ;
#205012=CARTESIAN_POINT ( 'NONE',  ( -0.2108831679770960255, 0.2438762813419328990, -1.931650693707862132 ) ) ;
#205015=CARTESIAN_POINT ( 'NONE',  ( 5.408877457991549953, -0.5154355754800542533, -2.056752310636373426 ) ) ;
#205016=CARTESIAN_POINT ( 'NONE',  ( 2.134188411380482098, -1.507708438093162018, -1.747028958505469909 ) ) ;
#205017=CARTESIAN_POINT ( 'NONE',  ( 3.420314466093795414, 0.8798059112791326575, 1.753580237611163994 ) ) ;
#205019=CARTESIAN_POINT ( 'NONE',  ( 5.875849835592577897, -2.013560656311346619, 0.4463529024570592751 ) ) ;
#205023=CARTESIAN_POINT ( 'NONE',  ( 5.559779856078610472, 1.205038519190555268, 1.616695979245158066 ) ) ;
#205027=CARTESIAN_POINT ( 'NONE',  ( 3.467796559821629820, -0.4283512159202977343, 2.128237193570106101 ) ) ;
#205029=CARTESIAN_POINT ( 'NONE',  ( 1.213308285724056690, 1.730450836393576886, -1.225479750871574458 ) ) ;
#205034=CARTESIAN_POINT ( 'NONE',  ( 1.141951006405941715, 0.8376953415718463303, -1.883039458060199900 ) ) ;
#205040=CARTESIAN_POINT ( 'NONE',  ( 3.844317892072905973, 1.020479721125296280, -1.617037373464407457 ) ) ;
#205042=CARTESIAN_POINT ( 'NONE',  ( 5.102326758870145973, -0.5985492928855026262, -1.665706573615277852 ) ) ;
#205046=CARTESIAN_POINT ( 'NONE',  ( -0.01774202353897573470, -1.183624524064251116, 1.371566177806067932 ) ) ;
#205048=CARTESIAN_POINT ( 'NONE',  ( 6.204688727450275110, 1.789332568231709608, 0.6845011832880606439 ) ) ;
#205049=CARTESIAN_POINT ( 'NONE',  ( 0.8540665308606997241, -0.7467690478978536994, 1.931163149162813619 ) ) ;
#205052=CARTESIAN_POINT ( 'NONE',  ( 6.051601594667258333, 0.5412791183288803154, -1.790613848972313571 ) ) ;
#205053=CARTESIAN_POINT ( 'NONE',  ( 2.824607995650964209, 1.719152210223941823, 0.6149139946348627372 ) ) ;
#205054=CARTESIAN_POINT ( 'NONE',  ( 5.285833163787800437, 1.479997892162682849, 1.637210856327932618 ) ) ;
#205057=CARTESIAN_POINT ( 'NONE',  ( 4.035635273026453085, 1.943268055400270811, -0.6920256600186375229 ) ) ;
#205062=CARTESIAN_POINT ( 'NONE',  ( 6.478973898625433492, 1.930320082341809629, 0.7489585856828018251 ) ) ;
#205064=CARTESIAN_POINT ( 'NONE',  ( 3.884175197147401892, -1.069116497136082700, 1.878640351225938421 ) ) ;
#205065=CARTESIAN_POINT ( 'NONE',  ( 4.354169037430507316, 0.8614980693376246279, -1.826848373156648497 ) ) ;
#205066=CARTESIAN_POINT ( 'NONE',  ( 1.592165322863370980, 0.9698756732311950568, -1.705302290208744687 ) ) ;
#205067=CARTESIAN_POINT ( 'NONE',  ( 6.620655732516610215, 1.221631503675042030, 2.386181433960798071 ) ) ;
#205073=CARTESIAN_POINT ( 'NONE',  ( 2.870327622459168726, -1.987497926849005836, -0.3399570244180456502 ) ) ;
#205077=CARTESIAN_POINT ( 'NONE',  ( 6.345967646908174054, -1.254484226688237669, -1.443505786478386899 ) ) ;
#205081=CARTESIAN_POINT ( 'NONE',  ( 4.956657736208940790, -1.899625167328807374, -0.6766988040120130998 ) ) ;
#205084=CARTESIAN_POINT ( 'NONE',  ( 6.000961845343044665, 1.407127125985812466, -0.9971243314716814465 ) ) ;
#205089=CARTESIAN_POINT ( 'NONE',  ( 4.569519670753737550, 1.814867081516871261, -0.4525428206468632975 ) ) ;
#205091=CARTESIAN_POINT ( 'NONE',  ( 2.307561340129569150, -1.660171796135110567, -1.236610361758017751 ) ) ;
#205095=CARTESIAN_POINT ( 'NONE',  ( 0.2457205463545810431, 1.994068899247893434, -0.2986513045247774500 ) ) ;
#205096=CARTESIAN_POINT ( 'NONE',  ( 0.6327121402699478203, 1.674153623460835627, 0.6926115325788273491 ) ) ;
#205102=CARTESIAN_POINT ( 'NONE',  ( 6.415652790497161639, -1.255571041358375384, -1.446825450776100919 ) ) ;
#205103=CIRCLE ( 'NONE', #111816, 0.04999999999999934358 ) ;
#205110=CARTESIAN_POINT ( 'NONE',  ( 3.327187652246216931, 0.05129554954072869377, 2.161254785723889515 ) ) ;
#205113=CARTESIAN_POINT ( 'NONE',  ( 1.318772358905948794, -0.7683209907942339933, -1.976687055281033611 ) ) ;
#205114=CARTESIAN_POINT ( 'NONE',  ( 6.211906940382025510, -1.811394037990306627, 0.2264786762415857968 ) ) ;
#205116=CARTESIAN_POINT ( 'NONE',  ( 1.616417101162690440, 1.326873100732330890, -1.458104111731808983 ) ) ;
#205117=CARTESIAN_POINT ( 'NONE',  ( 3.093911922779784440, 1.216618333484908998, 1.475457842794763996 ) ) ;
#205119=CARTESIAN_POINT ( 'NONE',  ( 5.266046268760843141, -1.960244874886694744, 0.1909964021715639393 ) ) ;
#205120=CARTESIAN_POINT ( 'NONE',  ( 0.3572357504952353158, 1.920940290975415854, -0.2841381762913769427 ) ) ;
#205125=CARTESIAN_POINT ( 'NONE',  ( 5.531871257421491883, -1.864710570029969317, 0.4231498525801706823 ) ) ;
#205128=CARTESIAN_POINT ( 'NONE',  ( 0.5521677985501523001, 0.6901698128830742185, -2.096122547012829962 ) ) ;
#205130=CARTESIAN_POINT ( 'NONE',  ( 5.971345465650553130, -1.727703365644253086, -1.033000238237492763 ) ) ;
#205132=CARTESIAN_POINT ( 'NONE',  ( 5.507046092540283766, -0.04465857163906890998, 2.016188657829049991 ) ) ;
#205134=CARTESIAN_POINT ( 'NONE',  ( 1.838419004579601834, -1.109345826794335688, 1.747895861591180156 ) ) ;
#205137=CARTESIAN_POINT ( 'NONE',  ( 0.3566080023540801336, 0.8287714912002723811, 1.996717379258300840 ) ) ;
#205143=CARTESIAN_POINT ( 'NONE',  ( 6.925078400183545035, 3.707308446744279617, 2.270182774727365516 ) ) ;
#205145=CARTESIAN_POINT ( 'NONE',  ( 4.482897354602959794, -1.733954122632981099, -0.03610910148283198728 ) ) ;
#205147=CARTESIAN_POINT ( 'NONE',  ( 2.184514099445804547, 1.195434181571125132, -1.690031224328606196 ) ) ;
#205148=CARTESIAN_POINT ( 'NONE',  ( 3.357133807288110727, 0.04956003552011908203, -2.116800119666595315 ) ) ;
#205151=CARTESIAN_POINT ( 'NONE',  ( 2.096482953606861432, 1.947282536051987201, 0.2939031187191037398 ) ) ;
#205153=CARTESIAN_POINT ( 'NONE',  ( -0.1581436608063293003, -1.178060542814472367, -1.506996232563104776 ) ) ;
#205154=CARTESIAN_POINT ( 'NONE',  ( 3.715000766203532034, -0.1696613574440029304, 2.286031353463747529 ) ) ;
#205155=CARTESIAN_POINT ( 'NONE',  ( 1.506192966688112644, -0.6554880476431452774, -1.704135612709246184 ) ) ;
#205160=CARTESIAN_POINT ( 'NONE',  ( 3.058842833410029272, 0.4931317667464900634, 1.951740033431844434 ) ) ;
#205161=CARTESIAN_POINT ( 'NONE',  ( 3.309375504473045293, -1.601080850277468715, -1.133301831143386007 ) ) ;
#205166=CARTESIAN_POINT ( 'NONE',  ( 6.158164957586691912, -1.479299979846586455, 1.477571280793017694 ) ) ;
#205167=CARTESIAN_POINT ( 'NONE',  ( 4.627684317651063139, -1.090007866362858291, -1.394274008033623113 ) ) ;
#205169=CARTESIAN_POINT ( 'NONE',  ( 0.8147124124333324779, 2.026155960571228043, 0.8354305900151803854 ) ) ;
#205170=CARTESIAN_POINT ( 'NONE',  ( 5.507646315527288117, -0.7876679103963373230, -1.551952608056671457 ) ) ;
#205173=CARTESIAN_POINT ( 'NONE',  ( 6.258407524398033495, 2.201109419358293628, -0.6625764064998507230 ) ) ;
#205175=CARTESIAN_POINT ( 'NONE',  ( 5.589090328658773643, 1.030979737101325400, -1.393799353210682046 ) ) ;
#205176=CARTESIAN_POINT ( 'NONE',  ( 2.121956728516772639, -2.140194184088719531, 0.5379336890513550795 ) ) ;
#205178=CARTESIAN_POINT ( 'NONE',  ( 5.266168369200141086, -2.161202989243858674, 0.2077703183603739345 ) ) ;
#205180=CARTESIAN_POINT ( 'NONE',  ( 0.7611333729100393519, -0.05844121263920940695, -2.116714853662078344 ) ) ;
#205181=CARTESIAN_POINT ( 'NONE',  ( 2.750000000000001332, 1.574424887750340441E-13, 2.052068128417947612 ) ) ;
#205183=CARTESIAN_POINT ( 'NONE',  ( 6.827182134110199030, 1.254919323356920025, 2.204230526214937758 ) ) ;
#205184=CARTESIAN_POINT ( 'NONE',  ( 4.348602224742101008, 0.5129591300635885087, 1.856786894687269207 ) ) ;
#205185=CARTESIAN_POINT ( 'NONE',  ( 1.647463811467297701, 0.2220449547728920447, 2.210189655316461277 ) ) ;
#205190=CARTESIAN_POINT ( 'NONE',  ( 3.493049024619375054, -2.141166226970441233, -0.5910787634417090652 ) ) ;
#205197=CARTESIAN_POINT ( 'NONE',  ( 1.881482635453747720, -0.5404922439061732309, -1.942541187959702764 ) ) ;
#205199=CARTESIAN_POINT ( 'NONE',  ( 6.109847269609326226, 0.6021898890512421554, -1.972802226155190297 ) ) ;
#205202=CARTESIAN_POINT ( 'NONE',  ( -0.09456490281532430042, -0.7861721075429689565, -1.663503389917226460 ) ) ;
#205205=CARTESIAN_POINT ( 'NONE',  ( 1.282078435845935616, -1.724974465617232999, -0.3947418589646100040 ) ) ;
#205206=CARTESIAN_POINT ( 'NONE',  ( 0.4928148368598186946, -2.006445878461552645, 0.2004378712678403507 ) ) ;
#205207=CARTESIAN_POINT ( 'NONE',  ( 6.181193141064822427, 1.207202257718576144, 1.253980304253142997 ) ) ;
#205208=CARTESIAN_POINT ( 'NONE',  ( 4.159948666787936844, 1.080635193647750292, 2.021704573604603095 ) ) ;
#205209=CARTESIAN_POINT ( 'NONE',  ( 2.607153984523866264, -1.821078476238715327, 0.2702138248509636242 ) ) ;
#205211=CARTESIAN_POINT ( 'NONE',  ( 3.346530664597209714, 0.4423686283943834563, 1.771051422834311051 ) ) ;
#205212=CARTESIAN_POINT ( 'NONE',  ( 3.727185537919291747, 2.006959858346604619, 0.1948421285040344286 ) ) ;
#205214=CARTESIAN_POINT ( 'NONE',  ( 3.766728628225763043, -1.521468805364207144, 1.674700015324230407 ) ) ;
#205216=CARTESIAN_POINT ( 'NONE',  ( 5.157299734135989411, -1.777537633589726163, -1.129047594716176217 ) ) ;
#205218=CARTESIAN_POINT ( 'NONE',  ( 2.242711981562468093, -2.029969483702593003, -0.4061203719310027549 ) ) ;
#205221=CARTESIAN_POINT ( 'NONE',  ( 5.250683377293950294, 2.089169806880130320, 0.3621421040747307973 ) ) ;
#205224=CARTESIAN_POINT ( 'NONE',  ( 1.225083325515680555, -0.04812572341393595021, 1.926057772195179485 ) ) ;
#205231=CARTESIAN_POINT ( 'NONE',  ( 0.4049022847291971483, -2.205595429402911201, -0.2640273158710532142 ) ) ;
#205232=CARTESIAN_POINT ( 'NONE',  ( 2.186679620839627969, -2.065140684961807249, -0.4117111178513747638 ) ) ;
#205235=CARTESIAN_POINT ( 'NONE',  ( 6.737149535461696814, -0.09068363363158969681, -1.858830251952103385 ) ) ;
#205240=CARTESIAN_POINT ( 'NONE',  ( 0.0004480315400831600455, -0.9938866557669153723, 1.873244595478529728 ) ) ;
#205243=CARTESIAN_POINT ( 'NONE',  ( 3.613678190204441254, 0.4790664972640528152, -1.902336835828049244 ) ) ;
#205244=CARTESIAN_POINT ( 'NONE',  ( 2.465889518630470789, 2.120156730345585938, -0.4209195040108040797 ) ) ;
#205245=CARTESIAN_POINT ( 'NONE',  ( 1.153568636672014369, 0.7464410156945017194, 1.683350060182234209 ) ) ;
#205248=CARTESIAN_POINT ( 'NONE',  ( 2.993823619545363801, -0.5058645990140339110, -1.665172204756032448 ) ) ;
#205251=CARTESIAN_POINT ( 'NONE',  ( 1.200320640528436789, -2.161883444890321915, 0.0006282887012112879947 ) ) ;
#205253=CARTESIAN_POINT ( 'NONE',  ( 2.671249783466634220, -0.7690017779844946499, -1.863883771055181660 ) ) ;
#205255=CARTESIAN_POINT ( 'NONE',  ( 0.3917762336288696523, 1.602822130585265015, 1.450656209987542855 ) ) ;
#205257=CARTESIAN_POINT ( 'NONE',  ( 2.289859582131337223, -0.8446868967569521880, 1.781483357239101117 ) ) ;
#205258=CARTESIAN_POINT ( 'NONE',  ( -0.02319159430947542386, 0.2540490248266329965, -1.846305437520213477 ) ) ;
#205263=CARTESIAN_POINT ( 'NONE',  ( -0.1106856583841060310, -0.002128758811529348188, -1.996853503091333470 ) ) ;
#205266=CARTESIAN_POINT ( 'NONE',  ( 2.402995385916364857, -0.3474029756719719808, -1.989407454614970261 ) ) ;
#205269=CARTESIAN_POINT ( 'NONE',  ( 5.438606028847273066, 2.272309368472532398, 0.4011960609803484901 ) ) ;
#205272=CARTESIAN_POINT ( 'NONE',  ( 4.241029431094700541, -0.1880360549168894613, -1.952691919460777026 ) ) ;
#205274=CARTESIAN_POINT ( 'NONE',  ( 0.08851783505585239520, -0.5350849913869708541, 1.944072358963434333 ) ) ;
#205276=CARTESIAN_POINT ( 'NONE',  ( 2.659486872612493613, 2.008994876937011398, -0.6687478447182227947 ) ) ;
#205280=CARTESIAN_POINT ( 'NONE',  ( 2.009460956091331685, -0.8672641894471898594, -1.624084198382821587 ) ) ;
#205285=CARTESIAN_POINT ( 'NONE',  ( 3.568700945156903614, 0.7666329941097769218, 1.977337035738421900 ) ) ;
#205286=CARTESIAN_POINT ( 'NONE',  ( 0.4449246239494052402, 0.5802587426733482046, -1.747387232072565189 ) ) ;
#205290=CARTESIAN_POINT ( 'NONE',  ( 3.936836037902153418, 0.2985264485904081111, 2.038899620686930536 ) ) ;
#205292=CARTESIAN_POINT ( 'NONE',  ( 1.909461114401575843, -0.8690924446688346183, -1.623246667998109682 ) ) ;
#205297=CARTESIAN_POINT ( 'NONE',  ( 0.6103625832605160673, -2.195865045534075133, 0.2202409711149767024 ) ) ;
#205298=CARTESIAN_POINT ( 'NONE',  ( 3.919400689748584465, -0.1713981403653370705, 2.255992170122776308 ) ) ;
#205300=CARTESIAN_POINT ( 'NONE',  ( 3.269578866965703767, 0.4354455071775619190, -1.758352452871074334 ) ) ;
#205301=CARTESIAN_POINT ( 'NONE',  ( 3.714002460163209562, 1.020071527678518164, -1.621341143276352703 ) ) ;
#205302=CARTESIAN_POINT ( 'NONE',  ( 5.371561628297467195, -0.3073141173523045167, 2.047320497149993646 ) ) ;
#205304=EDGE_CURVE ( 'NONE', #150638, #126115, #128385, .T. ) ;
#205305=CARTESIAN_POINT ( 'NONE',  ( 2.869950281991093810, 1.053363813896515788, 1.666286737264175866 ) ) ;
#205307=CARTESIAN_POINT ( 'NONE',  ( 0.9031967280443575774, 1.573137106080691572, 1.111599351221918663 ) ) ;
#205308=CARTESIAN_POINT ( 'NONE',  ( 3.537841792810627606, 0.8420186812403904764, -1.670516725672297031 ) ) ;
#205309=CARTESIAN_POINT ( 'NONE',  ( 2.139721691919532098, -2.060220725375282225, 1.039829281875967570 ) ) ;
#205310=CARTESIAN_POINT ( 'NONE',  ( 3.683913666659529795, -1.106983821303194171, -1.495880402381715824 ) ) ;
#205315=CARTESIAN_POINT ( 'NONE',  ( 0.9441299549096024979, 0.8517545906277513845, -1.926334332536754346 ) ) ;
#205319=CARTESIAN_POINT ( 'NONE',  ( 2.144932638433934002, 2.058100890041581810, 0.5106320605416380110 ) ) ;
#205321=CARTESIAN_POINT ( 'NONE',  ( 0.5979230068290807276, 1.359733756741304811, 1.493685216911154967 ) ) ;
#205325=CARTESIAN_POINT ( 'NONE',  ( 0.9312127099814873077, 0.1580370610147242560, 2.155845405312675211 ) ) ;
#205331=CARTESIAN_POINT ( 'NONE',  ( 6.315638730379727228, -1.320822524126588515, -1.523799118890494020 ) ) ;
#205333=CARTESIAN_POINT ( 'NONE',  ( 0.3631484714031462668, 0.2087870660046411420, -2.181583536649676525 ) ) ;
#205335=CARTESIAN_POINT ( 'NONE',  ( 0.1810634928296238622, -2.195609808662852824, -0.5457317257893978812 ) ) ;
#205339=CARTESIAN_POINT ( 'NONE',  ( 0.8607750341611281053, -0.04820650858186093651, -1.915179348411770954 ) ) ;
#205344=CARTESIAN_POINT ( 'NONE',  ( 2.666273504311657661, -1.189765394598929937, 1.249106299861786118 ) ) ;
#205346=CARTESIAN_POINT ( 'NONE',  ( 0.9832602892492541269, 1.182927327958797070, 1.316506037215345426 ) ) ;
#205348=CARTESIAN_POINT ( 'NONE',  ( 1.822903811843211264, 1.490285103888006280, -1.353523025221949450 ) ) ;
#205350=CARTESIAN_POINT ( 'NONE',  ( 4.717920652503574175, -2.164970738276258189, 0.4266498443898231185 ) ) ;
#205352=VERTEX_POINT ( 'NONE', #110050 ) ;
#205355=CARTESIAN_POINT ( 'NONE',  ( 4.143311163141574660, 0.1052805922370502884, 2.118007119816091688 ) ) ;
#205356=CARTESIAN_POINT ( 'NONE',  ( 3.919546125582054508, -1.392558991000433011, -1.458545569310132350 ) ) ;
#205360=CARTESIAN_POINT ( 'NONE',  ( 1.076777757339364205, -0.04213119042271313425, -1.870346338061685154 ) ) ;
#205372=CARTESIAN_POINT ( 'NONE',  ( 4.219064148821600746, 1.637239594409030330, -1.347683705884415106 ) ) ;
#205373=CARTESIAN_POINT ( 'NONE',  ( -0.1296875068447882473, 5.724785194352729256, -2.420566058096422779 ) ) ;
#205375=CARTESIAN_POINT ( 'NONE',  ( 5.782488548463037503, -1.922744423562244620, -0.4343835447332323740 ) ) ;
#205377=CARTESIAN_POINT ( 'NONE',  ( 0.3869771421881840201, -1.897093440144840937, -0.6742409396158774992 ) ) ;
#205378=ORIENTED_EDGE ( 'NONE', *, *, #204318, .F. ) ;
#205379=CARTESIAN_POINT ( 'NONE',  ( 6.175037754964278314, 1.841102675566621771, -1.045632355512320144 ) ) ;
#205381=CARTESIAN_POINT ( 'NONE',  ( 1.029834584532058672, 1.995790600324919506, -0.5504719462680053299 ) ) ;
#205385=CARTESIAN_POINT ( 'NONE',  ( 3.539087885488776397, -1.583190213782994515, -1.365486535101219534 ) ) ;
#205389=CARTESIAN_POINT ( 'NONE',  ( 2.291784574284541964, -0.7830779901500490858, 1.649245556672715995 ) ) ;
#205390=CARTESIAN_POINT ( 'NONE',  ( 1.558926746901686089, -1.530267751544078347, 0.9690644009569903128 ) ) ;
#205392=CARTESIAN_POINT ( 'NONE',  ( 5.953802724510454780, 0.6443607167232848765, -2.110727517106169682 ) ) ;
#205394=CARTESIAN_POINT ( 'NONE',  ( 4.173040645679537697, -2.057929556117383374, -0.7971749352265260491 ) ) ;
#205396=CARTESIAN_POINT ( 'NONE',  ( 2.578645926699867363, -1.317302948579327504, 1.386430337501590282 ) ) ;
#205398=CARTESIAN_POINT ( 'NONE',  ( 5.652806998763869828, -0.4994405740583847675, -2.009109930559597856 ) ) ;
#205400=CARTESIAN_POINT ( 'NONE',  ( 6.409741707328596938, -1.031184584194230647, -1.933826218581576439 ) ) ;
#205411=CARTESIAN_POINT ( 'NONE',  ( 6.209843387784004243, 0.6066176463192971546, -1.979359621541395331 ) ) ;
#205412=CARTESIAN_POINT ( 'NONE',  ( 4.617753627809100259, -1.889021752119159459, 0.3773520080231194673 ) ) ;
#205414=CARTESIAN_POINT ( 'NONE',  ( 1.634388897023292486, 0.6352195160324504153, 1.913798142305182415 ) ) ;
#205419=CARTESIAN_POINT ( 'NONE',  ( 1.851786237446376049, 2.185420115623282200, -0.1633297828415938846 ) ) ;
#205420=CARTESIAN_POINT ( 'NONE',  ( 5.022008369909983116, -0.9795521577263366364, -1.540466923627185292 ) ) ;
#205427=CARTESIAN_POINT ( 'NONE',  ( 2.366542893654680402, 0.08848056876738576160, -1.839231530397527736 ) ) ;
#205428=CARTESIAN_POINT ( 'NONE',  ( 6.029547050951932441, -0.2422988993314358630, 1.998484822443524322 ) ) ;
#205429=CARTESIAN_POINT ( 'NONE',  ( 1.775234297868668376, -2.280957755244545027, 0.2818987734495673192 ) ) ;
#205430=CARTESIAN_POINT ( 'NONE',  ( 0.2388273096324589895, -0.1346187373043924163, -1.830540737478093982 ) ) ;
#205433=CARTESIAN_POINT ( 'NONE',  ( 2.865378420500460876, -1.565876230000915692, -1.097592462808501645 ) ) ;
#205438=CARTESIAN_POINT ( 'NONE',  ( 2.665665183201745947, 1.120710701610077908, 1.764813211807507942 ) ) ;
#205439=CARTESIAN_POINT ( 'NONE',  ( 0.7427767429722329506, -1.606530860214189893, 0.9580933318182258684 ) ) ;
#205440=CARTESIAN_POINT ( 'NONE',  ( 2.319685276966905629, -1.560262528187049025, 1.276846253076675541 ) ) ;
#205444=CARTESIAN_POINT ( 'NONE',  ( 2.577381053492054264, -0.8929794387350452611, 1.493718712549793715 ) ) ;
#205448=CARTESIAN_POINT ( 'NONE',  ( 3.088212622510533301, -1.699425283745788162, -0.2941843989033367524 ) ) ;
#205449=( BOUNDED_CURVE ( )  B_SPLINE_CURVE ( 3, ( #81924, #13718, #144848, #115553 ),
 .UNSPECIFIED., .F., .T. ) 
 B_SPLINE_CURVE_WITH_KNOTS ( ( 4, 4 ),
 ( 0.5000000000000027756, 1.000000000000000000 ),
 .UNSPECIFIED. ) 
 CURVE ( )  GEOMETRIC_REPRESENTATION_ITEM ( )  RATIONAL_B_SPLINE_CURVE ( ( 0.9999999999999963363, 0.3333333333333333703, 0.3333333333333370896, 1.000000000000000000 ) ) 
 REPRESENTATION_ITEM ( '' )  );
#205450=CARTESIAN_POINT ( 'NONE',  ( 2.894263506066748093, -0.6386881658498286818, -2.096408367471907841 ) ) ;
#205451=CARTESIAN_POINT ( 'NONE',  ( 7.214646527853999024E-05, -1.701284277595259464, 0.3348680416483724720 ) ) ;
#205452=CARTESIAN_POINT ( 'NONE',  ( 4.969440760808212509, 0.2186952961555181096, -2.196011921426939129 ) ) ;
#205454=CARTESIAN_POINT ( 'NONE',  ( 2.044024736616629312, 1.494777392302085062, 1.574780046323517313 ) ) ;
#205455=CARTESIAN_POINT ( 'NONE',  ( 1.435882461153328515, 0.9014729512111450127, -1.587519582607027635 ) ) ;
#205457=CARTESIAN_POINT ( 'NONE',  ( 3.977823109611013930, -0.8067237889231733128, 1.957824063906116407 ) ) ;
#205460=CARTESIAN_POINT ( 'NONE',  ( 4.652058317211603011, 0.8762739730861779375, 2.118468771859642441 ) ) ;
#205464=CARTESIAN_POINT ( 'NONE',  ( -0.07530339154229391541, -0.9103892951793614019, -1.913193754492636067 ) ) ;
#205471=CARTESIAN_POINT ( 'NONE',  ( 4.799454022740247794, 1.388487131293577592, -1.462444391756134943 ) ) ;
#205473=CARTESIAN_POINT ( 'NONE',  ( 3.555586659033848740, 1.623084692090390080, 1.272569074839409398 ) ) ;
#205475=CARTESIAN_POINT ( 'NONE',  ( 6.883263157960364254, 6.036844454314826081, 2.541088405340941492 ) ) ;
#205479=CARTESIAN_POINT ( 'NONE',  ( 6.703104427915338448, -0.4847493572297522091, 2.145077170986497528 ) ) ;
#205480=CARTESIAN_POINT ( 'NONE',  ( 3.604138833494671346, -0.1455340571130462057, 2.011204217620660817 ) ) ;
#205481=CARTESIAN_POINT ( 'NONE',  ( 2.999365392321148516, -1.839032331094083927, 0.09308366406014097205 ) ) ;
#205483=CARTESIAN_POINT ( 'NONE',  ( 6.018537349360657984, 1.224031959697377658, -1.354583942311540667 ) ) ;
#205485=CARTESIAN_POINT ( 'NONE',  ( 6.719576162335838099, -2.196678875378419882, 0.5415391501680610897 ) ) ;
#205486=CARTESIAN_POINT ( 'NONE',  ( 2.121831256377606501, -2.042539606455844758, 0.5128510974094899755 ) ) ;
#205495=CARTESIAN_POINT ( 'NONE',  ( 2.127334043950947606, 1.896359100603739911, 0.9491756072362851349 ) ) ;
#205496=CARTESIAN_POINT ( 'NONE',  ( 4.219114570843409240, 1.715941675311336123, -1.410698622648777434 ) ) ;
#205497=CARTESIAN_POINT ( 'NONE',  ( 2.906388222866810978, 1.586772471669075424, -1.511725739355776366 ) ) ;
#205498=CARTESIAN_POINT ( 'NONE',  ( 0.8036966383840878914, 1.806304194667744500, 1.267646993260997723 ) ) ;
#205500=CARTESIAN_POINT ( 'NONE',  ( 4.650807877244386823, -0.4278111053654386486, -1.914496481071884970 ) ) ;
#205508=CARTESIAN_POINT ( 'NONE',  ( 3.902672080109194752, -2.098000727953463151, -0.3078000538283761078 ) ) ;
#205510=CARTESIAN_POINT ( 'NONE',  ( 5.383715653711652394, 1.448795075966866852, 1.604530791579752202 ) ) ;
#205511=CARTESIAN_POINT ( 'NONE',  ( 3.737712173649463399, 1.832726675769575486, 0.1767833568970395008 ) ) ;
#205514=CARTESIAN_POINT ( 'NONE',  ( 6.439394946090388316, 0.6587646163928980725, -1.611052209844960670 ) ) ;
#205515=CARTESIAN_POINT ( 'NONE',  ( 6.827182134110201694, 1.288579688585177685, 1.926502426867699569 ) ) ;
#205518=CARTESIAN_POINT ( 'NONE',  ( 4.522454563201145028, 1.332364063043836033, -1.702191164408660251 ) ) ;
#205520=CARTESIAN_POINT ( 'NONE',  ( 6.081407632663145435, 1.356090666932512789, -1.492028312255622824 ) ) ;
#205522=CARTESIAN_POINT ( 'NONE',  ( 3.907220446582274853, 1.852832235905249370, 1.113321777468062823 ) ) ;
#205523=CARTESIAN_POINT ( 'NONE',  ( 4.973880039175529788, 1.132619354422999436, 1.613344424267410204 ) ) ;
#205524=CARTESIAN_POINT ( 'NONE',  ( 4.024493581903946016, 1.720846971656955438, -0.2109413284564972679 ) ) ;
#205525=CARTESIAN_POINT ( 'NONE',  ( 0.5565083568685527116, -1.583368386835169783, 1.515454571103365344 ) ) ;
#205526=CARTESIAN_POINT ( 'NONE',  ( 0.6577796130948220243, -1.951556776833747620, -1.231164357708439017 ) ) ;
#205527=CARTESIAN_POINT ( 'NONE',  ( 3.866525002278593526, -1.386861471309716265, 1.524430686435477522 ) ) ;
#205528=CARTESIAN_POINT ( 'NONE',  ( 5.530791563722144311, -1.753914071513791528, 0.8342105869050663314 ) ) ;
#205534=CARTESIAN_POINT ( 'NONE',  ( 2.116530880626496192, -1.040147864624408003, -1.946245422063937802 ) ) ;
#205537=CARTESIAN_POINT ( 'NONE',  ( 0.4439182389155779673, -0.8842316343482552465, 1.637490449460777153 ) ) ;
#205538=CARTESIAN_POINT ( 'NONE',  ( -0.1291982275798443380, 0.7147424134107607241, -2.157361641090648874 ) ) ;
#205544=CARTESIAN_POINT ( 'NONE',  ( 2.553650737195617637, 0.5510486643308718513, -1.985768735985605549 ) ) ;
#205550=CARTESIAN_POINT ( 'NONE',  ( 0.7431281084272289839, -1.767980789219452342, 1.058748425497215262 ) ) ;
#205552=CARTESIAN_POINT ( 'NONE',  ( 4.669393045487420402, 1.064170941109745305, 1.502380130741477693 ) ) ;
#205557=CARTESIAN_POINT ( 'NONE',  ( 4.899154391205060577, 1.836108854712194649, -1.224054507610386366 ) ) ;
#205558=CARTESIAN_POINT ( 'NONE',  ( 0.2808502495336914206, -2.096634173354972486, -0.5254431554712820640 ) ) ;
#205560=CARTESIAN_POINT ( 'NONE',  ( 0.4043728756845180183, -1.898191424145349471, -0.2318213773434482650 ) ) ;
#205561=CARTESIAN_POINT ( 'NONE',  ( 0.5851731681005939434, 1.651346252830317551, 1.157095189655330314 ) ) ;
#205568=CARTESIAN_POINT ( 'NONE',  ( 0.4615142869485132637, 1.850934062480696252, -0.2700578556205368574 ) ) ;
#205569=CARTESIAN_POINT ( 'NONE',  ( 1.921111612355221654, -1.799121770747251547, 0.9110121207814986244 ) ) ;
#205573=CARTESIAN_POINT ( 'NONE',  ( 4.529967234949650035, -1.295318019757265349, -1.660530462842347177 ) ) ;
#205579=CARTESIAN_POINT ( 'NONE',  ( 3.832289616293593770, -1.041828873002103917, -1.730228960026259255 ) ) ;
#205581=CARTESIAN_POINT ( 'NONE',  ( 6.039522989413334209, 1.907243403200251208, -0.7859975451465596175 ) ) ;
#205583=CARTESIAN_POINT ( 'NONE',  ( 4.147864318636265146, 0.7325676050485960822, -2.033789780341701547 ) ) ;
#205589=CARTESIAN_POINT ( 'NONE',  ( 1.979201191301533047, 2.025398335218126622, 0.7825711269493199618 ) ) ;
#205592=CARTESIAN_POINT ( 'NONE',  ( 1.259045258496578557, 1.813921241667546758, -0.3151448728593714277 ) ) ;
#205594=CARTESIAN_POINT ( 'NONE',  ( 3.527062600443749307, -2.024233912922444478, 0.8403589366152917073 ) ) ;
#205595=CARTESIAN_POINT ( 'NONE',  ( 6.983263157960362122, 6.035089925019382129, 2.648702789725385198 ) ) ;
#205596=CARTESIAN_POINT ( 'NONE',  ( 3.872163259867720253, 1.254437384476282835, 1.882731698358128369 ) ) ;
#205602=CARTESIAN_POINT ( 'NONE',  ( 5.413276439055476175, -0.2588944790761596448, 1.750576072867173316 ) ) ;
#205604=CARTESIAN_POINT ( 'NONE',  ( 1.676933785844336944, -1.999498008410249383, -0.6612845060171600453 ) ) ;
#205608=CARTESIAN_POINT ( 'NONE',  ( 1.310928286630644646, -1.554615626247756177, 1.209165358520351674 ) ) ;
#205611=CARTESIAN_POINT ( 'NONE',  ( 6.082253981448354274, 0.9392408507493594794, 1.548964021007705139 ) ) ;
#205614=CARTESIAN_POINT ( 'NONE',  ( 5.242975984329111050, -1.603930480038592510, 0.9624218375651681923 ) ) ;
#205615=CARTESIAN_POINT ( 'NONE',  ( 4.944224162298806569, -0.9806570695735459253, 1.823293813017504039 ) ) ;
#205627=CARTESIAN_POINT ( 'NONE',  ( 4.492601031306558745, 1.923586649950057792, 0.3847822903023030428 ) ) ;
#205629=CARTESIAN_POINT ( 'NONE',  ( 2.020861031540205133, 2.010896488828680440, -0.1455087364366919322 ) ) ;
#205632=CARTESIAN_POINT ( 'NONE',  ( 1.915107840602244593, -0.2339084544023955492, 1.855816807740391150 ) ) ;
#205634=CARTESIAN_POINT ( 'NONE',  ( 4.025643311844375738, -0.3400233446379635760, 1.984125136466656558 ) ) ;
#205637=CARTESIAN_POINT ( 'NONE',  ( 2.970428505833659472, -2.086373159142587586, -0.3592635996705355050 ) ) ;
#205639=CARTESIAN_POINT ( 'NONE',  ( 4.738769824615551407, -2.007376682328159134, -0.5062664373569197851 ) ) ;
#205641=CARTESIAN_POINT ( 'NONE',  ( 0.9957797365991372107, -2.090933974770115444, 0.003689723154384760839 ) ) ;
#205642=CARTESIAN_POINT ( 'NONE',  ( 6.620655732516649294, 0.5674144795907026806, 2.226195167976598110 ) ) ;
#205643=CARTESIAN_POINT ( 'NONE',  ( 6.651389018303578204, -1.468406013062272253, -1.084454090978362428 ) ) ;
#205651=CARTESIAN_POINT ( 'NONE',  ( 6.235011639695052565, 1.786057601157979180, 0.6837302122261402770 ) ) ;
#205660=CARTESIAN_POINT ( 'NONE',  ( 5.132435489663482286, 0.5880379476735001498, 1.928747580961232444 ) ) ;
#205663=CARTESIAN_POINT ( 'NONE',  ( 0.1399997263886038068, 6.947785072119228467, -2.594798351071639253 ) ) ;
#205666=CARTESIAN_POINT ( 'NONE',  ( 2.114047118560181016, 1.964524245714272643, -0.1396653253868378186 ) ) ;
#205667=CARTESIAN_POINT ( 'NONE',  ( 4.587517648402447357, -0.5350702435001615243, 1.944077497823355483 ) ) ;
#205669=CARTESIAN_POINT ( 'NONE',  ( 6.727182134110196721, 7.051813866762763006, 2.787205683092201181 ) ) ;
#205670=CARTESIAN_POINT ( 'NONE',  ( 4.382901342696458258, 1.958101449220098988, -0.9841704303943515919 ) ) ;
#205672=CARTESIAN_POINT ( 'NONE',  ( 3.469672154888691296, 1.879743449303279634, -0.4207095485242727806 ) ) ;
#205675=CARTESIAN_POINT ( 'NONE',  ( 0.04788047853313340263, -1.708876078042343316, -1.396090968258607790 ) ) ;
#205682=CARTESIAN_POINT ( 'NONE',  ( 6.058133912487986272, -1.297239342979487509, 1.306937132449899508 ) ) ;
#205683=CARTESIAN_POINT ( 'NONE',  ( 2.473293533796361299, -1.752518403998115426, -0.9904139345979168230 ) ) ;
#205684=CARTESIAN_POINT ( 'NONE',  ( 5.325646502758397460, -1.669998024346308618, 1.579374382026963675 ) ) ;
#205686=CARTESIAN_POINT ( 'NONE',  ( 2.869781510094356669, -1.841417136736220650, 0.2678509365347056526 ) ) ;
#205693=CARTESIAN_POINT ( 'NONE',  ( 6.356985058417449430, 0.3567463788109735967, -2.059909276252298582 ) ) ;
#205699=CARTESIAN_POINT ( 'NONE',  ( 5.953657690368134858, 0.4940546211441557700, -1.652608054245385372 ) ) ;
#205701=CARTESIAN_POINT ( 'NONE',  ( 1.986549370914699963, -1.733795460411426959, 0.04323319158786724514 ) ) ;
#205706=CARTESIAN_POINT ( 'NONE',  ( 0.5849358142855852760, 1.980036476162419845, 0.6043757699017647811 ) ) ;
#205707=CARTESIAN_POINT ( 'NONE',  ( 5.320859459983126705, 1.688362619374352613, 0.6951667914897319278 ) ) ;
#205708=CARTESIAN_POINT ( 'NONE',  ( 2.131626046773547500, 1.878804184644796926, -0.5645400877590660560 ) ) ;
#205712=CARTESIAN_POINT ( 'NONE',  ( 3.457788318579996467, -1.606868461378293755, -1.383752881913953292 ) ) ;
#205715=CARTESIAN_POINT ( 'NONE',  ( 1.903268718874175480, -1.751121435885591548, 1.104011288380807532 ) ) ;
#205719=CARTESIAN_POINT ( 'NONE',  ( 2.912952216767932256, -0.6468334258018549887, -2.125021405654815787 ) ) ;
#205721=CARTESIAN_POINT ( 'NONE',  ( 1.424907242902058613, -1.669187457468356950, -1.580674740522235888 ) ) ;
#205723=CARTESIAN_POINT ( 'NONE',  ( 6.420768979138045118, -1.462686491410120970, 1.454469991251945649 ) ) ;
#205729=CARTESIAN_POINT ( 'NONE',  ( -0.1106727585415940990, -0.002281114264979232885, -2.003378291782103027 ) ) ;
#205730=CARTESIAN_POINT ( 'NONE',  ( 2.994803049195310596, 1.480226043003279424, -0.8850232739186939535 ) ) ;
#205731=CARTESIAN_POINT ( 'NONE',  ( 2.026577684455236561, 0.4465047249504557891, 1.966304233017155845 ) ) ;
#205732=CARTESIAN_POINT ( 'NONE',  ( 2.567332952821321790, -1.178922594190381146, 1.973231532614614148 ) ) ;
#205734=CARTESIAN_POINT ( 'NONE',  ( 3.110884140487602867, 1.641001393266024788, -1.557680395459557499 ) ) ;
#205735=CARTESIAN_POINT ( 'NONE',  ( 5.444006973519509351, 0.8546016068469390881, -1.925070404590538242 ) ) ;
#205738=CARTESIAN_POINT ( 'NONE',  ( 3.567426164108201903, 1.727176351593662007, -0.3850055527321315507 ) ) ;
#205740=CARTESIAN_POINT ( 'NONE',  ( 0.5688445697737016804, -2.160344153581617022, -0.7667740616737575010 ) ) ;
#205741=CARTESIAN_POINT ( 'NONE',  ( 5.859284738525260217, 1.813109059707292747, -0.3191327317438249489 ) ) ;
#205744=CARTESIAN_POINT ( 'NONE',  ( 5.683573789218531402, -0.9880169931659465998, 1.956149625775935430 ) ) ;
#205747=CARTESIAN_POINT ( 'NONE',  ( 6.426242046702522082, 1.060841730010402495, 1.777776562702712226 ) ) ;
#205748=CARTESIAN_POINT ( 'NONE',  ( 0.05782782957228919940, 1.164991625563294386, 1.645756161228327130 ) ) ;
#205751=CARTESIAN_POINT ( 'NONE',  ( 4.565017902933249161, -1.721472425840556930, -0.8649740032428044900 ) ) ;
#205755=CARTESIAN_POINT ( 'NONE',  ( 1.283751863706618535, 0.1568931172264090290, -2.215910488618375584 ) ) ;
#205765=CARTESIAN_POINT ( 'NONE',  ( 1.275752070009423367, -1.914805681740685106, 0.4264308320794732432 ) ) ;
#205769=CARTESIAN_POINT ( 'NONE',  ( 0.4321753131953905980, 1.186194839137414414, 1.687308244272892166 ) ) ;
#205773=CARTESIAN_POINT ( 'NONE',  ( 0.6204658552826959328, -1.213099742399858627, -1.909634413763374283 ) ) ;
#205777=CARTESIAN_POINT ( 'NONE',  ( 1.124039026005444475, 1.118881483734196935, -1.498852260102357947 ) ) ;
#205778=CARTESIAN_POINT ( 'NONE',  ( 0.3868564640647629282, -0.5820622975930835885, -1.633661194748408541 ) ) ;
#205780=CARTESIAN_POINT ( 'NONE',  ( 4.458633810090739225, -1.957822973221786444, -0.9849130632908836835 ) ) ;
#205781=CARTESIAN_POINT ( 'NONE',  ( 4.542184868284099508, 0.9910628492805847456, -2.084066998532303483 ) ) ;
#205782=CARTESIAN_POINT ( 'NONE',  ( 0.3564142383026321914, 0.7882222137287850927, 1.904402214580179331 ) ) ;
#205783=CARTESIAN_POINT ( 'NONE',  ( 2.835803868134049388, 1.927321602952759338, 0.2373744266383533696 ) ) ;
#205785=CIRCLE ( 'NONE', #91721, 0.04999999999999929501 ) ;
#205787=CARTESIAN_POINT ( 'NONE',  ( 5.203433420164765622, 1.869144303625443371, -1.001675624404389620 ) ) ;
#205789=CARTESIAN_POINT ( 'NONE',  ( 3.955704058034177351, -1.882473782773282700, -0.7231407674024927790 ) ) ;
#205793=CARTESIAN_POINT ( 'NONE',  ( 0.6272434487209905818, -1.734552980249819631, 0.5698080454362154379 ) ) ;
#205798=CARTESIAN_POINT ( 'NONE',  ( 5.928604924596339032, 1.985460353506541376, 0.5521678710885301600 ) ) ;
#205803=CARTESIAN_POINT ( 'NONE',  ( 4.705726078268232193, 1.497967940706146805, 1.354894159888963001 ) ) ;
#205804=CARTESIAN_POINT ( 'NONE',  ( 6.024141157665446222, -2.204869988984262896, 0.2693334978098835264 ) ) ;
#205809=CARTESIAN_POINT ( 'NONE',  ( 3.871991401782824749, 1.143396993664235417, 1.714400680826788426 ) ) ;
#205810=CARTESIAN_POINT ( 'NONE',  ( 4.535779832184696936, -1.617819081767550182, 1.203352566194588746 ) ) ;
#205817=CARTESIAN_POINT ( 'NONE',  ( 4.235703761680151835, -1.880146911114020325, -0.7282675588539261335 ) ) ;
#205818=CARTESIAN_POINT ( 'NONE',  ( 2.730204174461122069, 0.2256132759956077649, 1.827196471909063202 ) ) ;
#205820=CARTESIAN_POINT ( 'NONE',  ( 1.594773108836315956, -2.296930430523877575, -0.2226743027769726713 ) ) ;
#205823=CARTESIAN_POINT ( 'NONE',  ( 4.077527805175058973, 2.036875575534887961, -0.7240464584713502960 ) ) ;
#205826=CARTESIAN_POINT ( 'NONE',  ( 3.532835791020246141, 2.243242391287715964, -0.4999081842005962395 ) ) ;
#205829=CARTESIAN_POINT ( 'NONE',  ( 2.658895327995167701, -1.626580691111865207, -0.9237732865615968514 ) ) ;
#205830=CARTESIAN_POINT ( 'NONE',  ( 6.772342980177176841, -1.213407086615119423, 1.554582774731553707 ) ) ;
#205834=CARTESIAN_POINT ( 'NONE',  ( 1.102499568101540817, -2.207063161980229005, 0.003256074490760872773 ) ) ;
#205839=CARTESIAN_POINT ( 'NONE',  ( 6.350460794227542394, 0.6179267841925452087, 1.872200446973372179 ) ) ;
#205840=CARTESIAN_POINT ( 'NONE',  ( 5.356226580172758212, 2.305273348739949935, -0.1085102657557151934 ) ) ;
#205841=CARTESIAN_POINT ( 'NONE',  ( 6.689920442068890694, -1.216917952458838270, -1.408172490277598721 ) ) ;
#205842=ADVANCED_FACE ( 'NONE', ( #54863 ), #91561, .T. ) ;
#205843=CARTESIAN_POINT ( 'NONE',  ( 3.379784452013841367, -1.989113752706978433, 0.5454275443767720999 ) ) ;
#205850=CARTESIAN_POINT ( 'NONE',  ( 5.283699308645180892, -2.063335151747126339, 0.6760268296895615148 ) ) ;
#205852=CARTESIAN_POINT ( 'NONE',  ( 5.179192671508887180, 1.240781939916297372, 1.360553736468192554 ) ) ;
#205854=CARTESIAN_POINT ( 'NONE',  ( 6.620655732516643965, 2.083750514537034970, 2.135603474206409835 ) ) ;
#205855=CARTESIAN_POINT ( 'NONE',  ( 6.603104432341277530, -0.4828188497946246382, 2.145653685147373313 ) ) ;
#205857=CARTESIAN_POINT ( 'NONE',  ( 6.596538519236475828, -0.5955016034951933213, -2.182694285642503562 ) ) ;
#205862=CARTESIAN_POINT ( 'NONE',  ( 0.5043727151736315806, -1.897847990334254886, -0.2338014693106793551 ) ) ;
#205863=CARTESIAN_POINT ( 'NONE',  ( 1.445802646165544880, 1.767618460842989014, 0.09138547110125286310 ) ) ;
#205864=CARTESIAN_POINT ( 'NONE',  ( 6.024093331079843239, -1.997604944964962437, 0.2488386476607491182 ) ) ;
#205866=CARTESIAN_POINT ( 'NONE',  ( 3.251485182540703622, 1.868192404686802810, -0.4227579483004426653 ) ) ;
#205868=CARTESIAN_POINT ( 'NONE',  ( 4.105875410593727182, 0.6658617523271005423, -1.853701319000864656 ) ) ;
#205869=CARTESIAN_POINT ( 'NONE',  ( 0.2641366190093488164, 0.6592694798918593557, -2.015615888626711705 ) ) ;
#205871=CARTESIAN_POINT ( 'NONE',  ( 2.412791964582483129, 1.669947582624079274, 0.8431454209596804805 ) ) ;
#205872=CARTESIAN_POINT ( 'NONE',  ( 5.953657690368134858, 0.4940546211441557700, -1.652608054245385372 ) ) ;
#205874=CARTESIAN_POINT ( 'NONE',  ( 2.842613246588860942, 2.190307313262893185, 0.2694104812042824038 ) ) ;
#205877=CARTESIAN_POINT ( 'NONE',  ( 6.109812101310618360, 0.5708666350849945781, -1.876949146916474298 ) ) ;
#205885=CARTESIAN_POINT ( 'NONE',  ( 2.295452831283749440, -1.850383948470477602, 0.9288054807428181014 ) ) ;
#205890=CARTESIAN_POINT ( 'NONE',  ( 0.1354234094306828728, -0.09670520914860020190, 2.017474364592846570 ) ) ;
#205896=CARTESIAN_POINT ( 'NONE',  ( 5.448592227559037049, 1.351948914259465173, 1.495821383734572851 ) ) ;
#205897=CARTESIAN_POINT ( 'NONE',  ( 4.469893758321111576, -0.8975064867107468425, 1.692437687186749917 ) ) ;
#205898=CARTESIAN_POINT ( 'NONE',  ( 6.539320575229249144, 2.442570667128646900, 2.385998263081292148 ) ) ;
#205899=CARTESIAN_POINT ( 'NONE',  ( 2.261505105119133052, 2.148611799745976381, -0.4309092228176118478 ) ) ;
#205901=CARTESIAN_POINT ( 'NONE',  ( 1.933716311909070784, -1.854087253938462299, 0.4680378644332865989 ) ) ;
#205904=CARTESIAN_POINT ( 'NONE',  ( 0.2105648349144396136, 1.930425396462841725, 0.5826343419270895163 ) ) ;
#205906=CARTESIAN_POINT ( 'NONE',  ( 5.636325218313963603, 0.4264374063192889475, 2.149501299143250055 ) ) ;
#205908=CARTESIAN_POINT ( 'NONE',  ( 3.117853853556023846, -0.8486709934477435491, -1.501428560464845630 ) ) ;
#205910=CARTESIAN_POINT ( 'NONE',  ( 5.906510592826289319, -2.110524776404258507, -0.2060971850248518311 ) ) ;
#205916=CARTESIAN_POINT ( 'NONE',  ( 0.1399997263886038068, 0.2431072571701595186, -2.034387401959360187 ) ) ;
#205920=CARTESIAN_POINT ( 'NONE',  ( 2.648825499136245654, 0.2233988552288330709, 1.797577217741084921 ) ) ;
#205925=CARTESIAN_POINT ( 'NONE',  ( 4.336430608486574911, 1.111010274217393956, -1.430681851146862416 ) ) ;
#205929=CARTESIAN_POINT ( 'NONE',  ( 4.914427440023315441, 0.7117315627661743305, 1.719784830429422984 ) ) ;
#205931=CARTESIAN_POINT ( 'NONE',  ( 3.058105062934213692, -1.138753297271431375, 1.540237303602323804 ) ) ;
#205932=CARTESIAN_POINT ( 'NONE',  ( 0.8678470384533981674, 0.8956018474440343713, 1.590720368640268001 ) ) ;
#205933=PLANE ( 'NONE',  #118394 ) ;
#205941=CARTESIAN_POINT ( 'NONE',  ( 5.647300209178060193, 1.738727086691471024, -0.9248740175569410971 ) ) ;
#205944=CARTESIAN_POINT ( 'NONE',  ( 1.130938551725582109, -1.889365942417848832, 0.8953178049561462126 ) ) ;
#205945=CARTESIAN_POINT ( 'NONE',  ( 6.000991310419570901, 1.574649422783209740, -1.109465276731670613 ) ) ;
#205947=CARTESIAN_POINT ( 'NONE',  ( 2.115964440355810439, -0.8579360106165806465, -1.611413330227830176 ) ) ;
#205948=CARTESIAN_POINT ( 'NONE',  ( 2.930518499080053907, 1.225513248159842083, -1.835134156090315605 ) ) ;
#205950=CARTESIAN_POINT ( 'NONE',  ( 1.019614524654769872, -0.4619345408787678964, 1.855657206939323789 ) ) ;
#205951=CARTESIAN_POINT ( 'NONE',  ( 2.066797411385603578, 1.461431172244957333, -1.320572070109968799 ) ) ;
#205952=CARTESIAN_POINT ( 'NONE',  ( 2.472129730261590552, -1.859182766463037151, -0.5613441811427360983 ) ) ;
#205956=CARTESIAN_POINT ( 'NONE',  ( 6.350447304104193336, -1.851927549110881976, -0.1832485138882292142 ) ) ;
#205961=CARTESIAN_POINT ( 'NONE',  ( 2.173600921376659834, 1.351110561487681716, 1.725424542402646422 ) ) ;
#205965=CARTESIAN_POINT ( 'NONE',  ( 2.789462663364688844, 1.291185895303394116, 1.290987730777813702 ) ) ;
#205971=CARTESIAN_POINT ( 'NONE',  ( 2.438006290551326671, 0.9082397578730906362, -1.698968261161729831 ) ) ;
#205972=CARTESIAN_POINT ( 'NONE',  ( 6.244970037249994554, -0.2844439363869250559, -1.940879991452467479 ) ) ;
#205979=CARTESIAN_POINT ( 'NONE',  ( 5.436411051413860385, -1.154718516627372127, 1.718110687276501958 ) ) ;
#205980=CARTESIAN_POINT ( 'NONE',  ( 0.8547319020580852467, 0.3593373433725781108, -1.805665335529122784 ) ) ;
#205982=CARTESIAN_POINT ( 'NONE',  ( 5.449893634413335519, -2.076765696135183248, -0.9856196477224605790 ) ) ;
#205986=CARTESIAN_POINT ( 'NONE',  ( 6.620655732516684822, -0.005281389526603020787, 2.273887028200880511 ) ) ;
#205989=CARTESIAN_POINT ( 'NONE',  ( 4.540924088961058480, -1.502189473471927439, -1.230693300551897185 ) ) ;
#205990=EDGE_LOOP ( 'NONE', ( #95947, #161044 ) ) ;
#205993=CARTESIAN_POINT ( 'NONE',  ( 6.293217207623316156, -0.1008467329366956045, -1.909883259500498198 ) ) ;
#205994=CARTESIAN_POINT ( 'NONE',  ( 0.8731895615166852531, 1.663438651979048277, -0.4559567554138827528 ) ) ;
#205995=CARTESIAN_POINT ( 'NONE',  ( 5.436732529336289588, -1.586671906620169104, 1.244382051841623538 ) ) ;
#205999=CARTESIAN_POINT ( 'NONE',  ( 2.291069257668688408, 1.616616537889125516, 1.325633359429157831 ) ) ;
#206000=CARTESIAN_POINT ( 'NONE',  ( 1.357869778638900904, 0.7128107867309957379, 1.620144791207811297 ) ) ;
#206003=CARTESIAN_POINT ( 'NONE',  ( 4.576316751016760165, -2.222806176453680393, -0.5595744876762742681 ) ) ;
#206004=CARTESIAN_POINT ( 'NONE',  ( 2.308218407481243961, 1.554217257889878301, 0.7831649204469055547 ) ) ;
#206007=CARTESIAN_POINT ( 'NONE',  ( 2.424751807388926039, 0.7370815838836901612, 1.569499502796549262 ) ) ;
#206009=CARTESIAN_POINT ( 'NONE',  ( 1.433807476322545904, 1.104820645310525373, 1.497481488779895731 ) ) ;
#206010=CARTESIAN_POINT ( 'NONE',  ( 2.559224761666531567, 1.745036862030847624, -1.291676481929154408 ) ) ;
#206012=CARTESIAN_POINT ( 'NONE',  ( 3.960172920142067898, -1.157100329752266621, 1.651342637023434090 ) ) ;
#206013=CARTESIAN_POINT ( 'NONE',  ( 2.375000000000001776, 2.052068128417950277, -1.362642298365709419E-13 ) ) ;
#206015=CARTESIAN_POINT ( 'NONE',  ( 1.202032481184050816, -1.926566264184792709, -0.002868833312720530347 ) ) ;
#206017=CARTESIAN_POINT ( 'NONE',  ( 4.764059104694277735, 0.6956466834483631123, -2.109775416031458128 ) ) ;
#206023=CARTESIAN_POINT ( 'NONE',  ( 6.152596803620836496, 2.197069216644991663, 0.3270334163130541594 ) ) ;
#206024=CARTESIAN_POINT ( 'NONE',  ( 4.404711838702720428, 0.5211615849865286476, 1.891323523724611766 ) ) ;
#206028=CARTESIAN_POINT ( 'NONE',  ( 5.536487020692383076, 2.227601090660180638, 0.3946122451431322009 ) ) ;
#206031=CARTESIAN_POINT ( 'NONE',  ( 3.490735631032083841, 2.011810643276640054, 0.4545708190045735786 ) ) ;
#206037=CARTESIAN_POINT ( 'NONE',  ( 4.569519670753737550, 1.814867081516871261, -0.4525428206468632975 ) ) ;
#206038=CARTESIAN_POINT ( 'NONE',  ( 3.568775204899740316, -0.8506723435033979319, 1.511049830170706931 ) ) ;
#206039=CARTESIAN_POINT ( 'NONE',  ( 2.436699184107835592, -1.290689972581187339, -1.167790367532922646 ) ) ;
#206040=CARTESIAN_POINT ( 'NONE',  ( 0.8906306365582180584, -0.5635816346751547634, -2.221901885516941899 ) ) ;
#206041=CARTESIAN_POINT ( 'NONE',  ( 0.8860939741733677710, 1.483344945610004295, 1.634051305214024641 ) ) ;
#206042=CARTESIAN_POINT ( 'NONE',  ( 4.265234282975380431, 2.027484720304991495, -0.5098422324811486828 ) ) ;
#206043=CARTESIAN_POINT ( 'NONE',  ( 5.156170417566459108, -1.405356202774979524, 1.340433341176451520 ) ) ;
#206046=CARTESIAN_POINT ( 'NONE',  ( 0.2642963535325442703, 1.880433764241522088, -0.7283817610406128074 ) ) ;
#206047=CARTESIAN_POINT ( 'NONE',  ( -0.1577409392781377873, -1.310076727147227560, -1.668215054097483385 ) ) ;
#206052=CARTESIAN_POINT ( 'NONE',  ( 4.055160972438559774, -1.518969423100406946, -1.012540670841777013 ) ) ;
#206053=CARTESIAN_POINT ( 'NONE',  ( 2.257103711190447282, -1.706036888594957723, 1.399758388914617013 ) ) ;
#206059=CARTESIAN_POINT ( 'NONE',  ( 1.687766420876281037, 1.931502627210328837, -0.5905180581586618738 ) ) ;
#206061=CARTESIAN_POINT ( 'NONE',  ( 2.852234624111050110, -1.855622028292166714, -0.1419291048156411938 ) ) ;
#206067=CARTESIAN_POINT ( 'NONE',  ( 5.619710272201024814, -1.780234218580947436, 0.4041525643716862848 ) ) ;
#206072=CARTESIAN_POINT ( 'NONE',  ( 0.3855818064394588851, -0.09363725165581829324, 1.731465614217362559 ) ) ;
#206073=CARTESIAN_POINT ( 'NONE',  ( 6.615202361034350886, -1.784545987531281019, 0.4526050685512914007 ) ) ;
#206074=CARTESIAN_POINT ( 'NONE',  ( 4.899205829341429563, 1.920759858200033587, -1.278847778945918279 ) ) ;
#206076=CARTESIAN_POINT ( 'NONE',  ( 6.766866382711775429, -1.973269837180600561, -0.8828958408187634888 ) ) ;
#206078=CARTESIAN_POINT ( 'NONE',  ( 5.782642724008081103, -2.244312133422786015, 0.4951331349164668216 ) ) ;
#206081=CARTESIAN_POINT ( 'NONE',  ( 5.981297838379462384, 1.727768277425823396, -0.7175292643646775659 ) ) ;
#206083=CARTESIAN_POINT ( 'NONE',  ( 4.025576834063953946, -0.3218090080209669024, 1.884953445776993863 ) ) ;
#206085=CARTESIAN_POINT ( 'NONE',  ( 4.776106669258010307, 1.268914099295117781, 1.805409367619143390 ) ) ;
#206086=CARTESIAN_POINT ( 'NONE',  ( 4.909417703775454278, -2.009542366629351484, 0.6670832617777838758 ) ) ;
#206092=CARTESIAN_POINT ( 'NONE',  ( 2.837322237161111094, 0.2816050128923338058, 2.290267077920715710 ) ) ;
#206093=CARTESIAN_POINT ( 'NONE',  ( 3.982823771651412770, 1.862158852298421152, 0.6176278068941787325 ) ) ;
#206096=CARTESIAN_POINT ( 'NONE',  ( 6.807491137956053429, -1.653082740107037152, -1.233284719700310506 ) ) ;
#206100=CARTESIAN_POINT ( 'NONE',  ( 5.278529876733943915, -0.4946281652532491524, -1.954780475499573900 ) ) ;
#206104=CARTESIAN_POINT ( 'NONE',  ( 1.569424903267138571, 1.913428125876670549, 1.025899993198212901 ) ) ;
#206111=CARTESIAN_POINT ( 'NONE',  ( 1.405620310220422109, -0.5036079032930698141, 1.998149085168912986 ) ) ;
#206112=CARTESIAN_POINT ( 'NONE',  ( -0.02224634325202062834, 1.297472808610355521, -2.537530276547406149 ) ) ;
#206118=CARTESIAN_POINT ( 'NONE',  ( 3.686107007616833631, 1.064666855108999721, 1.588282736317746302 ) ) ;
#206120=CARTESIAN_POINT ( 'NONE',  ( 5.119873625132255412, -0.9486883152997215296, -1.493885749217472636 ) ) ;
#206124=CARTESIAN_POINT ( 'NONE',  ( 0.2685667436414033160, -0.2372314691254543417, -1.900927335933370488 ) ) ;
#206126=CARTESIAN_POINT ( 'NONE',  ( 0.4146172280090759665, 0.7909515328246279342, 1.913518691844050323 ) ) ;
#206128=CARTESIAN_POINT ( 'NONE',  ( 6.350466393003619814, 0.5888352225367661230, 1.775644890098279749 ) ) ;
#206129=CARTESIAN_POINT ( 'NONE',  ( 2.683998146737070378, -0.9385614705539682134, 1.565816405032012470 ) ) ;
#206130=CARTESIAN_POINT ( 'NONE',  ( 5.953802724510455668, 0.6443607167232848765, -2.110727517106169682 ) ) ;
#206133=CARTESIAN_POINT ( 'NONE',  ( 2.928243574330684496, 1.101304876339922467, 1.743887257993762763 ) ) ;
#206137=CARTESIAN_POINT ( 'NONE',  ( 0.7026770610618976454, -0.7276074859871292100, -2.035605373553108777 ) ) ;
#206138=CARTESIAN_POINT ( 'NONE',  ( 5.283670394142272464, -1.967056725255760474, 0.6460906113585006549 ) ) ;
#206140=CARTESIAN_POINT ( 'NONE',  ( 3.673254355229157664, 0.05708692194854488033, -2.161017345153878999 ) ) ;
#206142=CARTESIAN_POINT ( 'NONE',  ( 4.459631813825579272, -1.562525726068206833, -1.279702784981617825 ) ) ;
#206143=CARTESIAN_POINT ( 'NONE',  ( 2.295295855072278624, -1.753792786583353580, 0.8793850528211948347 ) ) ;
#206145=PRODUCT_DEFINITION_SHAPE ( 'NONE', 'NONE',  #141784 ) ;
#206151=CARTESIAN_POINT ( 'NONE',  ( 1.921111612355221654, -1.799121770747251547, 0.9110121207814986244 ) ) ;
#206155=CARTESIAN_POINT ( 'NONE',  ( 5.801015586618943232, -0.2871438832755985882, -1.890612906794430614 ) ) ;
#206159=CARTESIAN_POINT ( 'NONE',  ( 3.128529964930275131, 0.4926631579876327716, 1.955168413974050834 ) ) ;
#206162=CARTESIAN_POINT ( 'NONE',  ( 5.895441327320324554, 1.309037806329484521, 1.123130245766153612 ) ) ;
#206166=CARTESIAN_POINT ( 'NONE',  ( 4.727732462671866642, -1.149354582003499159, -1.475719300151681512 ) ) ;
#206167=CARTESIAN_POINT ( 'NONE',  ( 1.692325190600419305, 1.023896122633965566, -1.799289093316607469 ) ) ;
#206172=CARTESIAN_POINT ( 'NONE',  ( 0.4920785707626255112, -1.005892833030905598, 1.506422592618541278 ) ) ;
#206179=CARTESIAN_POINT ( 'NONE',  ( 5.659766488261158024, 1.145116341927857384, 1.535488998638125047 ) ) ;
#206186=CARTESIAN_POINT ( 'NONE',  ( 2.835029207381420502, 0.2633842809251253358, 2.145520918749081574 ) ) ;
#206190=CARTESIAN_POINT ( 'NONE',  ( 6.176747059734422507, -1.734417727105644680, -0.5698399933231483860 ) ) ;
#206192=CARTESIAN_POINT ( 'NONE',  ( 0.6671782056521896598, 0.1977593025605048904, -1.961437444221861837 ) ) ;
#206193=CARTESIAN_POINT ( 'NONE',  ( 3.586107075002854305, 1.066394011600999780, 1.587261316105821551 ) ) ;
#206196=CARTESIAN_POINT ( 'NONE',  ( 4.984792273111487759, 1.884092017856910273, 0.5737924883163454393 ) ) ;
#206198=CARTESIAN_POINT ( 'NONE',  ( 0.1990292396216531146, -0.5187523925454742280, 1.871322268447791703 ) ) ;
#206204=CARTESIAN_POINT ( 'NONE',  ( 3.510326737904199135, -1.910220267131033323, -0.09114558060911714943 ) ) ;
#206206=CARTESIAN_POINT ( 'NONE',  ( 1.097021799178355739, -0.5375665728563281398, -2.140183485690804410 ) ) ;
#206208=CARTESIAN_POINT ( 'NONE',  ( 6.182294962360654900, 1.036951722903585837, 1.725357817989848996 ) ) ;
#206210=CARTESIAN_POINT ( 'NONE',  ( 6.709597972018079837, -0.3944863986210072060, 1.789098616620278470 ) ) ;
#206212=CARTESIAN_POINT ( 'NONE',  ( 1.697802635435996743, -1.498143435978617655, -1.429203828351800487 ) ) ;
#206224=CARTESIAN_POINT ( 'NONE',  ( 6.825078400183556937, 1.282741234726336943, 1.971047034039685952 ) ) ;
#206226=CARTESIAN_POINT ( 'NONE',  ( 5.326719796100753967, 0.6952390240965979906, -1.588890972402807966 ) ) ;
#206228=CARTESIAN_POINT ( 'NONE',  ( 1.991162705694597301, 0.1987741427678466066, 2.060657922996151914 ) ) ;
#206229=CARTESIAN_POINT ( 'NONE',  ( 3.550509549652399066, -1.420143166946661317, 1.570484981737807706 ) ) ;
#206232=CARTESIAN_POINT ( 'NONE',  ( 1.938274800925225527, -1.057869798513750847, 1.661026717510836637 ) ) ;
#206235=CARTESIAN_POINT ( 'NONE',  ( 0.1055216070770526038, 1.418477292093557329, 1.282857148695019989 ) ) ;
#206236=CARTESIAN_POINT ( 'NONE',  ( 4.119262515598776098, -2.194098707595509623, 0.6636001952689452033 ) ) ;
#206237=CARTESIAN_POINT ( 'NONE',  ( 1.418276456094772708, 1.227529518603141190, -1.351586893430449576 ) ) ;
#206238=CIRCLE ( 'NONE', #168222, 0.1399999999999995137 ) ;
#206243=CARTESIAN_POINT ( 'NONE',  ( 2.426041559740747200, -1.990683941386611311, 0.2996653706425453367 ) ) ;
#206244=CARTESIAN_POINT ( 'NONE',  ( 2.799599750139214471, -1.450362073461785473, -1.321114446766240347 ) ) ;
#206248=CARTESIAN_POINT ( 'NONE',  ( 6.246049398119083662, 0.6547385654485110562, 1.985528007121174943 ) ) ;
#206249=CARTESIAN_POINT ( 'NONE',  ( 4.785902253289605390, -0.8326956132961546020, 1.561725933240491360 ) ) ;
#206251=CARTESIAN_POINT ( 'NONE',  ( 1.306853331985533107, 1.934050699793531836, 1.030479497498619557 ) ) ;
#206252=CARTESIAN_POINT ( 'NONE',  ( 5.718645868333249283, -0.03627580822302550745, 1.740135244698801431 ) ) ;
#206255=CARTESIAN_POINT ( 'NONE',  ( 0.2331713839410966271, 5.723577825403736163, -2.547423061495857954 ) ) ;
#206256=CARTESIAN_POINT ( 'NONE',  ( 6.574781987728091970, -0.9847942639734930115, 2.074158207377621910 ) ) ;
#206258=CARTESIAN_POINT ( 'NONE',  ( 6.028594920762765597, 1.707543762964639722, -0.2996114793598329551 ) ) ;
#206259=CARTESIAN_POINT ( 'NONE',  ( 5.318865801915546143, -1.576246948875639209, 1.493384065191505350 ) ) ;
#206261=CARTESIAN_POINT ( 'NONE',  ( 6.473846665049121540, -0.8576149079453172508, 1.823233050095712349 ) ) ;
#206262=CARTESIAN_POINT ( 'NONE',  ( 3.000000000000002665, -1.776620610948833047E-13, -2.052068128417948945 ) ) ;
#206264=CARTESIAN_POINT ( 'NONE',  ( 3.979452554116496898, 1.814262220864255815, -0.6480193189529972475 ) ) ;
#206266=CARTESIAN_POINT ( 'NONE',  ( 1.454100989278300560, -1.612054358864203785, -1.528463602881096284 ) ) ;
#206272=CARTESIAN_POINT ( 'NONE',  ( 3.071146466883535098, -1.680802468121232573, 1.452339882875167021 ) ) ;
#206279=CARTESIAN_POINT ( 'NONE',  ( 1.037732671793228700, -1.587836052788630603, 1.242728777923551409 ) ) ;
#206281=CARTESIAN_POINT ( 'NONE',  ( 6.602015036461629904, 0.7930265726678319416, -1.904331891608399996 ) ) ;
#206283=CARTESIAN_POINT ( 'NONE',  ( 6.128409194715155550, 0.1798751216713200540, 1.731140798666473968 ) ) ;
#206285=CARTESIAN_POINT ( 'NONE',  ( 1.352431244980515146, -1.399367522912741135, 1.083307108726710100 ) ) ;
#206286=CARTESIAN_POINT ( 'NONE',  ( 6.504571816962987363, -1.679391772619584833, 0.4319377402999846627 ) ) ;
#206287=CARTESIAN_POINT ( 'NONE',  ( 6.304260172732157663, 1.282988983046409848, -1.176258868317042294 ) ) ;
#206288=CARTESIAN_POINT ( 'NONE',  ( 3.861076399890978283, 0.2801353988391065419, -2.275111823818583456 ) ) ;
#206290=CARTESIAN_POINT ( 'NONE',  ( 2.150122221082468865, -1.423577340559305071, 1.167554138749151926 ) ) ;
#206293=CARTESIAN_POINT ( 'NONE',  ( 3.065264358586119009, 0.2694654384877669395, -1.805464241506696155 ) ) ;
#206294=CARTESIAN_POINT ( 'NONE',  ( 4.061172775696818782, -1.158689426361030561, 1.650081270007992318 ) ) ;
#206296=CARTESIAN_POINT ( 'NONE',  ( 3.274574482517400575, -1.349127789868936222, 1.816123189252472958 ) ) ;
#206298=CARTESIAN_POINT ( 'NONE',  ( 5.877981411467888329, 1.251756350581848309, 1.693418440539447234 ) ) ;
#206301=CARTESIAN_POINT ( 'NONE',  ( 2.980987059868035693, 1.948563265827065960, 0.6999735360200682877 ) ) ;
#206304=CARTESIAN_POINT ( 'NONE',  ( 4.477262591527907176, -1.894555094343739476, -0.9525379817736513433 ) ) ;
#206307=CARTESIAN_POINT ( 'NONE',  ( 1.119610834840406577, -1.879747399699664978, 0.4211694731556160365 ) ) ;
#206314=CARTESIAN_POINT ( 'NONE',  ( 0.1588220795745398928, 2.216043539545629937, 0.1551192601621682043 ) ) ;
#206315=CARTESIAN_POINT ( 'NONE',  ( 1.747240475267642257, -1.779442529384717808, 1.126025380906693352 ) ) ;
#206318=CARTESIAN_POINT ( 'NONE',  ( 5.823074758751579871, -1.681767765412798710, -0.7970822532109583802 ) ) ;
#206322=CARTESIAN_POINT ( 'NONE',  ( 0.1586465271753433603, 2.115359532055087310, 0.1496401998123952359 ) ) ;
#206325=CARTESIAN_POINT ( 'NONE',  ( 2.769914238037580745, -1.940913097850523128, 0.2850433363836765155 ) ) ;
#206326=CARTESIAN_POINT ( 'NONE',  ( 2.096749907087645415, -0.5762017740289016032, -2.083436276955972222 ) ) ;
#206330=CARTESIAN_POINT ( 'NONE',  ( 3.345385115808647392, 1.740516467222261499, -0.001323508237265763176 ) ) ;
#206334=CARTESIAN_POINT ( 'NONE',  ( 2.811874868751465417, -1.677748492350576770, 1.117661080827489606 ) ) ;
#206336=CARTESIAN_POINT ( 'NONE',  ( 2.817209029084859928, -0.1949976385870570150, 1.961808326198757335 ) ) ;
#206344=CARTESIAN_POINT ( 'NONE',  ( 2.807290699014941548, 1.731141667658737449, -1.040073625836896554 ) ) ;
#206346=CARTESIAN_POINT ( 'NONE',  ( 5.421043267468262705, 2.129509263528307716, 0.8893739899358196199 ) ) ;
#206349=CARTESIAN_POINT ( 'NONE',  ( 3.379693149055284174, -1.891888713350448947, 0.5187481205842571219 ) ) ;
#206351=CARTESIAN_POINT ( 'NONE',  ( 0.5455463417442986129, -1.458554840210561476, 1.392547631435703037 ) ) ;
#206353=CARTESIAN_POINT ( 'NONE',  ( 2.079462195143897851, 1.640249684897076898, 1.338979269010678985 ) ) ;
#206356=CARTESIAN_POINT ( 'NONE',  ( 2.062219658421380775, -1.683061746929171321, -0.7467898329211535291 ) ) ;
#206360=CARTESIAN_POINT ( 'NONE',  ( 3.357788437482766675, -1.608272433257527556, -1.382313803475518244 ) ) ;
#206361=CARTESIAN_POINT ( 'NONE',  ( 6.615187027077672255, -1.883050660437551205, 0.4742715046822160718 ) ) ;
#206366=CARTESIAN_POINT ( 'NONE',  ( 3.831368270176987334, -1.905513148489059283, 0.7852520889023787420 ) ) ;
#206368=CARTESIAN_POINT ( 'NONE',  ( 0.8898994657863326108, -0.4472179738511591895, -1.785967584704901912 ) ) ;
#206371=CARTESIAN_POINT ( 'NONE',  ( 1.331021600797330118, 2.127646391749141941, 0.5858054460900484761 ) ) ;
#206372=CARTESIAN_POINT ( 'NONE',  ( 3.286655449121218542, -2.228332854187901280, -0.3904065581350114611 ) ) ;
#206374=CARTESIAN_POINT ( 'NONE',  ( 3.744242849288460295, 0.9642487561531964957, -1.533428966541541039 ) ) ;
#206375=CARTESIAN_POINT ( 'NONE',  ( 2.588968054610871317, 1.620874238694985925, 1.020808031020562501 ) ) ;
#206376=CARTESIAN_POINT ( 'NONE',  ( 4.387213907293201487, 0.09840592021137170575, 2.068135374880715638 ) ) ;
#206379=CARTESIAN_POINT ( 'NONE',  ( 3.028153684870387607, 1.096474020163393792, -1.638230769948149534 ) ) ;
#206380=CARTESIAN_POINT ( 'NONE',  ( 0.7625677631861004224, -1.397537113076696036, 1.326088851308028449 ) ) ;
#206381=CARTESIAN_POINT ( 'NONE',  ( 3.520239479114236403, 1.187513476551487424, -1.445374034619356207 ) ) ;
#206382=CARTESIAN_POINT ( 'NONE',  ( 2.649405215588944262, -1.917952202864357414, 1.283049733485057908 ) ) ;
#206383=CARTESIAN_POINT ( 'NONE',  ( 3.789374314311170000, -1.720299746930791684, 0.7104884466354021155 ) ) ;
#206388=CARTESIAN_POINT ( 'NONE',  ( 0.1531350777018150311, -1.689991139269167109, 1.256553844878212978 ) ) ;
#206393=CARTESIAN_POINT ( 'NONE',  ( 2.338272602237463360, -1.224740070204191289, -1.730971256048131401 ) ) ;
#206394=CARTESIAN_POINT ( 'NONE',  ( 0.7033857886646873725, 1.779361102145039286, -0.9557781530431900263 ) ) ;
#206400=CARTESIAN_POINT ( 'NONE',  ( 1.405796033167512116, -0.5266655099175953092, 2.096309153942426562 ) ) ;
#206402=CARTESIAN_POINT ( 'NONE',  ( 6.825078400183548055, 2.461594334264828987, 2.239602747093616841 ) ) ;
#206404=CARTESIAN_POINT ( 'NONE',  ( -0.2104748580754183807, 2.005809028216706924, -2.517884123765606663 ) ) ;
#206405=CARTESIAN_POINT ( 'NONE',  ( 6.157435431667657610, 1.928259211291092123, -0.5899821858514133766 ) ) ;
#206410=CARTESIAN_POINT ( 'NONE',  ( 0.1458946441583548470, -1.751458424797154523, -1.431810583859528974 ) ) ;
#206414=CARTESIAN_POINT ( 'NONE',  ( -0.1353477234830356701, -0.1462924468558861324, -1.883848219957585446 ) ) ;
#206418=CARTESIAN_POINT ( 'NONE',  ( 2.332253321102405685, 1.672780984221501122, 0.4201815020834080427 ) ) ;
#206421=CARTESIAN_POINT ( 'NONE',  ( 1.299667926800106121, -1.769921777095804671, -0.007132476793576813211 ) ) ;
#206422=CARTESIAN_POINT ( 'NONE',  ( 2.016272687986338852, -2.012595170092303043, 0.05167081324058443031 ) ) ;
#206425=CARTESIAN_POINT ( 'NONE',  ( 4.559734661428293201, 0.4870809927834463537, -2.152189095746533720 ) ) ;
#206428=CARTESIAN_POINT ( 'NONE',  ( 4.688201205076114597, 1.221562550966972527, 1.733079268972044895 ) ) ;
#206429=CARTESIAN_POINT ( 'NONE',  ( 3.058220425488000327, -1.198843740453523043, 1.621196181159669347 ) ) ;
#206430=CARTESIAN_POINT ( 'NONE',  ( 2.917991513842286277, -1.809334129394428947, 0.09316547460730231767 ) ) ;
#206434=CARTESIAN_POINT ( 'NONE',  ( 1.692057038649401601, -1.861345348035767344, -0.1864469194169729449 ) ) ;
#206436=CARTESIAN_POINT ( 'NONE',  ( 6.428339884752386268, 1.046657586246093175, -1.495688092090130095 ) ) ;
#206438=CARTESIAN_POINT ( 'NONE',  ( 2.958105166426743704, -1.137214127935105790, 1.541527475959689308 ) ) ;
#206445=CARTESIAN_POINT ( 'NONE',  ( 4.008146050417991546, -0.8085630067716749192, 1.960596031080278356 ) ) ;
#206448=CARTESIAN_POINT ( 'NONE',  ( 3.919176214919489976, -0.1484353776938246439, 1.965847438023991423 ) ) ;
#206449=CARTESIAN_POINT ( 'NONE',  ( 0.1584477454876299096, 2.008078640038186258, 0.1440931537372847071 ) ) ;
#206452=CARTESIAN_POINT ( 'NONE',  ( -0.07047696482224277692, -1.639844204322737697, -1.338861086256079913 ) ) ;
#206454=CARTESIAN_POINT ( 'NONE',  ( 1.856005582152659317, -0.6995316168164237292, 1.948720873434762080 ) ) ;
#206459=CARTESIAN_POINT ( 'NONE',  ( 3.996100316046395484, -0.6559638842641742906, -1.985124821949519891 ) ) ;
#206462=CARTESIAN_POINT ( 'NONE',  ( 1.694096453153286497, -1.816434584207878622, -0.1825648128309723117 ) ) ;
#206463=CARTESIAN_POINT ( 'NONE',  ( 0.5393639851597960000, -1.720521155456521400, 0.5669088471357224268 ) ) ;
#206465=CARTESIAN_POINT ( 'NONE',  ( 5.971336403843029217, 0.1662174427981797931, -2.200672837095698497 ) ) ;
#206467=CARTESIAN_POINT ( 'NONE',  ( 4.471826267013489620, 2.141383520707430321, -0.5327586567505787629 ) ) ;
#206470=CARTESIAN_POINT ( 'NONE',  ( 3.141163725242692273, 0.04933110545866059571, 1.911816780882446221 ) ) ;
#206472=CARTESIAN_POINT ( 'NONE',  ( 5.424307079040113777, 1.017280057988108499, 1.803113764695261301 ) ) ;
#206473=DIRECTION ( 'NONE',  ( -0.9999980456341538426, 0.000000000000000000, -0.001977050295949311660 ) ) ;
#206475=CARTESIAN_POINT ( 'NONE',  ( 6.181208317857348256, 1.509947553572440704, 1.588605474358975478 ) ) ;
#206485=CARTESIAN_POINT ( 'NONE',  ( 6.121949425127414024, 2.040613181561203859, -0.3481179853092666865 ) ) ;
#206486=CARTESIAN_POINT ( 'NONE',  ( 4.143132006054106142, -1.675477906314150056, 0.9507637539484592448 ) ) ;
#206487=CARTESIAN_POINT ( 'NONE',  ( 0.05236148938883232462, -1.314980595004966002, 1.528755779884483523 ) ) ;
#206491=CARTESIAN_POINT ( 'NONE',  ( 0.3752731597879420677, 2.043270790221253908, -0.7926104125151807178 ) ) ;
#206492=CARTESIAN_POINT ( 'NONE',  ( 5.584540971669589737, -1.782103179330214449, -0.3958202769075992444 ) ) ;
#206498=CARTESIAN_POINT ( 'NONE',  ( 2.208333698829296310, 1.645431377724184463, 0.8263914577605266931 ) ) ;
#206499=CARTESIAN_POINT ( 'NONE',  ( 6.082294971626270197, 1.038730605371197324, 1.724430661308763213 ) ) ;
#206500=CARTESIAN_POINT ( 'NONE',  ( 0.8260327929942178349, -1.663255926670023976, 1.586464751714482979 ) ) ;
#206501=CARTESIAN_POINT ( 'NONE',  ( 6.332860960579021814, -1.861707940517230764, -0.6185968553879470644 ) ) ;
#206505=CARTESIAN_POINT ( 'NONE',  ( 0.7661813929631040576, -2.060537521029872643, 0.2012509062776293156 ) ) ;
#206507=CARTESIAN_POINT ( 'NONE',  ( 2.349268366499413840, 0.5549471352096692067, -2.015694315139557435 ) ) ;
#206508=CARTESIAN_POINT ( 'NONE',  ( 0.9185735243398345240, 1.726912363944958617, 0.7195956246372691156 ) ) ;
#206509=CARTESIAN_POINT ( 'NONE',  ( 2.372422516638694745, -0.4444355326964634090, 1.966343308868031103 ) ) ;
#206513=CARTESIAN_POINT ( 'NONE',  ( 2.489492129562159484, -1.735903792773977772, -0.1261859363600649764 ) ) ;
#206517=CARTESIAN_POINT ( 'NONE',  ( 3.246439759211931175, 0.4201230555563889579, 1.672790298054289693 ) ) ;
#206518=CARTESIAN_POINT ( 'NONE',  ( 2.929422067023911502, -1.473737196803912797, -1.622193633833472814 ) ) ;
#206519=CARTESIAN_POINT ( 'NONE',  ( 5.338574060078519423, 2.173733305800494175, 0.3801736985692484305 ) ) ;
#206522=CARTESIAN_POINT ( 'NONE',  ( 1.956167536658510953, -0.7342896127641992399, 2.043222018709658805 ) ) ;
#206523=CARTESIAN_POINT ( 'NONE',  ( 1.453431991042982041, 0.5316948868413253759, -1.746555546766684675 ) ) ;
#206524=CARTESIAN_POINT ( 'NONE',  ( 3.397769718358482738, -2.085282637925215177, 0.3663039253445389276 ) ) ;
#206525=FACE_OUTER_BOUND ( 'NONE', #190720, .T. ) ;
#206527=CARTESIAN_POINT ( 'NONE',  ( 3.105313311461850745, -0.4450742334846323756, 2.248595817482400783 ) ) ;
#206533=CARTESIAN_POINT ( 'NONE',  ( 6.639320575229294086, -0.003630812595115453199, 2.203388474976493594 ) ) ;
#206539=CARTESIAN_POINT ( 'NONE',  ( 4.676407821165474488, 1.496050514612049742, 1.352155788975975437 ) ) ;
#206541=CARTESIAN_POINT ( 'NONE',  ( 3.327062588944328603, -1.903923626093235955, -0.7937240881994469532 ) ) ;
#206546=CARTESIAN_POINT ( 'NONE',  ( 6.351546390744762682, 2.185874319550953793, -0.1572705277706408500 ) ) ;
#206547=CARTESIAN_POINT ( 'NONE',  ( 3.885388821667290493, -0.6351983117205138862, -1.913803978180687482 ) ) ;
#206548=CARTESIAN_POINT ( 'NONE',  ( 3.157574601152390414, 0.8305207305269333151, 1.643389852989694200 ) ) ;
#206553=CARTESIAN_POINT ( 'NONE',  ( 6.493173258741942178, 1.586635928914212013, -0.9027890188317910791 ) ) ;
#206554=CARTESIAN_POINT ( 'NONE',  ( 0.03630054827139220924, -1.841026678340401679, 1.376304820193236189 ) ) ;
#206556=CARTESIAN_POINT ( 'NONE',  ( 6.684454173705361768, -2.217265373380904681, -0.4495064082850850906 ) ) ;
#206557=CARTESIAN_POINT ( 'NONE',  ( 1.647240615436126543, -1.778467030350115774, 1.127781350514756475 ) ) ;
#206567=CARTESIAN_POINT ( 'NONE',  ( 2.303126745213024851, -0.3670769733005623814, -2.088442229865586697 ) ) ;
#206568=CARTESIAN_POINT ( 'NONE',  ( 3.850012423022421082, -1.533692773617735705, -1.607201352943017802 ) ) ;
#206569=CARTESIAN_POINT ( 'NONE',  ( 0.8147124124333324779, 2.026155960571228043, 0.8354305900151804964 ) ) ;
#206570=CARTESIAN_POINT ( 'NONE',  ( 0.8212658843103730621, 2.040464674744349338, 0.8412164853940640175 ) ) ;
#206572=CARTESIAN_POINT ( 'NONE',  ( 4.334394203492665909, -1.131343785558375226, 1.602600411086833931 ) ) ;
#206575=CARTESIAN_POINT ( 'NONE',  ( 6.610000000000006537, 0.6121396118998356783, 1.775466344933520846 ) ) ;
#206578=CARTESIAN_POINT ( 'NONE',  ( 2.918346969001627045, -2.117983955170518851, 0.1081942149789016649 ) ) ;
#206580=CARTESIAN_POINT ( 'NONE',  ( 6.051685545382852638, 0.6321331830463626789, -2.067208725892249799 ) ) ;
#206581=CARTESIAN_POINT ( 'NONE',  ( 4.335397732480402055, 0.7831895168094182846, -1.666506522714307437 ) ) ;
#206585=CARTESIAN_POINT ( 'NONE',  ( -0.02444708455723310775, -1.687298116421297456, -0.4264520246781302593 ) ) ;
#206586=CARTESIAN_POINT ( 'NONE',  ( 6.727182134110164746, 4.698490487241143043, 2.473633340027088678 ) ) ;
#206589=CARTESIAN_POINT ( 'NONE',  ( 4.663041391408608405, -1.929494027986548454, -0.9748474430888448561 ) ) ;
#206591=CARTESIAN_POINT ( 'NONE',  ( 5.800157620552712778, -1.823839058171864203, 0.8595007112896931867 ) ) ;
#206593=CARTESIAN_POINT ( 'NONE',  ( 3.713887418366210280, -2.130098009959373151, 0.3673708613747132534 ) ) ;
#206594=CARTESIAN_POINT ( 'NONE',  ( 3.919176214919489976, -0.1484353776938246439, 1.965847438023991423 ) ) ;
#206596=CARTESIAN_POINT ( 'NONE',  ( 1.097181765414790400, -0.5634973350938665693, -2.237626367659339088 ) ) ;
#206598=CARTESIAN_POINT ( 'NONE',  ( 3.391920509712963661, -0.8384013316644415292, 1.882726026762149285 ) ) ;
#206599=CARTESIAN_POINT ( 'NONE',  ( 5.302268720778519295, 1.468090865803386880, -1.271420572733022780 ) ) ;
#206603=CARTESIAN_POINT ( 'NONE',  ( 6.609999999999996767, 0.01081285896096208579, 1.720159828161059723 ) ) ;
#206607=CARTESIAN_POINT ( 'NONE',  ( 2.011028756337205348, 1.635159560789069655, -1.482119803565529859 ) ) ;
#206609=CARTESIAN_POINT ( 'NONE',  ( 6.842638302680406071, -1.923265442670134329, -0.3857968560932593660 ) ) ;
#206610=CARTESIAN_POINT ( 'NONE',  ( 6.539320575229278454, 3.689604457162498630, 2.617406275049142916 ) ) ;
#206616=CARTESIAN_POINT ( 'NONE',  ( 5.226429366918344144, 0.1390423275269437320, 1.835946739075666745 ) ) ;
#206618=CARTESIAN_POINT ( 'NONE',  ( 1.920846698078120474, 1.922532266116746325, 0.7428477115608185244 ) ) ;
#206624=CARTESIAN_POINT ( 'NONE',  ( 0.4794588345870378632, 1.923154262159839201, -0.7412630403166396986 ) ) ;
#206626=CARTESIAN_POINT ( 'NONE',  ( 5.091278345985558396, -0.6575378499774006125, 1.720029930423284448 ) ) ;
#206631=CARTESIAN_POINT ( 'NONE',  ( 4.758537496233657293, 0.8426522330295079799, 2.039869969286691731 ) ) ;
#206632=CARTESIAN_POINT ( 'NONE',  ( 0.8081717762262634608, -2.151237856378166224, 0.2110218573620133986 ) ) ;
#206634=CARTESIAN_POINT ( 'NONE',  ( -0.2108831679770960255, -0.001785917861228669690, -1.896958272444612792 ) ) ;
#206635=CARTESIAN_POINT ( 'NONE',  ( -0.03006412033006514162, -0.9462945741195265548, 1.780671068589256834 ) ) ;
#206638=CARTESIAN_POINT ( 'NONE',  ( 6.094389051209717856, -1.018956457145767214, 1.618003106988876283 ) ) ;
#206640=CARTESIAN_POINT ( 'NONE',  ( 0.8658264364783776479, 0.9185255527898968930, 1.629538061279064642 ) ) ;
#206642=CARTESIAN_POINT ( 'NONE',  ( 1.973842561262352469, -0.8578407463649927456, 1.825077436249371354 ) ) ;
#206644=CARTESIAN_POINT ( 'NONE',  ( 4.494815117402239935, -0.4609086856197233684, -2.054844913126519401 ) ) ;
#206649=CARTESIAN_POINT ( 'NONE',  ( 3.797132494115144308, -0.2020087959641834463, -2.009684039814496170 ) ) ;
#206653=CARTESIAN_POINT ( 'NONE',  ( 4.481803774187195444, 1.408218611193782221, 1.640057829624480101 ) ) ;
#206658=CARTESIAN_POINT ( 'NONE',  ( 1.487047289068929246, 2.092300142875534341, 0.5796043027312002272 ) ) ;
#206661=CARTESIAN_POINT ( 'NONE',  ( 0.6086344939593493208, -0.2706599535906920040, 1.821105742621460744 ) ) ;
#206664=CARTESIAN_POINT ( 'NONE',  ( 3.386445149735781257, -0.4294187885149694517, -2.148908265708626697 ) ) ;
#206666=CARTESIAN_POINT ( 'NONE',  ( 3.379979430277161079, 1.433683275776801214, 1.750306659111708463 ) ) ;
#206668=CARTESIAN_POINT ( 'NONE',  ( 4.628138809701114020, 2.011451458044950069, 0.1435230606586651581 ) ) ;
#206673=CARTESIAN_POINT ( 'NONE',  ( 3.901397652722672582, -0.5159380698404272270, 1.692823668428977912 ) ) ;
#206676=CARTESIAN_POINT ( 'NONE',  ( 1.219907122830860446, -2.054670964268051847, 0.4612076382107341277 ) ) ;
#206679=CARTESIAN_POINT ( 'NONE',  ( 1.293335457286367784, -1.782033794834203766, 0.8390149815750718165 ) ) ;
#206686=CARTESIAN_POINT ( 'NONE',  ( 4.610133579271312954, -0.8000244862099057386, -1.691074300901610261 ) ) ;
#206689=CARTESIAN_POINT ( 'NONE',  ( 4.241125740018336643, -0.1978421677554068614, -2.060750949040678570 ) ) ;
#206701=CARTESIAN_POINT ( 'NONE',  ( 4.439869198996494681, 1.279870211898268550, 1.486999339763886097 ) ) ;
#206702=CARTESIAN_POINT ( 'NONE',  ( 1.616564310028177243, 0.5879328921069119085, -1.928455639302439462 ) ) ;
#206705=CARTESIAN_POINT ( 'NONE',  ( 6.639320575229252341, 0.005161017367553630275, 1.896863882003448021 ) ) ;
#206706=CARTESIAN_POINT ( 'NONE',  ( 0.4911964603225346115, 1.381658100223854380, 1.261112594198803061 ) ) ;
#206708=CARTESIAN_POINT ( 'NONE',  ( 2.566654749391559687, 0.6821283815301434350, 1.894225559998161668 ) ) ;
#206710=CARTESIAN_POINT ( 'NONE',  ( 3.409862312649377003, -1.263030510572001885, -1.699084664797428479 ) ) ;
#206711=CARTESIAN_POINT ( 'NONE',  ( 4.914543119725925280, 0.7892175071393169317, 1.914236960262293508 ) ) ;
#206713=CARTESIAN_POINT ( 'NONE',  ( 6.597611690090901426, -2.090214587215084130, 0.04977907537380765746 ) ) ;
#206715=CARTESIAN_POINT ( 'NONE',  ( 5.631824825758743991, -1.159798792365024145, -1.409841961918213427 ) ) ;
#206723=CARTESIAN_POINT ( 'NONE',  ( 5.725241913846256914, 1.688569718951500986, 0.8975008795490189151 ) ) ;
#206732=CARTESIAN_POINT ( 'NONE',  ( 5.237907724141787291, 2.013986247903374327, -0.1017665992488273330 ) ) ;
#206738=CARTESIAN_POINT ( 'NONE',  ( 2.061320199224637051, 1.634538341387161475, 1.098309876814192565 ) ) ;
#206739=CARTESIAN_POINT ( 'NONE',  ( 3.269157808572686896, 1.821735364950356484, -0.8647411805496332260 ) ) ;
#206741=CARTESIAN_POINT ( 'NONE',  ( 6.827182134110239886, 1.995248472151121444, 2.590158597942037844 ) ) ;
#206742=CARTESIAN_POINT ( 'NONE',  ( 3.785266741157941262, 1.586943040539133154, 1.511552532079393885 ) ) ;
#206744=CARTESIAN_POINT ( 'NONE',  ( 2.256748493264736588, -1.490592131378381646, 1.220310119380305203 ) ) ;
#206747=CARTESIAN_POINT ( 'NONE',  ( 0.2329586101569866563, 0.008238550247445517935, -1.845944905557160398 ) ) ;
#206753=CARTESIAN_POINT ( 'NONE',  ( 6.339398910184078417, 0.6979989802004606947, -1.704029730133400866 ) ) ;
#206754=CARTESIAN_POINT ( 'NONE',  ( 3.299479658734363330, 1.818928663852859451, -0.8628815382619985375 ) ) ;
#206755=CARTESIAN_POINT ( 'NONE',  ( 4.534687899768989006, 2.230887184458398398, -0.5525863250545393068 ) ) ;
#206756=CARTESIAN_POINT ( 'NONE',  ( -0.1288028175206621384, 0.6694653996850441491, -2.353626493485785343 ) ) ;
#206757=CARTESIAN_POINT ( 'NONE',  ( 3.168646232094144199, 1.351176984073151788, -1.279899388936973192 ) ) ;
#206759=CARTESIAN_POINT ( 'NONE',  ( -0.1290005225502675879, 5.719648796287211567, -2.768066027128403217 ) ) ;
#206762=CARTESIAN_POINT ( 'NONE',  ( 5.724191925653110857, 2.015179739716387974, 0.5568145835738461669 ) ) ;
#206767=CARTESIAN_POINT ( 'NONE',  ( 6.692093555742618882, -0.7303567666399125580, 1.561414089659449944 ) ) ;
#206769=CARTESIAN_POINT ( 'NONE',  ( 1.529482971743981734, -1.465093928883187901, 0.9274137557628134854 ) ) ;
#206773=CARTESIAN_POINT ( 'NONE',  ( 6.121977192509519661, 2.140326789316211453, -0.3632143409003502077 ) ) ;
#206774=CARTESIAN_POINT ( 'NONE',  ( 4.969292227364340953, 0.1756445257206709631, -1.817221496977147854 ) ) ;
#206775=CARTESIAN_POINT ( 'NONE',  ( 1.674581101246939374, 1.321464807213859505, -1.450045219730737633 ) ) ;
#206780=CARTESIAN_POINT ( 'NONE',  ( 3.914780425095893968, -0.6665358524936614293, -2.013057630646164942 ) ) ;
#206786=CARTESIAN_POINT ( 'NONE',  ( 2.289971195246335078, -1.349064171463711936, -1.570471239911851669 ) ) ;
#206789=CARTESIAN_POINT ( 'NONE',  ( 3.739129200393681796, 2.109584919444119855, 0.6958237802787976545 ) ) ;
#206791=CARTESIAN_POINT ( 'NONE',  ( 2.040019973291283151, -1.774186676285171460, 1.461575674325124252 ) ) ;
#206793=CARTESIAN_POINT ( 'NONE',  ( 6.157095870780715074, 1.689533437190817722, -1.182850423791491856 ) ) ;
#206796=CARTESIAN_POINT ( 'NONE',  ( 6.374545129912787544, -0.09763137639631430664, -1.838803627010993313 ) ) ;
#206798=CARTESIAN_POINT ( 'NONE',  ( -0.2104748580754426390, 2.865278511227668634, -2.591885361450113834 ) ) ;
#206799=CARTESIAN_POINT ( 'NONE',  ( 3.399128784836574990, 1.359029604673635871, 1.061868196530877384 ) ) ;
#206800=CARTESIAN_POINT ( 'NONE',  ( 1.921111612355221654, -1.799121770747251547, 0.9110121207814986244 ) ) ;
#206801=CARTESIAN_POINT ( 'NONE',  ( 3.006738235175490548, -2.214768494356106121, 0.6152039052057678425 ) ) ;
#206802=CARTESIAN_POINT ( 'NONE',  ( 3.269090859574837804, -2.088958473869072741, -0.8692115097446629912 ) ) ;
#206803=CARTESIAN_POINT ( 'NONE',  ( 5.356126594405285601, 2.103725632816171309, -0.1020696835895683885 ) ) ;
#206805=CARTESIAN_POINT ( 'NONE',  ( 3.778344457583324711, -1.704853921413415296, -0.4744283172272641957 ) ) ;
#206807=CARTESIAN_POINT ( 'NONE',  ( 6.339416484298314280, 0.8816828672218860463, -2.116228320707528976 ) ) ;
#206808=CARTESIAN_POINT ( 'NONE',  ( 5.490138966579363178, -0.4511402564183407127, -1.784887083484905768 ) ) ;
#206811=CARTESIAN_POINT ( 'NONE',  ( 5.332042502257137606, 2.158596015244533373, 0.3771327725019049670 ) ) ;
#206814=CARTESIAN_POINT ( 'NONE',  ( 6.408651866624735405, 0.6456447432892989946, 1.967203394946090977 ) ) ;
#206815=CARTESIAN_POINT ( 'NONE',  ( 0.1457207355009884908, 1.993892511249679034, -0.3006540981884687214 ) ) ;
#206818=CARTESIAN_POINT ( 'NONE',  ( 3.949766350991973596, 0.6478974803514454539, -1.814415559773856490 ) ) ;
#206821=CARTESIAN_POINT ( 'NONE',  ( 6.469000917296717112, -1.638331675554663747, 1.346054232038436105 ) ) ;
#206832=CARTESIAN_POINT ( 'NONE',  ( 1.346068015636435522, -0.8851805579040676886, 1.750911360861057142 ) ) ;
#206835=CARTESIAN_POINT ( 'NONE',  ( 5.178158156489047315, -1.047961880893449882, -1.658324637040713867 ) ) ;
#206838=CARTESIAN_POINT ( 'NONE',  ( 6.825078400183575589, -0.005632053428735600553, 2.144262460745151255 ) ) ;
#206843=CARTESIAN_POINT ( 'NONE',  ( 0.6670070365902281972, 0.1896921041569209765, -1.860926112923621201 ) ) ;
#206844=CARTESIAN_POINT ( 'NONE',  ( 5.800041802258188106, -1.566351721726914725, 0.7437187281235900782 ) ) ;
#206846=CARTESIAN_POINT ( 'NONE',  ( 3.579775959861815515, -1.078688530630707243, 1.907616655872627964 ) ) ;
#206847=CARTESIAN_POINT ( 'NONE',  ( 4.366487424706978260, 1.084006333436113634, 2.037121594781437839 ) ) ;
#206848=CARTESIAN_POINT ( 'NONE',  ( 0.4970371946629085769, 1.713755840317375601, -1.144362063176207922 ) ) ;
#206849=CARTESIAN_POINT ( 'NONE',  ( 2.079929315299507753, -1.904492180933140322, -0.3787631973139488073 ) ) ;
#206852=CARTESIAN_POINT ( 'NONE',  ( 5.431924468521282634, -2.068440459917933794, 0.4666711972392265650 ) ) ;
#206854=CARTESIAN_POINT ( 'NONE',  ( 3.375625116643202972, -0.3961014713874110305, -1.976955985980306307 ) ) ;
#206858=CARTESIAN_POINT ( 'NONE',  ( 1.224926655537651676, -0.04696546880481740349, 1.825250005322680780 ) ) ;
#206862=ORIENTED_EDGE ( 'NONE', *, *, #92877, .T. ) ;
#206863=CARTESIAN_POINT ( 'NONE',  ( 5.700091634879108859, -2.061077814751426818, -0.002399610236311285148 ) ) ;
#206869=CARTESIAN_POINT ( 'NONE',  ( 4.371743357251212103, 0.4404049503993580639, -1.970906944672585315 ) ) ;
#206870=CARTESIAN_POINT ( 'NONE',  ( 5.725276803944279180, 1.957897222332797504, 1.049153726691682831 ) ) ;
#206875=CARTESIAN_POINT ( 'NONE',  ( 3.661055773700711224, -1.816817347422092555, -0.9728634070030485193 ) ) ;
#206876=CARTESIAN_POINT ( 'NONE',  ( 3.498672800139957406, -1.986100699840901651, 0.3474671148789992836 ) ) ;
#206882=CARTESIAN_POINT ( 'NONE',  ( 3.866564406427867251, -0.5879305547937460075, 1.928456347981069019 ) ) ;
#206883=CARTESIAN_POINT ( 'NONE',  ( 2.238008233095424515, 0.4029187984595939409, 1.796341404040911804 ) ) ;
#206884=CARTESIAN_POINT ( 'NONE',  ( 1.032322977361863847, -1.467698275133515695, -1.780829215104979157 ) ) ;
#206886=CARTESIAN_POINT ( 'NONE',  ( 3.532649767544591590, 2.108058052951222283, 0.4773693597190583060 ) ) ;
#206889=CARTESIAN_POINT ( 'NONE',  ( 3.392261881094984055, 0.05328783134446976599, 2.297904267588930960 ) ) ;
#206892=CARTESIAN_POINT ( 'NONE',  ( 2.781945002432617997, -0.9632652739061451364, 1.603442845774772474 ) ) ;
#206893=CARTESIAN_POINT ( 'NONE',  ( 5.594591524781380443, -0.4782570758292312707, -1.912467619381743811 ) ) ;
#206897=CARTESIAN_POINT ( 'NONE',  ( 0.2060869173217265982, -0.5842117877600698783, 2.128085570573131413 ) ) ;
#206902=CARTESIAN_POINT ( 'NONE',  ( 6.438353018038387887, 1.949953777973761015, 0.2897296601065552091 ) ) ;
#206903=CARTESIAN_POINT ( 'NONE',  ( 5.408889320884306073, 1.750735854880939746, -1.503546334452151134 ) ) ;
#206904=CARTESIAN_POINT ( 'NONE',  ( 5.617585446245374037, 0.3627780356338809464, -1.825160902907280613 ) ) ;
#206905=CARTESIAN_POINT ( 'NONE',  ( 2.852447711054075796, -2.056726475855717773, -0.1563953359742433491 ) ) ;
#206913=CARTESIAN_POINT ( 'NONE',  ( 4.914598841593178946, 0.8265366316180179362, 2.007889688367751724 ) ) ;
#206916=CARTESIAN_POINT ( 'NONE',  ( 3.544333174469185721, -1.503253232081468216, 1.062929765333266108 ) ) ;
#206920=CARTESIAN_POINT ( 'NONE',  ( 6.614806895146394972, -0.1608752592793839531, 2.155998228907447523 ) ) ;
#206922=CARTESIAN_POINT ( 'NONE',  ( 0.8083708232014105155, -2.251370329867402376, 0.2228818479251652163 ) ) ;
#206927=CARTESIAN_POINT ( 'NONE',  ( -0.07574839183086683192, -0.8175154495408327726, -1.727131953450977253 ) ) ;
#206928=CARTESIAN_POINT ( 'NONE',  ( 0.9711603072033472284, 1.707112214499702407, -0.4667758381974375648 ) ) ;
#206930=CARTESIAN_POINT ( 'NONE',  ( 5.391275966583902957, -0.05175381893108904618, -2.012593086484148142 ) ) ;
#206932=CARTESIAN_POINT ( 'NONE',  ( 4.225680580359360228, -2.015911352056736661, 0.6092541954213681610 ) ) ;
#206934=CARTESIAN_POINT ( 'NONE',  ( 3.796418445691573940, 1.352171417773648132, -1.357169225504866406 ) ) ;
#206935=CARTESIAN_POINT ( 'NONE',  ( -0.02244404828160087226, 0.2256878572204877031, -2.222431841814066278 ) ) ;
#206936=CARTESIAN_POINT ( 'NONE',  ( 4.088306882321583124, 1.055547913133596749, -1.662622193200061771 ) ) ;
#206937=CARTESIAN_POINT ( 'NONE',  ( 5.220965578766386450, 1.526617224004393369, -1.322549803791906786 ) ) ;
#206938=CARTESIAN_POINT ( 'NONE',  ( 2.694054421766533203, -1.865511834602461949, -0.1395888279770511053 ) ) ;
#206939=CARTESIAN_POINT ( 'NONE',  ( 4.951616564603428472, 0.5366251361543332710, -1.639350107105986831 ) ) ;
#206941=CARTESIAN_POINT ( 'NONE',  ( 2.491098823239074278, -0.3784457004711218042, -2.174036671264235387 ) ) ;
#206944=CARTESIAN_POINT ( 'NONE',  ( 6.742638286788313451, -1.923764577213080029, -0.3838556375530403630 ) ) ;
#206952=CARTESIAN_POINT ( 'NONE',  ( 1.680221237283368696, -1.148429780529091948, -1.722445320287042447 ) ) ;
#206956=CARTESIAN_POINT ( 'NONE',  ( 0.1529977018510132181, 0.3474608822290006782, 1.989397386523162226 ) ) ;
#206961=CARTESIAN_POINT ( 'NONE',  ( 5.061874962716293780, 1.677747168027879709, -1.117663061872615771 ) ) ;
#206962=CARTESIAN_POINT ( 'NONE',  ( 5.120295473698084798, 1.888475294726537079, 0.3208887515022250669 ) ) ;
#206964=CARTESIAN_POINT ( 'NONE',  ( 2.173600921376659834, 1.351110561487681716, 1.725424542402646422 ) ) ;
#206967=CARTESIAN_POINT ( 'NONE',  ( 2.759904966095374501, 0.6844231338998980618, -1.785916880244736715 ) ) ;
#206970=CARTESIAN_POINT ( 'NONE',  ( 0.4215001937674204280, -1.427952733550428288, -1.423947716221201976 ) ) ;
#206972=CARTESIAN_POINT ( 'NONE',  ( 2.894169963053084160, -0.6095376172369629808, -1.999899515593931199 ) ) ;
#206974=CARTESIAN_POINT ( 'NONE',  ( 1.992754126006650806, 1.502677205460640764, -0.8464738358340985203 ) ) ;
#206985=CARTESIAN_POINT ( 'NONE',  ( 2.560951022220711248, -1.505102882618135629, 1.007669420338821675 ) ) ;
#206989=CARTESIAN_POINT ( 'NONE',  ( 4.037629478943724592, -1.732251659483119433, 0.5297805909155322013 ) ) ;
#206994=CARTESIAN_POINT ( 'NONE',  ( 3.877287848637627210, -0.1385928533646582361, 1.855967808809717789 ) ) ;
#206996=CARTESIAN_POINT ( 'NONE',  ( 1.001416299785270247, -1.868574072159228994, 0.4210543004025939506 ) ) ;
#206997=CARTESIAN_POINT ( 'NONE',  ( 1.061231560844998034, 0.3605832424212577769, -1.789441408372116182 ) ) ;
#207005=CARTESIAN_POINT ( 'NONE',  ( 5.383641442822343137, -1.871314765454759055, 0.6142198095173864170 ) ) ;
#207008=CARTESIAN_POINT ( 'NONE',  ( 0.8321122680391360715, 2.060015930055682620, 0.3555243805062404117 ) ) ;
#207009=CARTESIAN_POINT ( 'NONE',  ( 6.387721611049761883, 1.328912806184729734, 1.394852177740999233 ) ) ;
#207011=CARTESIAN_POINT ( 'NONE',  ( 1.746812667857342349, -1.544096848276183209, 0.9736100143667850704 ) ) ;
#207012=CARTESIAN_POINT ( 'NONE',  ( 3.651171877326536030, -1.804458330144659950, 1.270265763067345066 ) ) ;
#207014=CARTESIAN_POINT ( 'NONE',  ( 0.6504702201592416078, 1.884490048413577368, 0.3244712162126031085 ) ) ;
#207016=CARTESIAN_POINT ( 'NONE',  ( 1.047236342219150407, 1.738656489303032737, -0.9252727719080054980 ) ) ;
#207017=CARTESIAN_POINT ( 'NONE',  ( 2.911592935152186090, -0.9596169164145462727, -1.688359700174842271 ) ) ;
#207021=CARTESIAN_POINT ( 'NONE',  ( 6.174622966819019787, 1.250768081284852951, -1.378062710742117059 ) ) ;
#207026=CARTESIAN_POINT ( 'NONE',  ( 2.595491417077447238, -0.6846416945752286098, 2.081959150545972914 ) ) ;
#207028=AXIS2_PLACEMENT_3D ( 'NONE', #197858, #133977, #49490 ) ;
#207031=CARTESIAN_POINT ( 'NONE',  ( 3.246530741642670304, 0.4443377543969920795, 1.770662692542070538 ) ) ;
#207037=CARTESIAN_POINT ( 'NONE',  ( 0.6274103741727736772, -1.829744589303895275, 0.6030480328435404713 ) ) ;
#207038=CARTESIAN_POINT ( 'NONE',  ( 5.875826477234549650, -1.914729252524836056, 0.4262945716600323731 ) ) ;
#207047=CARTESIAN_POINT ( 'NONE',  ( 5.612195314557796522, 2.068136773602911038, -0.09592777784667855245 ) ) ;
#207049=CARTESIAN_POINT ( 'NONE',  ( 5.045646660657260973, -1.666335398280174074, 1.583644221457411794 ) ) ;
#207053=CARTESIAN_POINT ( 'NONE',  ( 0.04153208042980033321, -1.776208762584199574, -1.448543121555950774 ) ) ;
#207056=CARTESIAN_POINT ( 'NONE',  ( 4.365135538708351248, 1.883338149218495516, -0.4730343525067778332 ) ) ;
#207061=CARTESIAN_POINT ( 'NONE',  ( 6.258066496116281741, 0.7254575739856858885, -1.769658340881982816 ) ) ;
#207062=CARTESIAN_POINT ( 'NONE',  ( 6.334932600541999470, 0.1746011871221597178, 1.715888227437605718 ) ) ;
#207063=CARTESIAN_POINT ( 'NONE',  ( 5.612517632836663495, 1.944729323200469873, 0.5331731267440716904 ) ) ;
#207067=CARTESIAN_POINT ( 'NONE',  ( 2.185595087713845697, -0.8928614526015861141, 1.890522631819052002 ) ) ;
#207068=CARTESIAN_POINT ( 'NONE',  ( 6.608682216863940084, 1.309337763449496705, -1.190854552318038051 ) ) ;
#207069=CARTESIAN_POINT ( 'NONE',  ( 5.608046130584797950, -0.04667949407829303371, 2.016033753796213635 ) ) ;
#207071=CARTESIAN_POINT ( 'NONE',  ( 2.537429240164018385, -1.699656577751871289, -1.538240582240576693 ) ) ;
#207072=CARTESIAN_POINT ( 'NONE',  ( 2.694910210795556260, -0.5461130550479543766, 1.652493440627414323 ) ) ;
#207074=CARTESIAN_POINT ( 'NONE',  ( 1.897353599431324866, 0.1640088499204050976, 1.726041979094733447 ) ) ;
#207076=CARTESIAN_POINT ( 'NONE',  ( 1.873285555135986824, -0.2318667498520594894, 1.846494694648516788 ) ) ;
#207077=CARTESIAN_POINT ( 'NONE',  ( 2.031898538270035637, 2.078123050159206286, -0.6288832818364347155 ) ) ;
#207078=CARTESIAN_POINT ( 'NONE',  ( 3.819546216251490822, -1.394084564108012403, -1.457236891723237449 ) ) ;
#207079=CARTESIAN_POINT ( 'NONE',  ( 3.875000000000003553, 2.052068128417946724, -2.337016516192933888E-13 ) ) ;
#207082=CARTESIAN_POINT ( 'NONE',  ( 1.237189336409921570, -1.742702465754492058, 0.8212270227533255973 ) ) ;
#207085=CARTESIAN_POINT ( 'NONE',  ( 3.639129310729662503, 2.110331241038451822, 0.6939571745526812441 ) ) ;
#207092=CARTESIAN_POINT ( 'NONE',  ( 5.959279902674206042, -1.877032357297861109, 1.187784507339540108 ) ) ;
#207093=CARTESIAN_POINT ( 'NONE',  ( 4.650807877244386823, -0.4278111053654386486, -1.914496481071884970 ) ) ;
#207097=CARTESIAN_POINT ( 'NONE',  ( 5.554102117330329769, 2.260170762534471578, -0.1031424389980051676 ) ) ;
#207100=CARTESIAN_POINT ( 'NONE',  ( 2.102078608570765450, 0.7915390796853873923, -1.904948021121543711 ) ) ;
#207106=CARTESIAN_POINT ( 'NONE',  ( 4.253091631423633778, -1.553859266942819284, -1.041061106808522929 ) ) ;
#207107=CARTESIAN_POINT ( 'NONE',  ( 3.094086244858067047, -0.3350832708051197373, 1.701246549458427015 ) ) ;
#207108=CARTESIAN_POINT ( 'NONE',  ( 0.6270410820986601630, 0.1761543355088228957, 2.285679397864130102 ) ) ;
#207109=CARTESIAN_POINT ( 'NONE',  ( 1.325528760500709780, -0.05309137938146882979, 2.206304558879538025 ) ) ;
#207110=CARTESIAN_POINT ( 'NONE',  ( 4.124618644571789616, 0.1043759322204278750, 2.088280726629719197 ) ) ;
#207111=CARTESIAN_POINT ( 'NONE',  ( 5.788998755281030029, 1.472039788614720290, 1.266697539889444446 ) ) ;
#207116=CARTESIAN_POINT ( 'NONE',  ( 0.03578008775950020093, -1.617816776142148250, 1.203357013023528932 ) ) ;
#207117=CARTESIAN_POINT ( 'NONE',  ( -0.05226516427493665962, -1.936187138999283297, 0.8653993394739032397 ) ) ;
#207123=CARTESIAN_POINT ( 'NONE',  ( 3.949673224339702138, 0.6133576713117370183, -1.719707012317383432 ) ) ;
#207124=CARTESIAN_POINT ( 'NONE',  ( 2.292262453775519404, -0.9438808975747980945, 1.994871701834355804 ) ) ;
#207129=CARTESIAN_POINT ( 'NONE',  ( 1.582292005822239167, 1.041880795974026608, 1.730197787189115433 ) ) ;
#207133=CARTESIAN_POINT ( 'NONE',  ( 3.221387034570993624, 0.2776250501920934921, -1.840009301959115051 ) ) ;
#207140=CARTESIAN_POINT ( 'NONE',  ( 4.371595934376539816, 1.770262903079304451, -0.4459408992859363319 ) ) ;
#207145=CARTESIAN_POINT ( 'NONE',  ( 6.819686488043297246, -1.560180513003786462, 1.276622200526676743 ) ) ;
#207146=CARTESIAN_POINT ( 'NONE',  ( 5.261588992693945421, 0.9106475924270783784, 1.600083007495013643 ) ) ;
#207147=CARTESIAN_POINT ( 'NONE',  ( 4.582853619701852566, -2.237698958467302823, -0.5636369891960175682 ) ) ;
#207149=CARTESIAN_POINT ( 'NONE',  ( 0.4036811037357163623, -0.5522049309486184443, 1.985320814919430132 ) ) ;
#207152=CARTESIAN_POINT ( 'NONE',  ( 5.642068729656325665, -0.04839715497878017969, -2.298027403377851385 ) ) ;
#207155=CARTESIAN_POINT ( 'NONE',  ( 6.016445890116215445, 1.255022122864515310, -1.387330985440645037 ) ) ;
#207157=CARTESIAN_POINT ( 'NONE',  ( 2.144650067465687648, 1.855875215511919363, 0.4610605321611755958 ) ) ;
#207159=CARTESIAN_POINT ( 'NONE',  ( 4.406973378220558679, 1.706932345810768359, -1.398813476408675260 ) ) ;
#207160=CARTESIAN_POINT ( 'NONE',  ( 4.364542673910889015, -2.054697287276555873, -0.5108639600793271063 ) ) ;
#207162=CARTESIAN_POINT ( 'NONE',  ( 6.883263157960368694, 4.693146704925188040, 2.608790034323371643 ) ) ;
#207165=CARTESIAN_POINT ( 'NONE',  ( 2.362750734746793757, 0.9868518204677073635, 2.086042234993300770 ) ) ;
#207166=CARTESIAN_POINT ( 'NONE',  ( 3.103904542773823660, 0.7086415210641981988, -1.829580771271981154 ) ) ;
#207168=CARTESIAN_POINT ( 'NONE',  ( 6.719587945281444874, 0.3584770237896938716, -2.031047634367310284 ) ) ;
#207172=CARTESIAN_POINT ( 'NONE',  ( 4.909388789075159742, -1.913262893431907141, 0.6371506334161003426 ) ) ;
#207177=CARTESIAN_POINT ( 'NONE',  ( 2.325261487346420797, -1.983500291700568852, -0.8831872222036639686 ) ) ;
#207183=CARTESIAN_POINT ( 'NONE',  ( 1.159529407832321501, 0.4047576141815812378, -2.020457351226915055 ) ) ;
#207185=FACE_OUTER_BOUND ( 'NONE', #24490, .T. ) ;
#207188=CARTESIAN_POINT ( 'NONE',  ( 3.035702773332124238, -1.842316306609870891, 0.5122265333450184421 ) ) ;
#207189=CARTESIAN_POINT ( 'NONE',  ( 4.785902253289605390, -0.8326956132961546020, 1.561725933240491360 ) ) ;
#207193=CARTESIAN_POINT ( 'NONE',  ( 0.09280537598354164641, 1.668161973260675834, 0.9417010505823987243 ) ) ;
#207196=CARTESIAN_POINT ( 'NONE',  ( 0.9419464005683108043, 1.389173191389100337, 1.535309223701806447 ) ) ;
#207198=CARTESIAN_POINT ( 'NONE',  ( 6.069203928793593050, 0.1358119448514639727, -1.865795782587629681 ) ) ;
#207199=CARTESIAN_POINT ( 'NONE',  ( 2.121465551170404140, -1.771062468586531047, 0.4427346646293239818 ) ) ;
#207200=CARTESIAN_POINT ( 'NONE',  ( 5.760442859251142522, 0.8911043219209063837, 2.019162844794204048 ) ) ;
#207204=CARTESIAN_POINT ( 'NONE',  ( 3.490735631032083841, 2.011810643276640054, 0.4545708190045735786 ) ) ;
#207210=CARTESIAN_POINT ( 'NONE',  ( 5.529760519541640384, 1.996289034380031913, -0.5486624943154896350 ) ) ;
#207212=CARTESIAN_POINT ( 'NONE',  ( 2.636181727411972098, 1.021492356387411427, -1.905029093917938399 ) ) ;
#207214=CARTESIAN_POINT ( 'NONE',  ( 3.615882686718306260, -0.5843173316345972035, 1.933312988646131103 ) ) ;
#207215=CARTESIAN_POINT ( 'NONE',  ( 2.594135478747404022, 0.9273930874063830432, -1.728848471177657942 ) ) ;
#207216=CARTESIAN_POINT ( 'NONE',  ( 6.720655732516620517, 2.957990990047154600, 2.526349433132681011 ) ) ;
#207221=CARTESIAN_POINT ( 'NONE',  ( 1.569546381206438967, 1.394087592100446971, 1.457234012747665508 ) ) ;
#207223=CARTESIAN_POINT ( 'NONE',  ( 5.759372899636661991, 2.159370146098410714, -0.3733810082120898599 ) ) ;
#207225=CARTESIAN_POINT ( 'NONE',  ( 6.328373294368253354, -0.9077179077918960948, -1.683272687665722467 ) ) ;
#207229=CARTESIAN_POINT ( 'NONE',  ( 2.759388848745081280, 1.913798524274639812, -0.6352183541234107667 ) ) ;
#207232=CARTESIAN_POINT ( 'NONE',  ( -0.01747323780270595983, -0.1290080397739183926, -1.696210917522892325 ) ) ;
#207236=CARTESIAN_POINT ( 'NONE',  ( 4.235518730357812345, -1.288231833625707701, -1.356488508162751128 ) ) ;
#207238=CARTESIAN_POINT ( 'NONE',  ( 1.323191598296684646, -1.869966582492128548, -0.8887066864656999465 ) ) ;
#207239=CARTESIAN_POINT ( 'NONE',  ( 6.619590326553026038, 0.3579758704960536719, -2.039031579972025554 ) ) ;
#207242=CARTESIAN_POINT ( 'NONE',  ( 0.03503794071320948805, -0.08894543905034424380, 1.809493548878613023 ) ) ;
#207248=CARTESIAN_POINT ( 'NONE',  ( 1.662477996687723669, -0.7030478115006146833, -1.831755296705489977 ) ) ;
#207250=CARTESIAN_POINT ( 'NONE',  ( 4.956599115817130752, -1.805213640821627052, -0.6413244422398997058 ) ) ;
#207257=CARTESIAN_POINT ( 'NONE',  ( 2.922914210685311431, 2.035003303901411265, 0.7295308445595325431 ) ) ;
#207260=CARTESIAN_POINT ( 'NONE',  ( -0.03470293633787284449, -1.699275230904277789, 1.268407768021381221 ) ) ;
#207261=CARTESIAN_POINT ( 'NONE',  ( 4.700122295916242088, -1.825221593135372578, -0.04401369772454033491 ) ) ;
#207263=CARTESIAN_POINT ( 'NONE',  ( 0.8957027828950543391, -0.7134963830764933235, 1.837871659531468804 ) ) ;
#207264=CARTESIAN_POINT ( 'NONE',  ( 3.849791259674230748, -1.322437695595569673, -1.381667681676468140 ) ) ;
#207267=CARTESIAN_POINT ( 'NONE',  ( 4.756286019550246102, -1.969087757444639042, -0.05037552155932183140 ) ) ;
#207269=CARTESIAN_POINT ( 'NONE',  ( 6.374560617330069512, -0.09999853314933374038, -1.939619642457596660 ) ) ;
#207273=CARTESIAN_POINT ( 'NONE',  ( 6.328397690248316110, -1.000878058022572903, -1.869571840794107986 ) ) ;
#207275=CARTESIAN_POINT ( 'NONE',  ( 3.668532269402470458, 0.6909111621477401766, 1.783275653667259597 ) ) ;
#207281=CARTESIAN_POINT ( 'NONE',  ( 5.531894615797754433, -1.963542475010676469, 0.4432068886008522779 ) ) ;
#207283=CARTESIAN_POINT ( 'NONE',  ( 6.604126001430527637, -1.825160783932573860, 0.05055279568313279792 ) ) ;
#207284=CARTESIAN_POINT ( 'NONE',  ( 6.727182134110221590, 3.706444386917655542, 2.325533714637216143 ) ) ;
#207285=CARTESIAN_POINT ( 'NONE',  ( 1.557173632797459462, 1.693725193156172315, -1.190412882225246438 ) ) ;
#207296=CARTESIAN_POINT ( 'NONE',  ( 6.825078400183575589, 6.038285016609903799, 2.450557349082567171 ) ) ;
#207299=CARTESIAN_POINT ( 'NONE',  ( 5.291581958225426874, 1.307657812419236176, -1.139094164941084841 ) ) ;
#207301=CARTESIAN_POINT ( 'NONE',  ( 2.834898843300116766, -1.979765732921334731, -0.6052725283285932401 ) ) ;
#207303=CARTESIAN_POINT ( 'NONE',  ( 3.532911237611217281, -1.729578172696862426, 1.220892919093808482 ) ) ;
#207306=CARTESIAN_POINT ( 'NONE',  ( 1.657020797538899748, 1.613050045282127032, -1.129676354644502556 ) ) ;
#207309=CARTESIAN_POINT ( 'NONE',  ( -0.01753026575586694516, -1.247696154478775021, 1.449428981083925150 ) ) ;
#207310=CARTESIAN_POINT ( 'NONE',  ( 3.750172280943805170, 0.8240398376481252729, 2.139190334408520577 ) ) ;
#207311=CARTESIAN_POINT ( 'NONE',  ( 1.805030607383810715, 1.517133602069477893, 1.015288170653723343 ) ) ;
#207317=CARTESIAN_POINT ( 'NONE',  ( 2.478773383088346716, -1.385198452255667290, 1.461135165768602029 ) ) ;
#207318=( BOUNDED_SURFACE ( )  B_SPLINE_SURFACE ( 3, 3, ( 
 ( #139440, #122199, #205475, #169782, #54976, #21371, #80550, #196437, #144531, #323, #131483 ),
 ( #32866, #210540, #115248, #82669, #179127, #29678, #30749, #14459, #132541, #97889, #48081 ),
 ( #162879, #78410, #180191, #148753, #116306, #114192, #98942, #49130, #198539, #65336, #181238 ),
 ( #161815, #197487, #50185, #164996, #16587, #62174, #146647, #66393, #13405, #96830, #163950 ),
 ( #63231, #160736, #182296, #212662, #33923, #129394, #95762, #31813, #195373, #64304, #15525 ),
 ( #79481, #130449, #47005, #12330, #213713, #128333, #81611, #145599, #147695, #194296, #45941 ),
 ( #112060, #178060, #211595, #113121, #104274, #134663, #202804, #153015, #55515, #102129, #84809 ) ),
 .UNSPECIFIED., .T., .F., .F. ) 
 B_SPLINE_SURFACE_WITH_KNOTS ( ( 4, 3, 4 ),
 ( 4, 1, 1, 1, 1, 1, 1, 1, 4 ),
 ( 0.000000000000000000, 0.5000000000000000000, 1.000000000000000000 ),
 ( 0.000000000000000000, 0.2254704865597413344, 0.3973194950497592193, 0.5246576192285303808, 0.6166070239209043846, 0.6823180413592140336, 0.7309932997181896042, 0.7717238569598857678, 1.000000000000000000 ),
 .UNSPECIFIED. ) 
 GEOMETRIC_REPRESENTATION_ITEM ( )  RATIONAL_B_SPLINE_SURFACE ( (
 ( 1.000000000000000000, 1.000000000000000000, 1.000000000000000222, 0.9999999999999997780, 1.000000000000000444, 0.9999999999999996669, 1.000000000000000222, 1.000000000000000222, 1.000000000000000222, 1.000000000000000222, 1.000000000000000222),
 ( 0.3333333333333333703, 0.3333333333333334259, 0.3333333333333333703, 0.3333333333333333703, 0.3333333333333334814, 0.3333333333333332038, 0.3333333333333334814, 0.3333333333333334259, 0.3333333333333334259, 0.3333333333333334259, 0.3333333333333334259),
 ( 0.3333333333333333703, 0.3333333333333334259, 0.3333333333333333703, 0.3333333333333333703, 0.3333333333333334814, 0.3333333333333332038, 0.3333333333333334814, 0.3333333333333334259, 0.3333333333333334259, 0.3333333333333334259, 0.3333333333333334259),
 ( 1.000000000000000000, 1.000000000000000000, 1.000000000000000222, 0.9999999999999997780, 1.000000000000000444, 0.9999999999999996669, 1.000000000000000222, 1.000000000000000222, 1.000000000000000222, 1.000000000000000222, 1.000000000000000222),
 ( 0.3333333333333333703, 0.3333333333333334259, 0.3333333333333333703, 0.3333333333333333703, 0.3333333333333334814, 0.3333333333333332038, 0.3333333333333334814, 0.3333333333333334259, 0.3333333333333334259, 0.3333333333333334259, 0.3333333333333334259),
 ( 0.3333333333333333703, 0.3333333333333334259, 0.3333333333333333703, 0.3333333333333333703, 0.3333333333333334814, 0.3333333333333332038, 0.3333333333333334814, 0.3333333333333334259, 0.3333333333333334259, 0.3333333333333334259, 0.3333333333333334259),
 ( 1.000000000000000000, 1.000000000000000000, 1.000000000000000222, 0.9999999999999997780, 1.000000000000000444, 0.9999999999999996669, 1.000000000000000222, 1.000000000000000222, 1.000000000000000222, 1.000000000000000222, 1.000000000000000222) ) ) 
 REPRESENTATION_ITEM ( '' )  SURFACE ( )  );
#207319=CARTESIAN_POINT ( 'NONE',  ( 2.272246806564695021, -0.9202570425024100276, -1.732484491337261456 ) ) ;
#207322=CARTESIAN_POINT ( 'NONE',  ( 0.07516593201277278757, 5.721767059778611220, -2.638283098249011971 ) ) ;
#207323=CARTESIAN_POINT ( 'NONE',  ( 5.156232390734752258, -1.514662699498746878, 1.441270160984737370 ) ) ;
#207324=CARTESIAN_POINT ( 'NONE',  ( 4.012378993168019825, 1.251447367628313767, -1.251755930634059100 ) ) ;
#207326=CARTESIAN_POINT ( 'NONE',  ( 6.404234474585668302, 1.703059896339639057, -1.534467582428314270 ) ) ;
#207327=CARTESIAN_POINT ( 'NONE',  ( 6.052664191884576717, -1.496297717267160765, -0.8884939375988825105 ) ) ;
#207330=CARTESIAN_POINT ( 'NONE',  ( 5.959697520924294167, -2.181652697926935502, -0.7244182876006750593 ) ) ;
#207332=CARTESIAN_POINT ( 'NONE',  ( -0.1232117409455633916, -0.1621322592461546530, -2.156395338765437764 ) ) ;
#207333=CARTESIAN_POINT ( 'NONE',  ( 5.852856049955673434, -0.7765510095132116541, 1.550312759826449671 ) ) ;
#207334=CARTESIAN_POINT ( 'NONE',  ( 5.986835238096758438, 2.090873126042319896, 0.5847848357620232251 ) ) ;
#207336=CARTESIAN_POINT ( 'NONE',  ( 0.2162074652159052257, 1.082675745310441862, -1.819457589102360551 ) ) ;
#207337=CARTESIAN_POINT ( 'NONE',  ( 6.062500000000003553, -1.451031289061355478, -1.451031289060867868 ) ) ;
#207339=CARTESIAN_POINT ( 'NONE',  ( 3.926716319054617266, 1.828954700887480245, 0.6050711068611572818 ) ) ;
#207341=CARTESIAN_POINT ( 'NONE',  ( 0.9091800373960364778, -0.5448693228766487984, -2.153321320651789161 ) ) ;
#207347=CARTESIAN_POINT ( 'NONE',  ( 2.614199364429617756, -0.6941352821057051870, 2.110140411616817868 ) ) ;
#207349=CARTESIAN_POINT ( 'NONE',  ( -0.02900071798682749002, 0.2267074960015900975, -2.207170277039482986 ) ) ;
#207353=CARTESIAN_POINT ( 'NONE',  ( 1.195935645703485539, 1.779627574718087635, 0.9480385367472210500 ) ) ;
#207355=CARTESIAN_POINT ( 'NONE',  ( 6.742638559370645268, -2.022111636011727498, -0.4062529910623476903 ) ) ;
#207360=CARTESIAN_POINT ( 'NONE',  ( 1.914973420724352726, -0.2224279105748054597, 1.755648307094020311 ) ) ;
#207361=CARTESIAN_POINT ( 'NONE',  ( 0.6685925339881376717, 1.356301626434471164, 1.492253803477984642 ) ) ;
#207362=CARTESIAN_POINT ( 'NONE',  ( 5.284588373313929388, 1.531378566088846371, -0.8270805780791794515 ) ) ;
#207363=CARTESIAN_POINT ( 'NONE',  ( 4.107168962890386688, -0.3918867163640211704, 2.258474592593032959 ) ) ;
#207365=CARTESIAN_POINT ( 'NONE',  ( 2.800538183361205302, 1.555518290611109800, 0.9846574483025125613 ) ) ;
#207368=CARTESIAN_POINT ( 'NONE',  ( 2.731258071184277103, -1.704167518380688140, 0.6551187846031493178 ) ) ;
#207369=CARTESIAN_POINT ( 'NONE',  ( 3.973279856364997809, -1.994869694282218386, -0.2930714778977619450 ) ) ;
#207371=CARTESIAN_POINT ( 'NONE',  ( 2.659333574217698004, -1.968172486592324244, -1.115815620033432154 ) ) ;
#207373=CARTESIAN_POINT ( 'NONE',  ( 5.262764605058766421, -1.527415466006694533, 1.450107492850923441 ) ) ;
#207375=CARTESIAN_POINT ( 'NONE',  ( 2.330607996690749140, -1.275545549462468120, 1.630658604070814199 ) ) ;
#207378=CARTESIAN_POINT ( 'NONE',  ( 4.600305182625006317, -0.9987976242244799296, 1.870504488178956759 ) ) ;
#207379=CARTESIAN_POINT ( 'NONE',  ( 0.9438256413601053829, 0.7817106414217175336, -1.760949446298063936 ) ) ;
#207385=CARTESIAN_POINT ( 'NONE',  ( 5.871359616481898414, -1.819694913365289768, -1.088597390283413402 ) ) ;
#207386=CARTESIAN_POINT ( 'NONE',  ( 1.782391780347460486, -1.127077160282144552, 1.778786634185139270 ) ) ;
#207389=CARTESIAN_POINT ( 'NONE',  ( 6.561375291409637711, 1.546756896810308035, 1.034385502077879382 ) ) ;
#207395=CARTESIAN_POINT ( 'NONE',  ( 0.6508261300204335464, 2.090236094481153550, 0.3566229023672163878 ) ) ;
#207398=CARTESIAN_POINT ( 'NONE',  ( 3.226955236329264398, -1.811681696138227160, -0.7532884077038404236 ) ) ;
#207399=CARTESIAN_POINT ( 'NONE',  ( 0.6905621207787122628, -2.145541755201633372, -0.2633910710312590275 ) ) ;
#207403=CARTESIAN_POINT ( 'NONE',  ( 2.097218849865792212, -1.740012409040556429, 0.04131442251954255129 ) ) ;
#207406=CARTESIAN_POINT ( 'NONE',  ( 2.688827190807027367, -1.158510681541668141, -1.649829502315000251 ) ) ;
#207407=CARTESIAN_POINT ( 'NONE',  ( 6.825078400183582694, 7.051583320515966591, 2.842498375355909435 ) ) ;
#207409=CARTESIAN_POINT ( 'NONE',  ( 2.571113415349820297, 0.09854779587974149546, -1.969128565948689458 ) ) ;
#207410=CARTESIAN_POINT ( 'NONE',  ( 6.345967646908174054, -1.254484226688237447, -1.443505786478386899 ) ) ;
#207415=CARTESIAN_POINT ( 'NONE',  ( 2.543622981932230243, -1.883669348803659549, 0.7290701893776069253 ) ) ;
#207417=CARTESIAN_POINT ( 'NONE',  ( 5.245303717312764569, -1.982421492789496753, 1.180877550764187545 ) ) ;
#207418=CARTESIAN_POINT ( 'NONE',  ( 6.566857081534598350, 1.454584517406570132, -1.316677807353151097 ) ) ;
#207419=CARTESIAN_POINT ( 'NONE',  ( 3.116010788575247936, 1.952738871351952232, -0.1875660449981580158 ) ) ;
#207421=CARTESIAN_POINT ( 'NONE',  ( 0.3346115673153668424, 0.6298721381652396811, -1.915601020889952322 ) ) ;
#207423=CARTESIAN_POINT ( 'NONE',  ( 2.712237125307418228, 1.172176456337461037, -1.763091465072692987 ) ) ;
#207426=CARTESIAN_POINT ( 'NONE',  ( 1.921575063125853022, 1.060747535801230379, -1.504664925706208578 ) ) ;
#207430=CARTESIAN_POINT ( 'NONE',  ( 2.566775492539817627, 0.7186216927172992541, 1.995234744298620910 ) ) ;
#207434=CARTESIAN_POINT ( 'NONE',  ( 4.235659074092642307, -1.418359850100110009, -1.495269491646352256 ) ) ;
#207437=CARTESIAN_POINT ( 'NONE',  ( 1.698526806778306586, 1.531337151408303621, 1.022036240780115346 ) ) ;
#207442=CARTESIAN_POINT ( 'NONE',  ( 1.348561525465460820, 2.204488851003219896, 0.1053889787279923829 ) ) ;
#207443=CARTESIAN_POINT ( 'NONE',  ( 2.847247395794590297, -1.882567391055539385, 1.254484791939513899 ) ) ;
#207445=CARTESIAN_POINT ( 'NONE',  ( 3.638735373827857167, 1.721918111813141916, 0.5631709482423822299 ) ) ;
#207446=CARTESIAN_POINT ( 'NONE',  ( 3.116317603207694464, 1.870113986138211670, 0.4147879586954768549 ) ) ;
#207447=CARTESIAN_POINT ( 'NONE',  ( 3.982925052038261526, 1.964963782255540359, 0.6523228965355857278 ) ) ;
#207449=CARTESIAN_POINT ( 'NONE',  ( 2.852367248507085229, 0.6625980423298013511, 1.856917580869015039 ) ) ;
#207450=CARTESIAN_POINT ( 'NONE',  ( 1.360239512323542010, 0.7782574302275366840, 1.762357998526616232 ) ) ;
#207451=CARTESIAN_POINT ( 'NONE',  ( 4.135518821028766112, -1.289757458839156934, -1.355179912160727085 ) ) ;
#207453=CARTESIAN_POINT ( 'NONE',  ( 1.963905137100800724, 0.3917726540721230832, -2.274054798471192296 ) ) ;
#207455=CARTESIAN_POINT ( 'NONE',  ( 3.912436197073854593, 0.6682525715841195479, 1.737132965711101873 ) ) ;
#207460=CARTESIAN_POINT ( 'NONE',  ( 0.3464870678724129016, 2.100606130083045198, 0.1525024232564754778 ) ) ;
#207463=CARTESIAN_POINT ( 'NONE',  ( 6.679002375395027613, -0.09866081283815136826, -2.159460157733564145 ) ) ;
#207464=CARTESIAN_POINT ( 'NONE',  ( 2.162495577681341707, 2.120227376586072854, 0.04728746717985036346 ) ) ;
#207465=CARTESIAN_POINT ( 'NONE',  ( 6.621752733038558603, -0.4373435798001067965, 1.978785184894470639 ) ) ;
#207469=CARTESIAN_POINT ( 'NONE',  ( 0.9136071317731933039, -0.3180670004044767740, 2.137961049616762921 ) ) ;
#207471=CARTESIAN_POINT ( 'NONE',  ( 6.825078400183556937, 1.282741234726336943, 1.971047034039685952 ) ) ;
#207474=CARTESIAN_POINT ( 'NONE',  ( 4.452361426671761713, -1.313546101436880109, 1.530156479064001207 ) ) ;
#207477=CARTESIAN_POINT ( 'NONE',  ( 0.5676901151186209971, 0.2185747425910676001, -2.251950761720759253 ) ) ;
#207481=CARTESIAN_POINT ( 'NONE',  ( 6.310172759758509109, 1.158674036163497734, -1.650093421473826316 ) ) ;
#207486=CARTESIAN_POINT ( 'NONE',  ( 2.824480366436402878, 1.624150206794371609, 0.5811974035451406007 ) ) ;
#207489=CARTESIAN_POINT ( 'NONE',  ( 1.475481261428980506, 1.048764899322068622, 1.425360520505250417 ) ) ;
#207490=CARTESIAN_POINT ( 'NONE',  ( 2.262359935378143394, 2.012689932058016495, 0.04726890441942610543 ) ) ;
#207492=CARTESIAN_POINT ( 'NONE',  ( 4.260898339918250066, -1.637375743694971408, 1.479669880875638999 ) ) ;
#207496=CARTESIAN_POINT ( 'NONE',  ( 4.178469031319306914, 1.000645923475869559, 1.869553197578948334 ) ) ;
#207497=CARTESIAN_POINT ( 'NONE',  ( 3.339470413395662085, 0.4871825726840799398, -1.956567533273507964 ) ) ;
#207498=CARTESIAN_POINT ( 'NONE',  ( 3.937629537800376500, -1.731762593766679403, 0.5317277010480087052 ) ) ;
#207504=CARTESIAN_POINT ( 'NONE',  ( 0.8482696660519238874, 0.5391449902514727777, 1.791282564952957124 ) ) ;
#207507=CARTESIAN_POINT ( 'NONE',  ( 6.305291373979138747, 1.520805759102667132, 1.009792402853857407 ) ) ;
#207509=CARTESIAN_POINT ( 'NONE',  ( 2.694441388940031601, 1.384233754937878258, -1.324569364742228972 ) ) ;
#207517=CARTESIAN_POINT ( 'NONE',  ( 2.988655875014298857, -1.259908772670719657, 1.705623289672608678 ) ) ;
#207518=CARTESIAN_POINT ( 'NONE',  ( -0.02948999725180430354, 5.724051133006486936, -2.520349822069901879 ) ) ;
#207520=CARTESIAN_POINT ( 'NONE',  ( 4.270748893545842861, -1.838291250766799223, -0.7124064801689540261 ) ) ;
#207521=CARTESIAN_POINT ( 'NONE',  ( 0.1057268774627964369, 1.494660468187744229, 1.348908602934977496 ) ) ;
#207523=CARTESIAN_POINT ( 'NONE',  ( 0.1404439707000069981, 0.8148842331482269996, 1.954324566802398744 ) ) ;
#207525=CARTESIAN_POINT ( 'NONE',  ( 1.240778115703184303, -2.019486815914430355, -0.4554155650244652853 ) ) ;
#207526=CARTESIAN_POINT ( 'NONE',  ( 2.167823750104383773, -1.194498894885902329, 1.531050872003832497 ) ) ;
#207530=CARTESIAN_POINT ( 'NONE',  ( 4.154300538700359091, -1.549125135342351856, 1.404095012314343416 ) ) ;
#207533=CARTESIAN_POINT ( 'NONE',  ( 0.7151241933986829391, 1.480140477221444373, 1.044027612606616140 ) ) ;
#207535=CARTESIAN_POINT ( 'NONE',  ( 5.338574060078519423, 2.173733305800494175, 0.3801736985692484305 ) ) ;
#207537=CARTESIAN_POINT ( 'NONE',  ( 3.698430944683338328, -2.204125419102770600, -0.1106900096672913392 ) ) ;
#207539=CARTESIAN_POINT ( 'NONE',  ( 2.965378323150099860, -1.564627974442783342, -1.099164922500090347 ) ) ;
#207541=CARTESIAN_POINT ( 'NONE',  ( 4.896967953096117654, 0.3505727482827174502, 2.040303948762006492 ) ) ;
#207543=CARTESIAN_POINT ( 'NONE',  ( 2.606508400632711719, -0.8264410288459265175, -1.997682696722333784 ) ) ;
#207544=CARTESIAN_POINT ( 'NONE',  ( 5.284801750429747536, 1.933107837519608685, -1.032524723389722787 ) ) ;
#207546=( NAMED_UNIT ( * ) PLANE_ANGLE_UNIT ( ) SI_UNIT ( $, .RADIAN. ) );
#207552=CARTESIAN_POINT ( 'NONE',  ( 5.823117640241993520, -1.869163851432435575, -0.8903994044791310181 ) ) ;
#207553=CARTESIAN_POINT ( 'NONE',  ( 4.758382555496592836, 0.7388506920381915366, 1.779377657810585767 ) ) ;
#207554=CARTESIAN_POINT ( 'NONE',  ( 0.4742327405582689170, -2.001515332587662233, -0.2440062454662216829 ) ) ;
#207558=CARTESIAN_POINT ( 'NONE',  ( 5.418793955257063644, -1.429144796294969932, 1.355356204701572143 ) ) ;
#207559=CARTESIAN_POINT ( 'NONE',  ( 6.632792736454030447, -2.050728487082712270, 1.024446431767987331 ) ) ;
#207560=CARTESIAN_POINT ( 'NONE',  ( 4.688025921862073453, -0.8580590012943272171, 1.611482198803436905 ) ) ;
#207568=CARTESIAN_POINT ( 'NONE',  ( 2.595044651933966495, -0.5755060336137384214, 1.749081985381637061 ) ) ;
#207569=CARTESIAN_POINT ( 'NONE',  ( -0.09313581672419719848, -0.4459848746838651623, -1.970588110806646753 ) ) ;
#207570=CARTESIAN_POINT ( 'NONE',  ( 0.5800033175489105464, 1.582751930679682228, -1.666757776657208145 ) ) ;
#207571=CARTESIAN_POINT ( 'NONE',  ( 5.682460714699895554, 1.171467074228413674, -1.573401077569417605 ) ) ;
#207575=CARTESIAN_POINT ( 'NONE',  ( 0.1685321339487330372, -0.8835925182541467526, -1.870455940253319183 ) ) ;
#207577=CARTESIAN_POINT ( 'NONE',  ( 2.419574211619343274, -1.206166186839405352, -1.707533215648052050 ) ) ;
#207578=CARTESIAN_POINT ( 'NONE',  ( 1.656895194024514906, -1.602792776363659133, -0.9643473572949823325 ) ) ;
#207579=CARTESIAN_POINT ( 'NONE',  ( 1.985703663612121472, 1.880146017696176619, 0.7282698753105636413 ) ) ;
#207581=CARTESIAN_POINT ( 'NONE',  ( 1.751089554790756342, 1.735802523247106377, -0.1280615824842730732 ) ) ;
#207585=CARTESIAN_POINT ( 'NONE',  ( 2.384998569339055408, 1.577468512335476358, -0.6981430484895093658 ) ) ;
#207586=CARTESIAN_POINT ( 'NONE',  ( 2.226364491882920404, 2.126620374013419301, 0.5291077681483095096 ) ) ;
#207588=CARTESIAN_POINT ( 'NONE',  ( 5.584669497696876483, -2.152379054646291756, -0.4867646435422824935 ) ) ;
#207590=CARTESIAN_POINT ( 'NONE',  ( 2.377987901236592982, -2.106814941015792808, 0.5239127008311114109 ) ) ;
#207591=CARTESIAN_POINT ( 'NONE',  ( 0.7326872660318053398, 0.1314506862302306234, 1.821024990000128518 ) ) ;
#207592=CARTESIAN_POINT ( 'NONE',  ( 3.432911303685074689, -1.728510519573158266, 1.222591858268074150 ) ) ;
#207593=CARTESIAN_POINT ( 'NONE',  ( 6.539320575229256249, 6.037491965140660000, 2.591644950450102680 ) ) ;
#207595=CARTESIAN_POINT ( 'NONE',  ( 3.562334897874219308, -1.538608923441080689, 1.699488912218325654 ) ) ;
#207598=CARTESIAN_POINT ( 'NONE',  ( 5.444044349889116674, -1.407711435423303792, -1.718264895412445536 ) ) ;
#207603=CARTESIAN_POINT ( 'NONE',  ( 6.825078400183575589, 6.038285016609903799, 2.450557349082567171 ) ) ;
#207605=CARTESIAN_POINT ( 'NONE',  ( 4.395157833011634096, -0.8647231026696032830, -1.821742675176166060 ) ) ;
#207607=CARTESIAN_POINT ( 'NONE',  ( 3.344635507851092981, -2.031254381041375456, -0.3572892473815546532 ) ) ;
#207611=ADVANCED_FACE ( 'NONE', ( #160122 ), #166176, .F. ) ;
#207613=CARTESIAN_POINT ( 'NONE',  ( 6.632779825423476439, -1.959453823303359377, 0.9815127000676395763 ) ) ;
#207614=CARTESIAN_POINT ( 'NONE',  ( 3.164685561777963230, 1.281361203394768111, 1.556908733426412450 ) ) ;
#207615=CARTESIAN_POINT ( 'NONE',  ( 2.208333698829296310, 1.645431377724184463, 0.8263914577605266931 ) ) ;
#207619=CARTESIAN_POINT ( 'NONE',  ( 5.983392046985362533, 1.685759371660649375, -0.7011634845648377912 ) ) ;
#207621=CARTESIAN_POINT ( 'NONE',  ( 6.051720714260678591, 0.6634699467917944959, -2.163057363297292035 ) ) ;
#207623=CARTESIAN_POINT ( 'NONE',  ( 1.998786363724443182, -0.5629491194198692483, -2.029361489363819882 ) ) ;
#207632=CARTESIAN_POINT ( 'NONE',  ( 2.602056794214495650, 1.574129494629309622, 1.567664267292529612 ) ) ;
#207634=CARTESIAN_POINT ( 'NONE',  ( 0.1005910224048736229, -2.206496634663042133, -0.04943112074598519229 ) ) ;
#207637=CARTESIAN_POINT ( 'NONE',  ( 4.492601031306558745, 1.923586649950057792, 0.3847822903023030428 ) ) ;
#207645=CARTESIAN_POINT ( 'NONE',  ( 3.392942708002244068, -2.044739723715986113, -0.5619712599038150236 ) ) ;
#207647=CARTESIAN_POINT ( 'NONE',  ( 5.172814640947125397, -2.034155943344346795, -0.7319064324283753864 ) ) ;
#207648=CARTESIAN_POINT ( 'NONE',  ( 3.684953445348177148, 1.336164438771630714, 1.267087564277062484 ) ) ;
#207649=CARTESIAN_POINT ( 'NONE',  ( 4.944546133779973651, -1.457238331152037825, 1.394083050251286870 ) ) ;
#207652=CARTESIAN_POINT ( 'NONE',  ( 6.597592293924691376, -1.739768381213904647, 0.05089061930978015791 ) ) ;
#207653=CARTESIAN_POINT ( 'NONE',  ( 6.827182134110234557, 2.482032550715262964, 2.096239902261677113 ) ) ;
#207658=CARTESIAN_POINT ( 'NONE',  ( 4.206063578812153203, -2.156103337031569200, 0.1562769059922017589 ) ) ;
#207659=CARTESIAN_POINT ( 'NONE',  ( 5.237657596305253627, -1.897407540178517316, -0.6818907625677357309 ) ) ;
#207661=CARTESIAN_POINT ( 'NONE',  ( 3.168983506954273999, -1.996715753333128118, -0.8287754370841573515 ) ) ;
#207663=CARTESIAN_POINT ( 'NONE',  ( 3.655507913172794332, 0.4821067936548150135, -1.911365640376050612 ) ) ;
#207665=CARTESIAN_POINT ( 'NONE',  ( 1.026927485578407406, 1.372003256358475864, -1.855264817478113226 ) ) ;
#207666=CARTESIAN_POINT ( 'NONE',  ( 2.425137330123087853, -0.003247232972201920167, 2.060967562036238210 ) ) ;
#207667=CARTESIAN_POINT ( 'NONE',  ( 5.161643714676827699, 0.9607356898342777063, 1.687723941809249117 ) ) ;
#207676=CARTESIAN_POINT ( 'NONE',  ( 2.292262453775519404, -0.9438808975747980945, 1.994871701834355804 ) ) ;
#207678=CARTESIAN_POINT ( 'NONE',  ( 6.596542563702321615, 1.939940506139478327, 0.2910815776849539627 ) ) ;
#207679=CARTESIAN_POINT ( 'NONE',  ( -0.1290005225502676156, 1.324981729379502537, -2.425680704180297464 ) ) ;
#207682=CARTESIAN_POINT ( 'NONE',  ( 0.1749903794560592474, 0.7218944060462629819, -2.038148089257747930 ) ) ;
#207684=CARTESIAN_POINT ( 'NONE',  ( 5.208873985248447802, -0.2666229848188906848, 1.821608446441948193 ) ) ;
#207686=CARTESIAN_POINT ( 'NONE',  ( 2.061468863205512925, 0.3533766173234990093, -2.030202010101101795 ) ) ;
#207691=CARTESIAN_POINT ( 'NONE',  ( 6.451439665316073935, -1.893653415279672902, 0.9546920624979161607 ) ) ;
#207694=CARTESIAN_POINT ( 'NONE',  ( 0.6200826401135750565, -1.101877700393244952, -1.741386573944928795 ) ) ;
#207696=CARTESIAN_POINT ( 'NONE',  ( 2.488518357381704238, 1.804271297518467820, 0.4556280478851971183 ) ) ;
#207697=CARTESIAN_POINT ( 'NONE',  ( 4.704558828624370470, 1.604442792107749760, 0.9031527321438773681 ) ) ;
#207704=CARTESIAN_POINT ( 'NONE',  ( 4.846401659255799466, 2.200796399388889935, 0.1645688927329121420 ) ) ;
#207705=CARTESIAN_POINT ( 'NONE',  ( 0.1753634416057497925, 0.0001173177735149660839, -2.144164757042037017 ) ) ;
#207707=CARTESIAN_POINT ( 'NONE',  ( 6.451413702892147661, -1.613775625804831693, 0.8233398690262339059 ) ) ;
#207708=CARTESIAN_POINT ( 'NONE',  ( -0.08279552664090458758, -1.841734517378278424, 0.8216794407479923734 ) ) ;
#207711=CARTESIAN_POINT ( 'NONE',  ( 5.936178161767468708, -1.066166440211462563, -1.587280745415058814 ) ) ;
#207713=CARTESIAN_POINT ( 'NONE',  ( 0.9009904985227291663, 1.526999960511504772, 1.080287613699250304 ) ) ;
#207714=CARTESIAN_POINT ( 'NONE',  ( 2.149625371984189126, 1.976669504256656218, -0.3981124878784659815 ) ) ;
#207716=CARTESIAN_POINT ( 'NONE',  ( 4.512399653719460169, -0.8998888299811370617, -1.904278430835882885 ) ) ;
#207720=CARTESIAN_POINT ( 'NONE',  ( 3.515882793631277536, -0.5824337298786783634, 1.934013565619496999 ) ) ;
#207723=CARTESIAN_POINT ( 'NONE',  ( 4.675171183009182663, 0.005162144975975196948, -2.161773191939574179 ) ) ;
#207728=CARTESIAN_POINT ( 'NONE',  ( 2.488948079679761172, 2.105553563057678712, 0.5292575070172370610 ) ) ;
#207731=CARTESIAN_POINT ( 'NONE',  ( 0.6261898170028465938, 0.1349980957352381883, 1.836376839866371569 ) ) ;
#207733=CARTESIAN_POINT ( 'NONE',  ( 1.716621854089026344, 2.046377219401524616, 0.7848826361863747714 ) ) ;
#207734=CARTESIAN_POINT ( 'NONE',  ( 6.883263157960364254, 2.038911835798001171, 2.358809022084580764 ) ) ;
#207735=CARTESIAN_POINT ( 'NONE',  ( 3.274574482517400575, -1.349127789868936222, 1.816123189252472958 ) ) ;
#207741=CARTESIAN_POINT ( 'NONE',  ( 4.604631121011967920, 1.368492104089440442, -1.122162792211104820 ) ) ;
#207743=CARTESIAN_POINT ( 'NONE',  ( 0.6046866811788155216, -0.7097959115549393738, -1.982883793842766362 ) ) ;
#207747=CARTESIAN_POINT ( 'NONE',  ( 6.398064575937244314, -0.9530261711272209890, -1.777004751544956962 ) ) ;
#207752=CARTESIAN_POINT ( 'NONE',  ( 5.119927267529915227, -1.001353885182048931, -1.579878405157906673 ) ) ;
#207753=CARTESIAN_POINT ( 'NONE',  ( 3.959880360806608213, -0.6057208360459276353, 1.979630382156400303 ) ) ;
#207761=CARTESIAN_POINT ( 'NONE',  ( 3.965250677406896962, 1.681448970545707855, 1.010551734412237446 ) ) ;
#207762=CARTESIAN_POINT ( 'NONE',  ( 1.528672481244568448, 1.986742605292156405, -0.3418812301651391605 ) ) ;
#207763=EDGE_CURVE ( 'NONE', #202900, #112905, #2922, .T. ) ;
#207765=CARTESIAN_POINT ( 'NONE',  ( 6.639320575229254118, 2.070803455257670844, 2.204946390281757207 ) ) ;
#207766=CARTESIAN_POINT ( 'NONE',  ( 0.6670070365902281972, 0.1896921041569209765, -1.860926112923621201 ) ) ;
#207768=CARTESIAN_POINT ( 'NONE',  ( 3.322524176979495980, -0.8198387518110359373, -1.838900561053190774 ) ) ;
#207770=CARTESIAN_POINT ( 'NONE',  ( 3.849298028564145380, 0.2572143275579537591, -2.101468238826177615 ) ) ;
#207772=CARTESIAN_POINT ( 'NONE',  ( 4.633297751427938316, 0.003287558298453730800, -2.070544812459538253 ) ) ;
#207774=CARTESIAN_POINT ( 'NONE',  ( 6.544877668737552945, -1.678188448499055685, -1.246566921223101865 ) ) ;
#207776=CARTESIAN_POINT ( 'NONE',  ( 5.069292194207453583, 0.1776299070984053985, -1.816928125296768393 ) ) ;
#207783=CARTESIAN_POINT ( 'NONE',  ( 6.604189988765333474, -0.8127675640051763573, 1.729262449380222222 ) ) ;
#207795=CARTESIAN_POINT ( 'NONE',  ( 0.1394461523057500818, 4.098109337479769465, -2.274588453029251500 ) ) ;
#207798=CARTESIAN_POINT ( 'NONE',  ( 2.184365610098043309, 1.138103218778206971, -1.607087707149345901 ) ) ;
#207799=CARTESIAN_POINT ( 'NONE',  ( 3.919546125582054508, -1.392558991000433011, -1.458545569310132350 ) ) ;
#207801=CARTESIAN_POINT ( 'NONE',  ( 6.827182134110200806, 2.035520418778674845, 2.394189263408800450 ) ) ;
#207802=CARTESIAN_POINT ( 'NONE',  ( 4.066501749483540706, -2.044453849244652233, -0.7895499924894524568 ) ) ;
#207804=CARTESIAN_POINT ( 'NONE',  ( 1.940333228260374021, 1.905070304733847752, 0.2851023952017122665 ) ) ;
#207807=CARTESIAN_POINT ( 'NONE',  ( 0.2333540202161220045, 5.723122673495201873, -2.639760918834464398 ) ) ;
#207814=ORIENTED_EDGE ( 'NONE', *, *, #7153, .F. ) ;
#207815=CARTESIAN_POINT ( 'NONE',  ( 5.741722636381445533, 1.839460222191912964, 0.08393339073512617876 ) ) ;
#207816=CARTESIAN_POINT ( 'NONE',  ( 2.860023507607223792, 0.7224298503675909977, -1.879176508647899535 ) ) ;
#207817=CARTESIAN_POINT ( 'NONE',  ( 4.288600692895239597, -2.201063653074202708, 0.6618141117178658606 ) ) ;
#207818=CARTESIAN_POINT ( 'NONE',  ( -0.1288028175206725467, 2.854926803129751001, -2.761885894952537779 ) ) ;
#207819=CARTESIAN_POINT ( 'NONE',  ( 3.344433574756133787, -1.832611177030788685, -0.3225857369167430821 ) ) ;
#207822=CARTESIAN_POINT ( 'NONE',  ( 6.416268857797894576, -1.911816439625917852, 0.05404522429636184067 ) ) ;
#207825=CARTESIAN_POINT ( 'NONE',  ( 5.495677747024089399, -2.090933975967598446, 0.001106539467419370270 ) ) ;
#207830=CARTESIAN_POINT ( 'NONE',  ( 6.164645834669005175, -1.214467819493704415, 1.225147371335724156 ) ) ;
#207833=CARTESIAN_POINT ( 'NONE',  ( 1.793227186479518398, 1.284509341651525638, -1.165198513391290103 ) ) ;
#207838=CARTESIAN_POINT ( 'NONE',  ( 5.313404054176891655, -1.830285002536722549, -1.167499077736388724 ) ) ;
#207839=CARTESIAN_POINT ( 'NONE',  ( 4.055160972438559774, -1.518969423100406946, -1.012540670841777013 ) ) ;
#207840=CARTESIAN_POINT ( 'NONE',  ( 2.184356868638567928, 1.133688150830698627, -1.600809071968431807 ) ) ;
#207845=CARTESIAN_POINT ( 'NONE',  ( 3.053504691927158898, -1.869126254513186591, 1.001442229663196182 ) ) ;
#207846=CARTESIAN_POINT ( 'NONE',  ( 6.827182134110224787, 2.015384445464900587, 2.492173930675382287 ) ) ;
#207849=CARTESIAN_POINT ( 'NONE',  ( 1.182579820358391931, 1.236233925375467058, -1.660450453320160058 ) ) ;
#207852=CARTESIAN_POINT ( 'NONE',  ( 3.317226741293349157, 1.750174726733638497, -1.367746370967915626 ) ) ;
#207854=CARTESIAN_POINT ( 'NONE',  ( 0.6164066528375180543, 0.1772060041554945342, 2.291936309153388862 ) ) ;
#207856=CARTESIAN_POINT ( 'NONE',  ( 0.4265131056294459433, -1.285834093136655643, 1.481649512794058543 ) ) ;
#207863=CARTESIAN_POINT ( 'NONE',  ( -0.2104748580754183807, 2.005809028216706924, -2.517884123765606663 ) ) ;
#207864=CARTESIAN_POINT ( 'NONE',  ( 2.537784596217841138, 0.8154259780687975745, -1.519840121599738803 ) ) ;
#207865=CARTESIAN_POINT ( 'NONE',  ( 0.9015777671340443611, -1.966303774932298021, 0.4465067697373495403 ) ) ;
#207866=CARTESIAN_POINT ( 'NONE',  ( 2.831036414133382806, 0.8244386821347724492, -2.145926533794308533 ) ) ;
#207867=CARTESIAN_POINT ( 'NONE',  ( 3.866728509311831985, -1.522874988181441180, 1.673262526929709670 ) ) ;
#207868=CARTESIAN_POINT ( 'NONE',  ( 5.215496775961459441, -0.3099510095366068696, 2.083004237123146307 ) ) ;
#207871=CARTESIAN_POINT ( 'NONE',  ( 3.954177229731909549, 0.6350985098286399122, 1.652046152411037694 ) ) ;
#207874=CARTESIAN_POINT ( 'NONE',  ( 6.614806897001766828, -0.1637801000826353548, 2.256214727502181994 ) ) ;
#207875=CARTESIAN_POINT ( 'NONE',  ( 5.912015133600425187, 1.233162958052456348, -1.367321061651972869 ) ) ;
#207878=CARTESIAN_POINT ( 'NONE',  ( 4.962908505822442251, 0.2168217322565079985, -2.180687389885840322 ) ) ;
#207881=CARTESIAN_POINT ( 'NONE',  ( 6.092251258522619395, 1.023830597077223903, -1.799436568697235783 ) ) ;
#207882=CARTESIAN_POINT ( 'NONE',  ( 0.5148617154710420918, 0.1531739628206352510, 2.010800830040265996 ) ) ;
#207884=CARTESIAN_POINT ( 'NONE',  ( 2.719263968888342653, -0.1887435353777958125, 1.917229668948018162 ) ) ;
#207887=CARTESIAN_POINT ( 'NONE',  ( -0.01689291694152022724, -1.444339507245323118, 1.687895485215410885 ) ) ;
#207896=CARTESIAN_POINT ( 'NONE',  ( 0.7659737006216191801, -1.952758744216346765, 0.1886366088557633325 ) ) ;
#207899=CARTESIAN_POINT ( 'NONE',  ( 5.353941776413853937, -0.7077614321437855072, 1.829919609802006741 ) ) ;
#207904=CARTESIAN_POINT ( 'NONE',  ( 6.579002408576895000, -0.1006694238701970334, -2.159482418181729813 ) ) ;
#207908=CARTESIAN_POINT ( 'NONE',  ( 6.837195077073701555, -1.761838062178729070, 0.8845485525767071699 ) ) ;
#207909=CARTESIAN_POINT ( 'NONE',  ( 6.204387268089465834, -1.258339971413184433, -1.193046581750532464 ) ) ;
#207911=CARTESIAN_POINT ( 'NONE',  ( 3.421585747727782678, -1.306972202059282218, -1.759028276249123168 ) ) ;
#207912=CARTESIAN_POINT ( 'NONE',  ( 4.190657675959572614, -2.281913287836007331, -0.3425691479843806508 ) ) ;
#207913=CARTESIAN_POINT ( 'NONE',  ( 5.782513925583750769, -2.009559558911724775, -0.4558285042701361589 ) ) ;
#207914=CARTESIAN_POINT ( 'NONE',  ( 2.027192386733965179, -1.268372964689370663, -1.470586975900304516 ) ) ;
#207918=CARTESIAN_POINT ( 'NONE',  ( 4.834296457332984076, -1.136628438424293508, -1.790084250976264002 ) ) ;
#207920=CARTESIAN_POINT ( 'NONE',  ( 3.744767666119628746, 2.000857235306313875, -0.2496062519145719194 ) ) ;
#207924=CARTESIAN_POINT ( 'NONE',  ( 0.2404813148422607627, 0.3085585699703840556, 1.799268721412583316 ) ) ;
#207929=CARTESIAN_POINT ( 'NONE',  ( 5.629779042149522184, -1.305697561153400965, -1.594503516446880154 ) ) ;
#207934=CARTESIAN_POINT ( 'NONE',  ( 4.793620647492384812, 1.883690600511141566, -0.7290150168693364519 ) ) ;
#207941=CARTESIAN_POINT ( 'NONE',  ( 4.733308493599470701, -1.885100903509504544, 0.8332785242166717010 ) ) ;
#207942=CARTESIAN_POINT ( 'NONE',  ( 2.777970385693105726, 1.728001979019553103, -1.038993764437286416 ) ) ;
#207949=CARTESIAN_POINT ( 'NONE',  ( 3.286482353612128815, -1.943773746517188039, 0.5350062169211177165 ) ) ;
#207950=CARTESIAN_POINT ( 'NONE',  ( 2.501689010688646242, -0.7045654096689784041, -1.701190496055771550 ) ) ;
#207951=CARTESIAN_POINT ( 'NONE',  ( 0.9092882892361430214, 1.744143012382966207, -1.511207573902007884 ) ) ;
#207953=CARTESIAN_POINT ( 'NONE',  ( 3.901784996602038813, -0.6316019492740264640, 2.067237329103743804 ) ) ;
#207957=CARTESIAN_POINT ( 'NONE',  ( 1.533845512228737551, 0.9248708299973290581, -1.625957014461040906 ) ) ;
#207958=CARTESIAN_POINT ( 'NONE',  ( 5.629747345311447937, -1.250075164085572954, -1.524477324586423377 ) ) ;
#207962=CARTESIAN_POINT ( 'NONE',  ( 0.9091299924109221831, 1.668792687453458878, -1.444214864661397035 ) ) ;
#207963=DIRECTION ( 'NONE',  ( 1.039099362110107450E-15, 1.000000000000000000, -4.583713267641621330E-32 ) ) ;
#207966=CARTESIAN_POINT ( 'NONE',  ( 6.539320575229278454, 0.5749733277502915296, 2.156147827957733742 ) ) ;
#207967=CARTESIAN_POINT ( 'NONE',  ( 5.295764336479223289, -0.7102129355434207980, 1.839261741220117097 ) ) ;
#207968=CARTESIAN_POINT ( 'NONE',  ( 5.549573066657292664, -1.816037693736268333, -1.423817124750816232 ) ) ;
#207969=CARTESIAN_POINT ( 'NONE',  ( 6.232830220009587308, -1.767433141015135822, -0.5829711297899267120 ) ) ;
#207970=CARTESIAN_POINT ( 'NONE',  ( 3.608308625203029862, 2.062741128266020851, 0.004805803398660184710 ) ) ;
#207977=CARTESIAN_POINT ( 'NONE',  ( 5.811019572999191141, -1.715256576162796032, 1.331060940585542030 ) ) ;
#207980=CARTESIAN_POINT ( 'NONE',  ( 4.212339636135824961, 1.685202893791247769, 0.7422218904534692019 ) ) ;
#207983=CARTESIAN_POINT ( 'NONE',  ( 6.286699343557897279, 1.907799665397521105, -1.078441415684105120 ) ) ;
#207985=CARTESIAN_POINT ( 'NONE',  ( 0.2107632190684857465, -0.9678151086435597961, -2.042474306115627414 ) ) ;
#207993=CARTESIAN_POINT ( 'NONE',  ( 1.023854850961497309, 1.058662087540670704, -1.418139054142423472 ) ) ;
#207994=CARTESIAN_POINT ( 'NONE',  ( 5.549481842319204716, -1.818904971374595503, 0.8629315129762565872 ) ) ;
#207996=CARTESIAN_POINT ( 'NONE',  ( 4.120224405726905736, -1.080582774747363306, -1.807441255628852828 ) ) ;
#207997=CARTESIAN_POINT ( 'NONE',  ( 3.022943291168778579, -1.688106736905025995, 0.9054777632113325536 ) ) ;
#207999=CARTESIAN_POINT ( 'NONE',  ( 4.650814871655007288, -0.4294639348428323511, -1.921992245654633447 ) ) ;
#208000=CARTESIAN_POINT ( 'NONE',  ( 5.484630696634174463, -1.278254659592213516, 1.563874148425943078 ) ) ;
#208001=CARTESIAN_POINT ( 'NONE',  ( 2.166681600665042229, -1.709288833360942617, -0.7604731621856930524 ) ) ;
#208002=CARTESIAN_POINT ( 'NONE',  ( 4.986778444009251743, -0.2158907008250054438, -1.711239743519934242 ) ) ;
#208003=CARTESIAN_POINT ( 'NONE',  ( 1.441514601552947417, -1.799640695080907182, 0.6472408003148700795 ) ) ;
#208005=CARTESIAN_POINT ( 'NONE',  ( 2.526237079854487089, -1.271617311931704686, -1.803507373242494438 ) ) ;
#208009=CARTESIAN_POINT ( 'NONE',  ( 6.760214184729610665, -1.961454122871961747, 0.04698431645466792650 ) ) ;
#208015=CARTESIAN_POINT ( 'NONE',  ( 1.820844063133007396, -1.465591517063179028, 1.462601037713284535 ) ) ;
#208020=CARTESIAN_POINT ( 'NONE',  ( 0.2936253167127310659, 1.883648094304795961, -0.7291253699766816476 ) ) ;
#208025=CARTESIAN_POINT ( 'NONE',  ( 5.009138659175729202, 2.010518709310470609, 0.1511151588593287465 ) ) ;
#208026=CARTESIAN_POINT ( 'NONE',  ( 4.575340585108073732, 1.423666108326137048, 1.282088096497513652 ) ) ;
#208027=CARTESIAN_POINT ( 'NONE',  ( 2.876726420669137863, -0.1638259704515396820, -2.185508879517850112 ) ) ;
#208030=CARTESIAN_POINT ( 'NONE',  ( 5.642843092333371224, 1.941422931094261450, 0.5326616679640855390 ) ) ;
#208031=CARTESIAN_POINT ( 'NONE',  ( 1.423922367354793606, -1.897583212610975734, 0.2371896777705190806 ) ) ;
#208034=CARTESIAN_POINT ( 'NONE',  ( 6.609000000000050612, -6.653734691735092887E-05, 2.100160721423645960 ) ) ;
#208036=CARTESIAN_POINT ( 'NONE',  ( 3.737900851971903915, 2.080878125540788215, 0.2026709130291924343 ) ) ;
#208038=CARTESIAN_POINT ( 'NONE',  ( 1.781837903662389477, -0.9264376740152606704, 1.454631767934653208 ) ) ;
#208042=CARTESIAN_POINT ( 'NONE',  ( 0.3792546940144908563, -0.1001052471676349837, 1.959448305358338693 ) ) ;
#208048=CARTESIAN_POINT ( 'NONE',  ( 3.000440247697288676, -1.785030861869114638, -0.3072999389705335926 ) ) ;
#208049=ORIENTED_EDGE ( 'NONE', *, *, #102848, .F. ) ;
#208052=CARTESIAN_POINT ( 'NONE',  ( 3.369578772036628145, 0.4373610723380080834, -1.757749666579068171 ) ) ;
#208056=CARTESIAN_POINT ( 'NONE',  ( 4.387043322907993925, 0.09000376980121749249, 1.858987348747977331 ) ) ;
#208057=CARTESIAN_POINT ( 'NONE',  ( 1.739701290322914540, 1.910364143156467298, -0.1427236045144583687 ) ) ;
#208058=CARTESIAN_POINT ( 'NONE',  ( 0.4986989427119004059, 1.520756344202650601, -1.009667857431728599 ) ) ;
#208067=CARTESIAN_POINT ( 'NONE',  ( 6.016450702237627901, 0.7947307017554460229, 1.802146183335861629 ) ) ;
#208070=CARTESIAN_POINT ( 'NONE',  ( 0.4981332788140432899, -0.7063641614380437028, -1.967824727186429978 ) ) ;
#208072=CARTESIAN_POINT ( 'NONE',  ( 4.981433139801599630, 1.797578344525651906, -0.6930591852608753989 ) ) ;
#208074=CARTESIAN_POINT ( 'NONE',  ( 1.465546361252961782, 1.799214786004127209, -0.3081908958329632742 ) ) ;
#208075=CARTESIAN_POINT ( 'NONE',  ( 2.561379550486083012, -1.920685204893451292, -1.086737900330703166 ) ) ;
#208077=CARTESIAN_POINT ( 'NONE',  ( 0.7735182334044669039, 0.3705173918269571431, -1.875978362188877036 ) ) ;
#208079=CARTESIAN_POINT ( 'NONE',  ( 0.5023235590321275534, 1.964037083787707028, 0.1483792944171925254 ) ) ;
#208080=CARTESIAN_POINT ( 'NONE',  ( 2.419391519165543070, -1.120004824200554916, -1.586377984052749879 ) ) ;
#208082=CARTESIAN_POINT ( 'NONE',  ( 1.300157425512000087, -1.823841169980220167, 0.8594962466553013325 ) ) ;
#208084=CARTESIAN_POINT ( 'NONE',  ( 6.121894333209238148, 1.833584433263518942, -0.3168336897404684382 ) ) ;
#208090=CARTESIAN_POINT ( 'NONE',  ( 2.208753784402537335, 1.959192758111829136, 0.9821998110004714899 ) ) ;
#208095=CARTESIAN_POINT ( 'NONE',  ( 2.473051018021198200, 0.08991741065280876855, -1.823594477012622228 ) ) ;
#208101=CARTESIAN_POINT ( 'NONE',  ( 0.5219392174641559468, -1.029590632097213687, -1.628125521969860712 ) ) ;
#208102=CARTESIAN_POINT ( 'NONE',  ( 6.086763564210844635, 1.889667650816441391, 0.5265613530214610094 ) ) ;
#208107=CARTESIAN_POINT ( 'NONE',  ( 5.513277522340928272, -2.138352208816508782, 0.4792397250529822905 ) ) ;
#208108=CARTESIAN_POINT ( 'NONE',  ( 3.625891163443736520, 2.020865133175090644, -0.4488579359705275329 ) ) ;
#208113=CARTESIAN_POINT ( 'NONE',  ( 4.606216143772843274, -0.1140155944862955434, 2.295953707746749117 ) ) ;
#208117=CARTESIAN_POINT ( 'NONE',  ( 0.2876181914312899157, 1.702867465475272901, 1.534690983289775712 ) ) ;
#208118=CARTESIAN_POINT ( 'NONE',  ( 6.620655732516611103, 3.701195159515461075, 2.440764268381501179 ) ) ;
#208120=CARTESIAN_POINT ( 'NONE',  ( 5.173749199105643903, -1.077276334994947460, 1.615559063095718839 ) ) ;
#208123=CARTESIAN_POINT ( 'NONE',  ( 5.519756697582541172, -0.4584384640409416289, 1.856529252577573619 ) ) ;
#208124=CARTESIAN_POINT ( 'NONE',  ( 6.053657651994457822, 0.4959367165196375549, -1.651908409946404976 ) ) ;
#208125=CARTESIAN_POINT ( 'NONE',  ( 5.225796113160614986, 0.8128206588041907432, -1.845625551132886288 ) ) ;
#208129=CARTESIAN_POINT ( 'NONE',  ( 1.957086829145736173, 0.3561595965777020756, -2.059905414565963433 ) ) ;
#208130=CARTESIAN_POINT ( 'NONE',  ( 6.714108650864204719, -0.8368934294483711955, -1.559304158387794015 ) ) ;
#208131=CARTESIAN_POINT ( 'NONE',  ( 5.625625018759272677, 0.3960990390993284205, 1.976956468877195894 ) ) ;
#208134=CARTESIAN_POINT ( 'NONE',  ( 2.713130565535960770, -0.2235823006870632790, 2.281328536464954038 ) ) ;
#208135=CARTESIAN_POINT ( 'NONE',  ( 1.745671189342316687, 0.5440799701325367277, 1.653152385070497887 ) ) ;
#208137=CARTESIAN_POINT ( 'NONE',  ( 1.932526292592825046, 0.8863411937694037901, 1.489983018702551787 ) ) ;
#208139=CARTESIAN_POINT ( 'NONE',  ( 1.556854020514925496, 1.524047875013130104, -1.067797667942985917 ) ) ;
#208140=CARTESIAN_POINT ( 'NONE',  ( 2.963510081828163223, 1.832883945819727689, 1.163594247970006990 ) ) ;
#208141=CARTESIAN_POINT ( 'NONE',  ( 3.081267818761534549, 1.592661989535900657, 1.236799713577160231 ) ) ;
#208142=CARTESIAN_POINT ( 'NONE',  ( 4.906250000000003553, 1.895863743163974213, -0.7852924748302423374 ) ) ;
#208145=CARTESIAN_POINT ( 'NONE',  ( 6.568979851886898480, -1.762530817088540758, -0.7781539781668064260 ) ) ;
#208147=CARTESIAN_POINT ( 'NONE',  ( 2.988771237642441569, -1.320003323290209751, 1.786578734224959497 ) ) ;
#208149=CARTESIAN_POINT ( 'NONE',  ( -0.2110808730067144090, 0.7535804146166940054, -1.881771259391984197 ) ) ;
#208154=CARTESIAN_POINT ( 'NONE',  ( 6.240512348869785342, 1.279970183950808860, -1.815422973897186543 ) ) ;
#208155=CARTESIAN_POINT ( 'NONE',  ( 4.299235682465595509, -1.708000122724560477, 0.9650500775852040025 ) ) ;
#208159=CARTESIAN_POINT ( 'NONE',  ( 5.571622904855764169, 2.182566619097675797, -0.5956038432519733528 ) ) ;
#208160=CARTESIAN_POINT ( 'NONE',  ( 2.664570663672768180, -0.7871131050594852852, -1.906781320289064885 ) ) ;
#208165=CARTESIAN_POINT ( 'NONE',  ( 3.936663633328242096, 0.2718032920513112627, 1.850550731861917653 ) ) ;
#208166=CARTESIAN_POINT ( 'NONE',  ( 2.302961303058923992, 1.131868135402936737, -1.313931383173136513 ) ) ;
#208167=CARTESIAN_POINT ( 'NONE',  ( 5.935146830689759234, -1.586316731616247200, -1.512381816529739353 ) ) ;
#208168=CARTESIAN_POINT ( 'NONE',  ( 1.167327668269029228, -1.995579438226593894, -0.9423882379527288577 ) ) ;
#208169=CARTESIAN_POINT ( 'NONE',  ( 5.226486033959851341, 0.1448775283907685063, 1.936603901228886926 ) ) ;
#208171=CARTESIAN_POINT ( 'NONE',  ( 0.000000000000000000, 0.000000000000000000, -1.999999999999999556 ) ) ;
#208172=CARTESIAN_POINT ( 'NONE',  ( 1.002577532868035526, -1.966644254196001196, 0.4445047019146358691 ) ) ;
#208173=CARTESIAN_POINT ( 'NONE',  ( -0.2104748580754166598, -0.006608320950483163522, -2.103482951484026753 ) ) ;
#208175=CARTESIAN_POINT ( 'NONE',  ( 6.416638760586134360, -1.319225726833603840, -1.525046029381103452 ) ) ;
#208180=CARTESIAN_POINT ( 'NONE',  ( 4.652862234063231739, -1.464609733205827879, 1.089778014065109657 ) ) ;
#208181=CARTESIAN_POINT ( 'NONE',  ( 2.151677955860908487, -1.772288797910109404, -1.314638326115322053 ) ) ;
#208186=CARTESIAN_POINT ( 'NONE',  ( 0.9846354891296082990, -1.278160710921724341, 1.563951078967614094 ) ) ;
#208190=CARTESIAN_POINT ( 'NONE',  ( 3.027998222813840901, 0.9912708380838133326, 1.574746995948882455 ) ) ;
#208192=CARTESIAN_POINT ( 'NONE',  ( 6.486953984781112403, -2.015912550161761629, 0.05229459904129707404 ) ) ;
#208196=CARTESIAN_POINT ( 'NONE',  ( 4.230939532379584200, 0.09184734775685021724, 1.823503176236190626 ) ) ;
#208200=CARTESIAN_POINT ( 'NONE',  ( 6.468125021464292246, 1.674632898861495134, 1.122323893169609565 ) ) ;
#208201=CARTESIAN_POINT ( 'NONE',  ( 5.437399513225577685, 0.7426265630364609072, -1.684910612069365321 ) ) ;
#208202=CARTESIAN_POINT ( 'NONE',  ( 4.424672798056923817, 1.421823072290354872, -1.817590327873227052 ) ) ;
#208205=CARTESIAN_POINT ( 'NONE',  ( 0.7903930413690943846, -2.044920356511644499, -0.2547782948326294816 ) ) ;
#208207=CARTESIAN_POINT ( 'NONE',  ( 1.962350597898457671, -1.776395552165145997, -0.7852436748517297449 ) ) ;
#208208=CARTESIAN_POINT ( 'NONE',  ( 6.186922437512073714, -1.269050685324083050, -1.916131536371464383 ) ) ;
#208212=CARTESIAN_POINT ( 'NONE',  ( 4.205816867194319464, -1.865656749788859647, 0.1373567816406878750 ) ) ;
#208214=CARTESIAN_POINT ( 'NONE',  ( 2.408343312057196872, -1.907530749141531423, -0.1368029246449145864 ) ) ;
#208216=CARTESIAN_POINT ( 'NONE',  ( 4.213639274598267370, -0.3785452818781535611, 2.174016619501429215 ) ) ;
#208221=CARTESIAN_POINT ( 'NONE',  ( 2.143765197515819843, 0.7580581125649475949, -1.819971111534921970 ) ) ;
#208222=CARTESIAN_POINT ( 'NONE',  ( 2.503307172793560298, 1.853534942699623045, -1.374368423928104876 ) ) ;
#208223=CARTESIAN_POINT ( 'NONE',  ( 2.506241959165692812, 1.961374882610424919, 0.05109738790698423877 ) ) ;
#208225=CARTESIAN_POINT ( 'NONE',  ( 6.754736851877535031, -0.5442653458712517489, -1.989433905422931748 ) ) ;
#208227=CARTESIAN_POINT ( 'NONE',  ( 4.030482632556767975, 0.5424685788828055300, 1.942097399793737633 ) ) ;
#208230=CARTESIAN_POINT ( 'NONE',  ( 4.751185534883737738, 0.1928377863454934504, -2.007255887737584121 ) ) ;
#208235=CARTESIAN_POINT ( 'NONE',  ( 1.938562956190786002, -1.164097522067691903, 1.832441342696682574 ) ) ;
#208238=CARTESIAN_POINT ( 'NONE',  ( 2.969827553264007047, 0.9974664638083343693, 1.582205488144486250 ) ) ;
#208239=CARTESIAN_POINT ( 'NONE',  ( 6.362596528949501895, -1.533591692085239266, 1.523617273982772247 ) ) ;
#208242=CARTESIAN_POINT ( 'NONE',  ( 6.827182134110203471, 1.269052739965634391, 2.024653661457261222 ) ) ;
#208244=CARTESIAN_POINT ( 'NONE',  ( 3.633378786761193968, -0.1378984027537045187, 1.907353237798288470 ) ) ;
#208245=CARTESIAN_POINT ( 'NONE',  ( 4.188192146485575584, -1.750654529572701179, -0.2590412592250490587 ) ) ;
#208246=CARTESIAN_POINT ( 'NONE',  ( 2.156764536687346467, 0.4205103164258168769, 1.865301821287323136 ) ) ;
#208249=CARTESIAN_POINT ( 'NONE',  ( 6.556256410252866651, -1.173993033552203968, 1.514159254448317782 ) ) ;
#208251=CARTESIAN_POINT ( 'NONE',  ( 1.311079954825690619, -1.633285661836245906, 1.272233187909928454 ) ) ;
#208253=CARTESIAN_POINT ( 'NONE',  ( 6.526239545637954720, 1.075124705556152138, -1.530631868311462362 ) ) ;
#208254=CARTESIAN_POINT ( 'NONE',  ( 1.629252094361890890, -1.719607636260962025, 0.6136192449261099746 ) ) ;
#208255=CARTESIAN_POINT ( 'NONE',  ( 5.496761087669068679, -0.5331231007881258588, -2.141394884921154151 ) ) ;
#208259=CARTESIAN_POINT ( 'NONE',  ( 3.139185485588998237, -0.1492200975972737820, -2.057319831125117737 ) ) ;
#208266=CARTESIAN_POINT ( 'NONE',  ( 4.861816338261779613, -0.5554421346023461492, 1.994381909410049669 ) ) ;
#208268=CARTESIAN_POINT ( 'NONE',  ( 3.005316911853897821, 1.824354345256746557, 1.159134172154026032 ) ) ;
#208270=CARTESIAN_POINT ( 'NONE',  ( 2.754561962923445684, 2.004688795240500365, 0.2448751400806712664 ) ) ;
#208271=CARTESIAN_POINT ( 'NONE',  ( 6.620655732516647518, 3.684600858287550906, 2.687722323901103660 ) ) ;
#208276=CARTESIAN_POINT ( 'NONE',  ( 1.147673126774436225, 1.985868168208399842, -0.3494872464938902357 ) ) ;
#208278=CARTESIAN_POINT ( 'NONE',  ( 5.689076433642084041, 1.658752129386225516, 1.432425853890168188 ) ) ;
#208280=CARTESIAN_POINT ( 'NONE',  ( 4.886922752366290368, -1.802716094696995786, -0.6387714794457154399 ) ) ;
#208284=CARTESIAN_POINT ( 'NONE',  ( 3.708611378246814638, 1.915606880664010747, 0.6298579873919087913 ) ) ;
#208286=CARTESIAN_POINT ( 'NONE',  ( 5.842733193948632220, 0.3409603658401075821, 1.690541223788865510 ) ) ;
#208290=CARTESIAN_POINT ( 'NONE',  ( 4.305816765424046011, -1.865681898550693107, 0.1353468896250972775 ) ) ;
#208292=CARTESIAN_POINT ( 'NONE',  ( 1.217730340897508645, 0.4076058164220326407, -2.029561569317724690 ) ) ;
#208296=CARTESIAN_POINT ( 'NONE',  ( 6.375650462676996533, 0.3020505593925585375, -1.785944618546008833 ) ) ;
#208299=CARTESIAN_POINT ( 'NONE',  ( -0.07068620461728526705, -1.560437159073333468, -1.276799021846956705 ) ) ;
#208301=CARTESIAN_POINT ( 'NONE',  ( 0.5096461351858303512, -0.6515609501748579335, 1.690550641884549954 ) ) ;
#208306=CARTESIAN_POINT ( 'NONE',  ( 0.2562055958934654210, -1.961350414083770977, -0.05204156388862594962 ) ) ;
#208308=CARTESIAN_POINT ( 'NONE',  ( 5.044510182127093678, -1.384340171167136369, 1.324308159167127075 ) ) ;
#208316=CARTESIAN_POINT ( 'NONE',  ( 2.342841879718413622, 0.4729757327756217156, 2.109170662781891359 ) ) ;
#208319=CARTESIAN_POINT ( 'NONE',  ( 0.1938080739139167730, 1.976361990896974508, -0.7691651810952588875 ) ) ;
#208320=CARTESIAN_POINT ( 'NONE',  ( 4.366094929315432083, 0.8608494910617261464, 1.609850404305966265 ) ) ;
#208322=CARTESIAN_POINT ( 'NONE',  ( 1.335163258876404857, -1.783904897583366012, 0.8392522581757311251 ) ) ;
#208323=CARTESIAN_POINT ( 'NONE',  ( 3.304848191199673213, -0.3775801424153284458, -1.874573493127674961 ) ) ;
#208326=CARTESIAN_POINT ( 'NONE',  ( 4.299236425489592506, -1.714783525531939690, 0.9686585690476202659 ) ) ;
#208328=CARTESIAN_POINT ( 'NONE',  ( 5.583525073002030048, -0.8696438758921558598, 1.736526053206193243 ) ) ;
#208332=CARTESIAN_POINT ( 'NONE',  ( 6.416280414004661203, -2.120105685773795212, 0.05337830808049835035 ) ) ;
#208334=CARTESIAN_POINT ( 'NONE',  ( 4.160738352132353768, 0.5130957772990808463, 1.842076966104645663 ) ) ;
#208335=ORIENTED_EDGE ( 'NONE', *, *, #161090, .T. ) ;
#208340=CARTESIAN_POINT ( 'NONE',  ( 5.479157358542966705, -1.820838119324312165, -0.8587918944957111389 ) ) ;
#208342=CARTESIAN_POINT ( 'NONE',  ( 6.674438497507635404, -1.118711561685633349, 1.443368817030561635 ) ) ;
#208343=CARTESIAN_POINT ( 'NONE',  ( 2.242711981562468093, -2.029969483702593003, -0.4061203719310027549 ) ) ;
#208347=CARTESIAN_POINT ( 'NONE',  ( 6.772336237553374438, -1.148929780121176414, 1.476827877338216854 ) ) ;
#208349=SURFACE_STYLE_FILL_AREA ( #9097 ) ;
#208355=CARTESIAN_POINT ( 'NONE',  ( 4.430095426116970714, -1.344173880920132458, -1.095666204706043700 ) ) ;
#208359=CARTESIAN_POINT ( 'NONE',  ( 2.325130699016836555, -1.891071737562114219, -0.8429460452448679364 ) ) ;
#208360=CARTESIAN_POINT ( 'NONE',  ( 3.743865479105834559, 2.100983596406953424, -0.2614307623071217557 ) ) ;
#208363=CARTESIAN_POINT ( 'NONE',  ( 2.237097273892864724, -0.09148514208244534762, -1.967424487969974711 ) ) ;
#208368=CARTESIAN_POINT ( 'NONE',  ( 3.539304732165698741, -1.735471681261467669, -1.497634786905965187 ) ) ;
#208369=CARTESIAN_POINT ( 'NONE',  ( 0.3986991128735201673, 1.519733473351183362, -1.011397189243423700 ) ) ;
#208373=CARTESIAN_POINT ( 'NONE',  ( 1.564699064445768784, 0.6353654490140858702, 1.910354371721780797 ) ) ;
#208374=CARTESIAN_POINT ( 'NONE',  ( 2.395295693335119935, -1.754585731169123752, 0.8775363634117984146 ) ) ;
#208378=CARTESIAN_POINT ( 'NONE',  ( 4.874988757033254849, 1.950858131582337007, -0.7520741601412093136 ) ) ;
#208379=CARTESIAN_POINT ( 'NONE',  ( 3.643183530381717716, -1.339777920602200467, -1.156514101391445948 ) ) ;
#208382=CARTESIAN_POINT ( 'NONE',  ( 6.298803545911215274, 1.902247386433516541, 1.278772944020603930 ) ) ;
#208383=CARTESIAN_POINT ( 'NONE',  ( 5.244012475127576955, 0.5104456934865635453, 1.663790013937071599 ) ) ;
#208385=CARTESIAN_POINT ( 'NONE',  ( 6.486976479784771321, -2.298278054978039275, 0.05155775693151467415 ) ) ;
#208386=CARTESIAN_POINT ( 'NONE',  ( 5.009033543107539899, 1.729337909971711662, 0.1259922892337256017 ) ) ;
#208387=CARTESIAN_POINT ( 'NONE',  ( 5.389208567375425751, 0.1545246996936377182, 2.165725388718000133 ) ) ;
#208389=CARTESIAN_POINT ( 'NONE',  ( 6.456263137377813877, -1.236968576560824040, 1.593241027169020052 ) ) ;
#208390=CARTESIAN_POINT ( 'NONE',  ( 4.906250000000003553, 1.895863743163974213, -0.7852924748302423374 ) ) ;
#208392=CARTESIAN_POINT ( 'NONE',  ( 4.665017848976360071, -1.720483299173672043, -0.8667214970639931515 ) ) ;
#208394=CARTESIAN_POINT ( 'NONE',  ( 0.4521970297205242240, -1.575145348204033180, -1.566492488853583387 ) ) ;
#208395=EDGE_LOOP ( 'NONE', ( #55923, #39345 ) ) ;
#208399=CARTESIAN_POINT ( 'NONE',  ( 2.104415045828517350, -0.9466870704337572162, 2.009588771043930411 ) ) ;
#208404=CARTESIAN_POINT ( 'NONE',  ( 0.8267963299631932994, 0.8146243292815741333, -1.844710905833810255 ) ) ;
#208406=CARTESIAN_POINT ( 'NONE',  ( 5.951645758832087907, 1.559603009536973284, 1.349993227703372156 ) ) ;
#208411=CARTESIAN_POINT ( 'NONE',  ( 0.7019891895669374549, -0.5885738721268447549, -1.669159149975569578 ) ) ;
#208412=CARTESIAN_POINT ( 'NONE',  ( 6.100242454504600786, -0.2022020391262440986, 1.722246827497366795 ) ) ;
#208413=CARTESIAN_POINT ( 'NONE',  ( 5.864775363713938816, 0.1190308195875185160, -1.736441914165016476 ) ) ;
#208414=CARTESIAN_POINT ( 'NONE',  ( 3.210744404368763405, 2.073164229931067304, 0.9784878017504093917 ) ) ;
#208416=CARTESIAN_POINT ( 'NONE',  ( 2.624749632297512569, -1.717891791495285592, 0.6627527109525217508 ) ) ;
#208419=CARTESIAN_POINT ( 'NONE',  ( 2.590611583786633254, -0.3098195481324728107, -1.798931244660670448 ) ) ;
#208420=CARTESIAN_POINT ( 'NONE',  ( 3.305314717767214638, 1.277042846462652204, -1.560500556308255238 ) ) ;
#208423=CARTESIAN_POINT ( 'NONE',  ( 5.192451847192011805, -2.089709803398311028, -0.2606072588380181076 ) ) ;
#208426=CARTESIAN_POINT ( 'NONE',  ( 2.119664376568120012, 0.3561266789769075292, -2.039353370234835872 ) ) ;
#208429=CARTESIAN_POINT ( 'NONE',  ( 4.863993733624056404, 0.6645719631460760279, -2.013739200842738608 ) ) ;
#208430=CARTESIAN_POINT ( 'NONE',  ( 0.3988885142760539293, 1.602443225120395720, -1.069099046168849876 ) ) ;
#208437=CARTESIAN_POINT ( 'NONE',  ( 6.381110825713084189, -1.939362502171553482, -0.8581636585355473246 ) ) ;
#208438=CARTESIAN_POINT ( 'NONE',  ( 2.063634109657853433, 0.3607628843028657939, -2.074664996798830874 ) ) ;
#208441=CARTESIAN_POINT ( 'NONE',  ( 6.051566885458855793, 1.408179756913958913, 1.216655509429155124 ) ) ;
#208446=CARTESIAN_POINT ( 'NONE',  ( 0.2992908618118708675, -0.2657624787030036240, -2.103842954668332599 ) ) ;
#208449=CARTESIAN_POINT ( 'NONE',  ( 2.699599903323801620, -1.451799986561516764, -1.319707477925702310 ) ) ;
#208450=CARTESIAN_POINT ( 'NONE',  ( 1.288190726105652217, -0.9714702286227733241, 1.931199087792371261 ) ) ;
#208455=CARTESIAN_POINT ( 'NONE',  ( 2.589492015636893907, -1.735658606974595619, -0.1281804514613407997 ) ) ;
#208459=CARTESIAN_POINT ( 'NONE',  ( 2.302111043707856020, -1.802142186715177674, 0.9039695891032775155 ) ) ;
#208460=FACE_OUTER_BOUND ( 'NONE', #87979, .T. ) ;
#208462=CARTESIAN_POINT ( 'NONE',  ( 2.377750047251852017, 1.211369778508808448, 1.555330764497768303 ) ) ;
#208463=CARTESIAN_POINT ( 'NONE',  ( 6.064708884584704585, 0.6063723501847050334, 1.813766235492550560 ) ) ;
#208468=CARTESIAN_POINT ( 'NONE',  ( 1.225266875139136458, 1.782313340379863442, 0.9499306202595361182 ) ) ;
#208470=CARTESIAN_POINT ( 'NONE',  ( 6.264718444480717352, -1.637942392629457178, 1.625721277839597745 ) ) ;
#208471=CARTESIAN_POINT ( 'NONE',  ( 6.391066755906244623, 0.1909826923555627554, 1.952524381009380861 ) ) ;
#208472=CARTESIAN_POINT ( 'NONE',  ( 2.992962298452767289, 0.2353761085502041883, 1.947492218917420637 ) ) ;
#208474=CARTESIAN_POINT ( 'NONE',  ( 0.7213275451133926985, 1.987047012402185731, 0.3419330716275259530 ) ) ;
#208476=CARTESIAN_POINT ( 'NONE',  ( 1.534521455381025801, 0.6695800964386169341, 2.008721144947374526 ) ) ;
#208479=CARTESIAN_POINT ( 'NONE',  ( 1.622747808203903963, -1.734053015003593101, 0.6191010992530541213 ) ) ;
#208482=CARTESIAN_POINT ( 'NONE',  ( 2.654661980655496301, 2.105093816413053709, 0.2552270188876659129 ) ) ;
#208486=CARTESIAN_POINT ( 'NONE',  ( 2.688805810584052658, -0.3489404079633807165, -2.030846992095108217 ) ) ;
#208488=CARTESIAN_POINT ( 'NONE',  ( 1.259045258496578557, 1.813921241667546758, -0.3151448728593714277 ) ) ;
#208493=CARTESIAN_POINT ( 'NONE',  ( 1.383733252933561086, 2.037972573443189717, -0.8472329510355591786 ) ) ;
#208494=CARTESIAN_POINT ( 'NONE',  ( 2.882378335548450465, -1.165601267607863978, 1.938926327226223822 ) ) ;
#208496=CARTESIAN_POINT ( 'NONE',  ( 2.794932832814459811, -0.1373201097526421111, -1.806460840857474937 ) ) ;
#208498=CARTESIAN_POINT ( 'NONE',  ( 3.432743858578292784, -1.563009043653120322, 1.107381117132580250 ) ) ;
#208499=CARTESIAN_POINT ( 'NONE',  ( 4.545415791725802457, 1.850806902094417783, -0.9279678557222792445 ) ) ;
#208501=CARTESIAN_POINT ( 'NONE',  ( 2.219545571343143120, -1.912749475042923475, 0.4771270530836198565 ) ) ;
#208502=CARTESIAN_POINT ( 'NONE',  ( 0.1824732010112985747, -1.867734037610004449, -0.4713708115406111676 ) ) ;
#208503=CARTESIAN_POINT ( 'NONE',  ( 2.869827659178546764, 0.9992216309704025079, 1.581230272166146644 ) ) ;
#208504=CARTESIAN_POINT ( 'NONE',  ( 1.823324434984688214, 2.154351390505971686, 0.8276274939288345012 ) ) ;
#208506=CARTESIAN_POINT ( 'NONE',  ( 4.105780043149899861, 0.6285678624660723246, -1.751810336424673542 ) ) ;
#208513=CARTESIAN_POINT ( 'NONE',  ( 0.9265589629697315033, 1.253077620556674932, -1.692570004448453957 ) ) ;
#208515=CARTESIAN_POINT ( 'NONE',  ( 5.975883356200851537, 1.282301362320131588, 1.740048508431484953 ) ) ;
#208516=CARTESIAN_POINT ( 'NONE',  ( 0.0002682147194760230472, -0.9481790448457677600, 1.783359508359374512 ) ) ;
#208521=CARTESIAN_POINT ( 'NONE',  ( 6.925078400183582339, 2.988348447159621113, 2.209593971251204714 ) ) ;
#208524=CARTESIAN_POINT ( 'NONE',  ( 4.399625206644591557, -1.976670321813909892, 0.3981083777728141038 ) ) ;
#208528=CARTESIAN_POINT ( 'NONE',  ( 5.735289742212391850, -1.956171686333206816, 0.9202595734885756773 ) ) ;
#208532=CARTESIAN_POINT ( 'NONE',  ( 6.116814581292481456, 0.2004514801264325186, 2.006445662566976651 ) ) ;
#208536=CARTESIAN_POINT ( 'NONE',  ( 1.277515311556869593, 1.024738337535425758, 1.387312573235904845 ) ) ;
#208540=CARTESIAN_POINT ( 'NONE',  ( 0.6140562859980386312, 1.226574898224697119, -1.275979240986246710 ) ) ;
#208542=CARTESIAN_POINT ( 'NONE',  ( 1.910792991191323065, -0.5388759818002909485, -1.939549710442307839 ) ) ;
#208543=CARTESIAN_POINT ( 'NONE',  ( 3.909358855915114006, 1.891329263188616938, 1.136761501516952766 ) ) ;
#208544=CARTESIAN_POINT ( 'NONE',  ( 5.260662464746663325, -0.7247129924745611129, -2.046699161452083526 ) ) ;
#208545=EDGE_LOOP ( 'NONE', ( #28964, #171022 ) ) ;
#208548=CARTESIAN_POINT ( 'NONE',  ( 3.229257539231108698, 1.917844101178723504, 0.9048822562475050679 ) ) ;
#208549=CARTESIAN_POINT ( 'NONE',  ( 3.093375225471244772, -0.3905761854139707667, 1.978056131710544063 ) ) ;
#208550=CARTESIAN_POINT ( 'NONE',  ( 3.832113882524991411, -0.9361971883012323303, -1.550792431135393334 ) ) ;
#208555=CARTESIAN_POINT ( 'NONE',  ( 6.322862864304120478, 1.705426906915354035, 0.6521430802832667295 ) ) ;
#208557=CARTESIAN_POINT ( 'NONE',  ( 1.815515222670351259, -1.254507992466627808, -1.447865379607627512 ) ) ;
#208562=CARTESIAN_POINT ( 'NONE',  ( 5.436455051933180016, 2.129025116502227810, 0.3735886874452337691 ) ) ;
#208566=CARTESIAN_POINT ( 'NONE',  ( 3.129257641292593650, 1.918792544363761454, 0.9031103230835100248 ) ) ;
#208569=CARTESIAN_POINT ( 'NONE',  ( 4.622318808457460015, 1.215050846432633946, -1.552280729921464708 ) ) ;
#208571=CARTESIAN_POINT ( 'NONE',  ( 6.328373294368253354, -0.9077179077918960948, -1.683272687665722467 ) ) ;
#208573=CARTESIAN_POINT ( 'NONE',  ( 5.946512563314596100, -1.495626773323457170, 1.498989405617740189 ) ) ;
#208575=CARTESIAN_POINT ( 'NONE',  ( 1.188034388246852480, -1.312013912954514971, -1.601590607232979524 ) ) ;
#208576=CARTESIAN_POINT ( 'NONE',  ( 2.431497994139957264, 0.9153433635570235039, -1.712687122320022626 ) ) ;
#208580=CARTESIAN_POINT ( 'NONE',  ( 3.451197694293614671, 0.5077425806990677470, -2.027912974856157291 ) ) ;
#208583=CARTESIAN_POINT ( 'NONE',  ( 0.5569035977302905227, -1.554463864252687122, 0.9298500530290281230 ) ) ;
#208585=CARTESIAN_POINT ( 'NONE',  ( 5.092482806099829062, -2.189899077852827780, -0.2726905915074183673 ) ) ;
#208587=CARTESIAN_POINT ( 'NONE',  ( 2.731697238759897672, -2.059418846490802313, 0.7933392487004320426 ) ) ;
#208591=CARTESIAN_POINT ( 'NONE',  ( 2.068876254944008508, -1.477226179422253871, 1.214308343151893510 ) ) ;
#208594=CARTESIAN_POINT ( 'NONE',  ( 4.791501694037465953, -1.894250426384594066, 0.8359921707915064504 ) ) ;
#208596=CARTESIAN_POINT ( 'NONE',  ( 3.045950098598048328, 0.7793912989166664751, -2.016482303682599841 ) ) ;
#208597=CARTESIAN_POINT ( 'NONE',  ( 5.091441847573507928, -0.7891374179831472935, 2.044738775321436997 ) ) ;
#208608=CARTESIAN_POINT ( 'NONE',  ( 5.612195314557796522, 2.068136773602911038, -0.09592777784667855245 ) ) ;
#208609=CARTESIAN_POINT ( 'NONE',  ( 3.879452639046445661, 1.813680402594812557, -0.6499425845708036720 ) ) ;
#208610=CARTESIAN_POINT ( 'NONE',  ( 0.01720424586787797083, -1.842442205116225695, 0.8197940039925479816 ) ) ;
#208614=CARTESIAN_POINT ( 'NONE',  ( 4.891434682365626507, -1.802310843600445800, 0.7943598514809721012 ) ) ;
#208615=CARTESIAN_POINT ( 'NONE',  ( 0.1995291103054769866, -0.5802879427523646161, 2.113158525371459096 ) ) ;
#208616=CARTESIAN_POINT ( 'NONE',  ( 4.178209475066913647, -1.049361115903378883, 1.493786327181771068 ) ) ;
#208622=CARTESIAN_POINT ( 'NONE',  ( 3.069684041021227827, -1.094477399149307306, 1.480508570315848482 ) ) ;
#208623=CARTESIAN_POINT ( 'NONE',  ( 6.258070432960613161, 0.7665029349510013024, -1.861766797742714585 ) ) ;
#208624=CARTESIAN_POINT ( 'NONE',  ( 1.406082690172899108, 0.4493768194517386849, 2.253890741632145200 ) ) ;
#208625=CARTESIAN_POINT ( 'NONE',  ( 5.489096970993415425, 0.1405823987245969631, 1.956747174436481274 ) ) ;
#208630=CARTESIAN_POINT ( 'NONE',  ( 0.4673438449808891004, 1.800595422158430825, 1.021790579661909781 ) ) ;
#208632=CARTESIAN_POINT ( 'NONE',  ( 1.716468666696397971, 1.951974251796151583, 0.7495149520271927601 ) ) ;
#208633=CARTESIAN_POINT ( 'NONE',  ( 6.526229032160782317, 1.014938005144504274, -1.449696215517197961 ) ) ;
#208637=CARTESIAN_POINT ( 'NONE',  ( 1.891783327304029205, -0.4647161096258972668, -1.677148923195219243 ) ) ;
#208642=CARTESIAN_POINT ( 'NONE',  ( 2.279564191164831666, 1.060311948399524695, 1.360390198354200386 ) ) ;
#208643=CARTESIAN_POINT ( 'NONE',  ( 2.947022816757136621, -1.793111998972513277, -1.259777465452505796 ) ) ;
#208644=CARTESIAN_POINT ( 'NONE',  ( 5.549527019956425278, -1.737703232767298545, -1.360318885177333570 ) ) ;
#208647=CARTESIAN_POINT ( 'NONE',  ( 2.835037514343414777, -2.076374246603398532, -0.6340929010987955694 ) ) ;
#208648=CARTESIAN_POINT ( 'NONE',  ( 0.6975366375942676500, -0.6598540886826111951, 1.702458561391326342 ) ) ;
#208649=CARTESIAN_POINT ( 'NONE',  ( 3.134099051248913970, 2.117513410275436936, -0.004568276605129357668 ) ) ;
#208650=CARTESIAN_POINT ( 'NONE',  ( 6.539320575229255361, 3.697401852651286180, 2.511149361313206096 ) ) ;
#208652=CARTESIAN_POINT ( 'NONE',  ( 4.089605575727714104, -0.8772585143675699637, 2.118060962191004037 ) ) ;
#208656=CARTESIAN_POINT ( 'NONE',  ( 6.428415558115947448, -1.044286553621230240, -1.960546399981792476 ) ) ;
#208661=CARTESIAN_POINT ( 'NONE',  ( 6.825078400183572036, 4.699117039843025090, 2.418333817060664082 ) ) ;
#208663=CARTESIAN_POINT ( 'NONE',  ( 4.641250102003463773, 0.7743139518727223392, 1.862017545363145565 ) ) ;
#208665=CARTESIAN_POINT ( 'NONE',  ( 2.131754086930433001, 1.975065156136386335, -0.5945119761870448771 ) ) ;
#208670=CARTESIAN_POINT ( 'NONE',  ( 5.613277516225614328, -2.138688192980051639, 0.4772630486022874652 ) ) ;
#208671=CARTESIAN_POINT ( 'NONE',  ( 3.727185537919291747, 2.006959858346604619, 0.1948421285040344286 ) ) ;
#208672=CARTESIAN_POINT ( 'NONE',  ( 2.032514702046281485, -1.644074058028240692, 0.8291662819630771786 ) ) ;
#208675=CARTESIAN_POINT ( 'NONE',  ( 0.08252656676070461994, -0.1270158569062987686, -1.696106202995291357 ) ) ;
#208678=CARTESIAN_POINT ( 'NONE',  ( 5.717715967963762580, -2.208827357630326560, 0.4893477075747532101 ) ) ;
#208680=CARTESIAN_POINT ( 'NONE',  ( 2.438226732591573409, 0.9919046538873840246, -1.857854779501419307 ) ) ;
#208691=CARTESIAN_POINT ( 'NONE',  ( 1.564851893998190135, 0.6701894319398638000, 2.011955567234039677 ) ) ;
#208692=CARTESIAN_POINT ( 'NONE',  ( 2.883289241188752072, -2.054055030226094480, -0.8463503915563088675 ) ) ;
#208693=CARTESIAN_POINT ( 'NONE',  ( 0.04788047853313340263, -1.708876078042343316, -1.396090968258607790 ) ) ;
#208696=CARTESIAN_POINT ( 'NONE',  ( 4.123457186961496213, 0.2424046295769199388, -1.946780420294342617 ) ) ;
#208704=CARTESIAN_POINT ( 'NONE',  ( 3.146849984228027974, 2.069795010335002239, 0.4607391970517027979 ) ) ;
#208706=CARTESIAN_POINT ( 'NONE',  ( 4.083022661009271914, -0.2092679848491978134, -2.151539631373246220 ) ) ;
#208707=CARTESIAN_POINT ( 'NONE',  ( 3.526749072549471453, -1.699942963128863838, 0.7078653300200201670 ) ) ;
#208710=CARTESIAN_POINT ( 'NONE',  ( 5.683501733545419654, -0.7767583057271000291, 1.557453612149447775 ) ) ;
#208711=CARTESIAN_POINT ( 'NONE',  ( 6.727182134110202050, 0.5964276595885747989, 1.864301751488647962 ) ) ;
#208715=CARTESIAN_POINT ( 'NONE',  ( 3.045950098598048328, 0.7793912989166664751, -2.016482303682599841 ) ) ;
#208717=CARTESIAN_POINT ( 'NONE',  ( 5.641953822799152363, -0.04667112846407085042, -2.015725140939367943 ) ) ;
#208719=CARTESIAN_POINT ( 'NONE',  ( 2.940462584922590938, 2.145230175562794717, 0.2658940370997217584 ) ) ;
#208720=CARTESIAN_POINT ( 'NONE',  ( 4.130118527232538028, 1.057347662480428108, -1.663647784685320818 ) ) ;
#208721=CARTESIAN_POINT ( 'NONE',  ( 0.06437606466144081552, -1.426665095847098330, 1.663708609037084951 ) ) ;
#208722=CARTESIAN_POINT ( 'NONE',  ( 0.8510977523443744586, 0.6731378975963157041, 2.207243034677327298 ) ) ;
#208723=CARTESIAN_POINT ( 'NONE',  ( 4.019036194231017767, -1.857530068489420705, 0.5666795103562488611 ) ) ;
#208728=CARTESIAN_POINT ( 'NONE',  ( 6.890000000000050306, -0.002781820520068867264, 1.999840353888074240 ) ) ;
#208732=CARTESIAN_POINT ( 'NONE',  ( 1.870444250305805856, 1.134645063044220858, 1.892580404734986121 ) ) ;
#208734=CARTESIAN_POINT ( 'NONE',  ( 6.877797714452785982, -1.903667959252927533, 0.4735691183095217527 ) ) ;
#208739=CARTESIAN_POINT ( 'NONE',  ( 6.720655732516647163, 0.005566325962592238996, 1.826293863978686982 ) ) ;
#208740=CARTESIAN_POINT ( 'NONE',  ( 5.894452933195246658, 1.502573388107550034, -1.063714819228026132 ) ) ;
#208741=ORIENTED_EDGE ( 'NONE', *, *, #45569, .F. ) ;
#208745=CARTESIAN_POINT ( 'NONE',  ( 6.504144398916748671, -0.9053081408615070158, 1.915699539216948688 ) ) ;
#208748=CARTESIAN_POINT ( 'NONE',  ( 0.2861016050247901510, -0.9718399577113141508, 1.817365962020002890 ) ) ;
#208751=CARTESIAN_POINT ( 'NONE',  ( 1.908444903620472477, 0.5799682436128813512, 1.768463464005122443 ) ) ;
#208752=CARTESIAN_POINT ( 'NONE',  ( 5.284640796330934087, 1.621094592300664328, -0.8731043043393662550 ) ) ;
#208759=CARTESIAN_POINT ( 'NONE',  ( 4.336686996305870068, 2.164023489887345164, 0.4319772483800735086 ) ) ;
#208760=CARTESIAN_POINT ( 'NONE',  ( 6.098944901167723032, 1.854799121126067485, -1.295245758874500996 ) ) ;
#208762=CARTESIAN_POINT ( 'NONE',  ( 5.326340473083292615, -0.8217345736999382977, -1.614601580891014354 ) ) ;
#208763=CARTESIAN_POINT ( 'NONE',  ( 6.016788071399586713, 0.1949370894720331426, 1.905806522959735627 ) ) ;
#208765=CARTESIAN_POINT ( 'NONE',  ( 5.215449470722859360, 1.565665547294055715, 1.097690013397538022 ) ) ;
#208766=CARTESIAN_POINT ( 'NONE',  ( 0.2154177506630133854, -1.835460468737951878, 0.3602540799089171131 ) ) ;
#208767=CARTESIAN_POINT ( 'NONE',  ( 2.905482715143858030, -1.942096844255640109, 0.5424705965835219246 ) ) ;
#208769=CARTESIAN_POINT ( 'NONE',  ( 3.615936863914733124, -2.074906038012876763, 0.3600020511305370707 ) ) ;
#208774=CARTESIAN_POINT ( 'NONE',  ( 3.463153198524880239, -1.648742896667846125, 1.166392943622736267 ) ) ;
#208778=CARTESIAN_POINT ( 'NONE',  ( 4.411504763889100289, -0.3743020017868466387, 2.128795073437335095 ) ) ;
#208784=CARTESIAN_POINT ( 'NONE',  ( 2.225261637991797325, -1.984409513266917502, -0.8813929409505830703 ) ) ;
#208787=CARTESIAN_POINT ( 'NONE',  ( 0.4504185290156897947, -1.555054577268409899, -0.9855837367087336709 ) ) ;
#208789=CARTESIAN_POINT ( 'NONE',  ( 2.296645709751913955, 1.758124065145909798, -1.308193547052277861 ) ) ;
#208791=CARTESIAN_POINT ( 'NONE',  ( 6.883263157960362477, 2.445608615952394871, 2.336423753955836791 ) ) ;
#208792=CARTESIAN_POINT ( 'NONE',  ( 2.132027182898531326, -1.478040878648724465, -1.713098503734461708 ) ) ;
#208799=CARTESIAN_POINT ( 'NONE',  ( 4.094789254117153554, 1.496004596371943496, -0.9451293409883186891 ) ) ;
#208801=CARTESIAN_POINT ( 'NONE',  ( 1.096861832941862236, -0.5116358106188825250, -2.042740603722263515 ) ) ;
#208805=CARTESIAN_POINT ( 'NONE',  ( 6.573846656420020196, -0.8593871168269312522, 1.822298249534954673 ) ) ;
#208807=CARTESIAN_POINT ( 'NONE',  ( 4.030043484472041193, 1.001115284758803625, -1.580040089582811280 ) ) ;
#208808=CARTESIAN_POINT ( 'NONE',  ( 4.750872686184268723, -0.4484009487188305720, -2.020967519627144604 ) ) ;
#208818=CARTESIAN_POINT ( 'NONE',  ( 3.719154087244529894, -1.729071306366702698, -0.9269775827704658244 ) ) ;
#208820=CARTESIAN_POINT ( 'NONE',  ( 0.8079699768257715409, -1.730602710733687877, 1.034004433739174500 ) ) ;
#208823=CARTESIAN_POINT ( 'NONE',  ( 6.639320575229255894, 7.053084031878349869, 2.494893166485531388 ) ) ;
#208824=CARTESIAN_POINT ( 'NONE',  ( 1.370139650511486007, -1.190941340819328564, 1.442406204513801971 ) ) ;
#208826=CARTESIAN_POINT ( 'NONE',  ( 3.041273912350466624, 0.05370876457178561797, 2.012661466405294863 ) ) ;
#208828=CARTESIAN_POINT ( 'NONE',  ( 3.111064062886280013, 0.05467929133608259024, 2.116691892344662929 ) ) ;
#208830=CARTESIAN_POINT ( 'NONE',  ( 5.336411075974297979, -1.153114810915600641, 1.719314882265559286 ) ) ;
#208832=CARTESIAN_POINT ( 'NONE',  ( -0.05888619351396630341, -1.618772603580875158, -1.322922665863958125 ) ) ;
#208834=CARTESIAN_POINT ( 'NONE',  ( 4.875911338656576888, 1.051942333337583468, 1.491839654383666947 ) ) ;
#208841=CARTESIAN_POINT ( 'NONE',  ( 5.215449470722859360, 1.565665547294055715, 1.097690013397538022 ) ) ;
#208855=CARTESIAN_POINT ( 'NONE',  ( 1.832793114640043131, -1.868399652882225981, -0.6228533014895777375 ) ) ;
#208856=CARTESIAN_POINT ( 'NONE',  ( 3.866814677988283044, -0.2004539179165897023, -2.006445418776988010 ) ) ;
#208859=CARTESIAN_POINT ( 'NONE',  ( 6.727182134110193168, 3.677753830905213128, 2.802861976130672783 ) ) ;
#208860=CARTESIAN_POINT ( 'NONE',  ( 3.416156609664961152, 1.390242785425911620, -1.694013327489252152 ) ) ;
#208862=CARTESIAN_POINT ( 'NONE',  ( 1.887598533328225692, 1.326653652590740418, 1.397000115363009609 ) ) ;
#208864=CARTESIAN_POINT ( 'NONE',  ( -0.1296875068448125334, 4.095146142119266308, -2.381513845672214913 ) ) ;
#208865=CARTESIAN_POINT ( 'NONE',  ( 0.1329588055935213564, 1.397696041676167678, -2.105440929937075989 ) ) ;
#208872=CARTESIAN_POINT ( 'NONE',  ( 6.233933901472759942, 1.822226914158030286, 0.2631550708301691466 ) ) ;
#208873=CARTESIAN_POINT ( 'NONE',  ( 3.106110754726201240, -0.8138748988139458129, 1.841402425526596387 ) ) ;
#208874=CARTESIAN_POINT ( 'NONE',  ( 4.798391170199634459, -2.103835099937763964, 0.9258070857356412997 ) ) ;
#208875=CARTESIAN_POINT ( 'NONE',  ( -0.02880301295726198432, 1.985184585160368664, -2.687100061827327302 ) ) ;
#208876=CARTESIAN_POINT ( 'NONE',  ( 1.867776877072557129, -1.847639373886921677, 0.2213648055933575276 ) ) ;
#208882=CARTESIAN_POINT ( 'NONE',  ( 4.546477914129923192, -1.678139501482888152, 1.246787890680167710 ) ) ;
#208883=CARTESIAN_POINT ( 'NONE',  ( 3.924554409752772699, 1.776107677202539925, 0.5873546117282567591 ) ) ;
#208888=CARTESIAN_POINT ( 'NONE',  ( 6.533849689656099358, -1.133137674240388248, -1.300586445545851344 ) ) ;
#208890=CARTESIAN_POINT ( 'NONE',  ( 1.635018144205732771, 0.5444147220468772419, 1.646514679669469849 ) ) ;
#208894=CARTESIAN_POINT ( 'NONE',  ( 5.981339239477990510, -0.06126731230964890806, 2.170386710549534470 ) ) ;
#208895=CARTESIAN_POINT ( 'NONE',  ( 4.230939532379584200, 0.09184734775685021724, 1.823503176236190626 ) ) ;
#208896=CARTESIAN_POINT ( 'NONE',  ( 1.692165188054130187, 0.9715730843921737137, -1.704227633833883759 ) ) ;
#208897=CARTESIAN_POINT ( 'NONE',  ( 6.473823543489908516, -0.9023987703748233002, 1.913193491996653783 ) ) ;
#208901=CARTESIAN_POINT ( 'NONE',  ( 2.543736517606724146, -1.977637755382474438, 0.7655657148115800892 ) ) ;
#208905=CARTESIAN_POINT ( 'NONE',  ( 0.2685318824256071601, -0.8817220219094963340, -1.871193708407721035 ) ) ;
#208908=CARTESIAN_POINT ( 'NONE',  ( 3.123905467589927820, -0.4314640245299468657, 2.178836924841739631 ) ) ;
#208910=CARTESIAN_POINT ( 'NONE',  ( 0.6690544563107813092, 1.549219078230345215, 1.698357357312555660 ) ) ;
#208912=CARTESIAN_POINT ( 'NONE',  ( 6.438341905586414171, -1.108352981827376738, 1.739313939070710857 ) ) ;
#208915=CARTESIAN_POINT ( 'NONE',  ( 0.1333542156527478262, 0.001576319744088505292, -2.046049510433409768 ) ) ;
#208916=CARTESIAN_POINT ( 'NONE',  ( 5.759284750224211713, 1.812880138157666465, -0.3211251414683007899 ) ) ;
#208918=CARTESIAN_POINT ( 'NONE',  ( -0.2102771530458459603, 1.310786636098780544, -2.452585248267840967 ) ) ;
#208919=CARTESIAN_POINT ( 'NONE',  ( 2.643205280608558194, -1.276243157467608302, -1.160367288944160968 ) ) ;
#208920=CARTESIAN_POINT ( 'NONE',  ( 1.481658059775035952, -0.6748446255696785023, 1.900416712880992343 ) ) ;
#208921=CARTESIAN_POINT ( 'NONE',  ( 3.129784643070336436, 0.5604733119842463251, 2.229205935122404725 ) ) ;
#208922=CARTESIAN_POINT ( 'NONE',  ( 2.425404053729601550, -0.002036344795489434568, 2.262578821637390547 ) ) ;
#208923=CARTESIAN_POINT ( 'NONE',  ( 5.672525241255916839, -1.337268198843853506, 1.627036470456619810 ) ) ;
#208925=CARTESIAN_POINT ( 'NONE',  ( 4.094789254117153554, 1.496004596371943496, -0.9451293409883186891 ) ) ;
#208927=CARTESIAN_POINT ( 'NONE',  ( 0.006404353242023088852, -0.9848532314915852126, -2.067437341614616120 ) ) ;
#208928=CARTESIAN_POINT ( 'NONE',  ( 4.189278935350455590, -0.7026162016144417155, 1.701997885059022497 ) ) ;
#208933=CARTESIAN_POINT ( 'NONE',  ( 5.068408068084750084, -2.062719301109996461, -0.7404068969242216802 ) ) ;
#208936=CARTESIAN_POINT ( 'NONE',  ( 5.125469573878929097, 0.2063957376101481500, -2.060066405364005426 ) ) ;
#208937=CARTESIAN_POINT ( 'NONE',  ( 0.2511858651975951151, 0.1928294586405615574, -2.007256720055437871 ) ) ;
#208939=CARTESIAN_POINT ( 'NONE',  ( 3.334515964829305457, 1.879714267205140565, 0.4213298384171912381 ) ) ;
#208942=CARTESIAN_POINT ( 'NONE',  ( 0.2643399247034176613, 0.6888887472211238094, -2.111998681152967183 ) ) ;
#208951=CARTESIAN_POINT ( 'NONE',  ( 1.117545225965112188, 0.3861695934333775337, -1.923310697798483293 ) ) ;
#208954=CARTESIAN_POINT ( 'NONE',  ( 6.754756207809571755, -1.674487575904315406, 1.366813541845832924 ) ) ;
#208957=CARTESIAN_POINT ( 'NONE',  ( 5.019951445752288244, 1.940773837913706057, -0.2859759768028962146 ) ) ;
#208960=CARTESIAN_POINT ( 'NONE',  ( 6.121977807712331909, -1.196819783530624015, -1.799967629666970881 ) ) ;
#208964=CARTESIAN_POINT ( 'NONE',  ( 6.784453690597813669, -1.932871751835860241, -0.3867854297147227394 ) ) ;
#208965=CARTESIAN_POINT ( 'NONE',  ( 6.257189190585941141, -1.725921076436988111, -0.1656679613657590366 ) ) ;
#208968=CARTESIAN_POINT ( 'NONE',  ( 2.560326853991791829, -1.509077608345666066, 1.589458984681046516 ) ) ;
#208969=CARTESIAN_POINT ( 'NONE',  ( 4.735574959254028826, -2.111847384580630038, 0.9304801611131856554 ) ) ;
#208970=CARTESIAN_POINT ( 'NONE',  ( 5.413377607122367152, -0.3064755606005803434, 2.037752308911133348 ) ) ;
#208971=CARTESIAN_POINT ( 'NONE',  ( 0.8670093773819181893, 1.871751486835357747, -0.5171616756182734198 ) ) ;
#208973=CARTESIAN_POINT ( 'NONE',  ( 4.640951271726033056, 2.030106984047326701, 0.6129599860185754867 ) ) ;
#208974=CARTESIAN_POINT ( 'NONE',  ( 2.373672848961404735, -0.3474683332905931232, -1.986100487175908258 ) ) ;
#208976=CARTESIAN_POINT ( 'NONE',  ( 6.088949818052607377, -0.3178892970779038096, -2.183640257897196513 ) ) ;
#208978=CARTESIAN_POINT ( 'NONE',  ( 0.1350027811974127134, -1.670744041527939094, 0.7364786222084362954 ) ) ;
#208984=CARTESIAN_POINT ( 'NONE',  ( 5.875869988399868404, 1.225711027941748466, 1.656622483273604729 ) ) ;
#208986=CARTESIAN_POINT ( 'NONE',  ( -0.2108831679770959699, 2.036692374882024037, -2.313561348563981657 ) ) ;
#208989=CARTESIAN_POINT ( 'NONE',  ( 4.916668454303085412, -0.6825918349771132876, -1.900952964002266210 ) ) ;
#208994=CARTESIAN_POINT ( 'NONE',  ( 3.766525121192493941, -1.385455288492474235, 1.525868174829993373 ) ) ;
#208995=CARTESIAN_POINT ( 'NONE',  ( 3.287732575140738245, 1.587837554856496469, -1.242726844152844956 ) ) ;
#208997=CARTESIAN_POINT ( 'NONE',  ( 6.727182134110194056, 3.682851444631680238, 2.702965647100653790 ) ) ;
#209001=CARTESIAN_POINT ( 'NONE',  ( 3.233749808020690342, -1.861731463674856979, -0.7741979076196570109 ) ) ;
#209002=CARTESIAN_POINT ( 'NONE',  ( 2.378628397106247849, 1.683441843134887428, -0.7459445200509451368 ) ) ;
#209003=CARTESIAN_POINT ( 'NONE',  ( 1.137850649969934347, -2.084210194689451789, 0.9910022104400189047 ) ) ;
#209005=CARTESIAN_POINT ( 'NONE',  ( 2.442841770826277958, 0.4709965094221583159, 2.109507199432036018 ) ) ;
#209009=CARTESIAN_POINT ( 'NONE',  ( 0.9888773766892227091, 1.651582696977689890, -0.8784067438419729257 ) ) ;
#209010=CARTESIAN_POINT ( 'NONE',  ( 5.840691970153715218, 0.3840316513750040572, 1.933538979438324867 ) ) ;
#209015=CARTESIAN_POINT ( 'NONE',  ( 0.4521680116954321371, 0.6883007682146925488, -2.096869779678663281 ) ) ;
#209016=CARTESIAN_POINT ( 'NONE',  ( 6.848098043024292814, -0.8888149443028300345, 1.868052569137634400 ) ) ;
#209019=CARTESIAN_POINT ( 'NONE',  ( 6.539320575229280230, 7.629137130509070275, 2.703262396134015866 ) ) ;
#209020=CARTESIAN_POINT ( 'NONE',  ( 5.067239680553584869, 0.1942248685237786265, -1.961885565008324006 ) ) ;
#209021=CARTESIAN_POINT ( 'NONE',  ( 0.08834397731360790762, 1.226219587655341448, 1.729930300845914815 ) ) ;
#209022=CARTESIAN_POINT ( 'NONE',  ( 4.846439200125199243, 2.301219453760998679, 0.1735292846544200795 ) ) ;
#209024=CARTESIAN_POINT ( 'NONE',  ( 3.309489505334945569, -1.683523595015530505, -1.191345380358753925 ) ) ;
#209032=CARTESIAN_POINT ( 'NONE',  ( 5.547405112160277874, 1.917339678720403118, -1.018715297254897401 ) ) ;
#209034=CARTESIAN_POINT ( 'NONE',  ( 3.948646536499214932, -1.533023199436277961, -1.019512891124202403 ) ) ;
#209036=CARTESIAN_POINT ( 'NONE',  ( 6.620655732516673275, 1.290356161719278028, 1.942653802560645460 ) ) ;
#209037=CARTESIAN_POINT ( 'NONE',  ( 5.899973326018037589, -0.7874313895239596350, -2.045375389432432467 ) ) ;
#209039=CARTESIAN_POINT ( 'NONE',  ( 0.1813603024932753938, -0.1560989159599696641, -2.227174003853182871 ) ) ;
#209045=CARTESIAN_POINT ( 'NONE',  ( 1.006321374186702311, 1.343689884961623227, -1.152001066587736267 ) ) ;
#209046=CARTESIAN_POINT ( 'NONE',  ( 5.145186220991746495, 0.1505098195577254938, 2.007535063509538809 ) ) ;
#209048=CARTESIAN_POINT ( 'NONE',  ( 3.645630060059632083, -1.593344849414342290, -1.377153647973597073 ) ) ;
#209049=CARTESIAN_POINT ( 'NONE',  ( 2.724132717865447084, 1.901453608201342238, 0.2316716071539808575 ) ) ;
#209051=CARTESIAN_POINT ( 'NONE',  ( 4.738697576358215535, -1.909850223682897807, -0.4806687167441258679 ) ) ;
#209052=CARTESIAN_POINT ( 'NONE',  ( 6.029558467290160984, -0.2429869472727399504, 2.005020512606956018 ) ) ;
#209053=CARTESIAN_POINT ( 'NONE',  ( 1.375632740723360836, 1.111493989511678881, 1.504490780774490499 ) ) ;
#209054=CARTESIAN_POINT ( 'NONE',  ( 5.039546052477672511, -1.223360384887246743, -1.216254805912063919 ) ) ;
#209055=CARTESIAN_POINT ( 'NONE',  ( 1.125099709691119276, 1.687896996356451629, 0.8989547360247207575 ) ) ;
#209057=CARTESIAN_POINT ( 'NONE',  ( 1.506762622594171930, -0.7967928049063888185, -2.058199171410409978 ) ) ;
#209061=CARTESIAN_POINT ( 'NONE',  ( 6.631728656526095556, -1.223761959379562114, -1.414937998750566361 ) ) ;
#209066=CARTESIAN_POINT ( 'NONE',  ( 1.609917502266303480, 0.6029389078928657497, -1.980602105166151095 ) ) ;
#209071=CARTESIAN_POINT ( 'NONE',  ( 0.1002680356884171620, -0.9499045104094726577, 1.782327323349098602 ) ) ;
#209077=CARTESIAN_POINT ( 'NONE',  ( 5.026720154644213068, 1.994564127574052437, -0.2930270067487000252 ) ) ;
#209078=CARTESIAN_POINT ( 'NONE',  ( 5.190618481123168593, 1.446159319891277661, -1.256491027437984354 ) ) ;
#209080=CARTESIAN_POINT ( 'NONE',  ( 2.560326853991791829, -1.509077608345666066, 1.589458984681046516 ) ) ;
#209081=CARTESIAN_POINT ( 'NONE',  ( 0.1335669894368864408, 5.721243636067999461, -2.747585559332069494 ) ) ;
#209083=CARTESIAN_POINT ( 'NONE',  ( 5.818613517226002507, -0.7285450932710479943, -1.876915101588324974 ) ) ;
#209084=CARTESIAN_POINT ( 'NONE',  ( 1.459083999156213229, -1.613880964290699938, 1.025699646091532857 ) ) ;
#209088=CARTESIAN_POINT ( 'NONE',  ( 6.450787963126683344, -1.935726721829626351, -0.8580517621625349811 ) ) ;
#209090=CARTESIAN_POINT ( 'NONE',  ( 3.860945534362031140, 0.2537485593089708336, -2.075202752206976697 ) ) ;
#209092=CARTESIAN_POINT ( 'NONE',  ( 1.799380453634431998, -0.5854278125525367305, 1.622511832645438190 ) ) ;
#209094=CARTESIAN_POINT ( 'NONE',  ( 6.416280414004661203, -2.120105685773795212, 0.05337830808049835035 ) ) ;
#209101=CARTESIAN_POINT ( 'NONE',  ( 2.701584635150193314, 1.282363399140455273, 1.279706459777726346 ) ) ;
#209107=CARTESIAN_POINT ( 'NONE',  ( 4.107922266221023300, -0.6895048676278795474, 1.675321109400946806 ) ) ;
#209108=FACE_OUTER_BOUND ( 'NONE', #166860, .T. ) ;
#209112=CARTESIAN_POINT ( 'NONE',  ( 3.666312420855986520, -0.7522870471967492145, -1.702408540065254883 ) ) ;
#209113=CARTESIAN_POINT ( 'NONE',  ( 1.247507242870619981, 1.886983585358002813, -0.3289482045247971165 ) ) ;
#209114=CARTESIAN_POINT ( 'NONE',  ( 0.6569167496461197908, -1.539450689919025450, -0.9809549629347169564 ) ) ;
#209125=CARTESIAN_POINT ( 'NONE',  ( 5.471530992243406999, -0.2926990004611991214, 1.947462276923512370 ) ) ;
#209128=CARTESIAN_POINT ( 'NONE',  ( 0.7090669197488512765, -0.3047467688393705187, 2.068175119304823451 ) ) ;
#209130=CARTESIAN_POINT ( 'NONE',  ( 5.034167752753979208, 0.9906028322895725768, -1.652054708979720399 ) ) ;
#209132=CARTESIAN_POINT ( 'NONE',  ( 0.9908991873810431006, 1.612194894691898250, -0.8564790819722142290 ) ) ;
#209133=CARTESIAN_POINT ( 'NONE',  ( 2.315298440750997777, 1.971968782506158924, 0.9909306302095726160 ) ) ;
#209135=CARTESIAN_POINT ( 'NONE',  ( 0.8086807686161383568, -0.4671638426185490967, -1.854305266343849734 ) ) ;
#209137=CARTESIAN_POINT ( 'NONE',  ( 1.012081461190861065, 1.967466754592902989, -0.09309286250217158054 ) ) ;
#209138=CARTESIAN_POINT ( 'NONE',  ( 2.454547613406708351, -1.690768538996465509, -0.9553028803331271579 ) ) ;
#209140=CARTESIAN_POINT ( 'NONE',  ( 1.018907413236518789, 2.013924516646655949, -0.09611688112247382398 ) ) ;
#209142=CARTESIAN_POINT ( 'NONE',  ( 5.330833089851809703, -1.751472900985746373, -0.6291486930528921162 ) ) ;
#209144=CARTESIAN_POINT ( 'NONE',  ( -0.1909996267163149852, 7.629137130509101361, -2.600377616606447617 ) ) ;
#209148=CARTESIAN_POINT ( 'NONE',  ( 1.646283778714407342, 0.6915601415973006150, 2.079641132013386517 ) ) ;
#209152=CARTESIAN_POINT ( 'NONE',  ( 3.070728972534173096, -1.687097908962056803, -0.6982200720766564839 ) ) ;
#209159=CARTESIAN_POINT ( 'NONE',  ( 0.6977243349758615043, -0.6943943954660827256, 1.797178231592330588 ) ) ;
#209160=CARTESIAN_POINT ( 'NONE',  ( 5.155110299917927463, 1.633153276354940342, -1.086568599608192409 ) ) ;
#209164=CARTESIAN_POINT ( 'NONE',  ( 5.372676843235411503, -0.05303982195071360595, -2.191091664329389399 ) ) ;
#209166=CARTESIAN_POINT ( 'NONE',  ( 4.452052287080165982, -0.7971045336818067817, 1.910850710330507907 ) ) ;
#209169=ORIENTED_EDGE ( 'NONE', *, *, #83250, .T. ) ;
#209170=CARTESIAN_POINT ( 'NONE',  ( 3.534061846033216714, -1.878541635090751560, 1.324563465849286859 ) ) ;
#209176=CARTESIAN_POINT ( 'NONE',  ( 4.171774378167571129, -1.117019396711134371, 1.588354668226848565 ) ) ;
#209180=CARTESIAN_POINT ( 'NONE',  ( 5.625241921295836889, 1.689600096388569561, 0.8957793909229803120 ) ) ;
#209181=CARTESIAN_POINT ( 'NONE',  ( 5.895441327320324554, 1.309037806329484521, 1.123130245766153612 ) ) ;
#209182=CARTESIAN_POINT ( 'NONE',  ( 4.803922858132807505, -1.082837210388952309, -1.700963621564715700 ) ) ;
#209184=CARTESIAN_POINT ( 'NONE',  ( 1.454063653991678473, 0.6380318336138122159, -2.112638918738508398 ) ) ;
#209187=CARTESIAN_POINT ( 'NONE',  ( 1.623107816722869412, -1.968041427791475728, 0.7057566781872460782 ) ) ;
#209188=CARTESIAN_POINT ( 'NONE',  ( 6.538360807962172672, 1.750891970090788119, 0.2567797125347607845 ) ) ;
#209189=CARTESIAN_POINT ( 'NONE',  ( 5.731092321990707283, 2.014232586630093191, 0.09613807139101374077 ) ) ;
#209191=CARTESIAN_POINT ( 'NONE',  ( 3.539304732165698741, -1.735471681261467669, -1.497634786905965187 ) ) ;
#209192=CARTESIAN_POINT ( 'NONE',  ( 1.147962396684144792, -1.373903031218721926, 1.068100470705938276 ) ) ;
#209193=CARTESIAN_POINT ( 'NONE',  ( 2.654661980655496301, 2.105093816413053709, 0.2552270188876659129 ) ) ;
#209195=CARTESIAN_POINT ( 'NONE',  ( 1.352469423652577607, -0.7852941029048329247, 1.545897522503926647 ) ) ;
#209197=CARTESIAN_POINT ( 'NONE',  ( 1.152544200391303786, -0.4473333697519957242, -1.806370492606963474 ) ) ;
#209198=CARTESIAN_POINT ( 'NONE',  ( 1.153041021216383299, -0.5271860560512993121, -2.106100485105724562 ) ) ;
#209199=CARTESIAN_POINT ( 'NONE',  ( 3.028530041973789722, 0.4946322284519070189, 1.954779462066410733 ) ) ;
#209200=CARTESIAN_POINT ( 'NONE',  ( 4.875000000000002665, 2.052068128417942727, -2.776269294175867294E-13 ) ) ;
#209202=CARTESIAN_POINT ( 'NONE',  ( 6.656866507323381477, -1.487278495449697147, 1.224136630395280534 ) ) ;
#209204=CARTESIAN_POINT ( 'NONE',  ( 3.428187820690358656, -2.188011084934568196, 0.3830038565930964367 ) ) ;
#209209=CARTESIAN_POINT ( 'NONE',  ( 4.211346380768822506, -1.629847038978438079, -1.091715234301626314 ) ) ;
#209214=CARTESIAN_POINT ( 'NONE',  ( 5.272873185648853323, -2.127775705341850898, -0.7691360568998426572 ) ) ;
#209215=CARTESIAN_POINT ( 'NONE',  ( 2.049356628244120682, 1.795697342706262578, -1.014786283375568976 ) ) ;
#209219=CARTESIAN_POINT ( 'NONE',  ( 3.321420150926617687, -1.803644938814071175, 0.4956094624995326381 ) ) ;
#209220=CARTESIAN_POINT ( 'NONE',  ( 2.285452750267936484, 1.391693986029099772, -1.034342955966370603 ) ) ;
#209221=CARTESIAN_POINT ( 'NONE',  ( 6.321842903100939104, 1.263506803105146847, -1.790488031206059372 ) ) ;
#209222=CARTESIAN_POINT ( 'NONE',  ( 0.8334014933106950185, 0.1641056870149599223, 2.200712145998296343 ) ) ;
#209223=CARTESIAN_POINT ( 'NONE',  ( 3.889662759143839299, 1.564074849111227516, 1.492423382767386730 ) ) ;
#209224=CARTESIAN_POINT ( 'NONE',  ( 5.208904604407663008, -0.2832176519766657630, 1.921071368630644649 ) ) ;
#209225=CARTESIAN_POINT ( 'NONE',  ( 0.3124999997796079620, 1.451031294483781764, 1.451031289061110341 ) ) ;
#209229=CARTESIAN_POINT ( 'NONE',  ( 5.344375030997434273, 0.3906003880304632636, -1.978050218768567792 ) ) ;
#209233=CARTESIAN_POINT ( 'NONE',  ( 3.369579884941567016, 1.780956498284639533, -0.4009276245297774266 ) ) ;
#209234=CARTESIAN_POINT ( 'NONE',  ( 2.046200460737709559, 0.8445575735530999051, -2.038961412367201298 ) ) ;
#209240=CARTESIAN_POINT ( 'NONE',  ( 0.7209703750307445702, 1.526537956607315172, -1.322641891180293516 ) ) ;
#209241=CARTESIAN_POINT ( 'NONE',  ( 1.453939175038564624, -1.538220317728825393, -1.459821603020584613 ) ) ;
#209244=CARTESIAN_POINT ( 'NONE',  ( 1.867776877072557129, -1.847639373886921677, 0.2213648055933575276 ) ) ;
#209246=CARTESIAN_POINT ( 'NONE',  ( 1.323354039402934390, -0.05256100377049736927, 2.161234000603563299 ) ) ;
#209247=CARTESIAN_POINT ( 'NONE',  ( 6.100232455412330168, -0.2440331339308223768, 2.001510902166554473 ) ) ;
#209248=ORIENTED_EDGE ( 'NONE', *, *, #80635, .F. ) ;
#209252=CARTESIAN_POINT ( 'NONE',  ( 3.809063337113669068, 1.566667275063510445, 0.9371452329686791316 ) ) ;
#209256=CARTESIAN_POINT ( 'NONE',  ( 6.098982473628085543, 0.9961464269193781584, -1.752763620266280187 ) ) ;
#209257=CARTESIAN_POINT ( 'NONE',  ( 5.929618730664214077, 0.9035273275350870215, -1.604119651413847603 ) ) ;
#209259=CARTESIAN_POINT ( 'NONE',  ( 4.266487514486948740, 1.085833288323118095, 2.036285375418740884 ) ) ;
#209261=CARTESIAN_POINT ( 'NONE',  ( 6.432923066502826082, 0.2047513753351773436, 2.151863363619124225 ) ) ;
#209262=CARTESIAN_POINT ( 'NONE',  ( 2.718228044968384882, 1.829540209339441503, 0.6518440813585175686 ) ) ;
#209263=CARTESIAN_POINT ( 'NONE',  ( 4.798391170199634459, -2.103835099937763964, 0.9258070857356412997 ) ) ;
#209267=CARTESIAN_POINT ( 'NONE',  ( 4.504681594071535677, 1.446009304718363087, -1.186774495104812699 ) ) ;
#209270=CARTESIAN_POINT ( 'NONE',  ( 2.865378420500460876, -1.565876230000915692, -1.097592462808501645 ) ) ;
#209273=CARTESIAN_POINT ( 'NONE',  ( 3.879664727460280904, 2.078262106501146622, -0.7427522710690689367 ) ) ;
#209274=CARTESIAN_POINT ( 'NONE',  ( 6.983263157960363010, 3.696136926403908340, 2.460428995873820579 ) ) ;
#209277=CARTESIAN_POINT ( 'NONE',  ( 1.581257511629934775, 1.823016439315219062, -0.7507060404894276839 ) ) ;
#209278=CARTESIAN_POINT ( 'NONE',  ( 1.747554699363640607, -1.948627443588932806, 1.235768562340158194 ) ) ;
#209279=CARTESIAN_POINT ( 'NONE',  ( 2.471086628630547288, 1.751123931924388089, 0.8847596551376719631 ) ) ;
#209281=CARTESIAN_POINT ( 'NONE',  ( 5.946154108440814490, -0.9325515945646453142, 1.839819606017919718 ) ) ;
#209283=CARTESIAN_POINT ( 'NONE',  ( 4.100796195634116792, 1.845626398921360822, 0.8128187495666516771 ) ) ;
#209289=CARTESIAN_POINT ( 'NONE',  ( 2.377987901236592982, -2.106814941015792808, 0.5239127008311114109 ) ) ;
#209293=CARTESIAN_POINT ( 'NONE',  ( 2.987410616422137455, 1.320145714686842497, 1.325460448179466066 ) ) ;
#209294=CARTESIAN_POINT ( 'NONE',  ( 6.837200347746461127, -1.934230338078479772, 0.9651617863762137484 ) ) ;
#209295=DIRECTION ( 'NONE',  ( -1.000000000000000000, 0.000000000000000000, 0.000000000000000000 ) ) ;
#209296=CARTESIAN_POINT ( 'NONE',  ( 6.727182134110198497, 4.703735537933666500, 2.273690654489219032 ) ) ;
#209299=CARTESIAN_POINT ( 'NONE',  ( 1.699719973799845185, 1.319605273547658220, 1.384218846220357291 ) ) ;
#209300=CARTESIAN_POINT ( 'NONE',  ( 3.819032205515503708, -0.1302183858614604506, 1.765120429581680916 ) ) ;
#209302=CARTESIAN_POINT ( 'NONE',  ( 1.330556988563241561, 1.283596529665396169, -1.417643162000304935 ) ) ;
#209305=CARTESIAN_POINT ( 'NONE',  ( 6.380494711820015930, -0.5163536399260219012, -1.844617532318414632 ) ) ;
#209307=CARTESIAN_POINT ( 'NONE',  ( 0.7310241076574041097, -1.948878508384953356, -0.6990896207654460071 ) ) ;
#209310=CARTESIAN_POINT ( 'NONE',  ( 5.084763247618332649, -0.2297073032716222263, -1.856415652357709778 ) ) ;
#209311=CARTESIAN_POINT ( 'NONE',  ( 1.576486190600217663, -1.733098801405801304, -0.5742540608338757568 ) ) ;
#209312=CARTESIAN_POINT ( 'NONE',  ( 5.268293329372571776, 1.085216321637239023, 1.921556908365213312 ) ) ;
#209315=CARTESIAN_POINT ( 'NONE',  ( 2.594246270321644676, 0.9746516854327008650, -1.817902028900773459 ) ) ;
#209322=CARTESIAN_POINT ( 'NONE',  ( 5.582505937350194181, 1.236201877336528643, -1.660625051266072960 ) ) ;
#209324=CARTESIAN_POINT ( 'NONE',  ( 2.337400524717429207, -1.931973293601353392, 0.9696072025056484689 ) ) ;
#209326=CARTESIAN_POINT ( 'NONE',  ( 2.772133559515827184, 2.009754670806723098, -0.2000300323863890006 ) ) ;
#209333=CARTESIAN_POINT ( 'NONE',  ( 1.833220611596135363, -1.622487599052296670, -1.197302888167578683 ) ) ;
#209335=CARTESIAN_POINT ( 'NONE',  ( 6.480031355044912900, -2.148842909532014289, -0.4297212958329286736 ) ) ;
#209337=CARTESIAN_POINT ( 'NONE',  ( 4.394721148579957770, -1.856311205515799090, -0.4593126252911488572 ) ) ;
#209342=CARTESIAN_POINT ( 'NONE',  ( 3.480092364642515701, -2.014234743589532695, -0.09611699103692641910 ) ) ;
#209345=CARTESIAN_POINT ( 'NONE',  ( 4.787984082328099689, -0.8109719804370466578, 1.522229471167990233 ) ) ;
#209349=CARTESIAN_POINT ( 'NONE',  ( 3.989402248074361612, 1.353031944225962624, 1.291829963354161892 ) ) ;
#209351=CARTESIAN_POINT ( 'NONE',  ( 1.569279613544020568, 1.823957739939351619, 0.9794188589333228112 ) ) ;
#209353=ORIENTED_EDGE ( 'NONE', *, *, #59450, .T. ) ;
#209354=CARTESIAN_POINT ( 'NONE',  ( 6.287769681992382509, 1.731225344711059266, -0.5331814487182000573 ) ) ;
#209358=CARTESIAN_POINT ( 'NONE',  ( -0.1056357528139931640, -1.757099710744941312, -0.4406103525058014392 ) ) ;
#209361=CARTESIAN_POINT ( 'NONE',  ( 2.625153213768507854, -2.044362554934661791, 0.7897752707372793779 ) ) ;
#209363=CARTESIAN_POINT ( 'NONE',  ( 0.4847190467827041105, 1.876267867961832980, 0.5731238010058882226 ) ) ;
#209366=CARTESIAN_POINT ( 'NONE',  ( 5.413669558995096054, -1.219043080348445329, -1.477637860945772763 ) ) ;
#209375=CARTESIAN_POINT ( 'NONE',  ( 1.393688021309073433, 1.637156065531343740, 1.411701162175371893 ) ) ;
#209379=CARTESIAN_POINT ( 'NONE',  ( 4.717693524642503355, -1.790169364231732674, 0.3569235582787863570 ) ) ;
#209381=CARTESIAN_POINT ( 'NONE',  ( 1.001173315506132422, 1.609201512179364135, 1.138472824994830379 ) ) ;
#209382=CARTESIAN_POINT ( 'NONE',  ( 3.129067941553372645, 1.730785544086024696, 0.8136490247460312908 ) ) ;
#209384=CARTESIAN_POINT ( 'NONE',  ( 3.807052887859848855, -1.611515334864065840, 1.132039114057415308 ) ) ;
#209386=CARTESIAN_POINT ( 'NONE',  ( 5.899939537456503125, -0.7029524595547633758, -1.810543181819963321 ) ) ;
#209392=CARTESIAN_POINT ( 'NONE',  ( 4.301352856729808494, 1.706663192164651122, -0.8627939227693476321 ) ) ;
#209396=CARTESIAN_POINT ( 'NONE',  ( 5.215494488825547670, 1.647103507230001096, 1.157162265453457239 ) ) ;
#209398=CARTESIAN_POINT ( 'NONE',  ( 6.217409598193539999, -0.2183660865492654257, 1.812524795094340835 ) ) ;
#209399=CARTESIAN_POINT ( 'NONE',  ( 5.647672796105281279, 1.985869605424210649, -0.3494789899042491932 ) ) ;
#209400=CARTESIAN_POINT ( 'NONE',  ( 2.014207461368537455, 2.064961549741591185, -0.1501100615294431728 ) ) ;
#209412=CARTESIAN_POINT ( 'NONE',  ( 3.902719751800659775, -0.8955246652143248332, -1.484863070527132622 ) ) ;
#209414=CARTESIAN_POINT ( 'NONE',  ( 1.393514648303464165, -1.873246724434135313, 0.8816542684770898308 ) ) ;
#209415=CARTESIAN_POINT ( 'NONE',  ( 2.952857568058687043, -1.957288919824872186, -0.8077276291160383481 ) ) ;
#209420=CARTESIAN_POINT ( 'NONE',  ( 0.6902129346560643697, 1.017158767820530940, -1.686321398027894825 ) ) ;
#209425=CARTESIAN_POINT ( 'NONE',  ( 3.258078344973667662, 1.030780755083884115, 2.047500790377681845 ) ) ;
#209426=CARTESIAN_POINT ( 'NONE',  ( 0.1526014871912773629, -1.468541917219987836, 1.084465738218153064 ) ) ;
#209427=CARTESIAN_POINT ( 'NONE',  ( 3.568532368641282648, 0.6928216322696268969, 1.782650395559831180 ) ) ;
#209432=CARTESIAN_POINT ( 'NONE',  ( 1.793228464370033581, -0.1031022715946017104, -2.010704963445380411 ) ) ;
#209433=CARTESIAN_POINT ( 'NONE',  ( 1.797631089865757259, -1.417250949620936895, -1.356651810197152086 ) ) ;
#209437=CARTESIAN_POINT ( 'NONE',  ( 5.419903170966573924, 1.246048553727102659, -1.678571210107776324 ) ) ;
#209438=CARTESIAN_POINT ( 'NONE',  ( 3.783871084116468886, -0.8724064270978303393, 1.539809854060821603 ) ) ;
#209441=CARTESIAN_POINT ( 'NONE',  ( 6.017577161850602430, -1.268579900078286471, -1.909058160655076053 ) ) ;
#209442=CARTESIAN_POINT ( 'NONE',  ( 5.437372246358883388, 0.6999822053482355200, -1.593550356025658976 ) ) ;
#209445=CARTESIAN_POINT ( 'NONE',  ( 4.340949964944015527, -0.9985633389030469376, 1.417159075928013046 ) ) ;
#209446=CARTESIAN_POINT ( 'NONE',  ( 6.039545795398320926, 2.008403840061912859, -0.8252953610491889913 ) ) ;
#209448=CARTESIAN_POINT ( 'NONE',  ( 0.4271636869729276698, -1.812546591343185298, 1.094284096637233583 ) ) ;
#209449=CARTESIAN_POINT ( 'NONE',  ( 5.687500000000004441, -1.451031289060884077, 1.451031289061342378 ) ) ;
#209452=CARTESIAN_POINT ( 'NONE',  ( 2.995051018759773420, 1.652986441767102743, -0.9890191681132395329 ) ) ;
#209454=CARTESIAN_POINT ( 'NONE',  ( 0.2413015266095243083, 2.127564327900688390, 0.6385326005407893080 ) ) ;
#209456=CARTESIAN_POINT ( 'NONE',  ( -0.1409997244346122836, 0.7174646053854060179, -2.082770303449644977 ) ) ;
#209459=CARTESIAN_POINT ( 'NONE',  ( 3.035994277891720827, -2.140246456218936721, 0.5942984311890684435 ) ) ;
#209465=CARTESIAN_POINT ( 'NONE',  ( 0.7740648250077889481, 1.777010169924503558, -0.9530137779002674225 ) ) ;
#209467=CARTESIAN_POINT ( 'NONE',  ( 5.389153705970353592, 0.1484172631736270231, 2.057380146747369576 ) ) ;
#209472=CARTESIAN_POINT ( 'NONE',  ( 0.5789240690485557561, 1.654349777479852346, -0.6291145533634836529 ) ) ;
#209473=CARTESIAN_POINT ( 'NONE',  ( 6.258463337875916466, 1.656396116010181219, -0.5134576769376431038 ) ) ;
#209474=CARTESIAN_POINT ( 'NONE',  ( 5.724081574600810463, 1.679587015112851578, 0.4559996917168698261 ) ) ;
#209475=CARTESIAN_POINT ( 'NONE',  ( 3.333774467322860868, 1.029290431845871989, -2.048349661755991313 ) ) ;
#209477=CARTESIAN_POINT ( 'NONE',  ( 1.851249556194194179, 1.836288347861175785, -0.1344999175661651392 ) ) ;
#209481=CARTESIAN_POINT ( 'NONE',  ( 1.852308540880560850, 0.5694407911355814367, 1.734573797025913189 ) ) ;
#209482=CARTESIAN_POINT ( 'NONE',  ( 3.164685561777963230, 1.281361203394768111, 1.556908733426412450 ) ) ;
#209485=CARTESIAN_POINT ( 'NONE',  ( 4.489357033980984291, 1.882333632172785487, -0.9445240646021864084 ) ) ;
#209488=CARTESIAN_POINT ( 'NONE',  ( 2.506376218629560171, 2.069854378281150709, 0.05321039126485183068 ) ) ;
#209491=CARTESIAN_POINT ( 'NONE',  ( 4.512424090126602394, -2.120028616272570332, -0.05109941365945279423 ) ) ;
#209492=CARTESIAN_POINT ( 'NONE',  ( 6.639283661800273961, -1.628176093627232479, 0.8261057939347238310 ) ) ;
#209500=CARTESIAN_POINT ( 'NONE',  ( 6.310795917644286490, -0.5669512758468171487, -2.043305014803979525 ) ) ;
#209501=CARTESIAN_POINT ( 'NONE',  ( 1.395691461817370804, 1.594359505120213960, 1.375974583626845993 ) ) ;
#209504=CARTESIAN_POINT ( 'NONE',  ( 5.946130789595732935, -0.8379359121385165921, 1.661726607698276181 ) ) ;
#209512=CARTESIAN_POINT ( 'NONE',  ( 2.629291921057617554, 0.09916324773191761976, -1.959495597191794225 ) ) ;
#209513=CARTESIAN_POINT ( 'NONE',  ( 1.340939272977889951, 0.4221563536682856332, 2.119910705745978508 ) ) ;
#209518=CARTESIAN_POINT ( 'NONE',  ( 2.758840240711700531, -1.728971274941538017, -0.1308756186972348801 ) ) ;
#209519=CARTESIAN_POINT ( 'NONE',  ( 1.939017046771335240, 0.6676067653633214194, -1.607389671016548949 ) ) ;
#209522=CARTESIAN_POINT ( 'NONE',  ( 2.442732317853496760, 1.238130588059358717, 1.591075322344523535 ) ) ;
#209523=CARTESIAN_POINT ( 'NONE',  ( 6.925078400183557470, 1.239878965558613322, 2.257517960274835200 ) ) ;
#209525=CARTESIAN_POINT ( 'NONE',  ( 1.200003858469798956, -1.971640592295399896, -0.002163809803111190443 ) ) ;
#209527=CARTESIAN_POINT ( 'NONE',  ( 5.502191098127390489, -0.8541586074963626318, 1.711093258865265643 ) ) ;
#209532=CARTESIAN_POINT ( 'NONE',  ( 1.031905740238812097, -1.969920897724128483, 0.4447463068311637846 ) ) ;
#209534=CARTESIAN_POINT ( 'NONE',  ( 5.825286519090714599, -0.06434016213947668650, 2.306860349555530654 ) ) ;
#209535=CARTESIAN_POINT ( 'NONE',  ( 5.476992472119650124, 1.812042599547862176, 0.7524171098330989516 ) ) ;
#209536=CARTESIAN_POINT ( 'NONE',  ( 3.520314338623427020, 0.8779579967637550775, 1.754372790864023646 ) ) ;
#209540=CARTESIAN_POINT ( 'NONE',  ( 0.6907973960054912821, 1.599150545848356364, -1.387813827701115610 ) ) ;
#209543=CARTESIAN_POINT ( 'NONE',  ( 1.517261703430743625, -1.021610662766696764, -1.531488883528262290 ) ) ;
#209546=CARTESIAN_POINT ( 'NONE',  ( 3.234745892528373634, 1.342314639517484087, -1.641720766639111817 ) ) ;
#209550=CARTESIAN_POINT ( 'NONE',  ( 3.497389175668437211, 1.622225323665491326, 1.270757995044344391 ) ) ;
#209552=CARTESIAN_POINT ( 'NONE',  ( 0.7844012160764175512, 1.623964078452419857, -0.8677550623670119423 ) ) ;
#209554=CARTESIAN_POINT ( 'NONE',  ( -0.02244404828160087226, 6.946777552644228138, -2.784171975256703124 ) ) ;
#209556=CARTESIAN_POINT ( 'NONE',  ( 0.3642759247451561322, 2.182245240920151375, -0.3280614795862640820 ) ) ;
#209557=CARTESIAN_POINT ( 'NONE',  ( 2.987861924072153563, 1.597690390425403173, 1.602079265715735223 ) ) ;
#209559=CARTESIAN_POINT ( 'NONE',  ( 2.408236768384981019, -1.806978867004911171, -0.1295660047265032311 ) ) ;
#209560=CARTESIAN_POINT ( 'NONE',  ( 3.063600739116902449, 1.219304168433880564, 1.477546071989847665 ) ) ;
#209561=CARTESIAN_POINT ( 'NONE',  ( 4.281733463571851139, -1.982135700070002615, 0.5980053909793592304 ) ) ;
#209563=CARTESIAN_POINT ( 'NONE',  ( 1.657037912627358001, -1.689797944177928279, -1.015304737199155483 ) ) ;
#209564=CARTESIAN_POINT ( 'NONE',  ( 0.3758376374219556393, 1.106279473776916378, 1.576890456013874120 ) ) ;
#209565=CARTESIAN_POINT ( 'NONE',  ( 3.291731440620565330, -0.7593194595177065187, 1.709801165022284408 ) ) ;
#209566=CARTESIAN_POINT ( 'NONE',  ( 2.842713172187049331, 2.290369893530233902, 0.2817356681584815004 ) ) ;
#209568=CARTESIAN_POINT ( 'NONE',  ( 2.558860573628952473, 1.496680913221506870, -1.105902276818030217 ) ) ;
#209571=CARTESIAN_POINT ( 'NONE',  ( 0.2392226684038156193, -0.1392734953599965297, -2.030321344557210139 ) ) ;
#209575=CARTESIAN_POINT ( 'NONE',  ( 6.264693295067493395, -1.491911088229242788, 1.486630704232002609 ) ) ;
#209578=CARTESIAN_POINT ( 'NONE',  ( 5.589210384452774960, 1.909260796540311000, -1.013481389624170115 ) ) ;
#209579=CARTESIAN_POINT ( 'NONE',  ( 6.633471379370169174, -0.1512203817595116073, 1.986116118494333227 ) ) ;
#209583=CARTESIAN_POINT ( 'NONE',  ( 6.825078400183553384, 4.701740280048592346, 2.318362489372997270 ) ) ;
#209586=CARTESIAN_POINT ( 'NONE',  ( 4.610564714392807240, 1.931124171932835809, 0.5807562064495259690 ) ) ;
#209591=CARTESIAN_POINT ( 'NONE',  ( 6.121977807712331909, -1.196819783530624015, -1.799967629666970881 ) ) ;
#209597=CARTESIAN_POINT ( 'NONE',  ( 6.591432905763006111, -0.4393008961055907546, 1.975236973087670656 ) ) ;
#209599=CARTESIAN_POINT ( 'NONE',  ( 6.589320575229281829, 7.629137130509070275, 2.703262396134015866 ) ) ;
#209600=CARTESIAN_POINT ( 'NONE',  ( 1.892754278755165664, 1.501794282950255965, -0.8482797957840328973 ) ) ;
#209604=CARTESIAN_POINT ( 'NONE',  ( 1.018396826474694761, 1.632260513341069252, 0.6844030214382245125 ) ) ;
#209605=CARTESIAN_POINT ( 'NONE',  ( 1.541653539051958122, -1.894817064119158401, 0.6801782934461576557 ) ) ;
#209607=CARTESIAN_POINT ( 'NONE',  ( 3.821466819111440927, -0.1649144712266135959, 2.200675313789305143 ) ) ;
#209609=CARTESIAN_POINT ( 'NONE',  ( 5.278266929526361118, -1.155484533919543422, -1.837868763204909994 ) ) ;
#209614=CARTESIAN_POINT ( 'NONE',  ( 3.369896858953733698, 0.5134250039646214292, -2.057278921464212207 ) ) ;
#209615=CARTESIAN_POINT ( 'NONE',  ( 3.321888824615967906, 0.9040932542298124597, -1.802426844439278142 ) ) ;
#209616=CARTESIAN_POINT ( 'NONE',  ( 3.005918303229858424, -0.7299923727487073188, 1.658169170237313583 ) ) ;
#209623=CARTESIAN_POINT ( 'NONE',  ( 6.445924739416000193, 0.6936395621829589686, -1.688995215704327313 ) ) ;
#209625=CARTESIAN_POINT ( 'NONE',  ( 1.780357001937494799, -0.5149467098792412934, -1.845104466984174962 ) ) ;
#209632=CARTESIAN_POINT ( 'NONE',  ( 5.084929678302337663, -0.2608814864752464491, -2.145832476913120068 ) ) ;
#209635=CARTESIAN_POINT ( 'NONE',  ( 2.918346969001627045, -2.117983955170518851, 0.1081942149789016649 ) ) ;
#209636=CARTESIAN_POINT ( 'NONE',  ( -0.1298852118744256712, 0.2531197755418754247, -1.761387242530809250 ) ) ;
#209638=CARTESIAN_POINT ( 'NONE',  ( 4.780523264075623224, -1.911459794658072697, -0.4817293046612564633 ) ) ;
#209639=CARTESIAN_POINT ( 'NONE',  ( 6.310809538426106258, -0.5167911955388967415, -1.841158844219364044 ) ) ;
#209641=CARTESIAN_POINT ( 'NONE',  ( 5.841034576552271318, -1.817201478619561383, -1.086431860386444681 ) ) ;
#209643=CARTESIAN_POINT ( 'NONE',  ( 6.777801591175982132, -1.910752814866881089, 0.4773036857264860156 ) ) ;
#209644=CARTESIAN_POINT ( 'NONE',  ( 2.519391418834667995, -1.118305101016278558, -1.587446049422422956 ) ) ;
#209648=CARTESIAN_POINT ( 'NONE',  ( 3.134800171978794125, -1.843606372480216082, 0.9858348089602610997 ) ) ;
#209651=CARTESIAN_POINT ( 'NONE',  ( 0.08225775502835978858, -1.185065876811146834, 1.370160863432666076 ) ) ;
#209653=CARTESIAN_POINT ( 'NONE',  ( 5.707716145626243964, -0.5396369327701348029, 2.139774205771049154 ) ) ;
#209655=CARTESIAN_POINT ( 'NONE',  ( 3.575398329460587554, 0.05639400328332971890, -2.206221599391814170 ) ) ;
#209658=CARTESIAN_POINT ( 'NONE',  ( 1.875505643822904300, 0.3255412885708880433, -1.884197853084010443 ) ) ;
#209660=CARTESIAN_POINT ( 'NONE',  ( 5.248515149483166553, -2.054309126314420642, -0.2569322651706855143 ) ) ;
#209662=CARTESIAN_POINT ( 'NONE',  ( 3.415052781332720055, 1.953485055394106107, 0.9259690932504063277 ) ) ;
#209663=CARTESIAN_POINT ( 'NONE',  ( 4.335597073515660149, 0.9364531651635084053, -1.981528385891350386 ) ) ;
#209665=DIRECTION ( 'NONE',  ( 2.949029909160572061E-17, 1.000000000000000000, -8.673600428462503284E-15 ) ) ;
#209671=CARTESIAN_POINT ( 'NONE',  ( 0.6158615555539399544, 0.1511424999406512648, 2.010826230049263863 ) ) ;
#209674=CARTESIAN_POINT ( 'NONE',  ( 4.135645376760338721, 1.951069878921590783, -0.6927527371542248069 ) ) ;
#209675=CARTESIAN_POINT ( 'NONE',  ( 4.195867187722844172, -0.7361232629885716694, 1.780507395703424978 ) ) ;
#209676=CARTESIAN_POINT ( 'NONE',  ( -0.0003749349099593791675, -1.976945657698804704, 0.3961262320883383592 ) ) ;
#209680=CARTESIAN_POINT ( 'NONE',  ( 4.170725306337518923, 1.395817779951594950, -1.389658704579323611 ) ) ;
#209681=CARTESIAN_POINT ( 'NONE',  ( 0.1467655724766807612, -1.757430454515636509, 1.308964887167405111 ) ) ;
#209682=CARTESIAN_POINT ( 'NONE',  ( 3.562960707638890501, -1.610701098693729350, -0.8595150645765645692 ) ) ;
#209689=CARTESIAN_POINT ( 'NONE',  ( 1.399689850468607277, -0.6632477835330424787, -1.717811453623831808 ) ) ;
#209690=CARTESIAN_POINT ( 'NONE',  ( 5.133069374350656133, 1.861756548879553996, 0.7665277172332859434 ) ) ;
#209691=CARTESIAN_POINT ( 'NONE',  ( 0.5448069426677571991, 2.143542105210020754, -0.8297726512136813781 ) ) ;
#209692=CARTESIAN_POINT ( 'NONE',  ( 5.049637047142223167, 1.450995767963231264, 1.320413740667214508 ) ) ;
#209698=CARTESIAN_POINT ( 'NONE',  ( 1.452797965663179314, -1.794991982752047965, -1.071751678227941929 ) ) ;
#209699=CARTESIAN_POINT ( 'NONE',  ( 6.561408083364261401, 0.2975169865880605835, -1.744492507556465011 ) ) ;
#209701=CARTESIAN_POINT ( 'NONE',  ( -0.1102773484824119132, -0.006951161900758253548, -2.203378182130751206 ) ) ;
#209702=CARTESIAN_POINT ( 'NONE',  ( 1.540153114873343609, -1.470452955542918660, 0.9307524122482965234 ) ) ;
#209706=CARTESIAN_POINT ( 'NONE',  ( 1.927930615940620873, 0.9947386370207593753, -1.408936266059911624 ) ) ;
#209707=CARTESIAN_POINT ( 'NONE',  ( 2.191216702865448784, 1.696344223602393786, 1.387594652289561248 ) ) ;
#209708=CARTESIAN_POINT ( 'NONE',  ( 4.371826309796801979, 2.140994599346605742, -0.5347268394074317088 ) ) ;
#209710=CARTESIAN_POINT ( 'NONE',  ( 2.342849523213458962, -2.128499089237919417, -0.4270345827348878132 ) ) ;
#209711=CARTESIAN_POINT ( 'NONE',  ( 1.541335573940459058, -1.321205422867760548, -1.260230113935792318 ) ) ;
#209712=CARTESIAN_POINT ( 'NONE',  ( 3.854788253679425125, -1.977088355604763148, -0.7582873983895296321 ) ) ;
#209713=CARTESIAN_POINT ( 'NONE',  ( 6.639320575229254118, 4.698690022235154196, 2.459427960261594492 ) ) ;
#209716=CARTESIAN_POINT ( 'NONE',  ( 3.351411269679291038, 0.5553372447333758677, -2.223988721106509470 ) ) ;
#209720=CARTESIAN_POINT ( 'NONE',  ( 6.445936322256165418, -1.448296609194921647, -1.684281199878513657 ) ) ;
#209726=CARTESIAN_POINT ( 'NONE',  ( 6.825078400183544503, 2.075476428726834577, 2.163873318353096931 ) ) ;
#209729=CARTESIAN_POINT ( 'NONE',  ( 3.832657856672664565, 0.6767144645295587457, -1.899618369658891748 ) ) ;
#209731=CARTESIAN_POINT ( 'NONE',  ( 2.571201674526869763, 1.840362857814400455, 0.9314759700368970829 ) ) ;
#209732=DIRECTION ( 'NONE',  ( -1.000000000000000000, 0.000000000000000000, 0.000000000000000000 ) ) ;
#209736=CARTESIAN_POINT ( 'NONE',  ( 5.595707529797693702, -2.191629465999441084, -0.002916574791289594515 ) ) ;
#209737=CARTESIAN_POINT ( 'NONE',  ( 2.391250195717840477, -0.7743161457766101208, -1.862016636315230844 ) ) ;
#209738=CARTESIAN_POINT ( 'NONE',  ( 2.050122339901743196, -1.422379512129726908, 1.169167124061460949 ) ) ;
#209741=CARTESIAN_POINT ( 'NONE',  ( 6.821331453475777629, -0.1281762050449504198, 1.796388512460028286 ) ) ;
#209742=CARTESIAN_POINT ( 'NONE',  ( 0.01878015289935238558, -2.097885004189947278, 0.9400277066241318202 ) ) ;
#209744=CARTESIAN_POINT ( 'NONE',  ( 5.946200445400964263, 2.259567648220105252, 0.1180026366056959042 ) ) ;
#209746=CARTESIAN_POINT ( 'NONE',  ( 1.365998295032941900, 2.074639164447332540, -0.3615360007043573187 ) ) ;
#209756=CARTESIAN_POINT ( 'NONE',  ( 2.479030958227887549, -1.528377378988081015, 1.612298682912993275 ) ) ;
#209760=CARTESIAN_POINT ( 'NONE',  ( 4.598074495912658044, 0.8407358649686399454, -1.772743347989129692 ) ) ;
#209769=CARTESIAN_POINT ( 'NONE',  ( 3.234745892528373634, 1.342314639517484087, -1.641720766639111817 ) ) ;
#209771=CARTESIAN_POINT ( 'NONE',  ( 4.610339536224768331, -0.9213992672730475508, -1.955631277330005968 ) ) ;
#209772=CARTESIAN_POINT ( 'NONE',  ( 3.667381569930192597, 1.025862638139760419, 1.528780434079744843 ) ) ;
#209775=CARTESIAN_POINT ( 'NONE',  ( 5.244012475127576955, 0.5104456934865635453, 1.663790013937071599 ) ) ;
#209779=CARTESIAN_POINT ( 'NONE',  ( 2.764712544972968811, -1.491509591961351910, 1.564943835847030229 ) ) ;
#209780=CARTESIAN_POINT ( 'NONE',  ( 5.325545996062735377, -1.462220743079494012, 1.388274341532859335 ) ) ;
#209782=CARTESIAN_POINT ( 'NONE',  ( 2.624079441566569582, -1.243859440641072123, -1.767801033134681843 ) ) ;
#209783=CARTESIAN_POINT ( 'NONE',  ( 3.444560810740458390, 0.4755345817112103246, 1.913044316819292767 ) ) ;
#209786=CARTESIAN_POINT ( 'NONE',  ( 4.282717048480193078, 1.733172068543160416, -0.8763712590400226654 ) ) ;
#209797=CARTESIAN_POINT ( 'NONE',  ( 1.852830919558448697, 0.6925466627333074499, 2.095365425716289032 ) ) ;
#209799=CARTESIAN_POINT ( 'NONE',  ( 6.807479307002794577, -1.573682814073861902, -1.171087784426767753 ) ) ;
#209804=CARTESIAN_POINT ( 'NONE',  ( 6.111994396789379280, -2.190734547077430872, 0.2660306753756238041 ) ) ;
#209805=CARTESIAN_POINT ( 'NONE',  ( 5.437399513225577685, 0.7426265630364609072, -1.684910612069365321 ) ) ;
#209810=CARTESIAN_POINT ( 'NONE',  ( 6.117454236943913770, 1.763945953808215394, 1.176740244630887222 ) ) ;
#209813=CARTESIAN_POINT ( 'NONE',  ( 0.1279053400650804195, -1.267571945882491447, -1.625495855733450457 ) ) ;
#209815=CARTESIAN_POINT ( 'NONE',  ( 1.943593235818155351, 1.280450557881509299, 1.350794863662147627 ) ) ;
#209816=CARTESIAN_POINT ( 'NONE',  ( 3.966218424140379728, -1.719484690100345325, -0.6589542199007536460 ) ) ;
#209820=CARTESIAN_POINT ( 'NONE',  ( 6.610000000000006537, 0.002781820520842553934, 2.000159646111852929 ) ) ;
#209822=CARTESIAN_POINT ( 'NONE',  ( 3.457846583235091753, 0.5364296187198510646, -2.140574738106671759 ) ) ;
#209823=CARTESIAN_POINT ( 'NONE',  ( 5.835331047353732536, -2.048883276207621229, 0.9597388403507837173 ) ) ;
#209825=CARTESIAN_POINT ( 'NONE',  ( 5.642768253578701376, 1.748184277621564808, 0.4749025624241067223 ) ) ;
#209826=CARTESIAN_POINT ( 'NONE',  ( 0.1808755166769344669, 1.673851406602990366, -1.124249698880399162 ) ) ;
#209828=CARTESIAN_POINT ( 'NONE',  ( 6.631728656526095556, -1.223761959379562114, -1.414937998750566361 ) ) ;
#209829=CARTESIAN_POINT ( 'NONE',  ( 6.129550632656369125, -0.2293275368827427663, 1.898405681093485953 ) ) ;
#209831=CARTESIAN_POINT ( 'NONE',  ( 0.7427767429722329506, -1.606530860214189893, 0.9580933318182258684 ) ) ;
#209832=CARTESIAN_POINT ( 'NONE',  ( 0.7257964430846426396, 0.8128130212789463904, -1.845628942776005088 ) ) ;
#209834=CARTESIAN_POINT ( 'NONE',  ( 4.037795408393930252, -1.452196710024173276, -1.525570609991099502 ) ) ;
#209838=CARTESIAN_POINT ( 'NONE',  ( 3.269790213696788683, 0.4867576797993823368, -1.960144559866239700 ) ) ;
#209841=CARTESIAN_POINT ( 'NONE',  ( 2.741676502816026595, -1.599691942034554337, -1.453933697666408120 ) ) ;
#209847=CARTESIAN_POINT ( 'NONE',  ( 0.4148109920584437948, 0.8315006815404235585, 2.005833495578440928 ) ) ;
#209852=CARTESIAN_POINT ( 'NONE',  ( 1.909981697816802049, -1.036543071415759298, -1.930953618257096993 ) ) ;
#209854=CARTESIAN_POINT ( 'NONE',  ( 2.149658728627835469, -1.817393572686412107, -1.347411789871997057 ) ) ;
#209861=CARTESIAN_POINT ( 'NONE',  ( 3.919032125857401905, -0.1322120426517567060, 1.764875357724977167 ) ) ;
#209863=CARTESIAN_POINT ( 'NONE',  ( 0.4464868854077256866, 2.100361318156780399, 0.1544987475943972732 ) ) ;
#209867=CARTESIAN_POINT ( 'NONE',  ( 6.415638736316127577, -1.319241173714128745, -1.525034172108488573 ) ) ;
#209871=CARTESIAN_POINT ( 'NONE',  ( 3.537841792810627606, 0.8420186812403904764, -1.670516725672297031 ) ) ;
#209872=CARTESIAN_POINT ( 'NONE',  ( 4.627825472248149552, 2.009385113269086087, -0.4979276649561757417 ) ) ;
#209880=CARTESIAN_POINT ( 'NONE',  ( 3.525789274851616639, 1.914599547803575330, -0.4273510147508317591 ) ) ;
#209882=CARTESIAN_POINT ( 'NONE',  ( 1.089219988750099732, 1.203171814842165288, -1.617568698395126292 ) ) ;
#209886=CARTESIAN_POINT ( 'NONE',  ( 0.9306671693925671063, 0.1315677519515070781, 1.865966016356377821 ) ) ;
#209888=CARTESIAN_POINT ( 'NONE',  ( 3.515888537569244132, -0.5802020150980004010, 1.927815774739343180 ) ) ;
#209890=CARTESIAN_POINT ( 'NONE',  ( 2.267339977356534142, 1.934377090824404455, -0.8611398932509596316 ) ) ;
#209891=CARTESIAN_POINT ( 'NONE',  ( 6.825078400183544503, 6.034152930826206962, 2.739236550662868197 ) ) ;
#209892=CARTESIAN_POINT ( 'NONE',  ( 3.332542965736586371, -1.235447621225284509, 1.661183390374972424 ) ) ;
#209894=CARTESIAN_POINT ( 'NONE',  ( 0.4860219701983969909, -2.075441973172939214, -0.2518264690121001514 ) ) ;
#209896=CARTESIAN_POINT ( 'NONE',  ( 5.561492448144861989, 0.3540975402388062965, -1.790731494587729067 ) ) ;
#209901=CARTESIAN_POINT ( 'NONE',  ( 6.475609205405274515, 2.113627995098281254, -0.6344055572156809264 ) ) ;
#209903=CARTESIAN_POINT ( 'NONE',  ( 4.617770051018644573, -0.5065499601877522240, 1.843912185298258066 ) ) ;
#209921=CARTESIAN_POINT ( 'NONE',  ( 2.377736956781382638, -1.911501772163497481, 0.4737601246572603064 ) ) ;
#209922=CARTESIAN_POINT ( 'NONE',  ( 2.987907820627898836, -2.013986125068282007, 0.1017690403029153645 ) ) ;
#209925=CARTESIAN_POINT ( 'NONE',  ( 6.727182134110222478, 7.629137130509071163, 2.789055895399249252 ) ) ;
#209926=CARTESIAN_POINT ( 'NONE',  ( 4.119203469048302146, -2.097337170177868693, 0.6352863671069891582 ) ) ;
#209928=CARTESIAN_POINT ( 'NONE',  ( 2.098540742119249458, -0.5114569845777928725, -1.857200404858405207 ) ) ;
#209931=CARTESIAN_POINT ( 'NONE',  ( 0.1329588055935760349, 4.094961471249922269, -2.400852151441670745 ) ) ;
#209938=CARTESIAN_POINT ( 'NONE',  ( 6.005383971424570255, -1.826508537601937432, 0.2321369796495567073 ) ) ;
#209939=CARTESIAN_POINT ( 'NONE',  ( 2.139316306618759711, 0.002201468654887753229, 2.013265973851806834 ) ) ;
#209940=CARTESIAN_POINT ( 'NONE',  ( 3.901994836520364718, 0.3331327188077978785, 2.274008445091058928 ) ) ;
#209941=CARTESIAN_POINT ( 'NONE',  ( -0.1291982275798443380, 0.7147424134107607241, -2.157361641090648874 ) ) ;
#209942=CARTESIAN_POINT ( 'NONE',  ( 2.535811996613965391, 1.140603387277869585, 1.470366759043324478 ) ) ;
#209944=CARTESIAN_POINT ( 'NONE',  ( 5.080287894202283105, 0.9478536798121822704, 1.660923459347658282 ) ) ;
#209947=CARTESIAN_POINT ( 'NONE',  ( 5.073812392315714348, -1.160337598488449196, 1.738990438290926921 ) ) ;
#209948=CARTESIAN_POINT ( 'NONE',  ( 3.397188523315307407, 1.473948685399184333, 1.151750840393983344 ) ) ;
#209954=CARTESIAN_POINT ( 'NONE',  ( 6.604117967919251875, -1.724316898024110811, 0.05080964468639861259 ) ) ;
#209956=CARTESIAN_POINT ( 'NONE',  ( 1.089978434334002433, -0.4226591196558672214, 1.681707840898168937 ) ) ;
#209959=CARTESIAN_POINT ( 'NONE',  ( 5.770445249457275771, -0.9694031614774318850, -1.942678356158732855 ) ) ;
#209960=CARTESIAN_POINT ( 'NONE',  ( 4.916531288042031989, 1.256637652550334883, -1.324621001416517840 ) ) ;
#209961=CARTESIAN_POINT ( 'NONE',  ( 1.938261246079517219, -1.053878627966830184, 1.654468565904606558 ) ) ;
#209962=CARTESIAN_POINT ( 'NONE',  ( 0.08772780073029294579, -0.5597381814076306528, 2.041856491864118439 ) ) ;
#209965=CARTESIAN_POINT ( 'NONE',  ( 2.719513590175401063, 1.792643918890064247, 1.132349250948051500 ) ) ;
#209969=CARTESIAN_POINT ( 'NONE',  ( 0.5146170122050791607, 0.7890519337857507809, 1.914186188738425942 ) ) ;
#209972=CARTESIAN_POINT ( 'NONE',  ( 2.965722808067718486, -1.817245444403335020, -1.277177951966218084 ) ) ;
#209974=CARTESIAN_POINT ( 'NONE',  ( 1.143681411288837824, 0.9377895679426456743, 2.098875006570381618 ) ) ;
#209976=CARTESIAN_POINT ( 'NONE',  ( 5.330950330247254065, -1.940297947978512960, -0.6998911787638012472 ) ) ;
#209979=CARTESIAN_POINT ( 'NONE',  ( 0.2329586101569866563, 0.2513371725885656938, -1.880733749865989068 ) ) ;
#209981=CARTESIAN_POINT ( 'NONE',  ( 6.093280168761200599, -0.6138376400152152357, 1.736067454429328416 ) ) ;
#209985=CARTESIAN_POINT ( 'NONE',  ( 3.082691909922595563, -0.1251556739016151387, -1.720276473149193297 ) ) ;
#209986=CARTESIAN_POINT ( 'NONE',  ( 0.8664231474371617558, -1.968446048378743374, -0.4370742218882397445 ) ) ;
#209987=CARTESIAN_POINT ( 'NONE',  ( 2.672825289193903942, 1.627854652907471777, 1.623211659370107363 ) ) ;
#209989=CARTESIAN_POINT ( 'NONE',  ( 2.882378335548450465, -1.165601267607863978, 1.938926327226223822 ) ) ;
#209990=CARTESIAN_POINT ( 'NONE',  ( 5.039724086851991913, -1.488677873513370331, -1.490019843855681536 ) ) ;
#209992=CARTESIAN_POINT ( 'NONE',  ( 4.147515422935190266, 0.5979684684156804098, -1.665763606213203518 ) ) ;
#209995=CARTESIAN_POINT ( 'NONE',  ( -0.01123377539814351088, -0.5141151231248282105, -2.242550872947962404 ) ) ;
#209996=CARTESIAN_POINT ( 'NONE',  ( 4.962772036422566480, 0.1772586797372834311, -1.832584332494808121 ) ) ;
#210000=CARTESIAN_POINT ( 'NONE',  ( 4.084055714405177895, -2.167483682527316713, -0.3223708474724209516 ) ) ;
#210006=CARTESIAN_POINT ( 'NONE',  ( 2.912629423498619197, 1.395154039405178903, -1.328744637545350882 ) ) ;
#210009=CARTESIAN_POINT ( 'NONE',  ( 0.3873739525321840960, -2.094434250752406079, -0.7407286751721677831 ) ) ;
#210017=CARTESIAN_POINT ( 'NONE',  ( 2.401564422585287684, -0.6675299454344629790, -1.607540830017651023 ) ) ;
#210021=CARTESIAN_POINT ( 'NONE',  ( 6.455963997168007396, 2.156291961557708525, -0.1537611777119098910 ) ) ;
#210022=CARTESIAN_POINT ( 'NONE',  ( 6.057081135787192316, 1.604708697955498087, -1.128374156723031430 ) ) ;
#210026=CARTESIAN_POINT ( 'NONE',  ( 5.331013795412237855, 0.1550192300789655642, 2.156197635354038411 ) ) ;
#210030=CARTESIAN_POINT ( 'NONE',  ( 0.2450992160058732550, -1.441561472518913867, -1.191725768352129622 ) ) ;
#210031=CARTESIAN_POINT ( 'NONE',  ( 5.923113090906284128, 0.7054357044574584013, 1.584025686543149680 ) ) ;
#210034=CARTESIAN_POINT ( 'NONE',  ( 2.911879292414458309, -1.082406496695037301, -1.905547650945007776 ) ) ;
#210035=CARTESIAN_POINT ( 'NONE',  ( 3.434905211628926480, 2.250879548190734436, 0.5077644651142860788 ) ) ;
#210036=CARTESIAN_POINT ( 'NONE',  ( 5.993449436079309578, 1.557461279572001756, 1.349564693925601189 ) ) ;
#210037=CARTESIAN_POINT ( 'NONE',  ( 0.9021669503554888836, 1.471007182523446311, -1.267884427665219471 ) ) ;
#210042=CARTESIAN_POINT ( 'NONE',  ( 4.289387122732970958, -0.003046686910593982868, -2.120778211268215419 ) ) ;
#210044=CARTESIAN_POINT ( 'NONE',  ( 1.916638904718031000, -1.319229391439219246, -1.525043083973671498 ) ) ;
#210046=CARTESIAN_POINT ( 'NONE',  ( 5.245248717291847385, -1.895131572898335115, 1.130396782059706950 ) ) ;
#210055=CARTESIAN_POINT ( 'NONE',  ( 5.014554672588167783, 1.422794387333496946, -1.491179163509145811 ) ) ;
#210060=CARTESIAN_POINT ( 'NONE',  ( 4.178382104804970076, 0.9538709814062135139, 1.780240436319034503 ) ) ;
#210065=CARTESIAN_POINT ( 'NONE',  ( 3.204032760728621643, -2.058606879712703286, 0.09948017704831073338 ) ) ;
#210066=CARTESIAN_POINT ( 'NONE',  ( 3.358046224211252095, 0.04667712216412447934, -2.016033814150198999 ) ) ;
#210073=CARTESIAN_POINT ( 'NONE',  ( 2.741564358335503382, -1.928455994415989139, -0.5879317209081732498 ) ) ;
#210074=CARTESIAN_POINT ( 'NONE',  ( 2.361056629804247020, 1.805642548105116596, -0.3588866333120652174 ) ) ;
#210075=CARTESIAN_POINT ( 'NONE',  ( 0.6808296902291348651, -1.277277952767090774, 1.921808783382691788 ) ) ;
#210077=CARTESIAN_POINT ( 'NONE',  ( 2.882270108570818223, -1.113908571083363164, 1.852364028112465810 ) ) ;
#210083=CARTESIAN_POINT ( 'NONE',  ( 0.8658264364783776479, 0.9185255527898968930, 1.629538061279064642 ) ) ;
#210084=CARTESIAN_POINT ( 'NONE',  ( 5.243030984088811408, -1.691212405323471835, 1.012918505260449464 ) ) ;
#210088=CARTESIAN_POINT ( 'NONE',  ( 0.04788047853313340263, -1.708876078042343316, -1.396090968258607790 ) ) ;
#210089=CARTESIAN_POINT ( 'NONE',  ( 6.426242046702522082, 1.060841730010402495, 1.777776562702712226 ) ) ;
#210092=CARTESIAN_POINT ( 'NONE',  ( 6.639320575229257670, 1.230867875982581738, 2.315960674347458781 ) ) ;
#210093=CARTESIAN_POINT ( 'NONE',  ( 4.909034519618480807, 1.714790629392642707, 0.9726076082038226378 ) ) ;
#210094=CARTESIAN_POINT ( 'NONE',  ( 6.152604576718359475, 1.998398145963925954, 0.2921455800133450631 ) ) ;
#210096=CARTESIAN_POINT ( 'NONE',  ( 4.424672798056923817, 1.421823072290354872, -1.817590327873227052 ) ) ;
#210097=CARTESIAN_POINT ( 'NONE',  ( 2.202078444200939789, 0.7933530804136761372, -1.904077301569401914 ) ) ;
#210104=CARTESIAN_POINT ( 'NONE',  ( 4.404835846824251888, 0.5749587956990888094, 2.093619418667266530 ) ) ;
#210106=CARTESIAN_POINT ( 'NONE',  ( 4.282634502089007533, 1.642705626968201216, -0.8318752211165170163 ) ) ;
#210109=CARTESIAN_POINT ( 'NONE',  ( 5.038714576072483631, -1.879839391954684746, 1.126354835186346603 ) ) ;
#210111=CARTESIAN_POINT ( 'NONE',  ( 6.297788943421148922, -0.7692995465161235336, 2.127847719713715335 ) ) ;
#210118=CARTESIAN_POINT ( 'NONE',  ( 0.2855648877363594629, -0.8402267237041045611, 1.557686187855854554 ) ) ;
#210119=CARTESIAN_POINT ( 'NONE',  ( 4.863935948449842783, 0.6292040250746065988, -1.912316011988722586 ) ) ;
#210121=CARTESIAN_POINT ( 'NONE',  ( 4.313572747864121482, -0.3622951029728087580, 2.074398424781583206 ) ) ;
#210122=CARTESIAN_POINT ( 'NONE',  ( 2.530754833220005384, -1.591195339209892312, 1.066270812275710966 ) ) ;
#210124=CARTESIAN_POINT ( 'NONE',  ( 3.631270037613967716, 0.05078019485712419873, -1.969077574667767783 ) ) ;
#210125=CARTESIAN_POINT ( 'NONE',  ( 5.168225562285083896, 2.017301038980311656, -0.1031631561184200713 ) ) ;
#210126=CARTESIAN_POINT ( 'NONE',  ( 2.149089010626914931, -1.500894351328721621, -1.116326037436713881 ) ) ;
#210127=CARTESIAN_POINT ( 'NONE',  ( 5.127475435434773132, -1.636205250265274191, 0.5461684234016728201 ) ) ;
#210128=CARTESIAN_POINT ( 'NONE',  ( 1.810667312839256304, -0.5133170510521027907, -1.842115474350584980 ) ) ;
#210130=CARTESIAN_POINT ( 'NONE',  ( 1.594636444620714633, -2.196503929104542951, -0.2137616909994101977 ) ) ;
#210138=CARTESIAN_POINT ( 'NONE',  ( 1.486871883557450369, 1.994755712061954123, 0.5540851298423480342 ) ) ;
#210143=CARTESIAN_POINT ( 'NONE',  ( 0.2057307448365216507, 1.498047248056989522, 1.354806506954453482 ) ) ;
#210147=CARTESIAN_POINT ( 'NONE',  ( 6.883263157960391787, -0.001104538646235289417, 1.946037152736757925 ) ) ;
#210149=CARTESIAN_POINT ( 'NONE',  ( 4.534529724472468715, 1.956261425488527106, -0.4871295050740409582 ) ) ;
#210150=CARTESIAN_POINT ( 'NONE',  ( 4.663251631000405517, 1.785207739607551414, -0.6954431434487169383 ) ) ;
#210152=CARTESIAN_POINT ( 'NONE',  ( 2.542740116143254347, -1.820367712357463530, 1.220030464664762393 ) ) ;
#210155=CARTESIAN_POINT ( 'NONE',  ( 5.625249212676971311, 1.777412282398885823, 0.9453524948108845694 ) ) ;
#210159=CARTESIAN_POINT ( 'NONE',  ( 5.466459189643565253, -2.065842013452086956, -0.4630074653421185071 ) ) ;
#210161=CARTESIAN_POINT ( 'NONE',  ( 3.650014318109519262, 0.7545864325827613683, 1.950000943494380135 ) ) ;
#210163=CARTESIAN_POINT ( 'NONE',  ( 1.500562974171329333, 1.412943827846969702, -0.9888553570028703055 ) ) ;
#210165=CARTESIAN_POINT ( 'NONE',  ( 4.869442314738527067, -1.792836814666173062, -1.132239877606910472 ) ) ;
#210175=CARTESIAN_POINT ( 'NONE',  ( 1.734716041023535160, 1.690356777636679686, 0.6517371015684128022 ) ) ;
#210179=EDGE_LOOP ( 'NONE', ( #11440, #154786, #53178, #143246 ) ) ;
#210181=CARTESIAN_POINT ( 'NONE',  ( 2.385177931559249398, 0.08740048966574034961, -1.809473338476126569 ) ) ;
#210182=CARTESIAN_POINT ( 'NONE',  ( 6.539320575229250920, 2.072231551265828475, 2.205269387046896679 ) ) ;
#210186=CARTESIAN_POINT ( 'NONE',  ( 4.053051418270800177, 1.573051355563404252, -0.9941624863331417483 ) ) ;
#210188=CARTESIAN_POINT ( 'NONE',  ( 1.335391617855705926, 0.5546556490612590817, -1.833562831147776739 ) ) ;
#210189=CARTESIAN_POINT ( 'NONE',  ( 1.272165501999738435, -1.161393580401563375, 1.408505525491813515 ) ) ;
#210198=CARTESIAN_POINT ( 'NONE',  ( 6.139503339746209321, 1.821095124518475217, -0.7503768741054758218 ) ) ;
#210201=CARTESIAN_POINT ( 'NONE',  ( -0.02340959012393610192, -0.1578203421408593821, -2.056509962333047614 ) ) ;
#210203=CARTESIAN_POINT ( 'NONE',  ( 5.473632971755619359, 1.856580101505003411, -0.5137103415125721106 ) ) ;
#210205=CARTESIAN_POINT ( 'NONE',  ( 1.518276268637512194, 1.228937244518006011, -1.350148523839814096 ) ) ;
#210206=CARTESIAN_POINT ( 'NONE',  ( 2.262606014870732096, 0.9450075053254001212, 1.994452002680577429 ) ) ;
#210210=CARTESIAN_POINT ( 'NONE',  ( 0.7659823462377189918, -1.960405762330315049, 0.1893847968462581133 ) ) ;
#210211=CARTESIAN_POINT ( 'NONE',  ( 2.788543057918268619, 1.664307371569521132, -1.000645113138714848 ) ) ;
#210212=CARTESIAN_POINT ( 'NONE',  ( 0.3157796101352361440, -1.620936768121715499, 1.198674607299075934 ) ) ;
#210214=CARTESIAN_POINT ( 'NONE',  ( 5.840631046605349042, -1.815184518647503742, -0.4092948386957768747 ) ) ;
#210220=CARTESIAN_POINT ( 'NONE',  ( 1.329895901633147748, 1.076045675571284166, -1.909117696414885934 ) ) ;
#210224=CARTESIAN_POINT ( 'NONE',  ( 2.226930044512597906, -0.0006860120723567450030, 1.825872481329051222 ) ) ;
#210230=CARTESIAN_POINT ( 'NONE',  ( 0.8910897993890665170, 1.699419447932304594, -0.9074141512597186932 ) ) ;
#210231=CARTESIAN_POINT ( 'NONE',  ( 5.682460714699895554, 1.171467074228413674, -1.573401077569417605 ) ) ;
#210235=CARTESIAN_POINT ( 'NONE',  ( 4.757479570170550787, 2.167726397749652367, -0.3216086267831194112 ) ) ;
#210237=CARTESIAN_POINT ( 'NONE',  ( 4.030184149050713316, 1.145922430192683805, 1.723988044715178081 ) ) ;
#210238=CARTESIAN_POINT ( 'NONE',  ( -0.1296875068448159751, 0.001480089298542403009, -1.826395826379861864 ) ) ;
#210242=CARTESIAN_POINT ( 'NONE',  ( 4.289826696582184518, 1.777288211397337170, -1.457785959652138530 ) ) ;
#210249=CARTESIAN_POINT ( 'NONE',  ( 3.486211078826762844, -0.3796756879693505837, -1.904310675543115394 ) ) ;
#210254=CARTESIAN_POINT ( 'NONE',  ( 5.730699431777452446, 1.279516236652695316, -1.421498520143074540 ) ) ;
#210256=CARTESIAN_POINT ( 'NONE',  ( 6.821331452548096586, -0.1252896706360993595, 1.696280295671446448 ) ) ;
#210257=CARTESIAN_POINT ( 'NONE',  ( 4.399625206644591557, -1.976670321813909892, 0.3981083777728141038 ) ) ;
#210259=CARTESIAN_POINT ( 'NONE',  ( 1.383733252933561086, 2.037972573443189717, -0.8472329510355591786 ) ) ;
#210262=CARTESIAN_POINT ( 'NONE',  ( 1.939510448661335484, 0.7990184383764920018, -1.932127011870365951 ) ) ;
#210263=CARTESIAN_POINT ( 'NONE',  ( 0.07459516483346910476, 0.007201286963451345932, -1.755573347271717655 ) ) ;
#210264=CARTESIAN_POINT ( 'NONE',  ( 6.012342310302175363, -1.897698807000438359, 0.6819931642896917001 ) ) ;
#210266=CARTESIAN_POINT ( 'NONE',  ( 3.240441643373017211, 0.5569673610456173929, 2.223450396423230391 ) ) ;
#210267=CARTESIAN_POINT ( 'NONE',  ( 0.9545595967530025039, 0.3431710391763979073, -1.705965249089304470 ) ) ;
#210269=CARTESIAN_POINT ( 'NONE',  ( 1.000851265249177890, 1.706856028473648257, 0.3036596661522768525 ) ) ;
#210272=CARTESIAN_POINT ( 'NONE',  ( 0.9948528382496389932, 2.139055259286365640, 0.3712904390174593949 ) ) ;
#210273=CARTESIAN_POINT ( 'NONE',  ( 2.096888995370162156, 1.803417055948232761, 0.9023429676050932491 ) ) ;
#210274=CARTESIAN_POINT ( 'NONE',  ( 4.062500000000002665, -1.451031289061280205, -1.451031289060952467 ) ) ;
#210276=CARTESIAN_POINT ( 'NONE',  ( 6.287721633157377532, 1.330437191854600076, 1.393544807510539218 ) ) ;
#210278=CARTESIAN_POINT ( 'NONE',  ( 3.814843914748572207, -0.6992408500761657653, -2.108525230111441218 ) ) ;
#210284=CARTESIAN_POINT ( 'NONE',  ( 5.231891002347484054, 1.715934187082169604, 0.2900348964059005774 ) ) ;
#210285=CARTESIAN_POINT ( 'NONE',  ( 4.896903505236655185, 0.3334610245491422265, 1.933150054703360654 ) ) ;
#210289=CARTESIAN_POINT ( 'NONE',  ( 5.097078980560620920, 1.884938936817718069, -1.250935519564094767 ) ) ;
#210290=CARTESIAN_POINT ( 'NONE',  ( 2.066913078360913314, 1.530046405743747506, -1.383527225477628297 ) ) ;
#210294=CARTESIAN_POINT ( 'NONE',  ( 3.602682612693074660, 1.476495159181415939, -1.148357684351591912 ) ) ;
#210295=CARTESIAN_POINT ( 'NONE',  ( 2.777623227853244003, 1.486122661887591123, -0.8934276201044144550 ) ) ;
#210297=CARTESIAN_POINT ( 'NONE',  ( 6.163654587501778970, 1.125051486859941718, 1.880622087419632882 ) ) ;
#210298=CARTESIAN_POINT ( 'NONE',  ( 0.9212656856641410208, 2.039593612490635532, 0.8430313063367624871 ) ) ;
#210299=CARTESIAN_POINT ( 'NONE',  ( 3.555696680978126079, 0.5271953485486252644, -2.096301903996622862 ) ) ;
#210300=CARTESIAN_POINT ( 'NONE',  ( 4.945229674018920107, 0.6074099038847360355, -1.844580613826458437 ) ) ;
#210302=CARTESIAN_POINT ( 'NONE',  ( 6.925078400183548588, 0.0006614011395407459748, 1.855452278108092656 ) ) ;
#210309=CARTESIAN_POINT ( 'NONE',  ( -0.1401555495076401980, -1.643345231473653190, -1.339971704266910812 ) ) ;
#210311=CARTESIAN_POINT ( 'NONE',  ( 5.326796142270829648, 0.8146286751641409474, -1.844708973168760924 ) ) ;
#210315=CARTESIAN_POINT ( 'NONE',  ( 2.842213963582499670, 1.811911227886909614, 0.2232855069103783507 ) ) ;
#210316=CARTESIAN_POINT ( 'NONE',  ( 2.608667852368121043, -0.8438080161984360394, -2.039271889284439254 ) ) ;
#210321=CARTESIAN_POINT ( 'NONE',  ( 0.5276105490271070231, -0.2919958673943868765, 1.998420469645475483 ) ) ;
#210322=CARTESIAN_POINT ( 'NONE',  ( 1.067215373428985092, -1.669322716927954753, 1.307481345630675529 ) ) ;
#210325=CARTESIAN_POINT ( 'NONE',  ( 1.551354284286353247, 1.404667267363783667, 1.220738542487237677 ) ) ;
#210327=CARTESIAN_POINT ( 'NONE',  ( 1.112450467520700537, -0.9725818059473789745, -1.930612204972524282 ) ) ;
#210328=CARTESIAN_POINT ( 'NONE',  ( 6.574846728087075931, -0.8593996854794653251, 1.822268861383633309 ) ) ;
#210332=CARTESIAN_POINT ( 'NONE',  ( 3.475057130574196407, 0.04366187338752242769, -1.825333387291371512 ) ) ;
#210337=CARTESIAN_POINT ( 'NONE',  ( 6.784528966312857179, -1.956291195211720346, 0.4871289682274528299 ) ) ;
#210338=CARTESIAN_POINT ( 'NONE',  ( 5.964778383650899407, 0.1308802983275309528, -1.836551591404868233 ) ) ;
#210339=CARTESIAN_POINT ( 'NONE',  ( 0.07700591528354228110, 6.948790505698306141, -2.505847838500625979 ) ) ;
#210340=CARTESIAN_POINT ( 'NONE',  ( 4.951972348128318657, 0.7275260799690360658, -2.190091995644850797 ) ) ;
#210342=CARTESIAN_POINT ( 'NONE',  ( 6.450466699499744827, 0.6713059571747861387, 2.054807225473152865 ) ) ;
#210343=CARTESIAN_POINT ( 'NONE',  ( 1.698673089578231599, 1.615691133820891467, 1.077277171393706379 ) ) ;
#210345=CARTESIAN_POINT ( 'NONE',  ( 4.306267096541755990, -2.002170989124392175, 1.128539623919281754 ) ) ;
#210349=CARTESIAN_POINT ( 'NONE',  ( 4.645289301550183936, -1.446173438076237217, -1.186536486241091204 ) ) ;
#210352=CARTESIAN_POINT ( 'NONE',  ( 2.548957913124219044, 0.2380835140640499836, 1.897471792728817386 ) ) ;
#210355=CARTESIAN_POINT ( 'NONE',  ( 4.020313978404310262, -1.133593497508533110, -1.893353337301090233 ) ) ;
#210360=CARTESIAN_POINT ( 'NONE',  ( 1.229685887263828770, -1.247259403286736124, -1.526659406866498481 ) ) ;
#210361=CARTESIAN_POINT ( 'NONE',  ( 1.185104535163916228, -2.251984199834490052, -0.5028348148315447963 ) ) ;
#210362=CARTESIAN_POINT ( 'NONE',  ( 2.330453122711079850, -1.209328770571056921, 1.544706564130463811 ) ) ;
#210364=CARTESIAN_POINT ( 'NONE',  ( 5.787952559958898568, -1.304071791706362449, -1.598039198280821749 ) ) ;
#210371=CARTESIAN_POINT ( 'NONE',  ( 2.202231255880624516, 0.8340544509695562159, -2.004656366586863303 ) ) ;
#210375=CARTESIAN_POINT ( 'NONE',  ( 2.688565094423268853, -0.3157439183511835945, -1.843535313746543336 ) ) ;
#210376=CARTESIAN_POINT ( 'NONE',  ( 0.2630567961459496784, -1.839733103847444928, -0.9287307787974752316 ) ) ;
#210377=CARTESIAN_POINT ( 'NONE',  ( 0.07775346131142897577, 0.6705917366217004627, -2.369298483346020667 ) ) ;
#210378=FILL_AREA_STYLE_COLOUR ( '', #65625 ) ;
#210380=CARTESIAN_POINT ( 'NONE',  ( 2.068876254944008508, -1.477226179422253649, 1.214308343151893510 ) ) ;
#210382=CARTESIAN_POINT ( 'NONE',  ( 4.486996778590452983, 1.580468086399078542, -0.7966448122273452892 ) ) ;
#210383=CARTESIAN_POINT ( 'NONE',  ( 2.402860538037488780, -0.3286879766849961082, -1.883663324302800035 ) ) ;
#210386=CARTESIAN_POINT ( 'NONE',  ( 5.519116348382159032, -1.729776616345682028, 0.8233883490022309015 ) ) ;
#210388=CARTESIAN_POINT ( 'NONE',  ( 6.461384246211865801, 1.636644077835234246, 1.095356925007910265 ) ) ;
#210392=CARTESIAN_POINT ( 'NONE',  ( 5.348468966913380029, 0.5439794105128460400, 1.789823788735760646 ) ) ;
#210393=CARTESIAN_POINT ( 'NONE',  ( 1.172165686010542274, -1.159919637379997814, 1.409874495853599141 ) ) ;
#210395=CARTESIAN_POINT ( 'NONE',  ( 4.494872972331320327, -0.4818267175418550208, -2.153482813429814069 ) ) ;
#210398=CARTESIAN_POINT ( 'NONE',  ( 3.262228214153365169, -2.060424958539575524, 0.09861793142403557644 ) ) ;
#210406=CARTESIAN_POINT ( 'NONE',  ( 5.635237798060349412, -0.04710594754482424346, -2.069988403558701062 ) ) ;
#210408=CARTESIAN_POINT ( 'NONE',  ( 2.935029080331118756, 0.2613785356864756770, 2.145644965459513109 ) ) ;
#210410=CARTESIAN_POINT ( 'NONE',  ( 3.018227828326583762, -2.017275923677069205, 0.1012127129823153504 ) ) ;
#210411=CARTESIAN_POINT ( 'NONE',  ( 6.720655732516626735, 6.034942950145537388, 2.668627893128409756 ) ) ;
#210417=CARTESIAN_POINT ( 'NONE',  ( 1.868375392651611122, -1.978555653031977446, -0.3886301775877995524 ) ) ;
#210418=CARTESIAN_POINT ( 'NONE',  ( 6.269083535738129598, 2.097726667780253074, -0.6343229546324488100 ) ) ;
#210420=CARTESIAN_POINT ( 'NONE',  ( 5.009976098083095408, -0.6827417919906975108, 1.786564173047608062 ) ) ;
#210424=CARTESIAN_POINT ( 'NONE',  ( 3.339470413395662085, 0.4871825726840799398, -1.956567533273507964 ) ) ;
#210427=CARTESIAN_POINT ( 'NONE',  ( 4.752814332062330394, -1.383916046847250669, 1.029161146002472549 ) ) ;
#210428=CARTESIAN_POINT ( 'NONE',  ( -0.1399997263889611598, 2.874570648431204578, -2.488748559936367233 ) ) ;
#210432=CARTESIAN_POINT ( 'NONE',  ( 1.200149190772631158, 0.8425179731405306738, -1.891261800508976298 ) ) ;
#210435=CARTESIAN_POINT ( 'NONE',  ( 5.215404452620196807, 1.484227587358154077, 1.038217761341611922 ) ) ;
#210438=CARTESIAN_POINT ( 'NONE',  ( 6.533875575962896143, -1.755123972569608615, 0.4478894030855648523 ) ) ;
#210442=CARTESIAN_POINT ( 'NONE',  ( 2.554835828347111093, -1.907293181126702653, -1.079063956894068754 ) ) ;
#210445=CARTESIAN_POINT ( 'NONE',  ( 0.3089402658475807195, -1.578002999302514642, 1.165503548361209063 ) ) ;
#210447=CARTESIAN_POINT ( 'NONE',  ( 4.517137023955775099, -1.749796063449124084, 0.7800368752974867759 ) ) ;
#210455=CARTESIAN_POINT ( 'NONE',  ( 2.254944280175336324, -1.671361177491991201, 1.370965666894090385 ) ) ;
#210458=CARTESIAN_POINT ( 'NONE',  ( 1.483130931141176889, 1.688290157389197077, -0.6950536248920418103 ) ) ;
#210460=CARTESIAN_POINT ( 'NONE',  ( 5.122008332510333162, -0.9777984688263160473, -1.541441239866998103 ) ) ;
#210463=CARTESIAN_POINT ( 'NONE',  ( 2.865378420500460876, -1.565876230000915692, -1.097592462808501645 ) ) ;
#210465=CARTESIAN_POINT ( 'NONE',  ( 3.771889708208826075, -1.940809680921409486, 0.3342159591338197400 ) ) ;
#210467=CARTESIAN_POINT ( 'NONE',  ( 5.653840721119872903, 0.7909470656678599942, 1.773883556849734644 ) ) ;
#210471=CARTESIAN_POINT ( 'NONE',  ( 5.519825572852568030, -0.5132647233585425628, 2.057443900658859182 ) ) ;
#210473=CARTESIAN_POINT ( 'NONE',  ( 4.213462193461685601, 1.537813053725526569, 1.136448645172025262 ) ) ;
#210477=CARTESIAN_POINT ( 'NONE',  ( 0.2884678563945877738, -1.037960011796670523, 1.947446179978419512 ) ) ;
#210478=CARTESIAN_POINT ( 'NONE',  ( 5.373694559265936199, 0.3904673514037678150, -1.974700560916352154 ) ) ;
#210480=CARTESIAN_POINT ( 'NONE',  ( 6.199803715563785289, -0.6102442156579389598, 1.720816905678754782 ) ) ;
#210481=CARTESIAN_POINT ( 'NONE',  ( 0.9067890187421032699, 0.5993529260880943177, 1.981728858978973218 ) ) ;
#210486=CARTESIAN_POINT ( 'NONE',  ( 6.578970801323708706, -0.09418725797194843485, -1.868394071727994543 ) ) ;
#210495=CARTESIAN_POINT ( 'NONE',  ( 3.445721922217106936, -1.531427584095602867, -0.8135701209448819027 ) ) ;
#210498=CARTESIAN_POINT ( 'NONE',  ( 1.200149190772631158, 0.8425179731405306738, -1.891261800508976298 ) ) ;
#210499=CARTESIAN_POINT ( 'NONE',  ( 2.073964263283359699, -0.9022394416563597197, 1.915483482535395909 ) ) ;
#210503=CARTESIAN_POINT ( 'NONE',  ( 0.7605272443651526215, -0.6583816729706105653, -1.856300379560266833 ) ) ;
#210508=CARTESIAN_POINT ( 'NONE',  ( 2.168323659614699750, -1.408312831382242614, 1.808550206204377009 ) ) ;
#210509=CARTESIAN_POINT ( 'NONE',  ( 0.5393321728033515505, -1.288848960320065462, -1.293324666950084190 ) ) ;
#210510=CARTESIAN_POINT ( 'NONE',  ( 3.867365959033176814, -1.592763314076732106, -1.058159689705892692 ) ) ;
#210515=CARTESIAN_POINT ( 'NONE',  ( 1.652591521987197831, 1.991881122867325660, 0.2913371046347946747 ) ) ;
#210516=CARTESIAN_POINT ( 'NONE',  ( 1.674581101246939374, 1.321464807213859505, -1.450045219730737633 ) ) ;
#210520=CARTESIAN_POINT ( 'NONE',  ( 4.628904841183094199, -1.911603206638176511, 0.8469096376574613005 ) ) ;
#210521=CARTESIAN_POINT ( 'NONE',  ( 3.713518252986651724, -1.743675808792734205, 0.3021571867034832382 ) ) ;
#210524=CARTESIAN_POINT ( 'NONE',  ( 6.714806895146447907, -0.1657305019511661481, 2.255884130952827249 ) ) ;
#210525=CARTESIAN_POINT ( 'NONE',  ( 4.154071219024037198, -1.287471232310585467, 1.171156097612672253 ) ) ;
#210528=CARTESIAN_POINT ( 'NONE',  ( -0.1104750535120268828, 5.720715034752038797, -2.697548938405624597 ) ) ;
#210529=CARTESIAN_POINT ( 'NONE',  ( 4.991369361657826964, 1.659364262194364725, 0.5025568866975324012 ) ) ;
#210531=CARTESIAN_POINT ( 'NONE',  ( 4.598189031992506948, 0.9324077545292840385, -1.960920063828344384 ) ) ;
#210533=CARTESIAN_POINT ( 'NONE',  ( -0.1353153266233823870, -2.055576600424202649, -0.5074567962913156816 ) ) ;
#210534=CARTESIAN_POINT ( 'NONE',  ( 6.343749999995762501, 1.895863743059895246, 0.7852924748296488122 ) ) ;
#210536=CARTESIAN_POINT ( 'NONE',  ( 3.663036927850862323, -1.698304795282145063, -0.9092769472496107230 ) ) ;
#210538=CARTESIAN_POINT ( 'NONE',  ( 6.539320575229294441, -0.001643797937642132567, 2.203502507913539521 ) ) ;
#210540=CARTESIAN_POINT ( 'NONE',  ( 6.883263157960370471, 7.052343128562386987, 2.644342559190917541 ) ) ;
#210543=CARTESIAN_POINT ( 'NONE',  ( 2.772393654007713870, 2.210366155326251025, -0.2202761458626761870 ) ) ;
#210548=CARTESIAN_POINT ( 'NONE',  ( 0.3873425458618062200, -0.6819987885887256462, -1.897696807414723796 ) ) ;
#210550=CARTESIAN_POINT ( 'NONE',  ( 5.775849841709651322, -2.013224797598807569, 0.4483296186361291902 ) ) ;
#210555=CARTESIAN_POINT ( 'NONE',  ( 6.837182164354378422, -1.670574593475544489, 0.8415915117672703172 ) ) ;
#210556=CARTESIAN_POINT ( 'NONE',  ( 5.889268099914369614, -0.6330491082502353040, -1.614684210577774115 ) ) ;
#210557=CARTESIAN_POINT ( 'NONE',  ( 5.179165720741062628, 1.174484231026547976, 1.284593650646998375 ) ) ;
#210559=CARTESIAN_POINT ( 'NONE',  ( 2.947136817621052618, -1.875550406973557349, -1.317825558608209713 ) ) ;
#210561=CARTESIAN_POINT ( 'NONE',  ( 1.587592257565925813, -1.832131100469553520, -0.1817911664281982032 ) ) ;
#210563=CARTESIAN_POINT ( 'NONE',  ( 2.406250000000001776, 1.895863743164033277, -0.7852924748301132185 ) ) ;
#210564=CARTESIAN_POINT ( 'NONE',  ( 1.711645973048509850, -1.812212506298327197, 0.2199163931802459171 ) ) ;
#210565=CARTESIAN_POINT ( 'NONE',  ( 2.883435573726996548, -0.5880205015329244000, -1.928751729079546173 ) ) ;
#210566=CARTESIAN_POINT ( 'NONE',  ( 1.781448188194576066, 1.512826363221421833, 1.585725795389548942 ) ) ;
#210568=CARTESIAN_POINT ( 'NONE',  ( 4.770599357992978184, -1.377743202910805875, 1.592837501749831519 ) ) ;
#210571=CARTESIAN_POINT ( 'NONE',  ( 1.170471352854907776, -0.9292243337341490328, -1.850172451097586990 ) ) ;
#210574=CARTESIAN_POINT ( 'NONE',  ( 4.301511568767760529, 1.893648340000140040, -0.9544086401246790752 ) ) ;
#210577=CARTESIAN_POINT ( 'NONE',  ( 6.305291373979138747, 1.520805759102667132, 1.009792402853857407 ) ) ;
#210586=CARTESIAN_POINT ( 'NONE',  ( 6.416280414004661203, -2.120105685773795212, 0.05337830808049835035 ) ) ;
#210587=CARTESIAN_POINT ( 'NONE',  ( 0.8332068151313138937, 0.1548093300561304564, 2.100314307419436588 ) ) ;
#210590=CARTESIAN_POINT ( 'NONE',  ( 5.489040303513849750, 0.1347565666095333348, 1.856089258439092893 ) ) ;
#210598=CARTESIAN_POINT ( 'NONE',  ( 2.154674626568295892, -0.5202524484802829585, -1.891573884155263396 ) ) ;
#210599=CARTESIAN_POINT ( 'NONE',  ( 0.7257156204387126275, -2.052300050329861847, 0.6792298617422781737 ) ) ;
#210603=CARTESIAN_POINT ( 'NONE',  ( 2.459901920361181826, 1.337243170739129239, 1.103576756174700746 ) ) ;
#210604=CARTESIAN_POINT ( 'NONE',  ( 2.044474178175458068, -1.396829902048246197, -1.037857226380611619 ) ) ;
#210608=CARTESIAN_POINT ( 'NONE',  ( 0.8079699768257715409, -1.730602710733687877, 1.034004433739174500 ) ) ;
#210609=CARTESIAN_POINT ( 'NONE',  ( 6.925078400183590333, 2.958959781645562170, 2.496897724761244497 ) ) ;
#210612=CARTESIAN_POINT ( 'NONE',  ( 1.235163454902254765, -1.783154728128878652, 0.8411200730164528627 ) ) ;
#210613=CARTESIAN_POINT ( 'NONE',  ( 5.730699431777452446, 1.279516236652695316, -1.421498520143074540 ) ) ;
#210618=CARTESIAN_POINT ( 'NONE',  ( 0.8737014391667098367, 0.3917534382160395290, -1.981132022265948756 ) ) ;
#210620=CARTESIAN_POINT ( 'NONE',  ( 4.753107839025799031, -1.856540859070819005, 1.370308287008913606 ) ) ;
#210621=CARTESIAN_POINT ( 'NONE',  ( 5.986763597034562068, 1.890319730748804439, 0.5246630281777532323 ) ) ;
#210622=CARTESIAN_POINT ( 'NONE',  ( 3.186327686730246800, 1.093712407854827706, -1.628379936052851917 ) ) ;
#210626=CARTESIAN_POINT ( 'NONE',  ( 1.499367237992894841, -0.2534978968403051591, 2.102027841304268119 ) ) ;
#210629=CARTESIAN_POINT ( 'NONE',  ( 1.042614295247261680, -1.450156864641814369, -1.134287774663629733 ) ) ;
#210632=CARTESIAN_POINT ( 'NONE',  ( 2.935903058640790597, -2.042584291827519660, 0.5695675404085094318 ) ) ;
#210636=CARTESIAN_POINT ( 'NONE',  ( 3.409498948718358680, -0.4055148060846422431, 2.020306737620365389 ) ) ;
#210638=CARTESIAN_POINT ( 'NONE',  ( -0.006632162239710717895, -1.840811702136424088, -0.04651623371411393176 ) ) ;
#210643=CARTESIAN_POINT ( 'NONE',  ( -0.004863692847738298151, -0.4900785244342681368, -2.159743284330918112 ) ) ;
#210644=CARTESIAN_POINT ( 'NONE',  ( 3.093345431676647994, 1.942085262481594965, -1.160266548027958367 ) ) ;
#210646=CARTESIAN_POINT ( 'NONE',  ( 2.935611553675514518, -1.744650271585326484, 0.4875094811955403284 ) ) ;
#210647=CARTESIAN_POINT ( 'NONE',  ( 3.344859342474030939, -1.692025585574646662, -0.8982749641134063490 ) ) ;
#210648=CARTESIAN_POINT ( 'NONE',  ( 4.562978833902987752, 1.602482145440896399, -1.310924660355553106 ) ) ;
#210650=CARTESIAN_POINT ( 'NONE',  ( 1.955877382181537838, 1.966306777096353153, -0.1432868284926436253 ) ) ;
#210651=CARTESIAN_POINT ( 'NONE',  ( 0.3055242992691169501, -0.5169788762636564616, 1.855657374570508278 ) ) ;
#210652=CARTESIAN_POINT ( 'NONE',  ( 2.623731232481395725, -1.075365945362505293, -1.530472918023266571 ) ) ;
#210653=CARTESIAN_POINT ( 'NONE',  ( 1.542099375240197245, -1.674077152000338797, -1.588604925253054745 ) ) ;
#210655=CARTESIAN_POINT ( 'NONE',  ( 2.594024687173156263, 0.8801344893799438740, -1.639794913454610148 ) ) ;
#210657=CARTESIAN_POINT ( 'NONE',  ( 6.549293068304288923, 1.796493013226226232, -1.013385894242497809 ) ) ;
#210662=CARTESIAN_POINT ( 'NONE',  ( 5.913134528375765697, 1.855721070963678443, 0.9956851948400150532 ) ) ;
#210664=CARTESIAN_POINT ( 'NONE',  ( 5.852838158510675015, -1.708014377640250991, 1.324763891615586386 ) ) ;
#210665=CARTESIAN_POINT ( 'NONE',  ( 6.024083573256426405, -2.004181050114914875, 0.2492093081243785258 ) ) ;
#210669=CARTESIAN_POINT ( 'NONE',  ( 6.825078400183593352, 2.989295776279639938, 2.209688085509611710 ) ) ;
#210672=CARTESIAN_POINT ( 'NONE',  ( 4.206267736153862735, 1.236801365491456028, -1.592660703826812352 ) ) ;
#210677=CARTESIAN_POINT ( 'NONE',  ( 6.315313271410192719, -0.2696487299426887363, 2.144762774094311375 ) ) ;
#210681=CARTESIAN_POINT ( 'NONE',  ( -0.1060672704247594272, -0.8202269080865699502, -1.729793120397028927 ) ) ;
#210683=CARTESIAN_POINT ( 'NONE',  ( 6.539320575229236709, 1.252639605590207150, 2.218328189723097754 ) ) ;
#210684=CARTESIAN_POINT ( 'NONE',  ( 1.822448697576475540, 1.608646582964175176, 0.6229558172686412432 ) ) ;
#210689=CARTESIAN_POINT ( 'NONE',  ( 6.661405586796748324, 0.3194099797865917467, -1.842918054787325843 ) ) ;
#210690=CARTESIAN_POINT ( 'NONE',  ( 0.6803381722274345345, 0.9942335676262317179, 1.750384451323853785 ) ) ;
#210691=CARTESIAN_POINT ( 'NONE',  ( 3.628125149645112568, -1.312672481567092708, -1.773765351669121415 ) ) ;
#210692=CARTESIAN_POINT ( 'NONE',  ( 5.700102493039955753, 0.8868678402436469543, -1.981866098488117789 ) ) ;
#210696=CARTESIAN_POINT ( 'NONE',  ( 3.686284471605893120, 1.179319764668992576, 1.762089746328721507 ) ) ;
#210697=CARTESIAN_POINT ( 'NONE',  ( 3.392203995056555232, -0.8197896108859267228, -1.842441248588816860 ) ) ;
#210698=CARTESIAN_POINT ( 'NONE',  ( 2.988311359655666077, -1.075548189349010864, 1.457604102852279926 ) ) ;
#210703=CARTESIAN_POINT ( 'NONE',  ( 0.07479286986305370977, 0.004866263145587856019, -1.855573292446038414 ) ) ;
#210707=CARTESIAN_POINT ( 'NONE',  ( 1.411203511878999173, -1.802517209299081102, 0.6490724346438890846 ) ) ;
#210713=CARTESIAN_POINT ( 'NONE',  ( 4.944278945467968533, 2.155654431248493985, 0.1625706239713892443 ) ) ;
#210716=CARTESIAN_POINT ( 'NONE',  ( 3.375340920106313813, -1.871962376360849278, -0.9962781187466958066 ) ) ;
#210717=CARTESIAN_POINT ( 'NONE',  ( -0.1296875068448125334, 2.048176110289974261, -2.243787855586779401 ) ) ;
#210720=CARTESIAN_POINT ( 'NONE',  ( 4.007068486172041588, 1.689080509644375505, 1.016306131198143836 ) ) ;
#210721=CARTESIAN_POINT ( 'NONE',  ( 6.240485052285455581, 1.095381943021833449, -1.567431287326017664 ) ) ;
#210724=CARTESIAN_POINT ( 'NONE',  ( 6.654754201047359707, -0.5240520113350942699, -1.898494369619908140 ) ) ;
#210725=CARTESIAN_POINT ( 'NONE',  ( 3.099484260031000193, -1.939694849350329431, 0.09605879933238459234 ) ) ;
#210729=CARTESIAN_POINT ( 'NONE',  ( 2.062552408159121775, -1.911915923569502684, -0.8461947581326088041 ) ) ;
#210732=CARTESIAN_POINT ( 'NONE',  ( 0.02954414540562703972, -1.776926038569931254, 0.3510683431443075153 ) ) ;
#210734=CARTESIAN_POINT ( 'NONE',  ( 4.547634279845023109, -1.704780727694398479, -1.401453192282381188 ) ) ;
#210736=CARTESIAN_POINT ( 'NONE',  ( 3.610573252990852744, -0.8922430012947217826, -2.018528625508857921 ) ) ;
#210739=CARTESIAN_POINT ( 'NONE',  ( 1.207504981961624813, 1.448612403150219885, 1.248453992567559512 ) ) ;
#210741=CARTESIAN_POINT ( 'NONE',  ( 4.598136200040512378, 0.8882050449813773119, -1.870312673664726644 ) ) ;
#210743=CARTESIAN_POINT ( 'NONE',  ( 3.379894511112140787, 1.369989894601089775, 1.672159933133889442 ) ) ;
#210744=CARTESIAN_POINT ( 'NONE',  ( 4.898067072109578035, -0.7382639882421681010, -2.063579870930781546 ) ) ;
#210752=CARTESIAN_POINT ( 'NONE',  ( 0.5807041986926939625, -0.7231374404764076003, 1.882475062126743204 ) ) ;
#210756=CARTESIAN_POINT ( 'NONE',  ( 4.891501605334720004, -1.894957309059261297, 0.8341102180390786991 ) ) ;
#210757=CARTESIAN_POINT ( 'NONE',  ( 3.369672229528171581, 1.879407295867494554, -0.4226879870903621494 ) ) ;
#210759=CARTESIAN_POINT ( 'NONE',  ( -0.01795374796791787686, -2.016030408028956167, -0.04665595434990427171 ) ) ;
#210762=CARTESIAN_POINT ( 'NONE',  ( 4.364079147461279895, -1.964463519307905193, 0.1404744649011815116 ) ) ;
#210763=CARTESIAN_POINT ( 'NONE',  ( 0.04132284026489921325, -1.696808583893465894, -1.386471574116483696 ) ) ;
#210764=CARTESIAN_POINT ( 'NONE',  ( 4.318856058802469811, 1.670182456744148336, 0.7377305746401883191 ) ) ;
#210770=CARTESIAN_POINT ( 'NONE',  ( 1.680954830071922812, 1.270413995023990106, 1.332975479855981416 ) ) ;
#210771=CARTESIAN_POINT ( 'NONE',  ( 5.572526294291941795, 0.8198877612898677336, 1.838878804361820274 ) ) ;
#210772=CARTESIAN_POINT ( 'NONE',  ( 0.9138903340461038693, 0.6688396875448484602, 2.198942881657910853 ) ) ;
#210773=CARTESIAN_POINT ( 'NONE',  ( 5.155110299917927463, 1.633153276354940342, -1.086568599608192409 ) ) ;
#210778=CARTESIAN_POINT ( 'NONE',  ( 1.241864343681793548, 2.088520813897582151, 0.09894013698169208670 ) ) ;
#210779=CARTESIAN_POINT ( 'NONE',  ( 6.825078400183545391, 0.005516643811322509937, 1.755566376062764222 ) ) ;
#210782=CARTESIAN_POINT ( 'NONE',  ( 0.7666889417085223091, 1.677783727127066804, -0.4624100818488885434 ) ) ;
#210786=CARTESIAN_POINT ( 'NONE',  ( 1.646655695949898135, -1.458533453692168358, 0.9204839396419748354 ) ) ;
#210787=CARTESIAN_POINT ( 'NONE',  ( 1.347511689332027807, 0.6317163119916607839, -2.098556723903362009 ) ) ;
#210788=CARTESIAN_POINT ( 'NONE',  ( 4.231241840954825584, 0.1069408422738199749, 2.204416794138922331 ) ) ;
#210790=CARTESIAN_POINT ( 'NONE',  ( 1.780376006863694904, -1.203675225865230569, -1.806662255390781180 ) ) ;
#210791=CARTESIAN_POINT ( 'NONE',  ( 0.2580658466875830337, 0.6954254843183353962, 1.688255465954719536 ) ) ;
#210792=CARTESIAN_POINT ( 'NONE',  ( 3.327469932021313692, -1.606305723110455608, -1.379610029357878798 ) ) ;
#210793=CARTESIAN_POINT ( 'NONE',  ( 6.639320575229291421, 7.053415594291638335, 2.394893074302415936 ) ) ;
#210795=CARTESIAN_POINT ( 'NONE',  ( 3.931398753607476593, -1.581038262191627686, -1.660111252351449185 ) ) ;
#210799=CARTESIAN_POINT ( 'NONE',  ( 5.883471028171038952, 0.1659795297097066691, -2.215133764073994982 ) ) ;
#210805=CARTESIAN_POINT ( 'NONE',  ( 4.483046177357690176, -2.016033783801042034, -0.04667830911464498911 ) ) ;
#210807=CARTESIAN_POINT ( 'NONE',  ( 2.465751394709358113, -0.4561089685623443968, 2.011347002571160836 ) ) ;
#210812=CARTESIAN_POINT ( 'NONE',  ( 5.085950966588184130, -2.174626929279792176, -0.2704268894557353975 ) ) ;
#210813=CARTESIAN_POINT ( 'NONE',  ( 2.092422861153935276, -0.4390285686692517175, 1.967888031366466395 ) ) ;
#210814=CARTESIAN_POINT ( 'NONE',  ( 2.155570461979210428, 0.7887370375637430264, 1.663910549085621415 ) ) ;
#210817=CARTESIAN_POINT ( 'NONE',  ( 4.805575371506604299, -0.4859443722219913830, 1.759630929660048526 ) ) ;
#210818=CARTESIAN_POINT ( 'NONE',  ( 6.486953984781112403, -2.015912550161761629, 0.05229459904129707404 ) ) ;
#210820=CARTESIAN_POINT ( 'NONE',  ( 5.541944591929171438, 0.9225863094920858654, -2.066052574227566385 ) ) ;
#210822=CARTESIAN_POINT ( 'NONE',  ( 0.2586047683651994666, 0.8082109201883975746, 1.945024607815620366 ) ) ;
#210833=CARTESIAN_POINT ( 'NONE',  ( 3.357896860617498369, -1.684415915708385114, -1.448384614443619434 ) ) ;
#210838=CARTESIAN_POINT ( 'NONE',  ( 3.473055881322492322, 1.772541284497713976, 0.8411618914155660764 ) ) ;
#210845=CARTESIAN_POINT ( 'NONE',  ( 2.883181758455736432, -1.960942133159260692, -0.8077274430827171559 ) ) ;
#210847=CARTESIAN_POINT ( 'NONE',  ( 4.750933126423753095, -1.738186171353903742, 1.284983810367075208 ) ) ;
#210848=CARTESIAN_POINT ( 'NONE',  ( 2.682954136603598272, 1.303717545168959990, 1.300458928786947688 ) ) ;
#210851=CARTESIAN_POINT ( 'NONE',  ( 6.070193552946823168, -1.654735283430305515, -0.5392940629580407208 ) ) ;
#210855=CARTESIAN_POINT ( 'NONE',  ( 3.063507763784904192, 0.3185916186679502715, -2.137983152197140413 ) ) ;
#210856=CARTESIAN_POINT ( 'NONE',  ( 4.622422610786712127, 0.4444332032229811325, -1.966343831704894907 ) ) ;
#210858=CARTESIAN_POINT ( 'NONE',  ( 2.729541802387557059, -2.017400560480298033, 0.7770373237434913261 ) ) ;
#210860=CARTESIAN_POINT ( 'NONE',  ( 4.077382496314372773, 1.857369029195341525, -0.6610406152272005897 ) ) ;
#210861=CARTESIAN_POINT ( 'NONE',  ( 4.599131018191075171, -0.5143685224620330176, 1.872658368587260647 ) ) ;
#210870=CARTESIAN_POINT ( 'NONE',  ( 0.8860939741733677710, 1.483344945610004295, 1.634051305214024641 ) ) ;
#210872=CARTESIAN_POINT ( 'NONE',  ( 5.928557400228100960, -1.247251702497784942, 1.514172074262534196 ) ) ;
#210876=CARTESIAN_POINT ( 'NONE',  ( 0.07499057489264347731, 6.948553613792602057, -2.550573651218261517 ) ) ;
#210877=CARTESIAN_POINT ( 'NONE',  ( 5.525302006934727395, -1.171079710934025186, -1.420692760577553226 ) ) ;
#210882=CARTESIAN_POINT ( 'NONE',  ( 5.765915565743810589, 0.6138260544302427402, -2.029845472315944921 ) ) ;
#210885=CARTESIAN_POINT ( 'NONE',  ( 6.766874334510889710, -1.882258232876810045, -0.8394616043497000746 ) ) ;
#210887=CARTESIAN_POINT ( 'NONE',  ( 2.295144308211858331, -1.664110045376477443, 0.8333370299275147941 ) ) ;
#210888=CARTESIAN_POINT ( 'NONE',  ( 3.948646536499214932, -1.533023199436277961, -1.019512891124202403 ) ) ;
#210894=CARTESIAN_POINT ( 'NONE',  ( 3.721466898765386500, -0.1629207441977159332, 2.200919931280575170 ) ) ;
#210895=CARTESIAN_POINT ( 'NONE',  ( 5.958357971250668683, 0.9089415708923481718, 2.071969630155451547 ) ) ;
#210897=CARTESIAN_POINT ( 'NONE',  ( 6.363521484574993003, -1.460773276151544176, -1.071267404939825640 ) ) ;
#210898=CARTESIAN_POINT ( 'NONE',  ( 6.122283701245728516, 1.895932525083013465, 0.2736375990538899572 ) ) ;
#210901=CARTESIAN_POINT ( 'NONE',  ( 6.350466393003619814, 0.5888352225367661230, 1.775644890098279749 ) ) ;
#210903=CARTESIAN_POINT ( 'NONE',  ( 6.578955313817166584, -0.09182192948648319752, -1.767577901409943086 ) ) ;
#210904=CARTESIAN_POINT ( 'NONE',  ( 1.815639016007553730, -1.320828798922760949, -1.523793687088881299 ) ) ;
#210906=CARTESIAN_POINT ( 'NONE',  ( 3.053452221204506323, -1.721964003836244039, -1.212301904834027333 ) ) ;
#210911=CARTESIAN_POINT ( 'NONE',  ( 2.513930914015961804, -0.6297079463782135900, 1.919214091249999088 ) ) ;
#210914=CARTESIAN_POINT ( 'NONE',  ( 3.708425082824120533, -0.8722964037291662809, -1.977944213000272455 ) ) ;
#210919=CARTESIAN_POINT ( 'NONE',  ( 0.6784789811392475389, -1.161776791282279397, -1.834017514133066129 ) ) ;
#210923=CARTESIAN_POINT ( 'NONE',  ( 1.997856853652695497, -2.190977152517746163, 0.05759783203293508680 ) ) ;
#210924=CARTESIAN_POINT ( 'NONE',  ( 6.883263157960365142, 1.273421409013283823, 2.069651443392322765 ) ) ;
#210925=CARTESIAN_POINT ( 'NONE',  ( 2.272703622300107362, -1.391801132404853147, 1.783687758696401504 ) ) ;
#210932=CARTESIAN_POINT ( 'NONE',  ( 4.674921082483953327, 0.0007207667814621705445, -1.769921774705035755 ) ) ;
#210935=CARTESIAN_POINT ( 'NONE',  ( 0.9738169395155724661, 2.029595412481857153, -0.5617393031529455127 ) ) ;
#210938=CARTESIAN_POINT ( 'NONE',  ( 5.870720304489429608, -0.2986452421533461465, -1.994069804803912049 ) ) ;
#210941=CARTESIAN_POINT ( 'NONE',  ( 3.959713429720784106, 1.856571849420919795, -0.2284545790810637578 ) ) ;
#210942=CARTESIAN_POINT ( 'NONE',  ( 3.239188805615275335, -0.1476314317495740769, -2.065021578984991724 ) ) ;
#210946=DIRECTION ( 'NONE',  ( -3.451266460341926649E-31, -5.200010849845536803E-32, 1.000000000000000000 ) ) ;
#210947=CARTESIAN_POINT ( 'NONE',  ( 6.825078400183575589, -0.005632053428735600553, 2.144262460745151255 ) ) ;
#210949=CARTESIAN_POINT ( 'NONE',  ( 2.805073129645048624, -1.632656238785214597, 1.087510969322850629 ) ) ;
#210950=CARTESIAN_POINT ( 'NONE',  ( 0.5794536021234627521, 1.392335491182377316, -1.458330535474762213 ) ) ;
#210953=CARTESIAN_POINT ( 'NONE',  ( 0.6318452133688509109, 0.9670987946563678328, -1.601024004909731513 ) ) ;
#210955=CARTESIAN_POINT ( 'NONE',  ( 2.900642264033539863, -1.984120583840060625, -0.3400495124021261084 ) ) ;
#210957=CARTESIAN_POINT ( 'NONE',  ( 2.073964263283359699, -0.9022394416563597197, 1.915483482535395909 ) ) ;
#210959=CARTESIAN_POINT ( 'NONE',  ( 3.947765587739564097, 1.497496809916948779, 1.429883829622953462 ) ) ;
#210961=CARTESIAN_POINT ( 'NONE',  ( 6.351524237630270520, 2.085149843271947301, -0.1523318108044656727 ) ) ;
#210963=CARTESIAN_POINT ( 'NONE',  ( 5.860330175037709921, 0.7421476303169188826, 1.668095884353037128 ) ) ;
#210968=CARTESIAN_POINT ( 'NONE',  ( 6.616270032800761314, -1.034323699838369359, -1.949367651511712207 ) ) ;
#210970=CARTESIAN_POINT ( 'NONE',  ( 5.514289750425454883, -1.912461473380810961, 0.004301308668797076962 ) ) ;
#210979=CARTESIAN_POINT ( 'NONE',  ( 4.376139848268215893, -1.078761963904120602, 1.527931137620001989 ) ) ;
#210986=CARTESIAN_POINT ( 'NONE',  ( 1.006626315519317139, 0.5665869296403948097, 1.886213005043664515 ) ) ;
#210988=CARTESIAN_POINT ( 'NONE',  ( 3.392203995056555232, -0.8197896108859267228, -1.842441248588816860 ) ) ;
#210992=CARTESIAN_POINT ( 'NONE',  ( 3.257961296797746265, 0.9855263100190698733, 1.957416934251283935 ) ) ;
#210994=CARTESIAN_POINT ( 'NONE',  ( 2.362220099979424059, 0.8219310624981416291, 1.742368475122471727 ) ) ;
#211005=CARTESIAN_POINT ( 'NONE',  ( 5.161589042655139181, 0.9124512986629171873, 1.599201395118980740 ) ) ;
#211006=CARTESIAN_POINT ( 'NONE',  ( 1.471341131262299706, -1.727646810417843959, -1.033094421854539036 ) ) ;
#211007=CARTESIAN_POINT ( 'NONE',  ( 4.481968937923656249, 2.098976780363570604, 0.9367997793626892111 ) ) ;
#211008=CARTESIAN_POINT ( 'NONE',  ( -0.1290005225502432740, 4.081813041011835175, -2.728655865233818201 ) ) ;
#211009=CARTESIAN_POINT ( 'NONE',  ( 2.272090887488043887, -0.8719313595505603365, -1.644003247725301264 ) ) ;
#211012=CARTESIAN_POINT ( 'NONE',  ( 6.883263157960364254, -0.007059606330772384697, 2.153658854459545857 ) ) ;
#211013=CARTESIAN_POINT ( 'NONE',  ( 5.379139070037473935, -1.731557697741787916, -0.8120211572784155063 ) ) ;
#211016=CARTESIAN_POINT ( 'NONE',  ( 4.353126977966869759, 0.4563941458865827805, -2.040161790709469791 ) ) ;
#211017=CARTESIAN_POINT ( 'NONE',  ( 2.940157781200231746, 1.856316385841882965, 0.2306766016651334850 ) ) ;
#211021=CARTESIAN_POINT ( 'NONE',  ( 5.443894040360703457, 0.6935754108010495633, -1.579493244201269908 ) ) ;
#211026=CARTESIAN_POINT ( 'NONE',  ( 5.489208499878581726, 0.1525156608223678933, 2.165750181564994215 ) ) ;
#211027=CARTESIAN_POINT ( 'NONE',  ( 4.424309136736732206, 1.121156565774838354, -1.440799707636587712 ) ) ;
#211028=CARTESIAN_POINT ( 'NONE',  ( 1.375751926856683127, -1.915142299924106339, 0.4244507266663796741 ) ) ;
#211029=CARTESIAN_POINT ( 'NONE',  ( -0.03531552556956805977, -2.054970391365168680, -0.5093743926467135807 ) ) ;
#211033=CARTESIAN_POINT ( 'NONE',  ( 2.174623584685225541, 0.9092215167782154994, 1.915816808323366871 ) ) ;
#211037=CARTESIAN_POINT ( 'NONE',  ( 0.6024989291013755910, 2.064475859885641640, 0.1558578049991043990 ) ) ;
#211038=CARTESIAN_POINT ( 'NONE',  ( 6.883263157960403333, 6.034387817901857964, 2.748704107105720773 ) ) ;
#211040=CARTESIAN_POINT ( 'NONE',  ( 2.719623178692368359, 1.877883874979644263, 1.186199984364836313 ) ) ;
#211042=CARTESIAN_POINT ( 'NONE',  ( 1.196342457394595993, 2.030139636617489085, 1.078195451733245047 ) ) ;
#211044=CARTESIAN_POINT ( 'NONE',  ( 5.295784840496287060, -1.454754056633072778, -1.462402424637335052 ) ) ;
#211048=CARTESIAN_POINT ( 'NONE',  ( 0.2333540202161427102, 1.346341334450983140, -2.298657068330804076 ) ) ;
#211049=CARTESIAN_POINT ( 'NONE',  ( 5.741722636381445533, 1.839460222191912964, 0.08393339073512617876 ) ) ;
#211052=CARTESIAN_POINT ( 'NONE',  ( -0.2104748580754183807, 4.084054299358617079, -2.658391380015924010 ) ) ;
#211053=CARTESIAN_POINT ( 'NONE',  ( 1.588428401085600461, -0.2480725091915989278, -1.706701089166535512 ) ) ;
#211054=CARTESIAN_POINT ( 'NONE',  ( 1.376185782568883020, -2.007256511855738612, -0.1928315418098166534 ) ) ;
#211055=CARTESIAN_POINT ( 'NONE',  ( 1.987358909443589283, -2.298030411116751992, 0.06136411900238383788 ) ) ;
#211057=CARTESIAN_POINT ( 'NONE',  ( 2.214515517796631805, -1.065126590517451843, -1.995962479041712534 ) ) ;
#211058=CARTESIAN_POINT ( 'NONE',  ( 3.651088154774425387, -1.721711045478736102, 1.212656735320973400 ) ) ;
#211060=CARTESIAN_POINT ( 'NONE',  ( 2.987294507434365087, 1.248747198882380394, 1.254300180652974550 ) ) ;
#211063=CARTESIAN_POINT ( 'NONE',  ( 5.583585467610721054, -1.033564708330332316, 2.046191781174087509 ) ) ;
#211065=CARTESIAN_POINT ( 'NONE',  ( 5.068220161613846031, -1.734768455660203434, -0.6171159064975312303 ) ) ;
#211070=CARTESIAN_POINT ( 'NONE',  ( 4.593798273609356997, -2.190911875110569174, -0.05534364095756416635 ) ) ;
#211075=CARTESIAN_POINT ( 'NONE',  ( 2.754421912756400026, 0.6492094756798562072, 1.813941749866236242 ) ) ;
#211078=CARTESIAN_POINT ( 'NONE',  ( 6.521762860236213655, -0.4636855090699961712, 2.076960040381255812 ) ) ;
#211088=CARTESIAN_POINT ( 'NONE',  ( 2.383973883943972805, -0.2989522671389834851, -1.714397271258593092 ) ) ;
#211090=CARTESIAN_POINT ( 'NONE',  ( 0.5198770262540284293, 1.941052373433370670, -0.2841105942011297736 ) ) ;
#211093=CARTESIAN_POINT ( 'NONE',  ( 6.192270064542984898, -2.150811787302907785, -0.2168040374768212541 ) ) ;
#211096=CARTESIAN_POINT ( 'NONE',  ( 6.086834708314957432, -0.3123483334277510348, -2.138898144987111838 ) ) ;
#211097=CARTESIAN_POINT ( 'NONE',  ( -0.2106725631050176961, 4.086973797293973476, -2.558389695104481554 ) ) ;
#211100=CARTESIAN_POINT ( 'NONE',  ( 0.3329892237508432773, -1.712944741146247063, 0.7519245212838022718 ) ) ;
#211101=CARTESIAN_POINT ( 'NONE',  ( 6.081315976822482483, 1.162057296412899676, -1.286934115659829736 ) ) ;
#211103=CARTESIAN_POINT ( 'NONE',  ( 3.228257827484398490, 2.138632370135685523, 0.4780590757816546854 ) ) ;
#211104=CARTESIAN_POINT ( 'NONE',  ( 2.960362034815271048, 2.296572897674476810, -0.2250602657276803420 ) ) ;
#211105=CARTESIAN_POINT ( 'NONE',  ( 5.958293153512181917, 0.8310434803317863217, 1.885964484847465705 ) ) ;
#211106=CARTESIAN_POINT ( 'NONE',  ( 1.482261173788253394, -0.2847754331270537231, -1.920845095517382362 ) ) ;
#211110=CARTESIAN_POINT ( 'NONE',  ( 4.008146050417991546, -0.8085630067716749192, 1.960596031080278356 ) ) ;
#211112=CARTESIAN_POINT ( 'NONE',  ( 2.004529941291322448, -1.955172360644286789, 0.4926429297785542283 ) ) ;
#211114=CARTESIAN_POINT ( 'NONE',  ( 5.139771110516938357, -1.557344429106276573, -1.563758303505815572 ) ) ;
#211117=CARTESIAN_POINT ( 'NONE',  ( 0.3283667639546791195, 1.746078182827022429, 0.5332771064449209897 ) ) ;
#211120=CARTESIAN_POINT ( 'NONE',  ( 6.825078400183511640, 3.679815135839346496, 2.758192972206894744 ) ) ;
#211123=CARTESIAN_POINT ( 'NONE',  ( 4.557529213136806590, 0.4535224272249741562, -2.010195360780684393 ) ) ;
#211128=CARTESIAN_POINT ( 'NONE',  ( 3.053383268589305644, -1.780226508164801213, 0.9538969713841909392 ) ) ;
#211133=CARTESIAN_POINT ( 'NONE',  ( 2.553650737195617637, 0.5510486643308718513, -1.985768735985605549 ) ) ;
#211134=CARTESIAN_POINT ( 'NONE',  ( 3.410779880581996437, -1.203353552534730309, -1.617818353255598085 ) ) ;
#211136=( BOUNDED_CURVE ( )  B_SPLINE_CURVE ( 3, ( #21934, #88044, #154115, #110759 ),
 .UNSPECIFIED., .F., .T. ) 
 B_SPLINE_CURVE_WITH_KNOTS ( ( 4, 4 ),
 ( 0.5000000000000011102, 1.000000000000000000 ),
 .UNSPECIFIED. ) 
 CURVE ( )  GEOMETRIC_REPRESENTATION_ITEM ( )  RATIONAL_B_SPLINE_CURVE ( ( 0.9999999999999985567, 0.3333333333333333703, 0.3333333333333348691, 1.000000000000000000 ) ) 
 REPRESENTATION_ITEM ( '' )  );
#211141=CARTESIAN_POINT ( 'NONE',  ( 3.145861080134567000, -0.1455099638626895786, -2.010896398064919488 ) ) ;
#211142=CARTESIAN_POINT ( 'NONE',  ( 0.8492453639068753279, 1.839163117542693904, -0.08803940487626948919 ) ) ;
#211143=CARTESIAN_POINT ( 'NONE',  ( 0.08326089795122111614, -2.240168680488762387, -0.5538300120674977123 ) ) ;
#211145=CARTESIAN_POINT ( 'NONE',  ( 2.267066545249882381, -1.975312647937790711, -0.8782872871702240847 ) ) ;
#211147=CARTESIAN_POINT ( 'NONE',  ( 5.032460059670339270, 0.6174496738353585368, 2.025276144886530627 ) ) ;
#211150=CARTESIAN_POINT ( 'NONE',  ( 0.7603692911175019553, -1.357789551990191246, 1.287012767582619510 ) ) ;
#211151=CARTESIAN_POINT ( 'NONE',  ( 6.227413254736037906, -1.856526228437559434, 0.6636957074077839414 ) ) ;
#211155=CARTESIAN_POINT ( 'NONE',  ( 5.865875422609286183, 2.075172955015105014, -0.3584678469405917500 ) ) ;
#211156=CARTESIAN_POINT ( 'NONE',  ( 5.951642636407409093, 1.565221049572671719, 1.355249363302114318 ) ) ;
#211159=CARTESIAN_POINT ( 'NONE',  ( 6.639320575229256782, 0.5729255850590134758, 2.155858052613166986 ) ) ;
#211160=CARTESIAN_POINT ( 'NONE',  ( 5.436387729582301098, 1.942169232299725046, 0.3377773032272758380 ) ) ;
#211161=CARTESIAN_POINT ( 'NONE',  ( -0.2046613956954954905, -0.1581703332043625232, -2.086340352340488646 ) ) ;
#211163=CARTESIAN_POINT ( 'NONE',  ( 4.125798732227327292, -2.208944405816467338, 0.6678306985251744043 ) ) ;
#211164=CARTESIAN_POINT ( 'NONE',  ( 1.920832408274443903, -1.461550516301242775, 1.455605961035913776 ) ) ;
#211171=CARTESIAN_POINT ( 'NONE',  ( 4.756392321286846858, -2.170573799849393470, -0.05792142139850359195 ) ) ;
#211174=CARTESIAN_POINT ( 'NONE',  ( 3.614658571667620279, -0.1319153736358945894, 1.836568937333193485 ) ) ;
#211176=CARTESIAN_POINT ( 'NONE',  ( 6.620655732516684822, 7.053712996964945248, 2.324417015927725760 ) ) ;
#211177=CARTESIAN_POINT ( 'NONE',  ( 4.933237592207079025, -1.549687834843778811, -1.549900206446311657 ) ) ;
#211179=CARTESIAN_POINT ( 'NONE',  ( 5.664971525351325532, -2.042639428312309935, -0.9732368426803981176 ) ) ;
#211186=CARTESIAN_POINT ( 'NONE',  ( 0.8481071238514601429, 0.5083433500535933236, 1.695271877703796504 ) ) ;
#211188=CARTESIAN_POINT ( 'NONE',  ( 5.356112940025661295, 0.8138243144468767509, -1.841424879227879119 ) ) ;
#211190=CARTESIAN_POINT ( 'NONE',  ( 4.647555896809190124, -1.626162052001564717, -1.338137134695188468 ) ) ;
#211191=CARTESIAN_POINT ( 'NONE',  ( 1.651812010259229968, 0.9862763539280462455, 1.642055979085883299 ) ) ;
#211193=CARTESIAN_POINT ( 'NONE',  ( 2.629305401816001808, 0.09940027615944720119, -1.967183499748959452 ) ) ;
#211194=CARTESIAN_POINT ( 'NONE',  ( 5.045178214694073127, 0.1526089617210572014, 2.014106518579480642 ) ) ;
#211195=CARTESIAN_POINT ( 'NONE',  ( 1.569004590881704075, 0.1408476687595125731, -1.865417194689425795 ) ) ;
#211196=CARTESIAN_POINT ( 'NONE',  ( 1.978885927095444863, 1.829411362569667743, 0.7090815385668995940 ) ) ;
#211197=CARTESIAN_POINT ( 'NONE',  ( 4.828557952505812878, 1.651878126777156730, 0.4964739870837226454 ) ) ;
#211198=CARTESIAN_POINT ( 'NONE',  ( 1.212987991671743204, 1.561712320281399835, -1.103468303573502673 ) ) ;
#211200=CARTESIAN_POINT ( 'NONE',  ( 1.172829962703396456, -1.397616723802884708, 1.707921395779465890 ) ) ;
#211205=CARTESIAN_POINT ( 'NONE',  ( 6.789956943122251509, -0.7972922127613899512, 1.690610701080223821 ) ) ;
#211208=CARTESIAN_POINT ( 'NONE',  ( 6.948098034395241207, -0.8905871627266357393, 1.867117781285509537 ) ) ;
#211209=CARTESIAN_POINT ( 'NONE',  ( 0.7134375191242479097, -1.748147108003229810, -1.108949491591210146 ) ) ;
#211214=CARTESIAN_POINT ( 'NONE',  ( 4.899148033862871898, -0.2601683324335196668, -2.104413843559429065 ) ) ;
#211219=CARTESIAN_POINT ( 'NONE',  ( 6.303176765056641706, -1.658072099422291057, 1.048360225930293321 ) ) ;
#211221=CARTESIAN_POINT ( 'NONE',  ( 4.200545946899570282, -1.388273439763810790, -1.462221600879671790 ) ) ;
#211222=CARTESIAN_POINT ( 'NONE',  ( 3.907376549751972572, -1.831493090834277249, 0.5616838290606884776 ) ) ;
#211223=CARTESIAN_POINT ( 'NONE',  ( 1.927518781310177065, -1.434474475899261581, -1.656937093973806174 ) ) ;
#211226=CARTESIAN_POINT ( 'NONE',  ( 4.816656863388896426, -0.6821788116995251006, -1.894207565886153910 ) ) ;
#211228=CARTESIAN_POINT ( 'NONE',  ( 5.976184116172984950, -2.107040639921609504, -0.2072291863110999888 ) ) ;
#211230=CARTESIAN_POINT ( 'NONE',  ( 3.386350598701783454, -0.4101191253191734387, -2.049945593880502681 ) ) ;
#211232=CARTESIAN_POINT ( 'NONE',  ( 1.764246635482754622, -1.222956780391671439, 1.216502489609740723 ) ) ;
#211234=CARTESIAN_POINT ( 'NONE',  ( 5.695592476053610298, 1.958610405324921588, -0.8133567297157192622 ) ) ;
#211243=CARTESIAN_POINT ( 'NONE',  ( 2.244508708441519840, 1.757319924227723762, 0.4390839574351864671 ) ) ;
#211249=CARTESIAN_POINT ( 'NONE',  ( 2.473076435208894530, -1.576862618776267100, -0.8914009245391883995 ) ) ;
#211256=CARTESIAN_POINT ( 'NONE',  ( 4.211269073929763351, -1.546465011353677532, -1.035020834652039090 ) ) ;
#211257=CARTESIAN_POINT ( 'NONE',  ( 2.038566206862189478, -1.479296367703235360, 1.217016582141629666 ) ) ;
#211258=CARTESIAN_POINT ( 'NONE',  ( 6.809608091213839920, -0.4246860027747687560, 1.886121680295702596 ) ) ;
#211264=CARTESIAN_POINT ( 'NONE',  ( 4.311352223092364433, -1.634989290354519342, -1.097634987119990191 ) ) ;
#211268=CARTESIAN_POINT ( 'NONE',  ( 0.6914939563917784637, -0.7507456521842426067, 1.951374281879012962 ) ) ;
#211270=CARTESIAN_POINT ( 'NONE',  ( 5.543948526327937998, 0.7806568236609288114, -1.761304856208524283 ) ) ;
#211273=CARTESIAN_POINT ( 'NONE',  ( 1.342497868159111984, 0.3520595052693386018, 1.791136884925909056 ) ) ;
#211274=CARTESIAN_POINT ( 'NONE',  ( 1.752831059180045115, 0.6944836804415283060, 2.094827981560241970 ) ) ;
#211276=CARTESIAN_POINT ( 'NONE',  ( -0.1229892814952095459, -1.709044814581164973, -0.8582256167319823881 ) ) ;
#211279=CARTESIAN_POINT ( 'NONE',  ( 0.2210688645036896216, -1.757681936009440893, -0.8888059845142733950 ) ) ;
#211280=CARTESIAN_POINT ( 'NONE',  ( 1.206472709818911637, 1.713414686832109179, 0.9141866466196489904 ) ) ;
#211281=CARTESIAN_POINT ( 'NONE',  ( 1.001327120302420548, 1.985796081718914419, 0.3474166314290441648 ) ) ;
#211283=CARTESIAN_POINT ( 'NONE',  ( 5.524199568661091853, 0.9153802634506421620, 1.620121770064205213 ) ) ;
#211286=CARTESIAN_POINT ( 'NONE',  ( 6.509000000000039421, 2.968845098214094147, 2.453284407971462411 ) ) ;
#211289=CARTESIAN_POINT ( 'NONE',  ( 1.786939262935317130, 1.904797134731281538, -1.083727916527020607 ) ) ;
#211293=CARTESIAN_POINT ( 'NONE',  ( 1.594096589105632011, -1.816728215151931058, -0.1805768397986490248 ) ) ;
#211298=CARTESIAN_POINT ( 'NONE',  ( 6.609000000000038177, 2.443064466336189788, 2.382833824652215160 ) ) ;
#211300=CARTESIAN_POINT ( 'NONE',  ( 1.154767827468632824, -1.519305277103833118, 1.184426060187010465 ) ) ;
#211301=CARTESIAN_POINT ( 'NONE',  ( 5.858247074779933783, -1.961936380223072263, -0.003592477671530979431 ) ) ;
#211304=CARTESIAN_POINT ( 'NONE',  ( 5.355090213057959403, 0.4282289882464126451, -2.149144931432686256 ) ) ;
#211305=AXIS2_PLACEMENT_3D ( 'NONE', #175668, #62959, #158351 ) ;
#211307=CARTESIAN_POINT ( 'NONE',  ( 3.819242646454374057, -1.823515126939363462, -0.9802443236400715243 ) ) ;
#211311=CARTESIAN_POINT ( 'NONE',  ( 3.991116696687820209, -2.292486273863734603, 0.1698809440028921647 ) ) ;
#211318=CARTESIAN_POINT ( 'NONE',  ( 3.714730536668510830, -0.1420231480665778423, 1.936809614188730544 ) ) ;
#211321=CARTESIAN_POINT ( 'NONE',  ( 5.168181644781757456, 1.909928461159452251, -0.09994665148223277895 ) ) ;
#211322=CARTESIAN_POINT ( 'NONE',  ( 6.493153095729292446, 1.497681883954028237, -0.8552637798607003461 ) ) ;
#211323=CARTESIAN_POINT ( 'NONE',  ( 4.592982591267942283, 1.756852934926198317, 0.9896879400849432074 ) ) ;
#211325=CARTESIAN_POINT ( 'NONE',  ( 0.1709339574563934483, -1.438030690398562239, 1.674123062825278563 ) ) ;
#211328=CARTESIAN_POINT ( 'NONE',  ( 1.271554197678253839, 1.246673013970694077, 1.678101005879296004 ) ) ;
#211329=CARTESIAN_POINT ( 'NONE',  ( 6.749276393231373739, -1.423207027788903067, -1.051611706393209111 ) ) ;
#211330=CARTESIAN_POINT ( 'NONE',  ( 5.274064633610318076, 1.777012466945230962, -0.9530095070046653571 ) ) ;
#211332=CARTESIAN_POINT ( 'NONE',  ( 2.677988851928223557, -1.177355775514120850, 1.966668201240986402 ) ) ;
#211333=CARTESIAN_POINT ( 'NONE',  ( 0.5326489567317398421, -1.227437504408007474, -1.234024486680666000 ) ) ;
#211336=CARTESIAN_POINT ( 'NONE',  ( 0.7547592729708142434, -1.719773315039843986, -0.2198852240756724863 ) ) ;
#211339=CARTESIAN_POINT ( 'NONE',  ( 1.416727708472965253, 0.8794254021464522619, 1.985261695379604507 ) ) ;
#211340=CARTESIAN_POINT ( 'NONE',  ( 2.536342520008515233, 0.6839386381054488595, 1.897109991223707937 ) ) ;
#211341=CARTESIAN_POINT ( 'NONE',  ( 3.812500000000003109, 1.451031289061270213, 1.451031289060960905 ) ) ;
#211343=CARTESIAN_POINT ( 'NONE',  ( 0.3406813593837527687, 0.3259726575214479394, 1.898462188649749249 ) ) ;
#211345=CARTESIAN_POINT ( 'NONE',  ( 3.850012423022421082, -1.533692773617735705, -1.607201352943017802 ) ) ;
#211352=CARTESIAN_POINT ( 'NONE',  ( 5.495574104867783305, -1.740626723225440209, 0.008114992421901638317 ) ) ;
#211354=CARTESIAN_POINT ( 'NONE',  ( 3.701569118832209959, -1.483977648892897960, -1.283320388228793130 ) ) ;
#211358=CARTESIAN_POINT ( 'NONE',  ( 4.095213043127944097, 1.914038588809761299, -1.205934879490217382 ) ) ;
#211359=CARTESIAN_POINT ( 'NONE',  ( 1.680209433476518521, -1.144093268944153641, -1.716113171863597797 ) ) ;
#211361=CARTESIAN_POINT ( 'NONE',  ( 2.536292628665572479, 1.067014414141453704, -1.995120597088717806 ) ) ;
#211364=CARTESIAN_POINT ( 'NONE',  ( 3.338976900156843453, -1.651226333174139693, 0.8788041501476551165 ) ) ;
#211365=CARTESIAN_POINT ( 'NONE',  ( 2.074501327421875096, -0.7402772072304538709, 1.568325542203717227 ) ) ;
#211366=CARTESIAN_POINT ( 'NONE',  ( -0.09359539843449991847, -0.9867227890145138236, -2.066685918926200571 ) ) ;
#211367=CARTESIAN_POINT ( 'NONE',  ( 6.264718444480717352, -1.637942392629457178, 1.625721277839597745 ) ) ;
#211368=CARTESIAN_POINT ( 'NONE',  ( 4.065412822539622439, 0.2671453805177248508, -2.145074402785766665 ) ) ;
#211369=CARTESIAN_POINT ( 'NONE',  ( 4.892492844921223494, 1.613610725055414141, -1.080192228897313145 ) ) ;
#211376=CARTESIAN_POINT ( 'NONE',  ( 6.135388727473008785, 0.6351960432287793168, 1.913804721665197883 ) ) ;
#211380=CARTESIAN_POINT ( 'NONE',  ( 3.070728972534173096, -1.687097908962056803, -0.6982200720766564839 ) ) ;
#211381=CARTESIAN_POINT ( 'NONE',  ( -0.1296875068448125057, 0.2507808023153486054, -1.861542470327881560 ) ) ;
#211387=CARTESIAN_POINT ( 'NONE',  ( -0.1227786480478709891, -1.806133744752127068, -0.9041943026713550324 ) ) ;
#211388=CARTESIAN_POINT ( 'NONE',  ( 0.7156801077207708417, 1.735845614737155707, 1.217653249118654468 ) ) ;
#211390=CARTESIAN_POINT ( 'NONE',  ( 1.709564315929460232, 0.5465817987246027743, -1.778839887662834185 ) ) ;
#211392=CARTESIAN_POINT ( 'NONE',  ( 6.403207051292992169, 1.711950105385249055, 1.147064539034772679 ) ) ;
#211393=CARTESIAN_POINT ( 'NONE',  ( 6.012342310302175363, -1.897698807000438359, 0.6819931642896917001 ) ) ;
#211398=CARTESIAN_POINT ( 'NONE',  ( 3.422296110638740174, 1.157362003623555236, -1.411967061744797691 ) ) ;
#211403=CARTESIAN_POINT ( 'NONE',  ( 6.450546045330813882, 1.388275245401158431, 1.462219883709668045 ) ) ;
#211404=CARTESIAN_POINT ( 'NONE',  ( 6.140549721451361798, -1.552764191669778304, 0.9890077265983505672 ) ) ;
#211405=CARTESIAN_POINT ( 'NONE',  ( 0.07680821025391608436, 6.948789780205374633, -2.405840108717867132 ) ) ;
#211406=CARTESIAN_POINT ( 'NONE',  ( 3.352467919438668620, 2.307868970251240714, 0.0003179301051748489328 ) ) ;
#211408=CARTESIAN_POINT ( 'NONE',  ( 5.993488848236776967, 1.632462841753023808, 1.416962642945495565 ) ) ;
#211409=CARTESIAN_POINT ( 'NONE',  ( 1.399837892970667630, -0.7005499098489911258, -1.811468074468420841 ) ) ;
#211413=CARTESIAN_POINT ( 'NONE',  ( 4.394144163123720581, 0.1076087731387373875, 2.295966082354545801 ) ) ;
#211416=CARTESIAN_POINT ( 'NONE',  ( 5.155093292349416600, -1.580716073637401076, -1.000049079914612449 ) ) ;
#211417=CARTESIAN_POINT ( 'NONE',  ( 1.336036003918249948, -1.064896177285217016, -1.588262137521757822 ) ) ;
#211420=CARTESIAN_POINT ( 'NONE',  ( 3.756632125300945368, 0.7937082651479386852, 2.059386989456575279 ) ) ;
#211427=CARTESIAN_POINT ( 'NONE',  ( 1.774623370849885085, -1.870687226035630646, -0.6220538675408300300 ) ) ;
#211428=CARTESIAN_POINT ( 'NONE',  ( 0.8159566880532771460, -0.3350741789154148553, 2.283031499596111402 ) ) ;
#211429=CARTESIAN_POINT ( 'NONE',  ( 2.769914238037580745, -1.940913097850523128, 0.2850433363836765155 ) ) ;
#211430=CARTESIAN_POINT ( 'NONE',  ( 5.770399673640999261, -0.9225087518928692942, -1.844811731271531086 ) ) ;
#211437=CARTESIAN_POINT ( 'NONE',  ( 0.5148107762544695820, 0.8296010825015688317, 2.006500992472683098 ) ) ;
#211441=CARTESIAN_POINT ( 'NONE',  ( 2.618241971997347317, 1.224968108320439342, -1.413705424714882586 ) ) ;
#211442=CARTESIAN_POINT ( 'NONE',  ( 6.503215372615936296, 1.793156143535659108, 1.206815395834538451 ) ) ;
#211443=CARTESIAN_POINT ( 'NONE',  ( 6.727182134110231360, 6.039168392632435989, 2.405853653942995773 ) ) ;
#211445=CARTESIAN_POINT ( 'NONE',  ( 2.139182944796279351, 0.001596215867826628054, 1.912461472203148771 ) ) ;
#211446=CARTESIAN_POINT ( 'NONE',  ( 4.328786618740396719, 0.08755327933733339507, 1.767792532789840498 ) ) ;
#211447=CARTESIAN_POINT ( 'NONE',  ( 1.945825403448407487, -1.250168254263404277, -1.447093241409423081 ) ) ;
#211449=CARTESIAN_POINT ( 'NONE',  ( 5.466386403393696192, -1.869944189333021090, -0.4150143681153609654 ) ) ;
#211451=CARTESIAN_POINT ( 'NONE',  ( 0.2915762745691782287, -1.893489616766583339, 0.8377075429084477332 ) ) ;
#211453=CARTESIAN_POINT ( 'NONE',  ( 2.303126745213024851, -0.3670769733005623814, -2.088442229865586697 ) ) ;
#211454=CARTESIAN_POINT ( 'NONE',  ( 4.750782166719051069, -1.502237938222051650, 1.114538048626475986 ) ) ;
#211455=CARTESIAN_POINT ( 'NONE',  ( 2.226930044512597906, -0.0006860120723567450030, 1.825872481329051222 ) ) ;
#211456=ORIENTED_EDGE ( 'NONE', *, *, #39650, .T. ) ;
#211457=CARTESIAN_POINT ( 'NONE',  ( 4.969440760808212509, 0.2186952961555181096, -2.196011921426939129 ) ) ;
#211460=CARTESIAN_POINT ( 'NONE',  ( 1.363816705371086568, -0.5030291501087379435, 2.000271598109978566 ) ) ;
#211469=CARTESIAN_POINT ( 'NONE',  ( 3.982925052038261526, 1.964963782255540359, 0.6523228965355857278 ) ) ;
#211471=CARTESIAN_POINT ( 'NONE',  ( 2.513140823169751847, 1.929641211675875878, 0.9743453106897670413 ) ) ;
#211473=CARTESIAN_POINT ( 'NONE',  ( 1.629563124460619239, -0.2448459300014929063, 2.004692427041386615 ) ) ;
#211474=CARTESIAN_POINT ( 'NONE',  ( 6.720655732516647163, -0.001531948155462491612, 2.073773125298985054 ) ) ;
#211480=CARTESIAN_POINT ( 'NONE',  ( 1.657435761918718331, 1.928256795251210631, -0.5899901959932273288 ) ) ;
#211481=CARTESIAN_POINT ( 'NONE',  ( 6.005464345382193869, -2.175231771021503668, 0.2666438670960933344 ) ) ;
#211483=CARTESIAN_POINT ( 'NONE',  ( 4.904515063324526025, -1.898637117948184017, -0.2282459111111398431 ) ) ;
#211487=CARTESIAN_POINT ( 'NONE',  ( 1.757435634535610136, 1.928746520693159550, -0.5880414618760835266 ) ) ;
#211490=CARTESIAN_POINT ( 'NONE',  ( 5.719686907728898539, -1.681737053624256628, 0.3821217278023018582 ) ) ;
#211499=CARTESIAN_POINT ( 'NONE',  ( 1.270471156847551075, -0.9273748054965322840, -1.850965650132020635 ) ) ;
#211501=CARTESIAN_POINT ( 'NONE',  ( 4.617698128633199062, -0.4785133679615029556, 1.747060762061508621 ) ) ;
#211503=CARTESIAN_POINT ( 'NONE',  ( 6.609999999999971898, -0.005249217919313342931, 2.280159464062641472 ) ) ;
#211504=CARTESIAN_POINT ( 'NONE',  ( 6.182253972182746971, 0.9374619682817868505, 1.549891177688822452 ) ) ;
#211507=CARTESIAN_POINT ( 'NONE',  ( 3.134921595499224445, -1.932508288125428741, 1.033376004005027715 ) ) ;
#211510=CARTESIAN_POINT ( 'NONE',  ( 0.1507198084474276056, -0.4258245693303016610, -1.922078969575198526 ) ) ;
#211512=CARTESIAN_POINT ( 'NONE',  ( 4.376519623831674366, -0.4236097701148673900, -1.868001571610947043 ) ) ;
#211518=CARTESIAN_POINT ( 'NONE',  ( 1.428841412761387986, 2.083414371474631377, 0.5762002773818803991 ) ) ;
#211521=CARTESIAN_POINT ( 'NONE',  ( 2.133574855335911291, -1.190200692204022470, -1.384352166806518625 ) ) ;
#211524=CARTESIAN_POINT ( 'NONE',  ( 4.119992258926360229, -0.9384382104282267267, -1.565754920925747973 ) ) ;
#211527=CARTESIAN_POINT ( 'NONE',  ( 4.211352281912852824, -1.636193967830642748, -1.096030559421146133 ) ) ;
#211529=CARTESIAN_POINT ( 'NONE',  ( 4.546391927783274056, -1.557747286768229600, 1.159548114344757019 ) ) ;
#211533=CARTESIAN_POINT ( 'NONE',  ( 5.027636390373714903, -0.3086946445357250379, 2.097867224209007730 ) ) ;
#211535=CARTESIAN_POINT ( 'NONE',  ( 2.772007568003355793, 1.902874960710929431, -0.1895390408453850317 ) ) ;
#211537=CARTESIAN_POINT ( 'NONE',  ( 6.983263157960370116, 2.969675876345272414, 2.399270433241917466 ) ) ;
#211540=CARTESIAN_POINT ( 'NONE',  ( 5.057293878089731187, -1.725371964895198840, 1.036928162195766889 ) ) ;
#211542=CARTESIAN_POINT ( 'NONE',  ( 6.182242880246401562, -0.9723386526096773341, 1.545037271442825100 ) ) ;
#211543=CARTESIAN_POINT ( 'NONE',  ( 0.5024991115675537801, 2.064720838319131779, 0.1538615064654233477 ) ) ;
#211557=CARTESIAN_POINT ( 'NONE',  ( 1.481394567461959522, -0.05474761849930119550, 2.069712792878583230 ) ) ;
#211558=CARTESIAN_POINT ( 'NONE',  ( 2.654045540373184409, 1.135223644230592743, 1.786994778491631797 ) ) ;
#211561=CARTESIAN_POINT ( 'NONE',  ( 0.4265231311835169792, -1.290831556599820074, 1.487489745873808555 ) ) ;
#211567=CARTESIAN_POINT ( 'NONE',  ( 2.273717984289443717, 1.411852697042052185, 1.805783550510152935 ) ) ;
#211568=CARTESIAN_POINT ( 'NONE',  ( 0.2756506080626683342, 1.048234779247591453, 1.494575289200591017 ) ) ;
#211569=CARTESIAN_POINT ( 'NONE',  ( 2.127084423382288314, 1.709874882824816478, 0.8565708355050825062 ) ) ;
#211572=CARTESIAN_POINT ( 'NONE',  ( 1.265886429849511163, 0.5802531365422005649, -1.927800331509860632 ) ) ;
#211573=CARTESIAN_POINT ( 'NONE',  ( 2.676550354755039773, 1.285117694784821518, -1.482265789204496143 ) ) ;
#211577=CARTESIAN_POINT ( 'NONE',  ( 4.611325087297634795, -2.050354119209703008, 0.4075000692524420876 ) ) ;
#211578=CARTESIAN_POINT ( 'NONE',  ( 3.309201167148849265, -0.3463371335676104223, 1.735430568453823374 ) ) ;
#211581=CARTESIAN_POINT ( 'NONE',  ( 6.351568543859240634, 2.286598795830016684, -0.1622092447367465551 ) ) ;
#211582=CARTESIAN_POINT ( 'NONE',  ( 3.995860056160570384, -0.5486252962480555606, -1.651658045138884257 ) ) ;
#211584=CARTESIAN_POINT ( 'NONE',  ( -0.1104750535120025967, -0.004616138082884357029, -2.103378236956429337 ) ) ;
#211585=CARTESIAN_POINT ( 'NONE',  ( 3.989331682606485519, 1.645927443309925353, 0.5452122354672321869 ) ) ;
#211586=CARTESIAN_POINT ( 'NONE',  ( 4.615793470729397718, 0.4799340867196815741, -2.117318520224883205 ) ) ;
#211588=CARTESIAN_POINT ( 'NONE',  ( 6.139861302770143858, 2.010801613648224961, -0.1531635369260639090 ) ) ;
#211589=CARTESIAN_POINT ( 'NONE',  ( 4.718750000000002665, -0.7852924748297362978, 1.895863743164184045 ) ) ;
#211591=CARTESIAN_POINT ( 'NONE',  ( 3.065363963417499615, 0.2843319914107733104, -1.905185398925368423 ) ) ;
#211593=CARTESIAN_POINT ( 'NONE',  ( 0.2939904269894151323, 2.070328538627811632, -0.8053792395062376874 ) ) ;
#211595=CARTESIAN_POINT ( 'NONE',  ( 6.883263157960364254, 6.036844454314826081, 2.541088405340941492 ) ) ;
#211598=CARTESIAN_POINT ( 'NONE',  ( 1.612303553688280600, -0.7442547213242669546, 2.093046284049724370 ) ) ;
#211599=CARTESIAN_POINT ( 'NONE',  ( 6.566857081534598350, 1.454584517406570132, -1.316677807353151097 ) ) ;
#211606=CARTESIAN_POINT ( 'NONE',  ( 6.074688485276667826, 1.387953460639863801, -1.525998863508086778 ) ) ;
#211611=CARTESIAN_POINT ( 'NONE',  ( 6.643822754079466542, 0.7155741859487285694, -1.728458771772640512 ) ) ;
#211612=CARTESIAN_POINT ( 'NONE',  ( 5.836466137708809399, 0.4949425091341461136, -1.662031903658898413 ) ) ;
#211613=CARTESIAN_POINT ( 'NONE',  ( 5.337372294182569199, 0.6981903941610733133, -1.594458651668466898 ) ) ;
#211615=CARTESIAN_POINT ( 'NONE',  ( 3.035043143063915760, -2.020573557004992971, 1.082744910948540307 ) ) ;
#211617=CARTESIAN_POINT ( 'NONE',  ( 1.165666007907351309, -1.169451938622353859, 1.422036577929463030 ) ) ;
#211620=CARTESIAN_POINT ( 'NONE',  ( 1.957752326685862077, 1.820926393389955988, -0.1310869387763091420 ) ) ;
#211622=CARTESIAN_POINT ( 'NONE',  ( 2.356092462967720458, 0.09613450340887133572, -2.014232768679749430 ) ) ;
#211623=CARTESIAN_POINT ( 'NONE',  ( 1.535386672163775668, -1.589036399888818618, -1.509351277865833563 ) ) ;
#211625=CARTESIAN_POINT ( 'NONE',  ( 4.049914914165038127, 0.7116930038560628224, -1.982186593211773706 ) ) ;
#211628=CARTESIAN_POINT ( 'NONE',  ( 1.012269475826784060, 2.068064858651061932, -0.09981174449213289779 ) ) ;
#211631=CARTESIAN_POINT ( 'NONE',  ( 3.949941927655271190, -1.463281269271698770, -1.534908012577620662 ) ) ;
#211632=CARTESIAN_POINT ( 'NONE',  ( 6.428339884752386268, 1.046657586246093175, -1.495688092090130095 ) ) ;
#211639=CARTESIAN_POINT ( 'NONE',  ( 0.01825978460381037782, -0.5840345307000054387, 2.143236301556954881 ) ) ;
#211640=CARTESIAN_POINT ( 'NONE',  ( 1.413257319143443658, 1.857191001717144685, 0.9929431703323916558 ) ) ;
#211644=CARTESIAN_POINT ( 'NONE',  ( 5.436322145542998641, -1.035505548906799023, 1.546008503351968821 ) ) ;
#211650=CARTESIAN_POINT ( 'NONE',  ( 1.943732651021431224, 1.350599318427040840, 1.423195245143428433 ) ) ;
#211651=CARTESIAN_POINT ( 'NONE',  ( 0.8663662989462637132, 1.066309655776727539, 1.880320099339624296 ) ) ;
#211655=CARTESIAN_POINT ( 'NONE',  ( 3.128000772048340927, 0.2569867100842055940, -1.714543959099825710 ) ) ;
#211656=CARTESIAN_POINT ( 'NONE',  ( 2.870765623479579531, 1.652405209062355773, -0.5463526510798635272 ) ) ;
#211659=CARTESIAN_POINT ( 'NONE',  ( 2.460294058246147664, 0.8780975587320086762, 1.864460488959890139 ) ) ;
#211662=CARTESIAN_POINT ( 'NONE',  ( 0.6849224457974397717, -1.076149790962807495, -1.704679027301945649 ) ) ;
#211663=CARTESIAN_POINT ( 'NONE',  ( 6.825078400183568483, -0.002763825414428457399, 2.044262525762724270 ) ) ;
#211665=CARTESIAN_POINT ( 'NONE',  ( 1.446098081747126951, 1.969109070040415910, 0.09893570862591105630 ) ) ;
#211666=CARTESIAN_POINT ( 'NONE',  ( 6.047114369478562956, 0.1942372860762129894, 1.902532258075719351 ) ) ;
#211671=CARTESIAN_POINT ( 'NONE',  ( 0.6979228276546626253, 1.358177971483988555, 1.494960626620364552 ) ) ;
#211673=CARTESIAN_POINT ( 'NONE',  ( 4.682853559034357183, -2.237096095179165633, -0.5655516052204231370 ) ) ;
#211674=CARTESIAN_POINT ( 'NONE',  ( 5.547302793442128177, 1.730978599593002043, -0.9233319674036490898 ) ) ;
#211676=CARTESIAN_POINT ( 'NONE',  ( 2.043732491806522056, 1.349072470436333715, 1.424505092005624807 ) ) ;
#211680=CARTESIAN_POINT ( 'NONE',  ( 1.429080218188124585, -1.785550482114751203, 1.137718905448012352 ) ) ;
#211683=CARTESIAN_POINT ( 'NONE',  ( 0.5855841007226803008, -1.826885663252286740, -0.2280376995877145263 ) ) ;
#211684=ORIENTED_EDGE ( 'NONE', *, *, #99041, .T. ) ;
#211685=CARTESIAN_POINT ( 'NONE',  ( 3.872083141701920805, -2.139866411213369624, 0.3658599195538684290 ) ) ;
#211687=CARTESIAN_POINT ( 'NONE',  ( 1.986737319265439394, -1.300789755646198476, 1.674730562594067829 ) ) ;
#211692=CARTESIAN_POINT ( 'NONE',  ( 3.040362567271452487, 2.044824973086068809, 0.2555446107466197714 ) ) ;
#211694=CARTESIAN_POINT ( 'NONE',  ( 0.4855842612344652975, -1.827229208960782447, -0.2260576252584786672 ) ) ;
#211699=CARTESIAN_POINT ( 'NONE',  ( 2.179354884421313088, -0.1095372306593382361, -2.259850278934079970 ) ) ;
#211702=CARTESIAN_POINT ( 'NONE',  ( 2.601584773815317497, 1.283861566028346779, 1.278364218381728090 ) ) ;
#211703=CARTESIAN_POINT ( 'NONE',  ( 1.868237732200584977, -1.879526469796377164, -0.3696609625283857614 ) ) ;
#211704=CARTESIAN_POINT ( 'NONE',  ( 3.543477799061961253, 1.872898848466747479, -0.8826743078152868849 ) ) ;
#211706=CARTESIAN_POINT ( 'NONE',  ( 1.498834128701274748, 1.612947343535120925, -1.133365233443942355 ) ) ;
#211707=CARTESIAN_POINT ( 'NONE',  ( 6.094356125077982078, -1.917462007409322267, -0.1864201481798656301 ) ) ;
#211708=CARTESIAN_POINT ( 'NONE',  ( 2.852262661058731386, 0.6285613048715790185, 1.762029509812724992 ) ) ;
#211709=CARTESIAN_POINT ( 'NONE',  ( 1.278406981455294744, 1.378070038918308038, 1.850917983980376658 ) ) ;
#211711=CARTESIAN_POINT ( 'NONE',  ( 2.418200368955259361, 0.7924288909779563239, 1.684046449600750561 ) ) ;
#211713=CARTESIAN_POINT ( 'NONE',  ( 4.879373355499653897, -0.1046096447297485965, 2.060157192773376611 ) ) ;
#211718=CARTESIAN_POINT ( 'NONE',  ( 6.194376850977553417, -2.095475641407635425, -0.2099330270173524471 ) ) ;
#211720=CARTESIAN_POINT ( 'NONE',  ( 5.501312752317829791, 1.763641270444433085, 1.249554385337699802 ) ) ;
#211721=CARTESIAN_POINT ( 'NONE',  ( 6.076820933934619084, -1.426746821240878704, 1.429770112406039795 ) ) ;
#211726=CARTESIAN_POINT ( 'NONE',  ( 6.825078400183550720, 7.629137130509051623, 2.355651831298340326 ) ) ;
#211729=CARTESIAN_POINT ( 'NONE',  ( 5.014861385384292269, 0.1531656238677771009, 2.010801456750747285 ) ) ;
#211734=CARTESIAN_POINT ( 'NONE',  ( 5.524359596833869013, 1.291058806671550485, -1.733668313432787933 ) ) ;
#211739=CARTESIAN_POINT ( 'NONE',  ( 5.589470316598125876, -0.4871849528341637425, 1.956566939648955339 ) ) ;
#211741=CARTESIAN_POINT ( 'NONE',  ( 2.015808680039221201, -0.8114285025175859145, -1.522100016238505216 ) ) ;
#211747=CARTESIAN_POINT ( 'NONE',  ( 6.063714619507535097, 1.842885348237649490, -0.3194776537047139264 ) ) ;
#211748=CARTESIAN_POINT ( 'NONE',  ( 0.5572895418005788803, -1.725428541193659182, 1.036833936551822655 ) ) ;
#211750=CARTESIAN_POINT ( 'NONE',  ( 3.171135245091468491, -2.038329301889611589, -0.8460836234857532778 ) ) ;
#211751=CARTESIAN_POINT ( 'NONE',  ( 5.594640809421455252, 2.137687854117083841, 0.3785394800270032167 ) ) ;
#211755=CARTESIAN_POINT ( 'NONE',  ( 3.440189854244297241, -1.264556376030629981, -1.702001827410426049 ) ) ;
#211756=CARTESIAN_POINT ( 'NONE',  ( 1.722280025409760329, 1.994874335020242695, 0.2930476355553628953 ) ) ;
#211757=CARTESIAN_POINT ( 'NONE',  ( 1.740194394521710430, 1.041001882027743353, -1.482411077883559747 ) ) ;
#211763=CARTESIAN_POINT ( 'NONE',  ( 1.622146050056040512, 1.895417417167859497, 0.2770879218524437415 ) ) ;
#211771=CARTESIAN_POINT ( 'NONE',  ( 5.664953204072169513, -1.952404353424816774, -0.9282482345986733385 ) ) ;
#211774=CARTESIAN_POINT ( 'NONE',  ( 2.795306286867365486, -0.1602278063087131110, -2.114629986603839829 ) ) ;
#211775=CARTESIAN_POINT ( 'NONE',  ( -0.1298852118743892559, 2.894271690123681573, -2.215574276383952768 ) ) ;
#211777=CARTESIAN_POINT ( 'NONE',  ( 2.917208927397921592, -0.1969847599093167145, 1.961514860040159292 ) ) ;
#211781=CARTESIAN_POINT ( 'NONE',  ( 0.8892259839063383353, 0.1505779921940515187, 2.064926437897919964 ) ) ;
#211782=CARTESIAN_POINT ( 'NONE',  ( 2.466655979050590197, 0.09513121245676225968, -1.939734245173969640 ) ) ;
#211787=CARTESIAN_POINT ( 'NONE',  ( 2.800817752552913209, 1.766549217158249085, 1.117748608743725169 ) ) ;
#211790=CARTESIAN_POINT ( 'NONE',  ( 6.217437059193511750, 1.592560689453832001, 1.058264445519964125 ) ) ;
#211792=CARTESIAN_POINT ( 'NONE',  ( 3.862124860921032354, 2.190326239153097543, -0.2693113811002012525 ) ) ;
#211794=CARTESIAN_POINT ( 'NONE',  ( 2.907470687441279455, 1.863611109782586484, 1.181582751932461095 ) ) ;
#211797=CARTESIAN_POINT ( 'NONE',  ( 2.051281676579026492, -1.707476168062868060, 0.8611843332394366612 ) ) ;
#211800=CARTESIAN_POINT ( 'NONE',  ( 4.387213907293201487, 0.09840592021137170575, 2.068135374880715638 ) ) ;
#211802=CARTESIAN_POINT ( 'NONE',  ( 2.008865009297224447, 1.601992838228694316, -1.451600824242594845 ) ) ;
#211803=CARTESIAN_POINT ( 'NONE',  ( 4.458633810090739225, -1.957822973221786444, -0.9849130632908836835 ) ) ;
#211810=CARTESIAN_POINT ( 'NONE',  ( -0.01695367945527340853, -2.016028864686558730, -0.04667425414178058563 ) ) ;
#211813=CARTESIAN_POINT ( 'NONE',  ( 5.207906454484914072, 0.6546344234062730916, -1.964071172066352400 ) ) ;
#211814=CARTESIAN_POINT ( 'NONE',  ( 3.615773638797363798, -1.897832126884700932, 0.3302691188315133863 ) ) ;
#211815=CARTESIAN_POINT ( 'NONE',  ( 5.413701396201449079, -1.343708383727526101, -1.636158592728423455 ) ) ;
#211818=CARTESIAN_POINT ( 'NONE',  ( 4.539879430399799354, 1.283355579558099091, 1.494016145327778045 ) ) ;
#211819=CARTESIAN_POINT ( 'NONE',  ( 6.017577161850602430, -1.268579900078286471, -1.909058160655076053 ) ) ;
#211820=CARTESIAN_POINT ( 'NONE',  ( 3.598116246361187542, -1.823677485248562435, -0.08826725125678223927 ) ) ;
#211826=CARTESIAN_POINT ( 'NONE',  ( 1.030510548812729965, -1.664561007783531332, 0.7873658874757857307 ) ) ;
#211827=CARTESIAN_POINT ( 'NONE',  ( 5.150644359860614863, 1.984129689857921486, 0.3399971717471597654 ) ) ;
#211828=CARTESIAN_POINT ( 'NONE',  ( 5.783868576693856234, 1.881360230585613413, -1.320557073901595047 ) ) ;
#211829=CARTESIAN_POINT ( 'NONE',  ( 5.471523917629521172, -0.2915489554583711174, 1.939870717765689534 ) ) ;
#211834=CARTESIAN_POINT ( 'NONE',  ( 1.892240118738715005, -0.5608018070641508368, -2.014042591102585877 ) ) ;
#211835=CARTESIAN_POINT ( 'NONE',  ( 0.5494049127674709432, 0.5909524230637287490, -1.774924738581270089 ) ) ;
#211837=CARTESIAN_POINT ( 'NONE',  ( -0.1102773484824301209, 0.2280386113255315761, -2.237141580442712829 ) ) ;
#211838=CARTESIAN_POINT ( 'NONE',  ( 0.4502399561126956273, -1.468881883692290113, -0.9332017962183251081 ) ) ;
#211842=CARTESIAN_POINT ( 'NONE',  ( 2.244387868473923575, 0.3767020243423558901, 1.683057829810198136 ) ) ;
#211843=CARTESIAN_POINT ( 'NONE',  ( 2.103317784989285677, -0.4765762082987561321, 2.138964651187735821 ) ) ;
#211844=CARTESIAN_POINT ( 'NONE',  ( -0.1347034368660744441, -0.1421164721313403212, -1.704521202080215847 ) ) ;
#211845=CARTESIAN_POINT ( 'NONE',  ( 3.826972293661185187, 2.095320012007126476, 0.6930106488920934060 ) ) ;
#211848=CARTESIAN_POINT ( 'NONE',  ( 1.797964266608031547, -1.570508639683061647, -1.499219477302183412 ) ) ;
#211850=CARTESIAN_POINT ( 'NONE',  ( 2.501287867402203879, -0.2026288386562236921, 2.107594835487134777 ) ) ;
#211854=CARTESIAN_POINT ( 'NONE',  ( 2.208868952076637804, 2.049428429192188705, 1.027153634429162743 ) ) ;
#211858=CARTESIAN_POINT ( 'NONE',  ( 5.936230101866142306, -1.231883464771424075, -1.848230934346828391 ) ) ;
#211864=CARTESIAN_POINT ( 'NONE',  ( 3.885388821667290493, -0.6351983117205138862, -1.913803978180687482 ) ) ;
#211866=CARTESIAN_POINT ( 'NONE',  ( 2.219651360329556233, 0.3568934070868194919, -2.031323280462021152 ) ) ;
#211872=CARTESIAN_POINT ( 'NONE',  ( 4.822331674454460426, 2.096538211656114647, 0.6379635903819569354 ) ) ;
#211873=CARTESIAN_POINT ( 'NONE',  ( 2.180314765559120183, 1.560501322096979449, 1.277041908422072991 ) ) ;
#211874=CARTESIAN_POINT ( 'NONE',  ( 2.014959344526063845, -1.785600367564584179, 0.4486904387498573676 ) ) ;
#211876=CARTESIAN_POINT ( 'NONE',  ( 2.312500000000001776, 1.451031289061216478, 1.451031289061020857 ) ) ;
#211877=CARTESIAN_POINT ( 'NONE',  ( 5.368107995252269227, 0.9013511576922846880, 1.587453057759043551 ) ) ;
#211878=CARTESIAN_POINT ( 'NONE',  ( 5.608046130584797950, -0.04667949407829303371, 2.016033753796213635 ) ) ;
#211880=CARTESIAN_POINT ( 'NONE',  ( 5.190393989392352303, -2.244764952986468831, -0.2824595779603657486 ) ) ;
#211882=CARTESIAN_POINT ( 'NONE',  ( 0.8210893850928849824, 1.946682464879319729, 0.8042085006434143146 ) ) ;
#211893=CARTESIAN_POINT ( 'NONE',  ( 1.881254504445781794, -1.940830296247602949, -0.8548571619346673200 ) ) ;
#211894=CARTESIAN_POINT ( 'NONE',  ( 2.303257990033405367, -0.3847559998488152000, -2.187706203110438175 ) ) ;
#211899=CARTESIAN_POINT ( 'NONE',  ( 2.910546574502240968, 0.6583626327048962557, 1.848246418561696913 ) ) ;
#211905=CARTESIAN_POINT ( 'NONE',  ( 2.074623746436579985, 0.9110886696130392481, 1.915067268644244702 ) ) ;
#211907=CARTESIAN_POINT ( 'NONE',  ( 4.135729569369491543, -1.488772398488470872, -1.567562023322838671 ) ) ;
#211908=CARTESIAN_POINT ( 'NONE',  ( 2.893917256732419396, -0.5369380550670297403, -1.761199466696103499 ) ) ;
#211911=CARTESIAN_POINT ( 'NONE',  ( 5.999919492459485859, -0.6329648550039753685, -1.621342527780894827 ) ) ;
#211916=CARTESIAN_POINT ( 'NONE',  ( 3.256853613824191029, -1.637998819981079990, 1.410756932016984377 ) ) ;
#211918=CARTESIAN_POINT ( 'NONE',  ( 4.956407584168041502, 1.492027487219639514, 1.356091576722208369 ) ) ;
#211920=CARTESIAN_POINT ( 'NONE',  ( 2.096749907087645415, -0.5762017740289016032, -2.083436276955972222 ) ) ;
#211922=CARTESIAN_POINT ( 'NONE',  ( 2.864479682042244679, -1.362014001507254379, 1.425398218059505728 ) ) ;
#211924=CARTESIAN_POINT ( 'NONE',  ( 4.159667821157567502, 0.9185609468507827113, 1.711114809252372915 ) ) ;
#211927=ORIENTED_EDGE ( 'NONE', *, *, #148167, .T. ) ;
#211933=CARTESIAN_POINT ( 'NONE',  ( 1.694636308673210801, -2.196210861363355082, -0.2157497520150277459 ) ) ;
#211935=CARTESIAN_POINT ( 'NONE',  ( 5.717619619964247946, 0.3862620380215216476, -1.923179868201368548 ) ) ;
#211940=CARTESIAN_POINT ( 'NONE',  ( 3.802549092506895878, 1.579937072410386278, 0.9450539169142122553 ) ) ;
#211944=CARTESIAN_POINT ( 'NONE',  ( 6.082307721193076944, 1.091511717630256673, 1.817998432235830908 ) ) ;
#211948=CARTESIAN_POINT ( 'NONE',  ( 6.450472299244985663, 0.6421947732520795205, 1.958257120725328315 ) ) ;
#211950=CARTESIAN_POINT ( 'NONE',  ( 1.890827768869116632, 0.1781016032055370568, 1.852494144255438346 ) ) ;
#211951=CARTESIAN_POINT ( 'NONE',  ( 4.071694929070113211, -1.056692140236010102, 1.507659738195665788 ) ) ;
#211955=CARTESIAN_POINT ( 'NONE',  ( 2.807470779205251343, 1.864772411128329477, 1.179945617918669143 ) ) ;
#211956=CARTESIAN_POINT ( 'NONE',  ( 5.940765808339826037, 0.4328084161881738945, 2.220481174026817772 ) ) ;
#211958=CARTESIAN_POINT ( 'NONE',  ( 6.047087830114247886, 0.1867083960328217995, 1.801967238635309165 ) ) ;
#211959=CARTESIAN_POINT ( 'NONE',  ( 4.874201634824506080, -1.902012294098894829, -0.2279625308443770371 ) ) ;
#211961=CARTESIAN_POINT ( 'NONE',  ( 6.051601594667258333, 0.5412791183288803154, -1.790613848972313571 ) ) ;
#211962=CARTESIAN_POINT ( 'NONE',  ( 5.863677653134839574, -0.4517109595482105555, 1.805248464757176041 ) ) ;
#211964=CARTESIAN_POINT ( 'NONE',  ( 0.09234973940512071489, -0.4041859633337717694, -1.833079292876439670 ) ) ;
#211965=CARTESIAN_POINT ( 'NONE',  ( 1.587125413319636635, 1.679225032509903404, 1.116207499648947943 ) ) ;
#211967=CARTESIAN_POINT ( 'NONE',  ( 2.772209899791327370, 1.127123820452385017, 1.778883819610539208 ) ) ;
#211972=CARTESIAN_POINT ( 'NONE',  ( 3.181903496825384092, 1.969597418195143446, -0.4466673548119536319 ) ) ;
#211975=CARTESIAN_POINT ( 'NONE',  ( 3.796290242343594468, -2.158924006851222988, -0.1102321833298808978 ) ) ;
#211981=CARTESIAN_POINT ( 'NONE',  ( 0.8190779338598102033, -1.572544420714114821, 1.497277704674306431 ) ) ;
#211985=CARTESIAN_POINT ( 'NONE',  ( 2.489988787850425656, -2.185901284972164405, -0.1580625509675498419 ) ) ;
#211987=CARTESIAN_POINT ( 'NONE',  ( 2.518781164845237175, 1.478067295746248400, -1.713045486838754794 ) ) ;
#211994=CARTESIAN_POINT ( 'NONE',  ( 3.426767255637660270, 0.04027588734063606429, 1.769438255327019593 ) ) ;
#211996=CARTESIAN_POINT ( 'NONE',  ( 5.983472182158235952, 2.041168445429199618, -0.8392293214988936212 ) ) ;
#212001=CARTESIAN_POINT ( 'NONE',  ( 4.904484127313208042, -1.798792703336571375, -0.2141664767603863595 ) ) ;
#212003=CARTESIAN_POINT ( 'NONE',  ( 3.906994808788874174, 1.604092888448312326, 0.9621832354540850174 ) ) ;
#212004=CARTESIAN_POINT ( 'NONE',  ( 3.028250241984064228, 1.103615759228196325, 1.751372171329562688 ) ) ;
#212010=CARTESIAN_POINT ( 'NONE',  ( 2.875390130891414042, -0.1950805366632331617, 1.952157403750237163 ) ) ;
#212011=CARTESIAN_POINT ( 'NONE',  ( 1.141953626738337890, -0.04666616626641807708, -2.015725262716171695 ) ) ;
#212014=CARTESIAN_POINT ( 'NONE',  ( 6.274684828636788225, -1.871173557121402542, -0.6205748305461754599 ) ) ;
#212016=CARTESIAN_POINT ( 'NONE',  ( 2.004154220962415689, -0.8570942286123193199, 1.821751609655430260 ) ) ;
#212018=CARTESIAN_POINT ( 'NONE',  ( 2.109133483290903222, 0.003435389629122351501, 2.117403154539731602 ) ) ;
#212021=CARTESIAN_POINT ( 'NONE',  ( 3.508316276398337319, 2.070544812355082254, 0.002818362966339192730 ) ) ;
#212023=CARTESIAN_POINT ( 'NONE',  ( 6.386679164125504293, 1.819714881846513199, -1.029135884875460372 ) ) ;
#212025=CARTESIAN_POINT ( 'NONE',  ( 4.207882836062684540, -1.820678405428953095, 0.1343838851760314757 ) ) ;
#212028=CARTESIAN_POINT ( 'NONE',  ( -0.02244404828157393894, 7.629137130509076492, -2.789100637983292774 ) ) ;
#212033=CARTESIAN_POINT ( 'NONE',  ( 5.461546741811521777, -1.510119879425949385, -1.173092037529008369 ) ) ;
#212038=CARTESIAN_POINT ( 'NONE',  ( 0.4328342922346357646, -1.301571265828086688, -1.302605208699902928 ) ) ;
#212041=CARTESIAN_POINT ( 'NONE',  ( 4.200366636497298245, -0.5845007089231197828, -1.776970133648393624 ) ) ;
#212052=CARTESIAN_POINT ( 'NONE',  ( 1.094512790084944287, 1.939365640515663181, 0.3419967617025142514 ) ) ;
#212053=CARTESIAN_POINT ( 'NONE',  ( 2.056267757160272325, -1.238304521155994209, 1.591332585091954854 ) ) ;
#212056=CARTESIAN_POINT ( 'NONE',  ( 2.150558370509841666, -1.692889690492072718, 1.391600924549152296 ) ) ;
#212059=CARTESIAN_POINT ( 'NONE',  ( 6.825078400183588023, 6.037369320589220045, 2.550557596425677254 ) ) ;
#212067=CARTESIAN_POINT ( 'NONE',  ( 4.933073973922719624, -1.305863698873997780, -1.298312775753200699 ) ) ;
#212068=CARTESIAN_POINT ( 'NONE',  ( 1.365886254406587064, 0.5821385057369383720, -1.927099543440218499 ) ) ;
#212069=CARTESIAN_POINT ( 'NONE',  ( 3.216491754421717530, -1.877423419238280822, -1.325616196499669108 ) ) ;
#212070=CARTESIAN_POINT ( 'NONE',  ( 2.447915292705178825, -0.8007319036262178225, 1.680036726287994719 ) ) ;
#212073=CARTESIAN_POINT ( 'NONE',  ( 6.029550621839829816, -0.2273517531893587407, 1.898748578088353733 ) ) ;
#212076=CARTESIAN_POINT ( 'NONE',  ( 5.196857871947656804, 1.709930586799845553, 1.202785367055765775 ) ) ;
#212077=CARTESIAN_POINT ( 'NONE',  ( 3.713615009860570915, -1.843089489661839053, 0.3189824552965599969 ) ) ;
#212079=CARTESIAN_POINT ( 'NONE',  ( 6.321814700078944860, 1.054209175812788502, -1.509406368332133930 ) ) ;
#212083=CARTESIAN_POINT ( 'NONE',  ( 5.145002536317147879, -1.476695180717332967, 0.8911356905443221788 ) ) ;
#212085=CARTESIAN_POINT ( 'NONE',  ( 0.5978079470381278959, -0.2563149341858957930, 1.714925299717950491 ) ) ;
#212089=CARTESIAN_POINT ( 'NONE',  ( 4.610331778354775700, 2.170709972759849116, -0.04705437256473897489 ) ) ;
#212090=CARTESIAN_POINT ( 'NONE',  ( 3.879382553896340013, 1.718498013671100777, -0.6167319420108534622 ) ) ;
#212091=CARTESIAN_POINT ( 'NONE',  ( 1.410910527293834260, -1.549868713165471590, 1.202602906592651788 ) ) ;
#212092=CARTESIAN_POINT ( 'NONE',  ( 0.4041146219485808877, -1.136702437883057470, -1.786057295064005013 ) ) ;
#212093=CARTESIAN_POINT ( 'NONE',  ( 6.497627784488766878, -2.291974509058695375, 0.05125074467529803363 ) ) ;
#212097=CARTESIAN_POINT ( 'NONE',  ( 2.473420802178166067, -1.846219560914775570, -1.042883725575906029 ) ) ;
#212101=CARTESIAN_POINT ( 'NONE',  ( 0.3388458784313007066, -2.007247006727829852, -0.5063607812752639603 ) ) ;
#212102=CARTESIAN_POINT ( 'NONE',  ( 6.983263157960383438, 0.5812290088160886325, 2.006563525967783868 ) ) ;
#212104=CARTESIAN_POINT ( 'NONE',  ( 2.034109888970101920, -2.153751770765993001, 0.5431444268512666262 ) ) ;
#212106=CARTESIAN_POINT ( 'NONE',  ( 0.4405775615070831042, -1.946229768708742647, -1.222969628347547966 ) ) ;
#212108=CARTESIAN_POINT ( 'NONE',  ( 5.700070374860989553, 0.8410407859656986451, -1.883500665774339833 ) ) ;
#212113=CARTESIAN_POINT ( 'NONE',  ( 0.2329586101569346424, 2.887341434808698981, -2.334705299551639079 ) ) ;
#212114=CARTESIAN_POINT ( 'NONE',  ( 5.302248432823610358, 1.390444127666954355, -1.207098008268410183 ) ) ;
#212116=CARTESIAN_POINT ( 'NONE',  ( 1.746655555778130253, -1.459509165399446529, 0.9187280511932097715 ) ) ;
#212117=CARTESIAN_POINT ( 'NONE',  ( 0.9543149826918421175, -1.275552737861269437, 1.561884623745241951 ) ) ;
#212118=CARTESIAN_POINT ( 'NONE',  ( 1.934640009471942035, -1.849324232932574530, -1.365145410983016117 ) ) ;
#212120=CARTESIAN_POINT ( 'NONE',  ( 1.985968398796404299, 1.559226912063184534, 1.639530705753606821 ) ) ;
#212121=CARTESIAN_POINT ( 'NONE',  ( 4.354198888085320185, 2.105621147513780045, -0.05115374888297812700 ) ) ;
#212123=CARTESIAN_POINT ( 'NONE',  ( 2.354462415756667593, -1.371198970962312691, 1.118854571612490245 ) ) ;
#212126=CARTESIAN_POINT ( 'NONE',  ( 5.776963781812925802, 2.119385065811297597, -0.8740618393795733798 ) ) ;
#212131=CARTESIAN_POINT ( 'NONE',  ( 6.258078541936050065, 0.8512804341574469191, -2.052012918514530160 ) ) ;
#212132=CARTESIAN_POINT ( 'NONE',  ( 4.628971764384363752, -2.004251508290517680, 0.8866568735110615940 ) ) ;
#212140=CARTESIAN_POINT ( 'NONE',  ( 5.748313822965784858, 1.043546352714582071, -1.845953426139717246 ) ) ;
#212146=CARTESIAN_POINT ( 'NONE',  ( 5.688959394570705541, 1.398425918548395153, 1.197878823674280779 ) ) ;
#212150=CARTESIAN_POINT ( 'NONE',  ( 2.735604107484723269, 1.727544688213778601, 0.2106955661135938018 ) ) ;
#212156=CARTESIAN_POINT ( 'NONE',  ( 6.579002408576895000, -0.1006694238701970334, -2.159482418181729813 ) ) ;
#212160=CARTESIAN_POINT ( 'NONE',  ( 5.471600609837615536, 2.084441204114939161, -0.5725544205837928002 ) ) ;
#212164=CARTESIAN_POINT ( 'NONE',  ( 5.817641553194794035, -1.923906765362886961, 0.4292884390787749527 ) ) ;
#212166=CARTESIAN_POINT ( 'NONE',  ( 4.745267847829638619, -1.681796892959321665, -0.4208994435666196798 ) ) ;
#212168=CARTESIAN_POINT ( 'NONE',  ( 2.138457411672203712, 0.4836887423533155483, 2.137355272389021899 ) ) ;
#212169=CARTESIAN_POINT ( 'NONE',  ( 3.610674682972123684, -0.9327887667434494601, -2.110822472020437601 ) ) ;
#212170=CARTESIAN_POINT ( 'NONE',  ( 5.501267734246070518, 1.682208477397129975, 1.190076826167464352 ) ) ;
#212171=CARTESIAN_POINT ( 'NONE',  ( 1.447104159573095572, 0.5638456037007446575, -1.858296221435972617 ) ) ;
#212175=CARTESIAN_POINT ( 'NONE',  ( 3.762070191281779774, 0.7111978290502696254, -1.997938288694045550 ) ) ;
#212176=CARTESIAN_POINT ( 'NONE',  ( 2.110000207431836472, 0.002812218110825881467, 2.016597019944998959 ) ) ;
#212178=CARTESIAN_POINT ( 'NONE',  ( 4.964015014492747291, 2.183396446337606989, -0.3195234977587738667 ) ) ;
#212184=CARTESIAN_POINT ( 'NONE',  ( 6.825078400183544503, 6.034152930826206962, 2.739236550662868197 ) ) ;
#212187=CARTESIAN_POINT ( 'NONE',  ( 3.959881651031765593, 2.045548025627259126, -0.2503382637644557263 ) ) ;
#212192=CARTESIAN_POINT ( 'NONE',  ( 3.387372106552827944, 0.04729818973902254198, -2.019286085025721267 ) ) ;
#212196=CARTESIAN_POINT ( 'NONE',  ( 3.344654342685839499, 0.4992920947068257842, 1.999368073990233308 ) ) ;
#212197=CARTESIAN_POINT ( 'NONE',  ( 3.024064729735044921, -1.777011313454954999, 0.9530116517338580451 ) ) ;
#212202=CARTESIAN_POINT ( 'NONE',  ( 1.376629057770164311, 1.701771572936720212, -0.7031625657484343872 ) ) ;
#212204=CARTESIAN_POINT ( 'NONE',  ( 6.674453038267287752, -1.361800985140369402, 1.737325302230605883 ) ) ;
#212206=CARTESIAN_POINT ( 'NONE',  ( 2.811983876933337179, -2.138515761559431461, 0.3140893029918228607 ) ) ;
#212208=CARTESIAN_POINT ( 'NONE',  ( 4.118443911689470660, 2.077242944681048975, 0.4093182092978660536 ) ) ;
#212211=CARTESIAN_POINT ( 'NONE',  ( 0.9361565222895779081, 1.842281575443193375, 0.3236747858033904302 ) ) ;
#212212=CARTESIAN_POINT ( 'NONE',  ( 4.364113771024707766, 0.9285358673545366370, 1.739096546318192882 ) ) ;
#212213=CARTESIAN_POINT ( 'NONE',  ( 4.944546133779973651, -1.457238331152037825, 1.394083050251286870 ) ) ;
#212218=CARTESIAN_POINT ( 'NONE',  ( 6.721333371289576419, -0.1616129481825591130, 2.070667135302119544 ) ) ;
#212220=CARTESIAN_POINT ( 'NONE',  ( 6.566853775770633561, 1.536883091774071453, -1.387433097640700774 ) ) ;
#212225=CARTESIAN_POINT ( 'NONE',  ( 4.979350729014382360, 1.839849877434216241, -0.7087157093622028503 ) ) ;
#212226=CARTESIAN_POINT ( 'NONE',  ( -0.2104748580754166598, -0.006608320950483163522, -2.103482951484026753 ) ) ;
#212229=CARTESIAN_POINT ( 'NONE',  ( 5.092513741553108986, -2.289745732339975692, -0.2867506301261530388 ) ) ;
#212230=CARTESIAN_POINT ( 'NONE',  ( 2.413000123442359701, -1.597275988187638607, 1.305004441579124208 ) ) ;
#212238=CARTESIAN_POINT ( 'NONE',  ( 4.070888617658403597, 1.538033944094893579, -1.532718761138168517 ) ) ;
#212241=CARTESIAN_POINT ( 'NONE',  ( 2.999365392321148516, -1.839032331094083927, 0.09308366406014097205 ) ) ;
#212243=CARTESIAN_POINT ( 'NONE',  ( 5.724229345562060089, 2.111793275502030554, 0.5857118945327836057 ) ) ;
#212245=CARTESIAN_POINT ( 'NONE',  ( 6.157125652023562878, -1.936745554134344349, -1.169425401991762259 ) ) ;
#212250=CARTESIAN_POINT ( 'NONE',  ( 6.098865926757823352, 1.445600302716108843, -1.020594415802724919 ) ) ;
#212251=CARTESIAN_POINT ( 'NONE',  ( 4.652993947568984545, 0.3464272572618365964, 1.982917695270119518 ) ) ;
#212253=CARTESIAN_POINT ( 'NONE',  ( 3.504997884693922483, 1.661208405451128245, -1.294291292614203170 ) ) ;
#212254=CARTESIAN_POINT ( 'NONE',  ( 2.372541684819210683, -0.3298082299327957378, -1.886833909188085912 ) ) ;
#212256=CARTESIAN_POINT ( 'NONE',  ( 2.857809274136946520, -0.6206004443085939570, 1.869272957157315007 ) ) ;
#212257=CARTESIAN_POINT ( 'NONE',  ( 1.182252951876180180, -1.824241171369020531, -0.4133900166373091767 ) ) ;
#212258=CARTESIAN_POINT ( 'NONE',  ( 1.767943819387544968, -1.947426213878332035, 0.2369139692007388165 ) ) ;
#212259=CARTESIAN_POINT ( 'NONE',  ( 4.142953665201137170, -1.499297852604332348, 0.8526725997853346062 ) ) ;
#212260=CARTESIAN_POINT ( 'NONE',  ( 0.8086807686161383568, -0.4671638426185490967, -1.854305266343849734 ) ) ;
#212262=CARTESIAN_POINT ( 'NONE',  ( 1.752831059180045115, 0.6944836804415283060, 2.094827981560241970 ) ) ;
#212268=CARTESIAN_POINT ( 'NONE',  ( 6.368043163206878354, -2.055323469740528264, 0.2474699835256082281 ) ) ;
#212269=CARTESIAN_POINT ( 'NONE',  ( 0.8716356842100521085, -0.3054578492302991721, 2.047597563663336118 ) ) ;
#212274=CARTESIAN_POINT ( 'NONE',  ( 5.567072742743464531, -1.671543079161823542, 1.304629437388994395 ) ) ;
#212279=CARTESIAN_POINT ( 'NONE',  ( 6.602011099637477010, 0.7519813002578833450, -1.812223124677159181 ) ) ;
#212281=CARTESIAN_POINT ( 'NONE',  ( 3.989611116449209405, 1.913510565032714883, 0.6351021849077125303 ) ) ;
#212282=CARTESIAN_POINT ( 'NONE',  ( 3.485460621946351534, -0.5511008185722067187, 1.834767741543178676 ) ) ;
#212284=CARTESIAN_POINT ( 'NONE',  ( 1.171705676731093604, 1.309414992938146893, 1.757219779060022580 ) ) ;
#212287=CARTESIAN_POINT ( 'NONE',  ( 5.677995041854309477, 1.982684118255732875, -0.3484467016405675688 ) ) ;
#212291=CARTESIAN_POINT ( 'NONE',  ( 5.993796379919574591, -2.101200072677239739, 0.2596931833054038630 ) ) ;
#212294=CARTESIAN_POINT ( 'NONE',  ( 1.909825778081200909, -0.9882315549833411428, -1.842464674945838654 ) ) ;
#212296=CARTESIAN_POINT ( 'NONE',  ( 0.8501349688851227437, 0.4944664728778884744, 1.652377535151504206 ) ) ;
#212300=FILL_AREA_STYLE_COLOUR ( '', #164480 ) ;
#212306=CARTESIAN_POINT ( 'NONE',  ( 1.892921280605066370, -0.08938092231483388272, -1.809401395368259280 ) ) ;
#212310=CARTESIAN_POINT ( 'NONE',  ( 6.539320575229251808, 2.472926584938171413, 2.181659282373017650 ) ) ;
#212314=CARTESIAN_POINT ( 'NONE',  ( 3.332308176975990577, -1.110599006344037853, 1.493168399320473627 ) ) ;
#212315=CARTESIAN_POINT ( 'NONE',  ( 0.01699859406821546334, -1.751214827781864436, 0.7768474416505846136 ) ) ;
#212316=CARTESIAN_POINT ( 'NONE',  ( 6.668979838189343035, -1.761623494860217631, -0.7799453142821392015 ) ) ;
#212323=CARTESIAN_POINT ( 'NONE',  ( 4.838697515689712958, -1.909247481386136647, -0.4825833779809485802 ) ) ;
#212327=CARTESIAN_POINT ( 'NONE',  ( 6.527279143455773536, -1.428284688129980440, -1.662137905815167294 ) ) ;
#212329=CARTESIAN_POINT ( 'NONE',  ( 5.333004766823168374, 0.1418691241366967226, 1.921211455432366044 ) ) ;
#212332=CARTESIAN_POINT ( 'NONE',  ( 0.5514207423844892375, 0.5776932562693118944, -1.731835939664846613 ) ) ;
#212333=CARTESIAN_POINT ( 'NONE',  ( 1.893488989520499377, 1.919108310403025763, -1.089527612406354873 ) ) ;
#212335=CARTESIAN_POINT ( 'NONE',  ( 0.3340484552533556362, -1.024938778295768849, -1.614363347046356756 ) ) ;
#212337=ORIENTED_EDGE ( 'NONE', *, *, #178838, .F. ) ;
#212338=CARTESIAN_POINT ( 'NONE',  ( 0.9066264771708797410, 0.5685364763899096729, 1.885722953041415906 ) ) ;
#212339=CARTESIAN_POINT ( 'NONE',  ( 1.575622484978753679, -1.037422314974449478, 1.641571771860099727 ) ) ;
#212340=CARTESIAN_POINT ( 'NONE',  ( 0.5267199648841465187, 1.994564833640038781, -0.2930222482238133419 ) ) ;
#212342=CARTESIAN_POINT ( 'NONE',  ( 5.717585430250381684, 0.3647202891138579539, -1.824662122815931875 ) ) ;
#212348=CARTESIAN_POINT ( 'NONE',  ( 1.206853476500208133, 1.935082376036290075, 1.028754739392373496 ) ) ;
#212353=CARTESIAN_POINT ( 'NONE',  ( 1.558932953716257730, -1.564965500463588732, -0.9399777662534372080 ) ) ;
#212356=CARTESIAN_POINT ( 'NONE',  ( 6.509000000000021657, 1.267728212239338959, 2.115804336118334295 ) ) ;
#212358=CARTESIAN_POINT ( 'NONE',  ( 0.2758378062712996681, 1.107980625233648597, 1.575821400459100463 ) ) ;
#212359=CARTESIAN_POINT ( 'NONE',  ( 4.258614474744500278, -0.6113484564182982695, -1.864166799412938724 ) ) ;
#212362=CARTESIAN_POINT ( 'NONE',  ( 4.036819321710017228, -1.906298169312226953, 1.081085072550565407 ) ) ;
#212364=CARTESIAN_POINT ( 'NONE',  ( 6.609000000000012420, 2.052634316153336691, 2.306727925381938604 ) ) ;
#212365=CARTESIAN_POINT ( 'NONE',  ( 3.713788242813487184, 0.5077267127921447631, -2.006887321594638784 ) ) ;
#212370=CARTESIAN_POINT ( 'NONE',  ( 4.131641605347593504, 0.6128431504758731219, 2.215418681923121191 ) ) ;
#212374=CARTESIAN_POINT ( 'NONE',  ( 6.720655732516653380, 6.038084619979597001, 2.521169617733058477 ) ) ;
#212377=CARTESIAN_POINT ( 'NONE',  ( 4.206929537583108392, -0.3307808895044571651, 1.913420690662092305 ) ) ;
#212380=CARTESIAN_POINT ( 'NONE',  ( 4.711142613322857109, 1.586760866459841379, -1.067142987418716604 ) ) ;
#212382=CARTESIAN_POINT ( 'NONE',  ( 5.702095886272589453, -1.724958192454665085, 0.004281591079305368218 ) ) ;
#212383=CARTESIAN_POINT ( 'NONE',  ( 4.821500071095637274, -1.429446227384461032, -1.422610148874188463 ) ) ;
#212384=CARTESIAN_POINT ( 'NONE',  ( 4.799617249347348569, 1.585997580420713593, -1.664126067976256840 ) ) ;
#212386=CARTESIAN_POINT ( 'NONE',  ( 1.207977004800918852, -0.5332226995428279714, 2.141375170867452660 ) ) ;
#212389=CARTESIAN_POINT ( 'NONE',  ( 6.239478240350173621, -1.283343308616216705, -1.218829697195593642 ) ) ;
#212391=CARTESIAN_POINT ( 'NONE',  ( 2.467065147740226116, 0.1108469335737295169, -2.289696780367215467 ) ) ;
#212392=CARTESIAN_POINT ( 'NONE',  ( 1.358879374581365429, 1.715036991836488056, -0.2946001921160408821 ) ) ;
#212394=CARTESIAN_POINT ( 'NONE',  ( 0.9304778391672563487, 0.8475688526466665929, 1.512457944649912012 ) ) ;
#212398=CARTESIAN_POINT ( 'NONE',  ( 0.9772844579341716242, 2.006041157791297991, 0.8309993691856133458 ) ) ;
#212399=CARTESIAN_POINT ( 'NONE',  ( 2.694546298722868549, 1.457235452327232395, -1.394086077981852911 ) ) ;
#212401=CARTESIAN_POINT ( 'NONE',  ( 6.533821582689818719, -1.260454884444404122, -1.457021811732343686 ) ) ;
#212403=CARTESIAN_POINT ( 'NONE',  ( 2.619623270456972630, 1.879045213996872965, 1.184562869268386054 ) ) ;
#212410=CARTESIAN_POINT ( 'NONE',  ( 5.636210787324313465, 0.3477544615747550361, 1.705165986005853229 ) ) ;
#212411=CARTESIAN_POINT ( 'NONE',  ( 3.226955236329264398, -1.811681696138227160, -0.7532884077038405346 ) ) ;
#212415=CARTESIAN_POINT ( 'NONE',  ( 6.777182134110200096, 7.629137130509069387, 2.789055895399249696 ) ) ;
#212416=CARTESIAN_POINT ( 'NONE',  ( 4.112777665030871610, 1.603588310063062794, -1.596181346845012117 ) ) ;
#212417=CARTESIAN_POINT ( 'NONE',  ( 0.5376419320063254847, 1.925266156408891316, -0.7407299734314594097 ) ) ;
#212420=CARTESIAN_POINT ( 'NONE',  ( 2.079355054740182229, -0.1115493103639639688, -2.259872350005930119 ) ) ;
#212423=CARTESIAN_POINT ( 'NONE',  ( 3.075316773429651818, 1.777364689479765003, -0.5833007003755164011 ) ) ;
#212424=CARTESIAN_POINT ( 'NONE',  ( 1.951430075251599838, -1.585913025431864742, -0.7019457847057923860 ) ) ;
#212425=CARTESIAN_POINT ( 'NONE',  ( 5.917560222199001352, -1.216239291071326001, -1.822900893127032962 ) ) ;
#212426=CARTESIAN_POINT ( 'NONE',  ( 0.08333923026508995024, -0.1592477204843331384, -2.171661519566956855 ) ) ;
#212427=CARTESIAN_POINT ( 'NONE',  ( 4.364260218091946975, 1.016419123106377276, 1.907829002176253175 ) ) ;
#212428=CARTESIAN_POINT ( 'NONE',  ( 4.312401332534675724, 1.776009277829879718, 0.7858599780834804038 ) ) ;
#212432=CARTESIAN_POINT ( 'NONE',  ( 2.000000000000001332, -1.212302805901314492E-13, -2.052068128417949389 ) ) ;
#212437=CARTESIAN_POINT ( 'NONE',  ( 5.555314621531947772, -1.277044735018734833, 1.560499014526220307 ) ) ;
#212441=CARTESIAN_POINT ( 'NONE',  ( 3.791466046568803705, 1.323482414808102137, 1.257835202898072380 ) ) ;
#212448=CARTESIAN_POINT ( 'NONE',  ( 0.1760434994887878080, 1.997199259934297366, -0.3004917578056826022 ) ) ;
#212449=CARTESIAN_POINT ( 'NONE',  ( 0.6277789859737945566, -0.3070864893036719945, 2.098006834332386994 ) ) ;
#212453=CARTESIAN_POINT ( 'NONE',  ( 6.825078400183568483, -0.002763825414428457399, 2.044262525762724270 ) ) ;
#212454=CARTESIAN_POINT ( 'NONE',  ( 5.854138739207011888, 0.1455364397412381439, -2.011204036175239018 ) ) ;
#212460=CARTESIAN_POINT ( 'NONE',  ( 0.07680821025391781909, 4.096870002413341538, -2.365840309731046975 ) ) ;
#212464=CARTESIAN_POINT ( 'NONE',  ( 5.817732461567613811, -1.591073081590412830, 1.238133459405404757 ) ) ;
#212465=CARTESIAN_POINT ( 'NONE',  ( 4.452959842461719830, 0.4008590389125502029, -1.796806262838637647 ) ) ;
#212466=CARTESIAN_POINT ( 'NONE',  ( 0.07700591528351626025, 0.2537022344677486996, -1.946355950789683043 ) ) ;
#212467=CARTESIAN_POINT ( 'NONE',  ( 3.264621958926614109, 1.037573782609865436, 2.061359394274730583 ) ) ;
#212469=CARTESIAN_POINT ( 'NONE',  ( 6.186834690482100108, -0.3103498281695793448, -2.139073744226393181 ) ) ;
#212471=CARTESIAN_POINT ( 'NONE',  ( 1.417416744832197484, -1.080314125112752155, -1.613661906057413331 ) ) ;
#212474=CARTESIAN_POINT ( 'NONE',  ( 4.780793123113402210, -2.255322609370190357, 0.4421783396322577775 ) ) ;
#212478=CARTESIAN_POINT ( 'NONE',  ( 4.381629165553334815, 1.221847395770376377, 1.416585496670008659 ) ) ;
#212480=CARTESIAN_POINT ( 'NONE',  ( 1.353610510645312237, -1.387278792934818705, -1.316581319992945920 ) ) ;
#212484=CARTESIAN_POINT ( 'NONE',  ( 3.176612885197922953, -1.314426786483071208, 1.772596291930063739 ) ) ;
#212490=CARTESIAN_POINT ( 'NONE',  ( 1.194530107633525517, -0.4747795734156860514, -1.913232634659914444 ) ) ;
#212492=CARTESIAN_POINT ( 'NONE',  ( 1.026927485578407406, 1.372003256358475864, -1.855264817478113226 ) ) ;
#212493=CARTESIAN_POINT ( 'NONE',  ( 0.9417639971489067952, 1.314929008279978495, 1.456166070238865018 ) ) ;
#212494=CARTESIAN_POINT ( 'NONE',  ( 5.647355161340581020, 1.821535332892617820, -0.9675206831420575249 ) ) ;
#212501=CARTESIAN_POINT ( 'NONE',  ( 0.3741910912563637948, -2.129432730031981080, 0.4223156635175562279 ) ) ;
#212507=CARTESIAN_POINT ( 'NONE',  ( 2.934663490303309974, 0.2251962677765201870, 1.856852477824536329 ) ) ;
#212508=CARTESIAN_POINT ( 'NONE',  ( 6.221977808853903724, -1.195094089922192016, -1.800988070004491792 ) ) ;
#212510=CARTESIAN_POINT ( 'NONE',  ( 0.07735805125225460321, 2.008365972388022946, -2.502973720202539276 ) ) ;
#212512=CARTESIAN_POINT ( 'NONE',  ( 2.367698891403247519, 0.5082884949165042965, -1.843433491391050838 ) ) ;
#212513=CARTESIAN_POINT ( 'NONE',  ( 3.836565602288672938, 0.2594712388852594143, 1.750573784680304890 ) ) ;
#212514=CARTESIAN_POINT ( 'NONE',  ( 0.8559432719405724033, 0.7744784914341161786, -1.748599447100062321 ) ) ;
#212517=CARTESIAN_POINT ( 'NONE',  ( 5.905858165902563073, -1.068448527453051966, -1.589740232873719128 ) ) ;
#212518=CARTESIAN_POINT ( 'NONE',  ( 6.531706384513794816, 1.885137803977337656, -0.5704747015483744299 ) ) ;
#212520=CARTESIAN_POINT ( 'NONE',  ( 2.619513681940002670, 1.793805257907291395, 1.130712135851599465 ) ) ;
#212522=CARTESIAN_POINT ( 'NONE',  ( 4.908994958506140982, 1.627828031611065152, 0.9215782234750914403 ) ) ;
#212523=CARTESIAN_POINT ( 'NONE',  ( 0.4690313652776016418, 0.1822212253758948297, -1.816563760317004395 ) ) ;
#212525=CARTESIAN_POINT ( 'NONE',  ( 4.090592613104036879, -2.182713160620152859, -0.3248913242878055385 ) ) ;
#212528=CARTESIAN_POINT ( 'NONE',  ( 1.961455461422195068, 1.713676499688887800, 1.147740006246004585 ) ) ;
#212538=CARTESIAN_POINT ( 'NONE',  ( 4.264170421968140445, -2.065031762457261610, 0.1491743435546449281 ) ) ;
#212541=CARTESIAN_POINT ( 'NONE',  ( 1.476082264964494906, 1.286352913914396545, 1.737049067733025032 ) ) ;
#212543=CARTESIAN_POINT ( 'NONE',  ( 1.770181643375926317, 2.014124636562672155, -0.1506882416659905133 ) ) ;
#212550=CARTESIAN_POINT ( 'NONE',  ( 0.3390778084843976137, -1.706115258973059490, -1.074657883261991076 ) ) ;
#212551=CARTESIAN_POINT ( 'NONE',  ( 5.126606437771586755, 0.1607948393855564151, 2.185736094377451089 ) ) ;
#212555=CARTESIAN_POINT ( 'NONE',  ( 4.517770118113122457, -0.5046507728132009207, 1.844564425022446885 ) ) ;
#212559=CARTESIAN_POINT ( 'NONE',  ( 2.601185598297011570, -0.1948207814224910128, 2.006963067508853005 ) ) ;
#212561=CARTESIAN_POINT ( 'NONE',  ( 0.08209332325101456607, -1.073118421065310413, 2.025687816139466246 ) ) ;
#212563=CARTESIAN_POINT ( 'NONE',  ( 4.998908393266289885, 1.432429904705156520, -0.9603719661937599739 ) ) ;
#212570=CARTESIAN_POINT ( 'NONE',  ( 5.285751626526108637, 1.744147384919532140, -0.4889748023358466145 ) ) ;
#212575=CARTESIAN_POINT ( 'NONE',  ( 5.813115421323210796, 1.476946679544950847, -1.048544953227096288 ) ) ;
#212578=CARTESIAN_POINT ( 'NONE',  ( 3.257961296797746265, 0.9855263100190698733, 1.957416934251283935 ) ) ;
#212580=CARTESIAN_POINT ( 'NONE',  ( 6.514093505496237668, 1.855963486094978965, -0.1381079127797563977 ) ) ;
#212582=CARTESIAN_POINT ( 'NONE',  ( 3.954619794068328087, -1.788705220947036878, -0.6861305607534126105 ) ) ;
#212588=CARTESIAN_POINT ( 'NONE',  ( 1.868271315571629509, 1.111147431007172726, 1.854118885846419262 ) ) ;
#212592=CARTESIAN_POINT ( 'NONE',  ( 1.834698128333624112, 0.1755570873784827179, 1.817110820650599923 ) ) ;
#212594=CARTESIAN_POINT ( 'NONE',  ( 3.645350208285046634, -1.381898811119431691, -1.193016960613018096 ) ) ;
#212597=CARTESIAN_POINT ( 'NONE',  ( 3.613681597605075346, 0.4810616251548325284, -1.909752186315590405 ) ) ;
#212599=CARTESIAN_POINT ( 'NONE',  ( 4.581548892214976298, -0.9124856661332171326, 1.714327114426909882 ) ) ;
#212603=CARTESIAN_POINT ( 'NONE',  ( 4.816704082729271086, -0.7169179515637627009, -1.995842421597990413 ) ) ;
#212609=CARTESIAN_POINT ( 'NONE',  ( 4.178388974671240597, 0.9510918172684652561, 1.774266679505158262 ) ) ;
#212611=CARTESIAN_POINT ( 'NONE',  ( 5.197797600609998625, -0.6536857159176562293, 1.704833070275885598 ) ) ;
#212612=CARTESIAN_POINT ( 'NONE',  ( 0.3091450132529197092, -1.663722454078466306, 1.232067777400827069 ) ) ;
#212616=CARTESIAN_POINT ( 'NONE',  ( 5.752782329262380756, -1.473788443143897675, 1.151991621687727507 ) ) ;
#212625=CARTESIAN_POINT ( 'NONE',  ( 1.288034235163344254, -1.310400469390052836, -1.602789277989056238 ) ) ;
#212626=CARTESIAN_POINT ( 'NONE',  ( 2.864987086846816577, -0.1587241086147250513, -2.111353475082369702 ) ) ;
#212629=CARTESIAN_POINT ( 'NONE',  ( 0.4616802850961505555, -0.5308588990461468038, 1.896450293990773472 ) ) ;
#212634=CARTESIAN_POINT ( 'NONE',  ( 2.414399183035727425, 1.495821068830467615, -1.737032439462746325 ) ) ;
#212635=CARTESIAN_POINT ( 'NONE',  ( 0.5744775230259161480, -1.718042477583326066, -0.6180270036199516648 ) ) ;
#212636=CARTESIAN_POINT ( 'NONE',  ( 2.355592738034977263, -1.419685808644566949, -1.281520755053264571 ) ) ;
#212639=CARTESIAN_POINT ( 'NONE',  ( 2.179941694947628683, 1.973542599225884153, -0.3968540688959447116 ) ) ;
#212640=CARTESIAN_POINT ( 'NONE',  ( 0.7605091544688712402, -0.6555486260201286441, -1.849146037077718852 ) ) ;
#212644=CARTESIAN_POINT ( 'NONE',  ( 3.416043810090535260, 1.326132273491455349, -1.616208110139333742 ) ) ;
#212645=CARTESIAN_POINT ( 'NONE',  ( 2.096244624822783731, -0.4688358662975153357, -1.706545078221621603 ) ) ;
#212648=CARTESIAN_POINT ( 'NONE',  ( 4.839906306838932970, 2.285852466752227752, 0.1720476854494106811 ) ) ;
#212649=CARTESIAN_POINT ( 'NONE',  ( 4.224340698251967119, 0.08847545473529906668, 1.738206131172301161 ) ) ;
#212652=CARTESIAN_POINT ( 'NONE',  ( 4.481622980438174864, 1.585354267084694957, 0.7024943803609559057 ) ) ;
#212653=CARTESIAN_POINT ( 'NONE',  ( 4.791568617006563002, -1.986896891843348723, 0.8757425373496147136 ) ) ;
#212655=CARTESIAN_POINT ( 'NONE',  ( 5.313685493615880162, -1.282986534165726944, -1.555701818360885280 ) ) ;
#212656=CARTESIAN_POINT ( 'NONE',  ( 6.750000000000005329, 1.157781160899305384, 2.098894642203967376 ) ) ;
#212658=CARTESIAN_POINT ( 'NONE',  ( 3.645458630373909159, -1.458056112162182893, -1.259071146193297075 ) ) ;
#212660=CARTESIAN_POINT ( 'NONE',  ( 5.678047454291774265, 2.188620968312010362, -0.3794988778502098592 ) ) ;
#212662=CARTESIAN_POINT ( 'NONE',  ( 6.983263157960327483, 4.697935251208478213, 2.408834092705824936 ) ) ;
#212665=CARTESIAN_POINT ( 'NONE',  ( 2.016565898353571473, -2.220703888365501921, 0.05821906423880519182 ) ) ;
#212673=CARTESIAN_POINT ( 'NONE',  ( 5.477030937198195559, 1.904485971043594628, 0.7926545740569268528 ) ) ;
#212678=CARTESIAN_POINT ( 'NONE',  ( 0.4207181242068900873, -0.09552205520973154618, 1.767312625620009126 ) ) ;
#212679=CARTESIAN_POINT ( 'NONE',  ( 5.361839092321889488, -0.05056905708066515570, -1.733610765856267388 ) ) ;
#212680=CARTESIAN_POINT ( 'NONE',  ( 5.020954538418783031, -1.650374644951870806, 0.5528329121840831473 ) ) ;
#212682=CARTESIAN_POINT ( 'NONE',  ( 3.140441720415044546, 0.5589363893779492054, 2.223061277538174174 ) ) ;
#212684=CARTESIAN_POINT ( 'NONE',  ( 1.253568445147245525, 0.7445567558202557112, 1.684058134371092752 ) ) ;
#212688=CARTESIAN_POINT ( 'NONE',  ( 1.905030480050071251, 1.515927946353814892, 1.016894063925778635 ) ) ;
#212689=CARTESIAN_POINT ( 'NONE',  ( 3.252577435111691617, 1.966644794889659043, -0.4445022851852917234 ) ) ;
#212690=CARTESIAN_POINT ( 'NONE',  ( 1.078377591563362436, -2.138745004354754897, -0.4770250503970187572 ) ) ;
#212692=CARTESIAN_POINT ( 'NONE',  ( 4.313572747864121482, -0.3622951029728087580, 2.074398424781583206 ) ) ;
#212696=CARTESIAN_POINT ( 'NONE',  ( 1.908725956546155178, 0.6474277305483535638, 1.966616875269424192 ) ) ;
#212699=CARTESIAN_POINT ( 'NONE',  ( 3.826904873358004888, 1.498484187726952799, -1.500593194838243605 ) ) ;
#212700=CARTESIAN_POINT ( 'NONE',  ( 0.2758378062712996681, 1.107980625233648597, 1.575821400459100463 ) ) ;
#212707=CARTESIAN_POINT ( 'NONE',  ( 2.724872815078176913, 1.459976238909798996, -1.395942890215768895 ) ) ;
#212708=CARTESIAN_POINT ( 'NONE',  ( 1.606614413041591360, -0.7575671727712609549, -1.965171518483445068 ) ) ;
#212711=CARTESIAN_POINT ( 'NONE',  ( 5.541811466629937399, 1.248470921604339923, 1.380218479220591155 ) ) ;
#212717=CARTESIAN_POINT ( 'NONE',  ( 6.649297902391459125, -1.653525193404258742, -1.229868563883255828 ) ) ;
#212722=CARTESIAN_POINT ( 'NONE',  ( 2.512703819571511232, 1.733401479428131609, 0.04661458952265155886 ) ) ;
#212723=CARTESIAN_POINT ( 'NONE',  ( 1.587455592251562297, -1.731706956562387711, -0.1728515053983879501 ) ) ;
#212724=CARTESIAN_POINT ( 'NONE',  ( 0.4468379896771547122, 2.301730118641607703, 0.1654463548556948105 ) ) ;
#212727=CARTESIAN_POINT ( 'NONE',  ( 2.706383518077785322, -0.7856088873096721548, -1.905365358233277240 ) ) ;
#212729=CARTESIAN_POINT ( 'NONE',  ( 1.247422469434919412, -1.966343046301596509, -0.4444367004674750210 ) ) ;
#212730=CARTESIAN_POINT ( 'NONE',  ( 6.825078400183582694, 7.052246674313852992, 2.642498189888539795 ) ) ;
#212732=CARTESIAN_POINT ( 'NONE',  ( 0.7078139640715176428, -1.962176506181498636, 0.1910761354673266577 ) ) ;
#212734=CARTESIAN_POINT ( 'NONE',  ( 4.904515063324526025, -1.898637117948184017, -0.2282459111111398431 ) ) ;
#212741=CARTESIAN_POINT ( 'NONE',  ( 0.6451828087791033894, 0.1507176824743546029, 2.014122433718650296 ) ) ;
#212744=CARTESIAN_POINT ( 'NONE',  ( 5.034332918631054810, 1.191367258472323831, -1.976142064534849307 ) ) ;
#212745=CARTESIAN_POINT ( 'NONE',  ( 5.600043156098196917, 0.7966083592686534764, -1.793046234938546757 ) ) ;
#212746=CARTESIAN_POINT ( 'NONE',  ( 1.569116724355507975, 1.727593668635756918, 0.9295332132536607839 ) ) ;
#212750=CARTESIAN_POINT ( 'NONE',  ( -0.1177638760072839408, -2.117013592363240271, -0.04492315971119444085 ) ) ;
#212753=CARTESIAN_POINT ( 'NONE',  ( 0.9371597039556851527, 0.7481776565299682602, -1.682445429299509909 ) ) ;
#212755=CARTESIAN_POINT ( 'NONE',  ( 4.768535058008659178, -0.9225228719554872114, -1.965435229472652479 ) ) ;
#212757=CARTESIAN_POINT ( 'NONE',  ( 1.723052270212792836, 1.567896913533245229, -1.427966198690698851 ) ) ;
#212761=CARTESIAN_POINT ( 'NONE',  ( 3.075518034276482293, 1.957894989606956182, -0.6432953703794060951 ) ) ;
#212763=CARTESIAN_POINT ( 'NONE',  ( -0.07694640568740516995, -1.131669979810394633, -1.452919414246391261 ) ) ;
#212767=CARTESIAN_POINT ( 'NONE',  ( 0.04788047853313340263, -1.708876078042343316, -1.396090968258607790 ) ) ;
#212768=CARTESIAN_POINT ( 'NONE',  ( 2.038691496156146865, 2.237626877524625524, 0.3332970034419027727 ) ) ;
#212770=CARTESIAN_POINT ( 'NONE',  ( 2.021461901335448896, -0.3940331753463456321, 1.768040416340182608 ) ) ;
#212771=CARTESIAN_POINT ( 'NONE',  ( 1.499098398830187362, -0.2305585200724231121, 1.901688874922660588 ) ) ;
#212772=CARTESIAN_POINT ( 'NONE',  ( 2.805202726412972858, -1.722705984639979704, 1.148039668612794051 ) ) ;
#212774=CARTESIAN_POINT ( 'NONE',  ( 2.026188796938654946, 1.136581424768828397, -1.610674104117129302 ) ) ;
#212775=CARTESIAN_POINT ( 'NONE',  ( 5.303319688262892129, 1.576177044413902717, 1.107479782286522996 ) ) ;
#212776=CARTESIAN_POINT ( 'NONE',  ( 3.115926070338378207, -0.9207206926411042325, -1.628290677324291780 ) ) ;
#212777=CARTESIAN_POINT ( 'NONE',  ( 1.085104692462773412, -2.252536170888468359, -0.5009029511823160918 ) ) ;
#212779=CARTESIAN_POINT ( 'NONE',  ( 2.734617598447198539, -1.779929554887052401, -0.5434082684390993956 ) ) ;
#212781=CARTESIAN_POINT ( 'NONE',  ( 5.477030937198195559, 1.904485971043594628, 0.7926545740569268528 ) ) ;
#212784=CARTESIAN_POINT ( 'NONE',  ( 6.088920695360399371, -0.3053041885118645271, -2.083579958893892137 ) ) ;
#212786=CARTESIAN_POINT ( 'NONE',  ( 6.169229141836319208, 0.1658205177522271423, -2.155315574850395155 ) ) ;
#212787=CARTESIAN_POINT ( 'NONE',  ( 0.3976880421775743635, -0.6195963491163231085, -1.733980255833282191 ) ) ;
#212788=CARTESIAN_POINT ( 'NONE',  ( 5.883464967995201356, 0.1463045851861736191, -2.014419601194089804 ) ) ;
#212789=DIRECTION ( 'NONE',  ( -3.451266460341926649E-31, -5.200010849845536803E-32, 1.000000000000000000 ) ) ;
#212795=CARTESIAN_POINT ( 'NONE',  ( 3.344935638061694139, -1.780668040901035143, -0.9463001528628791625 ) ) ;
#212800=CARTESIAN_POINT ( 'NONE',  ( 5.946190753372003535, 2.158995856162956084, 0.1107517376499680406 ) ) ;
#212806=CARTESIAN_POINT ( 'NONE',  ( 5.079703922733037835, -0.7231256174668048153, 1.882480835741196845 ) ) ;
#212808=CARTESIAN_POINT ( 'NONE',  ( 1.611479353654057034, -1.712177798104688620, 0.2083697849032482008 ) ) ;
#212813=CARTESIAN_POINT ( 'NONE',  ( 6.907498162232361238, -0.4094499450241483318, 1.831839262316947270 ) ) ;
#212814=CARTESIAN_POINT ( 'NONE',  ( 0.4518146667342719525, -1.425121331298753402, -1.422066715514385349 ) ) ;
#212817=CARTESIAN_POINT ( 'NONE',  ( 3.417197246517459597, 1.994164043739574232, 0.9453733912969732867 ) ) ;
#212818=CARTESIAN_POINT ( 'NONE',  ( 5.137628997053973912, 2.028260002996465250, -0.7749071676581267276 ) ) ;
#212822=CARTESIAN_POINT ( 'NONE',  ( 2.912858673564645784, -0.6176872867308530468, -2.028511212565413224 ) ) ;
#212823=CARTESIAN_POINT ( 'NONE',  ( 1.405875298092047698, -1.122519365368032984, -1.674874950958963549 ) ) ;
#212824=CARTESIAN_POINT ( 'NONE',  ( 1.845701740803426194, -1.185437281251604746, -1.369922693571566485 ) ) ;
#212830=CARTESIAN_POINT ( 'NONE',  ( 0.9365811914238668656, -1.507994439141499221, 1.181323522483549437 ) ) ;
#212838=CARTESIAN_POINT ( 'NONE',  ( 4.733611406029458735, 0.6279933214467496860, -1.916352419866963697 ) ) ;
#212839=CARTESIAN_POINT ( 'NONE',  ( 5.805597153138060129, -0.5296426447994294628, 2.095691122003799478 ) ) ;
#212842=CARTESIAN_POINT ( 'NONE',  ( 1.424255164902767934, -2.103954720533041556, 0.2648648325892372646 ) ) ;
#212844=CARTESIAN_POINT ( 'NONE',  ( 3.110573765929941725, 1.430363465515383625, -1.356829130874689815 ) ) ;
#212847=CARTESIAN_POINT ( 'NONE',  ( 6.812958078942359386, -1.523254609455872322, 1.248309864861799401 ) ) ;
#212848=CARTESIAN_POINT ( 'NONE',  ( 1.288897009404812666, 1.470358960358808309, 1.268651691623223110 ) ) ;
#212850=CARTESIAN_POINT ( 'NONE',  ( 6.875078400183573635, 7.629137130509068498, 2.744348168701661095 ) ) ;
#212853=CARTESIAN_POINT ( 'NONE',  ( 2.923863239626739663, 1.160869195616637706, -1.738502609096896467 ) ) ;
#212856=CARTESIAN_POINT ( 'NONE',  ( 6.621744163077868173, -0.4141588628726756149, 1.873750786029332316 ) ) ;
#212858=CARTESIAN_POINT ( 'NONE',  ( 4.371826309796801979, 2.140994599346605742, -0.5347268394074317088 ) ) ;
#212860=CARTESIAN_POINT ( 'NONE',  ( 3.276612781706738087, -1.315965827422488132, 1.771305981150771647 ) ) ;
#212862=CARTESIAN_POINT ( 'NONE',  ( 1.523922206041250949, -1.897707704667614959, 0.2351830868887184178 ) ) ;
#212865=CARTESIAN_POINT ( 'NONE',  ( 4.035645461687249913, 1.950487776689105335, -0.6946759356915441774 ) ) ;
#212868=CARTESIAN_POINT ( 'NONE',  ( 1.340939272977889951, 0.4221563536682856332, 2.119910705745978508 ) ) ;
#212869=CARTESIAN_POINT ( 'NONE',  ( 3.386445149735781257, -0.4294187885149694517, -2.148908265708626697 ) ) ;
#212871=EDGE_CURVE ( 'NONE', #180616, #97371, #68685, .T. ) ;
#212879=CARTESIAN_POINT ( 'NONE',  ( 0.6510177983308338412, 0.9963039324867200008, 1.753029211773032392 ) ) ;
#212882=CARTESIAN_POINT ( 'NONE',  ( 4.909070852169226562, -1.665950775781706028, 1.228889460859562854 ) ) ;
#212883=CARTESIAN_POINT ( 'NONE',  ( 3.703666587441448943, -0.5581696590808477021, 1.843871709287647764 ) ) ;
#212884=CARTESIAN_POINT ( 'NONE',  ( 5.747700551816460113, 2.085811977426319519, -0.3625847027708250514 ) ) ;
#212887=CARTESIAN_POINT ( 'NONE',  ( 3.889471302351163562, -1.821405649934451532, 0.7496272025103620784 ) ) ;
#212888=CARTESIAN_POINT ( 'NONE',  ( 5.648434673080700463, -1.810194131346474222, 1.406188067625735449 ) ) ;
#212889=CARTESIAN_POINT ( 'NONE',  ( 4.002439121739418404, -0.5745171773131328985, -1.733004836422600725 ) ) ;
#212896=CARTESIAN_POINT ( 'NONE',  ( 5.677995041854309477, 1.982684118255732875, -0.3484467016405675688 ) ) ;
#212897=CARTESIAN_POINT ( 'NONE',  ( 5.959697520924294167, -2.181652697926935502, -0.7244182876006750593 ) ) ;
#212898=CARTESIAN_POINT ( 'NONE',  ( 4.645332984504850771, 1.754159843842403976, -0.8783796436172899291 ) ) ;
#212903=CARTESIAN_POINT ( 'NONE',  ( 0.8200051061889235271, 1.242435332701301132, -1.681397122352365603 ) ) ;
#212904=CARTESIAN_POINT ( 'NONE',  ( 0.08069323953814251660, -0.1329233695197447052, -1.840450602299897431 ) ) ;
#212906=CARTESIAN_POINT ( 'NONE',  ( 6.580031058444741454, -1.904989947508778814, -0.3762313139713204801 ) ) ;
#212907=CARTESIAN_POINT ( 'NONE',  ( -0.2102771530458094895, 1.993718876163485421, -2.617492801249762913 ) ) ;
#212908=CARTESIAN_POINT ( 'NONE',  ( 0.6963323360776455528, 1.421588922443246084, 1.003805163531448441 ) ) ;
#212911=CARTESIAN_POINT ( 'NONE',  ( 1.699380632523245449, -0.5835770076011400631, 1.623301926564212794 ) ) ;
#212912=CARTESIAN_POINT ( 'NONE',  ( 1.452940684028160234, -1.882004992133184285, -1.122693704575933316 ) ) ;
#212913=CARTESIAN_POINT ( 'NONE',  ( 4.565167970240332274, -1.970479184476851886, -0.9938812724585781577 ) ) ;
#212914=CARTESIAN_POINT ( 'NONE',  ( 1.499139249613313574, 0.4210003976099167544, 2.129699363925404487 ) ) ;
#212915=CARTESIAN_POINT ( 'NONE',  ( 0.3283667639546791195, 1.746078182827022429, 0.5332771064449209897 ) ) ;
#212916=CARTESIAN_POINT ( 'NONE',  ( 2.677094534585529928, 1.813448998079300489, -1.092781719356890946 ) ) ;
#212919=CARTESIAN_POINT ( 'NONE',  ( 2.982263410219893274, -2.258884913406122408, -0.3895283529634691599 ) ) ;
#212923=CARTESIAN_POINT ( 'NONE',  ( 4.793709693897413082, 2.072883653632663137, -0.7987435787581667057 ) ) ;
#212929=CARTESIAN_POINT ( 'NONE',  ( 3.235000160576475992, 2.016597019841442240, -0.002811030766311505089 ) ) ;
#212931=CARTESIAN_POINT ( 'NONE',  ( 1.727463565662648026, 0.1559948080240464718, -2.056756566214789306 ) ) ;
#212936=CARTESIAN_POINT ( 'NONE',  ( 5.033237522093748417, -1.548190877955179179, -1.551241237171486098 ) ) ;
#212937=CARTESIAN_POINT ( 'NONE',  ( 1.986954140179174155, -2.015912935764123670, 0.05229865529512293942 ) ) ;
#212938=CARTESIAN_POINT ( 'NONE',  ( 1.100829259350871281, -0.4471758257712907247, 1.786007343351428966 ) ) ;
#212941=CARTESIAN_POINT ( 'NONE',  ( 5.702125722003772879, -1.825762228975034596, 0.002264948092654816680 ) ) ;
#212942=CARTESIAN_POINT ( 'NONE',  ( 5.660779783930850684, 1.203351582566011047, 1.617819807990819481 ) ) ;
#212944=CARTESIAN_POINT ( 'NONE',  ( 4.909165057579100377, 1.966063467186284663, 1.119528758242648525 ) ) ;
#212946=CARTESIAN_POINT ( 'NONE',  ( 0.8386649464857205416, 2.075244960028700181, 0.3580382472886770584 ) ) ;
#212948=CARTESIAN_POINT ( 'NONE',  ( 4.510256325466165173, 2.069976601481211542, -0.04757507122059301263 ) ) ;
#212956=CARTESIAN_POINT ( 'NONE',  ( 2.109928881651984778, 1.720655366031418332, 1.405045424887063410 ) ) ;
#212960=CARTESIAN_POINT ( 'NONE',  ( 3.754310534785664899, -1.959519245081872585, -0.09869234604030494018 ) ) ;
#212966=CARTESIAN_POINT ( 'NONE',  ( 2.672263739372262137, 2.109986773948614225, -0.2121620573234672125 ) ) ;
#212968=CARTESIAN_POINT ( 'NONE',  ( 4.223607183596161718, -2.069420184152844566, 0.6248923283326962563 ) ) ;
#212969=CARTESIAN_POINT ( 'NONE',  ( 2.524749765808989466, -1.717266272480859834, 0.6646640004178903105 ) ) ;
#212972=CARTESIAN_POINT ( 'NONE',  ( 6.017484387666114820, -0.9725936433230500944, -1.442976214814440716 ) ) ;
#212976=CARTESIAN_POINT ( 'NONE',  ( 2.922914210685311431, 2.035003303901411265, 0.7295308445595325431 ) ) ;
#212978=CARTESIAN_POINT ( 'NONE',  ( 4.921249881687197458, 0.7690040753521177885, 1.863882819927860535 ) ) ;
#212980=CARTESIAN_POINT ( 'NONE',  ( 2.799875798528407511, -0.6792266858460673795, 2.052276964324008635 ) ) ;
#212982=CARTESIAN_POINT ( 'NONE',  ( 2.653541938639871756, 0.5291849669812850321, -1.898919477364902741 ) ) ;
#212984=CARTESIAN_POINT ( 'NONE',  ( 4.036618323093550842, -1.688041843851136425, 0.9601762628524412868 ) ) ;
#212995=CARTESIAN_POINT ( 'NONE',  ( 0.9212656856641410208, 2.039593612490635532, 0.8430313063367624871 ) ) ;
#212997=CARTESIAN_POINT ( 'NONE',  ( 4.856279117655732058, -1.961245242753749674, -0.05215834203427943683 ) ) ;
#213000=CARTESIAN_POINT ( 'NONE',  ( 0.1747926744264677867, 0.7439089246787933263, -1.939883394317852616 ) ) ;
#213001=CARTESIAN_POINT ( 'NONE',  ( 4.382634408885896171, 1.643497958660003144, -0.8300281608688080404 ) ) ;
#213007=CARTESIAN_POINT ( 'NONE',  ( 4.957343421279006179, -1.817532610912236724, 1.092287347377165485 ) ) ;
#213010=CARTESIAN_POINT ( 'NONE',  ( 6.415316853601439995, -0.2566941480561866773, 2.044681889290477894 ) ) ;
#213012=CARTESIAN_POINT ( 'NONE',  ( 0.2911520677349140884, -1.704046917483082346, 0.7485983125269514149 ) ) ;
#213013=CARTESIAN_POINT ( 'NONE',  ( 3.315785976855676775, 1.165629053876730659, -1.425327459889616177 ) ) ;
#213019=CARTESIAN_POINT ( 'NONE',  ( 3.703933201646680828, -0.6411959742554216302, 2.111683309420588905 ) ) ;
#213020=CARTESIAN_POINT ( 'NONE',  ( 4.534621088391048715, 2.217606307645642261, 0.4472613530076152699 ) ) ;
#213022=CARTESIAN_POINT ( 'NONE',  ( 5.484552789610383172, -1.142847587564936207, 1.405643779654427661 ) ) ;
#213023=CARTESIAN_POINT ( 'NONE',  ( 5.155460239800898847, 1.844409812803897264, -0.5174689040137578910 ) ) ;
#213025=CARTESIAN_POINT ( 'NONE',  ( 5.805500895539822181, -0.4530025297027094888, 1.814837910242727226 ) ) ;
#213026=CARTESIAN_POINT ( 'NONE',  ( 5.898848723475273559, 0.3636257040535681995, 1.824992291636283293 ) ) ;
#213030=CARTESIAN_POINT ( 'NONE',  ( 6.543818844511720023, 0.6727183027174578056, -1.637219817372371100 ) ) ;
#213033=CARTESIAN_POINT ( 'NONE',  ( 1.551970632248239612, 1.040795554343958429, 1.727062486439542965 ) ) ;
#213036=CARTESIAN_POINT ( 'NONE',  ( 2.438226732591573409, 0.9919046538873840246, -1.857854779501419307 ) ) ;
#213040=CARTESIAN_POINT ( 'NONE',  ( 1.916276942859599597, -2.019257470013501088, 0.05376132052286108215 ) ) ;
#213044=CARTESIAN_POINT ( 'NONE',  ( 2.935029080331118756, 0.2613785356864756770, 2.145644965459513109 ) ) ;
#213045=CARTESIAN_POINT ( 'NONE',  ( 6.610000000000028741, 1.211438232176115237, 2.390254139237833808 ) ) ;
#213052=CARTESIAN_POINT ( 'NONE',  ( 0.4510473619779230003, -1.854578567552306767, -1.167393260480112493 ) ) ;
#213054=CARTESIAN_POINT ( 'NONE',  ( 2.624197652063056996, -1.302182479666073700, -1.850046142848650321 ) ) ;
#213061=CARTESIAN_POINT ( 'NONE',  ( 3.444378845967084324, 0.4270997545614327318, 1.717301222563255791 ) ) ;
#213063=CARTESIAN_POINT ( 'NONE',  ( 6.124089168553260798, -1.220954261165616783, -1.838047742986161026 ) ) ;
#213067=CARTESIAN_POINT ( 'NONE',  ( 5.413685477598253470, -1.281375732037979942, -1.556898226837098331 ) ) ;
#213069=CARTESIAN_POINT ( 'NONE',  ( 2.887410755087606695, 1.321643875934110479, 1.324118206929347563 ) ) ;
#213070=CARTESIAN_POINT ( 'NONE',  ( 3.309495622959734096, -1.689761761210720525, -1.195817184978978265 ) ) ;
#213076=CARTESIAN_POINT ( 'NONE',  ( 1.142663480069527671, 1.843847066288730074, 0.5072560978593986247 ) ) ;
#213077=CARTESIAN_POINT ( 'NONE',  ( 2.330453122711079850, -1.209328770571056921, 1.544706564130463811 ) ) ;
#213078=CARTESIAN_POINT ( 'NONE',  ( 0.9661724576192336489, 1.646585359754201061, 1.163093122096101162 ) ) ;
#213082=CARTESIAN_POINT ( 'NONE',  ( 6.784453690597813669, -1.932871751835860241, -0.3867854297147227394 ) ) ;
#213084=CARTESIAN_POINT ( 'NONE',  ( 1.758066197707741640, 0.7666020408202559588, -1.861725765494412599 ) ) ;
#213087=CARTESIAN_POINT ( 'NONE',  ( 2.003655485592752861, -2.052825532818176590, 0.5177380972332337183 ) ) ;
#213089=CARTESIAN_POINT ( 'NONE',  ( 3.895033709675084221, 0.3008086390649654662, 2.048262060622765279 ) ) ;
#213091=CARTESIAN_POINT ( 'NONE',  ( 5.929650942584956397, 1.031255971971676955, -1.818501217082470145 ) ) ;
#213093=CARTESIAN_POINT ( 'NONE',  ( 4.541915102786819425, 0.7800907816924649296, -1.650662693317282770 ) ) ;
#213096=CARTESIAN_POINT ( 'NONE',  ( 6.890000000000007674, 7.629137130509070275, 2.600000000000001421 ) ) ;
#213098=CARTESIAN_POINT ( 'NONE',  ( 6.387735258934439386, 1.517164627179751646, 1.602757196154185770 ) ) ;
#213101=CARTESIAN_POINT ( 'NONE',  ( 5.373660369522260005, 0.3689257714810100786, -1.876182517032434216 ) ) ;
#213108=CARTESIAN_POINT ( 'NONE',  ( 0.7844012160764175512, 1.623964078452419857, -0.8677550623670119423 ) ) ;
#213112=CARTESIAN_POINT ( 'NONE',  ( 4.446469999505775483, 0.4968273501132040026, 1.803309644091706021 ) ) ;
#213120=CARTESIAN_POINT ( 'NONE',  ( 1.129674139269299049, 1.899472608897791348, -0.5201393403096374879 ) ) ;
#213121=CARTESIAN_POINT ( 'NONE',  ( 1.915638884950950027, -1.319244919589783516, -1.525031147761625405 ) ) ;
#213125=CARTESIAN_POINT ( 'NONE',  ( 2.256057974219495499, 0.9384471748680022207, 1.980482673072603284 ) ) ;
#213137=CARTESIAN_POINT ( 'NONE',  ( 5.249485218566787736, 1.838879873951341004, -0.09611505855997715120 ) ) ;
#213138=CARTESIAN_POINT ( 'NONE',  ( 1.875641098811844154, 0.3420332329174725072, -1.983669356598726674 ) ) ;
#213139=CARTESIAN_POINT ( 'NONE',  ( 3.198860821731682513, -1.541234334381531568, -1.705209785003541700 ) ) ;
#213141=CARTESIAN_POINT ( 'NONE',  ( 1.568971434307638857, 1.638126988201485279, 0.8830449202173286105 ) ) ;
#213144=CARTESIAN_POINT ( 'NONE',  ( 5.765855477156511810, 0.5488314196105298359, -1.831976909803390896 ) ) ;
#213147=CARTESIAN_POINT ( 'NONE',  ( 4.651946873442760477, 0.8016356570225026124, 1.931162265472508910 ) ) ;
#213148=CARTESIAN_POINT ( 'NONE',  ( 3.871829239884491791, 1.038646522470688671, 1.555605274479121114 ) ) ;
#213150=CARTESIAN_POINT ( 'NONE',  ( 5.513187957602974976, -1.795010045117376496, 0.4093405989887277663 ) ) ;
#213153=CARTESIAN_POINT ( 'NONE',  ( 4.687984124052484880, -0.8092498044112338418, 1.523260386444349468 ) ) ;
#213158=CARTESIAN_POINT ( 'NONE',  ( 4.680651438812245324, 1.340593046976858771, -1.707629433300766664 ) ) ;
#213159=CARTESIAN_POINT ( 'NONE',  ( 3.141029808440584326, -1.609794727316344209, 0.8612202190056221784 ) ) ;
#213160=CARTESIAN_POINT ( 'NONE',  ( 0.7253527386562284018, 0.1980078388067410822, -1.951770168129369543 ) ) ;
#213161=CARTESIAN_POINT ( 'NONE',  ( 5.454358448847595575, -1.341013495729547644, 1.638584853213326031 ) ) ;
#213162=CARTESIAN_POINT ( 'NONE',  ( 5.759400667030329934, 2.259083744078540956, -0.3884743064591251738 ) ) ;
#213167=CARTESIAN_POINT ( 'NONE',  ( 1.875790325896836919, 0.3594715711359474652, -2.089634487563592824 ) ) ;
#213171=CARTESIAN_POINT ( 'NONE',  ( 6.368071955308375998, -2.155667716570781156, 0.2575352064990812928 ) ) ;
#213172=CARTESIAN_POINT ( 'NONE',  ( 6.983263157960368339, 1.271300847835453940, 2.069154070428773196 ) ) ;
#213174=CARTESIAN_POINT ( 'NONE',  ( 2.122025409673257812, -0.4832278914180427876, 2.167962204723080433 ) ) ;
#213176=CARTESIAN_POINT ( 'NONE',  ( 6.504528880466823537, -1.955196382115764964, 0.4926337920100053447 ) ) ;
#213178=CARTESIAN_POINT ( 'NONE',  ( 5.981316409642544407, -0.05633626937831189702, 2.061977559458886056 ) ) ;
#213183=CARTESIAN_POINT ( 'NONE',  ( 0.2333540202161610289, 7.629137130509112907, -2.645727818377396900 ) ) ;
#213184=CARTESIAN_POINT ( 'NONE',  ( 5.478019777291557979, -1.797689181224306321, -0.3974485807837144224 ) ) ;
#213185=AXIS2_PLACEMENT_3D ( 'NONE', #212850, #12522, #110108 ) ;
#213186=ADVANCED_FACE ( 'NONE', ( #131719 ), #98485, .F. ) ;
#213189=CARTESIAN_POINT ( 'NONE',  ( 1.606044756371062920, -0.6162743471601249690, -1.611104689205801188 ) ) ;
#213190=CARTESIAN_POINT ( 'NONE',  ( 0.5324358445358172709, 0.5899921999869184308, 1.928256190492839028 ) ) ;
#213191=CARTESIAN_POINT ( 'NONE',  ( 2.374040334453372925, -0.3969776081079456898, -2.264039395722910353 ) ) ;
#213193=CARTESIAN_POINT ( 'NONE',  ( 2.495744459589462227, 1.747532462024743882, 1.436835450399133407 ) ) ;
#213194=CARTESIAN_POINT ( 'NONE',  ( 4.020224483524700076, -1.082363273655801095, -1.806513482918799429 ) ) ;
#213196=CARTESIAN_POINT ( 'NONE',  ( 2.389615768203833479, -0.7611923103308501082, 1.597832513397597021 ) ) ;
#213201=CARTESIAN_POINT ( 'NONE',  ( 6.363560548480147183, -1.783403785914154049, -1.324293268510617017 ) ) ;
#213202=CARTESIAN_POINT ( 'NONE',  ( 3.293114190187882429, 1.727671002657789057, 1.348082825637614279 ) ) ;
#213209=CARTESIAN_POINT ( 'NONE',  ( 6.258074605086497932, 0.8102346573028992305, -1.959903593942226685 ) ) ;
#213215=CARTESIAN_POINT ( 'NONE',  ( 6.392148736875968851, -0.4980823202534768179, -1.772533436741857260 ) ) ;
#213218=CARTESIAN_POINT ( 'NONE',  ( 2.243362625160577384, 1.740107689937436808, 0.04144568419049177860 ) ) ;
#213220=CARTESIAN_POINT ( 'NONE',  ( 0.6429252097494702056, -0.2364460082661112295, -1.947484529462916836 ) ) ;
#213223=CARTESIAN_POINT ( 'NONE',  ( 6.368072262247213899, 1.106822706796772193, 1.856716078747308263 ) ) ;
#213226=CARTESIAN_POINT ( 'NONE',  ( 5.577088068215094729, -0.04877400797019536272, -2.161318155665878038 ) ) ;
#213230=CARTESIAN_POINT ( 'NONE',  ( 5.659438124648599633, 0.3871718161991606344, -1.932801920045317257 ) ) ;
#213231=CARTESIAN_POINT ( 'NONE',  ( 5.448516766998877436, 1.166291874360864345, 1.283151444216067638 ) ) ;
#213233=CARTESIAN_POINT ( 'NONE',  ( 1.945129482973105839, -1.762486321751283835, -1.302348873264857820 ) ) ;
#213234=CARTESIAN_POINT ( 'NONE',  ( 3.628207509315328760, -1.372338424813070556, -1.855037849730954091 ) ) ;
#213235=CARTESIAN_POINT ( 'NONE',  ( 5.237599208242285087, -1.454345255708370255, -1.460303020606460445 ) ) ;
#213236=CARTESIAN_POINT ( 'NONE',  ( 0.8318532965871343610, 1.913089267318631270, 0.3326846900589939815 ) ) ;
#213242=CARTESIAN_POINT ( 'NONE',  ( 4.517907016363444939, -0.5628432189327194912, 2.044499502628312371 ) ) ;
#213243=CARTESIAN_POINT ( 'NONE',  ( 2.619767714365705658, 0.2496074646863334634, 2.000857082853441327 ) ) ;
#213245=CARTESIAN_POINT ( 'NONE',  ( 4.753059971535213535, -1.774748228059085164, 1.311344899593884561 ) ) ;
#213255=CARTESIAN_POINT ( 'NONE',  ( 4.662995224183227982, -1.840047010505897029, -0.9283316357228312832 ) ) ;
#213259=CARTESIAN_POINT ( 'NONE',  ( 0.1329588055935395918, 0.006246367379872773060, -1.846049620084759590 ) ) ;
#213261=CARTESIAN_POINT ( 'NONE',  ( 2.983074145627107931, -1.866958838928289399, -0.7709177042417614256 ) ) ;
#213265=CARTESIAN_POINT ( 'NONE',  ( 2.676696200465655373, -1.971695749941338560, -0.5996849476793424394 ) ) ;
#213268=CARTESIAN_POINT ( 'NONE',  ( 1.657894046870052485, -1.302874822933766774, 1.301145727299134025 ) ) ;
#213269=CARTESIAN_POINT ( 'NONE',  ( 0.4523713176287887383, 0.7179250195528188438, -2.193251166140824715 ) ) ;
#213271=CARTESIAN_POINT ( 'NONE',  ( 2.847126979364768218, -1.798887516807456954, 1.198237791991546564 ) ) ;
#213273=CARTESIAN_POINT ( 'NONE',  ( 1.358611653602972646, -1.916354379050893009, -0.6279873632355145174 ) ) ;
#213274=CARTESIAN_POINT ( 'NONE',  ( 2.425563141628499064, 0.9819131520533967983, 2.078181775667542475 ) ) ;
#213277=CARTESIAN_POINT ( 'NONE',  ( 0.2857447052702493662, -0.8859512962964136706, 1.647562673099879138 ) ) ;
#213279=CARTESIAN_POINT ( 'NONE',  ( 4.785985848584410896, -0.9303070431277806751, 1.738173387191404684 ) ) ;
#213281=CARTESIAN_POINT ( 'NONE',  ( 4.821500071095637274, -1.429446227384461032, -1.422610148874188463 ) ) ;
#213285=CARTESIAN_POINT ( 'NONE',  ( 6.076811011874215573, -1.999271364452784638, -0.6623750905550094270 ) ) ;
#213286=CARTESIAN_POINT ( 'NONE',  ( 6.180147188013234150, -1.146869210499700920, -1.723488058659912392 ) ) ;
#213289=CARTESIAN_POINT ( 'NONE',  ( 6.539320575229247368, 1.272291865413360812, 2.120198356887960767 ) ) ;
#213290=CARTESIAN_POINT ( 'NONE',  ( 6.451426753955883164, -1.802380967894920527, 0.9117540809469369956 ) ) ;
#213292=CARTESIAN_POINT ( 'NONE',  ( 4.108297157686680912, -2.301651690510425841, 0.1678553853470560464 ) ) ;
#213293=CARTESIAN_POINT ( 'NONE',  ( 1.868110439076278384, -2.047461887716729656, 0.2484499435305431159 ) ) ;
#213300=CARTESIAN_POINT ( 'NONE',  ( 4.316952289276101418, -1.611618797226920252, 1.455085969030824211 ) ) ;
#213304=CARTESIAN_POINT ( 'NONE',  ( 3.403688466941825475, -0.7492148395099357261, -1.682118234477212537 ) ) ;
#213306=CARTESIAN_POINT ( 'NONE',  ( 5.179302069984247581, 1.471482994053765925, 1.624232740060495228 ) ) ;
#213308=CARTESIAN_POINT ( 'NONE',  ( 5.858358025671378755, 0.9108227554960802719, 2.071263147418811013 ) ) ;
#213313=CARTESIAN_POINT ( 'NONE',  ( 6.837169251635001999, -1.579311124772398767, 0.7986344709578310219 ) ) ;
#213315=CARTESIAN_POINT ( 'NONE',  ( 3.879544890376307453, 0.2443292893146010170, -1.998135132051428231 ) ) ;
#213317=CARTESIAN_POINT ( 'NONE',  ( 3.469845758843297823, 2.055011051013386769, -0.4596899858253248872 ) ) ;
#213318=CARTESIAN_POINT ( 'NONE',  ( 1.897908843228306663, -0.9047085692259320133, -1.688519222619834892 ) ) ;
#213320=CARTESIAN_POINT ( 'NONE',  ( 3.191813391966125124, -1.320872291013975630, -1.461159636213595459 ) ) ;
#213321=CARTESIAN_POINT ( 'NONE',  ( 4.886975862609196142, -1.903224527948672584, -0.6766701927056159027 ) ) ;
#213322=CARTESIAN_POINT ( 'NONE',  ( 0.4615142869485132637, 1.850934062480696252, -0.2700578556205368574 ) ) ;
#213323=CARTESIAN_POINT ( 'NONE',  ( 0.8362905744919849615, -1.092891352686057527, 1.629061181365853539 ) ) ;
#213324=CARTESIAN_POINT ( 'NONE',  ( 0.4922593472763935329, -1.060406550076501642, 1.591262010887870115 ) ) ;
#213330=CARTESIAN_POINT ( 'NONE',  ( 1.082579992370054311, 1.234693400583252609, -1.661741702728709802 ) ) ;
#213335=CARTESIAN_POINT ( 'NONE',  ( 5.268275487455277073, 2.118052368503114291, -0.1043780312826799589 ) ) ;
#213341=CARTESIAN_POINT ( 'NONE',  ( 6.250445965835445428, -1.952298026214387194, -0.1936728439068043650 ) ) ;
#213343=CARTESIAN_POINT ( 'NONE',  ( 4.393907559866160994, 0.09612058942952760032, 2.013924333851605297 ) ) ;
#213344=CARTESIAN_POINT ( 'NONE',  ( 3.432743858578292784, -1.563009043653120322, 1.107381117132580250 ) ) ;
#213346=CARTESIAN_POINT ( 'NONE',  ( 1.066276686178056377, -1.386418637449363889, 1.697306931840412370 ) ) ;
#213347=CARTESIAN_POINT ( 'NONE',  ( 0.1333692844072559280, 6.947498546895843674, -2.648624074793118233 ) ) ;
#213348=CARTESIAN_POINT ( 'NONE',  ( 2.934663490303309530, 0.2251962677765201870, 1.856852477824536329 ) ) ;
#213353=CARTESIAN_POINT ( 'NONE',  ( 6.116841120987044356, 0.2079722402913257440, 2.107011275531808003 ) ) ;
#213355=CARTESIAN_POINT ( 'NONE',  ( 2.015285228526709549, -2.027172053905087701, 0.5110949307850811696 ) ) ;
#213357=CARTESIAN_POINT ( 'NONE',  ( 0.7973487315477224557, -0.6271472479968034364, 1.606907058918445985 ) ) ;
#213367=CARTESIAN_POINT ( 'NONE',  ( 2.174188805400371294, 0.7754062184415695391, 1.637274071133995035 ) ) ;
#213371=CARTESIAN_POINT ( 'NONE',  ( 6.539320575229257138, 2.987941927008979537, 2.250856951216452906 ) ) ;
#213375=CARTESIAN_POINT ( 'NONE',  ( 2.787383077106736273, -1.737616373609903286, 0.6669969758191662823 ) ) ;
#213376=CARTESIAN_POINT ( 'NONE',  ( 0.4388990752801218975, -1.618778001572194647, -1.023919763412997286 ) ) ;
#213377=CARTESIAN_POINT ( 'NONE',  ( 6.475613818078473471, 1.843275991838376981, -0.5597920731088936730 ) ) ;
#213384=CARTESIAN_POINT ( 'NONE',  ( 4.733233314711627671, 0.004152288854553880422, -1.969629310717621040 ) ) ;
#213385=CARTESIAN_POINT ( 'NONE',  ( 1.313308151137903224, 1.731519532738003297, -1.223779428986125462 ) ) ;
#213389=CARTESIAN_POINT ( 'NONE',  ( 5.894512528888635750, 1.793468170635740710, -1.259063434910556500 ) ) ;
#213391=CARTESIAN_POINT ( 'NONE',  ( 4.260710244665906643, -1.428042822336324846, 1.293124370783913735 ) ) ;
#213394=CARTESIAN_POINT ( 'NONE',  ( 1.207977004800918852, -0.5332226995428279714, 2.141375170867452660 ) ) ;
#213400=CARTESIAN_POINT ( 'NONE',  ( 6.491062224718945117, 0.1893930596480186412, 1.960278089617428554 ) ) ;
#213401=CARTESIAN_POINT ( 'NONE',  ( 1.663517674946796143, 1.000093669912437644, 1.664638661912527962 ) ) ;
#213403=CARTESIAN_POINT ( 'NONE',  ( 0.1575669172422279607, -0.4392406603518673736, -1.974865693180789750 ) ) ;
#213405=CARTESIAN_POINT ( 'NONE',  ( 5.137489257405690957, 1.737274493258118113, -0.6675986409061424043 ) ) ;
#213407=CARTESIAN_POINT ( 'NONE',  ( 6.509000000000012776, 0.5843741663743782233, 2.053293374786519188 ) ) ;
#213410=CARTESIAN_POINT ( 'NONE',  ( 0.9783777488623355278, -2.139296967303818686, -0.4750931833387496694 ) ) ;
#213414=CARTESIAN_POINT ( 'NONE',  ( 2.191784710619415044, -0.7813054520266484726, 1.650194661559079456 ) ) ;
#213417=CARTESIAN_POINT ( 'NONE',  ( 6.609000000000064823, 1.245995683336246884, 2.213443714173808807 ) ) ;
#213419=CARTESIAN_POINT ( 'NONE',  ( 6.586557105272873969, -1.791547847876047594, -0.3505316570680468979 ) ) ;
#213420=CARTESIAN_POINT ( 'NONE',  ( 3.977359813172594905, -0.1486911861427446802, 1.956209631609528099 ) ) ;
#213423=CARTESIAN_POINT ( 'NONE',  ( 4.405938146338868933, -0.9375679901368579872, -1.981035393479456008 ) ) ;
#213425=CARTESIAN_POINT ( 'NONE',  ( 6.609000000000011532, 3.695567819995113634, 2.514302272609474809 ) ) ;
#213426=CARTESIAN_POINT ( 'NONE',  ( 2.922783962489564846, -1.430918204188264875, 1.496350883549990352 ) ) ;
#213430=CARTESIAN_POINT ( 'NONE',  ( 3.393488084526240733, -0.9333142364225041065, -2.100862151682027612 ) ) ;
#213434=CARTESIAN_POINT ( 'NONE',  ( 6.720655732516688019, 6.039915720534646759, 2.321169117395345705 ) ) ;
#213436=CARTESIAN_POINT ( 'NONE',  ( 4.347558855881414885, 1.941490382076584975, -0.04909019101095174475 ) ) ;
#213439=CARTESIAN_POINT ( 'NONE',  ( 4.605663860560767375, 1.420894170025093439, 1.280184534114735095 ) ) ;
#213441=CARTESIAN_POINT ( 'NONE',  ( 5.438411972298594854, 1.699845694858553857, 0.2911611187441583426 ) ) ;
#213442=CARTESIAN_POINT ( 'NONE',  ( 4.645720405014278853, 1.993893748393640086, -0.3006458143828410479 ) ) ;
#213443=CARTESIAN_POINT ( 'NONE',  ( 4.571052534358505781, -1.084669189052098082, 2.026668040654127090 ) ) ;
#213445=CARTESIAN_POINT ( 'NONE',  ( 0.8915962724085277902, 1.944627461026976034, -1.043433064090833140 ) ) ;
#213448=CARTESIAN_POINT ( 'NONE',  ( 6.397684210179588327, -0.5939413028648796722, 1.667199339893215448 ) ) ;
#213450=CARTESIAN_POINT ( 'NONE',  ( 2.185838763446645849, -0.9780977115210144346, 2.073240998862643458 ) ) ;
#213451=CARTESIAN_POINT ( 'NONE',  ( 1.376469814831126071, 1.609123190100629985, -0.6634216792447115152 ) ) ;
#213453=CARTESIAN_POINT ( 'NONE',  ( 1.246934265006810927, -1.689945720101847293, -0.3868003843893202953 ) ) ;
#213456=CARTESIAN_POINT ( 'NONE',  ( 1.188188303608740615, -1.377055334905618933, -1.678633986682298573 ) ) ;
#213457=CARTESIAN_POINT ( 'NONE',  ( 2.061732777098632230, 1.244387006429502396, 1.586668050434843158 ) ) ;
#213459=CARTESIAN_POINT ( 'NONE',  ( 5.602155610709171896, -1.926676517935271171, 0.002254597750208849581 ) ) ;
#213461=CARTESIAN_POINT ( 'NONE',  ( 2.268119307372215676, 0.5874642799142595351, -2.142291314107084954 ) ) ;
#213468=CARTESIAN_POINT ( 'NONE',  ( 5.302228144868663229, 1.312797389530523162, -1.142775443803839108 ) ) ;
#213469=CARTESIAN_POINT ( 'NONE',  ( 3.859774877264535053, -0.5717695562157121270, 1.876676618968641019 ) ) ;
#213473=CARTESIAN_POINT ( 'NONE',  ( 4.798257751182677389, -2.261729152689537781, -0.06211711723675371333 ) ) ;
#213474=CARTESIAN_POINT ( 'NONE',  ( 1.486864572717770283, 1.987365476997263292, 0.5519934122387574194 ) ) ;
#213477=CARTESIAN_POINT ( 'NONE',  ( 2.852682258652036840, 0.7612096163719231923, 2.130753183350143409 ) ) ;
#213478=EDGE_LOOP ( 'NONE', ( #132318, #162335, #186467, #203046 ) ) ;
#213480=CARTESIAN_POINT ( 'NONE',  ( 2.917106759524803472, -0.1871779394605546654, 1.861177454839262113 ) ) ;
#213481=CARTESIAN_POINT ( 'NONE',  ( 1.300929835083320274, 1.165380355416269609, -1.284392162598305021 ) ) ;
#213482=CARTESIAN_POINT ( 'NONE',  ( 5.706613541269077494, 1.932210019790636224, 1.034112652976440394 ) ) ;
#213483=CARTESIAN_POINT ( 'NONE',  ( 0.3763673390903346516, 1.272619870141003418, 1.802674353332263335 ) ) ;
#213484=CARTESIAN_POINT ( 'NONE',  ( 3.766626874709140704, -1.453462046928340579, 1.600284095077113333 ) ) ;
#213485=CARTESIAN_POINT ( 'NONE',  ( 4.154194137148957466, -1.438218894771810641, 1.305048227774636915 ) ) ;
#213488=CARTESIAN_POINT ( 'NONE',  ( 6.749288224047838902, -1.502610544577225760, -1.113804566994440970 ) ) ;
#213490=CARTESIAN_POINT ( 'NONE',  ( 0.4687500000003047007, 0.7852924748224731077, -1.895863743164100335 ) ) ;
#213494=CARTESIAN_POINT ( 'NONE',  ( 5.397111353752316987, -0.9091427841607623295, -1.799923777076550824 ) ) ;
#213498=CARTESIAN_POINT ( 'NONE',  ( 3.053144290054691901, -1.492835736363471888, -1.050712463094093385 ) ) ;
#213506=CARTESIAN_POINT ( 'NONE',  ( 6.252604593904901975, 1.998004417694958512, 0.2941112629052196614 ) ) ;
#213507=CARTESIAN_POINT ( 'NONE',  ( 1.084817099560590803, -1.342388549496125627, 1.641497191572589776 ) ) ;
#213511=CARTESIAN_POINT ( 'NONE',  ( 6.245006310359877411, -1.742422335079217843, 1.100243706638550423 ) ) ;
#213512=CARTESIAN_POINT ( 'NONE',  ( 5.590470263882489910, -0.4872053753022275724, 1.956560708789633285 ) ) ;
#213517=CARTESIAN_POINT ( 'NONE',  ( -0.1290005225502675879, -0.006633637972621592160, -2.173875058097324064 ) ) ;
#213519=CARTESIAN_POINT ( 'NONE',  ( 4.798203786142633653, -1.844427309015805649, 0.8145022673629878085 ) ) ;
#213520=CARTESIAN_POINT ( 'NONE',  ( 4.646344025792163990, -1.477054284018078256, 1.098930429567553047 ) ) ;
#213521=CARTESIAN_POINT ( 'NONE',  ( -0.02319159430949970999, 4.096340798889516854, -2.366022381217198767 ) ) ;
#213522=CARTESIAN_POINT ( 'NONE',  ( 2.737322364211117520, 0.2836107604972230578, 2.290143083710040717 ) ) ;
#213524=CARTESIAN_POINT ( 'NONE',  ( 6.081358973892867503, 1.999796440023202448, -0.8210498935554910727 ) ) ;
#213526=CARTESIAN_POINT ( 'NONE',  ( 0.8021671156859496721, 1.469769370800941166, -1.269469122775281456 ) ) ;
#213529=CARTESIAN_POINT ( 'NONE',  ( 4.288600692895239597, -2.201063653074202708, 0.6618141117178658606 ) ) ;
#213532=CARTESIAN_POINT ( 'NONE',  ( 3.942156681999692491, 1.861596489644477437, 0.1839347620080991341 ) ) ;
#213534=CARTESIAN_POINT ( 'NONE',  ( 1.634869402278725348, 1.785593253932623803, 0.6852637533772619749 ) ) ;
#213537=CARTESIAN_POINT ( 'NONE',  ( 3.123846942790895476, -2.126788776302591888, 0.5888931905130634359 ) ) ;
#213538=CARTESIAN_POINT ( 'NONE',  ( 6.983263157960401202, 2.460233018525457727, 2.229759568558951965 ) ) ;
#213543=CARTESIAN_POINT ( 'NONE',  ( 0.5792891803052163668, 1.841034274367932877, -0.7053527730483382108 ) ) ;
#213544=CARTESIAN_POINT ( 'NONE',  ( 1.097181765414790400, -0.5634973350938665693, -2.237626367659339088 ) ) ;
#213545=CARTESIAN_POINT ( 'NONE',  ( 1.240593047436115759, -1.913272810121857237, -0.4332019784048374289 ) ) ;
#213546=CARTESIAN_POINT ( 'NONE',  ( 5.366109125895877519, -2.053123361074739250, 0.1969011160823062045 ) ) ;
#213553=CARTESIAN_POINT ( 'NONE',  ( 1.094852686531849084, 2.138608527004157711, 0.3732488551555103173 ) ) ;
#213556=CARTESIAN_POINT ( 'NONE',  ( 6.603072989126265391, -0.3962418105841297722, 1.804722624154910360 ) ) ;
#213559=CARTESIAN_POINT ( 'NONE',  ( 0.8603690976232807319, -1.359099942111790416, 1.285485254608226269 ) ) ;
#213560=CARTESIAN_POINT ( 'NONE',  ( 5.712251288600169730, -0.9662322189689104279, -1.933677227328117532 ) ) ;
#213562=CARTESIAN_POINT ( 'NONE',  ( 0.07735805125225460321, 4.085280796943619563, -2.643583850410589964 ) ) ;
#213564=CARTESIAN_POINT ( 'NONE',  ( 2.473184984502617478, -1.664690511387197702, -0.9409074295685518896 ) ) ;
#213565=CARTESIAN_POINT ( 'NONE',  ( 3.168565732603556562, -1.634766719728536266, -0.6786406015907071598 ) ) ;
#213566=CARTESIAN_POINT ( 'NONE',  ( 0.5570965697654255422, -1.639946202723217450, 0.9833419947904218361 ) ) ;
#213568=CARTESIAN_POINT ( 'NONE',  ( 5.730082575778132181, 1.913663781862886104, 0.08886097549761286241 ) ) ;
#213570=CARTESIAN_POINT ( 'NONE',  ( 6.303175665915636827, -1.664687476133955846, 1.052260723566181833 ) ) ;
#213572=CARTESIAN_POINT ( 'NONE',  ( 0.8090202166558431163, -0.5209130535433897924, -2.055487714681260236 ) ) ;
#213574=CARTESIAN_POINT ( 'NONE',  ( 4.522238337509359773, 1.150754656758418593, -1.474723989322044959 ) ) ;
#213575=CARTESIAN_POINT ( 'NONE',  ( 0.9260630535584664091, 1.089557764695957554, -1.464779044915397455 ) ) ;
#213577=CARTESIAN_POINT ( 'NONE',  ( 5.057340365224886725, -1.863002784048470639, -1.182737378625432489 ) ) ;
#213580=CARTESIAN_POINT ( 'NONE',  ( 1.785667050844968351, -1.942997710132963407, 0.6927838567832644845 ) ) ;
#213586=CARTESIAN_POINT ( 'NONE',  ( 4.492674960910642667, 2.029786422369950216, 0.4070406814440513665 ) ) ;
#213588=CARTESIAN_POINT ( 'NONE',  ( 1.599129061979026822, 1.768144091905754500, -1.243190488262067683 ) ) ;
#213590=CARTESIAN_POINT ( 'NONE',  ( 1.928384432292037598, -0.9539229595667864103, -1.780212580967098335 ) ) ;
#213596=CARTESIAN_POINT ( 'NONE',  ( 0.2687680251878405424, -0.2516378192510167477, -2.000730910237565663 ) ) ;
#213597=CARTESIAN_POINT ( 'NONE',  ( 5.038714576072483631, -1.879839391954684746, 1.126354835186346603 ) ) ;
#213599=CARTESIAN_POINT ( 'NONE',  ( 3.761887187967042134, 0.6396200178584460216, -1.802413552503052463 ) ) ;
#213603=CARTESIAN_POINT ( 'NONE',  ( 1.933220473845993492, -1.621196910160098925, -1.198842755339262212 ) ) ;
#213605=CARTESIAN_POINT ( 'NONE',  ( 0.9082674546003096649, -1.036902680258915854, -2.044550831922228085 ) ) ;
#213607=CARTESIAN_POINT ( 'NONE',  ( 4.559404828610894356, 0.3762245950137115269, -1.683048502377647804 ) ) ;
#213611=CARTESIAN_POINT ( 'NONE',  ( 0.07516593201273635838, 6.947014887512039216, -2.639261810199782232 ) ) ;
#213615=CARTESIAN_POINT ( 'NONE',  ( 5.443967095383744237, -1.154075521934978532, -1.396247737120015930 ) ) ;
#213619=CARTESIAN_POINT ( 'NONE',  ( 5.777939495331589015, 1.783485896618082878, -0.3162516061415173718 ) ) ;
#213622=CARTESIAN_POINT ( 'NONE',  ( 2.853686581259745836, 2.180823047698337902, -0.2155538573413370296 ) ) ;
#213626=CARTESIAN_POINT ( 'NONE',  ( 6.373497979817693171, -0.2265250974912805249, 1.847160380126455559 ) ) ;
#213628=CARTESIAN_POINT ( 'NONE',  ( 3.427252967507479209, -1.452606091845513037, -1.248918174067833009 ) ) ;
#213634=CARTESIAN_POINT ( 'NONE',  ( 5.893796404173470727, -2.101076160772547219, 0.2616963346634570975 ) ) ;
#213635=CARTESIAN_POINT ( 'NONE',  ( 1.112450467520700537, -0.9725818059473788635, -1.930612204972524060 ) ) ;
#213639=CARTESIAN_POINT ( 'NONE',  ( 1.289775909805501719, -0.8246113042270180049, 1.628811597173693393 ) ) ;
#213641=CARTESIAN_POINT ( 'NONE',  ( 3.135583521505393545, -1.224952879796761041, -1.353777129306121818 ) ) ;
#213644=CARTESIAN_POINT ( 'NONE',  ( 2.822656803168353434, -1.360269829074612469, 1.424587346448534353 ) ) ;
#213646=CARTESIAN_POINT ( 'NONE',  ( 5.073749223668181152, -1.075672608635285687, 1.616763269924810231 ) ) ;
#213649=CARTESIAN_POINT ( 'NONE',  ( 5.291314375706784645, -0.05428322906628547939, -2.120082430678168706 ) ) ;
#213651=CARTESIAN_POINT ( 'NONE',  ( 2.877492880751183257, 0.2784179829431778219, -1.891769048003589138 ) ) ;
#213655=CARTESIAN_POINT ( 'NONE',  ( 4.354156267015011572, 0.8588168762691525959, -1.820826276449886150 ) ) ;
#213658=CARTESIAN_POINT ( 'NONE',  ( 4.898959864523320107, 1.516061528642864253, -1.016892643307308441 ) ) ;
#213659=CARTESIAN_POINT ( 'NONE',  ( 0.7310241076574041097, -1.948878508384953356, -0.6990896207654460071 ) ) ;
#213663=CARTESIAN_POINT ( 'NONE',  ( 5.207814216083940018, -1.861544245658670604, 0.1842191830812092979 ) ) ;
#213673=CARTESIAN_POINT ( 'NONE',  ( 1.622023338512183832, 2.040292009219225378, -0.3499636251925800079 ) ) ;
#213674=CARTESIAN_POINT ( 'NONE',  ( 2.478245404118933237, -2.111759443744887221, -0.1527427581556138059 ) ) ;
#213678=CARTESIAN_POINT ( 'NONE',  ( 6.948098034395241207, -0.8905871627266357393, 1.867117781285509537 ) ) ;
#213683=CARTESIAN_POINT ( 'NONE',  ( 2.572590238467100665, -2.194022629849821104, -0.6638836622538509813 ) ) ;
#213684=CARTESIAN_POINT ( 'NONE',  ( 6.609000000000038177, 0.002801690667396730672, 2.000160786441218530 ) ) ;
#213685=CARTESIAN_POINT ( 'NONE',  ( 2.478646075381494285, -1.315928518397539548, 1.387899491812602859 ) ) ;
#213689=CARTESIAN_POINT ( 'NONE',  ( 0.2463402104127752068, 1.031448792800106595, -1.728751203700854111 ) ) ;
#213690=CARTESIAN_POINT ( 'NONE',  ( 1.393326438508041942, -1.775833184744341375, 0.8338576968042878956 ) ) ;
#213694=CARTESIAN_POINT ( 'NONE',  ( 4.417973705048302335, 1.286473518301757712, -1.647865739169761978 ) ) ;
#213695=CARTESIAN_POINT ( 'NONE',  ( 2.289615904538056412, -0.7594197407109636311, 1.598781567136787318 ) ) ;
#213698=CARTESIAN_POINT ( 'NONE',  ( 5.156304180611417820, -1.663069175626085139, 1.577778581399520652 ) ) ;
#213699=CARTESIAN_POINT ( 'NONE',  ( 4.804519235412550771, 1.516407796731779722, 0.8538163389757484900 ) ) ;
#213702=CARTESIAN_POINT ( 'NONE',  ( 4.499182623014930549, 1.700326773844270667, 0.3381245445180857123 ) ) ;
#213703=CARTESIAN_POINT ( 'NONE',  ( 5.143125006682406131, -0.2608717942136177248, -2.155377805267975067 ) ) ;
#213705=CARTESIAN_POINT ( 'NONE',  ( 5.278529876733943915, -0.4946281652532491524, -1.954780475499573900 ) ) ;
#213706=CARTESIAN_POINT ( 'NONE',  ( 0.2812500008225146120, 0.7852924545924094835, 1.895863743164083681 ) ) ;
#213709=CARTESIAN_POINT ( 'NONE',  ( 2.362220099979424059, 0.8219310624981416291, 1.742368475122471727 ) ) ;
#213711=CARTESIAN_POINT ( 'NONE',  ( 5.308899460236623291, -0.5399372957704140497, -2.154654435841397930 ) ) ;
#213713=CARTESIAN_POINT ( 'NONE',  ( 6.883263157960401557, 3.701933627517115966, 2.360572570571787043 ) ) ;
#213716=CARTESIAN_POINT ( 'NONE',  ( 1.858359290357750160, 0.8465214129982703284, -2.053864850685551691 ) ) ;
#213721=AXIS2_PLACEMENT_3D ( 'NONE', #107742, #44829, #25343 ) ;
#213724=CARTESIAN_POINT ( 'NONE',  ( 4.756332342268011715, -2.062141065897259207, -0.05393103437261077132 ) ) ;
#213728=CARTESIAN_POINT ( 'NONE',  ( 6.380143124955812262, -1.000617425381218561, 1.580232162242324545 ) ) ;
#213729=CARTESIAN_POINT ( 'NONE',  ( 5.238767818816652877, 1.731821575490007703, -0.09270464131736801117 ) ) ;
#213730=CARTESIAN_POINT ( 'NONE',  ( 4.124340800031966126, 0.09048578169197672716, 1.738227929847275588 ) ) ;
#213732=CARTESIAN_POINT ( 'NONE',  ( 1.857357856600039048, 0.3871700131025680447, -2.259295229882941403 ) ) ;
#213734=CARTESIAN_POINT ( 'NONE',  ( 5.337476071801405375, 0.8461711052811745626, -1.912038999733718825 ) ) ;
#213735=CARTESIAN_POINT ( 'NONE',  ( 1.640310086786896049, -1.556016536173940645, 0.9838780322720328542 ) ) ;
#213737=CARTESIAN_POINT ( 'NONE',  ( 2.239018641000252607, -1.631965468365924377, 0.8183158014263000046 ) ) ;
#213738=CARTESIAN_POINT ( 'NONE',  ( 2.408827471728996361, -1.163269702728772392, -1.646838680093346996 ) ) ;
#213739=CARTESIAN_POINT ( 'NONE',  ( 1.025618320672251560, -1.392776288830662512, -1.691927514038966907 ) ) ;
#213742=CARTESIAN_POINT ( 'NONE',  ( 1.820844063133007396, -1.465591517063179028, 1.462601037713284535 ) ) ;
#213745=CARTESIAN_POINT ( 'NONE',  ( 3.932379033323248230, -1.091282289853046317, -1.817994770353311473 ) ) ;
#213747=CARTESIAN_POINT ( 'NONE',  ( 0.3109947909220554529, 1.675391530434092280, 0.9509023542121838313 ) ) ;
#213755=CARTESIAN_POINT ( 'NONE',  ( 3.568621913994294292, 0.7309530501433506577, 1.883054584751037819 ) ) ;
#213756=CARTESIAN_POINT ( 'NONE',  ( 0.5871190474453058528, -0.2578297629921856293, -2.090033075799145657 ) ) ;
#213759=CARTESIAN_POINT ( 'NONE',  ( 4.944130858096120740, -0.8794851946119870423, 1.640036094180880477 ) ) ;
#213766=CARTESIAN_POINT ( 'NONE',  ( 6.315316842782157991, -0.2547183123318246256, 2.045024454579154938 ) ) ;
#213770=CARTESIAN_POINT ( 'NONE',  ( 2.301686711942134256, -1.551025276819127496, 0.7750448480700108389 ) ) ;
#213771=CARTESIAN_POINT ( 'NONE',  ( 1.341335103225870240, 1.738211624227633978, 0.08822054626196448868 ) ) ;
#213772=CARTESIAN_POINT ( 'NONE',  ( 0.5171989335802311682, 1.588149187230869952, -1.674348222103681172 ) ) ;
#213775=CARTESIAN_POINT ( 'NONE',  ( 2.583338899891209017, 1.885494326376845775, -0.8321024974875782521 ) ) ;
#213776=CARTESIAN_POINT ( 'NONE',  ( 1.511092056569414366, 2.013677475703846476, 0.1017375232199163593 ) ) ;
#213777=CARTESIAN_POINT ( 'NONE',  ( 6.925078400183537042, 4.686282476709005884, 2.806848198465234479 ) ) ;
#213779=CARTESIAN_POINT ( 'NONE',  ( 0.6199196518563926395, -1.052708125740812628, -1.666702442819472774 ) ) ;
#213780=CARTESIAN_POINT ( 'NONE',  ( 4.447458312869024155, -1.746245811230532130, 0.7801085911468002010 ) ) ;
#213782=CARTESIAN_POINT ( 'NONE',  ( 5.848300530743933301, 2.204158087718602221, 0.1119919437090263481 ) ) ;
#213786=CARTESIAN_POINT ( 'NONE',  ( 0.3639331001695153001, 0.6315192924679478015, -1.918485960686921565 ) ) ;
#213788=CARTESIAN_POINT ( 'NONE',  ( 4.331326240856082421, 0.1090238329626690705, 2.305124713103424483 ) ) ;
#213789=CARTESIAN_POINT ( 'NONE',  ( 5.142999638377217408, -0.2383176028181442918, -1.947251298587366231 ) ) ;
#213790=CARTESIAN_POINT ( 'NONE',  ( 1.938261246079517219, -1.053878627966830184, 1.654468565904606558 ) ) ;
#213794=CARTESIAN_POINT ( 'NONE',  ( 0.4798920220053382590, -0.7558346266652364864, 1.978032726644059158 ) ) ;
#213797=CARTESIAN_POINT ( 'NONE',  ( 1.060217833243476182, -1.663605802054025418, -0.7890760572396152694 ) ) ;
#213799=CARTESIAN_POINT ( 'NONE',  ( 4.170888513267295039, 1.539375584636338390, -1.531221199927160770 ) ) ;
#213801=CARTESIAN_POINT ( 'NONE',  ( 2.285534418239891785, 0.09939759515392716793, -2.118372479656557061 ) ) ;
#213807=CARTESIAN_POINT ( 'NONE',  ( 2.389980588989379040, -0.8839831138988951675, 1.861718010716238547 ) ) ;
#213812=CARTESIAN_POINT ( 'NONE',  ( -0.02264175331115856130, 5.720791440175713838, -2.683188945093956335 ) ) ;
#213814=CARTESIAN_POINT ( 'NONE',  ( 5.303337639526568559, 1.684534858470821961, -0.9050978215178404618 ) ) ;
#213817=CARTESIAN_POINT ( 'NONE',  ( 1.634417699101225585, 1.115656568974830343, -1.968152581808318757 ) ) ;
#213819=CARTESIAN_POINT ( 'NONE',  ( 1.072181177352715453, 0.7354878280073854357, 1.655762779942154372 ) ) ;
#213820=CARTESIAN_POINT ( 'NONE',  ( 1.657307721912592458, 1.831997054396968361, -0.5600143317019135036 ) ) ;
#213822=CARTESIAN_POINT ( 'NONE',  ( 3.244645865714153032, -2.039272935636734285, -0.3565889006169955522 ) ) ;
#213824=CARTESIAN_POINT ( 'NONE',  ( 1.129686040349969556, -1.248873030102001902, -1.525460987127578605 ) ) ;
#213825=CARTESIAN_POINT ( 'NONE',  ( 5.109954983015153829, -1.917020813385891254, 0.1909056391717136592 ) ) ;
#213827=CARTESIAN_POINT ( 'NONE',  ( 0.6632354941851228425, -1.667548007495605944, 1.595465711622134242 ) ) ;
#213830=CARTESIAN_POINT ( 'NONE',  ( 4.861816908638716406, -0.5531579045409695805, 1.987044815706548562 ) ) ;
#213834=CARTESIAN_POINT ( 'NONE',  ( 6.493207903183886742, 1.834288230482609583, -1.034473908808232201 ) ) ;
#213837=CARTESIAN_POINT ( 'NONE',  ( 4.657600047955182454, 0.4785990281669267876, -2.107782517917502929 ) ) ;
#213838=CARTESIAN_POINT ( 'NONE',  ( 5.197918162715867929, 1.358090353789550342, 1.495039904793266095 ) ) ;
#213846=CARTESIAN_POINT ( 'NONE',  ( 3.925017756809038527, -1.752140073516525565, 0.9981236898717813499 ) ) ;
#213850=CARTESIAN_POINT ( 'NONE',  ( 4.768538688506021472, -1.414568798902924307, 1.634688457493836289 ) ) ;
#213854=CARTESIAN_POINT ( 'NONE',  ( 6.064077406165095496, -1.076301619396256237, 1.704949653848472302 ) ) ;
#213857=CARTESIAN_POINT ( 'NONE',  ( 0.5567383370381777663, -1.454440682700371079, -0.9269339563611042054 ) ) ;
#213862=CARTESIAN_POINT ( 'NONE',  ( 0.1745949693968693039, 0.009193469831081376581, -1.755468632744116686 ) ) ;
#213863=CARTESIAN_POINT ( 'NONE',  ( 0.8912715949961318440, -0.05164314158133917476, -2.012595864970234238 ) ) ;
#213864=CARTESIAN_POINT ( 'NONE',  ( 3.575398329460587554, 0.05639400328332971890, -2.206221599391814170 ) ) ;
#213868=CARTESIAN_POINT ( 'NONE',  ( 2.280079029133400326, 2.079044457705871096, -0.4163345062310334632 ) ) ;
#213869=CARTESIAN_POINT ( 'NONE',  ( 2.126577575561945821, 0.4445254776237593242, 1.966640697269490312 ) ) ;
#213870=CARTESIAN_POINT ( 'NONE',  ( 2.478518767674630308, -1.246658584539367176, 1.314663817856591699 ) ) ;
#213876=CARTESIAN_POINT ( 'NONE',  ( 6.609000000000045283, 0.005669918681758949128, 1.900160851458796651 ) ) ;
#213884=CARTESIAN_POINT ( 'NONE',  ( 3.573254463033649131, 0.05508235185803719847, -2.161170636208443963 ) ) ;
#213888=CARTESIAN_POINT ( 'NONE',  ( 2.391022662813433453, -2.030629854096975606, -0.6112283555373964061 ) ) ;
#213889=CARTESIAN_POINT ( 'NONE',  ( 6.581069972421211389, -0.09314021972051109155, -1.823315219958022482 ) ) ;
#213890=CARTESIAN_POINT ( 'NONE',  ( 2.846899755239293839, -1.641009487379685217, 1.092116875444639090 ) ) ;
#213891=CARTESIAN_POINT ( 'NONE',  ( 5.519756697582541172, -0.4584384640409416289, 1.856529252577573619 ) ) ;
#213894=CARTESIAN_POINT ( 'NONE',  ( 5.951603224533720038, 1.490215702738381331, 1.287855809377226102 ) ) ;
#213895=CARTESIAN_POINT ( 'NONE',  ( 1.394366005188719893, 1.587816662021741543, -1.117778254020968420 ) ) ;
#213900=CARTESIAN_POINT ( 'NONE',  ( 2.712926231669846810, -0.2040156676378352685, 2.080649193556554533 ) ) ;
#213904=CARTESIAN_POINT ( 'NONE',  ( 5.672493831469004100, 0.7790509395085333244, 1.746586765831580124 ) ) ;
#213906=CARTESIAN_POINT ( 'NONE',  ( 4.301547675229603129, 1.771612934706376707, 1.315755017190944676 ) ) ;
#213907=CARTESIAN_POINT ( 'NONE',  ( 1.554063478550568256, 0.6399170599369340406, -2.111937735441645980 ) ) ;
#213909=CARTESIAN_POINT ( 'NONE',  ( 0.3110002902955294468, 1.589785527739733695, -1.062417771062994287 ) ) ;
#213912=CARTESIAN_POINT ( 'NONE',  ( 3.842288295254093100, -1.023014542950370975, 1.799900136785845817 ) ) ;
#213914=CARTESIAN_POINT ( 'NONE',  ( 2.044033295145482043, 0.8276103948961744949, -1.997198329219296742 ) ) ;
#213915=CARTESIAN_POINT ( 'NONE',  ( 3.193114300108112147, 1.729001323093733111, 1.346577201094656395 ) ) ;
#213917=STYLED_ITEM ( 'NONE', ( #115981 ), #155333 ) ;
#213922=CARTESIAN_POINT ( 'NONE',  ( 6.557244222609861062, -1.057944526735156821, 1.374202748628235327 ) ) ;
#213924=CARTESIAN_POINT ( 'NONE',  ( 4.153231765667256603, 1.751622898902647663, -1.103220242290925190 ) ) ;
#213925=CARTESIAN_POINT ( 'NONE',  ( 5.273117041167244778, 1.866726688708058690, -0.9990383793265914525 ) ) ;
#213929=CARTESIAN_POINT ( 'NONE',  ( 3.660960169446208390, 1.555274301336776022, -1.208163239264722133 ) ) ;
#213930=CARTESIAN_POINT ( 'NONE',  ( 5.859400655334408015, 2.259312458388713196, -0.3864819027975390786 ) ) ;
#213931=CARTESIAN_POINT ( 'NONE',  ( 2.965264444195826243, 0.2674972279559268973, -1.805858685475017378 ) ) ;
#213938=CARTESIAN_POINT ( 'NONE',  ( 4.148693527746351251, 1.975194156771160170, 0.3885511358477158894 ) ) ;
#213939=CARTESIAN_POINT ( 'NONE',  ( 6.100222456320119058, -0.2858642287353658218, 2.280774976835740819 ) ) ;
#213940=CARTESIAN_POINT ( 'NONE',  ( 4.399235598239510381, -1.708881994454291675, 0.9632455365647660805 ) ) ;
#213945=CARTESIAN_POINT ( 'NONE',  ( 0.8551579053767807137, 0.4041549552570160575, -2.051131941465775821 ) ) ;
#213946=CARTESIAN_POINT ( 'NONE',  ( 6.280137008050575176, -0.9429096061123897199, 1.497559920798942512 ) ) ;
#213947=CARTESIAN_POINT ( 'NONE',  ( 2.396645607016957502, 1.759237466006560391, -1.306522788049699679 ) ) ;
#213948=CARTESIAN_POINT ( 'NONE',  ( 0.9951963871240524506, -1.740626720728695620, -0.001451476259923395245 ) ) ;
#213951=CARTESIAN_POINT ( 'NONE',  ( 0.2333690889706717397, 7.629137130509078268, -2.653349640194931247 ) ) ;
#213952=CARTESIAN_POINT ( 'NONE',  ( 1.171983892495536805, -1.097183398155553435, 1.330944738974817243 ) ) ;
#213953=CARTESIAN_POINT ( 'NONE',  ( 1.786939262935317130, 1.904797134731281538, -1.083727916527020607 ) ) ;
#213954=CARTESIAN_POINT ( 'NONE',  ( 4.090592613104036879, -2.182713160620152859, -0.3248913242878055385 ) ) ;
#213955=CARTESIAN_POINT ( 'NONE',  ( 1.147616990042895191, 1.915638116573715743, -1.021621585119661058 ) ) ;
#213957=CARTESIAN_POINT ( 'NONE',  ( 2.184896953550282461, 1.697450634274371595, -1.265404921814163641 ) ) ;
#213958=CARTESIAN_POINT ( 'NONE',  ( 6.727182134110227807, 1.996671600852136352, 2.590479658440256738 ) ) ;
#213961=CARTESIAN_POINT ( 'NONE',  ( 2.753816761298252036, 2.281055701876167685, -0.2276813034018300430 ) ) ;
#213965=CARTESIAN_POINT ( 'NONE',  ( 4.582826572872266802, -1.451171176318547529, 1.681852496032259614 ) ) ;
#213972=CARTESIAN_POINT ( 'NONE',  ( 3.252577435111691617, 1.966644794889659043, -0.4445022851852917234 ) ) ;
#213974=CARTESIAN_POINT ( 'NONE',  ( 1.622013285028017338, 2.032735996446675131, -0.3486163383695956575 ) ) ;
#213979=CARTESIAN_POINT ( 'NONE',  ( 3.767680093253112705, 1.217039798425190167, 1.822233383357040104 ) ) ;
#213980=CARTESIAN_POINT ( 'NONE',  ( 2.795546247670523954, 1.458556481301529706, -1.392545902517070111 ) ) ;
#213981=CARTESIAN_POINT ( 'NONE',  ( 1.048114208743459619, -1.451426956872736262, 1.132798186660122441 ) ) ;
#213983=CARTESIAN_POINT ( 'NONE',  ( 4.998959831394860664, 1.517082468864182632, -1.015166198912627049 ) ) ;
#213984=CARTESIAN_POINT ( 'NONE',  ( 5.801407773674092105, 1.352156682446105984, -1.496049708713815374 ) ) ;
#213986=CARTESIAN_POINT ( 'NONE',  ( 4.135799973978175892, -1.557659423114423847, -1.641163307807387950 ) ) ;
#213988=CARTESIAN_POINT ( 'NONE',  ( 0.8035136555551088966, 1.722860008830621847, 1.211028463478396988 ) ) ;
#213990=CARTESIAN_POINT ( 'NONE',  ( 5.037584538744971141, 1.933038169019934527, -0.7419538039311265321 ) ) ;
#214000=CARTESIAN_POINT ( 'NONE',  ( 0.4047333657465709278, -2.105317319661216047, -0.2534319464195868843 ) ) ;
#214001=CARTESIAN_POINT ( 'NONE',  ( 1.670502159040608170, 2.215024970770036017, -0.1695594764349258321 ) ) ;
#214005=CARTESIAN_POINT ( 'NONE',  ( 3.367582429956605061, -0.3852447139683997657, 1.923494667983568718 ) ) ;
#214012=CARTESIAN_POINT ( 'NONE',  ( 1.846092968827160119, -1.388944967848893430, -1.602481653760478020 ) ) ;
#214014=CARTESIAN_POINT ( 'NONE',  ( 6.092239754786219486, 0.9682357284593717806, -1.706234036142616928 ) ) ;
#214015=CARTESIAN_POINT ( 'NONE',  ( 3.485389320157119997, 1.955090977548096687, -0.9225387301767663528 ) ) ;
#214016=CARTESIAN_POINT ( 'NONE',  ( 3.298233973420101606, 1.449563003725433896, -1.135193286699177628 ) ) ;
#214019=CARTESIAN_POINT ( 'NONE',  ( 4.751753191611454596, 0.6700524488352653796, 1.606376638082593455 ) ) ;
#214022=CARTESIAN_POINT ( 'NONE',  ( 2.430746436576446179, 2.096607243605509208, 0.5259719050795114148 ) ) ;
#214023=CARTESIAN_POINT ( 'NONE',  ( 4.798203786142633653, -1.844427309015805649, 0.8145022673629878085 ) ) ;
#214026=CARTESIAN_POINT ( 'NONE',  ( 1.077287230265553397, -0.05381693868444264311, -2.161191418701657430 ) ) ;
#214027=CARTESIAN_POINT ( 'NONE',  ( 2.284392081957301812, -1.932574240873608629, -0.3883164474826616419 ) ) ;
#214028=CARTESIAN_POINT ( 'NONE',  ( 3.192849282005063127, 1.532776493767808113, 1.192484549457759613 ) ) ;
#214037=CARTESIAN_POINT ( 'NONE',  ( 1.431021430919703574, 2.126993092707793132, 0.5877070120439558121 ) ) ;
#214039=CARTESIAN_POINT ( 'NONE',  ( 5.313317156408340125, -1.655227327604656740, -1.052681782574490743 ) ) ;
#214040=CARTESIAN_POINT ( 'NONE',  ( 3.468056730359007744, -1.039945921192251266, 1.844253657775334121 ) ) ;
#214042=CARTESIAN_POINT ( 'NONE',  ( 0.1747926744264677590, 6.948552888299643904, -2.450368216405907962 ) ) ;
#214043=CARTESIAN_POINT ( 'NONE',  ( 4.312339554033173705, 1.684294245562456993, 0.7440144950455057637 ) ) ;
#214047=CARTESIAN_POINT ( 'NONE',  ( 5.203433420164765622, 1.869144303625443371, -1.001675624404389620 ) ) ;
#214050=CARTESIAN_POINT ( 'NONE',  ( 6.274695623702050362, -1.955332461540583600, -0.6509123137334557052 ) ) ;
#214052=CARTESIAN_POINT ( 'NONE',  ( 1.328301213181204421, -1.184495032981685014, 1.435421900094263403 ) ) ;
#214053=CARTESIAN_POINT ( 'NONE',  ( 3.614658571667620279, -0.1319153736358945894, 1.836568937333193485 ) ) ;
#214058=CARTESIAN_POINT ( 'NONE',  ( 3.809358915828209735, 1.892446193107431451, 1.135094405146239049 ) ) ;
#214059=CARTESIAN_POINT ( 'NONE',  ( 4.833442251172010984, -2.071103420340114187, 0.9108926349224757413 ) ) ;
#214061=CARTESIAN_POINT ( 'NONE',  ( 4.394648900434598104, -1.758782010937329110, -0.4337233627825891613 ) ) ;
#214062=CARTESIAN_POINT ( 'NONE',  ( 5.876186789644119557, -1.907177742178717716, -0.1804351137127818694 ) ) ;
#214064=CARTESIAN_POINT ( 'NONE',  ( 5.700035372616791385, -1.870836310086241294, 0.001406584917262864625 ) ) ;
#214067=CARTESIAN_POINT ( 'NONE',  ( 5.564867526603252124, 1.409050971242819417, -1.215897700512589052 ) ) ;
#214069=CARTESIAN_POINT ( 'NONE',  ( 6.034039731144309471, 0.8686908000094315518, -1.541921269980907949 ) ) ;
#214070=CARTESIAN_POINT ( 'NONE',  ( 1.007046422456716384, -0.04465021774549028655, 2.016188868504041665 ) ) ;
#214072=CARTESIAN_POINT ( 'NONE',  ( 2.912826151168836031, 1.525034000978764626, -1.452760968584436707 ) ) ;
#214077=CARTESIAN_POINT ( 'NONE',  ( 1.687766420876281037, 1.931502627210328837, -0.5905180581586618738 ) ) ;
#214080=CARTESIAN_POINT ( 'NONE',  ( 2.811983876933337179, -2.138515761559431461, 0.3140893029918228607 ) ) ;
#214081=CARTESIAN_POINT ( 'NONE',  ( 6.890000000000039648, 4.701345932300413644, 2.282685536056531461 ) ) ;
#214088=CARTESIAN_POINT ( 'NONE',  ( 1.505704256594592838, -2.174480876681058827, 0.2726767719730335826 ) ) ;
#214090=CARTESIAN_POINT ( 'NONE',  ( 1.745381597357411385, -1.910777759476259163, 1.211296049258607788 ) ) ;
#214098=CARTESIAN_POINT ( 'NONE',  ( 2.952157954411178675, 0.5926004979403748374, 1.667723606733088060 ) ) ;
#214099=CARTESIAN_POINT ( 'NONE',  ( 0.09494852110062798611, -0.4603312545960658864, -2.062269868324863253 ) ) ;
#214103=CARTESIAN_POINT ( 'NONE',  ( 4.974232547167513729, -2.001514726140873890, -0.2440111082952014510 ) ) ;
#214104=CARTESIAN_POINT ( 'NONE',  ( 4.869312882171149326, -1.534379415642408651, -0.9627496050425389251 ) ) ;
#214107=CARTESIAN_POINT ( 'NONE',  ( 2.834663617355744680, 0.2272019944037397543, 1.856728029318695627 ) ) ;
#214108=CARTESIAN_POINT ( 'NONE',  ( 3.713788242813487184, 0.5077267127921447631, -2.006887321594638784 ) ) ;
#214110=CARTESIAN_POINT ( 'NONE',  ( 2.531394148431935776, -0.1834752923718513118, 1.903540536635806912 ) ) ;
#214116=CARTESIAN_POINT ( 'NONE',  ( 0.8438408207818194340, -1.215224102361469161, -1.476598726422105656 ) ) ;
#214117=CARTESIAN_POINT ( 'NONE',  ( 3.332423539472821439, -1.170687260143790320, 1.574129132985650825 ) ) ;
#214121=CARTESIAN_POINT ( 'NONE',  ( 6.468046296993485988, 1.011472520757991767, 1.691939633080985272 ) ) ;
#214123=CARTESIAN_POINT ( 'NONE',  ( 1.810793108869549917, -0.5408357282137785660, -1.939109541719201912 ) ) ;
#214125=CARTESIAN_POINT ( 'NONE',  ( 2.478245404118933237, -2.111759443744887221, -0.1527427581556138059 ) ) ;
#214127=CARTESIAN_POINT ( 'NONE',  ( 3.631357695093720750, 0.05367941694835526995, -2.069842578854002468 ) ) ;
#214130=CARTESIAN_POINT ( 'NONE',  ( 6.404249610866886044, 1.549990571320001731, -1.403138301853884773 ) ) ;
#214132=CARTESIAN_POINT ( 'NONE',  ( 4.190329584092522097, -1.805708503706305423, -0.2678305112727846771 ) ) ;
#214137=CARTESIAN_POINT ( 'NONE',  ( 5.579209114504255496, -0.04897750150410771358, -2.206396493298476980 ) ) ;
#214141=CARTESIAN_POINT ( 'NONE',  ( 3.475170734053119048, -1.687717282722025924, -0.8990902037325496643 ) ) ;
#214148=CARTESIAN_POINT ( 'NONE',  ( 0.1515692981730529243, 0.7036590017722235135, 1.701685288394996665 ) ) ;
#214151=CARTESIAN_POINT ( 'NONE',  ( 4.516781199771729760, 1.709404882366181377, 0.7599583452636837766 ) ) ;
#214156=CARTESIAN_POINT ( 'NONE',  ( 1.428490153906246007, -1.253617920133040853, 1.518890472526812419 ) ) ;
#214157=CARTESIAN_POINT ( 'NONE',  ( 2.407827563459669307, -1.163288551851604513, -1.646826728940099738 ) ) ;
#214162=CARTESIAN_POINT ( 'NONE',  ( 2.730644157659181559, 0.2691629481662433099, 2.174792594416566249 ) ) ;
#214173=CARTESIAN_POINT ( 'NONE',  ( 4.862772069579198941, 0.1752732939881325724, -1.832877676746891726 ) ) ;
#214174=CARTESIAN_POINT ( 'NONE',  ( 1.858066033337543832, 0.7684160352657551929, -1.860855044080988785 ) ) ;
#214175=CARTESIAN_POINT ( 'NONE',  ( 3.673487740190139572, -0.9280425899400122081, -2.102842487114229275 ) ) ;
#214177=CARTESIAN_POINT ( 'NONE',  ( 1.393147051786493673, -1.685373162331062602, 0.7893452609444310264 ) ) ;
#214179=CARTESIAN_POINT ( 'NONE',  ( 6.082274476537278041, 0.9889857280602430967, 1.636697341158253272 ) ) ;
#214182=CARTESIAN_POINT ( 'NONE',  ( 3.597287555019304861, -0.6049611382589085151, 2.001324503170316849 ) ) ;
#214183=CARTESIAN_POINT ( 'NONE',  ( 2.096370420935515178, -0.4963513585865795275, -1.803540123670114736 ) ) ;
#214186=CARTESIAN_POINT ( 'NONE',  ( 6.022987620897008121, -1.731432113864934674, 0.6267441317700100933 ) ) ;
#214190=CARTESIAN_POINT ( 'NONE',  ( 4.811038506879902421, 1.503007855926122405, 0.8461308117306536314 ) ) ;
#214192=CARTESIAN_POINT ( 'NONE',  ( 0.3868564640647629282, -0.5820622975930835885, -1.633661194748408541 ) ) ;
#214195=CARTESIAN_POINT ( 'NONE',  ( 4.399414683135016269, -1.891862197681973834, 1.064912953861403944 ) ) ;
#214196=CARTESIAN_POINT ( 'NONE',  ( 3.035583632137848653, -1.226507576337819483, -1.352503160878690380 ) ) ;
#214197=CARTESIAN_POINT ( 'NONE',  ( 0.6023038706522118035, 1.956103482322549825, 0.1501044349687257751 ) ) ;
#214198=CARTESIAN_POINT ( 'NONE',  ( 5.559793223943660934, 1.263291928365728012, 1.699014672817029892 ) ) ;
#214199=CARTESIAN_POINT ( 'NONE',  ( 6.040627043210095692, -1.938779113641406759, 1.222911669862235096 ) ) ;
#214203=CARTESIAN_POINT ( 'NONE',  ( 1.928540351845555056, -1.002238520345886785, -1.868699319572619366 ) ) ;
#214209=CARTESIAN_POINT ( 'NONE',  ( 6.719587830005472995, 0.3798626643731088937, -2.137457590422507714 ) ) ;
#214210=CARTESIAN_POINT ( 'NONE',  ( 6.883263157960367806, 6.035304072343574688, 2.648703854151325032 ) ) ;
#214212=CARTESIAN_POINT ( 'NONE',  ( 1.858359290357750160, 0.8465214129982703284, -2.053864850685551691 ) ) ;
#214214=CARTESIAN_POINT ( 'NONE',  ( 0.001177798100650446610, -2.252613640939280515, 0.4573402144308849615 ) ) ;
#214216=CARTESIAN_POINT ( 'NONE',  ( 4.170800697546906299, 1.462118435030785646, -1.455038044888419702 ) ) ;
#214222=CARTESIAN_POINT ( 'NONE',  ( 4.546344060013487898, -1.475942220874026489, 1.100600019281534836 ) ) ;
#214225=CARTESIAN_POINT ( 'NONE',  ( 1.623609269016149437, -0.9540678014761799774, -1.436642212298586907 ) ) ;
#214226=CARTESIAN_POINT ( 'NONE',  ( -0.08279552664090458758, -1.841734517378278424, 0.8216794407479923734 ) ) ;
#214227=CARTESIAN_POINT ( 'NONE',  ( 2.198211363809216667, 2.055062875077425577, 1.030007645627160517 ) ) ;
#214229=CARTESIAN_POINT ( 'NONE',  ( 1.546537457781042235, 2.259796958156198077, 0.1114739384607699862 ) ) ;
#214230=CARTESIAN_POINT ( 'NONE',  ( 3.844438321715905715, 2.095922912919225389, 0.2063985846082766473 ) ) ;
#214232=CARTESIAN_POINT ( 'NONE',  ( 2.635733503900684838, 0.8381847041133619891, -1.558674532600109686 ) ) ;
#214238=CARTESIAN_POINT ( 'NONE',  ( 4.711300293261502681, 1.846222065370630050, -1.235088439349934841 ) ) ;
#214239=CARTESIAN_POINT ( 'NONE',  ( 3.328257738700185264, 2.138080787187321086, 0.4799892483983853042 ) ) ;
#214242=CARTESIAN_POINT ( 'NONE',  ( 6.551439628692993900, -1.894445571042557619, 0.9528467149547341641 ) ) ;
#214244=CARTESIAN_POINT ( 'NONE',  ( 6.610000000000006537, 2.052567036419289614, 2.306714106643445561 ) ) ;
#214246=CARTESIAN_POINT ( 'NONE',  ( 5.449516625918088053, -1.916229881892789866, 0.9086369058012438993 ) ) ;
#214250=CARTESIAN_POINT ( 'NONE',  ( 6.297764839082774735, -0.7330946318361495351, 2.033732118066629457 ) ) ;
#214252=CARTESIAN_POINT ( 'NONE',  ( 6.614805131849967879, -0.1256686391097518729, 1.812046779126045726 ) ) ;
#214255=CARTESIAN_POINT ( 'NONE',  ( 1.399541807966601104, -0.6259456572170263300, -1.624154832779246993 ) ) ;
#214257=CARTESIAN_POINT ( 'NONE',  ( 0.2386218892466463737, -1.902018210125755004, -0.4804332253167050149 ) ) ;
#214260=CARTESIAN_POINT ( 'NONE',  ( 4.838837662799537753, 0.3661284547709364734, 2.130314178654398205 ) ) ;
#214263=CARTESIAN_POINT ( 'NONE',  ( 4.663041391408608405, -1.929494027986548454, -0.9748474430888448561 ) ) ;
#214265=ORIENTED_EDGE ( 'NONE', *, *, #157150, .T. ) ;
#214267=CARTESIAN_POINT ( 'NONE',  ( 5.993430986175369846, 1.491191765471042041, 1.289477300995988118 ) ) ;
#214268=CARTESIAN_POINT ( 'NONE',  ( 5.483642203991152542, 1.602890455293109584, 0.6615300989148454880 ) ) ;
#214270=CARTESIAN_POINT ( 'NONE',  ( 2.402122600552298870, -0.8417629408748151798, -2.023652355447076001 ) ) ;
#214271=CARTESIAN_POINT ( 'NONE',  ( 3.663348518144835086, -2.033753252616496532, -1.090341736564947484 ) ) ;
#214272=CARTESIAN_POINT ( 'NONE',  ( 4.534483719690214798, 2.020231433191475467, 0.4058933888440272031 ) ) ;
#214273=CARTESIAN_POINT ( 'NONE',  ( 0.6209105903263291149, -1.844282116485985501, 0.6082893332694323529 ) ) ;
#214277=CARTESIAN_POINT ( 'NONE',  ( 3.603867943843573673, 1.538443694073919898, 1.459757404076333698 ) ) ;
#214279=CARTESIAN_POINT ( 'NONE',  ( 1.090470458312575053, -0.4872005951904456733, 1.956561897242928172 ) ) ;
#214281=CARTESIAN_POINT ( 'NONE',  ( 4.770673279661371780, -1.444480529215144804, 1.668407551275403300 ) ) ;
#214289=CARTESIAN_POINT ( 'NONE',  ( 4.821196345351608237, -0.1031141679418267343, 2.058443437638860285 ) ) ;
#214292=CARTESIAN_POINT ( 'NONE',  ( 3.774085898144818874, 2.004173781823472833, -0.2492677732841129534 ) ) ;
#214296=CARTESIAN_POINT ( 'NONE',  ( 2.641540400197890825, -1.526127808488053628, -1.385168266076434174 ) ) ;
#214301=CARTESIAN_POINT ( 'NONE',  ( -0.1411974294642228400, 2.034035580701949897, -2.316051970441324936 ) ) ;
#214302=CARTESIAN_POINT ( 'NONE',  ( 1.534833434108737515, -1.332603482217321389, -1.270662175854364362 ) ) ;
#214303=CARTESIAN_POINT ( 'NONE',  ( 6.709632191794143274, -0.4886956906769434061, 2.160084693451309601 ) ) ;
#214305=CARTESIAN_POINT ( 'NONE',  ( 1.897963814661303150, -0.7301937759345776824, 2.034636513274298064 ) ) ;
#214307=CARTESIAN_POINT ( 'NONE',  ( 1.569546381206438967, 1.394087592100446971, 1.457234012747665508 ) ) ;
#214310=CARTESIAN_POINT ( 'NONE',  ( 0.2154177506630133854, -1.835460468737951878, 0.3602540799089171131 ) ) ;
#214311=CARTESIAN_POINT ( 'NONE',  ( 4.539890248181537302, 0.8439850759212139675, -1.781816264247655157 ) ) ;
#214312=CARTESIAN_POINT ( 'NONE',  ( 4.153529959351897283, 1.954779968807466295, -0.4946301968136583849 ) ) ;
#214316=CARTESIAN_POINT ( 'NONE',  ( 5.690091061058023314, -0.9480630415420692181, 1.880679904143019776 ) ) ;
#214317=CARTESIAN_POINT ( 'NONE',  ( 5.002425025097493538, 2.064580399062130311, 0.1557331365308264881 ) ) ;
#214320=CARTESIAN_POINT ( 'NONE',  ( 6.539320575229249144, 2.442570667128646900, 2.385998263081292148 ) ) ;
#214321=CARTESIAN_POINT ( 'NONE',  ( 5.677991919488574624, 1.989193807575660555, -0.3493085226990484959 ) ) ;
#214323=CARTESIAN_POINT ( 'NONE',  ( 3.563348594130168578, -2.034784092110089926, -1.088618498840478566 ) ) ;
#214324=CARTESIAN_POINT ( 'NONE',  ( 1.375913251025398409, -2.013209319166248346, 0.4479213407221314669 ) ) ;
#214326=ADVANCED_FACE ( 'NONE', ( #106165 ), #173156, .F. ) ;
#214332=CARTESIAN_POINT ( 'NONE',  ( 4.650930581473819991, -0.4712930505080668575, -2.119270573956061554 ) ) ;
#214336=CARTESIAN_POINT ( 'NONE',  ( 3.298233973420101606, 1.449563003725433896, -1.135193286699177628 ) ) ;
#214338=CARTESIAN_POINT ( 'NONE',  ( 4.898067072109578035, -0.7382639882421681010, -2.063579870930781546 ) ) ;
#214340=CARTESIAN_POINT ( 'NONE',  ( 6.332949636392265269, 0.2142684956521986317, 2.252356394309730003 ) ) ;
#214346=CARTESIAN_POINT ( 'NONE',  ( 6.204346024843479412, -0.6390883176130756071, -1.650510209504873593 ) ) ;
#214347=CARTESIAN_POINT ( 'NONE',  ( 4.670568766136569572, 0.7725349690445941775, 1.859148924064259356 ) ) ;
#214349=CARTESIAN_POINT ( 'NONE',  ( 3.487430266828908998, 1.904693919176775552, -0.8987260315082377105 ) ) ;
#214350=CARTESIAN_POINT ( 'NONE',  ( 1.616650230726389248, 0.1894562617417178962, 1.906227014244334717 ) ) ;
#214352=CARTESIAN_POINT ( 'NONE',  ( 3.297268302959563524, -1.738273807845453600, 0.9259864402798111405 ) ) ;
#214353=CARTESIAN_POINT ( 'NONE',  ( 4.781513128076603003, 0.1936695275622651868, -2.010448953515688419 ) ) ;
#214354=CARTESIAN_POINT ( 'NONE',  ( 0.5494049127674709432, 0.5909524230637287490, -1.774924738581270089 ) ) ;
#214355=CARTESIAN_POINT ( 'NONE',  ( 1.451531895509536874, 1.483362660712842063, 1.284035263222626844 ) ) ;
#214356=CARTESIAN_POINT ( 'NONE',  ( 0.1934256698341470238, 1.783621342183003389, -0.6902995980747894667 ) ) ;
#214361=CARTESIAN_POINT ( 'NONE',  ( 6.332864056472936376, 0.1854757364097951722, 1.861418627818342664 ) ) ;
#214364=CARTESIAN_POINT ( 'NONE',  ( 6.262565978045822490, -0.7396069823457154246, -1.933831554736538338 ) ) ;
#214366=CARTESIAN_POINT ( 'NONE',  ( 0.4497787391488928810, 1.533077660697563793, 1.391591089521776681 ) ) ;
#214371=CARTESIAN_POINT ( 'NONE',  ( 5.039744756118590630, -2.013340025477545758, 0.6656774797743277849 ) ) ;
#214376=CARTESIAN_POINT ( 'NONE',  ( 5.881297811770386907, -0.04968318840743202180, 1.961410508136133712 ) ) ;
#214378=CARTESIAN_POINT ( 'NONE',  ( 2.899767358622063806, 0.2439914025648345919, 2.001204936777578602 ) ) ;
#214380=CARTESIAN_POINT ( 'NONE',  ( 3.661272352971048694, 1.801931492627879106, -0.6507149165355142761 ) ) ;
#214382=CARTESIAN_POINT ( 'NONE',  ( 2.068174269828721101, -1.345378145056834063, 1.729934933326432445 ) ) ;
#214384=CARTESIAN_POINT ( 'NONE',  ( 3.251090012001829788, -1.527204365403836306, -1.079795099579644591 ) ) ;
#214386=CARTESIAN_POINT ( 'NONE',  ( 4.676043659170272093, 1.990676093108449951, -0.2997180003130732739 ) ) ;
#214389=CARTESIAN_POINT ( 'NONE',  ( 5.484029812627264633, -2.117403151077674739, 0.0008096548943584136460 ) ) ;
#214391=FACE_OUTER_BOUND ( 'NONE', #160669, .T. ) ;
#214392=CARTESIAN_POINT ( 'NONE',  ( 1.839510613029649466, 0.7972044211956804682, -1.932997742640076400 ) ) ;
#214394=CARTESIAN_POINT ( 'NONE',  ( 0.5863794435163689478, -0.2038549220112067795, -1.712615276990290480 ) ) ;
#214395=EDGE_LOOP ( 'NONE', ( #48515, #121534, #118541, #212337 ) ) ;
#214403=CARTESIAN_POINT ( 'NONE',  ( 1.646807439477548707, 0.1776336960073976179, 1.802747333403993402 ) ) ;
#214408=CARTESIAN_POINT ( 'NONE',  ( 6.639320575229259447, 2.978120323461688201, 2.350396677589302374 ) ) ;
ENDSEC;
END-ISO-10303-21;
